ISO-10303-21;
HEADER;
/* Generated by software containing ST-Developer
 * from STEP Tools, Inc. (www.steptools.com) 
 */

FILE_DESCRIPTION(
/* description */ ('STEP AP214'),
/* implementation_level */ '2;1');

FILE_NAME(
/* name */ 'Vertical Precision Auger Screw.step',
/* time_stamp */ '2026-11-14T22:16:48-08:00',
/* author */ (''),
/* organization */ (''),
/* preprocessor_version */ 'ST-DEVELOPER v20.2',
/* originating_system */ 'Autodesk Translation Framework v15.17.0.0',
/* authorisation */ '');

FILE_SCHEMA (('AUTOMOTIVE_DESIGN { 1 0 10303 214 3 1 1 }'));
ENDSEC;

DATA;
#10=MECHANICAL_DESIGN_GEOMETRIC_PRESENTATION_REPRESENTATION('',(#5473,#5474),#276462);
#336=ELLIPSE('',#98932,245.0752161313,242.710009632518);
#337=ELLIPSE('',#98935,18.0481778016316,18.048088900566);
#2501=(
BOUNDED_SURFACE()
B_SPLINE_SURFACE(1,2,((#145815,#145816,#145817,#145818,#145819,#145820,
#145821,#145822,#145823,#145824,#145825,#145826,#145827,#145828,#145829,
#145830,#145831,#145832,#145833,#145834,#145835,#145836,#145837,#145838,
#145839,#145840,#145841,#145842,#145843,#145844,#145845,#145846,#145847,
#145848,#145849,#145850,#145851,#145852,#145853,#145854,#145855,#145856,
#145857,#145858,#145859,#145860,#145861,#145862,#145863,#145864,#145865,
#145866,#145867,#145868,#145869,#145870,#145871,#145872,#145873,#145874,
#145875,#145876,#145877,#145878,#145879,#145880,#145881,#145882,#145883,
#145884,#145885,#145886,#145887,#145888,#145889,#145890,#145891,#145892,
#145893,#145894,#145895,#145896,#145897,#145898,#145899,#145900,#145901,
#145902,#145903,#145904,#145905,#145906,#145907,#145908,#145909,#145910,
#145911,#145912,#145913,#145914,#145915,#145916,#145917,#145918,#145919,
#145920,#145921,#145922,#145923,#145924,#145925,#145926,#145927,#145928,
#145929,#145930,#145931,#145932,#145933,#145934,#145935,#145936,#145937,
#145938,#145939,#145940,#145941,#145942,#145943,#145944,#145945,#145946,
#145947,#145948,#145949,#145950,#145951,#145952,#145953,#145954,#145955,
#145956,#145957,#145958,#145959,#145960,#145961,#145962,#145963,#145964,
#145965,#145966,#145967,#145968,#145969,#145970,#145971,#145972,#145973,
#145974,#145975,#145976,#145977,#145978,#145979,#145980,#145981,#145982,
#145983,#145984,#145985,#145986,#145987,#145988,#145989,#145990,#145991,
#145992,#145993,#145994,#145995,#145996,#145997,#145998,#145999,#146000,
#146001,#146002,#146003,#146004,#146005,#146006,#146007,#146008,#146009,
#146010,#146011,#146012,#146013,#146014,#146015,#146016,#146017,#146018,
#146019,#146020,#146021,#146022,#146023,#146024,#146025,#146026,#146027,
#146028,#146029,#146030,#146031,#146032,#146033,#146034,#146035,#146036,
#146037,#146038,#146039,#146040,#146041,#146042,#146043,#146044,#146045,
#146046,#146047,#146048,#146049,#146050,#146051,#146052,#146053,#146054,
#146055,#146056,#146057,#146058,#146059,#146060,#146061,#146062,#146063,
#146064,#146065,#146066,#146067,#146068,#146069,#146070,#146071,#146072,
#146073,#146074,#146075,#146076,#146077,#146078,#146079,#146080,#146081,
#146082,#146083,#146084,#146085,#146086,#146087,#146088,#146089,#146090,
#146091,#146092,#146093,#146094,#146095,#146096,#146097,#146098,#146099,
#146100,#146101,#146102,#146103,#146104,#146105,#146106,#146107,#146108,
#146109,#146110,#146111,#146112,#146113,#146114,#146115,#146116,#146117,
#146118,#146119,#146120,#146121,#146122,#146123,#146124,#146125,#146126,
#146127,#146128,#146129,#146130,#146131,#146132,#146133,#146134,#146135,
#146136,#146137,#146138,#146139,#146140,#146141,#146142,#146143,#146144,
#146145,#146146,#146147,#146148,#146149,#146150,#146151,#146152,#146153,
#146154,#146155,#146156,#146157,#146158,#146159,#146160,#146161,#146162,
#146163,#146164,#146165,#146166,#146167,#146168,#146169,#146170,#146171,
#146172,#146173,#146174,#146175,#146176,#146177,#146178,#146179,#146180,
#146181,#146182,#146183,#146184,#146185,#146186,#146187,#146188,#146189,
#146190,#146191,#146192,#146193,#146194,#146195,#146196,#146197,#146198,
#146199,#146200,#146201,#146202,#146203,#146204,#146205,#146206,#146207,
#146208,#146209,#146210,#146211,#146212,#146213,#146214,#146215,#146216,
#146217,#146218,#146219,#146220,#146221,#146222,#146223,#146224,#146225,
#146226,#146227,#146228,#146229,#146230,#146231,#146232,#146233,#146234,
#146235,#146236,#146237,#146238,#146239,#146240,#146241,#146242,#146243,
#146244,#146245,#146246,#146247,#146248,#146249,#146250,#146251,#146252,
#146253,#146254,#146255,#146256,#146257,#146258,#146259,#146260,#146261,
#146262,#146263,#146264,#146265,#146266,#146267,#146268,#146269,#146270,
#146271,#146272,#146273,#146274,#146275,#146276,#146277,#146278,#146279,
#146280,#146281,#146282,#146283,#146284,#146285,#146286,#146287,#146288,
#146289,#146290,#146291,#146292,#146293,#146294,#146295,#146296,#146297,
#146298,#146299,#146300,#146301,#146302,#146303,#146304,#146305,#146306,
#146307,#146308,#146309,#146310,#146311,#146312,#146313,#146314,#146315,
#146316,#146317,#146318,#146319,#146320,#146321,#146322,#146323,#146324,
#146325,#146326,#146327,#146328,#146329,#146330,#146331,#146332,#146333,
#146334,#146335,#146336,#146337,#146338,#146339,#146340,#146341,#146342,
#146343,#146344,#146345,#146346,#146347,#146348,#146349,#146350,#146351,
#146352,#146353,#146354,#146355,#146356,#146357,#146358,#146359,#146360,
#146361,#146362,#146363,#146364,#146365,#146366,#146367,#146368,#146369,
#146370,#146371,#146372,#146373,#146374,#146375,#146376,#146377,#146378,
#146379,#146380,#146381,#146382,#146383,#146384,#146385,#146386,#146387,
#146388,#146389,#146390,#146391,#146392,#146393,#146394,#146395,#146396,
#146397,#146398,#146399,#146400,#146401,#146402,#146403,#146404,#146405,
#146406,#146407,#146408,#146409,#146410,#146411,#146412,#146413,#146414,
#146415,#146416,#146417,#146418,#146419,#146420,#146421,#146422,#146423,
#146424,#146425,#146426,#146427,#146428,#146429,#146430,#146431,#146432,
#146433,#146434,#146435,#146436,#146437,#146438,#146439,#146440,#146441,
#146442,#146443,#146444,#146445,#146446,#146447,#146448,#146449,#146450,
#146451,#146452,#146453,#146454,#146455,#146456,#146457,#146458,#146459,
#146460,#146461,#146462,#146463,#146464,#146465,#146466,#146467,#146468,
#146469,#146470,#146471,#146472,#146473,#146474,#146475,#146476,#146477,
#146478,#146479,#146480,#146481,#146482,#146483,#146484,#146485,#146486,
#146487,#146488,#146489,#146490,#146491,#146492,#146493,#146494,#146495,
#146496,#146497,#146498,#146499,#146500,#146501,#146502,#146503,#146504,
#146505,#146506,#146507,#146508,#146509,#146510,#146511,#146512,#146513,
#146514,#146515,#146516,#146517,#146518,#146519,#146520,#146521,#146522,
#146523,#146524,#146525,#146526,#146527,#146528,#146529,#146530,#146531,
#146532,#146533,#146534,#146535,#146536,#146537,#146538,#146539,#146540,
#146541,#146542,#146543,#146544,#146545,#146546,#146547,#146548,#146549,
#146550,#146551,#146552,#146553,#146554,#146555,#146556,#146557,#146558,
#146559,#146560,#146561,#146562,#146563,#146564,#146565,#146566,#146567,
#146568,#146569,#146570,#146571,#146572,#146573,#146574,#146575,#146576,
#146577,#146578,#146579,#146580,#146581,#146582,#146583,#146584,#146585,
#146586,#146587,#146588,#146589,#146590,#146591,#146592,#146593,#146594,
#146595,#146596,#146597,#146598,#146599,#146600,#146601,#146602,#146603,
#146604,#146605,#146606,#146607,#146608,#146609,#146610,#146611,#146612,
#146613,#146614,#146615,#146616,#146617,#146618,#146619,#146620,#146621,
#146622,#146623,#146624,#146625,#146626,#146627,#146628,#146629,#146630,
#146631,#146632,#146633,#146634,#146635,#146636,#146637,#146638,#146639,
#146640,#146641,#146642,#146643,#146644,#146645,#146646,#146647,#146648,
#146649,#146650,#146651,#146652,#146653,#146654,#146655,#146656,#146657,
#146658,#146659,#146660,#146661,#146662,#146663,#146664,#146665,#146666,
#146667,#146668,#146669,#146670,#146671,#146672,#146673,#146674,#146675,
#146676,#146677,#146678,#146679,#146680,#146681,#146682,#146683,#146684,
#146685,#146686,#146687,#146688,#146689,#146690,#146691,#146692,#146693,
#146694,#146695,#146696,#146697,#146698,#146699,#146700,#146701,#146702,
#146703,#146704,#146705,#146706,#146707,#146708,#146709,#146710,#146711,
#146712,#146713,#146714,#146715,#146716,#146717,#146718,#146719,#146720,
#146721,#146722,#146723,#146724,#146725,#146726,#146727,#146728,#146729,
#146730,#146731,#146732,#146733,#146734,#146735,#146736,#146737,#146738,
#146739,#146740,#146741,#146742,#146743,#146744,#146745,#146746,#146747,
#146748,#146749,#146750,#146751,#146752,#146753,#146754,#146755,#146756,
#146757,#146758,#146759,#146760,#146761,#146762,#146763,#146764,#146765,
#146766,#146767,#146768,#146769,#146770,#146771,#146772,#146773,#146774,
#146775,#146776,#146777,#146778,#146779,#146780,#146781,#146782,#146783,
#146784,#146785,#146786,#146787,#146788,#146789,#146790,#146791,#146792,
#146793,#146794,#146795,#146796,#146797,#146798,#146799,#146800,#146801,
#146802,#146803,#146804,#146805,#146806,#146807,#146808,#146809,#146810,
#146811,#146812,#146813,#146814,#146815,#146816,#146817,#146818,#146819,
#146820,#146821,#146822,#146823,#146824,#146825,#146826,#146827,#146828,
#146829,#146830,#146831,#146832,#146833,#146834,#146835,#146836,#146837,
#146838,#146839,#146840,#146841,#146842,#146843,#146844,#146845,#146846,
#146847,#146848,#146849,#146850,#146851,#146852,#146853,#146854,#146855,
#146856,#146857,#146858,#146859,#146860,#146861,#146862,#146863,#146864,
#146865,#146866,#146867,#146868,#146869,#146870,#146871,#146872,#146873,
#146874,#146875,#146876,#146877,#146878,#146879,#146880,#146881,#146882,
#146883,#146884,#146885,#146886,#146887,#146888,#146889,#146890,#146891,
#146892,#146893,#146894,#146895,#146896,#146897,#146898,#146899,#146900,
#146901,#146902,#146903,#146904,#146905,#146906,#146907,#146908,#146909,
#146910,#146911,#146912,#146913,#146914,#146915,#146916,#146917,#146918,
#146919,#146920,#146921,#146922,#146923,#146924,#146925,#146926,#146927,
#146928,#146929,#146930,#146931,#146932,#146933,#146934,#146935,#146936,
#146937,#146938,#146939,#146940,#146941,#146942,#146943,#146944,#146945,
#146946,#146947,#146948,#146949,#146950,#146951,#146952,#146953,#146954,
#146955,#146956,#146957,#146958,#146959,#146960,#146961,#146962,#146963,
#146964,#146965,#146966,#146967,#146968,#146969,#146970,#146971,#146972,
#146973,#146974,#146975,#146976,#146977,#146978,#146979,#146980,#146981,
#146982,#146983,#146984,#146985,#146986,#146987,#146988,#146989,#146990,
#146991,#146992,#146993,#146994,#146995,#146996,#146997,#146998,#146999,
#147000,#147001,#147002,#147003,#147004,#147005,#147006,#147007,#147008,
#147009,#147010,#147011,#147012,#147013,#147014,#147015,#147016,#147017,
#147018,#147019,#147020,#147021,#147022,#147023,#147024,#147025,#147026,
#147027,#147028,#147029,#147030,#147031,#147032,#147033,#147034,#147035,
#147036,#147037,#147038,#147039,#147040,#147041,#147042,#147043,#147044,
#147045,#147046,#147047,#147048,#147049,#147050,#147051,#147052,#147053,
#147054,#147055,#147056,#147057,#147058,#147059,#147060,#147061,#147062,
#147063,#147064,#147065,#147066,#147067,#147068,#147069,#147070,#147071,
#147072,#147073,#147074,#147075,#147076,#147077,#147078,#147079,#147080,
#147081,#147082,#147083,#147084,#147085,#147086,#147087,#147088,#147089,
#147090,#147091,#147092,#147093,#147094,#147095,#147096,#147097,#147098,
#147099,#147100,#147101,#147102,#147103,#147104,#147105,#147106,#147107,
#147108,#147109,#147110,#147111,#147112,#147113,#147114,#147115,#147116,
#147117,#147118,#147119,#147120,#147121,#147122,#147123,#147124,#147125,
#147126,#147127,#147128,#147129,#147130,#147131,#147132,#147133,#147134,
#147135,#147136,#147137,#147138,#147139,#147140,#147141,#147142,#147143,
#147144,#147145,#147146,#147147,#147148,#147149,#147150,#147151,#147152,
#147153,#147154,#147155,#147156,#147157,#147158,#147159,#147160,#147161,
#147162,#147163,#147164,#147165,#147166,#147167,#147168,#147169,#147170,
#147171,#147172,#147173,#147174,#147175,#147176,#147177,#147178,#147179,
#147180,#147181,#147182,#147183,#147184,#147185,#147186,#147187,#147188,
#147189,#147190,#147191,#147192,#147193,#147194,#147195,#147196,#147197,
#147198,#147199,#147200,#147201,#147202,#147203,#147204,#147205,#147206,
#147207,#147208,#147209,#147210,#147211,#147212,#147213,#147214,#147215,
#147216,#147217,#147218,#147219,#147220,#147221,#147222,#147223,#147224,
#147225,#147226,#147227,#147228,#147229,#147230,#147231,#147232,#147233,
#147234,#147235,#147236,#147237,#147238,#147239,#147240,#147241,#147242,
#147243,#147244,#147245,#147246,#147247,#147248,#147249,#147250,#147251,
#147252,#147253,#147254,#147255,#147256,#147257,#147258,#147259,#147260,
#147261,#147262,#147263,#147264,#147265,#147266,#147267,#147268,#147269,
#147270,#147271,#147272,#147273,#147274,#147275,#147276,#147277,#147278,
#147279,#147280,#147281,#147282,#147283,#147284,#147285,#147286,#147287,
#147288,#147289,#147290,#147291,#147292,#147293,#147294,#147295,#147296,
#147297,#147298,#147299,#147300,#147301,#147302,#147303,#147304,#147305,
#147306,#147307,#147308,#147309,#147310,#147311,#147312,#147313,#147314,
#147315,#147316,#147317,#147318,#147319,#147320,#147321,#147322,#147323,
#147324,#147325,#147326,#147327,#147328,#147329,#147330,#147331,#147332,
#147333,#147334,#147335,#147336,#147337,#147338,#147339,#147340,#147341,
#147342,#147343,#147344,#147345,#147346,#147347,#147348,#147349,#147350,
#147351,#147352,#147353,#147354,#147355,#147356,#147357,#147358,#147359,
#147360,#147361,#147362,#147363,#147364,#147365,#147366,#147367,#147368,
#147369,#147370,#147371,#147372,#147373,#147374,#147375,#147376,#147377,
#147378,#147379,#147380,#147381,#147382,#147383,#147384,#147385,#147386,
#147387,#147388,#147389,#147390,#147391,#147392,#147393,#147394,#147395,
#147396,#147397,#147398,#147399,#147400,#147401,#147402,#147403,#147404,
#147405,#147406,#147407,#147408,#147409,#147410,#147411,#147412,#147413,
#147414,#147415,#147416,#147417,#147418,#147419,#147420,#147421,#147422,
#147423,#147424,#147425,#147426,#147427,#147428,#147429,#147430,#147431,
#147432,#147433,#147434,#147435,#147436,#147437,#147438,#147439,#147440,
#147441,#147442,#147443,#147444,#147445,#147446,#147447,#147448,#147449,
#147450,#147451,#147452,#147453,#147454,#147455,#147456,#147457,#147458,
#147459,#147460,#147461,#147462,#147463,#147464,#147465,#147466,#147467,
#147468,#147469,#147470,#147471,#147472,#147473,#147474,#147475,#147476,
#147477,#147478,#147479,#147480,#147481,#147482,#147483,#147484,#147485,
#147486,#147487,#147488,#147489,#147490,#147491,#147492,#147493,#147494,
#147495,#147496,#147497,#147498,#147499,#147500,#147501,#147502,#147503,
#147504,#147505,#147506,#147507,#147508,#147509,#147510,#147511,#147512,
#147513,#147514,#147515,#147516,#147517,#147518,#147519,#147520,#147521,
#147522,#147523,#147524,#147525,#147526,#147527,#147528,#147529,#147530,
#147531,#147532,#147533,#147534,#147535,#147536,#147537,#147538,#147539,
#147540,#147541,#147542,#147543,#147544,#147545,#147546,#147547,#147548,
#147549,#147550,#147551,#147552,#147553,#147554,#147555,#147556,#147557,
#147558,#147559,#147560,#147561,#147562,#147563,#147564,#147565,#147566,
#147567,#147568,#147569,#147570,#147571,#147572,#147573,#147574,#147575,
#147576,#147577,#147578,#147579,#147580,#147581,#147582,#147583,#147584,
#147585,#147586,#147587,#147588,#147589,#147590,#147591,#147592,#147593,
#147594,#147595,#147596,#147597,#147598,#147599,#147600,#147601,#147602,
#147603,#147604,#147605,#147606,#147607,#147608,#147609,#147610,#147611,
#147612,#147613,#147614,#147615,#147616,#147617,#147618,#147619,#147620,
#147621,#147622,#147623,#147624,#147625,#147626,#147627,#147628,#147629,
#147630,#147631,#147632,#147633,#147634,#147635,#147636,#147637,#147638,
#147639,#147640,#147641,#147642,#147643,#147644,#147645,#147646,#147647,
#147648,#147649,#147650,#147651,#147652,#147653,#147654,#147655,#147656,
#147657,#147658,#147659,#147660,#147661,#147662,#147663,#147664,#147665,
#147666,#147667,#147668,#147669,#147670,#147671,#147672,#147673,#147674,
#147675,#147676,#147677,#147678,#147679,#147680,#147681,#147682,#147683,
#147684,#147685,#147686,#147687,#147688,#147689,#147690,#147691,#147692,
#147693,#147694,#147695,#147696,#147697,#147698,#147699,#147700,#147701,
#147702,#147703,#147704,#147705,#147706,#147707,#147708,#147709,#147710,
#147711,#147712,#147713,#147714,#147715,#147716,#147717,#147718,#147719,
#147720,#147721,#147722,#147723,#147724,#147725,#147726,#147727,#147728,
#147729,#147730,#147731,#147732,#147733,#147734,#147735,#147736,#147737,
#147738,#147739,#147740,#147741,#147742,#147743,#147744,#147745,#147746,
#147747,#147748,#147749,#147750,#147751,#147752,#147753,#147754,#147755,
#147756,#147757,#147758,#147759,#147760,#147761,#147762,#147763,#147764,
#147765,#147766,#147767,#147768,#147769,#147770,#147771,#147772,#147773,
#147774,#147775,#147776,#147777,#147778,#147779,#147780,#147781,#147782,
#147783,#147784,#147785,#147786,#147787,#147788,#147789,#147790,#147791,
#147792,#147793,#147794,#147795,#147796,#147797,#147798,#147799,#147800,
#147801,#147802,#147803,#147804,#147805,#147806,#147807,#147808,#147809,
#147810,#147811,#147812,#147813,#147814,#147815,#147816,#147817,#147818,
#147819,#147820,#147821,#147822,#147823,#147824,#147825,#147826,#147827),
(#147828,#147829,#147830,#147831,#147832,#147833,#147834,#147835,#147836,
#147837,#147838,#147839,#147840,#147841,#147842,#147843,#147844,#147845,
#147846,#147847,#147848,#147849,#147850,#147851,#147852,#147853,#147854,
#147855,#147856,#147857,#147858,#147859,#147860,#147861,#147862,#147863,
#147864,#147865,#147866,#147867,#147868,#147869,#147870,#147871,#147872,
#147873,#147874,#147875,#147876,#147877,#147878,#147879,#147880,#147881,
#147882,#147883,#147884,#147885,#147886,#147887,#147888,#147889,#147890,
#147891,#147892,#147893,#147894,#147895,#147896,#147897,#147898,#147899,
#147900,#147901,#147902,#147903,#147904,#147905,#147906,#147907,#147908,
#147909,#147910,#147911,#147912,#147913,#147914,#147915,#147916,#147917,
#147918,#147919,#147920,#147921,#147922,#147923,#147924,#147925,#147926,
#147927,#147928,#147929,#147930,#147931,#147932,#147933,#147934,#147935,
#147936,#147937,#147938,#147939,#147940,#147941,#147942,#147943,#147944,
#147945,#147946,#147947,#147948,#147949,#147950,#147951,#147952,#147953,
#147954,#147955,#147956,#147957,#147958,#147959,#147960,#147961,#147962,
#147963,#147964,#147965,#147966,#147967,#147968,#147969,#147970,#147971,
#147972,#147973,#147974,#147975,#147976,#147977,#147978,#147979,#147980,
#147981,#147982,#147983,#147984,#147985,#147986,#147987,#147988,#147989,
#147990,#147991,#147992,#147993,#147994,#147995,#147996,#147997,#147998,
#147999,#148000,#148001,#148002,#148003,#148004,#148005,#148006,#148007,
#148008,#148009,#148010,#148011,#148012,#148013,#148014,#148015,#148016,
#148017,#148018,#148019,#148020,#148021,#148022,#148023,#148024,#148025,
#148026,#148027,#148028,#148029,#148030,#148031,#148032,#148033,#148034,
#148035,#148036,#148037,#148038,#148039,#148040,#148041,#148042,#148043,
#148044,#148045,#148046,#148047,#148048,#148049,#148050,#148051,#148052,
#148053,#148054,#148055,#148056,#148057,#148058,#148059,#148060,#148061,
#148062,#148063,#148064,#148065,#148066,#148067,#148068,#148069,#148070,
#148071,#148072,#148073,#148074,#148075,#148076,#148077,#148078,#148079,
#148080,#148081,#148082,#148083,#148084,#148085,#148086,#148087,#148088,
#148089,#148090,#148091,#148092,#148093,#148094,#148095,#148096,#148097,
#148098,#148099,#148100,#148101,#148102,#148103,#148104,#148105,#148106,
#148107,#148108,#148109,#148110,#148111,#148112,#148113,#148114,#148115,
#148116,#148117,#148118,#148119,#148120,#148121,#148122,#148123,#148124,
#148125,#148126,#148127,#148128,#148129,#148130,#148131,#148132,#148133,
#148134,#148135,#148136,#148137,#148138,#148139,#148140,#148141,#148142,
#148143,#148144,#148145,#148146,#148147,#148148,#148149,#148150,#148151,
#148152,#148153,#148154,#148155,#148156,#148157,#148158,#148159,#148160,
#148161,#148162,#148163,#148164,#148165,#148166,#148167,#148168,#148169,
#148170,#148171,#148172,#148173,#148174,#148175,#148176,#148177,#148178,
#148179,#148180,#148181,#148182,#148183,#148184,#148185,#148186,#148187,
#148188,#148189,#148190,#148191,#148192,#148193,#148194,#148195,#148196,
#148197,#148198,#148199,#148200,#148201,#148202,#148203,#148204,#148205,
#148206,#148207,#148208,#148209,#148210,#148211,#148212,#148213,#148214,
#148215,#148216,#148217,#148218,#148219,#148220,#148221,#148222,#148223,
#148224,#148225,#148226,#148227,#148228,#148229,#148230,#148231,#148232,
#148233,#148234,#148235,#148236,#148237,#148238,#148239,#148240,#148241,
#148242,#148243,#148244,#148245,#148246,#148247,#148248,#148249,#148250,
#148251,#148252,#148253,#148254,#148255,#148256,#148257,#148258,#148259,
#148260,#148261,#148262,#148263,#148264,#148265,#148266,#148267,#148268,
#148269,#148270,#148271,#148272,#148273,#148274,#148275,#148276,#148277,
#148278,#148279,#148280,#148281,#148282,#148283,#148284,#148285,#148286,
#148287,#148288,#148289,#148290,#148291,#148292,#148293,#148294,#148295,
#148296,#148297,#148298,#148299,#148300,#148301,#148302,#148303,#148304,
#148305,#148306,#148307,#148308,#148309,#148310,#148311,#148312,#148313,
#148314,#148315,#148316,#148317,#148318,#148319,#148320,#148321,#148322,
#148323,#148324,#148325,#148326,#148327,#148328,#148329,#148330,#148331,
#148332,#148333,#148334,#148335,#148336,#148337,#148338,#148339,#148340,
#148341,#148342,#148343,#148344,#148345,#148346,#148347,#148348,#148349,
#148350,#148351,#148352,#148353,#148354,#148355,#148356,#148357,#148358,
#148359,#148360,#148361,#148362,#148363,#148364,#148365,#148366,#148367,
#148368,#148369,#148370,#148371,#148372,#148373,#148374,#148375,#148376,
#148377,#148378,#148379,#148380,#148381,#148382,#148383,#148384,#148385,
#148386,#148387,#148388,#148389,#148390,#148391,#148392,#148393,#148394,
#148395,#148396,#148397,#148398,#148399,#148400,#148401,#148402,#148403,
#148404,#148405,#148406,#148407,#148408,#148409,#148410,#148411,#148412,
#148413,#148414,#148415,#148416,#148417,#148418,#148419,#148420,#148421,
#148422,#148423,#148424,#148425,#148426,#148427,#148428,#148429,#148430,
#148431,#148432,#148433,#148434,#148435,#148436,#148437,#148438,#148439,
#148440,#148441,#148442,#148443,#148444,#148445,#148446,#148447,#148448,
#148449,#148450,#148451,#148452,#148453,#148454,#148455,#148456,#148457,
#148458,#148459,#148460,#148461,#148462,#148463,#148464,#148465,#148466,
#148467,#148468,#148469,#148470,#148471,#148472,#148473,#148474,#148475,
#148476,#148477,#148478,#148479,#148480,#148481,#148482,#148483,#148484,
#148485,#148486,#148487,#148488,#148489,#148490,#148491,#148492,#148493,
#148494,#148495,#148496,#148497,#148498,#148499,#148500,#148501,#148502,
#148503,#148504,#148505,#148506,#148507,#148508,#148509,#148510,#148511,
#148512,#148513,#148514,#148515,#148516,#148517,#148518,#148519,#148520,
#148521,#148522,#148523,#148524,#148525,#148526,#148527,#148528,#148529,
#148530,#148531,#148532,#148533,#148534,#148535,#148536,#148537,#148538,
#148539,#148540,#148541,#148542,#148543,#148544,#148545,#148546,#148547,
#148548,#148549,#148550,#148551,#148552,#148553,#148554,#148555,#148556,
#148557,#148558,#148559,#148560,#148561,#148562,#148563,#148564,#148565,
#148566,#148567,#148568,#148569,#148570,#148571,#148572,#148573,#148574,
#148575,#148576,#148577,#148578,#148579,#148580,#148581,#148582,#148583,
#148584,#148585,#148586,#148587,#148588,#148589,#148590,#148591,#148592,
#148593,#148594,#148595,#148596,#148597,#148598,#148599,#148600,#148601,
#148602,#148603,#148604,#148605,#148606,#148607,#148608,#148609,#148610,
#148611,#148612,#148613,#148614,#148615,#148616,#148617,#148618,#148619,
#148620,#148621,#148622,#148623,#148624,#148625,#148626,#148627,#148628,
#148629,#148630,#148631,#148632,#148633,#148634,#148635,#148636,#148637,
#148638,#148639,#148640,#148641,#148642,#148643,#148644,#148645,#148646,
#148647,#148648,#148649,#148650,#148651,#148652,#148653,#148654,#148655,
#148656,#148657,#148658,#148659,#148660,#148661,#148662,#148663,#148664,
#148665,#148666,#148667,#148668,#148669,#148670,#148671,#148672,#148673,
#148674,#148675,#148676,#148677,#148678,#148679,#148680,#148681,#148682,
#148683,#148684,#148685,#148686,#148687,#148688,#148689,#148690,#148691,
#148692,#148693,#148694,#148695,#148696,#148697,#148698,#148699,#148700,
#148701,#148702,#148703,#148704,#148705,#148706,#148707,#148708,#148709,
#148710,#148711,#148712,#148713,#148714,#148715,#148716,#148717,#148718,
#148719,#148720,#148721,#148722,#148723,#148724,#148725,#148726,#148727,
#148728,#148729,#148730,#148731,#148732,#148733,#148734,#148735,#148736,
#148737,#148738,#148739,#148740,#148741,#148742,#148743,#148744,#148745,
#148746,#148747,#148748,#148749,#148750,#148751,#148752,#148753,#148754,
#148755,#148756,#148757,#148758,#148759,#148760,#148761,#148762,#148763,
#148764,#148765,#148766,#148767,#148768,#148769,#148770,#148771,#148772,
#148773,#148774,#148775,#148776,#148777,#148778,#148779,#148780,#148781,
#148782,#148783,#148784,#148785,#148786,#148787,#148788,#148789,#148790,
#148791,#148792,#148793,#148794,#148795,#148796,#148797,#148798,#148799,
#148800,#148801,#148802,#148803,#148804,#148805,#148806,#148807,#148808,
#148809,#148810,#148811,#148812,#148813,#148814,#148815,#148816,#148817,
#148818,#148819,#148820,#148821,#148822,#148823,#148824,#148825,#148826,
#148827,#148828,#148829,#148830,#148831,#148832,#148833,#148834,#148835,
#148836,#148837,#148838,#148839,#148840,#148841,#148842,#148843,#148844,
#148845,#148846,#148847,#148848,#148849,#148850,#148851,#148852,#148853,
#148854,#148855,#148856,#148857,#148858,#148859,#148860,#148861,#148862,
#148863,#148864,#148865,#148866,#148867,#148868,#148869,#148870,#148871,
#148872,#148873,#148874,#148875,#148876,#148877,#148878,#148879,#148880,
#148881,#148882,#148883,#148884,#148885,#148886,#148887,#148888,#148889,
#148890,#148891,#148892,#148893,#148894,#148895,#148896,#148897,#148898,
#148899,#148900,#148901,#148902,#148903,#148904,#148905,#148906,#148907,
#148908,#148909,#148910,#148911,#148912,#148913,#148914,#148915,#148916,
#148917,#148918,#148919,#148920,#148921,#148922,#148923,#148924,#148925,
#148926,#148927,#148928,#148929,#148930,#148931,#148932,#148933,#148934,
#148935,#148936,#148937,#148938,#148939,#148940,#148941,#148942,#148943,
#148944,#148945,#148946,#148947,#148948,#148949,#148950,#148951,#148952,
#148953,#148954,#148955,#148956,#148957,#148958,#148959,#148960,#148961,
#148962,#148963,#148964,#148965,#148966,#148967,#148968,#148969,#148970,
#148971,#148972,#148973,#148974,#148975,#148976,#148977,#148978,#148979,
#148980,#148981,#148982,#148983,#148984,#148985,#148986,#148987,#148988,
#148989,#148990,#148991,#148992,#148993,#148994,#148995,#148996,#148997,
#148998,#148999,#149000,#149001,#149002,#149003,#149004,#149005,#149006,
#149007,#149008,#149009,#149010,#149011,#149012,#149013,#149014,#149015,
#149016,#149017,#149018,#149019,#149020,#149021,#149022,#149023,#149024,
#149025,#149026,#149027,#149028,#149029,#149030,#149031,#149032,#149033,
#149034,#149035,#149036,#149037,#149038,#149039,#149040,#149041,#149042,
#149043,#149044,#149045,#149046,#149047,#149048,#149049,#149050,#149051,
#149052,#149053,#149054,#149055,#149056,#149057,#149058,#149059,#149060,
#149061,#149062,#149063,#149064,#149065,#149066,#149067,#149068,#149069,
#149070,#149071,#149072,#149073,#149074,#149075,#149076,#149077,#149078,
#149079,#149080,#149081,#149082,#149083,#149084,#149085,#149086,#149087,
#149088,#149089,#149090,#149091,#149092,#149093,#149094,#149095,#149096,
#149097,#149098,#149099,#149100,#149101,#149102,#149103,#149104,#149105,
#149106,#149107,#149108,#149109,#149110,#149111,#149112,#149113,#149114,
#149115,#149116,#149117,#149118,#149119,#149120,#149121,#149122,#149123,
#149124,#149125,#149126,#149127,#149128,#149129,#149130,#149131,#149132,
#149133,#149134,#149135,#149136,#149137,#149138,#149139,#149140,#149141,
#149142,#149143,#149144,#149145,#149146,#149147,#149148,#149149,#149150,
#149151,#149152,#149153,#149154,#149155,#149156,#149157,#149158,#149159,
#149160,#149161,#149162,#149163,#149164,#149165,#149166,#149167,#149168,
#149169,#149170,#149171,#149172,#149173,#149174,#149175,#149176,#149177,
#149178,#149179,#149180,#149181,#149182,#149183,#149184,#149185,#149186,
#149187,#149188,#149189,#149190,#149191,#149192,#149193,#149194,#149195,
#149196,#149197,#149198,#149199,#149200,#149201,#149202,#149203,#149204,
#149205,#149206,#149207,#149208,#149209,#149210,#149211,#149212,#149213,
#149214,#149215,#149216,#149217,#149218,#149219,#149220,#149221,#149222,
#149223,#149224,#149225,#149226,#149227,#149228,#149229,#149230,#149231,
#149232,#149233,#149234,#149235,#149236,#149237,#149238,#149239,#149240,
#149241,#149242,#149243,#149244,#149245,#149246,#149247,#149248,#149249,
#149250,#149251,#149252,#149253,#149254,#149255,#149256,#149257,#149258,
#149259,#149260,#149261,#149262,#149263,#149264,#149265,#149266,#149267,
#149268,#149269,#149270,#149271,#149272,#149273,#149274,#149275,#149276,
#149277,#149278,#149279,#149280,#149281,#149282,#149283,#149284,#149285,
#149286,#149287,#149288,#149289,#149290,#149291,#149292,#149293,#149294,
#149295,#149296,#149297,#149298,#149299,#149300,#149301,#149302,#149303,
#149304,#149305,#149306,#149307,#149308,#149309,#149310,#149311,#149312,
#149313,#149314,#149315,#149316,#149317,#149318,#149319,#149320,#149321,
#149322,#149323,#149324,#149325,#149326,#149327,#149328,#149329,#149330,
#149331,#149332,#149333,#149334,#149335,#149336,#149337,#149338,#149339,
#149340,#149341,#149342,#149343,#149344,#149345,#149346,#149347,#149348,
#149349,#149350,#149351,#149352,#149353,#149354,#149355,#149356,#149357,
#149358,#149359,#149360,#149361,#149362,#149363,#149364,#149365,#149366,
#149367,#149368,#149369,#149370,#149371,#149372,#149373,#149374,#149375,
#149376,#149377,#149378,#149379,#149380,#149381,#149382,#149383,#149384,
#149385,#149386,#149387,#149388,#149389,#149390,#149391,#149392,#149393,
#149394,#149395,#149396,#149397,#149398,#149399,#149400,#149401,#149402,
#149403,#149404,#149405,#149406,#149407,#149408,#149409,#149410,#149411,
#149412,#149413,#149414,#149415,#149416,#149417,#149418,#149419,#149420,
#149421,#149422,#149423,#149424,#149425,#149426,#149427,#149428,#149429,
#149430,#149431,#149432,#149433,#149434,#149435,#149436,#149437,#149438,
#149439,#149440,#149441,#149442,#149443,#149444,#149445,#149446,#149447,
#149448,#149449,#149450,#149451,#149452,#149453,#149454,#149455,#149456,
#149457,#149458,#149459,#149460,#149461,#149462,#149463,#149464,#149465,
#149466,#149467,#149468,#149469,#149470,#149471,#149472,#149473,#149474,
#149475,#149476,#149477,#149478,#149479,#149480,#149481,#149482,#149483,
#149484,#149485,#149486,#149487,#149488,#149489,#149490,#149491,#149492,
#149493,#149494,#149495,#149496,#149497,#149498,#149499,#149500,#149501,
#149502,#149503,#149504,#149505,#149506,#149507,#149508,#149509,#149510,
#149511,#149512,#149513,#149514,#149515,#149516,#149517,#149518,#149519,
#149520,#149521,#149522,#149523,#149524,#149525,#149526,#149527,#149528,
#149529,#149530,#149531,#149532,#149533,#149534,#149535,#149536,#149537,
#149538,#149539,#149540,#149541,#149542,#149543,#149544,#149545,#149546,
#149547,#149548,#149549,#149550,#149551,#149552,#149553,#149554,#149555,
#149556,#149557,#149558,#149559,#149560,#149561,#149562,#149563,#149564,
#149565,#149566,#149567,#149568,#149569,#149570,#149571,#149572,#149573,
#149574,#149575,#149576,#149577,#149578,#149579,#149580,#149581,#149582,
#149583,#149584,#149585,#149586,#149587,#149588,#149589,#149590,#149591,
#149592,#149593,#149594,#149595,#149596,#149597,#149598,#149599,#149600,
#149601,#149602,#149603,#149604,#149605,#149606,#149607,#149608,#149609,
#149610,#149611,#149612,#149613,#149614,#149615,#149616,#149617,#149618,
#149619,#149620,#149621,#149622,#149623,#149624,#149625,#149626,#149627,
#149628,#149629,#149630,#149631,#149632,#149633,#149634,#149635,#149636,
#149637,#149638,#149639,#149640,#149641,#149642,#149643,#149644,#149645,
#149646,#149647,#149648,#149649,#149650,#149651,#149652,#149653,#149654,
#149655,#149656,#149657,#149658,#149659,#149660,#149661,#149662,#149663,
#149664,#149665,#149666,#149667,#149668,#149669,#149670,#149671,#149672,
#149673,#149674,#149675,#149676,#149677,#149678,#149679,#149680,#149681,
#149682,#149683,#149684,#149685,#149686,#149687,#149688,#149689,#149690,
#149691,#149692,#149693,#149694,#149695,#149696,#149697,#149698,#149699,
#149700,#149701,#149702,#149703,#149704,#149705,#149706,#149707,#149708,
#149709,#149710,#149711,#149712,#149713,#149714,#149715,#149716,#149717,
#149718,#149719,#149720,#149721,#149722,#149723,#149724,#149725,#149726,
#149727,#149728,#149729,#149730,#149731,#149732,#149733,#149734,#149735,
#149736,#149737,#149738,#149739,#149740,#149741,#149742,#149743,#149744,
#149745,#149746,#149747,#149748,#149749,#149750,#149751,#149752,#149753,
#149754,#149755,#149756,#149757,#149758,#149759,#149760,#149761,#149762,
#149763,#149764,#149765,#149766,#149767,#149768,#149769,#149770,#149771,
#149772,#149773,#149774,#149775,#149776,#149777,#149778,#149779,#149780,
#149781,#149782,#149783,#149784,#149785,#149786,#149787,#149788,#149789,
#149790,#149791,#149792,#149793,#149794,#149795,#149796,#149797,#149798,
#149799,#149800,#149801,#149802,#149803,#149804,#149805,#149806,#149807,
#149808,#149809,#149810,#149811,#149812,#149813,#149814,#149815,#149816,
#149817,#149818,#149819,#149820,#149821,#149822,#149823,#149824,#149825,
#149826,#149827,#149828,#149829,#149830,#149831,#149832,#149833,#149834,
#149835,#149836,#149837,#149838,#149839,#149840)),.UNSPECIFIED.,.F.,.F.,
 .F.)
B_SPLINE_SURFACE_WITH_KNOTS((2,2),(3,2,2,2,2,2,2,2,2,2,2,2,2,2,2,2,2,2,
2,2,2,2,2,2,2,2,2,2,2,2,2,2,2,2,2,2,2,2,2,2,2,2,2,2,2,2,2,2,2,2,2,2,2,2,
2,2,2,2,2,2,2,2,2,2,2,2,2,2,2,2,2,2,2,2,2,2,2,2,2,2,2,2,2,2,2,2,2,2,2,2,
2,2,2,2,2,2,2,2,2,2,2,2,2,2,2,2,2,2,2,2,2,2,2,2,2,2,2,2,2,2,2,2,2,2,2,2,
2,2,2,2,2,2,2,2,2,2,2,2,2,2,2,2,2,2,2,2,2,2,2,2,2,2,2,2,2,2,2,2,2,2,2,2,
2,2,2,2,2,2,2,2,2,2,2,2,2,2,2,2,2,2,2,2,2,2,2,2,2,2,2,2,2,2,2,2,2,2,2,2,
2,2,2,2,2,2,2,2,2,2,2,2,2,2,2,2,2,2,2,2,2,2,2,2,2,2,2,2,2,2,2,2,2,2,2,2,
2,2,2,2,2,2,2,2,2,2,2,2,2,2,2,2,2,2,2,2,2,2,2,2,2,2,2,2,2,2,2,2,2,2,2,2,
2,2,2,2,2,2,2,2,2,2,2,2,2,2,2,2,2,2,2,2,2,2,2,2,2,2,2,2,2,2,2,2,2,2,2,2,
2,2,2,2,2,2,2,2,2,2,2,2,2,2,2,2,2,2,2,2,2,2,2,2,2,2,2,2,2,2,2,2,2,2,2,2,
2,2,2,2,2,2,2,2,2,2,2,2,2,2,2,2,2,2,2,2,2,2,2,2,2,2,2,2,2,2,2,2,2,2,2,2,
2,2,2,2,2,2,2,2,2,2,2,2,2,2,2,2,2,2,2,2,2,2,2,2,2,2,2,2,2,2,2,2,2,2,2,2,
2,2,2,2,2,2,2,2,2,2,2,2,2,2,2,2,2,2,2,2,2,2,2,2,2,2,2,2,2,2,2,2,2,2,2,2,
2,2,2,2,2,2,2,2,2,2,2,2,2,2,2,2,2,2,2,2,2,2,2,2,2,2,2,2,2,2,2,2,2,2,2,2,
2,2,2,2,2,2,2,2,2,2,2,2,2,2,2,2,2,2,2,2,2,2,2,2,2,2,2,2,2,2,2,2,2,2,2,2,
2,2,2,2,2,2,2,2,2,2,2,2,2,2,2,2,2,2,2,2,2,2,2,2,2,2,2,2,2,2,2,2,2,2,2,2,
2,2,2,2,2,2,2,2,2,2,2,2,2,2,2,2,2,2,2,2,2,2,2,2,2,2,2,2,2,2,2,2,2,2,2,2,
2,2,2,2,2,2,2,2,2,2,2,2,2,2,2,2,2,2,2,2,2,2,2,2,2,2,2,2,2,2,2,2,2,2,2,2,
2,2,2,2,2,2,2,2,2,2,2,2,2,2,2,2,2,2,2,2,2,2,2,2,2,2,2,2,2,2,2,2,2,2,2,2,
2,2,2,2,2,2,2,2,2,2,2,2,2,2,2,2,2,2,2,2,2,2,2,2,2,2,2,2,2,2,2,2,2,2,2,2,
2,2,2,2,2,2,2,2,2,2,2,2,2,2,2,2,2,2,2,2,2,2,2,2,2,2,2,2,2,2,2,2,2,2,2,2,
2,2,2,2,2,2,2,2,2,2,2,2,2,2,2,2,2,2,2,2,2,2,2,2,2,2,2,2,2,2,2,2,2,2,2,2,
2,2,2,2,2,2,2,2,2,2,2,2,2,2,2,2,2,2,2,2,2,2,2,2,2,2,2,2,2,2,2,2,2,2,2,2,
2,2,2,2,2,2,2,2,2,2,2,2,2,2,2,2,2,2,2,2,2,2,2,2,2,2,2,2,2,2,2,2,2,2,2,2,
2,2,2,2,2,2,2,2,2,2,2,2,2,2,2,2,2,2,2,2,2,2,2,2,2,2,2,2,2,2,2,2,2,2,2,2,
2,2,2,2,2,2,2,2,2,2,2,2,2,2,2,2,2,2,2,2,2,2,2,2,2,2,2,2,2,2,2,2,2,2,2,2,
2,2,2,2,2,2,2,2,2,2,2,2,2,2,2,2,2,2,2,2,2,2,2,2,2,2,2,2,2,2,2,2,2,2,2,2,
2,2,2,2,2,2,2,2,2,2,2,2,2,2,2,2,2,2,2,2,2,2,2,2,2,2,2,2,2,2,2,2,2,2,2,2,
2,2,2,2,2,2,2,2,2,2,2,2,2,2,2,2,3),(0.,1.),(0.,0.000980392156862745,0.00196078431372549,
0.00294117647058824,0.00392156862745098,0.00490196078431373,0.00588235294117647,
0.00686274509803922,0.00784313725490196,0.00882352941176471,0.00980392156862745,
0.0107843137254902,0.0117647058823529,0.0127450980392157,0.0137254901960784,
0.0147058823529412,0.0156862745098039,0.0166666666666667,0.0176470588235294,
0.0186274509803922,0.0196078431372549,0.0205882352941176,0.0215686274509804,
0.0225490196078431,0.0235294117647059,0.0245098039215686,0.0254901960784314,
0.0264705882352941,0.0274509803921569,0.0284313725490196,0.0294117647058824,
0.0303921568627451,0.0313725490196078,0.0323529411764706,0.0333333333333333,
0.0343137254901961,0.0352941176470588,0.0362745098039216,0.0372549019607843,
0.0382352941176471,0.0392156862745098,0.0401960784313726,0.0411764705882353,
0.042156862745098,0.0431372549019608,0.0441176470588235,0.0450980392156863,
0.046078431372549,0.0470588235294118,0.0480392156862745,0.0490196078431373,
0.05,0.0509803921568627,0.0519607843137255,0.0529411764705882,0.053921568627451,
0.0549019607843137,0.0558823529411765,0.0568627450980392,0.057843137254902,
0.0588235294117647,0.0598039215686275,0.0607843137254902,0.0617647058823529,
0.0627450980392157,0.0637254901960784,0.0647058823529412,0.0656862745098039,
0.0666666666666667,0.0676470588235294,0.0686274509803922,0.0696078431372549,
0.0705882352941176,0.0715686274509804,0.0725490196078431,0.0735294117647059,
0.0745098039215686,0.0754901960784314,0.0764705882352941,0.0774509803921569,
0.0784313725490196,0.0794117647058823,0.0803921568627451,0.0813725490196078,
0.0823529411764706,0.0833333333333333,0.0843137254901961,0.0852941176470588,
0.0862745098039216,0.0872549019607843,0.0882352941176471,0.0892156862745098,
0.0901960784313725,0.0911764705882353,0.092156862745098,0.0931372549019608,
0.0941176470588235,0.0950980392156863,0.096078431372549,0.0970588235294118,
0.0980392156862745,0.0990196078431373,0.1,0.100980392156863,0.101960784313725,
0.102941176470588,0.103921568627451,0.104901960784314,0.105882352941176,
0.106862745098039,0.107843137254902,0.108823529411765,0.109803921568627,
0.11078431372549,0.111764705882353,0.112745098039216,0.113725490196078,
0.114705882352941,0.115686274509804,0.116666666666667,0.117647058823529,
0.118627450980392,0.119607843137255,0.120588235294118,0.12156862745098,
0.122549019607843,0.123529411764706,0.124509803921569,0.125490196078431,
0.126470588235294,0.127450980392157,0.12843137254902,0.129411764705882,
0.130392156862745,0.131372549019608,0.132352941176471,0.133333333333333,
0.134313725490196,0.135294117647059,0.136274509803922,0.137254901960784,
0.138235294117647,0.13921568627451,0.140196078431373,0.141176470588235,
0.142156862745098,0.143137254901961,0.144117647058824,0.145098039215686,
0.146078431372549,0.147058823529412,0.148039215686275,0.149019607843137,
0.15,0.150980392156863,0.151960784313725,0.152941176470588,0.153921568627451,
0.154901960784314,0.155882352941176,0.156862745098039,0.157843137254902,
0.158823529411765,0.159803921568627,0.16078431372549,0.161764705882353,
0.162745098039216,0.163725490196078,0.164705882352941,0.165686274509804,
0.166666666666667,0.167647058823529,0.168627450980392,0.169607843137255,
0.170588235294118,0.17156862745098,0.172549019607843,0.173529411764706,
0.174509803921569,0.175490196078431,0.176470588235294,0.177450980392157,
0.17843137254902,0.179411764705882,0.180392156862745,0.181372549019608,
0.182352941176471,0.183333333333333,0.184313725490196,0.185294117647059,
0.186274509803922,0.187254901960784,0.188235294117647,0.18921568627451,
0.190196078431373,0.191176470588235,0.192156862745098,0.193137254901961,
0.194117647058824,0.195098039215686,0.196078431372549,0.197058823529412,
0.198039215686275,0.199019607843137,0.2,0.200980392156863,0.201960784313725,
0.202941176470588,0.203921568627451,0.204901960784314,0.205882352941176,
0.206862745098039,0.207843137254902,0.208823529411765,0.209803921568627,
0.21078431372549,0.211764705882353,0.212745098039216,0.213725490196078,
0.214705882352941,0.215686274509804,0.216666666666667,0.217647058823529,
0.218627450980392,0.219607843137255,0.220588235294118,0.22156862745098,
0.222549019607843,0.223529411764706,0.224509803921569,0.225490196078431,
0.226470588235294,0.227450980392157,0.22843137254902,0.229411764705882,
0.230392156862745,0.231372549019608,0.232352941176471,0.233333333333333,
0.234313725490196,0.235294117647059,0.236274509803922,0.237254901960784,
0.238235294117647,0.23921568627451,0.240196078431373,0.241176470588235,
0.242156862745098,0.243137254901961,0.244117647058824,0.245098039215686,
0.246078431372549,0.247058823529412,0.248039215686275,0.249019607843137,
0.25,0.250980392156863,0.251960784313725,0.252941176470588,0.253921568627451,
0.254901960784314,0.255882352941176,0.256862745098039,0.257843137254902,
0.258823529411765,0.259803921568627,0.26078431372549,0.261764705882353,
0.262745098039216,0.263725490196078,0.264705882352941,0.265686274509804,
0.266666666666667,0.267647058823529,0.268627450980392,0.269607843137255,
0.270588235294118,0.27156862745098,0.272549019607843,0.273529411764706,
0.274509803921569,0.275490196078431,0.276470588235294,0.277450980392157,
0.27843137254902,0.279411764705882,0.280392156862745,0.281372549019608,
0.282352941176471,0.283333333333333,0.284313725490196,0.285294117647059,
0.286274509803922,0.287254901960784,0.288235294117647,0.28921568627451,
0.290196078431373,0.291176470588235,0.292156862745098,0.293137254901961,
0.294117647058824,0.295098039215686,0.296078431372549,0.297058823529412,
0.298039215686275,0.299019607843137,0.3,0.300980392156863,0.301960784313725,
0.302941176470588,0.303921568627451,0.304901960784314,0.305882352941176,
0.306862745098039,0.307843137254902,0.308823529411765,0.309803921568627,
0.31078431372549,0.311764705882353,0.312745098039216,0.313725490196078,
0.314705882352941,0.315686274509804,0.316666666666667,0.317647058823529,
0.318627450980392,0.319607843137255,0.320588235294118,0.32156862745098,
0.322549019607843,0.323529411764706,0.324509803921569,0.325490196078431,
0.326470588235294,0.327450980392157,0.32843137254902,0.329411764705882,
0.330392156862745,0.331372549019608,0.332352941176471,0.333333333333333,
0.334313725490196,0.335294117647059,0.336274509803922,0.337254901960784,
0.338235294117647,0.33921568627451,0.340196078431373,0.341176470588235,
0.342156862745098,0.343137254901961,0.344117647058824,0.345098039215686,
0.346078431372549,0.347058823529412,0.348039215686274,0.349019607843137,
0.35,0.350980392156863,0.351960784313726,0.352941176470588,0.353921568627451,
0.354901960784314,0.355882352941176,0.356862745098039,0.357843137254902,
0.358823529411765,0.359803921568627,0.36078431372549,0.361764705882353,
0.362745098039216,0.363725490196078,0.364705882352941,0.365686274509804,
0.366666666666667,0.367647058823529,0.368627450980392,0.369607843137255,
0.370588235294118,0.37156862745098,0.372549019607843,0.373529411764706,
0.374509803921569,0.375490196078431,0.376470588235294,0.377450980392157,
0.37843137254902,0.379411764705882,0.380392156862745,0.381372549019608,
0.382352941176471,0.383333333333333,0.384313725490196,0.385294117647059,
0.386274509803922,0.387254901960784,0.388235294117647,0.38921568627451,
0.390196078431373,0.391176470588235,0.392156862745098,0.393137254901961,
0.394117647058824,0.395098039215686,0.396078431372549,0.397058823529412,
0.398039215686274,0.399019607843137,0.4,0.400980392156863,0.401960784313726,
0.402941176470588,0.403921568627451,0.404901960784314,0.405882352941176,
0.406862745098039,0.407843137254902,0.408823529411765,0.409803921568627,
0.41078431372549,0.411764705882353,0.412745098039216,0.413725490196078,
0.414705882352941,0.415686274509804,0.416666666666667,0.417647058823529,
0.418627450980392,0.419607843137255,0.420588235294118,0.42156862745098,
0.422549019607843,0.423529411764706,0.424509803921569,0.425490196078431,
0.426470588235294,0.427450980392157,0.42843137254902,0.429411764705882,
0.430392156862745,0.431372549019608,0.432352941176471,0.433333333333333,
0.434313725490196,0.435294117647059,0.436274509803922,0.437254901960784,
0.438235294117647,0.43921568627451,0.440196078431373,0.441176470588235,
0.442156862745098,0.443137254901961,0.444117647058824,0.445098039215686,
0.446078431372549,0.447058823529412,0.448039215686275,0.449019607843137,
0.45,0.450980392156863,0.451960784313725,0.452941176470588,0.453921568627451,
0.454901960784314,0.455882352941176,0.456862745098039,0.457843137254902,
0.458823529411765,0.459803921568627,0.46078431372549,0.461764705882353,
0.462745098039216,0.463725490196078,0.464705882352941,0.465686274509804,
0.466666666666667,0.467647058823529,0.468627450980392,0.469607843137255,
0.470588235294118,0.47156862745098,0.472549019607843,0.473529411764706,
0.474509803921569,0.475490196078431,0.476470588235294,0.477450980392157,
0.47843137254902,0.479411764705882,0.480392156862745,0.481372549019608,
0.482352941176471,0.483333333333333,0.484313725490196,0.485294117647059,
0.486274509803922,0.487254901960784,0.488235294117647,0.48921568627451,
0.490196078431373,0.491176470588235,0.492156862745098,0.493137254901961,
0.494117647058824,0.495098039215686,0.496078431372549,0.497058823529412,
0.498039215686275,0.499019607843137,0.5,0.500980392156863,0.501960784313725,
0.502941176470588,0.503921568627451,0.504901960784314,0.505882352941176,
0.506862745098039,0.507843137254902,0.508823529411765,0.509803921568627,
0.51078431372549,0.511764705882353,0.512745098039216,0.513725490196078,
0.514705882352941,0.515686274509804,0.516666666666667,0.517647058823529,
0.518627450980392,0.519607843137255,0.520588235294118,0.52156862745098,
0.522549019607843,0.523529411764706,0.524509803921569,0.525490196078431,
0.526470588235294,0.527450980392157,0.52843137254902,0.529411764705882,
0.530392156862745,0.531372549019608,0.532352941176471,0.533333333333333,
0.534313725490196,0.535294117647059,0.536274509803922,0.537254901960784,
0.538235294117647,0.53921568627451,0.540196078431373,0.541176470588235,
0.542156862745098,0.543137254901961,0.544117647058823,0.545098039215686,
0.546078431372549,0.547058823529412,0.548039215686275,0.549019607843137,
0.55,0.550980392156863,0.551960784313726,0.552941176470588,0.553921568627451,
0.554901960784314,0.555882352941176,0.556862745098039,0.557843137254902,
0.558823529411765,0.559803921568627,0.56078431372549,0.561764705882353,
0.562745098039216,0.563725490196078,0.564705882352941,0.565686274509804,
0.566666666666667,0.567647058823529,0.568627450980392,0.569607843137255,
0.570588235294118,0.57156862745098,0.572549019607843,0.573529411764706,
0.574509803921569,0.575490196078431,0.576470588235294,0.577450980392157,
0.57843137254902,0.579411764705882,0.580392156862745,0.581372549019608,
0.582352941176471,0.583333333333333,0.584313725490196,0.585294117647059,
0.586274509803922,0.587254901960784,0.588235294117647,0.58921568627451,
0.590196078431373,0.591176470588235,0.592156862745098,0.593137254901961,
0.594117647058824,0.595098039215686,0.596078431372549,0.597058823529412,
0.598039215686274,0.599019607843137,0.6,0.600980392156863,0.601960784313725,
0.602941176470588,0.603921568627451,0.604901960784314,0.605882352941176,
0.606862745098039,0.607843137254902,0.608823529411765,0.609803921568628,
0.61078431372549,0.611764705882353,0.612745098039216,0.613725490196078,
0.614705882352941,0.615686274509804,0.616666666666667,0.617647058823529,
0.618627450980392,0.619607843137255,0.620588235294118,0.62156862745098,
0.622549019607843,0.623529411764706,0.624509803921569,0.625490196078431,
0.626470588235294,0.627450980392157,0.62843137254902,0.629411764705882,
0.630392156862745,0.631372549019608,0.632352941176471,0.633333333333333,
0.634313725490196,0.635294117647059,0.636274509803922,0.637254901960784,
0.638235294117647,0.63921568627451,0.640196078431372,0.641176470588235,
0.642156862745098,0.643137254901961,0.644117647058824,0.645098039215686,
0.646078431372549,0.647058823529412,0.648039215686275,0.649019607843137,
0.65,0.650980392156863,0.651960784313726,0.652941176470588,0.653921568627451,
0.654901960784314,0.655882352941176,0.656862745098039,0.657843137254902,
0.658823529411765,0.659803921568627,0.66078431372549,0.661764705882353,
0.662745098039216,0.663725490196078,0.664705882352941,0.665686274509804,
0.666666666666667,0.667647058823529,0.668627450980392,0.669607843137255,
0.670588235294118,0.67156862745098,0.672549019607843,0.673529411764706,
0.674509803921569,0.675490196078431,0.676470588235294,0.677450980392157,
0.67843137254902,0.679411764705882,0.680392156862745,0.681372549019608,
0.682352941176471,0.683333333333333,0.684313725490196,0.685294117647059,
0.686274509803922,0.687254901960784,0.688235294117647,0.68921568627451,
0.690196078431373,0.691176470588235,0.692156862745098,0.693137254901961,
0.694117647058824,0.695098039215686,0.696078431372549,0.697058823529412,
0.698039215686274,0.699019607843137,0.7,0.700980392156863,0.701960784313725,
0.702941176470588,0.703921568627451,0.704901960784314,0.705882352941177,
0.706862745098039,0.707843137254902,0.708823529411765,0.709803921568627,
0.71078431372549,0.711764705882353,0.712745098039216,0.713725490196078,
0.714705882352941,0.715686274509804,0.716666666666667,0.717647058823529,
0.718627450980392,0.719607843137255,0.720588235294118,0.72156862745098,
0.722549019607843,0.723529411764706,0.724509803921569,0.725490196078431,
0.726470588235294,0.727450980392157,0.72843137254902,0.729411764705882,
0.730392156862745,0.731372549019608,0.732352941176471,0.733333333333333,
0.734313725490196,0.735294117647059,0.736274509803922,0.737254901960784,
0.738235294117647,0.73921568627451,0.740196078431373,0.741176470588235,
0.742156862745098,0.743137254901961,0.744117647058824,0.745098039215686,
0.746078431372549,0.747058823529412,0.748039215686275,0.749019607843137,
0.75,0.750980392156863,0.751960784313725,0.752941176470588,0.753921568627451,
0.754901960784314,0.755882352941176,0.756862745098039,0.757843137254902,
0.758823529411765,0.759803921568627,0.76078431372549,0.761764705882353,
0.762745098039216,0.763725490196078,0.764705882352941,0.765686274509804,
0.766666666666667,0.767647058823529,0.768627450980392,0.769607843137255,
0.770588235294118,0.77156862745098,0.772549019607843,0.773529411764706,
0.774509803921569,0.775490196078431,0.776470588235294,0.777450980392157,
0.77843137254902,0.779411764705882,0.780392156862745,0.781372549019608,
0.782352941176471,0.783333333333333,0.784313725490196,0.785294117647059,
0.786274509803922,0.787254901960784,0.788235294117647,0.78921568627451,
0.790196078431373,0.791176470588235,0.792156862745098,0.793137254901961,
0.794117647058823,0.795098039215686,0.796078431372549,0.797058823529412,
0.798039215686275,0.799019607843137,0.8,0.800980392156863,0.801960784313726,
0.802941176470588,0.803921568627451,0.804901960784314,0.805882352941176,
0.806862745098039,0.807843137254902,0.808823529411765,0.809803921568627,
0.81078431372549,0.811764705882353,0.812745098039216,0.813725490196078,
0.814705882352941,0.815686274509804,0.816666666666667,0.817647058823529,
0.818627450980392,0.819607843137255,0.820588235294118,0.82156862745098,
0.822549019607843,0.823529411764706,0.824509803921569,0.825490196078431,
0.826470588235294,0.827450980392157,0.82843137254902,0.829411764705882,
0.830392156862745,0.831372549019608,0.832352941176471,0.833333333333333,
0.834313725490196,0.835294117647059,0.836274509803922,0.837254901960784,
0.838235294117647,0.83921568627451,0.840196078431373,0.841176470588235,
0.842156862745098,0.843137254901961,0.844117647058824,0.845098039215686,
0.846078431372549,0.847058823529412,0.848039215686274,0.849019607843137,
0.85,0.850980392156863,0.851960784313725,0.852941176470588,0.853921568627451,
0.854901960784314,0.855882352941176,0.856862745098039,0.857843137254902,
0.858823529411765,0.859803921568628,0.86078431372549,0.861764705882353,
0.862745098039216,0.863725490196078,0.864705882352941,0.865686274509804,
0.866666666666667,0.867647058823529,0.868627450980392,0.869607843137255,
0.870588235294118,0.87156862745098,0.872549019607843,0.873529411764706,
0.874509803921569,0.875490196078431,0.876470588235294,0.877450980392157,
0.87843137254902,0.879411764705882,0.880392156862745,0.881372549019608,
0.882352941176471,0.883333333333333,0.884313725490196,0.885294117647059,
0.886274509803922,0.887254901960784,0.888235294117647,0.88921568627451,
0.890196078431372,0.891176470588235,0.892156862745098,0.893137254901961,
0.894117647058824,0.895098039215686,0.896078431372549,0.897058823529412,
0.898039215686275,0.899019607843137,0.9,0.900980392156863,0.901960784313726,
0.902941176470588,0.903921568627451,0.904901960784314,0.905882352941176,
0.906862745098039,0.907843137254902,0.908823529411765,0.909803921568627,
0.91078431372549,0.911764705882353,0.912745098039216,0.913725490196078,
0.914705882352941,0.915686274509804,0.916666666666667,0.917647058823529,
0.918627450980392,0.919607843137255,0.920588235294118,0.92156862745098,
0.922549019607843,0.923529411764706,0.924509803921569,0.925490196078431,
0.926470588235294,0.927450980392157,0.92843137254902,0.929411764705882,
0.930392156862745,0.931372549019608,0.932352941176471,0.933333333333333,
0.934313725490196,0.935294117647059,0.936274509803922,0.937254901960784,
0.938235294117647,0.93921568627451,0.940196078431373,0.941176470588235,
0.942156862745098,0.943137254901961,0.944117647058824,0.945098039215686,
0.946078431372549,0.947058823529412,0.948039215686274,0.949019607843137,
0.95,0.950980392156863,0.951960784313725,0.952941176470588,0.953921568627451,
0.954901960784314,0.955882352941177,0.956862745098039,0.957843137254902,
0.958823529411765,0.959803921568627,0.96078431372549,0.961764705882353,
0.962745098039216,0.963725490196078,0.964705882352941,0.965686274509804,
0.966666666666667,0.967647058823529,0.968627450980392,0.969607843137255,
0.970588235294118,0.97156862745098,0.972549019607843,0.973529411764706,
0.974509803921569,0.975490196078431,0.976470588235294,0.977450980392157,
0.97843137254902,0.979411764705882,0.980392156862745,0.981372549019608,
0.982352941176471,0.983333333333333,0.984313725490196,0.985294117647059,
0.985937383514281),.UNSPECIFIED.)
GEOMETRIC_REPRESENTATION_ITEM()
RATIONAL_B_SPLINE_SURFACE(((1.,0.995734176295034,1.,0.995734176295034,1.,
0.995734176295034,1.,0.995734176295034,1.,0.995734176295034,1.,0.995734176295034,
1.,0.995734176295034,1.,0.995734176295034,1.,0.995734176295034,1.,0.995734176295034,
1.,0.995734176295034,1.,0.995734176295034,1.,0.995734176295034,1.,0.995734176295034,
1.,0.995734176295034,1.,0.995734176295034,1.,0.995734176295034,1.,0.995734176295034,
1.,0.995734176295034,1.,0.995734176295034,1.,0.995734176295034,1.,0.995734176295034,
1.,0.995734176295034,1.,0.995734176295034,1.,0.995734176295034,1.,0.995734176295034,
1.,0.995734176295034,1.,0.995734176295034,1.,0.995734176295034,1.,0.995734176295034,
1.,0.995734176295034,1.,0.995734176295034,1.,0.995734176295034,1.,0.995734176295034,
1.,0.995734176295034,1.,0.995734176295034,1.,0.995734176295034,1.,0.995734176295034,
1.,0.995734176295034,1.,0.995734176295034,1.,0.995734176295034,1.,0.995734176295034,
1.,0.995734176295034,1.,0.995734176295034,1.,0.995734176295034,1.,0.995734176295034,
1.,0.995734176295034,1.,0.995734176295034,1.,0.995734176295034,1.,0.995734176295034,
1.,0.995734176295034,1.,0.995734176295034,1.,0.995734176295034,1.,0.995734176295034,
1.,0.995734176295034,1.,0.995734176295034,1.,0.995734176295034,1.,0.995734176295034,
1.,0.995734176295034,1.,0.995734176295034,1.,0.995734176295034,1.,0.995734176295034,
1.,0.995734176295034,1.,0.995734176295034,1.,0.995734176295034,1.,0.995734176295034,
1.,0.995734176295034,1.,0.995734176295034,1.,0.995734176295034,1.,0.995734176295034,
1.,0.995734176295034,1.,0.995734176295034,1.,0.995734176295034,1.,0.995734176295034,
1.,0.995734176295034,1.,0.995734176295034,1.,0.995734176295034,1.,0.995734176295034,
1.,0.995734176295034,1.,0.995734176295034,1.,0.995734176295034,1.,0.995734176295034,
1.,0.995734176295034,1.,0.995734176295034,1.,0.995734176295034,1.,0.995734176295034,
1.,0.995734176295034,1.,0.995734176295034,1.,0.995734176295034,1.,0.995734176295034,
1.,0.995734176295034,1.,0.995734176295034,1.,0.995734176295034,1.,0.995734176295034,
1.,0.995734176295034,1.,0.995734176295034,1.,0.995734176295034,1.,0.995734176295034,
1.,0.995734176295034,1.,0.995734176295034,1.,0.995734176295034,1.,0.995734176295034,
1.,0.995734176295034,1.,0.995734176295034,1.,0.995734176295034,1.,0.995734176295034,
1.,0.995734176295034,1.,0.995734176295034,1.,0.995734176295034,1.,0.995734176295034,
1.,0.995734176295034,1.,0.995734176295034,1.,0.995734176295034,1.,0.995734176295034,
1.,0.995734176295034,1.,0.995734176295034,1.,0.995734176295034,1.,0.995734176295034,
1.,0.995734176295034,1.,0.995734176295034,1.,0.995734176295034,1.,0.995734176295034,
1.,0.995734176295034,1.,0.995734176295034,1.,0.995734176295034,1.,0.995734176295034,
1.,0.995734176295034,1.,0.995734176295034,1.,0.995734176295034,1.,0.995734176295034,
1.,0.995734176295034,1.,0.995734176295034,1.,0.995734176295034,1.,0.995734176295034,
1.,0.995734176295034,1.,0.995734176295034,1.,0.995734176295034,1.,0.995734176295034,
1.,0.995734176295034,1.,0.995734176295034,1.,0.995734176295034,1.,0.995734176295034,
1.,0.995734176295034,1.,0.995734176295034,1.,0.995734176295034,1.,0.995734176295034,
1.,0.995734176295034,1.,0.995734176295034,1.,0.995734176295034,1.,0.995734176295034,
1.,0.995734176295034,1.,0.995734176295034,1.,0.995734176295034,1.,0.995734176295034,
1.,0.995734176295034,1.,0.995734176295034,1.,0.995734176295034,1.,0.995734176295034,
1.,0.995734176295034,1.,0.995734176295034,1.,0.995734176295034,1.,0.995734176295034,
1.,0.995734176295034,1.,0.995734176295034,1.,0.995734176295034,1.,0.995734176295034,
1.,0.995734176295034,1.,0.995734176295034,1.,0.995734176295034,1.,0.995734176295034,
1.,0.995734176295034,1.,0.995734176295034,1.,0.995734176295034,1.,0.995734176295034,
1.,0.995734176295034,1.,0.995734176295034,1.,0.995734176295034,1.,0.995734176295034,
1.,0.995734176295034,1.,0.995734176295034,1.,0.995734176295034,1.,0.995734176295034,
1.,0.995734176295034,1.,0.995734176295034,1.,0.995734176295034,1.,0.995734176295034,
1.,0.995734176295034,1.,0.995734176295034,1.,0.995734176295034,1.,0.995734176295034,
1.,0.995734176295034,1.,0.995734176295034,1.,0.995734176295034,1.,0.995734176295034,
1.,0.995734176295034,1.,0.995734176295034,1.,0.995734176295034,1.,0.995734176295034,
1.,0.995734176295034,1.,0.995734176295034,1.,0.995734176295034,1.,0.995734176295034,
1.,0.995734176295034,1.,0.995734176295034,1.,0.995734176295034,1.,0.995734176295034,
1.,0.995734176295034,1.,0.995734176295034,1.,0.995734176295034,1.,0.995734176295034,
1.,0.995734176295034,1.,0.995734176295034,1.,0.995734176295034,1.,0.995734176295034,
1.,0.995734176295034,1.,0.995734176295034,1.,0.995734176295034,1.,0.995734176295034,
1.,0.995734176295034,1.,0.995734176295034,1.,0.995734176295034,1.,0.995734176295034,
1.,0.995734176295034,1.,0.995734176295034,1.,0.995734176295034,1.,0.995734176295034,
1.,0.995734176295034,1.,0.995734176295034,1.,0.995734176295034,1.,0.995734176295034,
1.,0.995734176295034,1.,0.995734176295034,1.,0.995734176295034,1.,0.995734176295034,
1.,0.995734176295034,1.,0.995734176295034,1.,0.995734176295034,1.,0.995734176295034,
1.,0.995734176295034,1.,0.995734176295034,1.,0.995734176295034,1.,0.995734176295034,
1.,0.995734176295034,1.,0.995734176295034,1.,0.995734176295034,1.,0.995734176295034,
1.,0.995734176295034,1.,0.995734176295034,1.,0.995734176295034,1.,0.995734176295034,
1.,0.995734176295034,1.,0.995734176295034,1.,0.995734176295034,1.,0.995734176295034,
1.,0.995734176295034,1.,0.995734176295034,1.,0.995734176295034,1.,0.995734176295034,
1.,0.995734176295034,1.,0.995734176295034,1.,0.995734176295034,1.,0.995734176295034,
1.,0.995734176295034,1.,0.995734176295034,1.,0.995734176295034,1.,0.995734176295034,
1.,0.995734176295034,1.,0.995734176295034,1.,0.995734176295034,1.,0.995734176295034,
1.,0.995734176295034,1.,0.995734176295034,1.,0.995734176295034,1.,0.995734176295034,
1.,0.995734176295034,1.,0.995734176295034,1.,0.995734176295034,1.,0.995734176295034,
1.,0.995734176295034,1.,0.995734176295034,1.,0.995734176295034,1.,0.995734176295034,
1.,0.995734176295034,1.,0.995734176295034,1.,0.995734176295034,1.,0.995734176295034,
1.,0.995734176295034,1.,0.995734176295034,1.,0.995734176295034,1.,0.995734176295034,
1.,0.995734176295034,1.,0.995734176295034,1.,0.995734176295034,1.,0.995734176295034,
1.,0.995734176295034,1.,0.995734176295034,1.,0.995734176295034,1.,0.995734176295034,
1.,0.995734176295034,1.,0.995734176295034,1.,0.995734176295034,1.,0.995734176295034,
1.,0.995734176295034,1.,0.995734176295034,1.,0.995734176295034,1.,0.995734176295034,
1.,0.995734176295034,1.,0.995734176295034,1.,0.995734176295034,1.,0.995734176295034,
1.,0.995734176295034,1.,0.995734176295034,1.,0.995734176295034,1.,0.995734176295034,
1.,0.995734176295034,1.,0.995734176295034,1.,0.995734176295034,1.,0.995734176295034,
1.,0.995734176295034,1.,0.995734176295034,1.,0.995734176295034,1.,0.995734176295034,
1.,0.995734176295034,1.,0.995734176295034,1.,0.995734176295034,1.,0.995734176295034,
1.,0.995734176295034,1.,0.995734176295034,1.,0.995734176295034,1.,0.995734176295034,
1.,0.995734176295034,1.,0.995734176295034,1.,0.995734176295034,1.,0.995734176295034,
1.,0.995734176295034,1.,0.995734176295034,1.,0.995734176295034,1.,0.995734176295034,
1.,0.995734176295034,1.,0.995734176295034,1.,0.995734176295034,1.,0.995734176295034,
1.,0.995734176295034,1.,0.995734176295034,1.,0.995734176295034,1.,0.995734176295034,
1.,0.995734176295034,1.,0.995734176295034,1.,0.995734176295034,1.,0.995734176295034,
1.,0.995734176295034,1.,0.995734176295034,1.,0.995734176295034,1.,0.995734176295034,
1.,0.995734176295034,1.,0.995734176295034,1.,0.995734176295034,1.,0.995734176295034,
1.,0.995734176295034,1.,0.995734176295034,1.,0.995734176295034,1.,0.995734176295034,
1.,0.995734176295034,1.,0.995734176295034,1.,0.995734176295034,1.,0.995734176295034,
1.,0.995734176295034,1.,0.995734176295034,1.,0.995734176295034,1.,0.995734176295034,
1.,0.995734176295034,1.,0.995734176295034,1.,0.995734176295034,1.,0.995734176295034,
1.,0.995734176295034,1.,0.995734176295034,1.,0.995734176295034,1.,0.995734176295034,
1.,0.995734176295034,1.,0.995734176295034,1.,0.995734176295034,1.,0.995734176295034,
1.,0.995734176295034,1.,0.995734176295034,1.,0.995734176295034,1.,0.995734176295034,
1.,0.995734176295034,1.,0.995734176295034,1.,0.995734176295034,1.,0.995734176295034,
1.,0.995734176295034,1.,0.995734176295034,1.,0.995734176295034,1.,0.995734176295034,
1.,0.995734176295034,1.,0.995734176295034,1.,0.995734176295034,1.,0.995734176295034,
1.,0.995734176295034,1.,0.995734176295034,1.,0.995734176295034,1.,0.995734176295034,
1.,0.995734176295034,1.,0.995734176295034,1.,0.995734176295034,1.,0.995734176295034,
1.,0.995734176295034,1.,0.995734176295034,1.,0.995734176295034,1.,0.995734176295034,
1.,0.995734176295034,1.,0.995734176295034,1.,0.995734176295034,1.,0.995734176295034,
1.,0.995734176295034,1.,0.995734176295034,1.,0.995734176295034,1.,0.995734176295034,
1.,0.995734176295034,1.,0.995734176295034,1.,0.995734176295034,1.,0.995734176295034,
1.,0.995734176295034,1.,0.995734176295034,1.,0.995734176295034,1.,0.995734176295034,
1.,0.995734176295034,1.,0.995734176295034,1.,0.995734176295034,1.,0.995734176295034,
1.,0.995734176295034,1.,0.995734176295034,1.,0.995734176295034,1.,0.995734176295034,
1.,0.995734176295034,1.,0.995734176295034,1.,0.995734176295034,1.,0.995734176295034,
1.,0.995734176295034,1.,0.995734176295034,1.,0.995734176295034,1.,0.995734176295034,
1.,0.995734176295034,1.,0.995734176295034,1.,0.995734176295034,1.,0.995734176295034,
1.,0.995734176295034,1.,0.995734176295034,1.,0.995734176295034,1.,0.995734176295034,
1.,0.995734176295034,1.,0.995734176295034,1.,0.995734176295034,1.,0.995734176295034,
1.,0.995734176295034,1.,0.995734176295034,1.,0.995734176295034,1.,0.995734176295034,
1.,0.995734176295034,1.,0.995734176295034,1.,0.995734176295034,1.,0.995734176295034,
1.,0.995734176295034,1.,0.995734176295034,1.,0.995734176295034,1.,0.995734176295034,
1.,0.995734176295034,1.,0.995734176295034,1.,0.995734176295034,1.,0.995734176295034,
1.,0.995734176295034,1.,0.995734176295034,1.,0.995734176295034,1.,0.995734176295034,
1.,0.995734176295034,1.,0.995734176295034,1.,0.995734176295034,1.,0.995734176295034,
1.,0.995734176295034,1.,0.995734176295034,1.,0.995734176295034,1.,0.995734176295034,
1.,0.995734176295034,1.,0.995734176295034,1.,0.995734176295034,1.,0.995734176295034,
1.,0.995734176295034,1.,0.995734176295034,1.,0.995734176295034,1.,0.995734176295034,
1.,0.995734176295034,1.,0.995734176295034,1.,0.995734176295034,1.,0.995734176295034,
1.,0.995734176295034,1.,0.995734176295034,1.,0.995734176295034,1.,0.995734176295034,
1.,0.995734176295034,1.,0.995734176295034,1.,0.995734176295034,1.,0.995734176295034,
1.,0.995734176295034,1.,0.995734176295034,1.,0.995734176295034,1.,0.995734176295034,
1.,0.995734176295034,1.,0.995734176295034,1.,0.995734176295034,1.,0.995734176295034,
1.,0.995734176295034,1.,0.995734176295034,1.,0.995734176295034,1.,0.995734176295034,
1.,0.995734176295034,1.,0.995734176295034,1.,0.995734176295034,1.,0.995734176295034,
1.,0.995734176295034,1.,0.995734176295034,1.,0.995734176295034,1.,0.995734176295034,
1.,0.995734176295034,1.,0.995734176295034,1.,0.995734176295034,1.,0.995734176295034,
1.,0.995734176295034,1.,0.995734176295034,1.,0.995734176295034,1.,0.995734176295034,
1.,0.995734176295034,1.,0.995734176295034,1.,0.995734176295034,1.,0.995734176295034,
1.,0.995734176295034,1.,0.995734176295034,1.,0.995734176295034,1.,0.995734176295034,
1.,0.995734176295034,1.,0.995734176295034,1.,0.995734176295034,1.,0.995734176295034,
1.,0.995734176295034,1.,0.995734176295034,1.,0.995734176295034,1.,0.995734176295034,
1.,0.995734176295034,1.,0.995734176295034,1.,0.995734176295034,1.,0.995734176295034,
1.,0.995734176295034,1.,0.995734176295034,1.,0.995734176295034,1.,0.995734176295034,
1.,0.995734176295034,1.,0.995734176295034,1.,0.995734176295034,1.,0.995734176295034,
1.,0.995734176295034,1.,0.995734176295034,1.,0.995734176295034,1.,0.995734176295034,
1.,0.995734176295034,1.,0.995734176295034,1.,0.995734176295034,1.,0.995734176295034,
1.,0.995734176295034,1.,0.995734176295034,1.,0.995734176295034,1.,0.995734176295034,
1.,0.995734176295034,1.,0.995734176295034,1.,0.995734176295034,1.,0.995734176295034,
1.,0.995734176295034,1.,0.995734176295034,1.,0.995734176295034,1.,0.995734176295034,
1.,0.995734176295034,1.,0.995734176295034,1.,0.995734176295034,1.,0.995734176295034,
1.,0.995734176295034,1.,0.995734176295034,1.,0.995734176295034,1.,0.995734176295034,
1.,0.995734176295034,1.,0.995734176295034,1.,0.995734176295034,1.,0.995734176295034,
1.,0.995734176295034,1.,0.995734176295034,1.,0.995734176295034,1.,0.995734176295034,
1.,0.995734176295034,1.,0.995734176295034,1.,0.995734176295034,1.,0.995734176295034,
1.,0.995734176295034,1.,0.995734176295034,1.,0.995734176295034,1.,0.995734176295034,
1.,0.995734176295034,1.,0.995734176295034,1.,0.995734176295034,1.,0.995734176295034,
1.,0.995734176295034,1.,0.995734176295034,1.,0.995734176295034,1.,0.995734176295034,
1.,0.995734176295034,1.,0.995734176295034,1.,0.995734176295034,1.,0.995734176295034,
1.,0.995734176295034,1.,0.995734176295034,1.,0.995734176295034,1.,0.995734176295034,
1.,0.995734176295034,1.,0.995734176295034,1.,0.995734176295034,1.,0.995734176295034,
1.,0.995734176295034,1.,0.995734176295034,1.,0.995734176295034,1.,0.995734176295034,
1.,0.995734176295034,1.,0.995734176295034,1.,0.995734176295034,1.,0.995734176295034,
1.,0.995734176295034,1.,0.995734176295034,1.,0.995734176295034,1.,0.995734176295034,
1.,0.995734176295034,1.,0.995734176295034,1.,0.995734176295034,1.,0.995734176295034,
1.,0.995734176295034,1.,0.995734176295034,1.,0.995734176295034,1.,0.995734176295034,
1.,0.995734176295034,1.,0.995734176295034,1.,0.995734176295034,1.,0.995734176295034,
1.,0.995734176295034,1.,0.995734176295034,1.,0.995734176295034,1.,0.995734176295034,
1.,0.995734176295034,1.,0.995734176295034,1.,0.995734176295034,1.,0.995734176295034,
1.,0.995734176295034,1.,0.995734176295034,1.,0.995734176295034,1.,0.995734176295034,
1.,0.995734176295034,1.,0.995734176295034,1.,0.995734176295034,1.,0.995734176295034,
1.,0.995734176295034,1.,0.995734176295034,1.,0.995734176295034,1.,0.995734176295034,
1.,0.995734176295034,1.,0.995734176295034,1.,0.995734176295034,1.,0.995734176295034,
1.,0.995734176295034,1.,0.995734176295034,1.,0.995734176295034,1.,0.995734176295034,
1.,0.995734176295034,1.,0.995734176295034,1.,0.995734176295034,1.,0.995734176295034,
1.,0.995734176295034,1.,0.995734176295034,1.,0.995734176295034,1.,0.995734176295034,
1.,0.995734176295034,1.,0.995734176295034,1.,0.995734176295034,1.,0.995734176295034,
1.,0.995734176295034,1.,0.995734176295034,1.,0.995734176295034,1.,0.995734176295034,
1.,0.995734176295034,1.,0.995734176295034,1.,0.995734176295034,1.,0.995734176295034,
1.,0.995734176295034,1.,0.995734176295034,1.,0.995734176295034,1.,0.995734176295034,
1.,0.995734176295034,1.,0.995734176295034,1.,0.995734176295034,1.,0.995734176295034,
1.,0.995734176295034,1.,0.995734176295034,1.,0.995734176295034,1.,0.995734176295034,
1.,0.995734176295034,1.,0.995734176295034,1.,0.995734176295034,1.,0.995734176295034,
1.,0.995734176295034,1.,0.995734176295034,1.,0.995734176295034,1.,0.995734176295034,
1.,0.995734176295034,1.,0.995734176295034,1.,0.995734176295034,1.,0.995734176295034,
1.,0.995734176295034,1.,0.995734176295034,1.,0.995734176295034,1.,0.995734176295034,
1.,0.995734176295034,1.,0.995734176295034,1.,0.995734176295034,1.,0.995734176295034,
1.,0.995734176295034,1.,0.995734176295034,1.,0.995734176295034,1.,0.995734176295034,
1.,0.995734176295034,1.,0.995734176295034,1.,0.995734176295034,1.,0.995734176295034,
1.,0.995734176295034,1.,0.995734176295034,1.,0.995734176295034,1.,0.995734176295034,
1.,0.995734176295034,1.,0.995734176295034,1.,0.995734176295034,1.,0.995734176295034,
1.,0.995734176295034,1.,0.995734176295034,1.,0.995734176295034,1.,0.995734176295034,
1.,0.995734176295034,1.,0.995734176295034,1.,0.995734176295034,1.,0.995734176295034,
1.,0.995734176295034,1.,0.995734176295034,1.,0.995734176295034,1.,0.995734176295034,
1.,0.995734176295034,1.,0.995734176295034,1.,0.995734176295034,1.,0.995734176295034,
1.,0.995734176295034,1.,0.995734176295034,1.,0.995734176295034,1.,0.995734176295034,
1.,0.995734176295034,1.,0.995734176295034,1.,0.995734176295034,1.,0.995734176295034,
1.,0.995734176295034,1.,0.995734176295034,1.,0.995734176295034,1.,0.995734176295034,
1.,0.995734176295034,1.,0.995734176295034,1.,0.995734176295034,1.,0.995734176295034,
1.,0.995734176295034,1.,0.995734176295034,1.,0.995734176295034,1.,0.995734176295034,
1.,0.995734176295034,1.,0.995734176295034,1.,0.995734176295034,1.,0.995734176295034,
1.,0.995734176295034,1.,0.995734176295034,1.,0.995734176295034,1.,0.995734176295034,
1.,0.995734176295034,1.,0.995734176295034,1.,0.995734176295034,1.,0.995734176295034,
1.,0.995734176295034,1.,0.995734176295034,1.,0.995734176295034,1.,0.995734176295034,
1.,0.995734176295034,1.,0.995734176295034,1.,0.995734176295034,1.,0.995734176295034,
1.,0.995734176295034,1.,0.995734176295034,1.,0.995734176295034,1.,0.995734176295034,
1.,0.995734176295034,1.,0.995734176295034,1.,0.995734176295034,1.,0.995734176295034,
1.,0.995734176295034,1.,0.995734176295034,1.,0.995734176295034,1.,0.995734176295034,
1.,0.995734176295034,1.,0.995734176295034,1.,0.995734176295034,1.,0.995734176295034,
1.,0.995734176295034,1.,0.995734176295034,1.,0.995734176295034,1.,0.995734176295034,
1.,0.995734176295034,1.,0.995734176295034,1.,0.995734176295034,1.,0.995734176295034,
1.,0.995734176295034,1.,0.995734176295034,1.,0.995734176295034,1.,0.995734176295034,
1.,0.995734176295034,1.,0.995734176295034,1.,0.995734176295034,1.,0.995734176295034,
1.,0.995734176295034,1.,0.995734176295034,1.,0.995734176295034,1.,0.995734176295034,
1.,0.995734176295034,1.,0.995734176295034,1.,0.995734176295034,1.,0.995734176295034,
1.,0.995734176295034,1.,0.995734176295034,1.,0.995734176295034,1.,0.995734176295034,
1.,0.995734176295034,1.,0.995734176295034,1.,0.995734176295034,1.,0.995734176295034,
1.,0.995734176295034,1.,0.995734176295034,1.,0.995734176295034,1.,0.995734176295034,
1.,0.995734176295034,1.,0.995734176295034,1.,0.995734176295034,1.,0.995734176295034,
1.,0.995734176295034,1.,0.995734176295034,1.,0.995734176295034,1.,0.995734176295034,
1.,0.995734176295034,1.,0.995734176295034,1.,0.995734176295034,1.,0.995734176295034,
1.,0.995734176295034,1.,0.995734176295034,1.,0.995734176295034,1.,0.995734176295034,
1.,0.995734176295034,1.,0.995734176295034,1.,0.995734176295034,1.,0.995734176295034,
1.,0.995734176295034,1.,0.995734176295034,1.,0.995734176295034,1.,0.995734176295034,
1.,0.995734176295034,1.,0.995734176295034,1.,0.995734176295034,1.,0.995734176295034,
1.,0.995734176295034,1.,0.995734176295034,1.,0.995734176295034,1.,0.995734176295034,
1.,0.995734176295034,1.,0.995734176295034,1.,0.995734176295034,1.,0.995734176295034,
1.,0.995734176295034,1.,0.995734176295034,1.,0.995734176295034,1.,0.995734176295034,
1.,0.995734176295034,1.,0.995734176295034,1.,0.995734176295034,1.,0.995734176295034,
1.,0.995734176295034,1.,0.995734176295034,1.,0.995734176295034,1.,0.995734176295034,
1.,0.995734176295034,1.,0.995734176295034,1.,0.995734176295034,1.,0.995734176295034,
1.,0.995734176295034,1.,0.995734176295034,1.,0.995734176295034,1.,0.995734176295034,
1.,0.995734176295034,1.,0.995734176295034,1.,0.995734176295034,1.,0.995734176295034,
1.,0.995734176295034,1.,0.995734176295034,1.,0.995734176295034,1.,0.995734176295034,
1.,0.995734176295034,1.,0.995734176295034,1.,0.995734176295034,1.,0.995734176295034,
1.,0.995734176295034,1.,0.995734176295034,1.,0.995734176295034,1.,0.995734176295034,
1.,0.995734176295034,1.,0.995734176295034,1.,0.995734176295034,1.,0.995734176295034,
1.,0.995734176295034,1.,0.995734176295034,1.,0.995734176295034,1.,0.995734176295034,
1.,0.995734176295034,1.,0.995734176295034,1.,0.995734176295034,1.,0.995734176295034,
1.,0.995734176295034,1.,0.995734176295034,1.,0.995734176295034,1.,0.995734176295034,
1.,0.995734176295034,1.,0.995734176295034,1.,0.995734176295034,1.,0.995734176295034,
1.,0.995734176295034,1.,0.995734176295034,1.,0.995734176295034,1.,0.995734176295034,
1.,0.995734176295034,1.,0.995734176295034,1.,0.995734176295034,1.,0.995734176295034,
1.,0.995734176295034,1.,0.995734176295034,1.,0.995734176295034,1.,0.995734176295034,
1.,0.995734176295034,1.,0.995734176295034,1.,0.995734176295034,1.,0.995734176295034,
1.,0.995734176295034,1.,0.995734176295034,1.,0.995734176295034,1.,0.995734176295034,
1.,0.995734176295034,1.,0.995734176295034,1.,0.995734176295034,1.,0.995734176295034,
1.,0.995734176295034,1.,0.995734176295034,1.,0.995734176295034,1.,0.995734176295034,
1.,0.995734176295034,1.,0.995734176295034,1.,0.995734176295034,1.,0.995734176295034,
1.,0.995734176295034,1.,0.995734176295034,1.,0.995734176295034,1.,0.995734176295034,
1.,0.995734176295034,1.,0.995734176295034,1.,0.995734176295034,1.,0.995734176295034,
1.,0.995734176295034,1.,0.995734176295034,1.,0.995734176295034,1.,0.995734176295034,
1.,0.995734176295034,1.,0.995734176295034,1.,0.995734176295034,1.,0.995734176295034,
1.,0.995734176295034,1.,0.995734176295034,1.,0.995734176295034,1.,0.995734176295034,
1.,0.995734176295034,1.,0.995734176295034,1.,0.995734176295034,1.,0.995734176295034,
1.,0.995734176295034,1.,0.995734176295034,1.,0.995734176295034,1.,0.995734176295034,
1.,0.995734176295034,1.,0.995734176295034,1.,0.995734176295034,1.,0.99720106003931,
0.998075063662495),(1.,0.995734176295034,1.,0.995734176295034,1.,0.995734176295034,
1.,0.995734176295034,1.,0.995734176295034,1.,0.995734176295034,1.,0.995734176295034,
1.,0.995734176295034,1.,0.995734176295034,1.,0.995734176295034,1.,0.995734176295034,
1.,0.995734176295034,1.,0.995734176295034,1.,0.995734176295034,1.,0.995734176295034,
1.,0.995734176295034,1.,0.995734176295034,1.,0.995734176295034,1.,0.995734176295034,
1.,0.995734176295034,1.,0.995734176295034,1.,0.995734176295034,1.,0.995734176295034,
1.,0.995734176295034,1.,0.995734176295034,1.,0.995734176295034,1.,0.995734176295034,
1.,0.995734176295034,1.,0.995734176295034,1.,0.995734176295034,1.,0.995734176295034,
1.,0.995734176295034,1.,0.995734176295034,1.,0.995734176295034,1.,0.995734176295034,
1.,0.995734176295034,1.,0.995734176295034,1.,0.995734176295034,1.,0.995734176295034,
1.,0.995734176295034,1.,0.995734176295034,1.,0.995734176295034,1.,0.995734176295034,
1.,0.995734176295034,1.,0.995734176295034,1.,0.995734176295034,1.,0.995734176295034,
1.,0.995734176295034,1.,0.995734176295034,1.,0.995734176295034,1.,0.995734176295034,
1.,0.995734176295034,1.,0.995734176295034,1.,0.995734176295034,1.,0.995734176295034,
1.,0.995734176295034,1.,0.995734176295034,1.,0.995734176295034,1.,0.995734176295034,
1.,0.995734176295034,1.,0.995734176295034,1.,0.995734176295034,1.,0.995734176295034,
1.,0.995734176295034,1.,0.995734176295034,1.,0.995734176295034,1.,0.995734176295034,
1.,0.995734176295034,1.,0.995734176295034,1.,0.995734176295034,1.,0.995734176295034,
1.,0.995734176295034,1.,0.995734176295034,1.,0.995734176295034,1.,0.995734176295034,
1.,0.995734176295034,1.,0.995734176295034,1.,0.995734176295034,1.,0.995734176295034,
1.,0.995734176295034,1.,0.995734176295034,1.,0.995734176295034,1.,0.995734176295034,
1.,0.995734176295034,1.,0.995734176295034,1.,0.995734176295034,1.,0.995734176295034,
1.,0.995734176295034,1.,0.995734176295034,1.,0.995734176295034,1.,0.995734176295034,
1.,0.995734176295034,1.,0.995734176295034,1.,0.995734176295034,1.,0.995734176295034,
1.,0.995734176295034,1.,0.995734176295034,1.,0.995734176295034,1.,0.995734176295034,
1.,0.995734176295034,1.,0.995734176295034,1.,0.995734176295034,1.,0.995734176295034,
1.,0.995734176295034,1.,0.995734176295034,1.,0.995734176295034,1.,0.995734176295034,
1.,0.995734176295034,1.,0.995734176295034,1.,0.995734176295034,1.,0.995734176295034,
1.,0.995734176295034,1.,0.995734176295034,1.,0.995734176295034,1.,0.995734176295034,
1.,0.995734176295034,1.,0.995734176295034,1.,0.995734176295034,1.,0.995734176295034,
1.,0.995734176295034,1.,0.995734176295034,1.,0.995734176295034,1.,0.995734176295034,
1.,0.995734176295034,1.,0.995734176295034,1.,0.995734176295034,1.,0.995734176295034,
1.,0.995734176295034,1.,0.995734176295034,1.,0.995734176295034,1.,0.995734176295034,
1.,0.995734176295034,1.,0.995734176295034,1.,0.995734176295034,1.,0.995734176295034,
1.,0.995734176295034,1.,0.995734176295034,1.,0.995734176295034,1.,0.995734176295034,
1.,0.995734176295034,1.,0.995734176295034,1.,0.995734176295034,1.,0.995734176295034,
1.,0.995734176295034,1.,0.995734176295034,1.,0.995734176295034,1.,0.995734176295034,
1.,0.995734176295034,1.,0.995734176295034,1.,0.995734176295034,1.,0.995734176295034,
1.,0.995734176295034,1.,0.995734176295034,1.,0.995734176295034,1.,0.995734176295034,
1.,0.995734176295034,1.,0.995734176295034,1.,0.995734176295034,1.,0.995734176295034,
1.,0.995734176295034,1.,0.995734176295034,1.,0.995734176295034,1.,0.995734176295034,
1.,0.995734176295034,1.,0.995734176295034,1.,0.995734176295034,1.,0.995734176295034,
1.,0.995734176295034,1.,0.995734176295034,1.,0.995734176295034,1.,0.995734176295034,
1.,0.995734176295034,1.,0.995734176295034,1.,0.995734176295034,1.,0.995734176295034,
1.,0.995734176295034,1.,0.995734176295034,1.,0.995734176295034,1.,0.995734176295034,
1.,0.995734176295034,1.,0.995734176295034,1.,0.995734176295034,1.,0.995734176295034,
1.,0.995734176295034,1.,0.995734176295034,1.,0.995734176295034,1.,0.995734176295034,
1.,0.995734176295034,1.,0.995734176295034,1.,0.995734176295034,1.,0.995734176295034,
1.,0.995734176295034,1.,0.995734176295034,1.,0.995734176295034,1.,0.995734176295034,
1.,0.995734176295034,1.,0.995734176295034,1.,0.995734176295034,1.,0.995734176295034,
1.,0.995734176295034,1.,0.995734176295034,1.,0.995734176295034,1.,0.995734176295034,
1.,0.995734176295034,1.,0.995734176295034,1.,0.995734176295034,1.,0.995734176295034,
1.,0.995734176295034,1.,0.995734176295034,1.,0.995734176295034,1.,0.995734176295034,
1.,0.995734176295034,1.,0.995734176295034,1.,0.995734176295034,1.,0.995734176295034,
1.,0.995734176295034,1.,0.995734176295034,1.,0.995734176295034,1.,0.995734176295034,
1.,0.995734176295034,1.,0.995734176295034,1.,0.995734176295034,1.,0.995734176295034,
1.,0.995734176295034,1.,0.995734176295034,1.,0.995734176295034,1.,0.995734176295034,
1.,0.995734176295034,1.,0.995734176295034,1.,0.995734176295034,1.,0.995734176295034,
1.,0.995734176295034,1.,0.995734176295034,1.,0.995734176295034,1.,0.995734176295034,
1.,0.995734176295034,1.,0.995734176295034,1.,0.995734176295034,1.,0.995734176295034,
1.,0.995734176295034,1.,0.995734176295034,1.,0.995734176295034,1.,0.995734176295034,
1.,0.995734176295034,1.,0.995734176295034,1.,0.995734176295034,1.,0.995734176295034,
1.,0.995734176295034,1.,0.995734176295034,1.,0.995734176295034,1.,0.995734176295034,
1.,0.995734176295034,1.,0.995734176295034,1.,0.995734176295034,1.,0.995734176295034,
1.,0.995734176295034,1.,0.995734176295034,1.,0.995734176295034,1.,0.995734176295034,
1.,0.995734176295034,1.,0.995734176295034,1.,0.995734176295034,1.,0.995734176295034,
1.,0.995734176295034,1.,0.995734176295034,1.,0.995734176295034,1.,0.995734176295034,
1.,0.995734176295034,1.,0.995734176295034,1.,0.995734176295034,1.,0.995734176295034,
1.,0.995734176295034,1.,0.995734176295034,1.,0.995734176295034,1.,0.995734176295034,
1.,0.995734176295034,1.,0.995734176295034,1.,0.995734176295034,1.,0.995734176295034,
1.,0.995734176295034,1.,0.995734176295034,1.,0.995734176295034,1.,0.995734176295034,
1.,0.995734176295034,1.,0.995734176295034,1.,0.995734176295034,1.,0.995734176295034,
1.,0.995734176295034,1.,0.995734176295034,1.,0.995734176295034,1.,0.995734176295034,
1.,0.995734176295034,1.,0.995734176295034,1.,0.995734176295034,1.,0.995734176295034,
1.,0.995734176295034,1.,0.995734176295034,1.,0.995734176295034,1.,0.995734176295034,
1.,0.995734176295034,1.,0.995734176295034,1.,0.995734176295034,1.,0.995734176295034,
1.,0.995734176295034,1.,0.995734176295034,1.,0.995734176295034,1.,0.995734176295034,
1.,0.995734176295034,1.,0.995734176295034,1.,0.995734176295034,1.,0.995734176295034,
1.,0.995734176295034,1.,0.995734176295034,1.,0.995734176295034,1.,0.995734176295034,
1.,0.995734176295034,1.,0.995734176295034,1.,0.995734176295034,1.,0.995734176295034,
1.,0.995734176295034,1.,0.995734176295034,1.,0.995734176295034,1.,0.995734176295034,
1.,0.995734176295034,1.,0.995734176295034,1.,0.995734176295034,1.,0.995734176295034,
1.,0.995734176295034,1.,0.995734176295034,1.,0.995734176295034,1.,0.995734176295034,
1.,0.995734176295034,1.,0.995734176295034,1.,0.995734176295034,1.,0.995734176295034,
1.,0.995734176295034,1.,0.995734176295034,1.,0.995734176295034,1.,0.995734176295034,
1.,0.995734176295034,1.,0.995734176295034,1.,0.995734176295034,1.,0.995734176295034,
1.,0.995734176295034,1.,0.995734176295034,1.,0.995734176295034,1.,0.995734176295034,
1.,0.995734176295034,1.,0.995734176295034,1.,0.995734176295034,1.,0.995734176295034,
1.,0.995734176295034,1.,0.995734176295034,1.,0.995734176295034,1.,0.995734176295034,
1.,0.995734176295034,1.,0.995734176295034,1.,0.995734176295034,1.,0.995734176295034,
1.,0.995734176295034,1.,0.995734176295034,1.,0.995734176295034,1.,0.995734176295034,
1.,0.995734176295034,1.,0.995734176295034,1.,0.995734176295034,1.,0.995734176295034,
1.,0.995734176295034,1.,0.995734176295034,1.,0.995734176295034,1.,0.995734176295034,
1.,0.995734176295034,1.,0.995734176295034,1.,0.995734176295034,1.,0.995734176295034,
1.,0.995734176295034,1.,0.995734176295034,1.,0.995734176295034,1.,0.995734176295034,
1.,0.995734176295034,1.,0.995734176295034,1.,0.995734176295034,1.,0.995734176295034,
1.,0.995734176295034,1.,0.995734176295034,1.,0.995734176295034,1.,0.995734176295034,
1.,0.995734176295034,1.,0.995734176295034,1.,0.995734176295034,1.,0.995734176295034,
1.,0.995734176295034,1.,0.995734176295034,1.,0.995734176295034,1.,0.995734176295034,
1.,0.995734176295034,1.,0.995734176295034,1.,0.995734176295034,1.,0.995734176295034,
1.,0.995734176295034,1.,0.995734176295034,1.,0.995734176295034,1.,0.995734176295034,
1.,0.995734176295034,1.,0.995734176295034,1.,0.995734176295034,1.,0.995734176295034,
1.,0.995734176295034,1.,0.995734176295034,1.,0.995734176295034,1.,0.995734176295034,
1.,0.995734176295034,1.,0.995734176295034,1.,0.995734176295034,1.,0.995734176295034,
1.,0.995734176295034,1.,0.995734176295034,1.,0.995734176295034,1.,0.995734176295034,
1.,0.995734176295034,1.,0.995734176295034,1.,0.995734176295034,1.,0.995734176295034,
1.,0.995734176295034,1.,0.995734176295034,1.,0.995734176295034,1.,0.995734176295034,
1.,0.995734176295034,1.,0.995734176295034,1.,0.995734176295034,1.,0.995734176295034,
1.,0.995734176295034,1.,0.995734176295034,1.,0.995734176295034,1.,0.995734176295034,
1.,0.995734176295034,1.,0.995734176295034,1.,0.995734176295034,1.,0.995734176295034,
1.,0.995734176295034,1.,0.995734176295034,1.,0.995734176295034,1.,0.995734176295034,
1.,0.995734176295034,1.,0.995734176295034,1.,0.995734176295034,1.,0.995734176295034,
1.,0.995734176295034,1.,0.995734176295034,1.,0.995734176295034,1.,0.995734176295034,
1.,0.995734176295034,1.,0.995734176295034,1.,0.995734176295034,1.,0.995734176295034,
1.,0.995734176295034,1.,0.995734176295034,1.,0.995734176295034,1.,0.995734176295034,
1.,0.995734176295034,1.,0.995734176295034,1.,0.995734176295034,1.,0.995734176295034,
1.,0.995734176295034,1.,0.995734176295034,1.,0.995734176295034,1.,0.995734176295034,
1.,0.995734176295034,1.,0.995734176295034,1.,0.995734176295034,1.,0.995734176295034,
1.,0.995734176295034,1.,0.995734176295034,1.,0.995734176295034,1.,0.995734176295034,
1.,0.995734176295034,1.,0.995734176295034,1.,0.995734176295034,1.,0.995734176295034,
1.,0.995734176295034,1.,0.995734176295034,1.,0.995734176295034,1.,0.995734176295034,
1.,0.995734176295034,1.,0.995734176295034,1.,0.995734176295034,1.,0.995734176295034,
1.,0.995734176295034,1.,0.995734176295034,1.,0.995734176295034,1.,0.995734176295034,
1.,0.995734176295034,1.,0.995734176295034,1.,0.995734176295034,1.,0.995734176295034,
1.,0.995734176295034,1.,0.995734176295034,1.,0.995734176295034,1.,0.995734176295034,
1.,0.995734176295034,1.,0.995734176295034,1.,0.995734176295034,1.,0.995734176295034,
1.,0.995734176295034,1.,0.995734176295034,1.,0.995734176295034,1.,0.995734176295034,
1.,0.995734176295034,1.,0.995734176295034,1.,0.995734176295034,1.,0.995734176295034,
1.,0.995734176295034,1.,0.995734176295034,1.,0.995734176295034,1.,0.995734176295034,
1.,0.995734176295034,1.,0.995734176295034,1.,0.995734176295034,1.,0.995734176295034,
1.,0.995734176295034,1.,0.995734176295034,1.,0.995734176295034,1.,0.995734176295034,
1.,0.995734176295034,1.,0.995734176295034,1.,0.995734176295034,1.,0.995734176295034,
1.,0.995734176295034,1.,0.995734176295034,1.,0.995734176295034,1.,0.995734176295034,
1.,0.995734176295034,1.,0.995734176295034,1.,0.995734176295034,1.,0.995734176295034,
1.,0.995734176295034,1.,0.995734176295034,1.,0.995734176295034,1.,0.995734176295034,
1.,0.995734176295034,1.,0.995734176295034,1.,0.995734176295034,1.,0.995734176295034,
1.,0.995734176295034,1.,0.995734176295034,1.,0.995734176295034,1.,0.995734176295034,
1.,0.995734176295034,1.,0.995734176295034,1.,0.995734176295034,1.,0.995734176295034,
1.,0.995734176295034,1.,0.995734176295034,1.,0.995734176295034,1.,0.995734176295034,
1.,0.995734176295034,1.,0.995734176295034,1.,0.995734176295034,1.,0.995734176295034,
1.,0.995734176295034,1.,0.995734176295034,1.,0.995734176295034,1.,0.995734176295034,
1.,0.995734176295034,1.,0.995734176295034,1.,0.995734176295034,1.,0.995734176295034,
1.,0.995734176295034,1.,0.995734176295034,1.,0.995734176295034,1.,0.995734176295034,
1.,0.995734176295034,1.,0.995734176295034,1.,0.995734176295034,1.,0.995734176295034,
1.,0.995734176295034,1.,0.995734176295034,1.,0.995734176295034,1.,0.995734176295034,
1.,0.995734176295034,1.,0.995734176295034,1.,0.995734176295034,1.,0.995734176295034,
1.,0.995734176295034,1.,0.995734176295034,1.,0.995734176295034,1.,0.995734176295034,
1.,0.995734176295034,1.,0.995734176295034,1.,0.995734176295034,1.,0.995734176295034,
1.,0.995734176295034,1.,0.995734176295034,1.,0.995734176295034,1.,0.995734176295034,
1.,0.995734176295034,1.,0.995734176295034,1.,0.995734176295034,1.,0.995734176295034,
1.,0.995734176295034,1.,0.995734176295034,1.,0.995734176295034,1.,0.995734176295034,
1.,0.995734176295034,1.,0.995734176295034,1.,0.995734176295034,1.,0.995734176295034,
1.,0.995734176295034,1.,0.995734176295034,1.,0.995734176295034,1.,0.995734176295034,
1.,0.995734176295034,1.,0.995734176295034,1.,0.995734176295034,1.,0.995734176295034,
1.,0.995734176295034,1.,0.995734176295034,1.,0.995734176295034,1.,0.995734176295034,
1.,0.995734176295034,1.,0.995734176295034,1.,0.995734176295034,1.,0.995734176295034,
1.,0.995734176295034,1.,0.995734176295034,1.,0.995734176295034,1.,0.995734176295034,
1.,0.995734176295034,1.,0.995734176295034,1.,0.995734176295034,1.,0.995734176295034,
1.,0.995734176295034,1.,0.995734176295034,1.,0.995734176295034,1.,0.995734176295034,
1.,0.995734176295034,1.,0.995734176295034,1.,0.995734176295034,1.,0.995734176295034,
1.,0.995734176295034,1.,0.995734176295034,1.,0.995734176295034,1.,0.995734176295034,
1.,0.995734176295034,1.,0.995734176295034,1.,0.995734176295034,1.,0.995734176295034,
1.,0.995734176295034,1.,0.995734176295034,1.,0.995734176295034,1.,0.995734176295034,
1.,0.995734176295034,1.,0.995734176295034,1.,0.995734176295034,1.,0.995734176295034,
1.,0.995734176295034,1.,0.995734176295034,1.,0.995734176295034,1.,0.995734176295034,
1.,0.995734176295034,1.,0.995734176295034,1.,0.995734176295034,1.,0.995734176295034,
1.,0.995734176295034,1.,0.995734176295034,1.,0.995734176295034,1.,0.995734176295034,
1.,0.995734176295034,1.,0.995734176295034,1.,0.995734176295034,1.,0.995734176295034,
1.,0.995734176295034,1.,0.995734176295034,1.,0.995734176295034,1.,0.995734176295034,
1.,0.995734176295034,1.,0.995734176295034,1.,0.995734176295034,1.,0.995734176295034,
1.,0.995734176295034,1.,0.995734176295034,1.,0.995734176295034,1.,0.995734176295034,
1.,0.995734176295034,1.,0.995734176295034,1.,0.995734176295034,1.,0.995734176295034,
1.,0.995734176295034,1.,0.995734176295034,1.,0.995734176295034,1.,0.995734176295034,
1.,0.995734176295034,1.,0.995734176295034,1.,0.995734176295034,1.,0.995734176295034,
1.,0.995734176295034,1.,0.995734176295034,1.,0.995734176295034,1.,0.995734176295034,
1.,0.995734176295034,1.,0.995734176295034,1.,0.995734176295034,1.,0.995734176295034,
1.,0.995734176295034,1.,0.995734176295034,1.,0.995734176295034,1.,0.995734176295034,
1.,0.995734176295034,1.,0.995734176295034,1.,0.995734176295034,1.,0.995734176295034,
1.,0.995734176295034,1.,0.995734176295034,1.,0.995734176295034,1.,0.995734176295034,
1.,0.995734176295034,1.,0.995734176295034,1.,0.995734176295034,1.,0.995734176295034,
1.,0.995734176295034,1.,0.995734176295034,1.,0.995734176295034,1.,0.995734176295034,
1.,0.995734176295034,1.,0.995734176295034,1.,0.995734176295034,1.,0.995734176295034,
1.,0.995734176295034,1.,0.995734176295034,1.,0.995734176295034,1.,0.995734176295034,
1.,0.995734176295034,1.,0.995734176295034,1.,0.995734176295034,1.,0.995734176295034,
1.,0.995734176295034,1.,0.995734176295034,1.,0.995734176295034,1.,0.995734176295034,
1.,0.995734176295034,1.,0.995734176295034,1.,0.995734176295034,1.,0.995734176295034,
1.,0.995734176295034,1.,0.995734176295034,1.,0.995734176295034,1.,0.995734176295034,
1.,0.995734176295034,1.,0.995734176295034,1.,0.995734176295034,1.,0.995734176295034,
1.,0.995734176295034,1.,0.995734176295034,1.,0.995734176295034,1.,0.995734176295034,
1.,0.995734176295034,1.,0.995734176295034,1.,0.995734176295034,1.,0.995734176295034,
1.,0.995734176295034,1.,0.995734176295034,1.,0.995734176295034,1.,0.995734176295034,
1.,0.995734176295034,1.,0.995734176295034,1.,0.995734176295034,1.,0.995734176295034,
1.,0.995734176295034,1.,0.995734176295034,1.,0.995734176295034,1.,0.995734176295034,
1.,0.995734176295034,1.,0.995734176295034,1.,0.995734176295034,1.,0.995734176295034,
1.,0.995734176295034,1.,0.995734176295034,1.,0.995734176295034,1.,0.995734176295034,
1.,0.995734176295034,1.,0.995734176295034,1.,0.995734176295034,1.,0.995734176295034,
1.,0.995734176295034,1.,0.995734176295034,1.,0.995734176295034,1.,0.995734176295034,
1.,0.995734176295034,1.,0.995734176295034,1.,0.995734176295034,1.,0.995734176295034,
1.,0.995734176295034,1.,0.995734176295034,1.,0.995734176295034,1.,0.995734176295034,
1.,0.995734176295034,1.,0.995734176295034,1.,0.995734176295034,1.,0.995734176295034,
1.,0.995734176295034,1.,0.995734176295034,1.,0.995734176295034,1.,0.995734176295034,
1.,0.995734176295034,1.,0.995734176295034,1.,0.995734176295034,1.,0.995734176295034,
1.,0.995734176295034,1.,0.995734176295034,1.,0.995734176295034,1.,0.995734176295034,
1.,0.995734176295034,1.,0.995734176295034,1.,0.995734176295034,1.,0.995734176295034,
1.,0.995734176295034,1.,0.995734176295034,1.,0.995734176295034,1.,0.995734176295034,
1.,0.995734176295034,1.,0.995734176295034,1.,0.995734176295034,1.,0.995734176295034,
1.,0.995734176295034,1.,0.995734176295034,1.,0.995734176295034,1.,0.995734176295034,
1.,0.995734176295034,1.,0.995734176295034,1.,0.995734176295034,1.,0.995734176295034,
1.,0.995734176295034,1.,0.995734176295034,1.,0.995734176295034,1.,0.995734176295034,
1.,0.995734176295034,1.,0.995734176295034,1.,0.995734176295034,1.,0.995734176295034,
1.,0.995734176295034,1.,0.995734176295034,1.,0.995734176295034,1.,0.995734176295034,
1.,0.995734176295034,1.,0.995734176295034,1.,0.995734176295034,1.,0.995734176295034,
1.,0.995734176295034,1.,0.995734176295034,1.,0.995734176295034,1.,0.995734176295034,
1.,0.995734176295034,1.,0.995734176295034,1.,0.995734176295034,1.,0.995734176295034,
1.,0.995734176295034,1.,0.995734176295034,1.,0.995734176295034,1.,0.995734176295034,
1.,0.995734176295034,1.,0.995734176295034,1.,0.995734176295034,1.,0.995734176295034,
1.,0.995734176295034,1.,0.995734176295034,1.,0.995734176295034,1.,0.995734176295034,
1.,0.995734176295034,1.,0.995734176295034,1.,0.995734176295034,1.,0.995734176295034,
1.,0.995734176295034,1.,0.995734176295034,1.,0.995734176295034,1.,0.995734176295034,
1.,0.995734176295034,1.,0.995734176295034,1.,0.995734176295034,1.,0.995734176295034,
1.,0.995734176295034,1.,0.995734176295034,1.,0.995734176295034,1.,0.995734176295034,
1.,0.995734176295034,1.,0.995734176295034,1.,0.995734176295034,1.,0.995734176295034,
1.,0.995734176295034,1.,0.995734176295034,1.,0.995734176295034,1.,0.995734176295034,
1.,0.995734176295034,1.,0.995734176295034,1.,0.995734176295034,1.,0.995734176295034,
1.,0.995734176295034,1.,0.995734176295034,1.,0.995734176295034,1.,0.995734176295034,
1.,0.995734176295034,1.,0.995734176295034,1.,0.995734176295034,1.,0.995734176295034,
1.,0.995734176295034,1.,0.995734176295034,1.,0.995734176295034,1.,0.995734176295034,
1.,0.995734176295034,1.,0.995734176295034,1.,0.995734176295034,1.,0.995734176295034,
1.,0.995734176295034,1.,0.995734176295034,1.,0.995734176295034,1.,0.995734176295034,
1.,0.995734176295034,1.,0.995734176295034,1.,0.995734176295034,1.,0.995734176295034,
1.,0.995734176295034,1.,0.995734176295034,1.,0.995734176295034,1.,0.995734176295034,
1.,0.995734176295034,1.,0.995734176295034,1.,0.995734176295034,1.,0.995734176295034,
1.,0.995734176295034,1.,0.995734176295034,1.,0.995734176295034,1.,0.995734176295034,
1.,0.995734176295034,1.,0.995734176295034,1.,0.995734176295034,1.,0.995734176295034,
1.,0.995734176295034,1.,0.995734176295034,1.,0.995734176295034,1.,0.995734176295034,
1.,0.995734176295034,1.,0.995734176295034,1.,0.995734176295034,1.,0.995734176295034,
1.,0.995734176295034,1.,0.995734176295034,1.,0.995734176295034,1.,0.995734176295034,
1.,0.995734176295034,1.,0.995734176295034,1.,0.995734176295034,1.,0.995734176295034,
1.,0.995734176295034,1.,0.995734176295034,1.,0.995734176295034,1.,0.995734176295034,
1.,0.995734176295034,1.,0.995734176295034,1.,0.995734176295034,1.,0.995734176295034,
1.,0.995734176295034,1.,0.995734176295034,1.,0.995734176295034,1.,0.995734176295034,
1.,0.995734176295034,1.,0.995734176295034,1.,0.995734176295034,1.,0.995734176295034,
1.,0.995734176295034,1.,0.995734176295034,1.,0.995734176295034,1.,0.995734176295034,
1.,0.995734176295034,1.,0.995734176295034,1.,0.995734176295034,1.,0.995734176295034,
1.,0.995734176295034,1.,0.995734176295034,1.,0.995734176295034,1.,0.995734176295034,
1.,0.995734176295034,1.,0.995734176295034,1.,0.995734176295034,1.,0.995734176295034,
1.,0.995734176295034,1.,0.995734176295034,1.,0.995734176295034,1.,0.995734176295034,
1.,0.995734176295034,1.,0.995734176295034,1.,0.995734176295034,1.,0.995734176295034,
1.,0.995734176295034,1.,0.995734176295034,1.,0.995734176295034,1.,0.995734176295034,
1.,0.995734176295034,1.,0.995734176295034,1.,0.995734176295034,1.,0.995734176295034,
1.,0.995734176295034,1.,0.995734176295034,1.,0.995734176295034,1.,0.995734176295034,
1.,0.995734176295034,1.,0.995734176295034,1.,0.99720106003931,0.998075063662495)))
REPRESENTATION_ITEM('')
SURFACE()
);
#2502=(
BOUNDED_SURFACE()
B_SPLINE_SURFACE(1,2,((#150388,#150389,#150390,#150391,#150392,#150393,
#150394,#150395,#150396,#150397,#150398,#150399,#150400,#150401,#150402,
#150403,#150404,#150405,#150406,#150407,#150408,#150409,#150410,#150411,
#150412,#150413,#150414,#150415,#150416,#150417,#150418,#150419,#150420,
#150421,#150422,#150423,#150424,#150425,#150426,#150427,#150428,#150429,
#150430,#150431,#150432,#150433,#150434,#150435,#150436,#150437,#150438,
#150439,#150440,#150441,#150442,#150443,#150444,#150445,#150446,#150447,
#150448,#150449,#150450,#150451,#150452,#150453,#150454,#150455,#150456,
#150457,#150458,#150459,#150460,#150461,#150462,#150463,#150464,#150465,
#150466,#150467,#150468,#150469,#150470,#150471,#150472,#150473,#150474,
#150475,#150476,#150477,#150478,#150479,#150480,#150481,#150482,#150483,
#150484,#150485,#150486,#150487,#150488,#150489,#150490,#150491,#150492,
#150493,#150494,#150495,#150496,#150497,#150498,#150499,#150500,#150501,
#150502,#150503,#150504,#150505,#150506,#150507,#150508,#150509,#150510,
#150511,#150512,#150513,#150514,#150515,#150516,#150517,#150518,#150519,
#150520,#150521,#150522,#150523,#150524,#150525,#150526,#150527,#150528,
#150529,#150530,#150531,#150532,#150533,#150534,#150535,#150536,#150537,
#150538,#150539,#150540,#150541,#150542,#150543,#150544,#150545,#150546,
#150547,#150548,#150549,#150550,#150551,#150552,#150553,#150554,#150555,
#150556,#150557,#150558,#150559,#150560,#150561,#150562,#150563,#150564,
#150565,#150566,#150567,#150568,#150569,#150570,#150571,#150572,#150573,
#150574,#150575,#150576,#150577,#150578,#150579,#150580,#150581,#150582,
#150583,#150584,#150585,#150586,#150587,#150588,#150589,#150590,#150591,
#150592,#150593,#150594,#150595,#150596,#150597,#150598,#150599,#150600,
#150601,#150602,#150603,#150604,#150605,#150606,#150607,#150608,#150609,
#150610,#150611,#150612,#150613,#150614,#150615,#150616,#150617,#150618,
#150619,#150620,#150621,#150622,#150623,#150624,#150625,#150626,#150627,
#150628,#150629,#150630,#150631,#150632,#150633,#150634,#150635,#150636,
#150637,#150638,#150639,#150640,#150641,#150642,#150643,#150644,#150645,
#150646,#150647,#150648,#150649,#150650,#150651,#150652,#150653,#150654,
#150655,#150656,#150657,#150658,#150659,#150660,#150661,#150662,#150663,
#150664,#150665,#150666,#150667,#150668,#150669,#150670,#150671,#150672,
#150673,#150674,#150675,#150676,#150677,#150678,#150679,#150680,#150681,
#150682,#150683,#150684,#150685,#150686,#150687,#150688,#150689,#150690,
#150691,#150692,#150693,#150694,#150695,#150696,#150697,#150698,#150699,
#150700,#150701,#150702,#150703,#150704,#150705,#150706,#150707,#150708,
#150709,#150710,#150711,#150712,#150713,#150714,#150715,#150716,#150717,
#150718,#150719,#150720,#150721,#150722,#150723,#150724,#150725,#150726,
#150727,#150728,#150729,#150730,#150731,#150732,#150733,#150734,#150735,
#150736,#150737,#150738,#150739,#150740,#150741,#150742,#150743,#150744,
#150745,#150746,#150747,#150748,#150749,#150750,#150751,#150752,#150753,
#150754,#150755,#150756,#150757,#150758,#150759,#150760,#150761,#150762,
#150763,#150764,#150765,#150766,#150767,#150768,#150769,#150770,#150771,
#150772,#150773,#150774,#150775,#150776,#150777,#150778,#150779,#150780,
#150781,#150782,#150783,#150784,#150785,#150786,#150787,#150788,#150789,
#150790,#150791,#150792,#150793,#150794,#150795,#150796,#150797,#150798,
#150799,#150800,#150801,#150802,#150803,#150804,#150805,#150806,#150807,
#150808,#150809,#150810,#150811,#150812,#150813,#150814,#150815,#150816,
#150817,#150818,#150819,#150820,#150821,#150822,#150823,#150824,#150825,
#150826,#150827,#150828,#150829,#150830,#150831,#150832,#150833,#150834,
#150835,#150836,#150837,#150838,#150839,#150840,#150841,#150842,#150843,
#150844,#150845,#150846,#150847,#150848,#150849,#150850,#150851,#150852,
#150853,#150854,#150855,#150856,#150857,#150858,#150859,#150860,#150861,
#150862,#150863,#150864,#150865,#150866,#150867,#150868,#150869,#150870,
#150871,#150872,#150873,#150874,#150875,#150876,#150877,#150878,#150879,
#150880,#150881,#150882,#150883,#150884,#150885,#150886,#150887,#150888,
#150889,#150890,#150891,#150892,#150893,#150894,#150895,#150896,#150897,
#150898,#150899,#150900,#150901,#150902,#150903,#150904,#150905,#150906,
#150907,#150908,#150909,#150910,#150911,#150912,#150913,#150914,#150915,
#150916,#150917,#150918,#150919,#150920,#150921,#150922,#150923,#150924,
#150925,#150926,#150927,#150928,#150929,#150930,#150931,#150932,#150933,
#150934,#150935,#150936,#150937,#150938,#150939,#150940,#150941,#150942,
#150943,#150944,#150945,#150946,#150947,#150948,#150949,#150950,#150951,
#150952,#150953,#150954,#150955,#150956,#150957,#150958,#150959,#150960,
#150961,#150962,#150963,#150964,#150965,#150966,#150967,#150968,#150969,
#150970,#150971,#150972,#150973,#150974,#150975,#150976,#150977,#150978,
#150979,#150980,#150981,#150982,#150983,#150984,#150985,#150986,#150987,
#150988,#150989,#150990,#150991,#150992,#150993,#150994,#150995,#150996,
#150997,#150998,#150999,#151000,#151001,#151002,#151003,#151004,#151005,
#151006,#151007,#151008,#151009,#151010,#151011,#151012,#151013,#151014,
#151015,#151016,#151017,#151018,#151019,#151020,#151021,#151022,#151023,
#151024,#151025,#151026,#151027,#151028,#151029,#151030,#151031,#151032,
#151033,#151034,#151035,#151036,#151037,#151038,#151039,#151040,#151041,
#151042,#151043,#151044,#151045,#151046,#151047,#151048,#151049,#151050,
#151051,#151052,#151053,#151054,#151055,#151056,#151057,#151058,#151059,
#151060,#151061,#151062,#151063,#151064,#151065,#151066,#151067,#151068,
#151069,#151070,#151071,#151072,#151073,#151074,#151075,#151076,#151077,
#151078,#151079,#151080,#151081,#151082,#151083,#151084,#151085,#151086,
#151087,#151088,#151089,#151090,#151091,#151092,#151093,#151094,#151095,
#151096,#151097,#151098,#151099,#151100,#151101,#151102,#151103,#151104,
#151105,#151106,#151107,#151108,#151109,#151110,#151111,#151112,#151113,
#151114,#151115,#151116,#151117,#151118,#151119,#151120,#151121,#151122,
#151123,#151124,#151125,#151126,#151127,#151128,#151129,#151130,#151131,
#151132,#151133,#151134,#151135,#151136,#151137,#151138,#151139,#151140,
#151141,#151142,#151143,#151144,#151145,#151146,#151147,#151148,#151149,
#151150,#151151,#151152,#151153,#151154,#151155,#151156,#151157,#151158,
#151159,#151160,#151161,#151162,#151163,#151164,#151165,#151166,#151167,
#151168,#151169,#151170,#151171,#151172,#151173,#151174,#151175,#151176,
#151177,#151178,#151179,#151180,#151181,#151182,#151183,#151184,#151185,
#151186,#151187,#151188,#151189,#151190,#151191,#151192,#151193,#151194,
#151195,#151196,#151197,#151198,#151199,#151200,#151201,#151202,#151203,
#151204,#151205,#151206,#151207,#151208,#151209,#151210,#151211,#151212,
#151213,#151214,#151215,#151216,#151217,#151218,#151219,#151220,#151221,
#151222,#151223,#151224,#151225,#151226,#151227,#151228,#151229,#151230,
#151231,#151232,#151233,#151234,#151235,#151236,#151237,#151238,#151239,
#151240,#151241,#151242,#151243,#151244,#151245,#151246,#151247,#151248,
#151249,#151250,#151251,#151252,#151253,#151254,#151255,#151256,#151257,
#151258,#151259,#151260,#151261,#151262,#151263,#151264,#151265,#151266,
#151267,#151268,#151269,#151270,#151271,#151272,#151273,#151274,#151275,
#151276,#151277,#151278,#151279,#151280,#151281,#151282,#151283,#151284,
#151285,#151286,#151287,#151288,#151289,#151290,#151291,#151292,#151293,
#151294,#151295,#151296,#151297,#151298,#151299,#151300,#151301,#151302,
#151303,#151304,#151305,#151306,#151307,#151308,#151309,#151310,#151311,
#151312,#151313,#151314,#151315,#151316,#151317,#151318,#151319,#151320,
#151321,#151322,#151323,#151324,#151325,#151326,#151327,#151328,#151329,
#151330,#151331,#151332,#151333,#151334,#151335,#151336,#151337,#151338,
#151339,#151340,#151341,#151342,#151343,#151344,#151345,#151346,#151347,
#151348,#151349,#151350,#151351,#151352,#151353,#151354,#151355,#151356,
#151357,#151358,#151359,#151360,#151361,#151362,#151363,#151364,#151365,
#151366,#151367,#151368,#151369,#151370,#151371,#151372,#151373,#151374,
#151375,#151376,#151377,#151378,#151379,#151380,#151381,#151382,#151383,
#151384,#151385,#151386,#151387,#151388,#151389,#151390,#151391,#151392,
#151393,#151394,#151395,#151396,#151397,#151398,#151399,#151400,#151401,
#151402,#151403,#151404,#151405,#151406,#151407,#151408,#151409,#151410,
#151411,#151412,#151413,#151414,#151415,#151416,#151417,#151418,#151419,
#151420,#151421,#151422,#151423,#151424,#151425,#151426,#151427,#151428,
#151429,#151430,#151431,#151432,#151433,#151434,#151435,#151436,#151437,
#151438,#151439,#151440,#151441,#151442,#151443,#151444,#151445,#151446,
#151447,#151448,#151449,#151450,#151451,#151452,#151453,#151454,#151455,
#151456,#151457,#151458,#151459,#151460,#151461,#151462,#151463,#151464,
#151465,#151466,#151467,#151468,#151469,#151470,#151471,#151472,#151473,
#151474,#151475,#151476,#151477,#151478,#151479,#151480,#151481,#151482,
#151483,#151484,#151485,#151486,#151487,#151488,#151489,#151490,#151491,
#151492,#151493,#151494,#151495,#151496,#151497,#151498,#151499,#151500,
#151501,#151502,#151503,#151504,#151505,#151506,#151507,#151508,#151509,
#151510,#151511,#151512,#151513,#151514,#151515,#151516,#151517,#151518,
#151519,#151520,#151521,#151522,#151523,#151524,#151525,#151526,#151527,
#151528,#151529,#151530,#151531,#151532,#151533,#151534,#151535,#151536,
#151537,#151538,#151539,#151540,#151541,#151542,#151543,#151544,#151545,
#151546,#151547,#151548,#151549,#151550,#151551,#151552,#151553,#151554,
#151555,#151556,#151557,#151558,#151559,#151560,#151561,#151562,#151563,
#151564,#151565,#151566,#151567,#151568,#151569,#151570,#151571,#151572,
#151573,#151574,#151575,#151576,#151577,#151578,#151579,#151580,#151581,
#151582,#151583,#151584,#151585,#151586,#151587,#151588,#151589,#151590,
#151591,#151592,#151593,#151594,#151595,#151596,#151597,#151598,#151599,
#151600,#151601,#151602,#151603,#151604,#151605,#151606,#151607,#151608,
#151609,#151610,#151611,#151612,#151613,#151614,#151615,#151616,#151617,
#151618,#151619,#151620,#151621,#151622,#151623,#151624,#151625,#151626,
#151627,#151628,#151629,#151630,#151631,#151632,#151633,#151634,#151635,
#151636,#151637,#151638,#151639,#151640,#151641,#151642,#151643,#151644,
#151645,#151646,#151647,#151648,#151649,#151650,#151651,#151652,#151653,
#151654,#151655,#151656,#151657,#151658,#151659,#151660,#151661,#151662,
#151663,#151664,#151665,#151666,#151667,#151668,#151669,#151670,#151671,
#151672,#151673,#151674,#151675,#151676,#151677,#151678,#151679,#151680,
#151681,#151682,#151683,#151684,#151685,#151686,#151687,#151688,#151689,
#151690,#151691,#151692,#151693,#151694,#151695,#151696,#151697,#151698,
#151699,#151700,#151701,#151702,#151703,#151704,#151705,#151706,#151707,
#151708,#151709,#151710,#151711,#151712,#151713,#151714,#151715,#151716,
#151717,#151718,#151719,#151720,#151721,#151722,#151723,#151724,#151725,
#151726,#151727,#151728,#151729,#151730,#151731,#151732,#151733,#151734,
#151735,#151736,#151737,#151738,#151739,#151740,#151741,#151742,#151743,
#151744,#151745,#151746,#151747,#151748,#151749,#151750,#151751,#151752,
#151753,#151754,#151755,#151756,#151757,#151758,#151759,#151760,#151761,
#151762,#151763,#151764,#151765,#151766,#151767,#151768,#151769,#151770,
#151771,#151772,#151773,#151774,#151775,#151776,#151777,#151778,#151779,
#151780,#151781,#151782,#151783,#151784,#151785,#151786,#151787,#151788,
#151789,#151790,#151791,#151792,#151793,#151794,#151795,#151796,#151797,
#151798,#151799,#151800,#151801,#151802,#151803,#151804,#151805,#151806,
#151807,#151808,#151809,#151810,#151811,#151812,#151813,#151814,#151815,
#151816,#151817,#151818,#151819,#151820,#151821,#151822,#151823,#151824,
#151825,#151826,#151827,#151828,#151829,#151830,#151831,#151832,#151833,
#151834,#151835,#151836,#151837,#151838,#151839,#151840,#151841,#151842,
#151843,#151844,#151845,#151846,#151847,#151848,#151849,#151850,#151851,
#151852,#151853,#151854,#151855,#151856,#151857,#151858,#151859,#151860,
#151861,#151862,#151863,#151864,#151865,#151866,#151867,#151868,#151869,
#151870,#151871,#151872,#151873,#151874,#151875,#151876,#151877,#151878,
#151879,#151880,#151881,#151882,#151883,#151884,#151885,#151886,#151887,
#151888,#151889,#151890,#151891,#151892,#151893,#151894,#151895,#151896,
#151897,#151898,#151899,#151900,#151901,#151902,#151903,#151904,#151905,
#151906,#151907,#151908,#151909,#151910,#151911,#151912,#151913,#151914,
#151915,#151916,#151917,#151918,#151919,#151920,#151921,#151922,#151923,
#151924,#151925,#151926,#151927,#151928,#151929,#151930,#151931,#151932,
#151933,#151934,#151935,#151936,#151937,#151938,#151939,#151940,#151941,
#151942,#151943,#151944,#151945,#151946,#151947,#151948,#151949,#151950,
#151951,#151952,#151953,#151954,#151955,#151956,#151957,#151958,#151959,
#151960,#151961,#151962,#151963,#151964,#151965,#151966,#151967,#151968,
#151969,#151970,#151971,#151972,#151973,#151974,#151975,#151976,#151977,
#151978,#151979,#151980,#151981,#151982,#151983,#151984,#151985,#151986,
#151987,#151988,#151989,#151990,#151991,#151992,#151993,#151994,#151995,
#151996,#151997,#151998,#151999,#152000,#152001,#152002,#152003,#152004,
#152005,#152006,#152007,#152008,#152009,#152010,#152011,#152012,#152013,
#152014,#152015,#152016,#152017,#152018,#152019,#152020,#152021,#152022,
#152023,#152024,#152025,#152026,#152027,#152028,#152029,#152030,#152031,
#152032,#152033,#152034,#152035,#152036,#152037,#152038,#152039,#152040,
#152041,#152042,#152043,#152044,#152045,#152046,#152047,#152048,#152049,
#152050,#152051,#152052,#152053,#152054,#152055,#152056,#152057,#152058,
#152059,#152060,#152061,#152062,#152063,#152064,#152065,#152066,#152067,
#152068,#152069,#152070,#152071,#152072,#152073,#152074,#152075,#152076,
#152077,#152078,#152079,#152080,#152081,#152082,#152083,#152084,#152085,
#152086,#152087,#152088,#152089,#152090,#152091,#152092,#152093,#152094,
#152095,#152096,#152097,#152098,#152099,#152100,#152101,#152102,#152103,
#152104,#152105,#152106,#152107,#152108,#152109,#152110,#152111,#152112,
#152113,#152114,#152115,#152116,#152117,#152118,#152119,#152120,#152121,
#152122,#152123,#152124,#152125,#152126,#152127,#152128,#152129,#152130,
#152131,#152132,#152133,#152134,#152135,#152136,#152137,#152138,#152139,
#152140,#152141,#152142,#152143,#152144,#152145,#152146,#152147,#152148,
#152149,#152150,#152151,#152152,#152153,#152154,#152155,#152156,#152157,
#152158,#152159,#152160,#152161,#152162,#152163,#152164,#152165,#152166,
#152167,#152168,#152169,#152170,#152171,#152172,#152173,#152174,#152175,
#152176,#152177,#152178,#152179,#152180,#152181,#152182,#152183,#152184,
#152185,#152186,#152187,#152188,#152189,#152190,#152191,#152192,#152193,
#152194,#152195,#152196,#152197,#152198,#152199,#152200,#152201,#152202,
#152203,#152204,#152205,#152206,#152207,#152208,#152209,#152210,#152211,
#152212,#152213,#152214,#152215,#152216,#152217,#152218,#152219,#152220,
#152221,#152222,#152223,#152224,#152225,#152226,#152227,#152228,#152229,
#152230,#152231,#152232,#152233,#152234,#152235,#152236,#152237,#152238,
#152239,#152240,#152241,#152242,#152243,#152244,#152245,#152246,#152247,
#152248,#152249,#152250,#152251,#152252,#152253,#152254,#152255,#152256,
#152257,#152258,#152259,#152260,#152261,#152262,#152263,#152264,#152265,
#152266,#152267,#152268,#152269,#152270,#152271,#152272,#152273,#152274,
#152275,#152276,#152277,#152278,#152279,#152280,#152281,#152282,#152283,
#152284,#152285,#152286,#152287,#152288,#152289,#152290,#152291,#152292,
#152293,#152294,#152295,#152296,#152297,#152298,#152299,#152300,#152301,
#152302,#152303,#152304,#152305,#152306,#152307,#152308,#152309,#152310,
#152311,#152312,#152313,#152314,#152315,#152316,#152317,#152318,#152319,
#152320,#152321,#152322,#152323,#152324,#152325,#152326,#152327,#152328,
#152329,#152330,#152331,#152332,#152333,#152334,#152335,#152336,#152337,
#152338,#152339,#152340,#152341,#152342,#152343,#152344,#152345,#152346,
#152347,#152348,#152349,#152350,#152351,#152352,#152353,#152354,#152355,
#152356,#152357,#152358,#152359,#152360,#152361,#152362,#152363,#152364,
#152365,#152366,#152367,#152368,#152369,#152370,#152371,#152372,#152373,
#152374,#152375,#152376,#152377,#152378,#152379,#152380,#152381,#152382,
#152383,#152384,#152385,#152386,#152387,#152388,#152389,#152390,#152391,
#152392,#152393,#152394,#152395,#152396,#152397,#152398,#152399,#152400),
(#152401,#152402,#152403,#152404,#152405,#152406,#152407,#152408,#152409,
#152410,#152411,#152412,#152413,#152414,#152415,#152416,#152417,#152418,
#152419,#152420,#152421,#152422,#152423,#152424,#152425,#152426,#152427,
#152428,#152429,#152430,#152431,#152432,#152433,#152434,#152435,#152436,
#152437,#152438,#152439,#152440,#152441,#152442,#152443,#152444,#152445,
#152446,#152447,#152448,#152449,#152450,#152451,#152452,#152453,#152454,
#152455,#152456,#152457,#152458,#152459,#152460,#152461,#152462,#152463,
#152464,#152465,#152466,#152467,#152468,#152469,#152470,#152471,#152472,
#152473,#152474,#152475,#152476,#152477,#152478,#152479,#152480,#152481,
#152482,#152483,#152484,#152485,#152486,#152487,#152488,#152489,#152490,
#152491,#152492,#152493,#152494,#152495,#152496,#152497,#152498,#152499,
#152500,#152501,#152502,#152503,#152504,#152505,#152506,#152507,#152508,
#152509,#152510,#152511,#152512,#152513,#152514,#152515,#152516,#152517,
#152518,#152519,#152520,#152521,#152522,#152523,#152524,#152525,#152526,
#152527,#152528,#152529,#152530,#152531,#152532,#152533,#152534,#152535,
#152536,#152537,#152538,#152539,#152540,#152541,#152542,#152543,#152544,
#152545,#152546,#152547,#152548,#152549,#152550,#152551,#152552,#152553,
#152554,#152555,#152556,#152557,#152558,#152559,#152560,#152561,#152562,
#152563,#152564,#152565,#152566,#152567,#152568,#152569,#152570,#152571,
#152572,#152573,#152574,#152575,#152576,#152577,#152578,#152579,#152580,
#152581,#152582,#152583,#152584,#152585,#152586,#152587,#152588,#152589,
#152590,#152591,#152592,#152593,#152594,#152595,#152596,#152597,#152598,
#152599,#152600,#152601,#152602,#152603,#152604,#152605,#152606,#152607,
#152608,#152609,#152610,#152611,#152612,#152613,#152614,#152615,#152616,
#152617,#152618,#152619,#152620,#152621,#152622,#152623,#152624,#152625,
#152626,#152627,#152628,#152629,#152630,#152631,#152632,#152633,#152634,
#152635,#152636,#152637,#152638,#152639,#152640,#152641,#152642,#152643,
#152644,#152645,#152646,#152647,#152648,#152649,#152650,#152651,#152652,
#152653,#152654,#152655,#152656,#152657,#152658,#152659,#152660,#152661,
#152662,#152663,#152664,#152665,#152666,#152667,#152668,#152669,#152670,
#152671,#152672,#152673,#152674,#152675,#152676,#152677,#152678,#152679,
#152680,#152681,#152682,#152683,#152684,#152685,#152686,#152687,#152688,
#152689,#152690,#152691,#152692,#152693,#152694,#152695,#152696,#152697,
#152698,#152699,#152700,#152701,#152702,#152703,#152704,#152705,#152706,
#152707,#152708,#152709,#152710,#152711,#152712,#152713,#152714,#152715,
#152716,#152717,#152718,#152719,#152720,#152721,#152722,#152723,#152724,
#152725,#152726,#152727,#152728,#152729,#152730,#152731,#152732,#152733,
#152734,#152735,#152736,#152737,#152738,#152739,#152740,#152741,#152742,
#152743,#152744,#152745,#152746,#152747,#152748,#152749,#152750,#152751,
#152752,#152753,#152754,#152755,#152756,#152757,#152758,#152759,#152760,
#152761,#152762,#152763,#152764,#152765,#152766,#152767,#152768,#152769,
#152770,#152771,#152772,#152773,#152774,#152775,#152776,#152777,#152778,
#152779,#152780,#152781,#152782,#152783,#152784,#152785,#152786,#152787,
#152788,#152789,#152790,#152791,#152792,#152793,#152794,#152795,#152796,
#152797,#152798,#152799,#152800,#152801,#152802,#152803,#152804,#152805,
#152806,#152807,#152808,#152809,#152810,#152811,#152812,#152813,#152814,
#152815,#152816,#152817,#152818,#152819,#152820,#152821,#152822,#152823,
#152824,#152825,#152826,#152827,#152828,#152829,#152830,#152831,#152832,
#152833,#152834,#152835,#152836,#152837,#152838,#152839,#152840,#152841,
#152842,#152843,#152844,#152845,#152846,#152847,#152848,#152849,#152850,
#152851,#152852,#152853,#152854,#152855,#152856,#152857,#152858,#152859,
#152860,#152861,#152862,#152863,#152864,#152865,#152866,#152867,#152868,
#152869,#152870,#152871,#152872,#152873,#152874,#152875,#152876,#152877,
#152878,#152879,#152880,#152881,#152882,#152883,#152884,#152885,#152886,
#152887,#152888,#152889,#152890,#152891,#152892,#152893,#152894,#152895,
#152896,#152897,#152898,#152899,#152900,#152901,#152902,#152903,#152904,
#152905,#152906,#152907,#152908,#152909,#152910,#152911,#152912,#152913,
#152914,#152915,#152916,#152917,#152918,#152919,#152920,#152921,#152922,
#152923,#152924,#152925,#152926,#152927,#152928,#152929,#152930,#152931,
#152932,#152933,#152934,#152935,#152936,#152937,#152938,#152939,#152940,
#152941,#152942,#152943,#152944,#152945,#152946,#152947,#152948,#152949,
#152950,#152951,#152952,#152953,#152954,#152955,#152956,#152957,#152958,
#152959,#152960,#152961,#152962,#152963,#152964,#152965,#152966,#152967,
#152968,#152969,#152970,#152971,#152972,#152973,#152974,#152975,#152976,
#152977,#152978,#152979,#152980,#152981,#152982,#152983,#152984,#152985,
#152986,#152987,#152988,#152989,#152990,#152991,#152992,#152993,#152994,
#152995,#152996,#152997,#152998,#152999,#153000,#153001,#153002,#153003,
#153004,#153005,#153006,#153007,#153008,#153009,#153010,#153011,#153012,
#153013,#153014,#153015,#153016,#153017,#153018,#153019,#153020,#153021,
#153022,#153023,#153024,#153025,#153026,#153027,#153028,#153029,#153030,
#153031,#153032,#153033,#153034,#153035,#153036,#153037,#153038,#153039,
#153040,#153041,#153042,#153043,#153044,#153045,#153046,#153047,#153048,
#153049,#153050,#153051,#153052,#153053,#153054,#153055,#153056,#153057,
#153058,#153059,#153060,#153061,#153062,#153063,#153064,#153065,#153066,
#153067,#153068,#153069,#153070,#153071,#153072,#153073,#153074,#153075,
#153076,#153077,#153078,#153079,#153080,#153081,#153082,#153083,#153084,
#153085,#153086,#153087,#153088,#153089,#153090,#153091,#153092,#153093,
#153094,#153095,#153096,#153097,#153098,#153099,#153100,#153101,#153102,
#153103,#153104,#153105,#153106,#153107,#153108,#153109,#153110,#153111,
#153112,#153113,#153114,#153115,#153116,#153117,#153118,#153119,#153120,
#153121,#153122,#153123,#153124,#153125,#153126,#153127,#153128,#153129,
#153130,#153131,#153132,#153133,#153134,#153135,#153136,#153137,#153138,
#153139,#153140,#153141,#153142,#153143,#153144,#153145,#153146,#153147,
#153148,#153149,#153150,#153151,#153152,#153153,#153154,#153155,#153156,
#153157,#153158,#153159,#153160,#153161,#153162,#153163,#153164,#153165,
#153166,#153167,#153168,#153169,#153170,#153171,#153172,#153173,#153174,
#153175,#153176,#153177,#153178,#153179,#153180,#153181,#153182,#153183,
#153184,#153185,#153186,#153187,#153188,#153189,#153190,#153191,#153192,
#153193,#153194,#153195,#153196,#153197,#153198,#153199,#153200,#153201,
#153202,#153203,#153204,#153205,#153206,#153207,#153208,#153209,#153210,
#153211,#153212,#153213,#153214,#153215,#153216,#153217,#153218,#153219,
#153220,#153221,#153222,#153223,#153224,#153225,#153226,#153227,#153228,
#153229,#153230,#153231,#153232,#153233,#153234,#153235,#153236,#153237,
#153238,#153239,#153240,#153241,#153242,#153243,#153244,#153245,#153246,
#153247,#153248,#153249,#153250,#153251,#153252,#153253,#153254,#153255,
#153256,#153257,#153258,#153259,#153260,#153261,#153262,#153263,#153264,
#153265,#153266,#153267,#153268,#153269,#153270,#153271,#153272,#153273,
#153274,#153275,#153276,#153277,#153278,#153279,#153280,#153281,#153282,
#153283,#153284,#153285,#153286,#153287,#153288,#153289,#153290,#153291,
#153292,#153293,#153294,#153295,#153296,#153297,#153298,#153299,#153300,
#153301,#153302,#153303,#153304,#153305,#153306,#153307,#153308,#153309,
#153310,#153311,#153312,#153313,#153314,#153315,#153316,#153317,#153318,
#153319,#153320,#153321,#153322,#153323,#153324,#153325,#153326,#153327,
#153328,#153329,#153330,#153331,#153332,#153333,#153334,#153335,#153336,
#153337,#153338,#153339,#153340,#153341,#153342,#153343,#153344,#153345,
#153346,#153347,#153348,#153349,#153350,#153351,#153352,#153353,#153354,
#153355,#153356,#153357,#153358,#153359,#153360,#153361,#153362,#153363,
#153364,#153365,#153366,#153367,#153368,#153369,#153370,#153371,#153372,
#153373,#153374,#153375,#153376,#153377,#153378,#153379,#153380,#153381,
#153382,#153383,#153384,#153385,#153386,#153387,#153388,#153389,#153390,
#153391,#153392,#153393,#153394,#153395,#153396,#153397,#153398,#153399,
#153400,#153401,#153402,#153403,#153404,#153405,#153406,#153407,#153408,
#153409,#153410,#153411,#153412,#153413,#153414,#153415,#153416,#153417,
#153418,#153419,#153420,#153421,#153422,#153423,#153424,#153425,#153426,
#153427,#153428,#153429,#153430,#153431,#153432,#153433,#153434,#153435,
#153436,#153437,#153438,#153439,#153440,#153441,#153442,#153443,#153444,
#153445,#153446,#153447,#153448,#153449,#153450,#153451,#153452,#153453,
#153454,#153455,#153456,#153457,#153458,#153459,#153460,#153461,#153462,
#153463,#153464,#153465,#153466,#153467,#153468,#153469,#153470,#153471,
#153472,#153473,#153474,#153475,#153476,#153477,#153478,#153479,#153480,
#153481,#153482,#153483,#153484,#153485,#153486,#153487,#153488,#153489,
#153490,#153491,#153492,#153493,#153494,#153495,#153496,#153497,#153498,
#153499,#153500,#153501,#153502,#153503,#153504,#153505,#153506,#153507,
#153508,#153509,#153510,#153511,#153512,#153513,#153514,#153515,#153516,
#153517,#153518,#153519,#153520,#153521,#153522,#153523,#153524,#153525,
#153526,#153527,#153528,#153529,#153530,#153531,#153532,#153533,#153534,
#153535,#153536,#153537,#153538,#153539,#153540,#153541,#153542,#153543,
#153544,#153545,#153546,#153547,#153548,#153549,#153550,#153551,#153552,
#153553,#153554,#153555,#153556,#153557,#153558,#153559,#153560,#153561,
#153562,#153563,#153564,#153565,#153566,#153567,#153568,#153569,#153570,
#153571,#153572,#153573,#153574,#153575,#153576,#153577,#153578,#153579,
#153580,#153581,#153582,#153583,#153584,#153585,#153586,#153587,#153588,
#153589,#153590,#153591,#153592,#153593,#153594,#153595,#153596,#153597,
#153598,#153599,#153600,#153601,#153602,#153603,#153604,#153605,#153606,
#153607,#153608,#153609,#153610,#153611,#153612,#153613,#153614,#153615,
#153616,#153617,#153618,#153619,#153620,#153621,#153622,#153623,#153624,
#153625,#153626,#153627,#153628,#153629,#153630,#153631,#153632,#153633,
#153634,#153635,#153636,#153637,#153638,#153639,#153640,#153641,#153642,
#153643,#153644,#153645,#153646,#153647,#153648,#153649,#153650,#153651,
#153652,#153653,#153654,#153655,#153656,#153657,#153658,#153659,#153660,
#153661,#153662,#153663,#153664,#153665,#153666,#153667,#153668,#153669,
#153670,#153671,#153672,#153673,#153674,#153675,#153676,#153677,#153678,
#153679,#153680,#153681,#153682,#153683,#153684,#153685,#153686,#153687,
#153688,#153689,#153690,#153691,#153692,#153693,#153694,#153695,#153696,
#153697,#153698,#153699,#153700,#153701,#153702,#153703,#153704,#153705,
#153706,#153707,#153708,#153709,#153710,#153711,#153712,#153713,#153714,
#153715,#153716,#153717,#153718,#153719,#153720,#153721,#153722,#153723,
#153724,#153725,#153726,#153727,#153728,#153729,#153730,#153731,#153732,
#153733,#153734,#153735,#153736,#153737,#153738,#153739,#153740,#153741,
#153742,#153743,#153744,#153745,#153746,#153747,#153748,#153749,#153750,
#153751,#153752,#153753,#153754,#153755,#153756,#153757,#153758,#153759,
#153760,#153761,#153762,#153763,#153764,#153765,#153766,#153767,#153768,
#153769,#153770,#153771,#153772,#153773,#153774,#153775,#153776,#153777,
#153778,#153779,#153780,#153781,#153782,#153783,#153784,#153785,#153786,
#153787,#153788,#153789,#153790,#153791,#153792,#153793,#153794,#153795,
#153796,#153797,#153798,#153799,#153800,#153801,#153802,#153803,#153804,
#153805,#153806,#153807,#153808,#153809,#153810,#153811,#153812,#153813,
#153814,#153815,#153816,#153817,#153818,#153819,#153820,#153821,#153822,
#153823,#153824,#153825,#153826,#153827,#153828,#153829,#153830,#153831,
#153832,#153833,#153834,#153835,#153836,#153837,#153838,#153839,#153840,
#153841,#153842,#153843,#153844,#153845,#153846,#153847,#153848,#153849,
#153850,#153851,#153852,#153853,#153854,#153855,#153856,#153857,#153858,
#153859,#153860,#153861,#153862,#153863,#153864,#153865,#153866,#153867,
#153868,#153869,#153870,#153871,#153872,#153873,#153874,#153875,#153876,
#153877,#153878,#153879,#153880,#153881,#153882,#153883,#153884,#153885,
#153886,#153887,#153888,#153889,#153890,#153891,#153892,#153893,#153894,
#153895,#153896,#153897,#153898,#153899,#153900,#153901,#153902,#153903,
#153904,#153905,#153906,#153907,#153908,#153909,#153910,#153911,#153912,
#153913,#153914,#153915,#153916,#153917,#153918,#153919,#153920,#153921,
#153922,#153923,#153924,#153925,#153926,#153927,#153928,#153929,#153930,
#153931,#153932,#153933,#153934,#153935,#153936,#153937,#153938,#153939,
#153940,#153941,#153942,#153943,#153944,#153945,#153946,#153947,#153948,
#153949,#153950,#153951,#153952,#153953,#153954,#153955,#153956,#153957,
#153958,#153959,#153960,#153961,#153962,#153963,#153964,#153965,#153966,
#153967,#153968,#153969,#153970,#153971,#153972,#153973,#153974,#153975,
#153976,#153977,#153978,#153979,#153980,#153981,#153982,#153983,#153984,
#153985,#153986,#153987,#153988,#153989,#153990,#153991,#153992,#153993,
#153994,#153995,#153996,#153997,#153998,#153999,#154000,#154001,#154002,
#154003,#154004,#154005,#154006,#154007,#154008,#154009,#154010,#154011,
#154012,#154013,#154014,#154015,#154016,#154017,#154018,#154019,#154020,
#154021,#154022,#154023,#154024,#154025,#154026,#154027,#154028,#154029,
#154030,#154031,#154032,#154033,#154034,#154035,#154036,#154037,#154038,
#154039,#154040,#154041,#154042,#154043,#154044,#154045,#154046,#154047,
#154048,#154049,#154050,#154051,#154052,#154053,#154054,#154055,#154056,
#154057,#154058,#154059,#154060,#154061,#154062,#154063,#154064,#154065,
#154066,#154067,#154068,#154069,#154070,#154071,#154072,#154073,#154074,
#154075,#154076,#154077,#154078,#154079,#154080,#154081,#154082,#154083,
#154084,#154085,#154086,#154087,#154088,#154089,#154090,#154091,#154092,
#154093,#154094,#154095,#154096,#154097,#154098,#154099,#154100,#154101,
#154102,#154103,#154104,#154105,#154106,#154107,#154108,#154109,#154110,
#154111,#154112,#154113,#154114,#154115,#154116,#154117,#154118,#154119,
#154120,#154121,#154122,#154123,#154124,#154125,#154126,#154127,#154128,
#154129,#154130,#154131,#154132,#154133,#154134,#154135,#154136,#154137,
#154138,#154139,#154140,#154141,#154142,#154143,#154144,#154145,#154146,
#154147,#154148,#154149,#154150,#154151,#154152,#154153,#154154,#154155,
#154156,#154157,#154158,#154159,#154160,#154161,#154162,#154163,#154164,
#154165,#154166,#154167,#154168,#154169,#154170,#154171,#154172,#154173,
#154174,#154175,#154176,#154177,#154178,#154179,#154180,#154181,#154182,
#154183,#154184,#154185,#154186,#154187,#154188,#154189,#154190,#154191,
#154192,#154193,#154194,#154195,#154196,#154197,#154198,#154199,#154200,
#154201,#154202,#154203,#154204,#154205,#154206,#154207,#154208,#154209,
#154210,#154211,#154212,#154213,#154214,#154215,#154216,#154217,#154218,
#154219,#154220,#154221,#154222,#154223,#154224,#154225,#154226,#154227,
#154228,#154229,#154230,#154231,#154232,#154233,#154234,#154235,#154236,
#154237,#154238,#154239,#154240,#154241,#154242,#154243,#154244,#154245,
#154246,#154247,#154248,#154249,#154250,#154251,#154252,#154253,#154254,
#154255,#154256,#154257,#154258,#154259,#154260,#154261,#154262,#154263,
#154264,#154265,#154266,#154267,#154268,#154269,#154270,#154271,#154272,
#154273,#154274,#154275,#154276,#154277,#154278,#154279,#154280,#154281,
#154282,#154283,#154284,#154285,#154286,#154287,#154288,#154289,#154290,
#154291,#154292,#154293,#154294,#154295,#154296,#154297,#154298,#154299,
#154300,#154301,#154302,#154303,#154304,#154305,#154306,#154307,#154308,
#154309,#154310,#154311,#154312,#154313,#154314,#154315,#154316,#154317,
#154318,#154319,#154320,#154321,#154322,#154323,#154324,#154325,#154326,
#154327,#154328,#154329,#154330,#154331,#154332,#154333,#154334,#154335,
#154336,#154337,#154338,#154339,#154340,#154341,#154342,#154343,#154344,
#154345,#154346,#154347,#154348,#154349,#154350,#154351,#154352,#154353,
#154354,#154355,#154356,#154357,#154358,#154359,#154360,#154361,#154362,
#154363,#154364,#154365,#154366,#154367,#154368,#154369,#154370,#154371,
#154372,#154373,#154374,#154375,#154376,#154377,#154378,#154379,#154380,
#154381,#154382,#154383,#154384,#154385,#154386,#154387,#154388,#154389,
#154390,#154391,#154392,#154393,#154394,#154395,#154396,#154397,#154398,
#154399,#154400,#154401,#154402,#154403,#154404,#154405,#154406,#154407,
#154408,#154409,#154410,#154411,#154412,#154413)),.UNSPECIFIED.,.F.,.F.,
 .F.)
B_SPLINE_SURFACE_WITH_KNOTS((2,2),(3,2,2,2,2,2,2,2,2,2,2,2,2,2,2,2,2,2,
2,2,2,2,2,2,2,2,2,2,2,2,2,2,2,2,2,2,2,2,2,2,2,2,2,2,2,2,2,2,2,2,2,2,2,2,
2,2,2,2,2,2,2,2,2,2,2,2,2,2,2,2,2,2,2,2,2,2,2,2,2,2,2,2,2,2,2,2,2,2,2,2,
2,2,2,2,2,2,2,2,2,2,2,2,2,2,2,2,2,2,2,2,2,2,2,2,2,2,2,2,2,2,2,2,2,2,2,2,
2,2,2,2,2,2,2,2,2,2,2,2,2,2,2,2,2,2,2,2,2,2,2,2,2,2,2,2,2,2,2,2,2,2,2,2,
2,2,2,2,2,2,2,2,2,2,2,2,2,2,2,2,2,2,2,2,2,2,2,2,2,2,2,2,2,2,2,2,2,2,2,2,
2,2,2,2,2,2,2,2,2,2,2,2,2,2,2,2,2,2,2,2,2,2,2,2,2,2,2,2,2,2,2,2,2,2,2,2,
2,2,2,2,2,2,2,2,2,2,2,2,2,2,2,2,2,2,2,2,2,2,2,2,2,2,2,2,2,2,2,2,2,2,2,2,
2,2,2,2,2,2,2,2,2,2,2,2,2,2,2,2,2,2,2,2,2,2,2,2,2,2,2,2,2,2,2,2,2,2,2,2,
2,2,2,2,2,2,2,2,2,2,2,2,2,2,2,2,2,2,2,2,2,2,2,2,2,2,2,2,2,2,2,2,2,2,2,2,
2,2,2,2,2,2,2,2,2,2,2,2,2,2,2,2,2,2,2,2,2,2,2,2,2,2,2,2,2,2,2,2,2,2,2,2,
2,2,2,2,2,2,2,2,2,2,2,2,2,2,2,2,2,2,2,2,2,2,2,2,2,2,2,2,2,2,2,2,2,2,2,2,
2,2,2,2,2,2,2,2,2,2,2,2,2,2,2,2,2,2,2,2,2,2,2,2,2,2,2,2,2,2,2,2,2,2,2,2,
2,2,2,2,2,2,2,2,2,2,2,2,2,2,2,2,2,2,2,2,2,2,2,2,2,2,2,2,2,2,2,2,2,2,2,2,
2,2,2,2,2,2,2,2,2,2,2,2,2,2,2,2,2,2,2,2,2,2,2,2,2,2,2,2,2,2,2,2,2,2,2,2,
2,2,2,2,2,2,2,2,2,2,2,2,2,2,2,2,2,2,2,2,2,2,2,2,2,2,2,2,2,2,2,2,2,2,2,2,
2,2,2,2,2,2,2,2,2,2,2,2,2,2,2,2,2,2,2,2,2,2,2,2,2,2,2,2,2,2,2,2,2,2,2,2,
2,2,2,2,2,2,2,2,2,2,2,2,2,2,2,2,2,2,2,2,2,2,2,2,2,2,2,2,2,2,2,2,2,2,2,2,
2,2,2,2,2,2,2,2,2,2,2,2,2,2,2,2,2,2,2,2,2,2,2,2,2,2,2,2,2,2,2,2,2,2,2,2,
2,2,2,2,2,2,2,2,2,2,2,2,2,2,2,2,2,2,2,2,2,2,2,2,2,2,2,2,2,2,2,2,2,2,2,2,
2,2,2,2,2,2,2,2,2,2,2,2,2,2,2,2,2,2,2,2,2,2,2,2,2,2,2,2,2,2,2,2,2,2,2,2,
2,2,2,2,2,2,2,2,2,2,2,2,2,2,2,2,2,2,2,2,2,2,2,2,2,2,2,2,2,2,2,2,2,2,2,2,
2,2,2,2,2,2,2,2,2,2,2,2,2,2,2,2,2,2,2,2,2,2,2,2,2,2,2,2,2,2,2,2,2,2,2,2,
2,2,2,2,2,2,2,2,2,2,2,2,2,2,2,2,2,2,2,2,2,2,2,2,2,2,2,2,2,2,2,2,2,2,2,2,
2,2,2,2,2,2,2,2,2,2,2,2,2,2,2,2,2,2,2,2,2,2,2,2,2,2,2,2,2,2,2,2,2,2,2,2,
2,2,2,2,2,2,2,2,2,2,2,2,2,2,2,2,2,2,2,2,2,2,2,2,2,2,2,2,2,2,2,2,2,2,2,2,
2,2,2,2,2,2,2,2,2,2,2,2,2,2,2,2,2,2,2,2,2,2,2,2,2,2,2,2,2,2,2,2,2,2,2,2,
2,2,2,2,2,2,2,2,2,2,2,2,2,2,2,2,2,2,2,2,2,2,2,2,2,2,2,2,2,2,2,2,2,2,2,2,
2,2,2,2,2,2,2,2,2,2,2,2,2,2,2,2,3),(0.,1.),(0.,0.000980392156862745,0.00196078431372549,
0.00294117647058824,0.00392156862745098,0.00490196078431373,0.00588235294117647,
0.00686274509803922,0.00784313725490196,0.00882352941176471,0.00980392156862745,
0.0107843137254902,0.0117647058823529,0.0127450980392157,0.0137254901960784,
0.0147058823529412,0.0156862745098039,0.0166666666666667,0.0176470588235294,
0.0186274509803922,0.0196078431372549,0.0205882352941176,0.0215686274509804,
0.0225490196078431,0.0235294117647059,0.0245098039215686,0.0254901960784314,
0.0264705882352941,0.0274509803921569,0.0284313725490196,0.0294117647058824,
0.0303921568627451,0.0313725490196078,0.0323529411764706,0.0333333333333333,
0.0343137254901961,0.0352941176470588,0.0362745098039216,0.0372549019607843,
0.0382352941176471,0.0392156862745098,0.0401960784313726,0.0411764705882353,
0.042156862745098,0.0431372549019608,0.0441176470588235,0.0450980392156863,
0.046078431372549,0.0470588235294118,0.0480392156862745,0.0490196078431373,
0.05,0.0509803921568627,0.0519607843137255,0.0529411764705882,0.053921568627451,
0.0549019607843137,0.0558823529411765,0.0568627450980392,0.057843137254902,
0.0588235294117647,0.0598039215686275,0.0607843137254902,0.0617647058823529,
0.0627450980392157,0.0637254901960784,0.0647058823529412,0.0656862745098039,
0.0666666666666667,0.0676470588235294,0.0686274509803922,0.0696078431372549,
0.0705882352941176,0.0715686274509804,0.0725490196078431,0.0735294117647059,
0.0745098039215686,0.0754901960784314,0.0764705882352941,0.0774509803921569,
0.0784313725490196,0.0794117647058823,0.0803921568627451,0.0813725490196078,
0.0823529411764706,0.0833333333333333,0.0843137254901961,0.0852941176470588,
0.0862745098039216,0.0872549019607843,0.0882352941176471,0.0892156862745098,
0.0901960784313725,0.0911764705882353,0.092156862745098,0.0931372549019608,
0.0941176470588235,0.0950980392156863,0.096078431372549,0.0970588235294118,
0.0980392156862745,0.0990196078431373,0.1,0.100980392156863,0.101960784313725,
0.102941176470588,0.103921568627451,0.104901960784314,0.105882352941176,
0.106862745098039,0.107843137254902,0.108823529411765,0.109803921568627,
0.11078431372549,0.111764705882353,0.112745098039216,0.113725490196078,
0.114705882352941,0.115686274509804,0.116666666666667,0.117647058823529,
0.118627450980392,0.119607843137255,0.120588235294118,0.12156862745098,
0.122549019607843,0.123529411764706,0.124509803921569,0.125490196078431,
0.126470588235294,0.127450980392157,0.12843137254902,0.129411764705882,
0.130392156862745,0.131372549019608,0.132352941176471,0.133333333333333,
0.134313725490196,0.135294117647059,0.136274509803922,0.137254901960784,
0.138235294117647,0.13921568627451,0.140196078431373,0.141176470588235,
0.142156862745098,0.143137254901961,0.144117647058824,0.145098039215686,
0.146078431372549,0.147058823529412,0.148039215686275,0.149019607843137,
0.15,0.150980392156863,0.151960784313725,0.152941176470588,0.153921568627451,
0.154901960784314,0.155882352941176,0.156862745098039,0.157843137254902,
0.158823529411765,0.159803921568627,0.16078431372549,0.161764705882353,
0.162745098039216,0.163725490196078,0.164705882352941,0.165686274509804,
0.166666666666667,0.167647058823529,0.168627450980392,0.169607843137255,
0.170588235294118,0.17156862745098,0.172549019607843,0.173529411764706,
0.174509803921569,0.175490196078431,0.176470588235294,0.177450980392157,
0.17843137254902,0.179411764705882,0.180392156862745,0.181372549019608,
0.182352941176471,0.183333333333333,0.184313725490196,0.185294117647059,
0.186274509803922,0.187254901960784,0.188235294117647,0.18921568627451,
0.190196078431373,0.191176470588235,0.192156862745098,0.193137254901961,
0.194117647058824,0.195098039215686,0.196078431372549,0.197058823529412,
0.198039215686275,0.199019607843137,0.2,0.200980392156863,0.201960784313725,
0.202941176470588,0.203921568627451,0.204901960784314,0.205882352941176,
0.206862745098039,0.207843137254902,0.208823529411765,0.209803921568627,
0.21078431372549,0.211764705882353,0.212745098039216,0.213725490196078,
0.214705882352941,0.215686274509804,0.216666666666667,0.217647058823529,
0.218627450980392,0.219607843137255,0.220588235294118,0.22156862745098,
0.222549019607843,0.223529411764706,0.224509803921569,0.225490196078431,
0.226470588235294,0.227450980392157,0.22843137254902,0.229411764705882,
0.230392156862745,0.231372549019608,0.232352941176471,0.233333333333333,
0.234313725490196,0.235294117647059,0.236274509803922,0.237254901960784,
0.238235294117647,0.23921568627451,0.240196078431373,0.241176470588235,
0.242156862745098,0.243137254901961,0.244117647058824,0.245098039215686,
0.246078431372549,0.247058823529412,0.248039215686275,0.249019607843137,
0.25,0.250980392156863,0.251960784313725,0.252941176470588,0.253921568627451,
0.254901960784314,0.255882352941176,0.256862745098039,0.257843137254902,
0.258823529411765,0.259803921568627,0.26078431372549,0.261764705882353,
0.262745098039216,0.263725490196078,0.264705882352941,0.265686274509804,
0.266666666666667,0.267647058823529,0.268627450980392,0.269607843137255,
0.270588235294118,0.27156862745098,0.272549019607843,0.273529411764706,
0.274509803921569,0.275490196078431,0.276470588235294,0.277450980392157,
0.27843137254902,0.279411764705882,0.280392156862745,0.281372549019608,
0.282352941176471,0.283333333333333,0.284313725490196,0.285294117647059,
0.286274509803922,0.287254901960784,0.288235294117647,0.28921568627451,
0.290196078431373,0.291176470588235,0.292156862745098,0.293137254901961,
0.294117647058824,0.295098039215686,0.296078431372549,0.297058823529412,
0.298039215686275,0.299019607843137,0.3,0.300980392156863,0.301960784313725,
0.302941176470588,0.303921568627451,0.304901960784314,0.305882352941176,
0.306862745098039,0.307843137254902,0.308823529411765,0.309803921568627,
0.31078431372549,0.311764705882353,0.312745098039216,0.313725490196078,
0.314705882352941,0.315686274509804,0.316666666666667,0.317647058823529,
0.318627450980392,0.319607843137255,0.320588235294118,0.32156862745098,
0.322549019607843,0.323529411764706,0.324509803921569,0.325490196078431,
0.326470588235294,0.327450980392157,0.32843137254902,0.329411764705882,
0.330392156862745,0.331372549019608,0.332352941176471,0.333333333333333,
0.334313725490196,0.335294117647059,0.336274509803922,0.337254901960784,
0.338235294117647,0.33921568627451,0.340196078431373,0.341176470588235,
0.342156862745098,0.343137254901961,0.344117647058824,0.345098039215686,
0.346078431372549,0.347058823529412,0.348039215686274,0.349019607843137,
0.35,0.350980392156863,0.351960784313726,0.352941176470588,0.353921568627451,
0.354901960784314,0.355882352941176,0.356862745098039,0.357843137254902,
0.358823529411765,0.359803921568627,0.36078431372549,0.361764705882353,
0.362745098039216,0.363725490196078,0.364705882352941,0.365686274509804,
0.366666666666667,0.367647058823529,0.368627450980392,0.369607843137255,
0.370588235294118,0.37156862745098,0.372549019607843,0.373529411764706,
0.374509803921569,0.375490196078431,0.376470588235294,0.377450980392157,
0.37843137254902,0.379411764705882,0.380392156862745,0.381372549019608,
0.382352941176471,0.383333333333333,0.384313725490196,0.385294117647059,
0.386274509803922,0.387254901960784,0.388235294117647,0.38921568627451,
0.390196078431373,0.391176470588235,0.392156862745098,0.393137254901961,
0.394117647058824,0.395098039215686,0.396078431372549,0.397058823529412,
0.398039215686274,0.399019607843137,0.4,0.400980392156863,0.401960784313726,
0.402941176470588,0.403921568627451,0.404901960784314,0.405882352941176,
0.406862745098039,0.407843137254902,0.408823529411765,0.409803921568627,
0.41078431372549,0.411764705882353,0.412745098039216,0.413725490196078,
0.414705882352941,0.415686274509804,0.416666666666667,0.417647058823529,
0.418627450980392,0.419607843137255,0.420588235294118,0.42156862745098,
0.422549019607843,0.423529411764706,0.424509803921569,0.425490196078431,
0.426470588235294,0.427450980392157,0.42843137254902,0.429411764705882,
0.430392156862745,0.431372549019608,0.432352941176471,0.433333333333333,
0.434313725490196,0.435294117647059,0.436274509803922,0.437254901960784,
0.438235294117647,0.43921568627451,0.440196078431373,0.441176470588235,
0.442156862745098,0.443137254901961,0.444117647058824,0.445098039215686,
0.446078431372549,0.447058823529412,0.448039215686275,0.449019607843137,
0.45,0.450980392156863,0.451960784313725,0.452941176470588,0.453921568627451,
0.454901960784314,0.455882352941176,0.456862745098039,0.457843137254902,
0.458823529411765,0.459803921568627,0.46078431372549,0.461764705882353,
0.462745098039216,0.463725490196078,0.464705882352941,0.465686274509804,
0.466666666666667,0.467647058823529,0.468627450980392,0.469607843137255,
0.470588235294118,0.47156862745098,0.472549019607843,0.473529411764706,
0.474509803921569,0.475490196078431,0.476470588235294,0.477450980392157,
0.47843137254902,0.479411764705882,0.480392156862745,0.481372549019608,
0.482352941176471,0.483333333333333,0.484313725490196,0.485294117647059,
0.486274509803922,0.487254901960784,0.488235294117647,0.48921568627451,
0.490196078431373,0.491176470588235,0.492156862745098,0.493137254901961,
0.494117647058824,0.495098039215686,0.496078431372549,0.497058823529412,
0.498039215686275,0.499019607843137,0.5,0.500980392156863,0.501960784313725,
0.502941176470588,0.503921568627451,0.504901960784314,0.505882352941176,
0.506862745098039,0.507843137254902,0.508823529411765,0.509803921568627,
0.51078431372549,0.511764705882353,0.512745098039216,0.513725490196078,
0.514705882352941,0.515686274509804,0.516666666666667,0.517647058823529,
0.518627450980392,0.519607843137255,0.520588235294118,0.52156862745098,
0.522549019607843,0.523529411764706,0.524509803921569,0.525490196078431,
0.526470588235294,0.527450980392157,0.52843137254902,0.529411764705882,
0.530392156862745,0.531372549019608,0.532352941176471,0.533333333333333,
0.534313725490196,0.535294117647059,0.536274509803922,0.537254901960784,
0.538235294117647,0.53921568627451,0.540196078431373,0.541176470588235,
0.542156862745098,0.543137254901961,0.544117647058823,0.545098039215686,
0.546078431372549,0.547058823529412,0.548039215686275,0.549019607843137,
0.55,0.550980392156863,0.551960784313726,0.552941176470588,0.553921568627451,
0.554901960784314,0.555882352941176,0.556862745098039,0.557843137254902,
0.558823529411765,0.559803921568627,0.56078431372549,0.561764705882353,
0.562745098039216,0.563725490196078,0.564705882352941,0.565686274509804,
0.566666666666667,0.567647058823529,0.568627450980392,0.569607843137255,
0.570588235294118,0.57156862745098,0.572549019607843,0.573529411764706,
0.574509803921569,0.575490196078431,0.576470588235294,0.577450980392157,
0.57843137254902,0.579411764705882,0.580392156862745,0.581372549019608,
0.582352941176471,0.583333333333333,0.584313725490196,0.585294117647059,
0.586274509803922,0.587254901960784,0.588235294117647,0.58921568627451,
0.590196078431373,0.591176470588235,0.592156862745098,0.593137254901961,
0.594117647058824,0.595098039215686,0.596078431372549,0.597058823529412,
0.598039215686274,0.599019607843137,0.6,0.600980392156863,0.601960784313725,
0.602941176470588,0.603921568627451,0.604901960784314,0.605882352941176,
0.606862745098039,0.607843137254902,0.608823529411765,0.609803921568628,
0.61078431372549,0.611764705882353,0.612745098039216,0.613725490196078,
0.614705882352941,0.615686274509804,0.616666666666667,0.617647058823529,
0.618627450980392,0.619607843137255,0.620588235294118,0.62156862745098,
0.622549019607843,0.623529411764706,0.624509803921569,0.625490196078431,
0.626470588235294,0.627450980392157,0.62843137254902,0.629411764705882,
0.630392156862745,0.631372549019608,0.632352941176471,0.633333333333333,
0.634313725490196,0.635294117647059,0.636274509803922,0.637254901960784,
0.638235294117647,0.63921568627451,0.640196078431372,0.641176470588235,
0.642156862745098,0.643137254901961,0.644117647058824,0.645098039215686,
0.646078431372549,0.647058823529412,0.648039215686275,0.649019607843137,
0.65,0.650980392156863,0.651960784313726,0.652941176470588,0.653921568627451,
0.654901960784314,0.655882352941176,0.656862745098039,0.657843137254902,
0.658823529411765,0.659803921568627,0.66078431372549,0.661764705882353,
0.662745098039216,0.663725490196078,0.664705882352941,0.665686274509804,
0.666666666666667,0.667647058823529,0.668627450980392,0.669607843137255,
0.670588235294118,0.67156862745098,0.672549019607843,0.673529411764706,
0.674509803921569,0.675490196078431,0.676470588235294,0.677450980392157,
0.67843137254902,0.679411764705882,0.680392156862745,0.681372549019608,
0.682352941176471,0.683333333333333,0.684313725490196,0.685294117647059,
0.686274509803922,0.687254901960784,0.688235294117647,0.68921568627451,
0.690196078431373,0.691176470588235,0.692156862745098,0.693137254901961,
0.694117647058824,0.695098039215686,0.696078431372549,0.697058823529412,
0.698039215686274,0.699019607843137,0.7,0.700980392156863,0.701960784313725,
0.702941176470588,0.703921568627451,0.704901960784314,0.705882352941177,
0.706862745098039,0.707843137254902,0.708823529411765,0.709803921568627,
0.71078431372549,0.711764705882353,0.712745098039216,0.713725490196078,
0.714705882352941,0.715686274509804,0.716666666666667,0.717647058823529,
0.718627450980392,0.719607843137255,0.720588235294118,0.72156862745098,
0.722549019607843,0.723529411764706,0.724509803921569,0.725490196078431,
0.726470588235294,0.727450980392157,0.72843137254902,0.729411764705882,
0.730392156862745,0.731372549019608,0.732352941176471,0.733333333333333,
0.734313725490196,0.735294117647059,0.736274509803922,0.737254901960784,
0.738235294117647,0.73921568627451,0.740196078431373,0.741176470588235,
0.742156862745098,0.743137254901961,0.744117647058824,0.745098039215686,
0.746078431372549,0.747058823529412,0.748039215686275,0.749019607843137,
0.75,0.750980392156863,0.751960784313725,0.752941176470588,0.753921568627451,
0.754901960784314,0.755882352941176,0.756862745098039,0.757843137254902,
0.758823529411765,0.759803921568627,0.76078431372549,0.761764705882353,
0.762745098039216,0.763725490196078,0.764705882352941,0.765686274509804,
0.766666666666667,0.767647058823529,0.768627450980392,0.769607843137255,
0.770588235294118,0.77156862745098,0.772549019607843,0.773529411764706,
0.774509803921569,0.775490196078431,0.776470588235294,0.777450980392157,
0.77843137254902,0.779411764705882,0.780392156862745,0.781372549019608,
0.782352941176471,0.783333333333333,0.784313725490196,0.785294117647059,
0.786274509803922,0.787254901960784,0.788235294117647,0.78921568627451,
0.790196078431373,0.791176470588235,0.792156862745098,0.793137254901961,
0.794117647058823,0.795098039215686,0.796078431372549,0.797058823529412,
0.798039215686275,0.799019607843137,0.8,0.800980392156863,0.801960784313726,
0.802941176470588,0.803921568627451,0.804901960784314,0.805882352941176,
0.806862745098039,0.807843137254902,0.808823529411765,0.809803921568627,
0.81078431372549,0.811764705882353,0.812745098039216,0.813725490196078,
0.814705882352941,0.815686274509804,0.816666666666667,0.817647058823529,
0.818627450980392,0.819607843137255,0.820588235294118,0.82156862745098,
0.822549019607843,0.823529411764706,0.824509803921569,0.825490196078431,
0.826470588235294,0.827450980392157,0.82843137254902,0.829411764705882,
0.830392156862745,0.831372549019608,0.832352941176471,0.833333333333333,
0.834313725490196,0.835294117647059,0.836274509803922,0.837254901960784,
0.838235294117647,0.83921568627451,0.840196078431373,0.841176470588235,
0.842156862745098,0.843137254901961,0.844117647058824,0.845098039215686,
0.846078431372549,0.847058823529412,0.848039215686274,0.849019607843137,
0.85,0.850980392156863,0.851960784313725,0.852941176470588,0.853921568627451,
0.854901960784314,0.855882352941176,0.856862745098039,0.857843137254902,
0.858823529411765,0.859803921568628,0.86078431372549,0.861764705882353,
0.862745098039216,0.863725490196078,0.864705882352941,0.865686274509804,
0.866666666666667,0.867647058823529,0.868627450980392,0.869607843137255,
0.870588235294118,0.87156862745098,0.872549019607843,0.873529411764706,
0.874509803921569,0.875490196078431,0.876470588235294,0.877450980392157,
0.87843137254902,0.879411764705882,0.880392156862745,0.881372549019608,
0.882352941176471,0.883333333333333,0.884313725490196,0.885294117647059,
0.886274509803922,0.887254901960784,0.888235294117647,0.88921568627451,
0.890196078431372,0.891176470588235,0.892156862745098,0.893137254901961,
0.894117647058824,0.895098039215686,0.896078431372549,0.897058823529412,
0.898039215686275,0.899019607843137,0.9,0.900980392156863,0.901960784313726,
0.902941176470588,0.903921568627451,0.904901960784314,0.905882352941176,
0.906862745098039,0.907843137254902,0.908823529411765,0.909803921568627,
0.91078431372549,0.911764705882353,0.912745098039216,0.913725490196078,
0.914705882352941,0.915686274509804,0.916666666666667,0.917647058823529,
0.918627450980392,0.919607843137255,0.920588235294118,0.92156862745098,
0.922549019607843,0.923529411764706,0.924509803921569,0.925490196078431,
0.926470588235294,0.927450980392157,0.92843137254902,0.929411764705882,
0.930392156862745,0.931372549019608,0.932352941176471,0.933333333333333,
0.934313725490196,0.935294117647059,0.936274509803922,0.937254901960784,
0.938235294117647,0.93921568627451,0.940196078431373,0.941176470588235,
0.942156862745098,0.943137254901961,0.944117647058824,0.945098039215686,
0.946078431372549,0.947058823529412,0.948039215686274,0.949019607843137,
0.95,0.950980392156863,0.951960784313725,0.952941176470588,0.953921568627451,
0.954901960784314,0.955882352941177,0.956862745098039,0.957843137254902,
0.958823529411765,0.959803921568627,0.96078431372549,0.961764705882353,
0.962745098039216,0.963725490196078,0.964705882352941,0.965686274509804,
0.966666666666667,0.967647058823529,0.968627450980392,0.969607843137255,
0.970588235294118,0.97156862745098,0.972549019607843,0.973529411764706,
0.974509803921569,0.975490196078431,0.976470588235294,0.977450980392157,
0.97843137254902,0.979411764705882,0.980392156862745,0.981372549019608,
0.982352941176471,0.983333333333333,0.984313725490196,0.985294117647059,
0.985937314000279),.UNSPECIFIED.)
GEOMETRIC_REPRESENTATION_ITEM()
RATIONAL_B_SPLINE_SURFACE(((1.,0.995734176295034,1.,0.995734176295034,1.,
0.995734176295034,1.,0.995734176295034,1.,0.995734176295034,1.,0.995734176295034,
1.,0.995734176295034,1.,0.995734176295034,1.,0.995734176295034,1.,0.995734176295034,
1.,0.995734176295034,1.,0.995734176295034,1.,0.995734176295034,1.,0.995734176295034,
1.,0.995734176295034,1.,0.995734176295034,1.,0.995734176295034,1.,0.995734176295034,
1.,0.995734176295034,1.,0.995734176295034,1.,0.995734176295034,1.,0.995734176295034,
1.,0.995734176295034,1.,0.995734176295034,1.,0.995734176295034,1.,0.995734176295034,
1.,0.995734176295034,1.,0.995734176295034,1.,0.995734176295034,1.,0.995734176295034,
1.,0.995734176295034,1.,0.995734176295034,1.,0.995734176295034,1.,0.995734176295034,
1.,0.995734176295034,1.,0.995734176295034,1.,0.995734176295034,1.,0.995734176295034,
1.,0.995734176295034,1.,0.995734176295034,1.,0.995734176295034,1.,0.995734176295034,
1.,0.995734176295034,1.,0.995734176295034,1.,0.995734176295034,1.,0.995734176295034,
1.,0.995734176295034,1.,0.995734176295034,1.,0.995734176295034,1.,0.995734176295034,
1.,0.995734176295034,1.,0.995734176295034,1.,0.995734176295034,1.,0.995734176295034,
1.,0.995734176295034,1.,0.995734176295034,1.,0.995734176295034,1.,0.995734176295034,
1.,0.995734176295034,1.,0.995734176295034,1.,0.995734176295034,1.,0.995734176295034,
1.,0.995734176295034,1.,0.995734176295034,1.,0.995734176295034,1.,0.995734176295034,
1.,0.995734176295034,1.,0.995734176295034,1.,0.995734176295034,1.,0.995734176295034,
1.,0.995734176295034,1.,0.995734176295034,1.,0.995734176295034,1.,0.995734176295034,
1.,0.995734176295034,1.,0.995734176295034,1.,0.995734176295034,1.,0.995734176295034,
1.,0.995734176295034,1.,0.995734176295034,1.,0.995734176295034,1.,0.995734176295034,
1.,0.995734176295034,1.,0.995734176295034,1.,0.995734176295034,1.,0.995734176295034,
1.,0.995734176295034,1.,0.995734176295034,1.,0.995734176295034,1.,0.995734176295034,
1.,0.995734176295034,1.,0.995734176295034,1.,0.995734176295034,1.,0.995734176295034,
1.,0.995734176295034,1.,0.995734176295034,1.,0.995734176295034,1.,0.995734176295034,
1.,0.995734176295034,1.,0.995734176295034,1.,0.995734176295034,1.,0.995734176295034,
1.,0.995734176295034,1.,0.995734176295034,1.,0.995734176295034,1.,0.995734176295034,
1.,0.995734176295034,1.,0.995734176295034,1.,0.995734176295034,1.,0.995734176295034,
1.,0.995734176295034,1.,0.995734176295034,1.,0.995734176295034,1.,0.995734176295034,
1.,0.995734176295034,1.,0.995734176295034,1.,0.995734176295034,1.,0.995734176295034,
1.,0.995734176295034,1.,0.995734176295034,1.,0.995734176295034,1.,0.995734176295034,
1.,0.995734176295034,1.,0.995734176295034,1.,0.995734176295034,1.,0.995734176295034,
1.,0.995734176295034,1.,0.995734176295034,1.,0.995734176295034,1.,0.995734176295034,
1.,0.995734176295034,1.,0.995734176295034,1.,0.995734176295034,1.,0.995734176295034,
1.,0.995734176295034,1.,0.995734176295034,1.,0.995734176295034,1.,0.995734176295034,
1.,0.995734176295034,1.,0.995734176295034,1.,0.995734176295034,1.,0.995734176295034,
1.,0.995734176295034,1.,0.995734176295034,1.,0.995734176295034,1.,0.995734176295034,
1.,0.995734176295034,1.,0.995734176295034,1.,0.995734176295034,1.,0.995734176295034,
1.,0.995734176295034,1.,0.995734176295034,1.,0.995734176295034,1.,0.995734176295034,
1.,0.995734176295034,1.,0.995734176295034,1.,0.995734176295034,1.,0.995734176295034,
1.,0.995734176295034,1.,0.995734176295034,1.,0.995734176295034,1.,0.995734176295034,
1.,0.995734176295034,1.,0.995734176295034,1.,0.995734176295034,1.,0.995734176295034,
1.,0.995734176295034,1.,0.995734176295034,1.,0.995734176295034,1.,0.995734176295034,
1.,0.995734176295034,1.,0.995734176295034,1.,0.995734176295034,1.,0.995734176295034,
1.,0.995734176295034,1.,0.995734176295034,1.,0.995734176295034,1.,0.995734176295034,
1.,0.995734176295034,1.,0.995734176295034,1.,0.995734176295034,1.,0.995734176295034,
1.,0.995734176295034,1.,0.995734176295034,1.,0.995734176295034,1.,0.995734176295034,
1.,0.995734176295034,1.,0.995734176295034,1.,0.995734176295034,1.,0.995734176295034,
1.,0.995734176295034,1.,0.995734176295034,1.,0.995734176295034,1.,0.995734176295034,
1.,0.995734176295034,1.,0.995734176295034,1.,0.995734176295034,1.,0.995734176295034,
1.,0.995734176295034,1.,0.995734176295034,1.,0.995734176295034,1.,0.995734176295034,
1.,0.995734176295034,1.,0.995734176295034,1.,0.995734176295034,1.,0.995734176295034,
1.,0.995734176295034,1.,0.995734176295034,1.,0.995734176295034,1.,0.995734176295034,
1.,0.995734176295034,1.,0.995734176295034,1.,0.995734176295034,1.,0.995734176295034,
1.,0.995734176295034,1.,0.995734176295034,1.,0.995734176295034,1.,0.995734176295034,
1.,0.995734176295034,1.,0.995734176295034,1.,0.995734176295034,1.,0.995734176295034,
1.,0.995734176295034,1.,0.995734176295034,1.,0.995734176295034,1.,0.995734176295034,
1.,0.995734176295034,1.,0.995734176295034,1.,0.995734176295034,1.,0.995734176295034,
1.,0.995734176295034,1.,0.995734176295034,1.,0.995734176295034,1.,0.995734176295034,
1.,0.995734176295034,1.,0.995734176295034,1.,0.995734176295034,1.,0.995734176295034,
1.,0.995734176295034,1.,0.995734176295034,1.,0.995734176295034,1.,0.995734176295034,
1.,0.995734176295034,1.,0.995734176295034,1.,0.995734176295034,1.,0.995734176295034,
1.,0.995734176295034,1.,0.995734176295034,1.,0.995734176295034,1.,0.995734176295034,
1.,0.995734176295034,1.,0.995734176295034,1.,0.995734176295034,1.,0.995734176295034,
1.,0.995734176295034,1.,0.995734176295034,1.,0.995734176295034,1.,0.995734176295034,
1.,0.995734176295034,1.,0.995734176295034,1.,0.995734176295034,1.,0.995734176295034,
1.,0.995734176295034,1.,0.995734176295034,1.,0.995734176295034,1.,0.995734176295034,
1.,0.995734176295034,1.,0.995734176295034,1.,0.995734176295034,1.,0.995734176295034,
1.,0.995734176295034,1.,0.995734176295034,1.,0.995734176295034,1.,0.995734176295034,
1.,0.995734176295034,1.,0.995734176295034,1.,0.995734176295034,1.,0.995734176295034,
1.,0.995734176295034,1.,0.995734176295034,1.,0.995734176295034,1.,0.995734176295034,
1.,0.995734176295034,1.,0.995734176295034,1.,0.995734176295034,1.,0.995734176295034,
1.,0.995734176295034,1.,0.995734176295034,1.,0.995734176295034,1.,0.995734176295034,
1.,0.995734176295034,1.,0.995734176295034,1.,0.995734176295034,1.,0.995734176295034,
1.,0.995734176295034,1.,0.995734176295034,1.,0.995734176295034,1.,0.995734176295034,
1.,0.995734176295034,1.,0.995734176295034,1.,0.995734176295034,1.,0.995734176295034,
1.,0.995734176295034,1.,0.995734176295034,1.,0.995734176295034,1.,0.995734176295034,
1.,0.995734176295034,1.,0.995734176295034,1.,0.995734176295034,1.,0.995734176295034,
1.,0.995734176295034,1.,0.995734176295034,1.,0.995734176295034,1.,0.995734176295034,
1.,0.995734176295034,1.,0.995734176295034,1.,0.995734176295034,1.,0.995734176295034,
1.,0.995734176295034,1.,0.995734176295034,1.,0.995734176295034,1.,0.995734176295034,
1.,0.995734176295034,1.,0.995734176295034,1.,0.995734176295034,1.,0.995734176295034,
1.,0.995734176295034,1.,0.995734176295034,1.,0.995734176295034,1.,0.995734176295034,
1.,0.995734176295034,1.,0.995734176295034,1.,0.995734176295034,1.,0.995734176295034,
1.,0.995734176295034,1.,0.995734176295034,1.,0.995734176295034,1.,0.995734176295034,
1.,0.995734176295034,1.,0.995734176295034,1.,0.995734176295034,1.,0.995734176295034,
1.,0.995734176295034,1.,0.995734176295034,1.,0.995734176295034,1.,0.995734176295034,
1.,0.995734176295034,1.,0.995734176295034,1.,0.995734176295034,1.,0.995734176295034,
1.,0.995734176295034,1.,0.995734176295034,1.,0.995734176295034,1.,0.995734176295034,
1.,0.995734176295034,1.,0.995734176295034,1.,0.995734176295034,1.,0.995734176295034,
1.,0.995734176295034,1.,0.995734176295034,1.,0.995734176295034,1.,0.995734176295034,
1.,0.995734176295034,1.,0.995734176295034,1.,0.995734176295034,1.,0.995734176295034,
1.,0.995734176295034,1.,0.995734176295034,1.,0.995734176295034,1.,0.995734176295034,
1.,0.995734176295034,1.,0.995734176295034,1.,0.995734176295034,1.,0.995734176295034,
1.,0.995734176295034,1.,0.995734176295034,1.,0.995734176295034,1.,0.995734176295034,
1.,0.995734176295034,1.,0.995734176295034,1.,0.995734176295034,1.,0.995734176295034,
1.,0.995734176295034,1.,0.995734176295034,1.,0.995734176295034,1.,0.995734176295034,
1.,0.995734176295034,1.,0.995734176295034,1.,0.995734176295034,1.,0.995734176295034,
1.,0.995734176295034,1.,0.995734176295034,1.,0.995734176295034,1.,0.995734176295034,
1.,0.995734176295034,1.,0.995734176295034,1.,0.995734176295034,1.,0.995734176295034,
1.,0.995734176295034,1.,0.995734176295034,1.,0.995734176295034,1.,0.995734176295034,
1.,0.995734176295034,1.,0.995734176295034,1.,0.995734176295034,1.,0.995734176295034,
1.,0.995734176295034,1.,0.995734176295034,1.,0.995734176295034,1.,0.995734176295034,
1.,0.995734176295034,1.,0.995734176295034,1.,0.995734176295034,1.,0.995734176295034,
1.,0.995734176295034,1.,0.995734176295034,1.,0.995734176295034,1.,0.995734176295034,
1.,0.995734176295034,1.,0.995734176295034,1.,0.995734176295034,1.,0.995734176295034,
1.,0.995734176295034,1.,0.995734176295034,1.,0.995734176295034,1.,0.995734176295034,
1.,0.995734176295034,1.,0.995734176295034,1.,0.995734176295034,1.,0.995734176295034,
1.,0.995734176295034,1.,0.995734176295034,1.,0.995734176295034,1.,0.995734176295034,
1.,0.995734176295034,1.,0.995734176295034,1.,0.995734176295034,1.,0.995734176295034,
1.,0.995734176295034,1.,0.995734176295034,1.,0.995734176295034,1.,0.995734176295034,
1.,0.995734176295034,1.,0.995734176295034,1.,0.995734176295034,1.,0.995734176295034,
1.,0.995734176295034,1.,0.995734176295034,1.,0.995734176295034,1.,0.995734176295034,
1.,0.995734176295034,1.,0.995734176295034,1.,0.995734176295034,1.,0.995734176295034,
1.,0.995734176295034,1.,0.995734176295034,1.,0.995734176295034,1.,0.995734176295034,
1.,0.995734176295034,1.,0.995734176295034,1.,0.995734176295034,1.,0.995734176295034,
1.,0.995734176295034,1.,0.995734176295034,1.,0.995734176295034,1.,0.995734176295034,
1.,0.995734176295034,1.,0.995734176295034,1.,0.995734176295034,1.,0.995734176295034,
1.,0.995734176295034,1.,0.995734176295034,1.,0.995734176295034,1.,0.995734176295034,
1.,0.995734176295034,1.,0.995734176295034,1.,0.995734176295034,1.,0.995734176295034,
1.,0.995734176295034,1.,0.995734176295034,1.,0.995734176295034,1.,0.995734176295034,
1.,0.995734176295034,1.,0.995734176295034,1.,0.995734176295034,1.,0.995734176295034,
1.,0.995734176295034,1.,0.995734176295034,1.,0.995734176295034,1.,0.995734176295034,
1.,0.995734176295034,1.,0.995734176295034,1.,0.995734176295034,1.,0.995734176295034,
1.,0.995734176295034,1.,0.995734176295034,1.,0.995734176295034,1.,0.995734176295034,
1.,0.995734176295034,1.,0.995734176295034,1.,0.995734176295034,1.,0.995734176295034,
1.,0.995734176295034,1.,0.995734176295034,1.,0.995734176295034,1.,0.995734176295034,
1.,0.995734176295034,1.,0.995734176295034,1.,0.995734176295034,1.,0.995734176295034,
1.,0.995734176295034,1.,0.995734176295034,1.,0.995734176295034,1.,0.995734176295034,
1.,0.995734176295034,1.,0.995734176295034,1.,0.995734176295034,1.,0.995734176295034,
1.,0.995734176295034,1.,0.995734176295034,1.,0.995734176295034,1.,0.995734176295034,
1.,0.995734176295034,1.,0.995734176295034,1.,0.995734176295034,1.,0.995734176295034,
1.,0.995734176295034,1.,0.995734176295034,1.,0.995734176295034,1.,0.995734176295034,
1.,0.995734176295034,1.,0.995734176295034,1.,0.995734176295034,1.,0.995734176295034,
1.,0.995734176295034,1.,0.995734176295034,1.,0.995734176295034,1.,0.995734176295034,
1.,0.995734176295034,1.,0.995734176295034,1.,0.995734176295034,1.,0.995734176295034,
1.,0.995734176295034,1.,0.995734176295034,1.,0.995734176295034,1.,0.995734176295034,
1.,0.995734176295034,1.,0.995734176295034,1.,0.995734176295034,1.,0.995734176295034,
1.,0.995734176295034,1.,0.995734176295034,1.,0.995734176295034,1.,0.995734176295034,
1.,0.995734176295034,1.,0.995734176295034,1.,0.995734176295034,1.,0.995734176295034,
1.,0.995734176295034,1.,0.995734176295034,1.,0.995734176295034,1.,0.995734176295034,
1.,0.995734176295034,1.,0.995734176295034,1.,0.995734176295034,1.,0.995734176295034,
1.,0.995734176295034,1.,0.995734176295034,1.,0.995734176295034,1.,0.995734176295034,
1.,0.995734176295034,1.,0.995734176295034,1.,0.995734176295034,1.,0.995734176295034,
1.,0.995734176295034,1.,0.995734176295034,1.,0.995734176295034,1.,0.995734176295034,
1.,0.995734176295034,1.,0.995734176295034,1.,0.995734176295034,1.,0.995734176295034,
1.,0.995734176295034,1.,0.995734176295034,1.,0.995734176295034,1.,0.995734176295034,
1.,0.995734176295034,1.,0.995734176295034,1.,0.995734176295034,1.,0.995734176295034,
1.,0.995734176295034,1.,0.995734176295034,1.,0.995734176295034,1.,0.995734176295034,
1.,0.995734176295034,1.,0.995734176295034,1.,0.995734176295034,1.,0.995734176295034,
1.,0.995734176295034,1.,0.995734176295034,1.,0.995734176295034,1.,0.995734176295034,
1.,0.995734176295034,1.,0.995734176295034,1.,0.995734176295034,1.,0.995734176295034,
1.,0.995734176295034,1.,0.995734176295034,1.,0.995734176295034,1.,0.995734176295034,
1.,0.995734176295034,1.,0.995734176295034,1.,0.995734176295034,1.,0.995734176295034,
1.,0.995734176295034,1.,0.995734176295034,1.,0.995734176295034,1.,0.995734176295034,
1.,0.995734176295034,1.,0.995734176295034,1.,0.995734176295034,1.,0.995734176295034,
1.,0.995734176295034,1.,0.995734176295034,1.,0.995734176295034,1.,0.995734176295034,
1.,0.995734176295034,1.,0.995734176295034,1.,0.995734176295034,1.,0.995734176295034,
1.,0.995734176295034,1.,0.995734176295034,1.,0.995734176295034,1.,0.995734176295034,
1.,0.995734176295034,1.,0.995734176295034,1.,0.995734176295034,1.,0.995734176295034,
1.,0.995734176295034,1.,0.995734176295034,1.,0.995734176295034,1.,0.995734176295034,
1.,0.995734176295034,1.,0.995734176295034,1.,0.995734176295034,1.,0.995734176295034,
1.,0.995734176295034,1.,0.995734176295034,1.,0.995734176295034,1.,0.995734176295034,
1.,0.995734176295034,1.,0.995734176295034,1.,0.995734176295034,1.,0.995734176295034,
1.,0.995734176295034,1.,0.995734176295034,1.,0.995734176295034,1.,0.995734176295034,
1.,0.995734176295034,1.,0.995734176295034,1.,0.995734176295034,1.,0.995734176295034,
1.,0.995734176295034,1.,0.995734176295034,1.,0.995734176295034,1.,0.995734176295034,
1.,0.995734176295034,1.,0.995734176295034,1.,0.995734176295034,1.,0.995734176295034,
1.,0.995734176295034,1.,0.995734176295034,1.,0.995734176295034,1.,0.995734176295034,
1.,0.995734176295034,1.,0.995734176295034,1.,0.995734176295034,1.,0.995734176295034,
1.,0.995734176295034,1.,0.995734176295034,1.,0.995734176295034,1.,0.995734176295034,
1.,0.995734176295034,1.,0.995734176295034,1.,0.995734176295034,1.,0.995734176295034,
1.,0.995734176295034,1.,0.995734176295034,1.,0.995734176295034,1.,0.995734176295034,
1.,0.995734176295034,1.,0.995734176295034,1.,0.995734176295034,1.,0.995734176295034,
1.,0.995734176295034,1.,0.995734176295034,1.,0.995734176295034,1.,0.995734176295034,
1.,0.995734176295034,1.,0.995734176295034,1.,0.995734176295034,1.,0.995734176295034,
1.,0.995734176295034,1.,0.995734176295034,1.,0.995734176295034,1.,0.995734176295034,
1.,0.995734176295034,1.,0.995734176295034,1.,0.995734176295034,1.,0.995734176295034,
1.,0.995734176295034,1.,0.995734176295034,1.,0.995734176295034,1.,0.995734176295034,
1.,0.995734176295034,1.,0.995734176295034,1.,0.995734176295034,1.,0.995734176295034,
1.,0.995734176295034,1.,0.995734176295034,1.,0.995734176295034,1.,0.995734176295034,
1.,0.995734176295034,1.,0.995734176295034,1.,0.995734176295034,1.,0.995734176295034,
1.,0.995734176295034,1.,0.995734176295034,1.,0.995734176295034,1.,0.995734176295034,
1.,0.995734176295034,1.,0.995734176295034,1.,0.995734176295034,1.,0.995734176295034,
1.,0.995734176295034,1.,0.995734176295034,1.,0.995734176295034,1.,0.995734176295034,
1.,0.995734176295034,1.,0.995734176295034,1.,0.995734176295034,1.,0.995734176295034,
1.,0.995734176295034,1.,0.995734176295034,1.,0.995734176295034,1.,0.995734176295034,
1.,0.995734176295034,1.,0.995734176295034,1.,0.995734176295034,1.,0.995734176295034,
1.,0.995734176295034,1.,0.995734176295034,1.,0.995734176295034,1.,0.995734176295034,
1.,0.995734176295034,1.,0.995734176295034,1.,0.995734176295034,1.,0.995734176295034,
1.,0.995734176295034,1.,0.995734176295034,1.,0.995734176295034,1.,0.995734176295034,
1.,0.995734176295034,1.,0.995734176295034,1.,0.995734176295034,1.,0.995734176295034,
1.,0.995734176295034,1.,0.995734176295034,1.,0.995734176295034,1.,0.995734176295034,
1.,0.995734176295034,1.,0.995734176295034,1.,0.995734176295034,1.,0.995734176295034,
1.,0.995734176295034,1.,0.995734176295034,1.,0.995734176295034,1.,0.995734176295034,
1.,0.995734176295034,1.,0.995734176295034,1.,0.995734176295034,1.,0.995734176295034,
1.,0.995734176295034,1.,0.995734176295034,1.,0.995734176295034,1.,0.995734176295034,
1.,0.995734176295034,1.,0.995734176295034,1.,0.995734176295034,1.,0.995734176295034,
1.,0.995734176295034,1.,0.995734176295034,1.,0.995734176295034,1.,0.995734176295034,
1.,0.995734176295034,1.,0.995734176295034,1.,0.995734176295034,1.,0.995734176295034,
1.,0.995734176295034,1.,0.995734176295034,1.,0.995734176295034,1.,0.995734176295034,
1.,0.995734176295034,1.,0.995734176295034,1.,0.995734176295034,1.,0.995734176295034,
1.,0.995734176295034,1.,0.995734176295034,1.,0.995734176295034,1.,0.995734176295034,
1.,0.995734176295034,1.,0.995734176295034,1.,0.995734176295034,1.,0.995734176295034,
1.,0.995734176295034,1.,0.995734176295034,1.,0.995734176295034,1.,0.995734176295034,
1.,0.995734176295034,1.,0.995734176295034,1.,0.995734176295034,1.,0.995734176295034,
1.,0.995734176295034,1.,0.995734176295034,1.,0.995734176295034,1.,0.995734176295034,
1.,0.995734176295034,1.,0.995734176295034,1.,0.995734176295034,1.,0.995734176295034,
1.,0.995734176295034,1.,0.995734176295034,1.,0.995734176295034,1.,0.995734176295034,
1.,0.995734176295034,1.,0.995734176295034,1.,0.995734176295034,1.,0.995734176295034,
1.,0.995734176295034,1.,0.995734176295034,1.,0.995734176295034,1.,0.995734176295034,
1.,0.995734176295034,1.,0.995734176295034,1.,0.995734176295034,1.,0.995734176295034,
1.,0.995734176295034,1.,0.995734176295034,1.,0.995734176295034,1.,0.995734176295034,
1.,0.995734176295034,1.,0.995734176295034,1.,0.995734176295034,1.,0.995734176295034,
1.,0.995734176295034,1.,0.995734176295034,1.,0.995734176295034,1.,0.995734176295034,
1.,0.995734176295034,1.,0.995734176295034,1.,0.995734176295034,1.,0.995734176295034,
1.,0.995734176295034,1.,0.995734176295034,1.,0.995734176295034,1.,0.995734176295034,
1.,0.995734176295034,1.,0.995734176295034,1.,0.995734176295034,1.,0.995734176295034,
1.,0.995734176295034,1.,0.995734176295034,1.,0.995734176295034,1.,0.995734176295034,
1.,0.995734176295034,1.,0.995734176295034,1.,0.995734176295034,1.,0.995734176295034,
1.,0.995734176295034,1.,0.995734176295034,1.,0.995734176295034,1.,0.995734176295034,
1.,0.995734176295034,1.,0.995734176295034,1.,0.995734176295034,1.,0.995734176295034,
1.,0.995734176295034,1.,0.995734176295034,1.,0.995734176295034,1.,0.995734176295034,
1.,0.995734176295034,1.,0.995734176295034,1.,0.995734176295034,1.,0.995734176295034,
1.,0.995734176295034,1.,0.995734176295034,1.,0.995734176295034,1.,0.995734176295034,
1.,0.995734176295034,1.,0.995734176295034,1.,0.995734176295034,1.,0.995734176295034,
1.,0.995734176295034,1.,0.995734176295034,1.,0.995734176295034,1.,0.995734176295034,
1.,0.995734176295034,1.,0.995734176295034,1.,0.995734176295034,1.,0.995734176295034,
1.,0.995734176295034,1.,0.995734176295034,1.,0.995734176295034,1.,0.995734176295034,
1.,0.995734176295034,1.,0.995734176295034,1.,0.995734176295034,1.,0.995734176295034,
1.,0.995734176295034,1.,0.995734176295034,1.,0.995734176295034,1.,0.995734176295034,
1.,0.995734176295034,1.,0.995734176295034,1.,0.995734176295034,1.,0.995734176295034,
1.,0.995734176295034,1.,0.995734176295034,1.,0.995734176295034,1.,0.995734176295034,
1.,0.995734176295034,1.,0.995734176295034,1.,0.995734176295034,1.,0.995734176295034,
1.,0.995734176295034,1.,0.995734176295034,1.,0.995734176295034,1.,0.995734176295034,
1.,0.995734176295034,1.,0.995734176295034,1.,0.995734176295034,1.,0.995734176295034,
1.,0.995734176295034,1.,0.995734176295034,1.,0.995734176295034,1.,0.995734176295034,
1.,0.995734176295034,1.,0.995734176295034,1.,0.995734176295034,1.,0.995734176295034,
1.,0.995734176295034,1.,0.995734176295034,1.,0.995734176295034,1.,0.995734176295034,
1.,0.995734176295034,1.,0.995734176295034,1.,0.995734176295034,1.,0.995734176295034,
1.,0.995734176295034,1.,0.995734176295034,1.,0.995734176295034,1.,0.995734176295034,
1.,0.995734176295034,1.,0.995734176295034,1.,0.995734176295034,1.,0.995734176295034,
1.,0.995734176295034,1.,0.995734176295034,1.,0.995734176295034,1.,0.995734176295034,
1.,0.995734176295034,1.,0.995734176295034,1.,0.995734176295034,1.,0.995734176295034,
1.,0.995734176295034,1.,0.995734176295034,1.,0.995734176295034,1.,0.995734176295034,
1.,0.995734176295034,1.,0.995734176295034,1.,0.995734176295034,1.,0.995734176295034,
1.,0.995734176295034,1.,0.995734176295034,1.,0.995734176295034,1.,0.995734176295034,
1.,0.995734176295034,1.,0.995734176295034,1.,0.995734176295034,1.,0.995734176295034,
1.,0.995734176295034,1.,0.995734176295034,1.,0.995734176295034,1.,0.995734176295034,
1.,0.995734176295034,1.,0.995734176295034,1.,0.995734176295034,1.,0.995734176295034,
1.,0.995734176295034,1.,0.995734176295034,1.,0.995734176295034,1.,0.995734176295034,
1.,0.995734176295034,1.,0.995734176295034,1.,0.995734176295034,1.,0.997201362504478,
0.998074874808407),(1.,0.995734176295034,1.,0.995734176295034,1.,0.995734176295034,
1.,0.995734176295034,1.,0.995734176295034,1.,0.995734176295034,1.,0.995734176295034,
1.,0.995734176295034,1.,0.995734176295034,1.,0.995734176295034,1.,0.995734176295034,
1.,0.995734176295034,1.,0.995734176295034,1.,0.995734176295034,1.,0.995734176295034,
1.,0.995734176295034,1.,0.995734176295034,1.,0.995734176295034,1.,0.995734176295034,
1.,0.995734176295034,1.,0.995734176295034,1.,0.995734176295034,1.,0.995734176295034,
1.,0.995734176295034,1.,0.995734176295034,1.,0.995734176295034,1.,0.995734176295034,
1.,0.995734176295034,1.,0.995734176295034,1.,0.995734176295034,1.,0.995734176295034,
1.,0.995734176295034,1.,0.995734176295034,1.,0.995734176295034,1.,0.995734176295034,
1.,0.995734176295034,1.,0.995734176295034,1.,0.995734176295034,1.,0.995734176295034,
1.,0.995734176295034,1.,0.995734176295034,1.,0.995734176295034,1.,0.995734176295034,
1.,0.995734176295034,1.,0.995734176295034,1.,0.995734176295034,1.,0.995734176295034,
1.,0.995734176295034,1.,0.995734176295034,1.,0.995734176295034,1.,0.995734176295034,
1.,0.995734176295034,1.,0.995734176295034,1.,0.995734176295034,1.,0.995734176295034,
1.,0.995734176295034,1.,0.995734176295034,1.,0.995734176295034,1.,0.995734176295034,
1.,0.995734176295034,1.,0.995734176295034,1.,0.995734176295034,1.,0.995734176295034,
1.,0.995734176295034,1.,0.995734176295034,1.,0.995734176295034,1.,0.995734176295034,
1.,0.995734176295034,1.,0.995734176295034,1.,0.995734176295034,1.,0.995734176295034,
1.,0.995734176295034,1.,0.995734176295034,1.,0.995734176295034,1.,0.995734176295034,
1.,0.995734176295034,1.,0.995734176295034,1.,0.995734176295034,1.,0.995734176295034,
1.,0.995734176295034,1.,0.995734176295034,1.,0.995734176295034,1.,0.995734176295034,
1.,0.995734176295034,1.,0.995734176295034,1.,0.995734176295034,1.,0.995734176295034,
1.,0.995734176295034,1.,0.995734176295034,1.,0.995734176295034,1.,0.995734176295034,
1.,0.995734176295034,1.,0.995734176295034,1.,0.995734176295034,1.,0.995734176295034,
1.,0.995734176295034,1.,0.995734176295034,1.,0.995734176295034,1.,0.995734176295034,
1.,0.995734176295034,1.,0.995734176295034,1.,0.995734176295034,1.,0.995734176295034,
1.,0.995734176295034,1.,0.995734176295034,1.,0.995734176295034,1.,0.995734176295034,
1.,0.995734176295034,1.,0.995734176295034,1.,0.995734176295034,1.,0.995734176295034,
1.,0.995734176295034,1.,0.995734176295034,1.,0.995734176295034,1.,0.995734176295034,
1.,0.995734176295034,1.,0.995734176295034,1.,0.995734176295034,1.,0.995734176295034,
1.,0.995734176295034,1.,0.995734176295034,1.,0.995734176295034,1.,0.995734176295034,
1.,0.995734176295034,1.,0.995734176295034,1.,0.995734176295034,1.,0.995734176295034,
1.,0.995734176295034,1.,0.995734176295034,1.,0.995734176295034,1.,0.995734176295034,
1.,0.995734176295034,1.,0.995734176295034,1.,0.995734176295034,1.,0.995734176295034,
1.,0.995734176295034,1.,0.995734176295034,1.,0.995734176295034,1.,0.995734176295034,
1.,0.995734176295034,1.,0.995734176295034,1.,0.995734176295034,1.,0.995734176295034,
1.,0.995734176295034,1.,0.995734176295034,1.,0.995734176295034,1.,0.995734176295034,
1.,0.995734176295034,1.,0.995734176295034,1.,0.995734176295034,1.,0.995734176295034,
1.,0.995734176295034,1.,0.995734176295034,1.,0.995734176295034,1.,0.995734176295034,
1.,0.995734176295034,1.,0.995734176295034,1.,0.995734176295034,1.,0.995734176295034,
1.,0.995734176295034,1.,0.995734176295034,1.,0.995734176295034,1.,0.995734176295034,
1.,0.995734176295034,1.,0.995734176295034,1.,0.995734176295034,1.,0.995734176295034,
1.,0.995734176295034,1.,0.995734176295034,1.,0.995734176295034,1.,0.995734176295034,
1.,0.995734176295034,1.,0.995734176295034,1.,0.995734176295034,1.,0.995734176295034,
1.,0.995734176295034,1.,0.995734176295034,1.,0.995734176295034,1.,0.995734176295034,
1.,0.995734176295034,1.,0.995734176295034,1.,0.995734176295034,1.,0.995734176295034,
1.,0.995734176295034,1.,0.995734176295034,1.,0.995734176295034,1.,0.995734176295034,
1.,0.995734176295034,1.,0.995734176295034,1.,0.995734176295034,1.,0.995734176295034,
1.,0.995734176295034,1.,0.995734176295034,1.,0.995734176295034,1.,0.995734176295034,
1.,0.995734176295034,1.,0.995734176295034,1.,0.995734176295034,1.,0.995734176295034,
1.,0.995734176295034,1.,0.995734176295034,1.,0.995734176295034,1.,0.995734176295034,
1.,0.995734176295034,1.,0.995734176295034,1.,0.995734176295034,1.,0.995734176295034,
1.,0.995734176295034,1.,0.995734176295034,1.,0.995734176295034,1.,0.995734176295034,
1.,0.995734176295034,1.,0.995734176295034,1.,0.995734176295034,1.,0.995734176295034,
1.,0.995734176295034,1.,0.995734176295034,1.,0.995734176295034,1.,0.995734176295034,
1.,0.995734176295034,1.,0.995734176295034,1.,0.995734176295034,1.,0.995734176295034,
1.,0.995734176295034,1.,0.995734176295034,1.,0.995734176295034,1.,0.995734176295034,
1.,0.995734176295034,1.,0.995734176295034,1.,0.995734176295034,1.,0.995734176295034,
1.,0.995734176295034,1.,0.995734176295034,1.,0.995734176295034,1.,0.995734176295034,
1.,0.995734176295034,1.,0.995734176295034,1.,0.995734176295034,1.,0.995734176295034,
1.,0.995734176295034,1.,0.995734176295034,1.,0.995734176295034,1.,0.995734176295034,
1.,0.995734176295034,1.,0.995734176295034,1.,0.995734176295034,1.,0.995734176295034,
1.,0.995734176295034,1.,0.995734176295034,1.,0.995734176295034,1.,0.995734176295034,
1.,0.995734176295034,1.,0.995734176295034,1.,0.995734176295034,1.,0.995734176295034,
1.,0.995734176295034,1.,0.995734176295034,1.,0.995734176295034,1.,0.995734176295034,
1.,0.995734176295034,1.,0.995734176295034,1.,0.995734176295034,1.,0.995734176295034,
1.,0.995734176295034,1.,0.995734176295034,1.,0.995734176295034,1.,0.995734176295034,
1.,0.995734176295034,1.,0.995734176295034,1.,0.995734176295034,1.,0.995734176295034,
1.,0.995734176295034,1.,0.995734176295034,1.,0.995734176295034,1.,0.995734176295034,
1.,0.995734176295034,1.,0.995734176295034,1.,0.995734176295034,1.,0.995734176295034,
1.,0.995734176295034,1.,0.995734176295034,1.,0.995734176295034,1.,0.995734176295034,
1.,0.995734176295034,1.,0.995734176295034,1.,0.995734176295034,1.,0.995734176295034,
1.,0.995734176295034,1.,0.995734176295034,1.,0.995734176295034,1.,0.995734176295034,
1.,0.995734176295034,1.,0.995734176295034,1.,0.995734176295034,1.,0.995734176295034,
1.,0.995734176295034,1.,0.995734176295034,1.,0.995734176295034,1.,0.995734176295034,
1.,0.995734176295034,1.,0.995734176295034,1.,0.995734176295034,1.,0.995734176295034,
1.,0.995734176295034,1.,0.995734176295034,1.,0.995734176295034,1.,0.995734176295034,
1.,0.995734176295034,1.,0.995734176295034,1.,0.995734176295034,1.,0.995734176295034,
1.,0.995734176295034,1.,0.995734176295034,1.,0.995734176295034,1.,0.995734176295034,
1.,0.995734176295034,1.,0.995734176295034,1.,0.995734176295034,1.,0.995734176295034,
1.,0.995734176295034,1.,0.995734176295034,1.,0.995734176295034,1.,0.995734176295034,
1.,0.995734176295034,1.,0.995734176295034,1.,0.995734176295034,1.,0.995734176295034,
1.,0.995734176295034,1.,0.995734176295034,1.,0.995734176295034,1.,0.995734176295034,
1.,0.995734176295034,1.,0.995734176295034,1.,0.995734176295034,1.,0.995734176295034,
1.,0.995734176295034,1.,0.995734176295034,1.,0.995734176295034,1.,0.995734176295034,
1.,0.995734176295034,1.,0.995734176295034,1.,0.995734176295034,1.,0.995734176295034,
1.,0.995734176295034,1.,0.995734176295034,1.,0.995734176295034,1.,0.995734176295034,
1.,0.995734176295034,1.,0.995734176295034,1.,0.995734176295034,1.,0.995734176295034,
1.,0.995734176295034,1.,0.995734176295034,1.,0.995734176295034,1.,0.995734176295034,
1.,0.995734176295034,1.,0.995734176295034,1.,0.995734176295034,1.,0.995734176295034,
1.,0.995734176295034,1.,0.995734176295034,1.,0.995734176295034,1.,0.995734176295034,
1.,0.995734176295034,1.,0.995734176295034,1.,0.995734176295034,1.,0.995734176295034,
1.,0.995734176295034,1.,0.995734176295034,1.,0.995734176295034,1.,0.995734176295034,
1.,0.995734176295034,1.,0.995734176295034,1.,0.995734176295034,1.,0.995734176295034,
1.,0.995734176295034,1.,0.995734176295034,1.,0.995734176295034,1.,0.995734176295034,
1.,0.995734176295034,1.,0.995734176295034,1.,0.995734176295034,1.,0.995734176295034,
1.,0.995734176295034,1.,0.995734176295034,1.,0.995734176295034,1.,0.995734176295034,
1.,0.995734176295034,1.,0.995734176295034,1.,0.995734176295034,1.,0.995734176295034,
1.,0.995734176295034,1.,0.995734176295034,1.,0.995734176295034,1.,0.995734176295034,
1.,0.995734176295034,1.,0.995734176295034,1.,0.995734176295034,1.,0.995734176295034,
1.,0.995734176295034,1.,0.995734176295034,1.,0.995734176295034,1.,0.995734176295034,
1.,0.995734176295034,1.,0.995734176295034,1.,0.995734176295034,1.,0.995734176295034,
1.,0.995734176295034,1.,0.995734176295034,1.,0.995734176295034,1.,0.995734176295034,
1.,0.995734176295034,1.,0.995734176295034,1.,0.995734176295034,1.,0.995734176295034,
1.,0.995734176295034,1.,0.995734176295034,1.,0.995734176295034,1.,0.995734176295034,
1.,0.995734176295034,1.,0.995734176295034,1.,0.995734176295034,1.,0.995734176295034,
1.,0.995734176295034,1.,0.995734176295034,1.,0.995734176295034,1.,0.995734176295034,
1.,0.995734176295034,1.,0.995734176295034,1.,0.995734176295034,1.,0.995734176295034,
1.,0.995734176295034,1.,0.995734176295034,1.,0.995734176295034,1.,0.995734176295034,
1.,0.995734176295034,1.,0.995734176295034,1.,0.995734176295034,1.,0.995734176295034,
1.,0.995734176295034,1.,0.995734176295034,1.,0.995734176295034,1.,0.995734176295034,
1.,0.995734176295034,1.,0.995734176295034,1.,0.995734176295034,1.,0.995734176295034,
1.,0.995734176295034,1.,0.995734176295034,1.,0.995734176295034,1.,0.995734176295034,
1.,0.995734176295034,1.,0.995734176295034,1.,0.995734176295034,1.,0.995734176295034,
1.,0.995734176295034,1.,0.995734176295034,1.,0.995734176295034,1.,0.995734176295034,
1.,0.995734176295034,1.,0.995734176295034,1.,0.995734176295034,1.,0.995734176295034,
1.,0.995734176295034,1.,0.995734176295034,1.,0.995734176295034,1.,0.995734176295034,
1.,0.995734176295034,1.,0.995734176295034,1.,0.995734176295034,1.,0.995734176295034,
1.,0.995734176295034,1.,0.995734176295034,1.,0.995734176295034,1.,0.995734176295034,
1.,0.995734176295034,1.,0.995734176295034,1.,0.995734176295034,1.,0.995734176295034,
1.,0.995734176295034,1.,0.995734176295034,1.,0.995734176295034,1.,0.995734176295034,
1.,0.995734176295034,1.,0.995734176295034,1.,0.995734176295034,1.,0.995734176295034,
1.,0.995734176295034,1.,0.995734176295034,1.,0.995734176295034,1.,0.995734176295034,
1.,0.995734176295034,1.,0.995734176295034,1.,0.995734176295034,1.,0.995734176295034,
1.,0.995734176295034,1.,0.995734176295034,1.,0.995734176295034,1.,0.995734176295034,
1.,0.995734176295034,1.,0.995734176295034,1.,0.995734176295034,1.,0.995734176295034,
1.,0.995734176295034,1.,0.995734176295034,1.,0.995734176295034,1.,0.995734176295034,
1.,0.995734176295034,1.,0.995734176295034,1.,0.995734176295034,1.,0.995734176295034,
1.,0.995734176295034,1.,0.995734176295034,1.,0.995734176295034,1.,0.995734176295034,
1.,0.995734176295034,1.,0.995734176295034,1.,0.995734176295034,1.,0.995734176295034,
1.,0.995734176295034,1.,0.995734176295034,1.,0.995734176295034,1.,0.995734176295034,
1.,0.995734176295034,1.,0.995734176295034,1.,0.995734176295034,1.,0.995734176295034,
1.,0.995734176295034,1.,0.995734176295034,1.,0.995734176295034,1.,0.995734176295034,
1.,0.995734176295034,1.,0.995734176295034,1.,0.995734176295034,1.,0.995734176295034,
1.,0.995734176295034,1.,0.995734176295034,1.,0.995734176295034,1.,0.995734176295034,
1.,0.995734176295034,1.,0.995734176295034,1.,0.995734176295034,1.,0.995734176295034,
1.,0.995734176295034,1.,0.995734176295034,1.,0.995734176295034,1.,0.995734176295034,
1.,0.995734176295034,1.,0.995734176295034,1.,0.995734176295034,1.,0.995734176295034,
1.,0.995734176295034,1.,0.995734176295034,1.,0.995734176295034,1.,0.995734176295034,
1.,0.995734176295034,1.,0.995734176295034,1.,0.995734176295034,1.,0.995734176295034,
1.,0.995734176295034,1.,0.995734176295034,1.,0.995734176295034,1.,0.995734176295034,
1.,0.995734176295034,1.,0.995734176295034,1.,0.995734176295034,1.,0.995734176295034,
1.,0.995734176295034,1.,0.995734176295034,1.,0.995734176295034,1.,0.995734176295034,
1.,0.995734176295034,1.,0.995734176295034,1.,0.995734176295034,1.,0.995734176295034,
1.,0.995734176295034,1.,0.995734176295034,1.,0.995734176295034,1.,0.995734176295034,
1.,0.995734176295034,1.,0.995734176295034,1.,0.995734176295034,1.,0.995734176295034,
1.,0.995734176295034,1.,0.995734176295034,1.,0.995734176295034,1.,0.995734176295034,
1.,0.995734176295034,1.,0.995734176295034,1.,0.995734176295034,1.,0.995734176295034,
1.,0.995734176295034,1.,0.995734176295034,1.,0.995734176295034,1.,0.995734176295034,
1.,0.995734176295034,1.,0.995734176295034,1.,0.995734176295034,1.,0.995734176295034,
1.,0.995734176295034,1.,0.995734176295034,1.,0.995734176295034,1.,0.995734176295034,
1.,0.995734176295034,1.,0.995734176295034,1.,0.995734176295034,1.,0.995734176295034,
1.,0.995734176295034,1.,0.995734176295034,1.,0.995734176295034,1.,0.995734176295034,
1.,0.995734176295034,1.,0.995734176295034,1.,0.995734176295034,1.,0.995734176295034,
1.,0.995734176295034,1.,0.995734176295034,1.,0.995734176295034,1.,0.995734176295034,
1.,0.995734176295034,1.,0.995734176295034,1.,0.995734176295034,1.,0.995734176295034,
1.,0.995734176295034,1.,0.995734176295034,1.,0.995734176295034,1.,0.995734176295034,
1.,0.995734176295034,1.,0.995734176295034,1.,0.995734176295034,1.,0.995734176295034,
1.,0.995734176295034,1.,0.995734176295034,1.,0.995734176295034,1.,0.995734176295034,
1.,0.995734176295034,1.,0.995734176295034,1.,0.995734176295034,1.,0.995734176295034,
1.,0.995734176295034,1.,0.995734176295034,1.,0.995734176295034,1.,0.995734176295034,
1.,0.995734176295034,1.,0.995734176295034,1.,0.995734176295034,1.,0.995734176295034,
1.,0.995734176295034,1.,0.995734176295034,1.,0.995734176295034,1.,0.995734176295034,
1.,0.995734176295034,1.,0.995734176295034,1.,0.995734176295034,1.,0.995734176295034,
1.,0.995734176295034,1.,0.995734176295034,1.,0.995734176295034,1.,0.995734176295034,
1.,0.995734176295034,1.,0.995734176295034,1.,0.995734176295034,1.,0.995734176295034,
1.,0.995734176295034,1.,0.995734176295034,1.,0.995734176295034,1.,0.995734176295034,
1.,0.995734176295034,1.,0.995734176295034,1.,0.995734176295034,1.,0.995734176295034,
1.,0.995734176295034,1.,0.995734176295034,1.,0.995734176295034,1.,0.995734176295034,
1.,0.995734176295034,1.,0.995734176295034,1.,0.995734176295034,1.,0.995734176295034,
1.,0.995734176295034,1.,0.995734176295034,1.,0.995734176295034,1.,0.995734176295034,
1.,0.995734176295034,1.,0.995734176295034,1.,0.995734176295034,1.,0.995734176295034,
1.,0.995734176295034,1.,0.995734176295034,1.,0.995734176295034,1.,0.995734176295034,
1.,0.995734176295034,1.,0.995734176295034,1.,0.995734176295034,1.,0.995734176295034,
1.,0.995734176295034,1.,0.995734176295034,1.,0.995734176295034,1.,0.995734176295034,
1.,0.995734176295034,1.,0.995734176295034,1.,0.995734176295034,1.,0.995734176295034,
1.,0.995734176295034,1.,0.995734176295034,1.,0.995734176295034,1.,0.995734176295034,
1.,0.995734176295034,1.,0.995734176295034,1.,0.995734176295034,1.,0.995734176295034,
1.,0.995734176295034,1.,0.995734176295034,1.,0.995734176295034,1.,0.995734176295034,
1.,0.995734176295034,1.,0.995734176295034,1.,0.995734176295034,1.,0.995734176295034,
1.,0.995734176295034,1.,0.995734176295034,1.,0.995734176295034,1.,0.995734176295034,
1.,0.995734176295034,1.,0.995734176295034,1.,0.995734176295034,1.,0.995734176295034,
1.,0.995734176295034,1.,0.995734176295034,1.,0.995734176295034,1.,0.995734176295034,
1.,0.995734176295034,1.,0.995734176295034,1.,0.995734176295034,1.,0.995734176295034,
1.,0.995734176295034,1.,0.995734176295034,1.,0.995734176295034,1.,0.995734176295034,
1.,0.995734176295034,1.,0.995734176295034,1.,0.995734176295034,1.,0.995734176295034,
1.,0.995734176295034,1.,0.995734176295034,1.,0.995734176295034,1.,0.995734176295034,
1.,0.995734176295034,1.,0.995734176295034,1.,0.995734176295034,1.,0.995734176295034,
1.,0.995734176295034,1.,0.995734176295034,1.,0.995734176295034,1.,0.995734176295034,
1.,0.995734176295034,1.,0.995734176295034,1.,0.995734176295034,1.,0.995734176295034,
1.,0.995734176295034,1.,0.995734176295034,1.,0.995734176295034,1.,0.995734176295034,
1.,0.995734176295034,1.,0.995734176295034,1.,0.995734176295034,1.,0.995734176295034,
1.,0.995734176295034,1.,0.995734176295034,1.,0.995734176295034,1.,0.995734176295034,
1.,0.995734176295034,1.,0.995734176295034,1.,0.995734176295034,1.,0.995734176295034,
1.,0.995734176295034,1.,0.995734176295034,1.,0.995734176295034,1.,0.995734176295034,
1.,0.995734176295034,1.,0.995734176295034,1.,0.995734176295034,1.,0.995734176295034,
1.,0.995734176295034,1.,0.995734176295034,1.,0.995734176295034,1.,0.995734176295034,
1.,0.995734176295034,1.,0.995734176295034,1.,0.995734176295034,1.,0.995734176295034,
1.,0.995734176295034,1.,0.995734176295034,1.,0.995734176295034,1.,0.995734176295034,
1.,0.995734176295034,1.,0.995734176295034,1.,0.995734176295034,1.,0.995734176295034,
1.,0.995734176295034,1.,0.995734176295034,1.,0.995734176295034,1.,0.995734176295034,
1.,0.995734176295034,1.,0.995734176295034,1.,0.995734176295034,1.,0.995734176295034,
1.,0.995734176295034,1.,0.995734176295034,1.,0.995734176295034,1.,0.995734176295034,
1.,0.995734176295034,1.,0.995734176295034,1.,0.995734176295034,1.,0.995734176295034,
1.,0.995734176295034,1.,0.995734176295034,1.,0.995734176295034,1.,0.995734176295034,
1.,0.995734176295034,1.,0.995734176295034,1.,0.995734176295034,1.,0.995734176295034,
1.,0.995734176295034,1.,0.995734176295034,1.,0.995734176295034,1.,0.995734176295034,
1.,0.995734176295034,1.,0.995734176295034,1.,0.995734176295034,1.,0.995734176295034,
1.,0.995734176295034,1.,0.995734176295034,1.,0.995734176295034,1.,0.995734176295034,
1.,0.995734176295034,1.,0.995734176295034,1.,0.995734176295034,1.,0.995734176295034,
1.,0.995734176295034,1.,0.995734176295034,1.,0.995734176295034,1.,0.995734176295034,
1.,0.995734176295034,1.,0.995734176295034,1.,0.995734176295034,1.,0.995734176295034,
1.,0.995734176295034,1.,0.995734176295034,1.,0.995734176295034,1.,0.995734176295034,
1.,0.995734176295034,1.,0.995734176295034,1.,0.995734176295034,1.,0.995734176295034,
1.,0.995734176295034,1.,0.995734176295034,1.,0.995734176295034,1.,0.995734176295034,
1.,0.995734176295034,1.,0.995734176295034,1.,0.995734176295034,1.,0.995734176295034,
1.,0.995734176295034,1.,0.995734176295034,1.,0.995734176295034,1.,0.995734176295034,
1.,0.995734176295034,1.,0.995734176295034,1.,0.995734176295034,1.,0.995734176295034,
1.,0.995734176295034,1.,0.995734176295034,1.,0.995734176295034,1.,0.995734176295034,
1.,0.995734176295034,1.,0.995734176295034,1.,0.995734176295034,1.,0.995734176295034,
1.,0.995734176295034,1.,0.995734176295034,1.,0.995734176295034,1.,0.995734176295034,
1.,0.995734176295034,1.,0.995734176295034,1.,0.995734176295034,1.,0.995734176295034,
1.,0.995734176295034,1.,0.995734176295034,1.,0.995734176295034,1.,0.995734176295034,
1.,0.995734176295034,1.,0.995734176295034,1.,0.995734176295034,1.,0.995734176295034,
1.,0.995734176295034,1.,0.995734176295034,1.,0.995734176295034,1.,0.995734176295034,
1.,0.995734176295034,1.,0.995734176295034,1.,0.995734176295034,1.,0.995734176295034,
1.,0.995734176295034,1.,0.995734176295034,1.,0.995734176295034,1.,0.995734176295034,
1.,0.995734176295034,1.,0.995734176295034,1.,0.995734176295034,1.,0.995734176295034,
1.,0.995734176295034,1.,0.995734176295034,1.,0.995734176295034,1.,0.995734176295034,
1.,0.995734176295034,1.,0.995734176295034,1.,0.995734176295034,1.,0.995734176295034,
1.,0.995734176295034,1.,0.995734176295034,1.,0.995734176295034,1.,0.995734176295034,
1.,0.995734176295034,1.,0.995734176295034,1.,0.995734176295034,1.,0.995734176295034,
1.,0.995734176295034,1.,0.995734176295034,1.,0.995734176295034,1.,0.995734176295034,
1.,0.995734176295034,1.,0.995734176295034,1.,0.995734176295034,1.,0.995734176295034,
1.,0.995734176295034,1.,0.995734176295034,1.,0.995734176295034,1.,0.995734176295034,
1.,0.995734176295034,1.,0.995734176295034,1.,0.995734176295034,1.,0.995734176295034,
1.,0.995734176295034,1.,0.995734176295034,1.,0.995734176295034,1.,0.995734176295034,
1.,0.995734176295034,1.,0.995734176295034,1.,0.995734176295034,1.,0.995734176295034,
1.,0.995734176295034,1.,0.995734176295034,1.,0.995734176295034,1.,0.995734176295034,
1.,0.995734176295034,1.,0.995734176295034,1.,0.995734176295034,1.,0.995734176295034,
1.,0.995734176295034,1.,0.995734176295034,1.,0.995734176295034,1.,0.995734176295034,
1.,0.995734176295034,1.,0.995734176295034,1.,0.995734176295034,1.,0.995734176295034,
1.,0.995734176295034,1.,0.995734176295034,1.,0.995734176295034,1.,0.995734176295034,
1.,0.995734176295034,1.,0.995734176295034,1.,0.995734176295034,1.,0.995734176295034,
1.,0.995734176295034,1.,0.995734176295034,1.,0.995734176295034,1.,0.995734176295034,
1.,0.995734176295034,1.,0.995734176295034,1.,0.995734176295034,1.,0.995734176295034,
1.,0.995734176295034,1.,0.995734176295034,1.,0.995734176295034,1.,0.995734176295034,
1.,0.995734176295034,1.,0.995734176295034,1.,0.995734176295034,1.,0.995734176295034,
1.,0.995734176295034,1.,0.995734176295034,1.,0.995734176295034,1.,0.995734176295034,
1.,0.995734176295034,1.,0.995734176295034,1.,0.995734176295034,1.,0.995734176295034,
1.,0.995734176295034,1.,0.995734176295034,1.,0.995734176295034,1.,0.995734176295034,
1.,0.995734176295034,1.,0.995734176295034,1.,0.997201362504478,0.998074874808407)))
REPRESENTATION_ITEM('')
SURFACE()
);
#2503=(
BOUNDED_SURFACE()
B_SPLINE_SURFACE(1,2,((#154459,#154460,#154461,#154462,#154463,#154464,
#154465,#154466,#154467,#154468,#154469,#154470,#154471,#154472,#154473,
#154474,#154475,#154476,#154477,#154478,#154479,#154480,#154481,#154482,
#154483,#154484,#154485,#154486,#154487,#154488,#154489,#154490,#154491,
#154492,#154493,#154494,#154495,#154496,#154497,#154498,#154499,#154500,
#154501,#154502,#154503,#154504,#154505,#154506,#154507,#154508,#154509,
#154510,#154511,#154512,#154513,#154514,#154515,#154516,#154517,#154518,
#154519,#154520,#154521,#154522,#154523,#154524,#154525,#154526,#154527,
#154528,#154529,#154530,#154531,#154532,#154533,#154534,#154535,#154536,
#154537,#154538,#154539,#154540,#154541,#154542,#154543,#154544,#154545,
#154546,#154547,#154548,#154549,#154550,#154551,#154552,#154553,#154554,
#154555,#154556,#154557,#154558,#154559,#154560,#154561,#154562,#154563,
#154564,#154565,#154566,#154567,#154568,#154569,#154570,#154571,#154572,
#154573,#154574,#154575,#154576,#154577,#154578,#154579,#154580,#154581,
#154582,#154583,#154584,#154585,#154586,#154587,#154588,#154589,#154590,
#154591,#154592,#154593,#154594,#154595,#154596,#154597,#154598,#154599,
#154600,#154601,#154602,#154603,#154604,#154605,#154606,#154607,#154608,
#154609,#154610,#154611,#154612,#154613,#154614,#154615,#154616,#154617,
#154618,#154619,#154620,#154621,#154622,#154623,#154624,#154625,#154626,
#154627,#154628,#154629,#154630,#154631,#154632,#154633,#154634,#154635,
#154636,#154637,#154638,#154639,#154640,#154641,#154642,#154643,#154644,
#154645,#154646,#154647,#154648,#154649,#154650,#154651,#154652,#154653,
#154654,#154655,#154656,#154657,#154658,#154659,#154660,#154661,#154662,
#154663,#154664,#154665,#154666,#154667,#154668,#154669,#154670,#154671,
#154672,#154673,#154674,#154675,#154676,#154677,#154678,#154679,#154680,
#154681,#154682,#154683,#154684,#154685,#154686,#154687,#154688,#154689,
#154690,#154691,#154692,#154693,#154694,#154695,#154696,#154697,#154698,
#154699,#154700,#154701,#154702,#154703,#154704,#154705,#154706,#154707,
#154708,#154709,#154710,#154711,#154712,#154713,#154714,#154715,#154716,
#154717,#154718,#154719,#154720,#154721,#154722,#154723,#154724,#154725,
#154726,#154727,#154728,#154729,#154730,#154731,#154732,#154733,#154734,
#154735,#154736,#154737,#154738,#154739,#154740,#154741,#154742,#154743,
#154744,#154745,#154746,#154747,#154748,#154749,#154750,#154751,#154752,
#154753,#154754,#154755,#154756,#154757,#154758,#154759,#154760,#154761,
#154762,#154763,#154764,#154765,#154766,#154767,#154768,#154769,#154770,
#154771,#154772,#154773,#154774,#154775,#154776,#154777,#154778,#154779,
#154780,#154781,#154782,#154783,#154784,#154785,#154786,#154787,#154788,
#154789,#154790,#154791,#154792,#154793,#154794,#154795,#154796,#154797,
#154798,#154799,#154800,#154801,#154802,#154803,#154804,#154805,#154806,
#154807,#154808,#154809,#154810,#154811,#154812,#154813,#154814,#154815,
#154816,#154817,#154818,#154819,#154820,#154821,#154822,#154823,#154824,
#154825,#154826,#154827,#154828,#154829,#154830,#154831,#154832,#154833,
#154834,#154835,#154836,#154837,#154838,#154839,#154840,#154841,#154842,
#154843,#154844,#154845,#154846,#154847,#154848,#154849,#154850,#154851,
#154852,#154853,#154854,#154855,#154856,#154857,#154858,#154859,#154860,
#154861,#154862,#154863,#154864,#154865,#154866,#154867,#154868,#154869,
#154870,#154871,#154872,#154873,#154874,#154875,#154876,#154877,#154878,
#154879,#154880,#154881,#154882,#154883,#154884,#154885,#154886,#154887,
#154888,#154889,#154890,#154891,#154892,#154893,#154894,#154895,#154896,
#154897,#154898,#154899,#154900,#154901,#154902,#154903,#154904,#154905,
#154906,#154907,#154908,#154909,#154910,#154911,#154912,#154913,#154914,
#154915,#154916,#154917,#154918,#154919,#154920,#154921,#154922,#154923,
#154924,#154925,#154926,#154927,#154928,#154929,#154930,#154931,#154932,
#154933,#154934,#154935,#154936,#154937,#154938,#154939,#154940,#154941,
#154942,#154943,#154944,#154945,#154946,#154947,#154948,#154949,#154950,
#154951,#154952,#154953,#154954,#154955,#154956,#154957,#154958,#154959,
#154960,#154961,#154962,#154963,#154964,#154965,#154966,#154967,#154968,
#154969,#154970,#154971,#154972,#154973,#154974,#154975,#154976,#154977,
#154978,#154979,#154980,#154981,#154982,#154983,#154984,#154985,#154986,
#154987,#154988,#154989,#154990,#154991,#154992,#154993,#154994,#154995,
#154996,#154997,#154998,#154999,#155000,#155001,#155002,#155003,#155004,
#155005,#155006,#155007,#155008,#155009,#155010,#155011,#155012,#155013,
#155014,#155015,#155016,#155017,#155018,#155019,#155020,#155021,#155022,
#155023,#155024,#155025,#155026,#155027,#155028,#155029,#155030,#155031,
#155032,#155033,#155034,#155035,#155036,#155037,#155038,#155039,#155040,
#155041,#155042,#155043,#155044,#155045,#155046,#155047,#155048,#155049,
#155050,#155051,#155052,#155053,#155054,#155055,#155056,#155057,#155058,
#155059,#155060,#155061,#155062,#155063,#155064,#155065,#155066,#155067,
#155068,#155069,#155070,#155071,#155072,#155073,#155074,#155075,#155076,
#155077,#155078,#155079,#155080,#155081,#155082,#155083,#155084,#155085,
#155086,#155087,#155088,#155089,#155090,#155091,#155092,#155093,#155094,
#155095,#155096,#155097,#155098,#155099,#155100,#155101,#155102,#155103,
#155104,#155105,#155106,#155107,#155108,#155109,#155110,#155111,#155112,
#155113,#155114,#155115,#155116,#155117,#155118,#155119,#155120,#155121,
#155122,#155123,#155124,#155125,#155126,#155127,#155128,#155129,#155130,
#155131,#155132,#155133,#155134,#155135,#155136,#155137,#155138,#155139,
#155140,#155141,#155142,#155143,#155144,#155145,#155146,#155147,#155148,
#155149,#155150,#155151,#155152,#155153,#155154,#155155,#155156,#155157,
#155158,#155159,#155160,#155161,#155162,#155163,#155164,#155165,#155166,
#155167,#155168,#155169,#155170,#155171,#155172,#155173,#155174,#155175,
#155176,#155177,#155178,#155179,#155180,#155181,#155182,#155183,#155184,
#155185,#155186,#155187,#155188,#155189,#155190,#155191,#155192,#155193,
#155194,#155195,#155196,#155197,#155198,#155199,#155200,#155201,#155202,
#155203,#155204,#155205,#155206,#155207,#155208,#155209,#155210,#155211,
#155212,#155213,#155214,#155215,#155216,#155217,#155218,#155219,#155220,
#155221,#155222,#155223,#155224,#155225,#155226,#155227,#155228,#155229,
#155230,#155231,#155232,#155233,#155234,#155235,#155236,#155237,#155238,
#155239,#155240,#155241,#155242,#155243,#155244,#155245,#155246,#155247,
#155248,#155249,#155250,#155251,#155252,#155253,#155254,#155255,#155256,
#155257,#155258,#155259,#155260,#155261,#155262,#155263,#155264,#155265,
#155266,#155267,#155268,#155269,#155270,#155271,#155272,#155273,#155274,
#155275,#155276,#155277,#155278,#155279,#155280,#155281,#155282,#155283,
#155284,#155285,#155286,#155287,#155288,#155289,#155290,#155291,#155292,
#155293,#155294,#155295,#155296,#155297,#155298,#155299,#155300,#155301,
#155302,#155303,#155304,#155305,#155306,#155307,#155308,#155309,#155310,
#155311,#155312,#155313,#155314,#155315,#155316,#155317,#155318,#155319,
#155320,#155321,#155322,#155323,#155324,#155325,#155326,#155327,#155328,
#155329,#155330,#155331,#155332,#155333,#155334,#155335,#155336,#155337,
#155338,#155339,#155340,#155341,#155342,#155343,#155344,#155345,#155346,
#155347,#155348,#155349,#155350,#155351,#155352,#155353,#155354,#155355,
#155356,#155357,#155358,#155359,#155360,#155361,#155362,#155363,#155364,
#155365,#155366,#155367,#155368,#155369,#155370,#155371,#155372,#155373,
#155374,#155375,#155376,#155377,#155378,#155379,#155380,#155381,#155382,
#155383,#155384,#155385,#155386,#155387,#155388,#155389,#155390,#155391,
#155392,#155393,#155394,#155395,#155396,#155397,#155398,#155399,#155400,
#155401,#155402,#155403,#155404,#155405,#155406,#155407,#155408,#155409,
#155410,#155411,#155412,#155413,#155414,#155415,#155416,#155417,#155418,
#155419,#155420,#155421,#155422,#155423,#155424,#155425,#155426,#155427,
#155428,#155429,#155430,#155431,#155432,#155433,#155434,#155435,#155436,
#155437,#155438,#155439,#155440,#155441,#155442,#155443,#155444,#155445,
#155446,#155447,#155448,#155449,#155450,#155451,#155452,#155453,#155454,
#155455,#155456,#155457,#155458,#155459,#155460,#155461,#155462,#155463,
#155464,#155465,#155466,#155467,#155468,#155469,#155470,#155471,#155472,
#155473,#155474,#155475,#155476,#155477,#155478,#155479,#155480,#155481,
#155482,#155483,#155484,#155485,#155486,#155487,#155488,#155489,#155490,
#155491,#155492,#155493,#155494,#155495,#155496,#155497,#155498,#155499,
#155500,#155501,#155502,#155503,#155504,#155505,#155506,#155507,#155508,
#155509,#155510,#155511,#155512,#155513,#155514,#155515,#155516,#155517,
#155518,#155519,#155520,#155521,#155522,#155523,#155524,#155525,#155526,
#155527,#155528,#155529,#155530,#155531,#155532,#155533,#155534,#155535,
#155536,#155537,#155538,#155539,#155540,#155541,#155542,#155543,#155544,
#155545,#155546,#155547,#155548,#155549,#155550,#155551,#155552,#155553,
#155554,#155555,#155556,#155557,#155558,#155559,#155560,#155561,#155562,
#155563,#155564,#155565,#155566,#155567,#155568,#155569,#155570,#155571,
#155572,#155573,#155574,#155575,#155576,#155577,#155578,#155579,#155580,
#155581,#155582,#155583,#155584,#155585,#155586,#155587,#155588,#155589,
#155590,#155591,#155592,#155593,#155594,#155595,#155596,#155597,#155598,
#155599,#155600,#155601,#155602,#155603,#155604,#155605,#155606,#155607,
#155608,#155609,#155610,#155611,#155612,#155613,#155614,#155615,#155616,
#155617,#155618,#155619,#155620,#155621,#155622,#155623,#155624,#155625,
#155626,#155627,#155628,#155629,#155630,#155631,#155632,#155633,#155634,
#155635,#155636,#155637,#155638,#155639,#155640,#155641,#155642,#155643,
#155644,#155645,#155646,#155647,#155648,#155649,#155650,#155651,#155652,
#155653,#155654,#155655,#155656,#155657,#155658,#155659,#155660,#155661,
#155662,#155663,#155664,#155665,#155666,#155667,#155668,#155669,#155670,
#155671,#155672,#155673,#155674,#155675,#155676,#155677,#155678,#155679,
#155680,#155681,#155682,#155683,#155684,#155685,#155686,#155687,#155688,
#155689,#155690,#155691,#155692,#155693,#155694,#155695,#155696,#155697,
#155698,#155699,#155700,#155701,#155702,#155703,#155704,#155705,#155706,
#155707,#155708,#155709,#155710,#155711,#155712,#155713,#155714,#155715,
#155716,#155717,#155718,#155719,#155720,#155721,#155722,#155723,#155724,
#155725,#155726,#155727,#155728,#155729,#155730,#155731,#155732,#155733,
#155734,#155735,#155736,#155737,#155738,#155739,#155740,#155741,#155742,
#155743,#155744,#155745,#155746,#155747,#155748,#155749,#155750,#155751,
#155752,#155753,#155754,#155755,#155756,#155757,#155758,#155759,#155760,
#155761,#155762,#155763,#155764,#155765,#155766,#155767,#155768,#155769,
#155770,#155771,#155772,#155773,#155774,#155775,#155776,#155777,#155778,
#155779,#155780,#155781,#155782,#155783,#155784,#155785,#155786,#155787,
#155788,#155789,#155790,#155791,#155792,#155793,#155794,#155795,#155796,
#155797,#155798,#155799,#155800,#155801,#155802,#155803,#155804,#155805,
#155806,#155807,#155808,#155809,#155810,#155811,#155812,#155813,#155814,
#155815,#155816,#155817,#155818,#155819,#155820,#155821,#155822,#155823,
#155824,#155825,#155826,#155827,#155828,#155829,#155830,#155831,#155832,
#155833,#155834,#155835,#155836,#155837,#155838,#155839,#155840,#155841,
#155842,#155843,#155844,#155845,#155846,#155847,#155848,#155849,#155850,
#155851,#155852,#155853,#155854,#155855,#155856,#155857,#155858,#155859,
#155860,#155861,#155862,#155863,#155864,#155865,#155866,#155867,#155868,
#155869,#155870,#155871,#155872,#155873,#155874,#155875,#155876,#155877,
#155878,#155879,#155880,#155881,#155882,#155883,#155884,#155885,#155886,
#155887,#155888,#155889,#155890,#155891,#155892,#155893,#155894,#155895,
#155896,#155897,#155898,#155899,#155900,#155901,#155902,#155903,#155904,
#155905,#155906,#155907,#155908,#155909,#155910,#155911,#155912,#155913,
#155914,#155915,#155916,#155917,#155918,#155919,#155920,#155921,#155922,
#155923,#155924,#155925,#155926,#155927,#155928,#155929,#155930,#155931,
#155932,#155933,#155934,#155935,#155936,#155937,#155938,#155939,#155940,
#155941,#155942,#155943,#155944,#155945,#155946,#155947,#155948,#155949,
#155950,#155951,#155952,#155953,#155954,#155955,#155956,#155957,#155958,
#155959,#155960,#155961,#155962,#155963,#155964,#155965,#155966,#155967,
#155968,#155969,#155970,#155971,#155972,#155973,#155974,#155975,#155976,
#155977,#155978,#155979,#155980,#155981,#155982,#155983,#155984,#155985,
#155986,#155987,#155988,#155989,#155990,#155991,#155992,#155993,#155994,
#155995,#155996,#155997,#155998,#155999,#156000,#156001,#156002,#156003,
#156004,#156005,#156006,#156007,#156008,#156009,#156010,#156011,#156012,
#156013,#156014,#156015,#156016,#156017,#156018,#156019,#156020,#156021,
#156022,#156023,#156024,#156025,#156026,#156027,#156028,#156029,#156030,
#156031,#156032,#156033,#156034,#156035,#156036,#156037,#156038,#156039,
#156040,#156041,#156042,#156043,#156044,#156045,#156046,#156047,#156048,
#156049,#156050,#156051,#156052,#156053,#156054,#156055,#156056,#156057,
#156058,#156059,#156060,#156061,#156062,#156063,#156064,#156065,#156066,
#156067,#156068,#156069,#156070,#156071,#156072,#156073,#156074,#156075,
#156076,#156077,#156078,#156079,#156080,#156081,#156082,#156083,#156084,
#156085,#156086,#156087,#156088,#156089,#156090,#156091,#156092,#156093,
#156094,#156095,#156096,#156097,#156098,#156099,#156100,#156101,#156102,
#156103,#156104,#156105,#156106,#156107,#156108,#156109,#156110,#156111,
#156112,#156113,#156114,#156115,#156116,#156117,#156118,#156119,#156120,
#156121,#156122,#156123,#156124,#156125,#156126,#156127,#156128,#156129,
#156130,#156131,#156132,#156133,#156134,#156135,#156136,#156137,#156138,
#156139,#156140,#156141,#156142,#156143,#156144,#156145,#156146,#156147,
#156148,#156149,#156150,#156151,#156152,#156153,#156154,#156155,#156156,
#156157,#156158,#156159,#156160,#156161,#156162,#156163,#156164,#156165,
#156166,#156167,#156168,#156169,#156170,#156171,#156172,#156173,#156174,
#156175,#156176,#156177,#156178,#156179,#156180,#156181,#156182,#156183,
#156184,#156185,#156186,#156187,#156188,#156189,#156190,#156191,#156192,
#156193,#156194,#156195,#156196,#156197,#156198,#156199,#156200,#156201,
#156202,#156203,#156204,#156205,#156206,#156207,#156208,#156209,#156210,
#156211,#156212,#156213,#156214,#156215,#156216,#156217,#156218,#156219,
#156220,#156221,#156222,#156223,#156224,#156225,#156226,#156227,#156228,
#156229,#156230,#156231,#156232,#156233,#156234,#156235,#156236,#156237,
#156238,#156239,#156240,#156241,#156242,#156243,#156244,#156245,#156246,
#156247,#156248,#156249,#156250,#156251,#156252,#156253,#156254,#156255,
#156256,#156257,#156258,#156259,#156260,#156261,#156262,#156263,#156264,
#156265,#156266,#156267,#156268,#156269,#156270,#156271,#156272,#156273,
#156274,#156275,#156276,#156277,#156278,#156279,#156280,#156281,#156282,
#156283,#156284,#156285,#156286,#156287,#156288,#156289,#156290,#156291,
#156292,#156293,#156294,#156295,#156296,#156297,#156298,#156299,#156300,
#156301,#156302,#156303,#156304,#156305,#156306,#156307,#156308,#156309,
#156310,#156311,#156312,#156313,#156314,#156315,#156316,#156317,#156318,
#156319,#156320,#156321,#156322,#156323,#156324,#156325,#156326,#156327,
#156328,#156329,#156330,#156331,#156332,#156333,#156334,#156335,#156336,
#156337,#156338,#156339,#156340,#156341,#156342,#156343,#156344,#156345,
#156346,#156347,#156348,#156349,#156350,#156351,#156352,#156353,#156354,
#156355,#156356,#156357,#156358,#156359,#156360,#156361,#156362,#156363,
#156364,#156365,#156366,#156367,#156368,#156369,#156370,#156371,#156372,
#156373,#156374,#156375,#156376,#156377,#156378,#156379,#156380,#156381,
#156382,#156383,#156384,#156385,#156386,#156387,#156388,#156389,#156390,
#156391,#156392,#156393,#156394,#156395,#156396,#156397,#156398,#156399,
#156400,#156401,#156402,#156403,#156404,#156405,#156406,#156407,#156408,
#156409,#156410,#156411,#156412,#156413,#156414,#156415,#156416,#156417,
#156418,#156419,#156420,#156421,#156422,#156423,#156424,#156425,#156426,
#156427,#156428,#156429,#156430,#156431,#156432,#156433,#156434,#156435,
#156436,#156437,#156438,#156439,#156440,#156441,#156442,#156443,#156444,
#156445,#156446,#156447,#156448,#156449,#156450,#156451,#156452,#156453,
#156454,#156455,#156456,#156457,#156458,#156459,#156460,#156461,#156462,
#156463,#156464,#156465,#156466,#156467,#156468,#156469,#156470,#156471,
#156472,#156473),(#156474,#156475,#156476,#156477,#156478,#156479,#156480,
#156481,#156482,#156483,#156484,#156485,#156486,#156487,#156488,#156489,
#156490,#156491,#156492,#156493,#156494,#156495,#156496,#156497,#156498,
#156499,#156500,#156501,#156502,#156503,#156504,#156505,#156506,#156507,
#156508,#156509,#156510,#156511,#156512,#156513,#156514,#156515,#156516,
#156517,#156518,#156519,#156520,#156521,#156522,#156523,#156524,#156525,
#156526,#156527,#156528,#156529,#156530,#156531,#156532,#156533,#156534,
#156535,#156536,#156537,#156538,#156539,#156540,#156541,#156542,#156543,
#156544,#156545,#156546,#156547,#156548,#156549,#156550,#156551,#156552,
#156553,#156554,#156555,#156556,#156557,#156558,#156559,#156560,#156561,
#156562,#156563,#156564,#156565,#156566,#156567,#156568,#156569,#156570,
#156571,#156572,#156573,#156574,#156575,#156576,#156577,#156578,#156579,
#156580,#156581,#156582,#156583,#156584,#156585,#156586,#156587,#156588,
#156589,#156590,#156591,#156592,#156593,#156594,#156595,#156596,#156597,
#156598,#156599,#156600,#156601,#156602,#156603,#156604,#156605,#156606,
#156607,#156608,#156609,#156610,#156611,#156612,#156613,#156614,#156615,
#156616,#156617,#156618,#156619,#156620,#156621,#156622,#156623,#156624,
#156625,#156626,#156627,#156628,#156629,#156630,#156631,#156632,#156633,
#156634,#156635,#156636,#156637,#156638,#156639,#156640,#156641,#156642,
#156643,#156644,#156645,#156646,#156647,#156648,#156649,#156650,#156651,
#156652,#156653,#156654,#156655,#156656,#156657,#156658,#156659,#156660,
#156661,#156662,#156663,#156664,#156665,#156666,#156667,#156668,#156669,
#156670,#156671,#156672,#156673,#156674,#156675,#156676,#156677,#156678,
#156679,#156680,#156681,#156682,#156683,#156684,#156685,#156686,#156687,
#156688,#156689,#156690,#156691,#156692,#156693,#156694,#156695,#156696,
#156697,#156698,#156699,#156700,#156701,#156702,#156703,#156704,#156705,
#156706,#156707,#156708,#156709,#156710,#156711,#156712,#156713,#156714,
#156715,#156716,#156717,#156718,#156719,#156720,#156721,#156722,#156723,
#156724,#156725,#156726,#156727,#156728,#156729,#156730,#156731,#156732,
#156733,#156734,#156735,#156736,#156737,#156738,#156739,#156740,#156741,
#156742,#156743,#156744,#156745,#156746,#156747,#156748,#156749,#156750,
#156751,#156752,#156753,#156754,#156755,#156756,#156757,#156758,#156759,
#156760,#156761,#156762,#156763,#156764,#156765,#156766,#156767,#156768,
#156769,#156770,#156771,#156772,#156773,#156774,#156775,#156776,#156777,
#156778,#156779,#156780,#156781,#156782,#156783,#156784,#156785,#156786,
#156787,#156788,#156789,#156790,#156791,#156792,#156793,#156794,#156795,
#156796,#156797,#156798,#156799,#156800,#156801,#156802,#156803,#156804,
#156805,#156806,#156807,#156808,#156809,#156810,#156811,#156812,#156813,
#156814,#156815,#156816,#156817,#156818,#156819,#156820,#156821,#156822,
#156823,#156824,#156825,#156826,#156827,#156828,#156829,#156830,#156831,
#156832,#156833,#156834,#156835,#156836,#156837,#156838,#156839,#156840,
#156841,#156842,#156843,#156844,#156845,#156846,#156847,#156848,#156849,
#156850,#156851,#156852,#156853,#156854,#156855,#156856,#156857,#156858,
#156859,#156860,#156861,#156862,#156863,#156864,#156865,#156866,#156867,
#156868,#156869,#156870,#156871,#156872,#156873,#156874,#156875,#156876,
#156877,#156878,#156879,#156880,#156881,#156882,#156883,#156884,#156885,
#156886,#156887,#156888,#156889,#156890,#156891,#156892,#156893,#156894,
#156895,#156896,#156897,#156898,#156899,#156900,#156901,#156902,#156903,
#156904,#156905,#156906,#156907,#156908,#156909,#156910,#156911,#156912,
#156913,#156914,#156915,#156916,#156917,#156918,#156919,#156920,#156921,
#156922,#156923,#156924,#156925,#156926,#156927,#156928,#156929,#156930,
#156931,#156932,#156933,#156934,#156935,#156936,#156937,#156938,#156939,
#156940,#156941,#156942,#156943,#156944,#156945,#156946,#156947,#156948,
#156949,#156950,#156951,#156952,#156953,#156954,#156955,#156956,#156957,
#156958,#156959,#156960,#156961,#156962,#156963,#156964,#156965,#156966,
#156967,#156968,#156969,#156970,#156971,#156972,#156973,#156974,#156975,
#156976,#156977,#156978,#156979,#156980,#156981,#156982,#156983,#156984,
#156985,#156986,#156987,#156988,#156989,#156990,#156991,#156992,#156993,
#156994,#156995,#156996,#156997,#156998,#156999,#157000,#157001,#157002,
#157003,#157004,#157005,#157006,#157007,#157008,#157009,#157010,#157011,
#157012,#157013,#157014,#157015,#157016,#157017,#157018,#157019,#157020,
#157021,#157022,#157023,#157024,#157025,#157026,#157027,#157028,#157029,
#157030,#157031,#157032,#157033,#157034,#157035,#157036,#157037,#157038,
#157039,#157040,#157041,#157042,#157043,#157044,#157045,#157046,#157047,
#157048,#157049,#157050,#157051,#157052,#157053,#157054,#157055,#157056,
#157057,#157058,#157059,#157060,#157061,#157062,#157063,#157064,#157065,
#157066,#157067,#157068,#157069,#157070,#157071,#157072,#157073,#157074,
#157075,#157076,#157077,#157078,#157079,#157080,#157081,#157082,#157083,
#157084,#157085,#157086,#157087,#157088,#157089,#157090,#157091,#157092,
#157093,#157094,#157095,#157096,#157097,#157098,#157099,#157100,#157101,
#157102,#157103,#157104,#157105,#157106,#157107,#157108,#157109,#157110,
#157111,#157112,#157113,#157114,#157115,#157116,#157117,#157118,#157119,
#157120,#157121,#157122,#157123,#157124,#157125,#157126,#157127,#157128,
#157129,#157130,#157131,#157132,#157133,#157134,#157135,#157136,#157137,
#157138,#157139,#157140,#157141,#157142,#157143,#157144,#157145,#157146,
#157147,#157148,#157149,#157150,#157151,#157152,#157153,#157154,#157155,
#157156,#157157,#157158,#157159,#157160,#157161,#157162,#157163,#157164,
#157165,#157166,#157167,#157168,#157169,#157170,#157171,#157172,#157173,
#157174,#157175,#157176,#157177,#157178,#157179,#157180,#157181,#157182,
#157183,#157184,#157185,#157186,#157187,#157188,#157189,#157190,#157191,
#157192,#157193,#157194,#157195,#157196,#157197,#157198,#157199,#157200,
#157201,#157202,#157203,#157204,#157205,#157206,#157207,#157208,#157209,
#157210,#157211,#157212,#157213,#157214,#157215,#157216,#157217,#157218,
#157219,#157220,#157221,#157222,#157223,#157224,#157225,#157226,#157227,
#157228,#157229,#157230,#157231,#157232,#157233,#157234,#157235,#157236,
#157237,#157238,#157239,#157240,#157241,#157242,#157243,#157244,#157245,
#157246,#157247,#157248,#157249,#157250,#157251,#157252,#157253,#157254,
#157255,#157256,#157257,#157258,#157259,#157260,#157261,#157262,#157263,
#157264,#157265,#157266,#157267,#157268,#157269,#157270,#157271,#157272,
#157273,#157274,#157275,#157276,#157277,#157278,#157279,#157280,#157281,
#157282,#157283,#157284,#157285,#157286,#157287,#157288,#157289,#157290,
#157291,#157292,#157293,#157294,#157295,#157296,#157297,#157298,#157299,
#157300,#157301,#157302,#157303,#157304,#157305,#157306,#157307,#157308,
#157309,#157310,#157311,#157312,#157313,#157314,#157315,#157316,#157317,
#157318,#157319,#157320,#157321,#157322,#157323,#157324,#157325,#157326,
#157327,#157328,#157329,#157330,#157331,#157332,#157333,#157334,#157335,
#157336,#157337,#157338,#157339,#157340,#157341,#157342,#157343,#157344,
#157345,#157346,#157347,#157348,#157349,#157350,#157351,#157352,#157353,
#157354,#157355,#157356,#157357,#157358,#157359,#157360,#157361,#157362,
#157363,#157364,#157365,#157366,#157367,#157368,#157369,#157370,#157371,
#157372,#157373,#157374,#157375,#157376,#157377,#157378,#157379,#157380,
#157381,#157382,#157383,#157384,#157385,#157386,#157387,#157388,#157389,
#157390,#157391,#157392,#157393,#157394,#157395,#157396,#157397,#157398,
#157399,#157400,#157401,#157402,#157403,#157404,#157405,#157406,#157407,
#157408,#157409,#157410,#157411,#157412,#157413,#157414,#157415,#157416,
#157417,#157418,#157419,#157420,#157421,#157422,#157423,#157424,#157425,
#157426,#157427,#157428,#157429,#157430,#157431,#157432,#157433,#157434,
#157435,#157436,#157437,#157438,#157439,#157440,#157441,#157442,#157443,
#157444,#157445,#157446,#157447,#157448,#157449,#157450,#157451,#157452,
#157453,#157454,#157455,#157456,#157457,#157458,#157459,#157460,#157461,
#157462,#157463,#157464,#157465,#157466,#157467,#157468,#157469,#157470,
#157471,#157472,#157473,#157474,#157475,#157476,#157477,#157478,#157479,
#157480,#157481,#157482,#157483,#157484,#157485,#157486,#157487,#157488,
#157489,#157490,#157491,#157492,#157493,#157494,#157495,#157496,#157497,
#157498,#157499,#157500,#157501,#157502,#157503,#157504,#157505,#157506,
#157507,#157508,#157509,#157510,#157511,#157512,#157513,#157514,#157515,
#157516,#157517,#157518,#157519,#157520,#157521,#157522,#157523,#157524,
#157525,#157526,#157527,#157528,#157529,#157530,#157531,#157532,#157533,
#157534,#157535,#157536,#157537,#157538,#157539,#157540,#157541,#157542,
#157543,#157544,#157545,#157546,#157547,#157548,#157549,#157550,#157551,
#157552,#157553,#157554,#157555,#157556,#157557,#157558,#157559,#157560,
#157561,#157562,#157563,#157564,#157565,#157566,#157567,#157568,#157569,
#157570,#157571,#157572,#157573,#157574,#157575,#157576,#157577,#157578,
#157579,#157580,#157581,#157582,#157583,#157584,#157585,#157586,#157587,
#157588,#157589,#157590,#157591,#157592,#157593,#157594,#157595,#157596,
#157597,#157598,#157599,#157600,#157601,#157602,#157603,#157604,#157605,
#157606,#157607,#157608,#157609,#157610,#157611,#157612,#157613,#157614,
#157615,#157616,#157617,#157618,#157619,#157620,#157621,#157622,#157623,
#157624,#157625,#157626,#157627,#157628,#157629,#157630,#157631,#157632,
#157633,#157634,#157635,#157636,#157637,#157638,#157639,#157640,#157641,
#157642,#157643,#157644,#157645,#157646,#157647,#157648,#157649,#157650,
#157651,#157652,#157653,#157654,#157655,#157656,#157657,#157658,#157659,
#157660,#157661,#157662,#157663,#157664,#157665,#157666,#157667,#157668,
#157669,#157670,#157671,#157672,#157673,#157674,#157675,#157676,#157677,
#157678,#157679,#157680,#157681,#157682,#157683,#157684,#157685,#157686,
#157687,#157688,#157689,#157690,#157691,#157692,#157693,#157694,#157695,
#157696,#157697,#157698,#157699,#157700,#157701,#157702,#157703,#157704,
#157705,#157706,#157707,#157708,#157709,#157710,#157711,#157712,#157713,
#157714,#157715,#157716,#157717,#157718,#157719,#157720,#157721,#157722,
#157723,#157724,#157725,#157726,#157727,#157728,#157729,#157730,#157731,
#157732,#157733,#157734,#157735,#157736,#157737,#157738,#157739,#157740,
#157741,#157742,#157743,#157744,#157745,#157746,#157747,#157748,#157749,
#157750,#157751,#157752,#157753,#157754,#157755,#157756,#157757,#157758,
#157759,#157760,#157761,#157762,#157763,#157764,#157765,#157766,#157767,
#157768,#157769,#157770,#157771,#157772,#157773,#157774,#157775,#157776,
#157777,#157778,#157779,#157780,#157781,#157782,#157783,#157784,#157785,
#157786,#157787,#157788,#157789,#157790,#157791,#157792,#157793,#157794,
#157795,#157796,#157797,#157798,#157799,#157800,#157801,#157802,#157803,
#157804,#157805,#157806,#157807,#157808,#157809,#157810,#157811,#157812,
#157813,#157814,#157815,#157816,#157817,#157818,#157819,#157820,#157821,
#157822,#157823,#157824,#157825,#157826,#157827,#157828,#157829,#157830,
#157831,#157832,#157833,#157834,#157835,#157836,#157837,#157838,#157839,
#157840,#157841,#157842,#157843,#157844,#157845,#157846,#157847,#157848,
#157849,#157850,#157851,#157852,#157853,#157854,#157855,#157856,#157857,
#157858,#157859,#157860,#157861,#157862,#157863,#157864,#157865,#157866,
#157867,#157868,#157869,#157870,#157871,#157872,#157873,#157874,#157875,
#157876,#157877,#157878,#157879,#157880,#157881,#157882,#157883,#157884,
#157885,#157886,#157887,#157888,#157889,#157890,#157891,#157892,#157893,
#157894,#157895,#157896,#157897,#157898,#157899,#157900,#157901,#157902,
#157903,#157904,#157905,#157906,#157907,#157908,#157909,#157910,#157911,
#157912,#157913,#157914,#157915,#157916,#157917,#157918,#157919,#157920,
#157921,#157922,#157923,#157924,#157925,#157926,#157927,#157928,#157929,
#157930,#157931,#157932,#157933,#157934,#157935,#157936,#157937,#157938,
#157939,#157940,#157941,#157942,#157943,#157944,#157945,#157946,#157947,
#157948,#157949,#157950,#157951,#157952,#157953,#157954,#157955,#157956,
#157957,#157958,#157959,#157960,#157961,#157962,#157963,#157964,#157965,
#157966,#157967,#157968,#157969,#157970,#157971,#157972,#157973,#157974,
#157975,#157976,#157977,#157978,#157979,#157980,#157981,#157982,#157983,
#157984,#157985,#157986,#157987,#157988,#157989,#157990,#157991,#157992,
#157993,#157994,#157995,#157996,#157997,#157998,#157999,#158000,#158001,
#158002,#158003,#158004,#158005,#158006,#158007,#158008,#158009,#158010,
#158011,#158012,#158013,#158014,#158015,#158016,#158017,#158018,#158019,
#158020,#158021,#158022,#158023,#158024,#158025,#158026,#158027,#158028,
#158029,#158030,#158031,#158032,#158033,#158034,#158035,#158036,#158037,
#158038,#158039,#158040,#158041,#158042,#158043,#158044,#158045,#158046,
#158047,#158048,#158049,#158050,#158051,#158052,#158053,#158054,#158055,
#158056,#158057,#158058,#158059,#158060,#158061,#158062,#158063,#158064,
#158065,#158066,#158067,#158068,#158069,#158070,#158071,#158072,#158073,
#158074,#158075,#158076,#158077,#158078,#158079,#158080,#158081,#158082,
#158083,#158084,#158085,#158086,#158087,#158088,#158089,#158090,#158091,
#158092,#158093,#158094,#158095,#158096,#158097,#158098,#158099,#158100,
#158101,#158102,#158103,#158104,#158105,#158106,#158107,#158108,#158109,
#158110,#158111,#158112,#158113,#158114,#158115,#158116,#158117,#158118,
#158119,#158120,#158121,#158122,#158123,#158124,#158125,#158126,#158127,
#158128,#158129,#158130,#158131,#158132,#158133,#158134,#158135,#158136,
#158137,#158138,#158139,#158140,#158141,#158142,#158143,#158144,#158145,
#158146,#158147,#158148,#158149,#158150,#158151,#158152,#158153,#158154,
#158155,#158156,#158157,#158158,#158159,#158160,#158161,#158162,#158163,
#158164,#158165,#158166,#158167,#158168,#158169,#158170,#158171,#158172,
#158173,#158174,#158175,#158176,#158177,#158178,#158179,#158180,#158181,
#158182,#158183,#158184,#158185,#158186,#158187,#158188,#158189,#158190,
#158191,#158192,#158193,#158194,#158195,#158196,#158197,#158198,#158199,
#158200,#158201,#158202,#158203,#158204,#158205,#158206,#158207,#158208,
#158209,#158210,#158211,#158212,#158213,#158214,#158215,#158216,#158217,
#158218,#158219,#158220,#158221,#158222,#158223,#158224,#158225,#158226,
#158227,#158228,#158229,#158230,#158231,#158232,#158233,#158234,#158235,
#158236,#158237,#158238,#158239,#158240,#158241,#158242,#158243,#158244,
#158245,#158246,#158247,#158248,#158249,#158250,#158251,#158252,#158253,
#158254,#158255,#158256,#158257,#158258,#158259,#158260,#158261,#158262,
#158263,#158264,#158265,#158266,#158267,#158268,#158269,#158270,#158271,
#158272,#158273,#158274,#158275,#158276,#158277,#158278,#158279,#158280,
#158281,#158282,#158283,#158284,#158285,#158286,#158287,#158288,#158289,
#158290,#158291,#158292,#158293,#158294,#158295,#158296,#158297,#158298,
#158299,#158300,#158301,#158302,#158303,#158304,#158305,#158306,#158307,
#158308,#158309,#158310,#158311,#158312,#158313,#158314,#158315,#158316,
#158317,#158318,#158319,#158320,#158321,#158322,#158323,#158324,#158325,
#158326,#158327,#158328,#158329,#158330,#158331,#158332,#158333,#158334,
#158335,#158336,#158337,#158338,#158339,#158340,#158341,#158342,#158343,
#158344,#158345,#158346,#158347,#158348,#158349,#158350,#158351,#158352,
#158353,#158354,#158355,#158356,#158357,#158358,#158359,#158360,#158361,
#158362,#158363,#158364,#158365,#158366,#158367,#158368,#158369,#158370,
#158371,#158372,#158373,#158374,#158375,#158376,#158377,#158378,#158379,
#158380,#158381,#158382,#158383,#158384,#158385,#158386,#158387,#158388,
#158389,#158390,#158391,#158392,#158393,#158394,#158395,#158396,#158397,
#158398,#158399,#158400,#158401,#158402,#158403,#158404,#158405,#158406,
#158407,#158408,#158409,#158410,#158411,#158412,#158413,#158414,#158415,
#158416,#158417,#158418,#158419,#158420,#158421,#158422,#158423,#158424,
#158425,#158426,#158427,#158428,#158429,#158430,#158431,#158432,#158433,
#158434,#158435,#158436,#158437,#158438,#158439,#158440,#158441,#158442,
#158443,#158444,#158445,#158446,#158447,#158448,#158449,#158450,#158451,
#158452,#158453,#158454,#158455,#158456,#158457,#158458,#158459,#158460,
#158461,#158462,#158463,#158464,#158465,#158466,#158467,#158468,#158469,
#158470,#158471,#158472,#158473,#158474,#158475,#158476,#158477,#158478,
#158479,#158480,#158481,#158482,#158483,#158484,#158485,#158486,#158487,
#158488)),.UNSPECIFIED.,.F.,.F.,.F.)
B_SPLINE_SURFACE_WITH_KNOTS((2,2),(3,2,2,2,2,2,2,2,2,2,2,2,2,2,2,2,2,2,
2,2,2,2,2,2,2,2,2,2,2,2,2,2,2,2,2,2,2,2,2,2,2,2,2,2,2,2,2,2,2,2,2,2,2,2,
2,2,2,2,2,2,2,2,2,2,2,2,2,2,2,2,2,2,2,2,2,2,2,2,2,2,2,2,2,2,2,2,2,2,2,2,
2,2,2,2,2,2,2,2,2,2,2,2,2,2,2,2,2,2,2,2,2,2,2,2,2,2,2,2,2,2,2,2,2,2,2,2,
2,2,2,2,2,2,2,2,2,2,2,2,2,2,2,2,2,2,2,2,2,2,2,2,2,2,2,2,2,2,2,2,2,2,2,2,
2,2,2,2,2,2,2,2,2,2,2,2,2,2,2,2,2,2,2,2,2,2,2,2,2,2,2,2,2,2,2,2,2,2,2,2,
2,2,2,2,2,2,2,2,2,2,2,2,2,2,2,2,2,2,2,2,2,2,2,2,2,2,2,2,2,2,2,2,2,2,2,2,
2,2,2,2,2,2,2,2,2,2,2,2,2,2,2,2,2,2,2,2,2,2,2,2,2,2,2,2,2,2,2,2,2,2,2,2,
2,2,2,2,2,2,2,2,2,2,2,2,2,2,2,2,2,2,2,2,2,2,2,2,2,2,2,2,2,2,2,2,2,2,2,2,
2,2,2,2,2,2,2,2,2,2,2,2,2,2,2,2,2,2,2,2,2,2,2,2,2,2,2,2,2,2,2,2,2,2,2,2,
2,2,2,2,2,2,2,2,2,2,2,2,2,2,2,2,2,2,2,2,2,2,2,2,2,2,2,2,2,2,2,2,2,2,2,2,
2,2,2,2,2,2,2,2,2,2,2,2,2,2,2,2,2,2,2,2,2,2,2,2,2,2,2,2,2,2,2,2,2,2,2,2,
2,2,2,2,2,2,2,2,2,2,2,2,2,2,2,2,2,2,2,2,2,2,2,2,2,2,2,2,2,2,2,2,2,2,2,2,
2,2,2,2,2,2,2,2,2,2,2,2,2,2,2,2,2,2,2,2,2,2,2,2,2,2,2,2,2,2,2,2,2,2,2,2,
2,2,2,2,2,2,2,2,2,2,2,2,2,2,2,2,2,2,2,2,2,2,2,2,2,2,2,2,2,2,2,2,2,2,2,2,
2,2,2,2,2,2,2,2,2,2,2,2,2,2,2,2,2,2,2,2,2,2,2,2,2,2,2,2,2,2,2,2,2,2,2,2,
2,2,2,2,2,2,2,2,2,2,2,2,2,2,2,2,2,2,2,2,2,2,2,2,2,2,2,2,2,2,2,2,2,2,2,2,
2,2,2,2,2,2,2,2,2,2,2,2,2,2,2,2,2,2,2,2,2,2,2,2,2,2,2,2,2,2,2,2,2,2,2,2,
2,2,2,2,2,2,2,2,2,2,2,2,2,2,2,2,2,2,2,2,2,2,2,2,2,2,2,2,2,2,2,2,2,2,2,2,
2,2,2,2,2,2,2,2,2,2,2,2,2,2,2,2,2,2,2,2,2,2,2,2,2,2,2,2,2,2,2,2,2,2,2,2,
2,2,2,2,2,2,2,2,2,2,2,2,2,2,2,2,2,2,2,2,2,2,2,2,2,2,2,2,2,2,2,2,2,2,2,2,
2,2,2,2,2,2,2,2,2,2,2,2,2,2,2,2,2,2,2,2,2,2,2,2,2,2,2,2,2,2,2,2,2,2,2,2,
2,2,2,2,2,2,2,2,2,2,2,2,2,2,2,2,2,2,2,2,2,2,2,2,2,2,2,2,2,2,2,2,2,2,2,2,
2,2,2,2,2,2,2,2,2,2,2,2,2,2,2,2,2,2,2,2,2,2,2,2,2,2,2,2,2,2,2,2,2,2,2,2,
2,2,2,2,2,2,2,2,2,2,2,2,2,2,2,2,2,2,2,2,2,2,2,2,2,2,2,2,2,2,2,2,2,2,2,2,
2,2,2,2,2,2,2,2,2,2,2,2,2,2,2,2,2,2,2,2,2,2,2,2,2,2,2,2,2,2,2,2,2,2,2,2,
2,2,2,2,2,2,2,2,2,2,2,2,2,2,2,2,2,2,2,2,2,2,2,2,2,2,2,2,2,2,2,2,2,2,2,2,
2,2,2,2,2,2,2,2,2,2,2,2,2,2,2,2,2,2,2,2,2,2,2,2,2,2,2,2,2,2,2,2,2,2,2,2,
2,2,2,2,2,2,2,2,2,2,2,2,2,2,2,2,2,3),(0.,1.),(0.,0.000980392156862745,0.00196078431372549,
0.00294117647058824,0.00392156862745098,0.00490196078431373,0.00588235294117647,
0.00686274509803922,0.00784313725490196,0.00882352941176471,0.00980392156862745,
0.0107843137254902,0.0117647058823529,0.0127450980392157,0.0137254901960784,
0.0147058823529412,0.0156862745098039,0.0166666666666667,0.0176470588235294,
0.0186274509803922,0.0196078431372549,0.0205882352941176,0.0215686274509804,
0.0225490196078431,0.0235294117647059,0.0245098039215686,0.0254901960784314,
0.0264705882352941,0.0274509803921569,0.0284313725490196,0.0294117647058824,
0.0303921568627451,0.0313725490196078,0.0323529411764706,0.0333333333333333,
0.0343137254901961,0.0352941176470588,0.0362745098039216,0.0372549019607843,
0.0382352941176471,0.0392156862745098,0.0401960784313726,0.0411764705882353,
0.042156862745098,0.0431372549019608,0.0441176470588235,0.0450980392156863,
0.046078431372549,0.0470588235294118,0.0480392156862745,0.0490196078431373,
0.05,0.0509803921568627,0.0519607843137255,0.0529411764705882,0.053921568627451,
0.0549019607843137,0.0558823529411765,0.0568627450980392,0.057843137254902,
0.0588235294117647,0.0598039215686275,0.0607843137254902,0.0617647058823529,
0.0627450980392157,0.0637254901960784,0.0647058823529412,0.0656862745098039,
0.0666666666666667,0.0676470588235294,0.0686274509803922,0.0696078431372549,
0.0705882352941176,0.0715686274509804,0.0725490196078431,0.0735294117647059,
0.0745098039215686,0.0754901960784314,0.0764705882352941,0.0774509803921569,
0.0784313725490196,0.0794117647058823,0.0803921568627451,0.0813725490196078,
0.0823529411764706,0.0833333333333333,0.0843137254901961,0.0852941176470588,
0.0862745098039216,0.0872549019607843,0.0882352941176471,0.0892156862745098,
0.0901960784313725,0.0911764705882353,0.092156862745098,0.0931372549019608,
0.0941176470588235,0.0950980392156863,0.096078431372549,0.0970588235294118,
0.0980392156862745,0.0990196078431373,0.1,0.100980392156863,0.101960784313725,
0.102941176470588,0.103921568627451,0.104901960784314,0.105882352941176,
0.106862745098039,0.107843137254902,0.108823529411765,0.109803921568627,
0.11078431372549,0.111764705882353,0.112745098039216,0.113725490196078,
0.114705882352941,0.115686274509804,0.116666666666667,0.117647058823529,
0.118627450980392,0.119607843137255,0.120588235294118,0.12156862745098,
0.122549019607843,0.123529411764706,0.124509803921569,0.125490196078431,
0.126470588235294,0.127450980392157,0.12843137254902,0.129411764705882,
0.130392156862745,0.131372549019608,0.132352941176471,0.133333333333333,
0.134313725490196,0.135294117647059,0.136274509803922,0.137254901960784,
0.138235294117647,0.13921568627451,0.140196078431373,0.141176470588235,
0.142156862745098,0.143137254901961,0.144117647058824,0.145098039215686,
0.146078431372549,0.147058823529412,0.148039215686275,0.149019607843137,
0.15,0.150980392156863,0.151960784313725,0.152941176470588,0.153921568627451,
0.154901960784314,0.155882352941176,0.156862745098039,0.157843137254902,
0.158823529411765,0.159803921568627,0.16078431372549,0.161764705882353,
0.162745098039216,0.163725490196078,0.164705882352941,0.165686274509804,
0.166666666666667,0.167647058823529,0.168627450980392,0.169607843137255,
0.170588235294118,0.17156862745098,0.172549019607843,0.173529411764706,
0.174509803921569,0.175490196078431,0.176470588235294,0.177450980392157,
0.17843137254902,0.179411764705882,0.180392156862745,0.181372549019608,
0.182352941176471,0.183333333333333,0.184313725490196,0.185294117647059,
0.186274509803922,0.187254901960784,0.188235294117647,0.18921568627451,
0.190196078431373,0.191176470588235,0.192156862745098,0.193137254901961,
0.194117647058824,0.195098039215686,0.196078431372549,0.197058823529412,
0.198039215686275,0.199019607843137,0.2,0.200980392156863,0.201960784313725,
0.202941176470588,0.203921568627451,0.204901960784314,0.205882352941176,
0.206862745098039,0.207843137254902,0.208823529411765,0.209803921568627,
0.21078431372549,0.211764705882353,0.212745098039216,0.213725490196078,
0.214705882352941,0.215686274509804,0.216666666666667,0.217647058823529,
0.218627450980392,0.219607843137255,0.220588235294118,0.22156862745098,
0.222549019607843,0.223529411764706,0.224509803921569,0.225490196078431,
0.226470588235294,0.227450980392157,0.22843137254902,0.229411764705882,
0.230392156862745,0.231372549019608,0.232352941176471,0.233333333333333,
0.234313725490196,0.235294117647059,0.236274509803922,0.237254901960784,
0.238235294117647,0.23921568627451,0.240196078431373,0.241176470588235,
0.242156862745098,0.243137254901961,0.244117647058824,0.245098039215686,
0.246078431372549,0.247058823529412,0.248039215686275,0.249019607843137,
0.25,0.250980392156863,0.251960784313725,0.252941176470588,0.253921568627451,
0.254901960784314,0.255882352941176,0.256862745098039,0.257843137254902,
0.258823529411765,0.259803921568627,0.26078431372549,0.261764705882353,
0.262745098039216,0.263725490196078,0.264705882352941,0.265686274509804,
0.266666666666667,0.267647058823529,0.268627450980392,0.269607843137255,
0.270588235294118,0.27156862745098,0.272549019607843,0.273529411764706,
0.274509803921569,0.275490196078431,0.276470588235294,0.277450980392157,
0.27843137254902,0.279411764705882,0.280392156862745,0.281372549019608,
0.282352941176471,0.283333333333333,0.284313725490196,0.285294117647059,
0.286274509803922,0.287254901960784,0.288235294117647,0.28921568627451,
0.290196078431373,0.291176470588235,0.292156862745098,0.293137254901961,
0.294117647058824,0.295098039215686,0.296078431372549,0.297058823529412,
0.298039215686275,0.299019607843137,0.3,0.300980392156863,0.301960784313725,
0.302941176470588,0.303921568627451,0.304901960784314,0.305882352941176,
0.306862745098039,0.307843137254902,0.308823529411765,0.309803921568627,
0.31078431372549,0.311764705882353,0.312745098039216,0.313725490196078,
0.314705882352941,0.315686274509804,0.316666666666667,0.317647058823529,
0.318627450980392,0.319607843137255,0.320588235294118,0.32156862745098,
0.322549019607843,0.323529411764706,0.324509803921569,0.325490196078431,
0.326470588235294,0.327450980392157,0.32843137254902,0.329411764705882,
0.330392156862745,0.331372549019608,0.332352941176471,0.333333333333333,
0.334313725490196,0.335294117647059,0.336274509803922,0.337254901960784,
0.338235294117647,0.33921568627451,0.340196078431373,0.341176470588235,
0.342156862745098,0.343137254901961,0.344117647058824,0.345098039215686,
0.346078431372549,0.347058823529412,0.348039215686274,0.349019607843137,
0.35,0.350980392156863,0.351960784313726,0.352941176470588,0.353921568627451,
0.354901960784314,0.355882352941176,0.356862745098039,0.357843137254902,
0.358823529411765,0.359803921568627,0.36078431372549,0.361764705882353,
0.362745098039216,0.363725490196078,0.364705882352941,0.365686274509804,
0.366666666666667,0.367647058823529,0.368627450980392,0.369607843137255,
0.370588235294118,0.37156862745098,0.372549019607843,0.373529411764706,
0.374509803921569,0.375490196078431,0.376470588235294,0.377450980392157,
0.37843137254902,0.379411764705882,0.380392156862745,0.381372549019608,
0.382352941176471,0.383333333333333,0.384313725490196,0.385294117647059,
0.386274509803922,0.387254901960784,0.388235294117647,0.38921568627451,
0.390196078431373,0.391176470588235,0.392156862745098,0.393137254901961,
0.394117647058824,0.395098039215686,0.396078431372549,0.397058823529412,
0.398039215686274,0.399019607843137,0.4,0.400980392156863,0.401960784313726,
0.402941176470588,0.403921568627451,0.404901960784314,0.405882352941176,
0.406862745098039,0.407843137254902,0.408823529411765,0.409803921568627,
0.41078431372549,0.411764705882353,0.412745098039216,0.413725490196078,
0.414705882352941,0.415686274509804,0.416666666666667,0.417647058823529,
0.418627450980392,0.419607843137255,0.420588235294118,0.42156862745098,
0.422549019607843,0.423529411764706,0.424509803921569,0.425490196078431,
0.426470588235294,0.427450980392157,0.42843137254902,0.429411764705882,
0.430392156862745,0.431372549019608,0.432352941176471,0.433333333333333,
0.434313725490196,0.435294117647059,0.436274509803922,0.437254901960784,
0.438235294117647,0.43921568627451,0.440196078431373,0.441176470588235,
0.442156862745098,0.443137254901961,0.444117647058824,0.445098039215686,
0.446078431372549,0.447058823529412,0.448039215686275,0.449019607843137,
0.45,0.450980392156863,0.451960784313725,0.452941176470588,0.453921568627451,
0.454901960784314,0.455882352941176,0.456862745098039,0.457843137254902,
0.458823529411765,0.459803921568627,0.46078431372549,0.461764705882353,
0.462745098039216,0.463725490196078,0.464705882352941,0.465686274509804,
0.466666666666667,0.467647058823529,0.468627450980392,0.469607843137255,
0.470588235294118,0.47156862745098,0.472549019607843,0.473529411764706,
0.474509803921569,0.475490196078431,0.476470588235294,0.477450980392157,
0.47843137254902,0.479411764705882,0.480392156862745,0.481372549019608,
0.482352941176471,0.483333333333333,0.484313725490196,0.485294117647059,
0.486274509803922,0.487254901960784,0.488235294117647,0.48921568627451,
0.490196078431373,0.491176470588235,0.492156862745098,0.493137254901961,
0.494117647058824,0.495098039215686,0.496078431372549,0.497058823529412,
0.498039215686275,0.499019607843137,0.5,0.500980392156863,0.501960784313725,
0.502941176470588,0.503921568627451,0.504901960784314,0.505882352941176,
0.506862745098039,0.507843137254902,0.508823529411765,0.509803921568627,
0.51078431372549,0.511764705882353,0.512745098039216,0.513725490196078,
0.514705882352941,0.515686274509804,0.516666666666667,0.517647058823529,
0.518627450980392,0.519607843137255,0.520588235294118,0.52156862745098,
0.522549019607843,0.523529411764706,0.524509803921569,0.525490196078431,
0.526470588235294,0.527450980392157,0.52843137254902,0.529411764705882,
0.530392156862745,0.531372549019608,0.532352941176471,0.533333333333333,
0.534313725490196,0.535294117647059,0.536274509803922,0.537254901960784,
0.538235294117647,0.53921568627451,0.540196078431373,0.541176470588235,
0.542156862745098,0.543137254901961,0.544117647058823,0.545098039215686,
0.546078431372549,0.547058823529412,0.548039215686275,0.549019607843137,
0.55,0.550980392156863,0.551960784313726,0.552941176470588,0.553921568627451,
0.554901960784314,0.555882352941176,0.556862745098039,0.557843137254902,
0.558823529411765,0.559803921568627,0.56078431372549,0.561764705882353,
0.562745098039216,0.563725490196078,0.564705882352941,0.565686274509804,
0.566666666666667,0.567647058823529,0.568627450980392,0.569607843137255,
0.570588235294118,0.57156862745098,0.572549019607843,0.573529411764706,
0.574509803921569,0.575490196078431,0.576470588235294,0.577450980392157,
0.57843137254902,0.579411764705882,0.580392156862745,0.581372549019608,
0.582352941176471,0.583333333333333,0.584313725490196,0.585294117647059,
0.586274509803922,0.587254901960784,0.588235294117647,0.58921568627451,
0.590196078431373,0.591176470588235,0.592156862745098,0.593137254901961,
0.594117647058824,0.595098039215686,0.596078431372549,0.597058823529412,
0.598039215686274,0.599019607843137,0.6,0.600980392156863,0.601960784313725,
0.602941176470588,0.603921568627451,0.604901960784314,0.605882352941176,
0.606862745098039,0.607843137254902,0.608823529411765,0.609803921568628,
0.61078431372549,0.611764705882353,0.612745098039216,0.613725490196078,
0.614705882352941,0.615686274509804,0.616666666666667,0.617647058823529,
0.618627450980392,0.619607843137255,0.620588235294118,0.62156862745098,
0.622549019607843,0.623529411764706,0.624509803921569,0.625490196078431,
0.626470588235294,0.627450980392157,0.62843137254902,0.629411764705882,
0.630392156862745,0.631372549019608,0.632352941176471,0.633333333333333,
0.634313725490196,0.635294117647059,0.636274509803922,0.637254901960784,
0.638235294117647,0.63921568627451,0.640196078431372,0.641176470588235,
0.642156862745098,0.643137254901961,0.644117647058824,0.645098039215686,
0.646078431372549,0.647058823529412,0.648039215686275,0.649019607843137,
0.65,0.650980392156863,0.651960784313726,0.652941176470588,0.653921568627451,
0.654901960784314,0.655882352941176,0.656862745098039,0.657843137254902,
0.658823529411765,0.659803921568627,0.66078431372549,0.661764705882353,
0.662745098039216,0.663725490196078,0.664705882352941,0.665686274509804,
0.666666666666667,0.667647058823529,0.668627450980392,0.669607843137255,
0.670588235294118,0.67156862745098,0.672549019607843,0.673529411764706,
0.674509803921569,0.675490196078431,0.676470588235294,0.677450980392157,
0.67843137254902,0.679411764705882,0.680392156862745,0.681372549019608,
0.682352941176471,0.683333333333333,0.684313725490196,0.685294117647059,
0.686274509803922,0.687254901960784,0.688235294117647,0.68921568627451,
0.690196078431373,0.691176470588235,0.692156862745098,0.693137254901961,
0.694117647058824,0.695098039215686,0.696078431372549,0.697058823529412,
0.698039215686274,0.699019607843137,0.7,0.700980392156863,0.701960784313725,
0.702941176470588,0.703921568627451,0.704901960784314,0.705882352941177,
0.706862745098039,0.707843137254902,0.708823529411765,0.709803921568627,
0.71078431372549,0.711764705882353,0.712745098039216,0.713725490196078,
0.714705882352941,0.715686274509804,0.716666666666667,0.717647058823529,
0.718627450980392,0.719607843137255,0.720588235294118,0.72156862745098,
0.722549019607843,0.723529411764706,0.724509803921569,0.725490196078431,
0.726470588235294,0.727450980392157,0.72843137254902,0.729411764705882,
0.730392156862745,0.731372549019608,0.732352941176471,0.733333333333333,
0.734313725490196,0.735294117647059,0.736274509803922,0.737254901960784,
0.738235294117647,0.73921568627451,0.740196078431373,0.741176470588235,
0.742156862745098,0.743137254901961,0.744117647058824,0.745098039215686,
0.746078431372549,0.747058823529412,0.748039215686275,0.749019607843137,
0.75,0.750980392156863,0.751960784313725,0.752941176470588,0.753921568627451,
0.754901960784314,0.755882352941176,0.756862745098039,0.757843137254902,
0.758823529411765,0.759803921568627,0.76078431372549,0.761764705882353,
0.762745098039216,0.763725490196078,0.764705882352941,0.765686274509804,
0.766666666666667,0.767647058823529,0.768627450980392,0.769607843137255,
0.770588235294118,0.77156862745098,0.772549019607843,0.773529411764706,
0.774509803921569,0.775490196078431,0.776470588235294,0.777450980392157,
0.77843137254902,0.779411764705882,0.780392156862745,0.781372549019608,
0.782352941176471,0.783333333333333,0.784313725490196,0.785294117647059,
0.786274509803922,0.787254901960784,0.788235294117647,0.78921568627451,
0.790196078431373,0.791176470588235,0.792156862745098,0.793137254901961,
0.794117647058823,0.795098039215686,0.796078431372549,0.797058823529412,
0.798039215686275,0.799019607843137,0.8,0.800980392156863,0.801960784313726,
0.802941176470588,0.803921568627451,0.804901960784314,0.805882352941176,
0.806862745098039,0.807843137254902,0.808823529411765,0.809803921568627,
0.81078431372549,0.811764705882353,0.812745098039216,0.813725490196078,
0.814705882352941,0.815686274509804,0.816666666666667,0.817647058823529,
0.818627450980392,0.819607843137255,0.820588235294118,0.82156862745098,
0.822549019607843,0.823529411764706,0.824509803921569,0.825490196078431,
0.826470588235294,0.827450980392157,0.82843137254902,0.829411764705882,
0.830392156862745,0.831372549019608,0.832352941176471,0.833333333333333,
0.834313725490196,0.835294117647059,0.836274509803922,0.837254901960784,
0.838235294117647,0.83921568627451,0.840196078431373,0.841176470588235,
0.842156862745098,0.843137254901961,0.844117647058824,0.845098039215686,
0.846078431372549,0.847058823529412,0.848039215686274,0.849019607843137,
0.85,0.850980392156863,0.851960784313725,0.852941176470588,0.853921568627451,
0.854901960784314,0.855882352941176,0.856862745098039,0.857843137254902,
0.858823529411765,0.859803921568628,0.86078431372549,0.861764705882353,
0.862745098039216,0.863725490196078,0.864705882352941,0.865686274509804,
0.866666666666667,0.867647058823529,0.868627450980392,0.869607843137255,
0.870588235294118,0.87156862745098,0.872549019607843,0.873529411764706,
0.874509803921569,0.875490196078431,0.876470588235294,0.877450980392157,
0.87843137254902,0.879411764705882,0.880392156862745,0.881372549019608,
0.882352941176471,0.883333333333333,0.884313725490196,0.885294117647059,
0.886274509803922,0.887254901960784,0.888235294117647,0.88921568627451,
0.890196078431372,0.891176470588235,0.892156862745098,0.893137254901961,
0.894117647058824,0.895098039215686,0.896078431372549,0.897058823529412,
0.898039215686275,0.899019607843137,0.9,0.900980392156863,0.901960784313726,
0.902941176470588,0.903921568627451,0.904901960784314,0.905882352941176,
0.906862745098039,0.907843137254902,0.908823529411765,0.909803921568627,
0.91078431372549,0.911764705882353,0.912745098039216,0.913725490196078,
0.914705882352941,0.915686274509804,0.916666666666667,0.917647058823529,
0.918627450980392,0.919607843137255,0.920588235294118,0.92156862745098,
0.922549019607843,0.923529411764706,0.924509803921569,0.925490196078431,
0.926470588235294,0.927450980392157,0.92843137254902,0.929411764705882,
0.930392156862745,0.931372549019608,0.932352941176471,0.933333333333333,
0.934313725490196,0.935294117647059,0.936274509803922,0.937254901960784,
0.938235294117647,0.93921568627451,0.940196078431373,0.941176470588235,
0.942156862745098,0.943137254901961,0.944117647058824,0.945098039215686,
0.946078431372549,0.947058823529412,0.948039215686274,0.949019607843137,
0.95,0.950980392156863,0.951960784313725,0.952941176470588,0.953921568627451,
0.954901960784314,0.955882352941177,0.956862745098039,0.957843137254902,
0.958823529411765,0.959803921568627,0.96078431372549,0.961764705882353,
0.962745098039216,0.963725490196078,0.964705882352941,0.965686274509804,
0.966666666666667,0.967647058823529,0.968627450980392,0.969607843137255,
0.970588235294118,0.97156862745098,0.972549019607843,0.973529411764706,
0.974509803921569,0.975490196078431,0.976470588235294,0.977450980392157,
0.97843137254902,0.979411764705882,0.980392156862745,0.981372549019608,
0.982352941176471,0.983333333333333,0.984313725490196,0.985294117647059,
0.985937295874546,0.995796668833291),.UNSPECIFIED.)
GEOMETRIC_REPRESENTATION_ITEM()
RATIONAL_B_SPLINE_SURFACE(((1.,0.995734176295034,1.,0.995734176295034,1.,
0.995734176295034,1.,0.995734176295034,1.,0.995734176295034,1.,0.995734176295034,
1.,0.995734176295034,1.,0.995734176295034,1.,0.995734176295034,1.,0.995734176295034,
1.,0.995734176295034,1.,0.995734176295034,1.,0.995734176295034,1.,0.995734176295034,
1.,0.995734176295034,1.,0.995734176295034,1.,0.995734176295034,1.,0.995734176295034,
1.,0.995734176295034,1.,0.995734176295034,1.,0.995734176295034,1.,0.995734176295034,
1.,0.995734176295034,1.,0.995734176295034,1.,0.995734176295034,1.,0.995734176295034,
1.,0.995734176295034,1.,0.995734176295034,1.,0.995734176295034,1.,0.995734176295034,
1.,0.995734176295034,1.,0.995734176295034,1.,0.995734176295034,1.,0.995734176295034,
1.,0.995734176295034,1.,0.995734176295034,1.,0.995734176295034,1.,0.995734176295034,
1.,0.995734176295034,1.,0.995734176295034,1.,0.995734176295034,1.,0.995734176295034,
1.,0.995734176295034,1.,0.995734176295034,1.,0.995734176295034,1.,0.995734176295034,
1.,0.995734176295034,1.,0.995734176295034,1.,0.995734176295034,1.,0.995734176295034,
1.,0.995734176295034,1.,0.995734176295034,1.,0.995734176295034,1.,0.995734176295034,
1.,0.995734176295034,1.,0.995734176295034,1.,0.995734176295034,1.,0.995734176295034,
1.,0.995734176295034,1.,0.995734176295034,1.,0.995734176295034,1.,0.995734176295034,
1.,0.995734176295034,1.,0.995734176295034,1.,0.995734176295034,1.,0.995734176295034,
1.,0.995734176295034,1.,0.995734176295034,1.,0.995734176295034,1.,0.995734176295034,
1.,0.995734176295034,1.,0.995734176295034,1.,0.995734176295034,1.,0.995734176295034,
1.,0.995734176295034,1.,0.995734176295034,1.,0.995734176295034,1.,0.995734176295034,
1.,0.995734176295034,1.,0.995734176295034,1.,0.995734176295034,1.,0.995734176295034,
1.,0.995734176295034,1.,0.995734176295034,1.,0.995734176295034,1.,0.995734176295034,
1.,0.995734176295034,1.,0.995734176295034,1.,0.995734176295034,1.,0.995734176295034,
1.,0.995734176295034,1.,0.995734176295034,1.,0.995734176295034,1.,0.995734176295034,
1.,0.995734176295034,1.,0.995734176295034,1.,0.995734176295034,1.,0.995734176295034,
1.,0.995734176295034,1.,0.995734176295034,1.,0.995734176295034,1.,0.995734176295034,
1.,0.995734176295034,1.,0.995734176295034,1.,0.995734176295034,1.,0.995734176295034,
1.,0.995734176295034,1.,0.995734176295034,1.,0.995734176295034,1.,0.995734176295034,
1.,0.995734176295034,1.,0.995734176295034,1.,0.995734176295034,1.,0.995734176295034,
1.,0.995734176295034,1.,0.995734176295034,1.,0.995734176295034,1.,0.995734176295034,
1.,0.995734176295034,1.,0.995734176295034,1.,0.995734176295034,1.,0.995734176295034,
1.,0.995734176295034,1.,0.995734176295034,1.,0.995734176295034,1.,0.995734176295034,
1.,0.995734176295034,1.,0.995734176295034,1.,0.995734176295034,1.,0.995734176295034,
1.,0.995734176295034,1.,0.995734176295034,1.,0.995734176295034,1.,0.995734176295034,
1.,0.995734176295034,1.,0.995734176295034,1.,0.995734176295034,1.,0.995734176295034,
1.,0.995734176295034,1.,0.995734176295034,1.,0.995734176295034,1.,0.995734176295034,
1.,0.995734176295034,1.,0.995734176295034,1.,0.995734176295034,1.,0.995734176295034,
1.,0.995734176295034,1.,0.995734176295034,1.,0.995734176295034,1.,0.995734176295034,
1.,0.995734176295034,1.,0.995734176295034,1.,0.995734176295034,1.,0.995734176295034,
1.,0.995734176295034,1.,0.995734176295034,1.,0.995734176295034,1.,0.995734176295034,
1.,0.995734176295034,1.,0.995734176295034,1.,0.995734176295034,1.,0.995734176295034,
1.,0.995734176295034,1.,0.995734176295034,1.,0.995734176295034,1.,0.995734176295034,
1.,0.995734176295034,1.,0.995734176295034,1.,0.995734176295034,1.,0.995734176295034,
1.,0.995734176295034,1.,0.995734176295034,1.,0.995734176295034,1.,0.995734176295034,
1.,0.995734176295034,1.,0.995734176295034,1.,0.995734176295034,1.,0.995734176295034,
1.,0.995734176295034,1.,0.995734176295034,1.,0.995734176295034,1.,0.995734176295034,
1.,0.995734176295034,1.,0.995734176295034,1.,0.995734176295034,1.,0.995734176295034,
1.,0.995734176295034,1.,0.995734176295034,1.,0.995734176295034,1.,0.995734176295034,
1.,0.995734176295034,1.,0.995734176295034,1.,0.995734176295034,1.,0.995734176295034,
1.,0.995734176295034,1.,0.995734176295034,1.,0.995734176295034,1.,0.995734176295034,
1.,0.995734176295034,1.,0.995734176295034,1.,0.995734176295034,1.,0.995734176295034,
1.,0.995734176295034,1.,0.995734176295034,1.,0.995734176295034,1.,0.995734176295034,
1.,0.995734176295034,1.,0.995734176295034,1.,0.995734176295034,1.,0.995734176295034,
1.,0.995734176295034,1.,0.995734176295034,1.,0.995734176295034,1.,0.995734176295034,
1.,0.995734176295034,1.,0.995734176295034,1.,0.995734176295034,1.,0.995734176295034,
1.,0.995734176295034,1.,0.995734176295034,1.,0.995734176295034,1.,0.995734176295034,
1.,0.995734176295034,1.,0.995734176295034,1.,0.995734176295034,1.,0.995734176295034,
1.,0.995734176295034,1.,0.995734176295034,1.,0.995734176295034,1.,0.995734176295034,
1.,0.995734176295034,1.,0.995734176295034,1.,0.995734176295034,1.,0.995734176295034,
1.,0.995734176295034,1.,0.995734176295034,1.,0.995734176295034,1.,0.995734176295034,
1.,0.995734176295034,1.,0.995734176295034,1.,0.995734176295034,1.,0.995734176295034,
1.,0.995734176295034,1.,0.995734176295034,1.,0.995734176295034,1.,0.995734176295034,
1.,0.995734176295034,1.,0.995734176295034,1.,0.995734176295034,1.,0.995734176295034,
1.,0.995734176295034,1.,0.995734176295034,1.,0.995734176295034,1.,0.995734176295034,
1.,0.995734176295034,1.,0.995734176295034,1.,0.995734176295034,1.,0.995734176295034,
1.,0.995734176295034,1.,0.995734176295034,1.,0.995734176295034,1.,0.995734176295034,
1.,0.995734176295034,1.,0.995734176295034,1.,0.995734176295034,1.,0.995734176295034,
1.,0.995734176295034,1.,0.995734176295034,1.,0.995734176295034,1.,0.995734176295034,
1.,0.995734176295034,1.,0.995734176295034,1.,0.995734176295034,1.,0.995734176295034,
1.,0.995734176295034,1.,0.995734176295034,1.,0.995734176295034,1.,0.995734176295034,
1.,0.995734176295034,1.,0.995734176295034,1.,0.995734176295034,1.,0.995734176295034,
1.,0.995734176295034,1.,0.995734176295034,1.,0.995734176295034,1.,0.995734176295034,
1.,0.995734176295034,1.,0.995734176295034,1.,0.995734176295034,1.,0.995734176295034,
1.,0.995734176295034,1.,0.995734176295034,1.,0.995734176295034,1.,0.995734176295034,
1.,0.995734176295034,1.,0.995734176295034,1.,0.995734176295034,1.,0.995734176295034,
1.,0.995734176295034,1.,0.995734176295034,1.,0.995734176295034,1.,0.995734176295034,
1.,0.995734176295034,1.,0.995734176295034,1.,0.995734176295034,1.,0.995734176295034,
1.,0.995734176295034,1.,0.995734176295034,1.,0.995734176295034,1.,0.995734176295034,
1.,0.995734176295034,1.,0.995734176295034,1.,0.995734176295034,1.,0.995734176295034,
1.,0.995734176295034,1.,0.995734176295034,1.,0.995734176295034,1.,0.995734176295034,
1.,0.995734176295034,1.,0.995734176295034,1.,0.995734176295034,1.,0.995734176295034,
1.,0.995734176295034,1.,0.995734176295034,1.,0.995734176295034,1.,0.995734176295034,
1.,0.995734176295034,1.,0.995734176295034,1.,0.995734176295034,1.,0.995734176295034,
1.,0.995734176295034,1.,0.995734176295034,1.,0.995734176295034,1.,0.995734176295034,
1.,0.995734176295034,1.,0.995734176295034,1.,0.995734176295034,1.,0.995734176295034,
1.,0.995734176295034,1.,0.995734176295034,1.,0.995734176295034,1.,0.995734176295034,
1.,0.995734176295034,1.,0.995734176295034,1.,0.995734176295034,1.,0.995734176295034,
1.,0.995734176295034,1.,0.995734176295034,1.,0.995734176295034,1.,0.995734176295034,
1.,0.995734176295034,1.,0.995734176295034,1.,0.995734176295034,1.,0.995734176295034,
1.,0.995734176295034,1.,0.995734176295034,1.,0.995734176295034,1.,0.995734176295034,
1.,0.995734176295034,1.,0.995734176295034,1.,0.995734176295034,1.,0.995734176295034,
1.,0.995734176295034,1.,0.995734176295034,1.,0.995734176295034,1.,0.995734176295034,
1.,0.995734176295034,1.,0.995734176295034,1.,0.995734176295034,1.,0.995734176295034,
1.,0.995734176295034,1.,0.995734176295034,1.,0.995734176295034,1.,0.995734176295034,
1.,0.995734176295034,1.,0.995734176295034,1.,0.995734176295034,1.,0.995734176295034,
1.,0.995734176295034,1.,0.995734176295034,1.,0.995734176295034,1.,0.995734176295034,
1.,0.995734176295034,1.,0.995734176295034,1.,0.995734176295034,1.,0.995734176295034,
1.,0.995734176295034,1.,0.995734176295034,1.,0.995734176295034,1.,0.995734176295034,
1.,0.995734176295034,1.,0.995734176295034,1.,0.995734176295034,1.,0.995734176295034,
1.,0.995734176295034,1.,0.995734176295034,1.,0.995734176295034,1.,0.995734176295034,
1.,0.995734176295034,1.,0.995734176295034,1.,0.995734176295034,1.,0.995734176295034,
1.,0.995734176295034,1.,0.995734176295034,1.,0.995734176295034,1.,0.995734176295034,
1.,0.995734176295034,1.,0.995734176295034,1.,0.995734176295034,1.,0.995734176295034,
1.,0.995734176295034,1.,0.995734176295034,1.,0.995734176295034,1.,0.995734176295034,
1.,0.995734176295034,1.,0.995734176295034,1.,0.995734176295034,1.,0.995734176295034,
1.,0.995734176295034,1.,0.995734176295034,1.,0.995734176295034,1.,0.995734176295034,
1.,0.995734176295034,1.,0.995734176295034,1.,0.995734176295034,1.,0.995734176295034,
1.,0.995734176295034,1.,0.995734176295034,1.,0.995734176295034,1.,0.995734176295034,
1.,0.995734176295034,1.,0.995734176295034,1.,0.995734176295034,1.,0.995734176295034,
1.,0.995734176295034,1.,0.995734176295034,1.,0.995734176295034,1.,0.995734176295034,
1.,0.995734176295034,1.,0.995734176295034,1.,0.995734176295034,1.,0.995734176295034,
1.,0.995734176295034,1.,0.995734176295034,1.,0.995734176295034,1.,0.995734176295034,
1.,0.995734176295034,1.,0.995734176295034,1.,0.995734176295034,1.,0.995734176295034,
1.,0.995734176295034,1.,0.995734176295034,1.,0.995734176295034,1.,0.995734176295034,
1.,0.995734176295034,1.,0.995734176295034,1.,0.995734176295034,1.,0.995734176295034,
1.,0.995734176295034,1.,0.995734176295034,1.,0.995734176295034,1.,0.995734176295034,
1.,0.995734176295034,1.,0.995734176295034,1.,0.995734176295034,1.,0.995734176295034,
1.,0.995734176295034,1.,0.995734176295034,1.,0.995734176295034,1.,0.995734176295034,
1.,0.995734176295034,1.,0.995734176295034,1.,0.995734176295034,1.,0.995734176295034,
1.,0.995734176295034,1.,0.995734176295034,1.,0.995734176295034,1.,0.995734176295034,
1.,0.995734176295034,1.,0.995734176295034,1.,0.995734176295034,1.,0.995734176295034,
1.,0.995734176295034,1.,0.995734176295034,1.,0.995734176295034,1.,0.995734176295034,
1.,0.995734176295034,1.,0.995734176295034,1.,0.995734176295034,1.,0.995734176295034,
1.,0.995734176295034,1.,0.995734176295034,1.,0.995734176295034,1.,0.995734176295034,
1.,0.995734176295034,1.,0.995734176295034,1.,0.995734176295034,1.,0.995734176295034,
1.,0.995734176295034,1.,0.995734176295034,1.,0.995734176295034,1.,0.995734176295034,
1.,0.995734176295034,1.,0.995734176295034,1.,0.995734176295034,1.,0.995734176295034,
1.,0.995734176295034,1.,0.995734176295034,1.,0.995734176295034,1.,0.995734176295034,
1.,0.995734176295034,1.,0.995734176295034,1.,0.995734176295034,1.,0.995734176295034,
1.,0.995734176295034,1.,0.995734176295034,1.,0.995734176295034,1.,0.995734176295034,
1.,0.995734176295034,1.,0.995734176295034,1.,0.995734176295034,1.,0.995734176295034,
1.,0.995734176295034,1.,0.995734176295034,1.,0.995734176295034,1.,0.995734176295034,
1.,0.995734176295034,1.,0.995734176295034,1.,0.995734176295034,1.,0.995734176295034,
1.,0.995734176295034,1.,0.995734176295034,1.,0.995734176295034,1.,0.995734176295034,
1.,0.995734176295034,1.,0.995734176295034,1.,0.995734176295034,1.,0.995734176295034,
1.,0.995734176295034,1.,0.995734176295034,1.,0.995734176295034,1.,0.995734176295034,
1.,0.995734176295034,1.,0.995734176295034,1.,0.995734176295034,1.,0.995734176295034,
1.,0.995734176295034,1.,0.995734176295034,1.,0.995734176295034,1.,0.995734176295034,
1.,0.995734176295034,1.,0.995734176295034,1.,0.995734176295034,1.,0.995734176295034,
1.,0.995734176295034,1.,0.995734176295034,1.,0.995734176295034,1.,0.995734176295034,
1.,0.995734176295034,1.,0.995734176295034,1.,0.995734176295034,1.,0.995734176295034,
1.,0.995734176295034,1.,0.995734176295034,1.,0.995734176295034,1.,0.995734176295034,
1.,0.995734176295034,1.,0.995734176295034,1.,0.995734176295034,1.,0.995734176295034,
1.,0.995734176295034,1.,0.995734176295034,1.,0.995734176295034,1.,0.995734176295034,
1.,0.995734176295034,1.,0.995734176295034,1.,0.995734176295034,1.,0.995734176295034,
1.,0.995734176295034,1.,0.995734176295034,1.,0.995734176295034,1.,0.995734176295034,
1.,0.995734176295034,1.,0.995734176295034,1.,0.995734176295034,1.,0.995734176295034,
1.,0.995734176295034,1.,0.995734176295034,1.,0.995734176295034,1.,0.995734176295034,
1.,0.995734176295034,1.,0.995734176295034,1.,0.995734176295034,1.,0.995734176295034,
1.,0.995734176295034,1.,0.995734176295034,1.,0.995734176295034,1.,0.995734176295034,
1.,0.995734176295034,1.,0.995734176295034,1.,0.995734176295034,1.,0.995734176295034,
1.,0.995734176295034,1.,0.995734176295034,1.,0.995734176295034,1.,0.995734176295034,
1.,0.995734176295034,1.,0.995734176295034,1.,0.995734176295034,1.,0.995734176295034,
1.,0.995734176295034,1.,0.995734176295034,1.,0.995734176295034,1.,0.995734176295034,
1.,0.995734176295034,1.,0.995734176295034,1.,0.995734176295034,1.,0.995734176295034,
1.,0.995734176295034,1.,0.995734176295034,1.,0.995734176295034,1.,0.995734176295034,
1.,0.995734176295034,1.,0.995734176295034,1.,0.995734176295034,1.,0.995734176295034,
1.,0.995734176295034,1.,0.995734176295034,1.,0.995734176295034,1.,0.995734176295034,
1.,0.995734176295034,1.,0.995734176295034,1.,0.995734176295034,1.,0.995734176295034,
1.,0.995734176295034,1.,0.995734176295034,1.,0.995734176295034,1.,0.995734176295034,
1.,0.995734176295034,1.,0.995734176295034,1.,0.995734176295034,1.,0.995734176295034,
1.,0.995734176295034,1.,0.995734176295034,1.,0.995734176295034,1.,0.995734176295034,
1.,0.995734176295034,1.,0.995734176295034,1.,0.995734176295034,1.,0.995734176295034,
1.,0.995734176295034,1.,0.995734176295034,1.,0.995734176295034,1.,0.995734176295034,
1.,0.995734176295034,1.,0.995734176295034,1.,0.995734176295034,1.,0.995734176295034,
1.,0.995734176295034,1.,0.995734176295034,1.,0.995734176295034,1.,0.995734176295034,
1.,0.995734176295034,1.,0.995734176295034,1.,0.995734176295034,1.,0.995734176295034,
1.,0.995734176295034,1.,0.995734176295034,1.,0.995734176295034,1.,0.995734176295034,
1.,0.995734176295034,1.,0.995734176295034,1.,0.995734176295034,1.,0.995734176295034,
1.,0.995734176295034,1.,0.995734176295034,1.,0.995734176295034,1.,0.995734176295034,
1.,0.995734176295034,1.,0.995734176295034,1.,0.995734176295034,1.,0.995734176295034,
1.,0.995734176295034,1.,0.995734176295034,1.,0.995734176295034,1.,0.995734176295034,
1.,0.995734176295034,1.,0.995734176295034,1.,0.995734176295034,1.,0.995734176295034,
1.,0.995734176295034,1.,0.995734176295034,1.,0.995734176295034,1.,0.995734176295034,
1.,0.995734176295034,1.,0.995734176295034,1.,0.995734176295034,1.,0.995734176295034,
1.,0.995734176295034,1.,0.995734176295034,1.,0.995734176295034,1.,0.995734176295034,
1.,0.995734176295034,1.,0.995734176295034,1.,0.995734176295034,1.,0.995734176295034,
1.,0.995734176295034,1.,0.995734176295034,1.,0.995734176295034,1.,0.995734176295034,
1.,0.995734176295034,1.,0.995734176295034,1.,0.995734176295034,1.,0.995734176295034,
1.,0.995734176295034,1.,0.995734176295034,1.,0.995734176295034,1.,0.995734176295034,
1.,0.995734176295034,1.,0.995734176295034,1.,0.995734176295034,1.,0.995734176295034,
1.,0.995734176295034,1.,0.995734176295034,1.,0.995734176295034,1.,0.995734176295034,
1.,0.995734176295034,1.,0.995734176295034,1.,0.995734176295034,1.,0.995734176295034,
1.,0.995734176295034,1.,0.995734176295034,1.,0.995734176295034,1.,0.995734176295034,
1.,0.995734176295034,1.,0.995734176295034,1.,0.995734176295034,1.,0.995734176295034,
1.,0.995734176295034,1.,0.995734176295034,1.,0.995734176295034,1.,0.995734176295034,
1.,0.995734176295034,1.,0.995734176295034,1.,0.995734176295034,1.,0.995734176295034,
1.,0.995734176295034,1.,0.995734176295034,1.,0.995734176295034,1.,0.995734176295034,
1.,0.995734176295034,1.,0.995734176295034,1.,0.995734176295034,1.,0.995734176295034,
1.,0.995734176295034,1.,0.995734176295034,1.,0.995734176295034,1.,0.995734176295034,
1.,0.995734176295034,1.,0.995734176295034,1.,0.995734176295034,1.,0.995734176295034,
1.,0.995734176295034,1.,0.995734176295034,1.,0.995734176295034,1.,0.995734176295034,
1.,0.995734176295034,1.,0.995734176295034,1.,0.995734176295034,1.,0.995734176295034,
1.,0.995734176295034,1.,0.995734176295034,1.,0.995734176295034,1.,0.995734176295034,
1.,0.995734176295034,1.,0.995734176295034,1.,0.995734176295034,1.,0.995734176295034,
1.,0.995734176295034,1.,0.995734176295034,1.,0.995734176295034,1.,0.995734176295034,
1.,0.995734176295034,1.,0.995734176295034,1.,0.995734176295034,1.,0.995734176295034,
1.,0.995734176295034,1.,0.995734176295034,1.,0.995734176295034,1.,0.995734176295034,
1.,0.995734176295034,1.,0.995734176295034,1.,0.995734176295034,1.,0.995734176295034,
1.,0.995734176295034,1.,0.995734176295034,1.,0.995734176295034,1.,0.995734176295034,
1.,0.995734176295034,1.,0.995734176295034,1.,0.995734176295034,1.,0.995734176295034,
1.,0.995734176295034,1.,0.995734176295034,1.,0.995734176295034,1.,0.995734176295034,
1.,0.995734176295034,1.,0.995734176295034,1.,0.995734176295034,1.,0.995734176295034,
1.,0.995734176295034,1.,0.995734176295034,1.,0.995734176295034,1.,0.995734176295034,
1.,0.995734176295034,1.,0.995734176295034,1.,0.995734176295034,1.,0.995734176295034,
1.,0.995734176295034,1.,0.995734176295034,1.,0.995734176295034,1.,0.995734176295034,
1.,0.995734176295034,1.,0.995734176295034,1.,0.995734176295034,1.,0.995734176295034,
1.,0.995734176295034,1.,0.995734176295034,1.,0.995734176295034,1.,0.995734176295034,
1.,0.995734176295034,1.,0.995734176295034,1.,0.995734176295034,1.,0.995734176295034,
1.,0.995734176295034,1.,0.995734176295034,1.,0.995734176295034,1.,0.995734176295034,
1.,0.995734176295034,1.,0.995734176295034,1.,0.995734176295034,1.,0.995734176295034,
1.,0.995734176295034,1.,0.995734176295034,1.,0.995734176295034,1.,0.995734176295034,
1.,0.995734176295034,1.,0.995734176295034,1.,0.995734176295034,1.,0.995734176295034,
1.,0.995734176295034,1.,0.995734176295034,1.,0.995734176295034,1.,0.995734176295034,
1.,0.995734176295034,1.,0.995734176295034,1.,0.995734176295034,1.,0.995734176295034,
1.,0.995734176295034,1.,0.995734176295034,1.,0.995734176295034,1.,0.995734176295034,
1.,0.995734176295034,1.,0.995734176295034,1.,0.995734176295034,1.,0.995734176295034,
1.,0.995734176295034,1.,0.995734176295034,1.,0.995734176295034,1.,0.995734176295034,
1.,0.995734176295034,1.,0.995734176295034,1.,0.995734176295034,1.,0.995734176295034,
1.,0.995734176295034,1.,0.995734176295034,1.,0.995734176295034,1.,0.995734176295034,
1.,0.995734176295034,1.,0.995734176295034,1.,0.995734176295034,1.,0.995734176295034,
1.,0.995734176295034,1.,0.995734176295034,1.,0.995734176295034,1.,0.995734176295034,
1.,0.995734176295034,1.,0.995734176295034,1.,0.995734176295034,1.,0.995734176295034,
1.,0.995734176295034,1.,0.995734176295034,1.,0.995734176295034,1.,0.995734176295034,
1.,0.995734176295034,1.,0.995734176295034,1.,0.995734176295034,1.,0.995734176295034,
1.,0.995734176295034,1.,0.995734176295034,1.,0.995734176295034,1.,0.995734176295034,
1.,0.995734176295034,1.,0.995734176295034,1.,0.995734176295034,1.,0.995734176295034,
1.,0.995734176295034,1.,0.995734176295034,1.,0.995734176295034,1.,0.995734176295034,
1.,0.995734176295034,1.,0.995734176295034,1.,0.995734176295034,1.,0.995734176295034,
1.,0.995734176295034,1.,0.995734176295034,1.,0.995734176295034,1.,0.995734176295034,
1.,0.995734176295034,1.,0.995734176295034,1.,0.995734176295034,1.,0.995734176295034,
1.,0.995734176295034,1.,0.995734176295034,1.,0.995734176295034,1.,0.995734176295034,
1.,0.995734176295034,1.,0.995734176295034,1.,0.995734176295034,1.,0.995734176295034,
1.,0.995734176295034,1.,0.995734176295034,1.,0.995734176295034,1.,0.995734176295034,
1.,0.995734176295034,1.,0.995734176295034,1.,0.995734176295034,1.,0.995734176295034,
1.,0.995734176295034,1.,0.995734176295034,1.,0.995734176295034,1.,0.995734176295034,
1.,0.995734176295034,1.,0.995734176295034,1.,0.995734176295034,1.,0.995734176295034,
1.,0.995734176295034,1.,0.995734176295034,1.,0.995734176295034,1.,0.995734176295034,
1.,0.995734176295034,1.,0.995734176295034,1.,0.995734176295034,1.,0.995734176295034,
1.,0.995734176295034,1.,0.995734176295034,1.,0.995734176295034,1.,0.995734176295034,
1.,0.995734176295034,1.,0.995734176295034,1.,0.995734176295034,1.,0.995734176295034,
1.,0.995734176295034,1.,0.995734176295034,1.,0.995734176295034,1.,0.995734176295034,
1.,0.995734176295034,1.,0.995734176295034,1.,0.995734176295034,1.,0.995734176295034,
1.,0.995734176295034,1.,0.995734176295034,1.,0.995734176295034,1.,0.995734176295034,
1.,0.995734176295034,1.,0.995734176295034,1.,0.995734176295034,1.,0.995734176295034,
1.,0.995734176295034,1.,0.995734176295034,1.,0.995734176295034,1.,0.995734176295034,
1.,0.995734176295034,1.,0.995734176295034,1.,0.995734176295034,1.,0.995734176295034,
1.,0.995734176295034,1.,0.995734176295034,1.,0.995734176295034,1.,0.995734176295034,
1.,0.995734176295034,1.,0.995734176295034,1.,0.995734176295034,1.,0.995734176295034,
1.,0.995734176295034,1.,0.995734176295034,1.,0.995734176295034,1.,0.995734176295034,
1.,0.995734176295034,1.,0.995734176295034,1.,0.995734176295034,1.,0.995734176295034,
1.,0.995734176295034,1.,0.995734176295034,1.,0.995734176295034,1.,0.997201441372082,
0.998074825578922,0.998074825578922,0.998074825578922),(1.,0.995734176295034,
1.,0.995734176295034,1.,0.995734176295034,1.,0.995734176295034,1.,0.995734176295034,
1.,0.995734176295034,1.,0.995734176295034,1.,0.995734176295034,1.,0.995734176295034,
1.,0.995734176295034,1.,0.995734176295034,1.,0.995734176295034,1.,0.995734176295034,
1.,0.995734176295034,1.,0.995734176295034,1.,0.995734176295034,1.,0.995734176295034,
1.,0.995734176295034,1.,0.995734176295034,1.,0.995734176295034,1.,0.995734176295034,
1.,0.995734176295034,1.,0.995734176295034,1.,0.995734176295034,1.,0.995734176295034,
1.,0.995734176295034,1.,0.995734176295034,1.,0.995734176295034,1.,0.995734176295034,
1.,0.995734176295034,1.,0.995734176295034,1.,0.995734176295034,1.,0.995734176295034,
1.,0.995734176295034,1.,0.995734176295034,1.,0.995734176295034,1.,0.995734176295034,
1.,0.995734176295034,1.,0.995734176295034,1.,0.995734176295034,1.,0.995734176295034,
1.,0.995734176295034,1.,0.995734176295034,1.,0.995734176295034,1.,0.995734176295034,
1.,0.995734176295034,1.,0.995734176295034,1.,0.995734176295034,1.,0.995734176295034,
1.,0.995734176295034,1.,0.995734176295034,1.,0.995734176295034,1.,0.995734176295034,
1.,0.995734176295034,1.,0.995734176295034,1.,0.995734176295034,1.,0.995734176295034,
1.,0.995734176295034,1.,0.995734176295034,1.,0.995734176295034,1.,0.995734176295034,
1.,0.995734176295034,1.,0.995734176295034,1.,0.995734176295034,1.,0.995734176295034,
1.,0.995734176295034,1.,0.995734176295034,1.,0.995734176295034,1.,0.995734176295034,
1.,0.995734176295034,1.,0.995734176295034,1.,0.995734176295034,1.,0.995734176295034,
1.,0.995734176295034,1.,0.995734176295034,1.,0.995734176295034,1.,0.995734176295034,
1.,0.995734176295034,1.,0.995734176295034,1.,0.995734176295034,1.,0.995734176295034,
1.,0.995734176295034,1.,0.995734176295034,1.,0.995734176295034,1.,0.995734176295034,
1.,0.995734176295034,1.,0.995734176295034,1.,0.995734176295034,1.,0.995734176295034,
1.,0.995734176295034,1.,0.995734176295034,1.,0.995734176295034,1.,0.995734176295034,
1.,0.995734176295034,1.,0.995734176295034,1.,0.995734176295034,1.,0.995734176295034,
1.,0.995734176295034,1.,0.995734176295034,1.,0.995734176295034,1.,0.995734176295034,
1.,0.995734176295034,1.,0.995734176295034,1.,0.995734176295034,1.,0.995734176295034,
1.,0.995734176295034,1.,0.995734176295034,1.,0.995734176295034,1.,0.995734176295034,
1.,0.995734176295034,1.,0.995734176295034,1.,0.995734176295034,1.,0.995734176295034,
1.,0.995734176295034,1.,0.995734176295034,1.,0.995734176295034,1.,0.995734176295034,
1.,0.995734176295034,1.,0.995734176295034,1.,0.995734176295034,1.,0.995734176295034,
1.,0.995734176295034,1.,0.995734176295034,1.,0.995734176295034,1.,0.995734176295034,
1.,0.995734176295034,1.,0.995734176295034,1.,0.995734176295034,1.,0.995734176295034,
1.,0.995734176295034,1.,0.995734176295034,1.,0.995734176295034,1.,0.995734176295034,
1.,0.995734176295034,1.,0.995734176295034,1.,0.995734176295034,1.,0.995734176295034,
1.,0.995734176295034,1.,0.995734176295034,1.,0.995734176295034,1.,0.995734176295034,
1.,0.995734176295034,1.,0.995734176295034,1.,0.995734176295034,1.,0.995734176295034,
1.,0.995734176295034,1.,0.995734176295034,1.,0.995734176295034,1.,0.995734176295034,
1.,0.995734176295034,1.,0.995734176295034,1.,0.995734176295034,1.,0.995734176295034,
1.,0.995734176295034,1.,0.995734176295034,1.,0.995734176295034,1.,0.995734176295034,
1.,0.995734176295034,1.,0.995734176295034,1.,0.995734176295034,1.,0.995734176295034,
1.,0.995734176295034,1.,0.995734176295034,1.,0.995734176295034,1.,0.995734176295034,
1.,0.995734176295034,1.,0.995734176295034,1.,0.995734176295034,1.,0.995734176295034,
1.,0.995734176295034,1.,0.995734176295034,1.,0.995734176295034,1.,0.995734176295034,
1.,0.995734176295034,1.,0.995734176295034,1.,0.995734176295034,1.,0.995734176295034,
1.,0.995734176295034,1.,0.995734176295034,1.,0.995734176295034,1.,0.995734176295034,
1.,0.995734176295034,1.,0.995734176295034,1.,0.995734176295034,1.,0.995734176295034,
1.,0.995734176295034,1.,0.995734176295034,1.,0.995734176295034,1.,0.995734176295034,
1.,0.995734176295034,1.,0.995734176295034,1.,0.995734176295034,1.,0.995734176295034,
1.,0.995734176295034,1.,0.995734176295034,1.,0.995734176295034,1.,0.995734176295034,
1.,0.995734176295034,1.,0.995734176295034,1.,0.995734176295034,1.,0.995734176295034,
1.,0.995734176295034,1.,0.995734176295034,1.,0.995734176295034,1.,0.995734176295034,
1.,0.995734176295034,1.,0.995734176295034,1.,0.995734176295034,1.,0.995734176295034,
1.,0.995734176295034,1.,0.995734176295034,1.,0.995734176295034,1.,0.995734176295034,
1.,0.995734176295034,1.,0.995734176295034,1.,0.995734176295034,1.,0.995734176295034,
1.,0.995734176295034,1.,0.995734176295034,1.,0.995734176295034,1.,0.995734176295034,
1.,0.995734176295034,1.,0.995734176295034,1.,0.995734176295034,1.,0.995734176295034,
1.,0.995734176295034,1.,0.995734176295034,1.,0.995734176295034,1.,0.995734176295034,
1.,0.995734176295034,1.,0.995734176295034,1.,0.995734176295034,1.,0.995734176295034,
1.,0.995734176295034,1.,0.995734176295034,1.,0.995734176295034,1.,0.995734176295034,
1.,0.995734176295034,1.,0.995734176295034,1.,0.995734176295034,1.,0.995734176295034,
1.,0.995734176295034,1.,0.995734176295034,1.,0.995734176295034,1.,0.995734176295034,
1.,0.995734176295034,1.,0.995734176295034,1.,0.995734176295034,1.,0.995734176295034,
1.,0.995734176295034,1.,0.995734176295034,1.,0.995734176295034,1.,0.995734176295034,
1.,0.995734176295034,1.,0.995734176295034,1.,0.995734176295034,1.,0.995734176295034,
1.,0.995734176295034,1.,0.995734176295034,1.,0.995734176295034,1.,0.995734176295034,
1.,0.995734176295034,1.,0.995734176295034,1.,0.995734176295034,1.,0.995734176295034,
1.,0.995734176295034,1.,0.995734176295034,1.,0.995734176295034,1.,0.995734176295034,
1.,0.995734176295034,1.,0.995734176295034,1.,0.995734176295034,1.,0.995734176295034,
1.,0.995734176295034,1.,0.995734176295034,1.,0.995734176295034,1.,0.995734176295034,
1.,0.995734176295034,1.,0.995734176295034,1.,0.995734176295034,1.,0.995734176295034,
1.,0.995734176295034,1.,0.995734176295034,1.,0.995734176295034,1.,0.995734176295034,
1.,0.995734176295034,1.,0.995734176295034,1.,0.995734176295034,1.,0.995734176295034,
1.,0.995734176295034,1.,0.995734176295034,1.,0.995734176295034,1.,0.995734176295034,
1.,0.995734176295034,1.,0.995734176295034,1.,0.995734176295034,1.,0.995734176295034,
1.,0.995734176295034,1.,0.995734176295034,1.,0.995734176295034,1.,0.995734176295034,
1.,0.995734176295034,1.,0.995734176295034,1.,0.995734176295034,1.,0.995734176295034,
1.,0.995734176295034,1.,0.995734176295034,1.,0.995734176295034,1.,0.995734176295034,
1.,0.995734176295034,1.,0.995734176295034,1.,0.995734176295034,1.,0.995734176295034,
1.,0.995734176295034,1.,0.995734176295034,1.,0.995734176295034,1.,0.995734176295034,
1.,0.995734176295034,1.,0.995734176295034,1.,0.995734176295034,1.,0.995734176295034,
1.,0.995734176295034,1.,0.995734176295034,1.,0.995734176295034,1.,0.995734176295034,
1.,0.995734176295034,1.,0.995734176295034,1.,0.995734176295034,1.,0.995734176295034,
1.,0.995734176295034,1.,0.995734176295034,1.,0.995734176295034,1.,0.995734176295034,
1.,0.995734176295034,1.,0.995734176295034,1.,0.995734176295034,1.,0.995734176295034,
1.,0.995734176295034,1.,0.995734176295034,1.,0.995734176295034,1.,0.995734176295034,
1.,0.995734176295034,1.,0.995734176295034,1.,0.995734176295034,1.,0.995734176295034,
1.,0.995734176295034,1.,0.995734176295034,1.,0.995734176295034,1.,0.995734176295034,
1.,0.995734176295034,1.,0.995734176295034,1.,0.995734176295034,1.,0.995734176295034,
1.,0.995734176295034,1.,0.995734176295034,1.,0.995734176295034,1.,0.995734176295034,
1.,0.995734176295034,1.,0.995734176295034,1.,0.995734176295034,1.,0.995734176295034,
1.,0.995734176295034,1.,0.995734176295034,1.,0.995734176295034,1.,0.995734176295034,
1.,0.995734176295034,1.,0.995734176295034,1.,0.995734176295034,1.,0.995734176295034,
1.,0.995734176295034,1.,0.995734176295034,1.,0.995734176295034,1.,0.995734176295034,
1.,0.995734176295034,1.,0.995734176295034,1.,0.995734176295034,1.,0.995734176295034,
1.,0.995734176295034,1.,0.995734176295034,1.,0.995734176295034,1.,0.995734176295034,
1.,0.995734176295034,1.,0.995734176295034,1.,0.995734176295034,1.,0.995734176295034,
1.,0.995734176295034,1.,0.995734176295034,1.,0.995734176295034,1.,0.995734176295034,
1.,0.995734176295034,1.,0.995734176295034,1.,0.995734176295034,1.,0.995734176295034,
1.,0.995734176295034,1.,0.995734176295034,1.,0.995734176295034,1.,0.995734176295034,
1.,0.995734176295034,1.,0.995734176295034,1.,0.995734176295034,1.,0.995734176295034,
1.,0.995734176295034,1.,0.995734176295034,1.,0.995734176295034,1.,0.995734176295034,
1.,0.995734176295034,1.,0.995734176295034,1.,0.995734176295034,1.,0.995734176295034,
1.,0.995734176295034,1.,0.995734176295034,1.,0.995734176295034,1.,0.995734176295034,
1.,0.995734176295034,1.,0.995734176295034,1.,0.995734176295034,1.,0.995734176295034,
1.,0.995734176295034,1.,0.995734176295034,1.,0.995734176295034,1.,0.995734176295034,
1.,0.995734176295034,1.,0.995734176295034,1.,0.995734176295034,1.,0.995734176295034,
1.,0.995734176295034,1.,0.995734176295034,1.,0.995734176295034,1.,0.995734176295034,
1.,0.995734176295034,1.,0.995734176295034,1.,0.995734176295034,1.,0.995734176295034,
1.,0.995734176295034,1.,0.995734176295034,1.,0.995734176295034,1.,0.995734176295034,
1.,0.995734176295034,1.,0.995734176295034,1.,0.995734176295034,1.,0.995734176295034,
1.,0.995734176295034,1.,0.995734176295034,1.,0.995734176295034,1.,0.995734176295034,
1.,0.995734176295034,1.,0.995734176295034,1.,0.995734176295034,1.,0.995734176295034,
1.,0.995734176295034,1.,0.995734176295034,1.,0.995734176295034,1.,0.995734176295034,
1.,0.995734176295034,1.,0.995734176295034,1.,0.995734176295034,1.,0.995734176295034,
1.,0.995734176295034,1.,0.995734176295034,1.,0.995734176295034,1.,0.995734176295034,
1.,0.995734176295034,1.,0.995734176295034,1.,0.995734176295034,1.,0.995734176295034,
1.,0.995734176295034,1.,0.995734176295034,1.,0.995734176295034,1.,0.995734176295034,
1.,0.995734176295034,1.,0.995734176295034,1.,0.995734176295034,1.,0.995734176295034,
1.,0.995734176295034,1.,0.995734176295034,1.,0.995734176295034,1.,0.995734176295034,
1.,0.995734176295034,1.,0.995734176295034,1.,0.995734176295034,1.,0.995734176295034,
1.,0.995734176295034,1.,0.995734176295034,1.,0.995734176295034,1.,0.995734176295034,
1.,0.995734176295034,1.,0.995734176295034,1.,0.995734176295034,1.,0.995734176295034,
1.,0.995734176295034,1.,0.995734176295034,1.,0.995734176295034,1.,0.995734176295034,
1.,0.995734176295034,1.,0.995734176295034,1.,0.995734176295034,1.,0.995734176295034,
1.,0.995734176295034,1.,0.995734176295034,1.,0.995734176295034,1.,0.995734176295034,
1.,0.995734176295034,1.,0.995734176295034,1.,0.995734176295034,1.,0.995734176295034,
1.,0.995734176295034,1.,0.995734176295034,1.,0.995734176295034,1.,0.995734176295034,
1.,0.995734176295034,1.,0.995734176295034,1.,0.995734176295034,1.,0.995734176295034,
1.,0.995734176295034,1.,0.995734176295034,1.,0.995734176295034,1.,0.995734176295034,
1.,0.995734176295034,1.,0.995734176295034,1.,0.995734176295034,1.,0.995734176295034,
1.,0.995734176295034,1.,0.995734176295034,1.,0.995734176295034,1.,0.995734176295034,
1.,0.995734176295034,1.,0.995734176295034,1.,0.995734176295034,1.,0.995734176295034,
1.,0.995734176295034,1.,0.995734176295034,1.,0.995734176295034,1.,0.995734176295034,
1.,0.995734176295034,1.,0.995734176295034,1.,0.995734176295034,1.,0.995734176295034,
1.,0.995734176295034,1.,0.995734176295034,1.,0.995734176295034,1.,0.995734176295034,
1.,0.995734176295034,1.,0.995734176295034,1.,0.995734176295034,1.,0.995734176295034,
1.,0.995734176295034,1.,0.995734176295034,1.,0.995734176295034,1.,0.995734176295034,
1.,0.995734176295034,1.,0.995734176295034,1.,0.995734176295034,1.,0.995734176295034,
1.,0.995734176295034,1.,0.995734176295034,1.,0.995734176295034,1.,0.995734176295034,
1.,0.995734176295034,1.,0.995734176295034,1.,0.995734176295034,1.,0.995734176295034,
1.,0.995734176295034,1.,0.995734176295034,1.,0.995734176295034,1.,0.995734176295034,
1.,0.995734176295034,1.,0.995734176295034,1.,0.995734176295034,1.,0.995734176295034,
1.,0.995734176295034,1.,0.995734176295034,1.,0.995734176295034,1.,0.995734176295034,
1.,0.995734176295034,1.,0.995734176295034,1.,0.995734176295034,1.,0.995734176295034,
1.,0.995734176295034,1.,0.995734176295034,1.,0.995734176295034,1.,0.995734176295034,
1.,0.995734176295034,1.,0.995734176295034,1.,0.995734176295034,1.,0.995734176295034,
1.,0.995734176295034,1.,0.995734176295034,1.,0.995734176295034,1.,0.995734176295034,
1.,0.995734176295034,1.,0.995734176295034,1.,0.995734176295034,1.,0.995734176295034,
1.,0.995734176295034,1.,0.995734176295034,1.,0.995734176295034,1.,0.995734176295034,
1.,0.995734176295034,1.,0.995734176295034,1.,0.995734176295034,1.,0.995734176295034,
1.,0.995734176295034,1.,0.995734176295034,1.,0.995734176295034,1.,0.995734176295034,
1.,0.995734176295034,1.,0.995734176295034,1.,0.995734176295034,1.,0.995734176295034,
1.,0.995734176295034,1.,0.995734176295034,1.,0.995734176295034,1.,0.995734176295034,
1.,0.995734176295034,1.,0.995734176295034,1.,0.995734176295034,1.,0.995734176295034,
1.,0.995734176295034,1.,0.995734176295034,1.,0.995734176295034,1.,0.995734176295034,
1.,0.995734176295034,1.,0.995734176295034,1.,0.995734176295034,1.,0.995734176295034,
1.,0.995734176295034,1.,0.995734176295034,1.,0.995734176295034,1.,0.995734176295034,
1.,0.995734176295034,1.,0.995734176295034,1.,0.995734176295034,1.,0.995734176295034,
1.,0.995734176295034,1.,0.995734176295034,1.,0.995734176295034,1.,0.995734176295034,
1.,0.995734176295034,1.,0.995734176295034,1.,0.995734176295034,1.,0.995734176295034,
1.,0.995734176295034,1.,0.995734176295034,1.,0.995734176295034,1.,0.995734176295034,
1.,0.995734176295034,1.,0.995734176295034,1.,0.995734176295034,1.,0.995734176295034,
1.,0.995734176295034,1.,0.995734176295034,1.,0.995734176295034,1.,0.995734176295034,
1.,0.995734176295034,1.,0.995734176295034,1.,0.995734176295034,1.,0.995734176295034,
1.,0.995734176295034,1.,0.995734176295034,1.,0.995734176295034,1.,0.995734176295034,
1.,0.995734176295034,1.,0.995734176295034,1.,0.995734176295034,1.,0.995734176295034,
1.,0.995734176295034,1.,0.995734176295034,1.,0.995734176295034,1.,0.995734176295034,
1.,0.995734176295034,1.,0.995734176295034,1.,0.995734176295034,1.,0.995734176295034,
1.,0.995734176295034,1.,0.995734176295034,1.,0.995734176295034,1.,0.995734176295034,
1.,0.995734176295034,1.,0.995734176295034,1.,0.995734176295034,1.,0.995734176295034,
1.,0.995734176295034,1.,0.995734176295034,1.,0.995734176295034,1.,0.995734176295034,
1.,0.995734176295034,1.,0.995734176295034,1.,0.995734176295034,1.,0.995734176295034,
1.,0.995734176295034,1.,0.995734176295034,1.,0.995734176295034,1.,0.995734176295034,
1.,0.995734176295034,1.,0.995734176295034,1.,0.995734176295034,1.,0.995734176295034,
1.,0.995734176295034,1.,0.995734176295034,1.,0.995734176295034,1.,0.995734176295034,
1.,0.995734176295034,1.,0.995734176295034,1.,0.995734176295034,1.,0.995734176295034,
1.,0.995734176295034,1.,0.995734176295034,1.,0.995734176295034,1.,0.995734176295034,
1.,0.995734176295034,1.,0.995734176295034,1.,0.995734176295034,1.,0.995734176295034,
1.,0.995734176295034,1.,0.995734176295034,1.,0.995734176295034,1.,0.995734176295034,
1.,0.995734176295034,1.,0.995734176295034,1.,0.995734176295034,1.,0.995734176295034,
1.,0.995734176295034,1.,0.995734176295034,1.,0.995734176295034,1.,0.995734176295034,
1.,0.995734176295034,1.,0.995734176295034,1.,0.995734176295034,1.,0.995734176295034,
1.,0.995734176295034,1.,0.995734176295034,1.,0.995734176295034,1.,0.995734176295034,
1.,0.995734176295034,1.,0.995734176295034,1.,0.995734176295034,1.,0.995734176295034,
1.,0.995734176295034,1.,0.995734176295034,1.,0.995734176295034,1.,0.995734176295034,
1.,0.995734176295034,1.,0.995734176295034,1.,0.995734176295034,1.,0.995734176295034,
1.,0.995734176295034,1.,0.995734176295034,1.,0.995734176295034,1.,0.995734176295034,
1.,0.995734176295034,1.,0.995734176295034,1.,0.995734176295034,1.,0.995734176295034,
1.,0.995734176295034,1.,0.995734176295034,1.,0.995734176295034,1.,0.995734176295034,
1.,0.995734176295034,1.,0.995734176295034,1.,0.995734176295034,1.,0.995734176295034,
1.,0.995734176295034,1.,0.995734176295034,1.,0.995734176295034,1.,0.995734176295034,
1.,0.995734176295034,1.,0.995734176295034,1.,0.995734176295034,1.,0.995734176295034,
1.,0.995734176295034,1.,0.995734176295034,1.,0.995734176295034,1.,0.995734176295034,
1.,0.995734176295034,1.,0.995734176295034,1.,0.995734176295034,1.,0.995734176295034,
1.,0.995734176295034,1.,0.995734176295034,1.,0.995734176295034,1.,0.995734176295034,
1.,0.995734176295034,1.,0.995734176295034,1.,0.995734176295034,1.,0.995734176295034,
1.,0.995734176295034,1.,0.995734176295034,1.,0.995734176295034,1.,0.995734176295034,
1.,0.995734176295034,1.,0.995734176295034,1.,0.995734176295034,1.,0.995734176295034,
1.,0.995734176295034,1.,0.995734176295034,1.,0.995734176295034,1.,0.995734176295034,
1.,0.995734176295034,1.,0.995734176295034,1.,0.995734176295034,1.,0.995734176295034,
1.,0.995734176295034,1.,0.995734176295034,1.,0.995734176295034,1.,0.995734176295034,
1.,0.995734176295034,1.,0.995734176295034,1.,0.995734176295034,1.,0.995734176295034,
1.,0.995734176295034,1.,0.995734176295034,1.,0.995734176295034,1.,0.995734176295034,
1.,0.995734176295034,1.,0.995734176295034,1.,0.995734176295034,1.,0.995734176295034,
1.,0.995734176295034,1.,0.995734176295034,1.,0.995734176295034,1.,0.995734176295034,
1.,0.995734176295034,1.,0.995734176295034,1.,0.995734176295034,1.,0.995734176295034,
1.,0.995734176295034,1.,0.995734176295034,1.,0.995734176295034,1.,0.995734176295034,
1.,0.995734176295034,1.,0.995734176295034,1.,0.995734176295034,1.,0.995734176295034,
1.,0.995734176295034,1.,0.995734176295034,1.,0.995734176295034,1.,0.995734176295034,
1.,0.995734176295034,1.,0.995734176295034,1.,0.995734176295034,1.,0.995734176295034,
1.,0.995734176295034,1.,0.995734176295034,1.,0.995734176295034,1.,0.995734176295034,
1.,0.995734176295034,1.,0.995734176295034,1.,0.995734176295034,1.,0.995734176295034,
1.,0.995734176295034,1.,0.995734176295034,1.,0.995734176295034,1.,0.995734176295034,
1.,0.995734176295034,1.,0.995734176295034,1.,0.995734176295034,1.,0.995734176295034,
1.,0.995734176295034,1.,0.995734176295034,1.,0.995734176295034,1.,0.995734176295034,
1.,0.995734176295034,1.,0.995734176295034,1.,0.995734176295034,1.,0.995734176295034,
1.,0.995734176295034,1.,0.995734176295034,1.,0.995734176295034,1.,0.995734176295034,
1.,0.995734176295034,1.,0.995734176295034,1.,0.995734176295034,1.,0.995734176295034,
1.,0.995734176295034,1.,0.995734176295034,1.,0.995734176295034,1.,0.995734176295034,
1.,0.995734176295034,1.,0.995734176295034,1.,0.995734176295034,1.,0.995734176295034,
1.,0.995734176295034,1.,0.995734176295034,1.,0.995734176295034,1.,0.995734176295034,
1.,0.995734176295034,1.,0.995734176295034,1.,0.995734176295034,1.,0.995734176295034,
1.,0.995734176295034,1.,0.995734176295034,1.,0.995734176295034,1.,0.995734176295034,
1.,0.995734176295034,1.,0.995734176295034,1.,0.995734176295034,1.,0.995734176295034,
1.,0.995734176295034,1.,0.995734176295034,1.,0.995734176295034,1.,0.995734176295034,
1.,0.995734176295034,1.,0.995734176295034,1.,0.995734176295034,1.,0.995734176295034,
1.,0.995734176295034,1.,0.995734176295034,1.,0.995734176295034,1.,0.995734176295034,
1.,0.995734176295034,1.,0.995734176295034,1.,0.995734176295034,1.,0.995734176295034,
1.,0.995734176295034,1.,0.995734176295034,1.,0.995734176295034,1.,0.995734176295034,
1.,0.995734176295034,1.,0.995734176295034,1.,0.995734176295034,1.,0.995734176295034,
1.,0.995734176295034,1.,0.995734176295034,1.,0.995734176295034,1.,0.995734176295034,
1.,0.995734176295034,1.,0.995734176295034,1.,0.995734176295034,1.,0.995734176295034,
1.,0.995734176295034,1.,0.995734176295034,1.,0.995734176295034,1.,0.995734176295034,
1.,0.995734176295034,1.,0.995734176295034,1.,0.995734176295034,1.,0.995734176295034,
1.,0.995734176295034,1.,0.995734176295034,1.,0.995734176295034,1.,0.995734176295034,
1.,0.995734176295034,1.,0.995734176295034,1.,0.995734176295034,1.,0.995734176295034,
1.,0.995734176295034,1.,0.995734176295034,1.,0.995734176295034,1.,0.995734176295034,
1.,0.995734176295034,1.,0.995734176295034,1.,0.995734176295034,1.,0.995734176295034,
1.,0.995734176295034,1.,0.995734176295034,1.,0.995734176295034,1.,0.995734176295034,
1.,0.995734176295034,1.,0.995734176295034,1.,0.995734176295034,1.,0.995734176295034,
1.,0.995734176295034,1.,0.995734176295034,1.,0.995734176295034,1.,0.995734176295034,
1.,0.995734176295034,1.,0.995734176295034,1.,0.995734176295034,1.,0.995734176295034,
1.,0.995734176295034,1.,0.995734176295034,1.,0.995734176295034,1.,0.995734176295034,
1.,0.995734176295034,1.,0.995734176295034,1.,0.995734176295034,1.,0.995734176295034,
1.,0.995734176295034,1.,0.995734176295034,1.,0.995734176295034,1.,0.995734176295034,
1.,0.995734176295034,1.,0.995734176295034,1.,0.995734176295034,1.,0.995734176295034,
1.,0.995734176295034,1.,0.995734176295034,1.,0.995734176295034,1.,0.995734176295034,
1.,0.995734176295034,1.,0.995734176295034,1.,0.995734176295034,1.,0.995734176295034,
1.,0.995734176295034,1.,0.995734176295034,1.,0.995734176295034,1.,0.995734176295034,
1.,0.995734176295034,1.,0.995734176295034,1.,0.995734176295034,1.,0.995734176295034,
1.,0.995734176295034,1.,0.995734176295034,1.,0.995734176295034,1.,0.995734176295034,
1.,0.997201441372082,0.998074825578922,0.998074825578922,0.998074825578922)))
REPRESENTATION_ITEM('')
SURFACE()
);
#2504=(
BOUNDED_SURFACE()
B_SPLINE_SURFACE(1,2,((#158529,#158530,#158531,#158532,#158533,#158534,
#158535,#158536,#158537,#158538,#158539,#158540,#158541,#158542,#158543,
#158544,#158545,#158546,#158547,#158548,#158549,#158550,#158551,#158552,
#158553,#158554,#158555,#158556,#158557,#158558,#158559,#158560,#158561,
#158562,#158563,#158564,#158565,#158566,#158567,#158568,#158569,#158570,
#158571,#158572,#158573,#158574,#158575,#158576,#158577,#158578,#158579,
#158580,#158581,#158582,#158583,#158584,#158585,#158586,#158587,#158588,
#158589,#158590,#158591,#158592,#158593,#158594,#158595,#158596,#158597,
#158598,#158599,#158600,#158601,#158602,#158603,#158604,#158605,#158606,
#158607,#158608,#158609,#158610,#158611,#158612,#158613,#158614,#158615,
#158616,#158617,#158618,#158619,#158620,#158621,#158622,#158623,#158624,
#158625,#158626,#158627,#158628,#158629,#158630,#158631,#158632,#158633,
#158634,#158635,#158636,#158637,#158638,#158639,#158640,#158641,#158642,
#158643,#158644,#158645,#158646,#158647,#158648,#158649,#158650,#158651,
#158652,#158653,#158654,#158655,#158656,#158657,#158658,#158659,#158660,
#158661,#158662,#158663,#158664,#158665,#158666,#158667,#158668,#158669,
#158670,#158671,#158672,#158673,#158674,#158675,#158676,#158677,#158678,
#158679,#158680,#158681,#158682,#158683,#158684,#158685,#158686,#158687,
#158688,#158689,#158690,#158691,#158692,#158693,#158694,#158695,#158696,
#158697,#158698,#158699,#158700,#158701,#158702,#158703,#158704,#158705,
#158706,#158707,#158708,#158709,#158710,#158711,#158712,#158713,#158714,
#158715,#158716,#158717,#158718,#158719,#158720,#158721,#158722,#158723,
#158724,#158725,#158726,#158727,#158728,#158729,#158730,#158731,#158732,
#158733,#158734,#158735,#158736,#158737,#158738,#158739,#158740,#158741,
#158742,#158743,#158744,#158745,#158746,#158747,#158748,#158749,#158750,
#158751,#158752,#158753,#158754,#158755,#158756,#158757,#158758,#158759,
#158760,#158761,#158762,#158763,#158764,#158765,#158766,#158767,#158768,
#158769,#158770,#158771,#158772,#158773,#158774,#158775,#158776,#158777,
#158778,#158779,#158780,#158781,#158782,#158783,#158784,#158785,#158786,
#158787,#158788,#158789,#158790,#158791,#158792,#158793,#158794,#158795,
#158796,#158797,#158798,#158799,#158800,#158801,#158802,#158803,#158804,
#158805,#158806,#158807,#158808,#158809,#158810,#158811,#158812,#158813,
#158814,#158815,#158816,#158817,#158818,#158819,#158820,#158821,#158822,
#158823,#158824,#158825,#158826,#158827,#158828,#158829,#158830,#158831,
#158832,#158833,#158834,#158835,#158836,#158837,#158838,#158839,#158840,
#158841,#158842,#158843,#158844,#158845,#158846,#158847,#158848,#158849,
#158850,#158851,#158852,#158853,#158854,#158855,#158856,#158857,#158858,
#158859,#158860,#158861,#158862,#158863,#158864,#158865,#158866,#158867,
#158868,#158869,#158870,#158871,#158872,#158873,#158874,#158875,#158876,
#158877,#158878,#158879,#158880,#158881,#158882,#158883,#158884,#158885,
#158886,#158887,#158888,#158889,#158890,#158891,#158892,#158893,#158894,
#158895,#158896,#158897,#158898,#158899,#158900,#158901,#158902,#158903,
#158904,#158905,#158906,#158907,#158908,#158909,#158910,#158911,#158912,
#158913,#158914,#158915,#158916,#158917,#158918,#158919,#158920,#158921,
#158922,#158923,#158924,#158925,#158926,#158927,#158928,#158929,#158930,
#158931,#158932,#158933,#158934,#158935,#158936,#158937,#158938,#158939,
#158940,#158941,#158942,#158943,#158944,#158945,#158946,#158947,#158948,
#158949,#158950,#158951,#158952,#158953,#158954,#158955,#158956,#158957,
#158958,#158959,#158960,#158961,#158962,#158963,#158964,#158965,#158966,
#158967,#158968,#158969,#158970,#158971,#158972,#158973,#158974,#158975,
#158976,#158977,#158978,#158979,#158980,#158981,#158982,#158983,#158984,
#158985,#158986,#158987,#158988,#158989,#158990,#158991,#158992,#158993,
#158994,#158995,#158996,#158997,#158998,#158999,#159000,#159001,#159002,
#159003,#159004,#159005,#159006,#159007,#159008,#159009,#159010,#159011,
#159012,#159013,#159014,#159015,#159016,#159017,#159018,#159019,#159020,
#159021,#159022,#159023,#159024,#159025,#159026,#159027,#159028,#159029,
#159030,#159031,#159032,#159033,#159034,#159035,#159036,#159037,#159038,
#159039,#159040,#159041,#159042,#159043,#159044,#159045,#159046,#159047,
#159048,#159049,#159050,#159051,#159052,#159053,#159054,#159055,#159056,
#159057,#159058,#159059,#159060,#159061,#159062,#159063,#159064,#159065,
#159066,#159067,#159068,#159069,#159070,#159071,#159072,#159073,#159074,
#159075,#159076,#159077,#159078,#159079,#159080,#159081,#159082,#159083,
#159084,#159085,#159086,#159087,#159088,#159089,#159090,#159091,#159092,
#159093,#159094,#159095,#159096,#159097,#159098,#159099,#159100,#159101,
#159102,#159103,#159104,#159105,#159106,#159107,#159108,#159109,#159110,
#159111,#159112,#159113,#159114,#159115,#159116,#159117,#159118,#159119,
#159120,#159121,#159122,#159123,#159124,#159125,#159126,#159127,#159128,
#159129,#159130,#159131,#159132,#159133,#159134,#159135,#159136,#159137,
#159138,#159139,#159140,#159141,#159142,#159143,#159144,#159145,#159146,
#159147,#159148,#159149,#159150,#159151,#159152,#159153,#159154,#159155,
#159156,#159157,#159158,#159159,#159160,#159161,#159162,#159163,#159164,
#159165,#159166,#159167,#159168,#159169,#159170,#159171,#159172,#159173,
#159174,#159175,#159176,#159177,#159178,#159179,#159180,#159181,#159182,
#159183,#159184,#159185,#159186,#159187,#159188,#159189,#159190,#159191,
#159192,#159193,#159194,#159195,#159196,#159197,#159198,#159199,#159200,
#159201,#159202,#159203,#159204,#159205,#159206,#159207,#159208,#159209,
#159210,#159211,#159212,#159213,#159214,#159215,#159216,#159217,#159218,
#159219,#159220,#159221,#159222,#159223,#159224,#159225,#159226,#159227,
#159228,#159229,#159230,#159231,#159232,#159233,#159234,#159235,#159236,
#159237,#159238,#159239,#159240,#159241,#159242,#159243,#159244,#159245,
#159246,#159247,#159248,#159249,#159250,#159251,#159252,#159253,#159254,
#159255,#159256,#159257,#159258,#159259,#159260,#159261,#159262,#159263,
#159264,#159265,#159266,#159267,#159268,#159269,#159270,#159271,#159272,
#159273,#159274,#159275,#159276,#159277,#159278,#159279,#159280,#159281,
#159282,#159283,#159284,#159285,#159286,#159287,#159288,#159289,#159290,
#159291,#159292,#159293,#159294,#159295,#159296,#159297,#159298,#159299,
#159300,#159301,#159302,#159303,#159304,#159305,#159306,#159307,#159308,
#159309,#159310,#159311,#159312,#159313,#159314,#159315,#159316,#159317,
#159318,#159319,#159320,#159321,#159322,#159323,#159324,#159325,#159326,
#159327,#159328,#159329,#159330,#159331,#159332,#159333,#159334,#159335,
#159336,#159337,#159338,#159339,#159340,#159341,#159342,#159343,#159344,
#159345,#159346,#159347,#159348,#159349,#159350,#159351,#159352,#159353,
#159354,#159355,#159356,#159357,#159358,#159359,#159360,#159361,#159362,
#159363,#159364,#159365,#159366,#159367,#159368,#159369,#159370,#159371,
#159372,#159373,#159374,#159375,#159376,#159377,#159378,#159379,#159380,
#159381,#159382,#159383,#159384,#159385,#159386,#159387,#159388,#159389,
#159390,#159391,#159392,#159393,#159394,#159395,#159396,#159397,#159398,
#159399,#159400,#159401,#159402,#159403,#159404,#159405,#159406,#159407,
#159408,#159409,#159410,#159411,#159412,#159413,#159414,#159415,#159416,
#159417,#159418,#159419,#159420,#159421,#159422,#159423,#159424,#159425,
#159426,#159427,#159428,#159429,#159430,#159431,#159432,#159433,#159434,
#159435,#159436,#159437,#159438,#159439,#159440,#159441,#159442,#159443,
#159444,#159445,#159446,#159447,#159448,#159449,#159450,#159451,#159452,
#159453,#159454,#159455,#159456,#159457,#159458,#159459,#159460,#159461,
#159462,#159463,#159464,#159465,#159466,#159467,#159468,#159469,#159470,
#159471,#159472,#159473,#159474,#159475,#159476,#159477,#159478,#159479,
#159480,#159481,#159482,#159483,#159484,#159485,#159486,#159487,#159488,
#159489,#159490,#159491,#159492,#159493,#159494,#159495,#159496,#159497,
#159498,#159499,#159500,#159501,#159502,#159503,#159504,#159505,#159506,
#159507,#159508,#159509,#159510,#159511,#159512,#159513,#159514,#159515,
#159516,#159517,#159518,#159519,#159520,#159521,#159522,#159523,#159524,
#159525,#159526,#159527,#159528,#159529,#159530,#159531,#159532,#159533,
#159534,#159535,#159536,#159537,#159538,#159539,#159540,#159541,#159542,
#159543,#159544,#159545,#159546,#159547,#159548,#159549,#159550,#159551,
#159552,#159553,#159554,#159555,#159556,#159557,#159558,#159559,#159560,
#159561,#159562,#159563,#159564,#159565,#159566,#159567,#159568,#159569,
#159570,#159571,#159572,#159573,#159574,#159575,#159576,#159577,#159578,
#159579,#159580,#159581,#159582,#159583,#159584,#159585,#159586,#159587,
#159588,#159589,#159590,#159591,#159592,#159593,#159594,#159595,#159596,
#159597,#159598,#159599,#159600,#159601,#159602,#159603,#159604,#159605,
#159606,#159607,#159608,#159609,#159610,#159611,#159612,#159613,#159614,
#159615,#159616,#159617,#159618,#159619,#159620,#159621,#159622,#159623,
#159624,#159625,#159626,#159627,#159628,#159629,#159630,#159631,#159632,
#159633,#159634,#159635,#159636,#159637,#159638,#159639,#159640,#159641,
#159642,#159643,#159644,#159645,#159646,#159647,#159648,#159649,#159650,
#159651,#159652,#159653,#159654,#159655,#159656,#159657,#159658,#159659,
#159660,#159661,#159662,#159663,#159664,#159665,#159666,#159667,#159668,
#159669,#159670,#159671,#159672,#159673,#159674,#159675,#159676,#159677,
#159678,#159679,#159680,#159681,#159682,#159683,#159684,#159685,#159686,
#159687,#159688,#159689,#159690,#159691,#159692,#159693,#159694,#159695,
#159696,#159697,#159698,#159699,#159700,#159701,#159702,#159703,#159704,
#159705,#159706,#159707,#159708,#159709,#159710,#159711,#159712,#159713,
#159714,#159715,#159716,#159717,#159718,#159719,#159720,#159721,#159722,
#159723,#159724,#159725,#159726,#159727,#159728,#159729,#159730,#159731,
#159732,#159733,#159734,#159735,#159736,#159737,#159738,#159739,#159740,
#159741,#159742,#159743,#159744,#159745,#159746,#159747,#159748,#159749,
#159750,#159751,#159752,#159753,#159754,#159755,#159756,#159757,#159758,
#159759,#159760,#159761,#159762,#159763,#159764,#159765,#159766,#159767,
#159768,#159769,#159770,#159771,#159772,#159773,#159774,#159775,#159776,
#159777,#159778,#159779,#159780,#159781,#159782,#159783,#159784,#159785,
#159786,#159787,#159788,#159789,#159790,#159791,#159792,#159793,#159794,
#159795,#159796,#159797,#159798,#159799,#159800,#159801,#159802,#159803,
#159804,#159805,#159806,#159807,#159808,#159809,#159810,#159811,#159812,
#159813,#159814,#159815,#159816,#159817,#159818,#159819,#159820,#159821,
#159822,#159823,#159824,#159825,#159826,#159827,#159828,#159829,#159830,
#159831,#159832,#159833,#159834,#159835,#159836,#159837,#159838,#159839,
#159840,#159841,#159842,#159843,#159844,#159845,#159846,#159847,#159848,
#159849,#159850,#159851,#159852,#159853,#159854,#159855,#159856,#159857,
#159858,#159859,#159860,#159861,#159862,#159863,#159864,#159865,#159866,
#159867,#159868,#159869,#159870,#159871,#159872,#159873,#159874,#159875,
#159876,#159877,#159878,#159879,#159880,#159881,#159882,#159883,#159884,
#159885,#159886,#159887,#159888,#159889,#159890,#159891,#159892,#159893,
#159894,#159895,#159896,#159897,#159898,#159899,#159900,#159901,#159902,
#159903,#159904,#159905,#159906,#159907,#159908,#159909,#159910,#159911,
#159912,#159913,#159914,#159915,#159916,#159917,#159918,#159919,#159920,
#159921,#159922,#159923,#159924,#159925,#159926,#159927,#159928,#159929,
#159930,#159931,#159932,#159933,#159934,#159935,#159936,#159937,#159938,
#159939,#159940,#159941,#159942,#159943,#159944,#159945,#159946,#159947,
#159948,#159949,#159950,#159951,#159952,#159953,#159954,#159955,#159956,
#159957,#159958,#159959,#159960,#159961,#159962,#159963,#159964,#159965,
#159966,#159967,#159968,#159969,#159970,#159971,#159972,#159973,#159974,
#159975,#159976,#159977,#159978,#159979,#159980,#159981,#159982,#159983,
#159984,#159985,#159986,#159987,#159988,#159989,#159990,#159991,#159992,
#159993,#159994,#159995,#159996,#159997,#159998,#159999,#160000,#160001,
#160002,#160003,#160004,#160005,#160006,#160007,#160008,#160009,#160010,
#160011,#160012,#160013,#160014,#160015,#160016,#160017,#160018,#160019,
#160020,#160021,#160022,#160023,#160024,#160025,#160026,#160027,#160028,
#160029,#160030,#160031,#160032,#160033,#160034,#160035,#160036,#160037,
#160038,#160039,#160040,#160041,#160042,#160043,#160044,#160045,#160046,
#160047,#160048,#160049,#160050,#160051,#160052,#160053,#160054,#160055,
#160056,#160057,#160058,#160059,#160060,#160061,#160062,#160063,#160064,
#160065,#160066,#160067,#160068,#160069,#160070,#160071,#160072,#160073,
#160074,#160075,#160076,#160077,#160078,#160079,#160080,#160081,#160082,
#160083,#160084,#160085,#160086,#160087,#160088,#160089,#160090,#160091,
#160092,#160093,#160094,#160095,#160096,#160097,#160098,#160099,#160100,
#160101,#160102,#160103,#160104,#160105,#160106,#160107,#160108,#160109,
#160110,#160111,#160112,#160113,#160114,#160115,#160116,#160117,#160118,
#160119,#160120,#160121,#160122,#160123,#160124,#160125,#160126,#160127,
#160128,#160129,#160130,#160131,#160132,#160133,#160134,#160135,#160136,
#160137,#160138,#160139,#160140,#160141,#160142,#160143,#160144,#160145,
#160146,#160147,#160148,#160149,#160150,#160151,#160152,#160153,#160154,
#160155,#160156,#160157,#160158,#160159,#160160,#160161,#160162,#160163,
#160164,#160165,#160166,#160167,#160168,#160169,#160170,#160171,#160172,
#160173,#160174,#160175,#160176,#160177,#160178,#160179,#160180,#160181,
#160182,#160183,#160184,#160185,#160186,#160187,#160188,#160189,#160190,
#160191,#160192,#160193,#160194,#160195,#160196,#160197,#160198,#160199,
#160200,#160201,#160202,#160203,#160204,#160205,#160206,#160207,#160208,
#160209,#160210,#160211,#160212,#160213,#160214,#160215,#160216,#160217,
#160218,#160219,#160220,#160221,#160222,#160223,#160224,#160225,#160226,
#160227,#160228,#160229,#160230,#160231,#160232,#160233,#160234,#160235,
#160236,#160237,#160238,#160239,#160240,#160241,#160242,#160243,#160244,
#160245,#160246,#160247,#160248,#160249,#160250,#160251,#160252,#160253,
#160254,#160255,#160256,#160257,#160258,#160259,#160260,#160261,#160262,
#160263,#160264,#160265,#160266,#160267,#160268,#160269,#160270,#160271,
#160272,#160273,#160274,#160275,#160276,#160277,#160278,#160279,#160280,
#160281,#160282,#160283,#160284,#160285,#160286,#160287,#160288,#160289,
#160290,#160291,#160292,#160293,#160294,#160295,#160296,#160297,#160298,
#160299,#160300,#160301,#160302,#160303,#160304,#160305,#160306,#160307,
#160308,#160309,#160310,#160311,#160312,#160313,#160314,#160315,#160316,
#160317,#160318,#160319,#160320,#160321,#160322,#160323,#160324,#160325,
#160326,#160327,#160328,#160329,#160330,#160331,#160332,#160333,#160334,
#160335,#160336,#160337,#160338,#160339,#160340,#160341,#160342,#160343,
#160344,#160345,#160346,#160347,#160348,#160349,#160350,#160351,#160352,
#160353,#160354,#160355,#160356,#160357,#160358,#160359,#160360,#160361,
#160362,#160363,#160364,#160365,#160366,#160367,#160368,#160369,#160370,
#160371,#160372,#160373,#160374,#160375,#160376,#160377,#160378,#160379,
#160380,#160381,#160382,#160383,#160384,#160385,#160386,#160387,#160388,
#160389,#160390,#160391,#160392,#160393,#160394,#160395,#160396,#160397,
#160398,#160399,#160400,#160401,#160402,#160403,#160404,#160405,#160406,
#160407,#160408,#160409,#160410,#160411,#160412,#160413,#160414,#160415,
#160416,#160417,#160418,#160419,#160420,#160421,#160422,#160423,#160424,
#160425,#160426,#160427,#160428,#160429,#160430,#160431,#160432,#160433,
#160434,#160435,#160436,#160437,#160438,#160439,#160440,#160441,#160442,
#160443,#160444,#160445,#160446,#160447,#160448,#160449,#160450,#160451,
#160452,#160453,#160454,#160455,#160456,#160457,#160458,#160459,#160460,
#160461,#160462,#160463,#160464,#160465,#160466,#160467,#160468,#160469,
#160470,#160471,#160472,#160473,#160474,#160475,#160476,#160477,#160478,
#160479,#160480,#160481,#160482,#160483,#160484,#160485,#160486,#160487,
#160488,#160489,#160490,#160491,#160492,#160493,#160494,#160495,#160496,
#160497,#160498,#160499,#160500,#160501,#160502,#160503,#160504,#160505,
#160506,#160507,#160508,#160509,#160510,#160511,#160512,#160513,#160514,
#160515,#160516,#160517,#160518,#160519,#160520,#160521,#160522,#160523,
#160524,#160525,#160526,#160527,#160528,#160529,#160530,#160531,#160532,
#160533,#160534,#160535,#160536,#160537,#160538,#160539,#160540,#160541),
(#160542,#160543,#160544,#160545,#160546,#160547,#160548,#160549,#160550,
#160551,#160552,#160553,#160554,#160555,#160556,#160557,#160558,#160559,
#160560,#160561,#160562,#160563,#160564,#160565,#160566,#160567,#160568,
#160569,#160570,#160571,#160572,#160573,#160574,#160575,#160576,#160577,
#160578,#160579,#160580,#160581,#160582,#160583,#160584,#160585,#160586,
#160587,#160588,#160589,#160590,#160591,#160592,#160593,#160594,#160595,
#160596,#160597,#160598,#160599,#160600,#160601,#160602,#160603,#160604,
#160605,#160606,#160607,#160608,#160609,#160610,#160611,#160612,#160613,
#160614,#160615,#160616,#160617,#160618,#160619,#160620,#160621,#160622,
#160623,#160624,#160625,#160626,#160627,#160628,#160629,#160630,#160631,
#160632,#160633,#160634,#160635,#160636,#160637,#160638,#160639,#160640,
#160641,#160642,#160643,#160644,#160645,#160646,#160647,#160648,#160649,
#160650,#160651,#160652,#160653,#160654,#160655,#160656,#160657,#160658,
#160659,#160660,#160661,#160662,#160663,#160664,#160665,#160666,#160667,
#160668,#160669,#160670,#160671,#160672,#160673,#160674,#160675,#160676,
#160677,#160678,#160679,#160680,#160681,#160682,#160683,#160684,#160685,
#160686,#160687,#160688,#160689,#160690,#160691,#160692,#160693,#160694,
#160695,#160696,#160697,#160698,#160699,#160700,#160701,#160702,#160703,
#160704,#160705,#160706,#160707,#160708,#160709,#160710,#160711,#160712,
#160713,#160714,#160715,#160716,#160717,#160718,#160719,#160720,#160721,
#160722,#160723,#160724,#160725,#160726,#160727,#160728,#160729,#160730,
#160731,#160732,#160733,#160734,#160735,#160736,#160737,#160738,#160739,
#160740,#160741,#160742,#160743,#160744,#160745,#160746,#160747,#160748,
#160749,#160750,#160751,#160752,#160753,#160754,#160755,#160756,#160757,
#160758,#160759,#160760,#160761,#160762,#160763,#160764,#160765,#160766,
#160767,#160768,#160769,#160770,#160771,#160772,#160773,#160774,#160775,
#160776,#160777,#160778,#160779,#160780,#160781,#160782,#160783,#160784,
#160785,#160786,#160787,#160788,#160789,#160790,#160791,#160792,#160793,
#160794,#160795,#160796,#160797,#160798,#160799,#160800,#160801,#160802,
#160803,#160804,#160805,#160806,#160807,#160808,#160809,#160810,#160811,
#160812,#160813,#160814,#160815,#160816,#160817,#160818,#160819,#160820,
#160821,#160822,#160823,#160824,#160825,#160826,#160827,#160828,#160829,
#160830,#160831,#160832,#160833,#160834,#160835,#160836,#160837,#160838,
#160839,#160840,#160841,#160842,#160843,#160844,#160845,#160846,#160847,
#160848,#160849,#160850,#160851,#160852,#160853,#160854,#160855,#160856,
#160857,#160858,#160859,#160860,#160861,#160862,#160863,#160864,#160865,
#160866,#160867,#160868,#160869,#160870,#160871,#160872,#160873,#160874,
#160875,#160876,#160877,#160878,#160879,#160880,#160881,#160882,#160883,
#160884,#160885,#160886,#160887,#160888,#160889,#160890,#160891,#160892,
#160893,#160894,#160895,#160896,#160897,#160898,#160899,#160900,#160901,
#160902,#160903,#160904,#160905,#160906,#160907,#160908,#160909,#160910,
#160911,#160912,#160913,#160914,#160915,#160916,#160917,#160918,#160919,
#160920,#160921,#160922,#160923,#160924,#160925,#160926,#160927,#160928,
#160929,#160930,#160931,#160932,#160933,#160934,#160935,#160936,#160937,
#160938,#160939,#160940,#160941,#160942,#160943,#160944,#160945,#160946,
#160947,#160948,#160949,#160950,#160951,#160952,#160953,#160954,#160955,
#160956,#160957,#160958,#160959,#160960,#160961,#160962,#160963,#160964,
#160965,#160966,#160967,#160968,#160969,#160970,#160971,#160972,#160973,
#160974,#160975,#160976,#160977,#160978,#160979,#160980,#160981,#160982,
#160983,#160984,#160985,#160986,#160987,#160988,#160989,#160990,#160991,
#160992,#160993,#160994,#160995,#160996,#160997,#160998,#160999,#161000,
#161001,#161002,#161003,#161004,#161005,#161006,#161007,#161008,#161009,
#161010,#161011,#161012,#161013,#161014,#161015,#161016,#161017,#161018,
#161019,#161020,#161021,#161022,#161023,#161024,#161025,#161026,#161027,
#161028,#161029,#161030,#161031,#161032,#161033,#161034,#161035,#161036,
#161037,#161038,#161039,#161040,#161041,#161042,#161043,#161044,#161045,
#161046,#161047,#161048,#161049,#161050,#161051,#161052,#161053,#161054,
#161055,#161056,#161057,#161058,#161059,#161060,#161061,#161062,#161063,
#161064,#161065,#161066,#161067,#161068,#161069,#161070,#161071,#161072,
#161073,#161074,#161075,#161076,#161077,#161078,#161079,#161080,#161081,
#161082,#161083,#161084,#161085,#161086,#161087,#161088,#161089,#161090,
#161091,#161092,#161093,#161094,#161095,#161096,#161097,#161098,#161099,
#161100,#161101,#161102,#161103,#161104,#161105,#161106,#161107,#161108,
#161109,#161110,#161111,#161112,#161113,#161114,#161115,#161116,#161117,
#161118,#161119,#161120,#161121,#161122,#161123,#161124,#161125,#161126,
#161127,#161128,#161129,#161130,#161131,#161132,#161133,#161134,#161135,
#161136,#161137,#161138,#161139,#161140,#161141,#161142,#161143,#161144,
#161145,#161146,#161147,#161148,#161149,#161150,#161151,#161152,#161153,
#161154,#161155,#161156,#161157,#161158,#161159,#161160,#161161,#161162,
#161163,#161164,#161165,#161166,#161167,#161168,#161169,#161170,#161171,
#161172,#161173,#161174,#161175,#161176,#161177,#161178,#161179,#161180,
#161181,#161182,#161183,#161184,#161185,#161186,#161187,#161188,#161189,
#161190,#161191,#161192,#161193,#161194,#161195,#161196,#161197,#161198,
#161199,#161200,#161201,#161202,#161203,#161204,#161205,#161206,#161207,
#161208,#161209,#161210,#161211,#161212,#161213,#161214,#161215,#161216,
#161217,#161218,#161219,#161220,#161221,#161222,#161223,#161224,#161225,
#161226,#161227,#161228,#161229,#161230,#161231,#161232,#161233,#161234,
#161235,#161236,#161237,#161238,#161239,#161240,#161241,#161242,#161243,
#161244,#161245,#161246,#161247,#161248,#161249,#161250,#161251,#161252,
#161253,#161254,#161255,#161256,#161257,#161258,#161259,#161260,#161261,
#161262,#161263,#161264,#161265,#161266,#161267,#161268,#161269,#161270,
#161271,#161272,#161273,#161274,#161275,#161276,#161277,#161278,#161279,
#161280,#161281,#161282,#161283,#161284,#161285,#161286,#161287,#161288,
#161289,#161290,#161291,#161292,#161293,#161294,#161295,#161296,#161297,
#161298,#161299,#161300,#161301,#161302,#161303,#161304,#161305,#161306,
#161307,#161308,#161309,#161310,#161311,#161312,#161313,#161314,#161315,
#161316,#161317,#161318,#161319,#161320,#161321,#161322,#161323,#161324,
#161325,#161326,#161327,#161328,#161329,#161330,#161331,#161332,#161333,
#161334,#161335,#161336,#161337,#161338,#161339,#161340,#161341,#161342,
#161343,#161344,#161345,#161346,#161347,#161348,#161349,#161350,#161351,
#161352,#161353,#161354,#161355,#161356,#161357,#161358,#161359,#161360,
#161361,#161362,#161363,#161364,#161365,#161366,#161367,#161368,#161369,
#161370,#161371,#161372,#161373,#161374,#161375,#161376,#161377,#161378,
#161379,#161380,#161381,#161382,#161383,#161384,#161385,#161386,#161387,
#161388,#161389,#161390,#161391,#161392,#161393,#161394,#161395,#161396,
#161397,#161398,#161399,#161400,#161401,#161402,#161403,#161404,#161405,
#161406,#161407,#161408,#161409,#161410,#161411,#161412,#161413,#161414,
#161415,#161416,#161417,#161418,#161419,#161420,#161421,#161422,#161423,
#161424,#161425,#161426,#161427,#161428,#161429,#161430,#161431,#161432,
#161433,#161434,#161435,#161436,#161437,#161438,#161439,#161440,#161441,
#161442,#161443,#161444,#161445,#161446,#161447,#161448,#161449,#161450,
#161451,#161452,#161453,#161454,#161455,#161456,#161457,#161458,#161459,
#161460,#161461,#161462,#161463,#161464,#161465,#161466,#161467,#161468,
#161469,#161470,#161471,#161472,#161473,#161474,#161475,#161476,#161477,
#161478,#161479,#161480,#161481,#161482,#161483,#161484,#161485,#161486,
#161487,#161488,#161489,#161490,#161491,#161492,#161493,#161494,#161495,
#161496,#161497,#161498,#161499,#161500,#161501,#161502,#161503,#161504,
#161505,#161506,#161507,#161508,#161509,#161510,#161511,#161512,#161513,
#161514,#161515,#161516,#161517,#161518,#161519,#161520,#161521,#161522,
#161523,#161524,#161525,#161526,#161527,#161528,#161529,#161530,#161531,
#161532,#161533,#161534,#161535,#161536,#161537,#161538,#161539,#161540,
#161541,#161542,#161543,#161544,#161545,#161546,#161547,#161548,#161549,
#161550,#161551,#161552,#161553,#161554,#161555,#161556,#161557,#161558,
#161559,#161560,#161561,#161562,#161563,#161564,#161565,#161566,#161567,
#161568,#161569,#161570,#161571,#161572,#161573,#161574,#161575,#161576,
#161577,#161578,#161579,#161580,#161581,#161582,#161583,#161584,#161585,
#161586,#161587,#161588,#161589,#161590,#161591,#161592,#161593,#161594,
#161595,#161596,#161597,#161598,#161599,#161600,#161601,#161602,#161603,
#161604,#161605,#161606,#161607,#161608,#161609,#161610,#161611,#161612,
#161613,#161614,#161615,#161616,#161617,#161618,#161619,#161620,#161621,
#161622,#161623,#161624,#161625,#161626,#161627,#161628,#161629,#161630,
#161631,#161632,#161633,#161634,#161635,#161636,#161637,#161638,#161639,
#161640,#161641,#161642,#161643,#161644,#161645,#161646,#161647,#161648,
#161649,#161650,#161651,#161652,#161653,#161654,#161655,#161656,#161657,
#161658,#161659,#161660,#161661,#161662,#161663,#161664,#161665,#161666,
#161667,#161668,#161669,#161670,#161671,#161672,#161673,#161674,#161675,
#161676,#161677,#161678,#161679,#161680,#161681,#161682,#161683,#161684,
#161685,#161686,#161687,#161688,#161689,#161690,#161691,#161692,#161693,
#161694,#161695,#161696,#161697,#161698,#161699,#161700,#161701,#161702,
#161703,#161704,#161705,#161706,#161707,#161708,#161709,#161710,#161711,
#161712,#161713,#161714,#161715,#161716,#161717,#161718,#161719,#161720,
#161721,#161722,#161723,#161724,#161725,#161726,#161727,#161728,#161729,
#161730,#161731,#161732,#161733,#161734,#161735,#161736,#161737,#161738,
#161739,#161740,#161741,#161742,#161743,#161744,#161745,#161746,#161747,
#161748,#161749,#161750,#161751,#161752,#161753,#161754,#161755,#161756,
#161757,#161758,#161759,#161760,#161761,#161762,#161763,#161764,#161765,
#161766,#161767,#161768,#161769,#161770,#161771,#161772,#161773,#161774,
#161775,#161776,#161777,#161778,#161779,#161780,#161781,#161782,#161783,
#161784,#161785,#161786,#161787,#161788,#161789,#161790,#161791,#161792,
#161793,#161794,#161795,#161796,#161797,#161798,#161799,#161800,#161801,
#161802,#161803,#161804,#161805,#161806,#161807,#161808,#161809,#161810,
#161811,#161812,#161813,#161814,#161815,#161816,#161817,#161818,#161819,
#161820,#161821,#161822,#161823,#161824,#161825,#161826,#161827,#161828,
#161829,#161830,#161831,#161832,#161833,#161834,#161835,#161836,#161837,
#161838,#161839,#161840,#161841,#161842,#161843,#161844,#161845,#161846,
#161847,#161848,#161849,#161850,#161851,#161852,#161853,#161854,#161855,
#161856,#161857,#161858,#161859,#161860,#161861,#161862,#161863,#161864,
#161865,#161866,#161867,#161868,#161869,#161870,#161871,#161872,#161873,
#161874,#161875,#161876,#161877,#161878,#161879,#161880,#161881,#161882,
#161883,#161884,#161885,#161886,#161887,#161888,#161889,#161890,#161891,
#161892,#161893,#161894,#161895,#161896,#161897,#161898,#161899,#161900,
#161901,#161902,#161903,#161904,#161905,#161906,#161907,#161908,#161909,
#161910,#161911,#161912,#161913,#161914,#161915,#161916,#161917,#161918,
#161919,#161920,#161921,#161922,#161923,#161924,#161925,#161926,#161927,
#161928,#161929,#161930,#161931,#161932,#161933,#161934,#161935,#161936,
#161937,#161938,#161939,#161940,#161941,#161942,#161943,#161944,#161945,
#161946,#161947,#161948,#161949,#161950,#161951,#161952,#161953,#161954,
#161955,#161956,#161957,#161958,#161959,#161960,#161961,#161962,#161963,
#161964,#161965,#161966,#161967,#161968,#161969,#161970,#161971,#161972,
#161973,#161974,#161975,#161976,#161977,#161978,#161979,#161980,#161981,
#161982,#161983,#161984,#161985,#161986,#161987,#161988,#161989,#161990,
#161991,#161992,#161993,#161994,#161995,#161996,#161997,#161998,#161999,
#162000,#162001,#162002,#162003,#162004,#162005,#162006,#162007,#162008,
#162009,#162010,#162011,#162012,#162013,#162014,#162015,#162016,#162017,
#162018,#162019,#162020,#162021,#162022,#162023,#162024,#162025,#162026,
#162027,#162028,#162029,#162030,#162031,#162032,#162033,#162034,#162035,
#162036,#162037,#162038,#162039,#162040,#162041,#162042,#162043,#162044,
#162045,#162046,#162047,#162048,#162049,#162050,#162051,#162052,#162053,
#162054,#162055,#162056,#162057,#162058,#162059,#162060,#162061,#162062,
#162063,#162064,#162065,#162066,#162067,#162068,#162069,#162070,#162071,
#162072,#162073,#162074,#162075,#162076,#162077,#162078,#162079,#162080,
#162081,#162082,#162083,#162084,#162085,#162086,#162087,#162088,#162089,
#162090,#162091,#162092,#162093,#162094,#162095,#162096,#162097,#162098,
#162099,#162100,#162101,#162102,#162103,#162104,#162105,#162106,#162107,
#162108,#162109,#162110,#162111,#162112,#162113,#162114,#162115,#162116,
#162117,#162118,#162119,#162120,#162121,#162122,#162123,#162124,#162125,
#162126,#162127,#162128,#162129,#162130,#162131,#162132,#162133,#162134,
#162135,#162136,#162137,#162138,#162139,#162140,#162141,#162142,#162143,
#162144,#162145,#162146,#162147,#162148,#162149,#162150,#162151,#162152,
#162153,#162154,#162155,#162156,#162157,#162158,#162159,#162160,#162161,
#162162,#162163,#162164,#162165,#162166,#162167,#162168,#162169,#162170,
#162171,#162172,#162173,#162174,#162175,#162176,#162177,#162178,#162179,
#162180,#162181,#162182,#162183,#162184,#162185,#162186,#162187,#162188,
#162189,#162190,#162191,#162192,#162193,#162194,#162195,#162196,#162197,
#162198,#162199,#162200,#162201,#162202,#162203,#162204,#162205,#162206,
#162207,#162208,#162209,#162210,#162211,#162212,#162213,#162214,#162215,
#162216,#162217,#162218,#162219,#162220,#162221,#162222,#162223,#162224,
#162225,#162226,#162227,#162228,#162229,#162230,#162231,#162232,#162233,
#162234,#162235,#162236,#162237,#162238,#162239,#162240,#162241,#162242,
#162243,#162244,#162245,#162246,#162247,#162248,#162249,#162250,#162251,
#162252,#162253,#162254,#162255,#162256,#162257,#162258,#162259,#162260,
#162261,#162262,#162263,#162264,#162265,#162266,#162267,#162268,#162269,
#162270,#162271,#162272,#162273,#162274,#162275,#162276,#162277,#162278,
#162279,#162280,#162281,#162282,#162283,#162284,#162285,#162286,#162287,
#162288,#162289,#162290,#162291,#162292,#162293,#162294,#162295,#162296,
#162297,#162298,#162299,#162300,#162301,#162302,#162303,#162304,#162305,
#162306,#162307,#162308,#162309,#162310,#162311,#162312,#162313,#162314,
#162315,#162316,#162317,#162318,#162319,#162320,#162321,#162322,#162323,
#162324,#162325,#162326,#162327,#162328,#162329,#162330,#162331,#162332,
#162333,#162334,#162335,#162336,#162337,#162338,#162339,#162340,#162341,
#162342,#162343,#162344,#162345,#162346,#162347,#162348,#162349,#162350,
#162351,#162352,#162353,#162354,#162355,#162356,#162357,#162358,#162359,
#162360,#162361,#162362,#162363,#162364,#162365,#162366,#162367,#162368,
#162369,#162370,#162371,#162372,#162373,#162374,#162375,#162376,#162377,
#162378,#162379,#162380,#162381,#162382,#162383,#162384,#162385,#162386,
#162387,#162388,#162389,#162390,#162391,#162392,#162393,#162394,#162395,
#162396,#162397,#162398,#162399,#162400,#162401,#162402,#162403,#162404,
#162405,#162406,#162407,#162408,#162409,#162410,#162411,#162412,#162413,
#162414,#162415,#162416,#162417,#162418,#162419,#162420,#162421,#162422,
#162423,#162424,#162425,#162426,#162427,#162428,#162429,#162430,#162431,
#162432,#162433,#162434,#162435,#162436,#162437,#162438,#162439,#162440,
#162441,#162442,#162443,#162444,#162445,#162446,#162447,#162448,#162449,
#162450,#162451,#162452,#162453,#162454,#162455,#162456,#162457,#162458,
#162459,#162460,#162461,#162462,#162463,#162464,#162465,#162466,#162467,
#162468,#162469,#162470,#162471,#162472,#162473,#162474,#162475,#162476,
#162477,#162478,#162479,#162480,#162481,#162482,#162483,#162484,#162485,
#162486,#162487,#162488,#162489,#162490,#162491,#162492,#162493,#162494,
#162495,#162496,#162497,#162498,#162499,#162500,#162501,#162502,#162503,
#162504,#162505,#162506,#162507,#162508,#162509,#162510,#162511,#162512,
#162513,#162514,#162515,#162516,#162517,#162518,#162519,#162520,#162521,
#162522,#162523,#162524,#162525,#162526,#162527,#162528,#162529,#162530,
#162531,#162532,#162533,#162534,#162535,#162536,#162537,#162538,#162539,
#162540,#162541,#162542,#162543,#162544,#162545,#162546,#162547,#162548,
#162549,#162550,#162551,#162552,#162553,#162554)),.UNSPECIFIED.,.F.,.F.,
 .F.)
B_SPLINE_SURFACE_WITH_KNOTS((2,2),(3,2,2,2,2,2,2,2,2,2,2,2,2,2,2,2,2,2,
2,2,2,2,2,2,2,2,2,2,2,2,2,2,2,2,2,2,2,2,2,2,2,2,2,2,2,2,2,2,2,2,2,2,2,2,
2,2,2,2,2,2,2,2,2,2,2,2,2,2,2,2,2,2,2,2,2,2,2,2,2,2,2,2,2,2,2,2,2,2,2,2,
2,2,2,2,2,2,2,2,2,2,2,2,2,2,2,2,2,2,2,2,2,2,2,2,2,2,2,2,2,2,2,2,2,2,2,2,
2,2,2,2,2,2,2,2,2,2,2,2,2,2,2,2,2,2,2,2,2,2,2,2,2,2,2,2,2,2,2,2,2,2,2,2,
2,2,2,2,2,2,2,2,2,2,2,2,2,2,2,2,2,2,2,2,2,2,2,2,2,2,2,2,2,2,2,2,2,2,2,2,
2,2,2,2,2,2,2,2,2,2,2,2,2,2,2,2,2,2,2,2,2,2,2,2,2,2,2,2,2,2,2,2,2,2,2,2,
2,2,2,2,2,2,2,2,2,2,2,2,2,2,2,2,2,2,2,2,2,2,2,2,2,2,2,2,2,2,2,2,2,2,2,2,
2,2,2,2,2,2,2,2,2,2,2,2,2,2,2,2,2,2,2,2,2,2,2,2,2,2,2,2,2,2,2,2,2,2,2,2,
2,2,2,2,2,2,2,2,2,2,2,2,2,2,2,2,2,2,2,2,2,2,2,2,2,2,2,2,2,2,2,2,2,2,2,2,
2,2,2,2,2,2,2,2,2,2,2,2,2,2,2,2,2,2,2,2,2,2,2,2,2,2,2,2,2,2,2,2,2,2,2,2,
2,2,2,2,2,2,2,2,2,2,2,2,2,2,2,2,2,2,2,2,2,2,2,2,2,2,2,2,2,2,2,2,2,2,2,2,
2,2,2,2,2,2,2,2,2,2,2,2,2,2,2,2,2,2,2,2,2,2,2,2,2,2,2,2,2,2,2,2,2,2,2,2,
2,2,2,2,2,2,2,2,2,2,2,2,2,2,2,2,2,2,2,2,2,2,2,2,2,2,2,2,2,2,2,2,2,2,2,2,
2,2,2,2,2,2,2,2,2,2,2,2,2,2,2,2,2,2,2,2,2,2,2,2,2,2,2,2,2,2,2,2,2,2,2,2,
2,2,2,2,2,2,2,2,2,2,2,2,2,2,2,2,2,2,2,2,2,2,2,2,2,2,2,2,2,2,2,2,2,2,2,2,
2,2,2,2,2,2,2,2,2,2,2,2,2,2,2,2,2,2,2,2,2,2,2,2,2,2,2,2,2,2,2,2,2,2,2,2,
2,2,2,2,2,2,2,2,2,2,2,2,2,2,2,2,2,2,2,2,2,2,2,2,2,2,2,2,2,2,2,2,2,2,2,2,
2,2,2,2,2,2,2,2,2,2,2,2,2,2,2,2,2,2,2,2,2,2,2,2,2,2,2,2,2,2,2,2,2,2,2,2,
2,2,2,2,2,2,2,2,2,2,2,2,2,2,2,2,2,2,2,2,2,2,2,2,2,2,2,2,2,2,2,2,2,2,2,2,
2,2,2,2,2,2,2,2,2,2,2,2,2,2,2,2,2,2,2,2,2,2,2,2,2,2,2,2,2,2,2,2,2,2,2,2,
2,2,2,2,2,2,2,2,2,2,2,2,2,2,2,2,2,2,2,2,2,2,2,2,2,2,2,2,2,2,2,2,2,2,2,2,
2,2,2,2,2,2,2,2,2,2,2,2,2,2,2,2,2,2,2,2,2,2,2,2,2,2,2,2,2,2,2,2,2,2,2,2,
2,2,2,2,2,2,2,2,2,2,2,2,2,2,2,2,2,2,2,2,2,2,2,2,2,2,2,2,2,2,2,2,2,2,2,2,
2,2,2,2,2,2,2,2,2,2,2,2,2,2,2,2,2,2,2,2,2,2,2,2,2,2,2,2,2,2,2,2,2,2,2,2,
2,2,2,2,2,2,2,2,2,2,2,2,2,2,2,2,2,2,2,2,2,2,2,2,2,2,2,2,2,2,2,2,2,2,2,2,
2,2,2,2,2,2,2,2,2,2,2,2,2,2,2,2,2,2,2,2,2,2,2,2,2,2,2,2,2,2,2,2,2,2,2,2,
2,2,2,2,2,2,2,2,2,2,2,2,2,2,2,2,2,2,2,2,2,2,2,2,2,2,2,2,2,2,2,2,2,2,2,2,
2,2,2,2,2,2,2,2,2,2,2,2,2,2,2,2,3),(0.,1.),(0.,0.000980392156862745,0.00196078431372549,
0.00294117647058824,0.00392156862745098,0.00490196078431373,0.00588235294117647,
0.00686274509803922,0.00784313725490196,0.00882352941176471,0.00980392156862745,
0.0107843137254902,0.0117647058823529,0.0127450980392157,0.0137254901960784,
0.0147058823529412,0.0156862745098039,0.0166666666666667,0.0176470588235294,
0.0186274509803922,0.0196078431372549,0.0205882352941176,0.0215686274509804,
0.0225490196078431,0.0235294117647059,0.0245098039215686,0.0254901960784314,
0.0264705882352941,0.0274509803921569,0.0284313725490196,0.0294117647058824,
0.0303921568627451,0.0313725490196078,0.0323529411764706,0.0333333333333333,
0.0343137254901961,0.0352941176470588,0.0362745098039216,0.0372549019607843,
0.0382352941176471,0.0392156862745098,0.0401960784313726,0.0411764705882353,
0.042156862745098,0.0431372549019608,0.0441176470588235,0.0450980392156863,
0.046078431372549,0.0470588235294118,0.0480392156862745,0.0490196078431373,
0.05,0.0509803921568627,0.0519607843137255,0.0529411764705882,0.053921568627451,
0.0549019607843137,0.0558823529411765,0.0568627450980392,0.057843137254902,
0.0588235294117647,0.0598039215686275,0.0607843137254902,0.0617647058823529,
0.0627450980392157,0.0637254901960784,0.0647058823529412,0.0656862745098039,
0.0666666666666667,0.0676470588235294,0.0686274509803922,0.0696078431372549,
0.0705882352941176,0.0715686274509804,0.0725490196078431,0.0735294117647059,
0.0745098039215686,0.0754901960784314,0.0764705882352941,0.0774509803921569,
0.0784313725490196,0.0794117647058823,0.0803921568627451,0.0813725490196078,
0.0823529411764706,0.0833333333333333,0.0843137254901961,0.0852941176470588,
0.0862745098039216,0.0872549019607843,0.0882352941176471,0.0892156862745098,
0.0901960784313725,0.0911764705882353,0.092156862745098,0.0931372549019608,
0.0941176470588235,0.0950980392156863,0.096078431372549,0.0970588235294118,
0.0980392156862745,0.0990196078431373,0.1,0.100980392156863,0.101960784313725,
0.102941176470588,0.103921568627451,0.104901960784314,0.105882352941176,
0.106862745098039,0.107843137254902,0.108823529411765,0.109803921568627,
0.11078431372549,0.111764705882353,0.112745098039216,0.113725490196078,
0.114705882352941,0.115686274509804,0.116666666666667,0.117647058823529,
0.118627450980392,0.119607843137255,0.120588235294118,0.12156862745098,
0.122549019607843,0.123529411764706,0.124509803921569,0.125490196078431,
0.126470588235294,0.127450980392157,0.12843137254902,0.129411764705882,
0.130392156862745,0.131372549019608,0.132352941176471,0.133333333333333,
0.134313725490196,0.135294117647059,0.136274509803922,0.137254901960784,
0.138235294117647,0.13921568627451,0.140196078431373,0.141176470588235,
0.142156862745098,0.143137254901961,0.144117647058824,0.145098039215686,
0.146078431372549,0.147058823529412,0.148039215686275,0.149019607843137,
0.15,0.150980392156863,0.151960784313725,0.152941176470588,0.153921568627451,
0.154901960784314,0.155882352941176,0.156862745098039,0.157843137254902,
0.158823529411765,0.159803921568627,0.16078431372549,0.161764705882353,
0.162745098039216,0.163725490196078,0.164705882352941,0.165686274509804,
0.166666666666667,0.167647058823529,0.168627450980392,0.169607843137255,
0.170588235294118,0.17156862745098,0.172549019607843,0.173529411764706,
0.174509803921569,0.175490196078431,0.176470588235294,0.177450980392157,
0.17843137254902,0.179411764705882,0.180392156862745,0.181372549019608,
0.182352941176471,0.183333333333333,0.184313725490196,0.185294117647059,
0.186274509803922,0.187254901960784,0.188235294117647,0.18921568627451,
0.190196078431373,0.191176470588235,0.192156862745098,0.193137254901961,
0.194117647058824,0.195098039215686,0.196078431372549,0.197058823529412,
0.198039215686275,0.199019607843137,0.2,0.200980392156863,0.201960784313725,
0.202941176470588,0.203921568627451,0.204901960784314,0.205882352941176,
0.206862745098039,0.207843137254902,0.208823529411765,0.209803921568627,
0.21078431372549,0.211764705882353,0.212745098039216,0.213725490196078,
0.214705882352941,0.215686274509804,0.216666666666667,0.217647058823529,
0.218627450980392,0.219607843137255,0.220588235294118,0.22156862745098,
0.222549019607843,0.223529411764706,0.224509803921569,0.225490196078431,
0.226470588235294,0.227450980392157,0.22843137254902,0.229411764705882,
0.230392156862745,0.231372549019608,0.232352941176471,0.233333333333333,
0.234313725490196,0.235294117647059,0.236274509803922,0.237254901960784,
0.238235294117647,0.23921568627451,0.240196078431373,0.241176470588235,
0.242156862745098,0.243137254901961,0.244117647058824,0.245098039215686,
0.246078431372549,0.247058823529412,0.248039215686275,0.249019607843137,
0.25,0.250980392156863,0.251960784313725,0.252941176470588,0.253921568627451,
0.254901960784314,0.255882352941176,0.256862745098039,0.257843137254902,
0.258823529411765,0.259803921568627,0.26078431372549,0.261764705882353,
0.262745098039216,0.263725490196078,0.264705882352941,0.265686274509804,
0.266666666666667,0.267647058823529,0.268627450980392,0.269607843137255,
0.270588235294118,0.27156862745098,0.272549019607843,0.273529411764706,
0.274509803921569,0.275490196078431,0.276470588235294,0.277450980392157,
0.27843137254902,0.279411764705882,0.280392156862745,0.281372549019608,
0.282352941176471,0.283333333333333,0.284313725490196,0.285294117647059,
0.286274509803922,0.287254901960784,0.288235294117647,0.28921568627451,
0.290196078431373,0.291176470588235,0.292156862745098,0.293137254901961,
0.294117647058824,0.295098039215686,0.296078431372549,0.297058823529412,
0.298039215686275,0.299019607843137,0.3,0.300980392156863,0.301960784313725,
0.302941176470588,0.303921568627451,0.304901960784314,0.305882352941176,
0.306862745098039,0.307843137254902,0.308823529411765,0.309803921568627,
0.31078431372549,0.311764705882353,0.312745098039216,0.313725490196078,
0.314705882352941,0.315686274509804,0.316666666666667,0.317647058823529,
0.318627450980392,0.319607843137255,0.320588235294118,0.32156862745098,
0.322549019607843,0.323529411764706,0.324509803921569,0.325490196078431,
0.326470588235294,0.327450980392157,0.32843137254902,0.329411764705882,
0.330392156862745,0.331372549019608,0.332352941176471,0.333333333333333,
0.334313725490196,0.335294117647059,0.336274509803922,0.337254901960784,
0.338235294117647,0.33921568627451,0.340196078431373,0.341176470588235,
0.342156862745098,0.343137254901961,0.344117647058824,0.345098039215686,
0.346078431372549,0.347058823529412,0.348039215686274,0.349019607843137,
0.35,0.350980392156863,0.351960784313726,0.352941176470588,0.353921568627451,
0.354901960784314,0.355882352941176,0.356862745098039,0.357843137254902,
0.358823529411765,0.359803921568627,0.36078431372549,0.361764705882353,
0.362745098039216,0.363725490196078,0.364705882352941,0.365686274509804,
0.366666666666667,0.367647058823529,0.368627450980392,0.369607843137255,
0.370588235294118,0.37156862745098,0.372549019607843,0.373529411764706,
0.374509803921569,0.375490196078431,0.376470588235294,0.377450980392157,
0.37843137254902,0.379411764705882,0.380392156862745,0.381372549019608,
0.382352941176471,0.383333333333333,0.384313725490196,0.385294117647059,
0.386274509803922,0.387254901960784,0.388235294117647,0.38921568627451,
0.390196078431373,0.391176470588235,0.392156862745098,0.393137254901961,
0.394117647058824,0.395098039215686,0.396078431372549,0.397058823529412,
0.398039215686274,0.399019607843137,0.4,0.400980392156863,0.401960784313726,
0.402941176470588,0.403921568627451,0.404901960784314,0.405882352941176,
0.406862745098039,0.407843137254902,0.408823529411765,0.409803921568627,
0.41078431372549,0.411764705882353,0.412745098039216,0.413725490196078,
0.414705882352941,0.415686274509804,0.416666666666667,0.417647058823529,
0.418627450980392,0.419607843137255,0.420588235294118,0.42156862745098,
0.422549019607843,0.423529411764706,0.424509803921569,0.425490196078431,
0.426470588235294,0.427450980392157,0.42843137254902,0.429411764705882,
0.430392156862745,0.431372549019608,0.432352941176471,0.433333333333333,
0.434313725490196,0.435294117647059,0.436274509803922,0.437254901960784,
0.438235294117647,0.43921568627451,0.440196078431373,0.441176470588235,
0.442156862745098,0.443137254901961,0.444117647058824,0.445098039215686,
0.446078431372549,0.447058823529412,0.448039215686275,0.449019607843137,
0.45,0.450980392156863,0.451960784313725,0.452941176470588,0.453921568627451,
0.454901960784314,0.455882352941176,0.456862745098039,0.457843137254902,
0.458823529411765,0.459803921568627,0.46078431372549,0.461764705882353,
0.462745098039216,0.463725490196078,0.464705882352941,0.465686274509804,
0.466666666666667,0.467647058823529,0.468627450980392,0.469607843137255,
0.470588235294118,0.47156862745098,0.472549019607843,0.473529411764706,
0.474509803921569,0.475490196078431,0.476470588235294,0.477450980392157,
0.47843137254902,0.479411764705882,0.480392156862745,0.481372549019608,
0.482352941176471,0.483333333333333,0.484313725490196,0.485294117647059,
0.486274509803922,0.487254901960784,0.488235294117647,0.48921568627451,
0.490196078431373,0.491176470588235,0.492156862745098,0.493137254901961,
0.494117647058824,0.495098039215686,0.496078431372549,0.497058823529412,
0.498039215686275,0.499019607843137,0.5,0.500980392156863,0.501960784313725,
0.502941176470588,0.503921568627451,0.504901960784314,0.505882352941176,
0.506862745098039,0.507843137254902,0.508823529411765,0.509803921568627,
0.51078431372549,0.511764705882353,0.512745098039216,0.513725490196078,
0.514705882352941,0.515686274509804,0.516666666666667,0.517647058823529,
0.518627450980392,0.519607843137255,0.520588235294118,0.52156862745098,
0.522549019607843,0.523529411764706,0.524509803921569,0.525490196078431,
0.526470588235294,0.527450980392157,0.52843137254902,0.529411764705882,
0.530392156862745,0.531372549019608,0.532352941176471,0.533333333333333,
0.534313725490196,0.535294117647059,0.536274509803922,0.537254901960784,
0.538235294117647,0.53921568627451,0.540196078431373,0.541176470588235,
0.542156862745098,0.543137254901961,0.544117647058823,0.545098039215686,
0.546078431372549,0.547058823529412,0.548039215686275,0.549019607843137,
0.55,0.550980392156863,0.551960784313726,0.552941176470588,0.553921568627451,
0.554901960784314,0.555882352941176,0.556862745098039,0.557843137254902,
0.558823529411765,0.559803921568627,0.56078431372549,0.561764705882353,
0.562745098039216,0.563725490196078,0.564705882352941,0.565686274509804,
0.566666666666667,0.567647058823529,0.568627450980392,0.569607843137255,
0.570588235294118,0.57156862745098,0.572549019607843,0.573529411764706,
0.574509803921569,0.575490196078431,0.576470588235294,0.577450980392157,
0.57843137254902,0.579411764705882,0.580392156862745,0.581372549019608,
0.582352941176471,0.583333333333333,0.584313725490196,0.585294117647059,
0.586274509803922,0.587254901960784,0.588235294117647,0.58921568627451,
0.590196078431373,0.591176470588235,0.592156862745098,0.593137254901961,
0.594117647058824,0.595098039215686,0.596078431372549,0.597058823529412,
0.598039215686274,0.599019607843137,0.6,0.600980392156863,0.601960784313725,
0.602941176470588,0.603921568627451,0.604901960784314,0.605882352941176,
0.606862745098039,0.607843137254902,0.608823529411765,0.609803921568628,
0.61078431372549,0.611764705882353,0.612745098039216,0.613725490196078,
0.614705882352941,0.615686274509804,0.616666666666667,0.617647058823529,
0.618627450980392,0.619607843137255,0.620588235294118,0.62156862745098,
0.622549019607843,0.623529411764706,0.624509803921569,0.625490196078431,
0.626470588235294,0.627450980392157,0.62843137254902,0.629411764705882,
0.630392156862745,0.631372549019608,0.632352941176471,0.633333333333333,
0.634313725490196,0.635294117647059,0.636274509803922,0.637254901960784,
0.638235294117647,0.63921568627451,0.640196078431372,0.641176470588235,
0.642156862745098,0.643137254901961,0.644117647058824,0.645098039215686,
0.646078431372549,0.647058823529412,0.648039215686275,0.649019607843137,
0.65,0.650980392156863,0.651960784313726,0.652941176470588,0.653921568627451,
0.654901960784314,0.655882352941176,0.656862745098039,0.657843137254902,
0.658823529411765,0.659803921568627,0.66078431372549,0.661764705882353,
0.662745098039216,0.663725490196078,0.664705882352941,0.665686274509804,
0.666666666666667,0.667647058823529,0.668627450980392,0.669607843137255,
0.670588235294118,0.67156862745098,0.672549019607843,0.673529411764706,
0.674509803921569,0.675490196078431,0.676470588235294,0.677450980392157,
0.67843137254902,0.679411764705882,0.680392156862745,0.681372549019608,
0.682352941176471,0.683333333333333,0.684313725490196,0.685294117647059,
0.686274509803922,0.687254901960784,0.688235294117647,0.68921568627451,
0.690196078431373,0.691176470588235,0.692156862745098,0.693137254901961,
0.694117647058824,0.695098039215686,0.696078431372549,0.697058823529412,
0.698039215686274,0.699019607843137,0.7,0.700980392156863,0.701960784313725,
0.702941176470588,0.703921568627451,0.704901960784314,0.705882352941177,
0.706862745098039,0.707843137254902,0.708823529411765,0.709803921568627,
0.71078431372549,0.711764705882353,0.712745098039216,0.713725490196078,
0.714705882352941,0.715686274509804,0.716666666666667,0.717647058823529,
0.718627450980392,0.719607843137255,0.720588235294118,0.72156862745098,
0.722549019607843,0.723529411764706,0.724509803921569,0.725490196078431,
0.726470588235294,0.727450980392157,0.72843137254902,0.729411764705882,
0.730392156862745,0.731372549019608,0.732352941176471,0.733333333333333,
0.734313725490196,0.735294117647059,0.736274509803922,0.737254901960784,
0.738235294117647,0.73921568627451,0.740196078431373,0.741176470588235,
0.742156862745098,0.743137254901961,0.744117647058824,0.745098039215686,
0.746078431372549,0.747058823529412,0.748039215686275,0.749019607843137,
0.75,0.750980392156863,0.751960784313725,0.752941176470588,0.753921568627451,
0.754901960784314,0.755882352941176,0.756862745098039,0.757843137254902,
0.758823529411765,0.759803921568627,0.76078431372549,0.761764705882353,
0.762745098039216,0.763725490196078,0.764705882352941,0.765686274509804,
0.766666666666667,0.767647058823529,0.768627450980392,0.769607843137255,
0.770588235294118,0.77156862745098,0.772549019607843,0.773529411764706,
0.774509803921569,0.775490196078431,0.776470588235294,0.777450980392157,
0.77843137254902,0.779411764705882,0.780392156862745,0.781372549019608,
0.782352941176471,0.783333333333333,0.784313725490196,0.785294117647059,
0.786274509803922,0.787254901960784,0.788235294117647,0.78921568627451,
0.790196078431373,0.791176470588235,0.792156862745098,0.793137254901961,
0.794117647058823,0.795098039215686,0.796078431372549,0.797058823529412,
0.798039215686275,0.799019607843137,0.8,0.800980392156863,0.801960784313726,
0.802941176470588,0.803921568627451,0.804901960784314,0.805882352941176,
0.806862745098039,0.807843137254902,0.808823529411765,0.809803921568627,
0.81078431372549,0.811764705882353,0.812745098039216,0.813725490196078,
0.814705882352941,0.815686274509804,0.816666666666667,0.817647058823529,
0.818627450980392,0.819607843137255,0.820588235294118,0.82156862745098,
0.822549019607843,0.823529411764706,0.824509803921569,0.825490196078431,
0.826470588235294,0.827450980392157,0.82843137254902,0.829411764705882,
0.830392156862745,0.831372549019608,0.832352941176471,0.833333333333333,
0.834313725490196,0.835294117647059,0.836274509803922,0.837254901960784,
0.838235294117647,0.83921568627451,0.840196078431373,0.841176470588235,
0.842156862745098,0.843137254901961,0.844117647058824,0.845098039215686,
0.846078431372549,0.847058823529412,0.848039215686274,0.849019607843137,
0.85,0.850980392156863,0.851960784313725,0.852941176470588,0.853921568627451,
0.854901960784314,0.855882352941176,0.856862745098039,0.857843137254902,
0.858823529411765,0.859803921568628,0.86078431372549,0.861764705882353,
0.862745098039216,0.863725490196078,0.864705882352941,0.865686274509804,
0.866666666666667,0.867647058823529,0.868627450980392,0.869607843137255,
0.870588235294118,0.87156862745098,0.872549019607843,0.873529411764706,
0.874509803921569,0.875490196078431,0.876470588235294,0.877450980392157,
0.87843137254902,0.879411764705882,0.880392156862745,0.881372549019608,
0.882352941176471,0.883333333333333,0.884313725490196,0.885294117647059,
0.886274509803922,0.887254901960784,0.888235294117647,0.88921568627451,
0.890196078431372,0.891176470588235,0.892156862745098,0.893137254901961,
0.894117647058824,0.895098039215686,0.896078431372549,0.897058823529412,
0.898039215686275,0.899019607843137,0.9,0.900980392156863,0.901960784313726,
0.902941176470588,0.903921568627451,0.904901960784314,0.905882352941176,
0.906862745098039,0.907843137254902,0.908823529411765,0.909803921568627,
0.91078431372549,0.911764705882353,0.912745098039216,0.913725490196078,
0.914705882352941,0.915686274509804,0.916666666666667,0.917647058823529,
0.918627450980392,0.919607843137255,0.920588235294118,0.92156862745098,
0.922549019607843,0.923529411764706,0.924509803921569,0.925490196078431,
0.926470588235294,0.927450980392157,0.92843137254902,0.929411764705882,
0.930392156862745,0.931372549019608,0.932352941176471,0.933333333333333,
0.934313725490196,0.935294117647059,0.936274509803922,0.937254901960784,
0.938235294117647,0.93921568627451,0.940196078431373,0.941176470588235,
0.942156862745098,0.943137254901961,0.944117647058824,0.945098039215686,
0.946078431372549,0.947058823529412,0.948039215686274,0.949019607843137,
0.95,0.950980392156863,0.951960784313725,0.952941176470588,0.953921568627451,
0.954901960784314,0.955882352941177,0.956862745098039,0.957843137254902,
0.958823529411765,0.959803921568627,0.96078431372549,0.961764705882353,
0.962745098039216,0.963725490196078,0.964705882352941,0.965686274509804,
0.966666666666667,0.967647058823529,0.968627450980392,0.969607843137255,
0.970588235294118,0.97156862745098,0.972549019607843,0.973529411764706,
0.974509803921569,0.975490196078431,0.976470588235294,0.977450980392157,
0.97843137254902,0.979411764705882,0.980392156862745,0.981372549019608,
0.982352941176471,0.983333333333333,0.984313725490196,0.985294117647059,
0.985937314000278),.UNSPECIFIED.)
GEOMETRIC_REPRESENTATION_ITEM()
RATIONAL_B_SPLINE_SURFACE(((1.,0.995734176295034,1.,0.995734176295034,1.,
0.995734176295034,1.,0.995734176295034,1.,0.995734176295034,1.,0.995734176295034,
1.,0.995734176295034,1.,0.995734176295034,1.,0.995734176295034,1.,0.995734176295034,
1.,0.995734176295034,1.,0.995734176295034,1.,0.995734176295034,1.,0.995734176295034,
1.,0.995734176295034,1.,0.995734176295034,1.,0.995734176295034,1.,0.995734176295034,
1.,0.995734176295034,1.,0.995734176295034,1.,0.995734176295034,1.,0.995734176295034,
1.,0.995734176295034,1.,0.995734176295034,1.,0.995734176295034,1.,0.995734176295034,
1.,0.995734176295034,1.,0.995734176295034,1.,0.995734176295034,1.,0.995734176295034,
1.,0.995734176295034,1.,0.995734176295034,1.,0.995734176295034,1.,0.995734176295034,
1.,0.995734176295034,1.,0.995734176295034,1.,0.995734176295034,1.,0.995734176295034,
1.,0.995734176295034,1.,0.995734176295034,1.,0.995734176295034,1.,0.995734176295034,
1.,0.995734176295034,1.,0.995734176295034,1.,0.995734176295034,1.,0.995734176295034,
1.,0.995734176295034,1.,0.995734176295034,1.,0.995734176295034,1.,0.995734176295034,
1.,0.995734176295034,1.,0.995734176295034,1.,0.995734176295034,1.,0.995734176295034,
1.,0.995734176295034,1.,0.995734176295034,1.,0.995734176295034,1.,0.995734176295034,
1.,0.995734176295034,1.,0.995734176295034,1.,0.995734176295034,1.,0.995734176295034,
1.,0.995734176295034,1.,0.995734176295034,1.,0.995734176295034,1.,0.995734176295034,
1.,0.995734176295034,1.,0.995734176295034,1.,0.995734176295034,1.,0.995734176295034,
1.,0.995734176295034,1.,0.995734176295034,1.,0.995734176295034,1.,0.995734176295034,
1.,0.995734176295034,1.,0.995734176295034,1.,0.995734176295034,1.,0.995734176295034,
1.,0.995734176295034,1.,0.995734176295034,1.,0.995734176295034,1.,0.995734176295034,
1.,0.995734176295034,1.,0.995734176295034,1.,0.995734176295034,1.,0.995734176295034,
1.,0.995734176295034,1.,0.995734176295034,1.,0.995734176295034,1.,0.995734176295034,
1.,0.995734176295034,1.,0.995734176295034,1.,0.995734176295034,1.,0.995734176295034,
1.,0.995734176295034,1.,0.995734176295034,1.,0.995734176295034,1.,0.995734176295034,
1.,0.995734176295034,1.,0.995734176295034,1.,0.995734176295034,1.,0.995734176295034,
1.,0.995734176295034,1.,0.995734176295034,1.,0.995734176295034,1.,0.995734176295034,
1.,0.995734176295034,1.,0.995734176295034,1.,0.995734176295034,1.,0.995734176295034,
1.,0.995734176295034,1.,0.995734176295034,1.,0.995734176295034,1.,0.995734176295034,
1.,0.995734176295034,1.,0.995734176295034,1.,0.995734176295034,1.,0.995734176295034,
1.,0.995734176295034,1.,0.995734176295034,1.,0.995734176295034,1.,0.995734176295034,
1.,0.995734176295034,1.,0.995734176295034,1.,0.995734176295034,1.,0.995734176295034,
1.,0.995734176295034,1.,0.995734176295034,1.,0.995734176295034,1.,0.995734176295034,
1.,0.995734176295034,1.,0.995734176295034,1.,0.995734176295034,1.,0.995734176295034,
1.,0.995734176295034,1.,0.995734176295034,1.,0.995734176295034,1.,0.995734176295034,
1.,0.995734176295034,1.,0.995734176295034,1.,0.995734176295034,1.,0.995734176295034,
1.,0.995734176295034,1.,0.995734176295034,1.,0.995734176295034,1.,0.995734176295034,
1.,0.995734176295034,1.,0.995734176295034,1.,0.995734176295034,1.,0.995734176295034,
1.,0.995734176295034,1.,0.995734176295034,1.,0.995734176295034,1.,0.995734176295034,
1.,0.995734176295034,1.,0.995734176295034,1.,0.995734176295034,1.,0.995734176295034,
1.,0.995734176295034,1.,0.995734176295034,1.,0.995734176295034,1.,0.995734176295034,
1.,0.995734176295034,1.,0.995734176295034,1.,0.995734176295034,1.,0.995734176295034,
1.,0.995734176295034,1.,0.995734176295034,1.,0.995734176295034,1.,0.995734176295034,
1.,0.995734176295034,1.,0.995734176295034,1.,0.995734176295034,1.,0.995734176295034,
1.,0.995734176295034,1.,0.995734176295034,1.,0.995734176295034,1.,0.995734176295034,
1.,0.995734176295034,1.,0.995734176295034,1.,0.995734176295034,1.,0.995734176295034,
1.,0.995734176295034,1.,0.995734176295034,1.,0.995734176295034,1.,0.995734176295034,
1.,0.995734176295034,1.,0.995734176295034,1.,0.995734176295034,1.,0.995734176295034,
1.,0.995734176295034,1.,0.995734176295034,1.,0.995734176295034,1.,0.995734176295034,
1.,0.995734176295034,1.,0.995734176295034,1.,0.995734176295034,1.,0.995734176295034,
1.,0.995734176295034,1.,0.995734176295034,1.,0.995734176295034,1.,0.995734176295034,
1.,0.995734176295034,1.,0.995734176295034,1.,0.995734176295034,1.,0.995734176295034,
1.,0.995734176295034,1.,0.995734176295034,1.,0.995734176295034,1.,0.995734176295034,
1.,0.995734176295034,1.,0.995734176295034,1.,0.995734176295034,1.,0.995734176295034,
1.,0.995734176295034,1.,0.995734176295034,1.,0.995734176295034,1.,0.995734176295034,
1.,0.995734176295034,1.,0.995734176295034,1.,0.995734176295034,1.,0.995734176295034,
1.,0.995734176295034,1.,0.995734176295034,1.,0.995734176295034,1.,0.995734176295034,
1.,0.995734176295034,1.,0.995734176295034,1.,0.995734176295034,1.,0.995734176295034,
1.,0.995734176295034,1.,0.995734176295034,1.,0.995734176295034,1.,0.995734176295034,
1.,0.995734176295034,1.,0.995734176295034,1.,0.995734176295034,1.,0.995734176295034,
1.,0.995734176295034,1.,0.995734176295034,1.,0.995734176295034,1.,0.995734176295034,
1.,0.995734176295034,1.,0.995734176295034,1.,0.995734176295034,1.,0.995734176295034,
1.,0.995734176295034,1.,0.995734176295034,1.,0.995734176295034,1.,0.995734176295034,
1.,0.995734176295034,1.,0.995734176295034,1.,0.995734176295034,1.,0.995734176295034,
1.,0.995734176295034,1.,0.995734176295034,1.,0.995734176295034,1.,0.995734176295034,
1.,0.995734176295034,1.,0.995734176295034,1.,0.995734176295034,1.,0.995734176295034,
1.,0.995734176295034,1.,0.995734176295034,1.,0.995734176295034,1.,0.995734176295034,
1.,0.995734176295034,1.,0.995734176295034,1.,0.995734176295034,1.,0.995734176295034,
1.,0.995734176295034,1.,0.995734176295034,1.,0.995734176295034,1.,0.995734176295034,
1.,0.995734176295034,1.,0.995734176295034,1.,0.995734176295034,1.,0.995734176295034,
1.,0.995734176295034,1.,0.995734176295034,1.,0.995734176295034,1.,0.995734176295034,
1.,0.995734176295034,1.,0.995734176295034,1.,0.995734176295034,1.,0.995734176295034,
1.,0.995734176295034,1.,0.995734176295034,1.,0.995734176295034,1.,0.995734176295034,
1.,0.995734176295034,1.,0.995734176295034,1.,0.995734176295034,1.,0.995734176295034,
1.,0.995734176295034,1.,0.995734176295034,1.,0.995734176295034,1.,0.995734176295034,
1.,0.995734176295034,1.,0.995734176295034,1.,0.995734176295034,1.,0.995734176295034,
1.,0.995734176295034,1.,0.995734176295034,1.,0.995734176295034,1.,0.995734176295034,
1.,0.995734176295034,1.,0.995734176295034,1.,0.995734176295034,1.,0.995734176295034,
1.,0.995734176295034,1.,0.995734176295034,1.,0.995734176295034,1.,0.995734176295034,
1.,0.995734176295034,1.,0.995734176295034,1.,0.995734176295034,1.,0.995734176295034,
1.,0.995734176295034,1.,0.995734176295034,1.,0.995734176295034,1.,0.995734176295034,
1.,0.995734176295034,1.,0.995734176295034,1.,0.995734176295034,1.,0.995734176295034,
1.,0.995734176295034,1.,0.995734176295034,1.,0.995734176295034,1.,0.995734176295034,
1.,0.995734176295034,1.,0.995734176295034,1.,0.995734176295034,1.,0.995734176295034,
1.,0.995734176295034,1.,0.995734176295034,1.,0.995734176295034,1.,0.995734176295034,
1.,0.995734176295034,1.,0.995734176295034,1.,0.995734176295034,1.,0.995734176295034,
1.,0.995734176295034,1.,0.995734176295034,1.,0.995734176295034,1.,0.995734176295034,
1.,0.995734176295034,1.,0.995734176295034,1.,0.995734176295034,1.,0.995734176295034,
1.,0.995734176295034,1.,0.995734176295034,1.,0.995734176295034,1.,0.995734176295034,
1.,0.995734176295034,1.,0.995734176295034,1.,0.995734176295034,1.,0.995734176295034,
1.,0.995734176295034,1.,0.995734176295034,1.,0.995734176295034,1.,0.995734176295034,
1.,0.995734176295034,1.,0.995734176295034,1.,0.995734176295034,1.,0.995734176295034,
1.,0.995734176295034,1.,0.995734176295034,1.,0.995734176295034,1.,0.995734176295034,
1.,0.995734176295034,1.,0.995734176295034,1.,0.995734176295034,1.,0.995734176295034,
1.,0.995734176295034,1.,0.995734176295034,1.,0.995734176295034,1.,0.995734176295034,
1.,0.995734176295034,1.,0.995734176295034,1.,0.995734176295034,1.,0.995734176295034,
1.,0.995734176295034,1.,0.995734176295034,1.,0.995734176295034,1.,0.995734176295034,
1.,0.995734176295034,1.,0.995734176295034,1.,0.995734176295034,1.,0.995734176295034,
1.,0.995734176295034,1.,0.995734176295034,1.,0.995734176295034,1.,0.995734176295034,
1.,0.995734176295034,1.,0.995734176295034,1.,0.995734176295034,1.,0.995734176295034,
1.,0.995734176295034,1.,0.995734176295034,1.,0.995734176295034,1.,0.995734176295034,
1.,0.995734176295034,1.,0.995734176295034,1.,0.995734176295034,1.,0.995734176295034,
1.,0.995734176295034,1.,0.995734176295034,1.,0.995734176295034,1.,0.995734176295034,
1.,0.995734176295034,1.,0.995734176295034,1.,0.995734176295034,1.,0.995734176295034,
1.,0.995734176295034,1.,0.995734176295034,1.,0.995734176295034,1.,0.995734176295034,
1.,0.995734176295034,1.,0.995734176295034,1.,0.995734176295034,1.,0.995734176295034,
1.,0.995734176295034,1.,0.995734176295034,1.,0.995734176295034,1.,0.995734176295034,
1.,0.995734176295034,1.,0.995734176295034,1.,0.995734176295034,1.,0.995734176295034,
1.,0.995734176295034,1.,0.995734176295034,1.,0.995734176295034,1.,0.995734176295034,
1.,0.995734176295034,1.,0.995734176295034,1.,0.995734176295034,1.,0.995734176295034,
1.,0.995734176295034,1.,0.995734176295034,1.,0.995734176295034,1.,0.995734176295034,
1.,0.995734176295034,1.,0.995734176295034,1.,0.995734176295034,1.,0.995734176295034,
1.,0.995734176295034,1.,0.995734176295034,1.,0.995734176295034,1.,0.995734176295034,
1.,0.995734176295034,1.,0.995734176295034,1.,0.995734176295034,1.,0.995734176295034,
1.,0.995734176295034,1.,0.995734176295034,1.,0.995734176295034,1.,0.995734176295034,
1.,0.995734176295034,1.,0.995734176295034,1.,0.995734176295034,1.,0.995734176295034,
1.,0.995734176295034,1.,0.995734176295034,1.,0.995734176295034,1.,0.995734176295034,
1.,0.995734176295034,1.,0.995734176295034,1.,0.995734176295034,1.,0.995734176295034,
1.,0.995734176295034,1.,0.995734176295034,1.,0.995734176295034,1.,0.995734176295034,
1.,0.995734176295034,1.,0.995734176295034,1.,0.995734176295034,1.,0.995734176295034,
1.,0.995734176295034,1.,0.995734176295034,1.,0.995734176295034,1.,0.995734176295034,
1.,0.995734176295034,1.,0.995734176295034,1.,0.995734176295034,1.,0.995734176295034,
1.,0.995734176295034,1.,0.995734176295034,1.,0.995734176295034,1.,0.995734176295034,
1.,0.995734176295034,1.,0.995734176295034,1.,0.995734176295034,1.,0.995734176295034,
1.,0.995734176295034,1.,0.995734176295034,1.,0.995734176295034,1.,0.995734176295034,
1.,0.995734176295034,1.,0.995734176295034,1.,0.995734176295034,1.,0.995734176295034,
1.,0.995734176295034,1.,0.995734176295034,1.,0.995734176295034,1.,0.995734176295034,
1.,0.995734176295034,1.,0.995734176295034,1.,0.995734176295034,1.,0.995734176295034,
1.,0.995734176295034,1.,0.995734176295034,1.,0.995734176295034,1.,0.995734176295034,
1.,0.995734176295034,1.,0.995734176295034,1.,0.995734176295034,1.,0.995734176295034,
1.,0.995734176295034,1.,0.995734176295034,1.,0.995734176295034,1.,0.995734176295034,
1.,0.995734176295034,1.,0.995734176295034,1.,0.995734176295034,1.,0.995734176295034,
1.,0.995734176295034,1.,0.995734176295034,1.,0.995734176295034,1.,0.995734176295034,
1.,0.995734176295034,1.,0.995734176295034,1.,0.995734176295034,1.,0.995734176295034,
1.,0.995734176295034,1.,0.995734176295034,1.,0.995734176295034,1.,0.995734176295034,
1.,0.995734176295034,1.,0.995734176295034,1.,0.995734176295034,1.,0.995734176295034,
1.,0.995734176295034,1.,0.995734176295034,1.,0.995734176295034,1.,0.995734176295034,
1.,0.995734176295034,1.,0.995734176295034,1.,0.995734176295034,1.,0.995734176295034,
1.,0.995734176295034,1.,0.995734176295034,1.,0.995734176295034,1.,0.995734176295034,
1.,0.995734176295034,1.,0.995734176295034,1.,0.995734176295034,1.,0.995734176295034,
1.,0.995734176295034,1.,0.995734176295034,1.,0.995734176295034,1.,0.995734176295034,
1.,0.995734176295034,1.,0.995734176295034,1.,0.995734176295034,1.,0.995734176295034,
1.,0.995734176295034,1.,0.995734176295034,1.,0.995734176295034,1.,0.995734176295034,
1.,0.995734176295034,1.,0.995734176295034,1.,0.995734176295034,1.,0.995734176295034,
1.,0.995734176295034,1.,0.995734176295034,1.,0.995734176295034,1.,0.995734176295034,
1.,0.995734176295034,1.,0.995734176295034,1.,0.995734176295034,1.,0.995734176295034,
1.,0.995734176295034,1.,0.995734176295034,1.,0.995734176295034,1.,0.995734176295034,
1.,0.995734176295034,1.,0.995734176295034,1.,0.995734176295034,1.,0.995734176295034,
1.,0.995734176295034,1.,0.995734176295034,1.,0.995734176295034,1.,0.995734176295034,
1.,0.995734176295034,1.,0.995734176295034,1.,0.995734176295034,1.,0.995734176295034,
1.,0.995734176295034,1.,0.995734176295034,1.,0.995734176295034,1.,0.995734176295034,
1.,0.995734176295034,1.,0.995734176295034,1.,0.995734176295034,1.,0.995734176295034,
1.,0.995734176295034,1.,0.995734176295034,1.,0.995734176295034,1.,0.995734176295034,
1.,0.995734176295034,1.,0.995734176295034,1.,0.995734176295034,1.,0.995734176295034,
1.,0.995734176295034,1.,0.995734176295034,1.,0.995734176295034,1.,0.995734176295034,
1.,0.995734176295034,1.,0.995734176295034,1.,0.995734176295034,1.,0.995734176295034,
1.,0.995734176295034,1.,0.995734176295034,1.,0.995734176295034,1.,0.995734176295034,
1.,0.995734176295034,1.,0.995734176295034,1.,0.995734176295034,1.,0.995734176295034,
1.,0.995734176295034,1.,0.995734176295034,1.,0.995734176295034,1.,0.995734176295034,
1.,0.995734176295034,1.,0.995734176295034,1.,0.995734176295034,1.,0.995734176295034,
1.,0.995734176295034,1.,0.995734176295034,1.,0.995734176295034,1.,0.995734176295034,
1.,0.995734176295034,1.,0.995734176295034,1.,0.995734176295034,1.,0.995734176295034,
1.,0.995734176295034,1.,0.995734176295034,1.,0.995734176295034,1.,0.995734176295034,
1.,0.995734176295034,1.,0.995734176295034,1.,0.995734176295034,1.,0.995734176295034,
1.,0.995734176295034,1.,0.995734176295034,1.,0.995734176295034,1.,0.995734176295034,
1.,0.995734176295034,1.,0.995734176295034,1.,0.995734176295034,1.,0.995734176295034,
1.,0.995734176295034,1.,0.995734176295034,1.,0.995734176295034,1.,0.995734176295034,
1.,0.995734176295034,1.,0.995734176295034,1.,0.995734176295034,1.,0.995734176295034,
1.,0.995734176295034,1.,0.995734176295034,1.,0.995734176295034,1.,0.995734176295034,
1.,0.995734176295034,1.,0.995734176295034,1.,0.995734176295034,1.,0.995734176295034,
1.,0.995734176295034,1.,0.995734176295034,1.,0.995734176295034,1.,0.995734176295034,
1.,0.995734176295034,1.,0.995734176295034,1.,0.995734176295034,1.,0.995734176295034,
1.,0.995734176295034,1.,0.995734176295034,1.,0.995734176295034,1.,0.995734176295034,
1.,0.995734176295034,1.,0.995734176295034,1.,0.995734176295034,1.,0.995734176295034,
1.,0.995734176295034,1.,0.995734176295034,1.,0.995734176295034,1.,0.995734176295034,
1.,0.995734176295034,1.,0.995734176295034,1.,0.995734176295034,1.,0.995734176295034,
1.,0.995734176295034,1.,0.995734176295034,1.,0.995734176295034,1.,0.995734176295034,
1.,0.995734176295034,1.,0.995734176295034,1.,0.995734176295034,1.,0.995734176295034,
1.,0.995734176295034,1.,0.995734176295034,1.,0.995734176295034,1.,0.995734176295034,
1.,0.995734176295034,1.,0.995734176295034,1.,0.995734176295034,1.,0.995734176295034,
1.,0.995734176295034,1.,0.995734176295034,1.,0.995734176295034,1.,0.995734176295034,
1.,0.995734176295034,1.,0.995734176295034,1.,0.995734176295034,1.,0.995734176295034,
1.,0.995734176295034,1.,0.995734176295034,1.,0.995734176295034,1.,0.995734176295034,
1.,0.995734176295034,1.,0.995734176295034,1.,0.995734176295034,1.,0.995734176295034,
1.,0.995734176295034,1.,0.995734176295034,1.,0.995734176295034,1.,0.995734176295034,
1.,0.995734176295034,1.,0.995734176295034,1.,0.995734176295034,1.,0.995734176295034,
1.,0.995734176295034,1.,0.995734176295034,1.,0.995734176295034,1.,0.995734176295034,
1.,0.995734176295034,1.,0.995734176295034,1.,0.995734176295034,1.,0.995734176295034,
1.,0.995734176295034,1.,0.995734176295034,1.,0.995734176295034,1.,0.995734176295034,
1.,0.995734176295034,1.,0.995734176295034,1.,0.995734176295034,1.,0.995734176295034,
1.,0.995734176295034,1.,0.995734176295034,1.,0.995734176295034,1.,0.995734176295034,
1.,0.995734176295034,1.,0.995734176295034,1.,0.995734176295034,1.,0.995734176295034,
1.,0.995734176295034,1.,0.995734176295034,1.,0.995734176295034,1.,0.995734176295034,
1.,0.995734176295034,1.,0.995734176295034,1.,0.995734176295034,1.,0.995734176295034,
1.,0.995734176295034,1.,0.995734176295034,1.,0.995734176295034,1.,0.995734176295034,
1.,0.995734176295034,1.,0.995734176295034,1.,0.995734176295034,1.,0.995734176295034,
1.,0.995734176295034,1.,0.995734176295034,1.,0.995734176295034,1.,0.995734176295034,
1.,0.995734176295034,1.,0.995734176295034,1.,0.995734176295034,1.,0.995734176295034,
1.,0.995734176295034,1.,0.995734176295034,1.,0.995734176295034,1.,0.995734176295034,
1.,0.995734176295034,1.,0.995734176295034,1.,0.995734176295034,1.,0.995734176295034,
1.,0.995734176295034,1.,0.995734176295034,1.,0.995734176295034,1.,0.995734176295034,
1.,0.995734176295034,1.,0.995734176295034,1.,0.995734176295034,1.,0.995734176295034,
1.,0.995734176295034,1.,0.995734176295034,1.,0.995734176295034,1.,0.995734176295034,
1.,0.995734176295034,1.,0.995734176295034,1.,0.995734176295034,1.,0.995734176295034,
1.,0.995734176295034,1.,0.995734176295034,1.,0.995734176295034,1.,0.995734176295034,
1.,0.995734176295034,1.,0.995734176295034,1.,0.995734176295034,1.,0.995734176295034,
1.,0.995734176295034,1.,0.995734176295034,1.,0.995734176295034,1.,0.995734176295034,
1.,0.995734176295034,1.,0.995734176295034,1.,0.995734176295034,1.,0.995734176295034,
1.,0.995734176295034,1.,0.995734176295034,1.,0.995734176295034,1.,0.995734176295034,
1.,0.995734176295034,1.,0.995734176295034,1.,0.995734176295034,1.,0.995734176295034,
1.,0.995734176295034,1.,0.995734176295034,1.,0.995734176295034,1.,0.995734176295034,
1.,0.995734176295034,1.,0.995734176295034,1.,0.995734176295034,1.,0.995734176295034,
1.,0.995734176295034,1.,0.995734176295034,1.,0.995734176295034,1.,0.995734176295034,
1.,0.995734176295034,1.,0.995734176295034,1.,0.995734176295034,1.,0.995734176295034,
1.,0.995734176295034,1.,0.995734176295034,1.,0.995734176295034,1.,0.995734176295034,
1.,0.995734176295034,1.,0.995734176295034,1.,0.995734176295034,1.,0.995734176295034,
1.,0.995734176295034,1.,0.995734176295034,1.,0.995734176295034,1.,0.995734176295034,
1.,0.995734176295034,1.,0.995734176295034,1.,0.995734176295034,1.,0.995734176295034,
1.,0.995734176295034,1.,0.995734176295034,1.,0.995734176295034,1.,0.995734176295034,
1.,0.995734176295034,1.,0.995734176295034,1.,0.995734176295034,1.,0.995734176295034,
1.,0.995734176295034,1.,0.995734176295034,1.,0.995734176295034,1.,0.995734176295034,
1.,0.995734176295034,1.,0.995734176295034,1.,0.995734176295034,1.,0.995734176295034,
1.,0.995734176295034,1.,0.995734176295034,1.,0.995734176295034,1.,0.995734176295034,
1.,0.995734176295034,1.,0.995734176295034,1.,0.995734176295034,1.,0.995734176295034,
1.,0.995734176295034,1.,0.995734176295034,1.,0.995734176295034,1.,0.995734176295034,
1.,0.995734176295034,1.,0.995734176295034,1.,0.995734176295034,1.,0.995734176295034,
1.,0.995734176295034,1.,0.995734176295034,1.,0.995734176295034,1.,0.995734176295034,
1.,0.995734176295034,1.,0.995734176295034,1.,0.995734176295034,1.,0.995734176295034,
1.,0.995734176295034,1.,0.995734176295034,1.,0.995734176295034,1.,0.995734176295034,
1.,0.995734176295034,1.,0.995734176295034,1.,0.995734176295034,1.,0.995734176295034,
1.,0.995734176295034,1.,0.995734176295034,1.,0.995734176295034,1.,0.995734176295034,
1.,0.995734176295034,1.,0.995734176295034,1.,0.995734176295034,1.,0.995734176295034,
1.,0.995734176295034,1.,0.995734176295034,1.,0.995734176295034,1.,0.995734176295034,
1.,0.995734176295034,1.,0.995734176295034,1.,0.995734176295034,1.,0.995734176295034,
1.,0.995734176295034,1.,0.995734176295034,1.,0.995734176295034,1.,0.995734176295034,
1.,0.995734176295034,1.,0.995734176295034,1.,0.995734176295034,1.,0.995734176295034,
1.,0.995734176295034,1.,0.995734176295034,1.,0.995734176295034,1.,0.995734176295034,
1.,0.995734176295034,1.,0.995734176295034,1.,0.995734176295034,1.,0.995734176295034,
1.,0.995734176295034,1.,0.995734176295034,1.,0.995734176295034,1.,0.995734176295034,
1.,0.995734176295034,1.,0.995734176295034,1.,0.995734176295034,1.,0.995734176295034,
1.,0.995734176295034,1.,0.995734176295034,1.,0.995734176295034,1.,0.995734176295034,
1.,0.995734176295034,1.,0.995734176295034,1.,0.995734176295034,1.,0.995734176295034,
1.,0.995734176295034,1.,0.995734176295034,1.,0.995734176295034,1.,0.995734176295034,
1.,0.995734176295034,1.,0.995734176295034,1.,0.995734176295034,1.,0.995734176295034,
1.,0.995734176295034,1.,0.995734176295034,1.,0.995734176295034,1.,0.995734176295034,
1.,0.995734176295034,1.,0.995734176295034,1.,0.995734176295034,1.,0.995734176295034,
1.,0.995734176295034,1.,0.995734176295034,1.,0.995734176295034,1.,0.995734176295034,
1.,0.995734176295034,1.,0.995734176295034,1.,0.995734176295034,1.,0.995734176295034,
1.,0.995734176295034,1.,0.995734176295034,1.,0.995734176295034,1.,0.995734176295034,
1.,0.995734176295034,1.,0.995734176295034,1.,0.995734176295034,1.,0.995734176295034,
1.,0.995734176295034,1.,0.995734176295034,1.,0.995734176295034,1.,0.995734176295034,
1.,0.995734176295034,1.,0.995734176295034,1.,0.995734176295034,1.,0.997201362504479,
0.998074874808407),(1.,0.995734176295034,1.,0.995734176295034,1.,0.995734176295034,
1.,0.995734176295034,1.,0.995734176295034,1.,0.995734176295034,1.,0.995734176295034,
1.,0.995734176295034,1.,0.995734176295034,1.,0.995734176295034,1.,0.995734176295034,
1.,0.995734176295034,1.,0.995734176295034,1.,0.995734176295034,1.,0.995734176295034,
1.,0.995734176295034,1.,0.995734176295034,1.,0.995734176295034,1.,0.995734176295034,
1.,0.995734176295034,1.,0.995734176295034,1.,0.995734176295034,1.,0.995734176295034,
1.,0.995734176295034,1.,0.995734176295034,1.,0.995734176295034,1.,0.995734176295034,
1.,0.995734176295034,1.,0.995734176295034,1.,0.995734176295034,1.,0.995734176295034,
1.,0.995734176295034,1.,0.995734176295034,1.,0.995734176295034,1.,0.995734176295034,
1.,0.995734176295034,1.,0.995734176295034,1.,0.995734176295034,1.,0.995734176295034,
1.,0.995734176295034,1.,0.995734176295034,1.,0.995734176295034,1.,0.995734176295034,
1.,0.995734176295034,1.,0.995734176295034,1.,0.995734176295034,1.,0.995734176295034,
1.,0.995734176295034,1.,0.995734176295034,1.,0.995734176295034,1.,0.995734176295034,
1.,0.995734176295034,1.,0.995734176295034,1.,0.995734176295034,1.,0.995734176295034,
1.,0.995734176295034,1.,0.995734176295034,1.,0.995734176295034,1.,0.995734176295034,
1.,0.995734176295034,1.,0.995734176295034,1.,0.995734176295034,1.,0.995734176295034,
1.,0.995734176295034,1.,0.995734176295034,1.,0.995734176295034,1.,0.995734176295034,
1.,0.995734176295034,1.,0.995734176295034,1.,0.995734176295034,1.,0.995734176295034,
1.,0.995734176295034,1.,0.995734176295034,1.,0.995734176295034,1.,0.995734176295034,
1.,0.995734176295034,1.,0.995734176295034,1.,0.995734176295034,1.,0.995734176295034,
1.,0.995734176295034,1.,0.995734176295034,1.,0.995734176295034,1.,0.995734176295034,
1.,0.995734176295034,1.,0.995734176295034,1.,0.995734176295034,1.,0.995734176295034,
1.,0.995734176295034,1.,0.995734176295034,1.,0.995734176295034,1.,0.995734176295034,
1.,0.995734176295034,1.,0.995734176295034,1.,0.995734176295034,1.,0.995734176295034,
1.,0.995734176295034,1.,0.995734176295034,1.,0.995734176295034,1.,0.995734176295034,
1.,0.995734176295034,1.,0.995734176295034,1.,0.995734176295034,1.,0.995734176295034,
1.,0.995734176295034,1.,0.995734176295034,1.,0.995734176295034,1.,0.995734176295034,
1.,0.995734176295034,1.,0.995734176295034,1.,0.995734176295034,1.,0.995734176295034,
1.,0.995734176295034,1.,0.995734176295034,1.,0.995734176295034,1.,0.995734176295034,
1.,0.995734176295034,1.,0.995734176295034,1.,0.995734176295034,1.,0.995734176295034,
1.,0.995734176295034,1.,0.995734176295034,1.,0.995734176295034,1.,0.995734176295034,
1.,0.995734176295034,1.,0.995734176295034,1.,0.995734176295034,1.,0.995734176295034,
1.,0.995734176295034,1.,0.995734176295034,1.,0.995734176295034,1.,0.995734176295034,
1.,0.995734176295034,1.,0.995734176295034,1.,0.995734176295034,1.,0.995734176295034,
1.,0.995734176295034,1.,0.995734176295034,1.,0.995734176295034,1.,0.995734176295034,
1.,0.995734176295034,1.,0.995734176295034,1.,0.995734176295034,1.,0.995734176295034,
1.,0.995734176295034,1.,0.995734176295034,1.,0.995734176295034,1.,0.995734176295034,
1.,0.995734176295034,1.,0.995734176295034,1.,0.995734176295034,1.,0.995734176295034,
1.,0.995734176295034,1.,0.995734176295034,1.,0.995734176295034,1.,0.995734176295034,
1.,0.995734176295034,1.,0.995734176295034,1.,0.995734176295034,1.,0.995734176295034,
1.,0.995734176295034,1.,0.995734176295034,1.,0.995734176295034,1.,0.995734176295034,
1.,0.995734176295034,1.,0.995734176295034,1.,0.995734176295034,1.,0.995734176295034,
1.,0.995734176295034,1.,0.995734176295034,1.,0.995734176295034,1.,0.995734176295034,
1.,0.995734176295034,1.,0.995734176295034,1.,0.995734176295034,1.,0.995734176295034,
1.,0.995734176295034,1.,0.995734176295034,1.,0.995734176295034,1.,0.995734176295034,
1.,0.995734176295034,1.,0.995734176295034,1.,0.995734176295034,1.,0.995734176295034,
1.,0.995734176295034,1.,0.995734176295034,1.,0.995734176295034,1.,0.995734176295034,
1.,0.995734176295034,1.,0.995734176295034,1.,0.995734176295034,1.,0.995734176295034,
1.,0.995734176295034,1.,0.995734176295034,1.,0.995734176295034,1.,0.995734176295034,
1.,0.995734176295034,1.,0.995734176295034,1.,0.995734176295034,1.,0.995734176295034,
1.,0.995734176295034,1.,0.995734176295034,1.,0.995734176295034,1.,0.995734176295034,
1.,0.995734176295034,1.,0.995734176295034,1.,0.995734176295034,1.,0.995734176295034,
1.,0.995734176295034,1.,0.995734176295034,1.,0.995734176295034,1.,0.995734176295034,
1.,0.995734176295034,1.,0.995734176295034,1.,0.995734176295034,1.,0.995734176295034,
1.,0.995734176295034,1.,0.995734176295034,1.,0.995734176295034,1.,0.995734176295034,
1.,0.995734176295034,1.,0.995734176295034,1.,0.995734176295034,1.,0.995734176295034,
1.,0.995734176295034,1.,0.995734176295034,1.,0.995734176295034,1.,0.995734176295034,
1.,0.995734176295034,1.,0.995734176295034,1.,0.995734176295034,1.,0.995734176295034,
1.,0.995734176295034,1.,0.995734176295034,1.,0.995734176295034,1.,0.995734176295034,
1.,0.995734176295034,1.,0.995734176295034,1.,0.995734176295034,1.,0.995734176295034,
1.,0.995734176295034,1.,0.995734176295034,1.,0.995734176295034,1.,0.995734176295034,
1.,0.995734176295034,1.,0.995734176295034,1.,0.995734176295034,1.,0.995734176295034,
1.,0.995734176295034,1.,0.995734176295034,1.,0.995734176295034,1.,0.995734176295034,
1.,0.995734176295034,1.,0.995734176295034,1.,0.995734176295034,1.,0.995734176295034,
1.,0.995734176295034,1.,0.995734176295034,1.,0.995734176295034,1.,0.995734176295034,
1.,0.995734176295034,1.,0.995734176295034,1.,0.995734176295034,1.,0.995734176295034,
1.,0.995734176295034,1.,0.995734176295034,1.,0.995734176295034,1.,0.995734176295034,
1.,0.995734176295034,1.,0.995734176295034,1.,0.995734176295034,1.,0.995734176295034,
1.,0.995734176295034,1.,0.995734176295034,1.,0.995734176295034,1.,0.995734176295034,
1.,0.995734176295034,1.,0.995734176295034,1.,0.995734176295034,1.,0.995734176295034,
1.,0.995734176295034,1.,0.995734176295034,1.,0.995734176295034,1.,0.995734176295034,
1.,0.995734176295034,1.,0.995734176295034,1.,0.995734176295034,1.,0.995734176295034,
1.,0.995734176295034,1.,0.995734176295034,1.,0.995734176295034,1.,0.995734176295034,
1.,0.995734176295034,1.,0.995734176295034,1.,0.995734176295034,1.,0.995734176295034,
1.,0.995734176295034,1.,0.995734176295034,1.,0.995734176295034,1.,0.995734176295034,
1.,0.995734176295034,1.,0.995734176295034,1.,0.995734176295034,1.,0.995734176295034,
1.,0.995734176295034,1.,0.995734176295034,1.,0.995734176295034,1.,0.995734176295034,
1.,0.995734176295034,1.,0.995734176295034,1.,0.995734176295034,1.,0.995734176295034,
1.,0.995734176295034,1.,0.995734176295034,1.,0.995734176295034,1.,0.995734176295034,
1.,0.995734176295034,1.,0.995734176295034,1.,0.995734176295034,1.,0.995734176295034,
1.,0.995734176295034,1.,0.995734176295034,1.,0.995734176295034,1.,0.995734176295034,
1.,0.995734176295034,1.,0.995734176295034,1.,0.995734176295034,1.,0.995734176295034,
1.,0.995734176295034,1.,0.995734176295034,1.,0.995734176295034,1.,0.995734176295034,
1.,0.995734176295034,1.,0.995734176295034,1.,0.995734176295034,1.,0.995734176295034,
1.,0.995734176295034,1.,0.995734176295034,1.,0.995734176295034,1.,0.995734176295034,
1.,0.995734176295034,1.,0.995734176295034,1.,0.995734176295034,1.,0.995734176295034,
1.,0.995734176295034,1.,0.995734176295034,1.,0.995734176295034,1.,0.995734176295034,
1.,0.995734176295034,1.,0.995734176295034,1.,0.995734176295034,1.,0.995734176295034,
1.,0.995734176295034,1.,0.995734176295034,1.,0.995734176295034,1.,0.995734176295034,
1.,0.995734176295034,1.,0.995734176295034,1.,0.995734176295034,1.,0.995734176295034,
1.,0.995734176295034,1.,0.995734176295034,1.,0.995734176295034,1.,0.995734176295034,
1.,0.995734176295034,1.,0.995734176295034,1.,0.995734176295034,1.,0.995734176295034,
1.,0.995734176295034,1.,0.995734176295034,1.,0.995734176295034,1.,0.995734176295034,
1.,0.995734176295034,1.,0.995734176295034,1.,0.995734176295034,1.,0.995734176295034,
1.,0.995734176295034,1.,0.995734176295034,1.,0.995734176295034,1.,0.995734176295034,
1.,0.995734176295034,1.,0.995734176295034,1.,0.995734176295034,1.,0.995734176295034,
1.,0.995734176295034,1.,0.995734176295034,1.,0.995734176295034,1.,0.995734176295034,
1.,0.995734176295034,1.,0.995734176295034,1.,0.995734176295034,1.,0.995734176295034,
1.,0.995734176295034,1.,0.995734176295034,1.,0.995734176295034,1.,0.995734176295034,
1.,0.995734176295034,1.,0.995734176295034,1.,0.995734176295034,1.,0.995734176295034,
1.,0.995734176295034,1.,0.995734176295034,1.,0.995734176295034,1.,0.995734176295034,
1.,0.995734176295034,1.,0.995734176295034,1.,0.995734176295034,1.,0.995734176295034,
1.,0.995734176295034,1.,0.995734176295034,1.,0.995734176295034,1.,0.995734176295034,
1.,0.995734176295034,1.,0.995734176295034,1.,0.995734176295034,1.,0.995734176295034,
1.,0.995734176295034,1.,0.995734176295034,1.,0.995734176295034,1.,0.995734176295034,
1.,0.995734176295034,1.,0.995734176295034,1.,0.995734176295034,1.,0.995734176295034,
1.,0.995734176295034,1.,0.995734176295034,1.,0.995734176295034,1.,0.995734176295034,
1.,0.995734176295034,1.,0.995734176295034,1.,0.995734176295034,1.,0.995734176295034,
1.,0.995734176295034,1.,0.995734176295034,1.,0.995734176295034,1.,0.995734176295034,
1.,0.995734176295034,1.,0.995734176295034,1.,0.995734176295034,1.,0.995734176295034,
1.,0.995734176295034,1.,0.995734176295034,1.,0.995734176295034,1.,0.995734176295034,
1.,0.995734176295034,1.,0.995734176295034,1.,0.995734176295034,1.,0.995734176295034,
1.,0.995734176295034,1.,0.995734176295034,1.,0.995734176295034,1.,0.995734176295034,
1.,0.995734176295034,1.,0.995734176295034,1.,0.995734176295034,1.,0.995734176295034,
1.,0.995734176295034,1.,0.995734176295034,1.,0.995734176295034,1.,0.995734176295034,
1.,0.995734176295034,1.,0.995734176295034,1.,0.995734176295034,1.,0.995734176295034,
1.,0.995734176295034,1.,0.995734176295034,1.,0.995734176295034,1.,0.995734176295034,
1.,0.995734176295034,1.,0.995734176295034,1.,0.995734176295034,1.,0.995734176295034,
1.,0.995734176295034,1.,0.995734176295034,1.,0.995734176295034,1.,0.995734176295034,
1.,0.995734176295034,1.,0.995734176295034,1.,0.995734176295034,1.,0.995734176295034,
1.,0.995734176295034,1.,0.995734176295034,1.,0.995734176295034,1.,0.995734176295034,
1.,0.995734176295034,1.,0.995734176295034,1.,0.995734176295034,1.,0.995734176295034,
1.,0.995734176295034,1.,0.995734176295034,1.,0.995734176295034,1.,0.995734176295034,
1.,0.995734176295034,1.,0.995734176295034,1.,0.995734176295034,1.,0.995734176295034,
1.,0.995734176295034,1.,0.995734176295034,1.,0.995734176295034,1.,0.995734176295034,
1.,0.995734176295034,1.,0.995734176295034,1.,0.995734176295034,1.,0.995734176295034,
1.,0.995734176295034,1.,0.995734176295034,1.,0.995734176295034,1.,0.995734176295034,
1.,0.995734176295034,1.,0.995734176295034,1.,0.995734176295034,1.,0.995734176295034,
1.,0.995734176295034,1.,0.995734176295034,1.,0.995734176295034,1.,0.995734176295034,
1.,0.995734176295034,1.,0.995734176295034,1.,0.995734176295034,1.,0.995734176295034,
1.,0.995734176295034,1.,0.995734176295034,1.,0.995734176295034,1.,0.995734176295034,
1.,0.995734176295034,1.,0.995734176295034,1.,0.995734176295034,1.,0.995734176295034,
1.,0.995734176295034,1.,0.995734176295034,1.,0.995734176295034,1.,0.995734176295034,
1.,0.995734176295034,1.,0.995734176295034,1.,0.995734176295034,1.,0.995734176295034,
1.,0.995734176295034,1.,0.995734176295034,1.,0.995734176295034,1.,0.995734176295034,
1.,0.995734176295034,1.,0.995734176295034,1.,0.995734176295034,1.,0.995734176295034,
1.,0.995734176295034,1.,0.995734176295034,1.,0.995734176295034,1.,0.995734176295034,
1.,0.995734176295034,1.,0.995734176295034,1.,0.995734176295034,1.,0.995734176295034,
1.,0.995734176295034,1.,0.995734176295034,1.,0.995734176295034,1.,0.995734176295034,
1.,0.995734176295034,1.,0.995734176295034,1.,0.995734176295034,1.,0.995734176295034,
1.,0.995734176295034,1.,0.995734176295034,1.,0.995734176295034,1.,0.995734176295034,
1.,0.995734176295034,1.,0.995734176295034,1.,0.995734176295034,1.,0.995734176295034,
1.,0.995734176295034,1.,0.995734176295034,1.,0.995734176295034,1.,0.995734176295034,
1.,0.995734176295034,1.,0.995734176295034,1.,0.995734176295034,1.,0.995734176295034,
1.,0.995734176295034,1.,0.995734176295034,1.,0.995734176295034,1.,0.995734176295034,
1.,0.995734176295034,1.,0.995734176295034,1.,0.995734176295034,1.,0.995734176295034,
1.,0.995734176295034,1.,0.995734176295034,1.,0.995734176295034,1.,0.995734176295034,
1.,0.995734176295034,1.,0.995734176295034,1.,0.995734176295034,1.,0.995734176295034,
1.,0.995734176295034,1.,0.995734176295034,1.,0.995734176295034,1.,0.995734176295034,
1.,0.995734176295034,1.,0.995734176295034,1.,0.995734176295034,1.,0.995734176295034,
1.,0.995734176295034,1.,0.995734176295034,1.,0.995734176295034,1.,0.995734176295034,
1.,0.995734176295034,1.,0.995734176295034,1.,0.995734176295034,1.,0.995734176295034,
1.,0.995734176295034,1.,0.995734176295034,1.,0.995734176295034,1.,0.995734176295034,
1.,0.995734176295034,1.,0.995734176295034,1.,0.995734176295034,1.,0.995734176295034,
1.,0.995734176295034,1.,0.995734176295034,1.,0.995734176295034,1.,0.995734176295034,
1.,0.995734176295034,1.,0.995734176295034,1.,0.995734176295034,1.,0.995734176295034,
1.,0.995734176295034,1.,0.995734176295034,1.,0.995734176295034,1.,0.995734176295034,
1.,0.995734176295034,1.,0.995734176295034,1.,0.995734176295034,1.,0.995734176295034,
1.,0.995734176295034,1.,0.995734176295034,1.,0.995734176295034,1.,0.995734176295034,
1.,0.995734176295034,1.,0.995734176295034,1.,0.995734176295034,1.,0.995734176295034,
1.,0.995734176295034,1.,0.995734176295034,1.,0.995734176295034,1.,0.995734176295034,
1.,0.995734176295034,1.,0.995734176295034,1.,0.995734176295034,1.,0.995734176295034,
1.,0.995734176295034,1.,0.995734176295034,1.,0.995734176295034,1.,0.995734176295034,
1.,0.995734176295034,1.,0.995734176295034,1.,0.995734176295034,1.,0.995734176295034,
1.,0.995734176295034,1.,0.995734176295034,1.,0.995734176295034,1.,0.995734176295034,
1.,0.995734176295034,1.,0.995734176295034,1.,0.995734176295034,1.,0.995734176295034,
1.,0.995734176295034,1.,0.995734176295034,1.,0.995734176295034,1.,0.995734176295034,
1.,0.995734176295034,1.,0.995734176295034,1.,0.995734176295034,1.,0.995734176295034,
1.,0.995734176295034,1.,0.995734176295034,1.,0.995734176295034,1.,0.995734176295034,
1.,0.995734176295034,1.,0.995734176295034,1.,0.995734176295034,1.,0.995734176295034,
1.,0.995734176295034,1.,0.995734176295034,1.,0.995734176295034,1.,0.995734176295034,
1.,0.995734176295034,1.,0.995734176295034,1.,0.995734176295034,1.,0.995734176295034,
1.,0.995734176295034,1.,0.995734176295034,1.,0.995734176295034,1.,0.995734176295034,
1.,0.995734176295034,1.,0.995734176295034,1.,0.995734176295034,1.,0.995734176295034,
1.,0.995734176295034,1.,0.995734176295034,1.,0.995734176295034,1.,0.995734176295034,
1.,0.995734176295034,1.,0.995734176295034,1.,0.995734176295034,1.,0.995734176295034,
1.,0.995734176295034,1.,0.995734176295034,1.,0.995734176295034,1.,0.995734176295034,
1.,0.995734176295034,1.,0.995734176295034,1.,0.995734176295034,1.,0.995734176295034,
1.,0.995734176295034,1.,0.995734176295034,1.,0.995734176295034,1.,0.995734176295034,
1.,0.995734176295034,1.,0.995734176295034,1.,0.995734176295034,1.,0.995734176295034,
1.,0.995734176295034,1.,0.995734176295034,1.,0.995734176295034,1.,0.995734176295034,
1.,0.995734176295034,1.,0.995734176295034,1.,0.995734176295034,1.,0.995734176295034,
1.,0.995734176295034,1.,0.995734176295034,1.,0.995734176295034,1.,0.995734176295034,
1.,0.995734176295034,1.,0.995734176295034,1.,0.995734176295034,1.,0.995734176295034,
1.,0.995734176295034,1.,0.995734176295034,1.,0.995734176295034,1.,0.995734176295034,
1.,0.995734176295034,1.,0.995734176295034,1.,0.995734176295034,1.,0.995734176295034,
1.,0.995734176295034,1.,0.995734176295034,1.,0.995734176295034,1.,0.995734176295034,
1.,0.995734176295034,1.,0.995734176295034,1.,0.995734176295034,1.,0.995734176295034,
1.,0.995734176295034,1.,0.995734176295034,1.,0.995734176295034,1.,0.995734176295034,
1.,0.995734176295034,1.,0.995734176295034,1.,0.995734176295034,1.,0.995734176295034,
1.,0.995734176295034,1.,0.995734176295034,1.,0.995734176295034,1.,0.995734176295034,
1.,0.995734176295034,1.,0.995734176295034,1.,0.995734176295034,1.,0.995734176295034,
1.,0.995734176295034,1.,0.995734176295034,1.,0.995734176295034,1.,0.995734176295034,
1.,0.995734176295034,1.,0.995734176295034,1.,0.995734176295034,1.,0.995734176295034,
1.,0.995734176295034,1.,0.995734176295034,1.,0.995734176295034,1.,0.995734176295034,
1.,0.995734176295034,1.,0.995734176295034,1.,0.995734176295034,1.,0.995734176295034,
1.,0.995734176295034,1.,0.995734176295034,1.,0.995734176295034,1.,0.995734176295034,
1.,0.995734176295034,1.,0.995734176295034,1.,0.995734176295034,1.,0.995734176295034,
1.,0.995734176295034,1.,0.995734176295034,1.,0.995734176295034,1.,0.995734176295034,
1.,0.995734176295034,1.,0.995734176295034,1.,0.995734176295034,1.,0.995734176295034,
1.,0.995734176295034,1.,0.995734176295034,1.,0.995734176295034,1.,0.995734176295034,
1.,0.995734176295034,1.,0.995734176295034,1.,0.995734176295034,1.,0.995734176295034,
1.,0.995734176295034,1.,0.995734176295034,1.,0.995734176295034,1.,0.995734176295034,
1.,0.995734176295034,1.,0.995734176295034,1.,0.995734176295034,1.,0.995734176295034,
1.,0.995734176295034,1.,0.995734176295034,1.,0.995734176295034,1.,0.995734176295034,
1.,0.995734176295034,1.,0.995734176295034,1.,0.995734176295034,1.,0.995734176295034,
1.,0.995734176295034,1.,0.995734176295034,1.,0.995734176295034,1.,0.995734176295034,
1.,0.995734176295034,1.,0.995734176295034,1.,0.995734176295034,1.,0.995734176295034,
1.,0.995734176295034,1.,0.995734176295034,1.,0.995734176295034,1.,0.995734176295034,
1.,0.995734176295034,1.,0.995734176295034,1.,0.995734176295034,1.,0.995734176295034,
1.,0.995734176295034,1.,0.995734176295034,1.,0.995734176295034,1.,0.995734176295034,
1.,0.995734176295034,1.,0.995734176295034,1.,0.995734176295034,1.,0.995734176295034,
1.,0.995734176295034,1.,0.995734176295034,1.,0.995734176295034,1.,0.995734176295034,
1.,0.995734176295034,1.,0.995734176295034,1.,0.995734176295034,1.,0.995734176295034,
1.,0.995734176295034,1.,0.995734176295034,1.,0.995734176295034,1.,0.995734176295034,
1.,0.995734176295034,1.,0.995734176295034,1.,0.995734176295034,1.,0.995734176295034,
1.,0.995734176295034,1.,0.995734176295034,1.,0.995734176295034,1.,0.995734176295034,
1.,0.995734176295034,1.,0.995734176295034,1.,0.995734176295034,1.,0.995734176295034,
1.,0.995734176295034,1.,0.995734176295034,1.,0.995734176295034,1.,0.995734176295034,
1.,0.995734176295034,1.,0.995734176295034,1.,0.995734176295034,1.,0.995734176295034,
1.,0.995734176295034,1.,0.995734176295034,1.,0.995734176295034,1.,0.995734176295034,
1.,0.995734176295034,1.,0.995734176295034,1.,0.995734176295034,1.,0.995734176295034,
1.,0.995734176295034,1.,0.995734176295034,1.,0.995734176295034,1.,0.995734176295034,
1.,0.995734176295034,1.,0.995734176295034,1.,0.995734176295034,1.,0.995734176295034,
1.,0.995734176295034,1.,0.995734176295034,1.,0.995734176295034,1.,0.995734176295034,
1.,0.995734176295034,1.,0.995734176295034,1.,0.995734176295034,1.,0.995734176295034,
1.,0.995734176295034,1.,0.995734176295034,1.,0.995734176295034,1.,0.995734176295034,
1.,0.995734176295034,1.,0.995734176295034,1.,0.995734176295034,1.,0.995734176295034,
1.,0.995734176295034,1.,0.995734176295034,1.,0.995734176295034,1.,0.995734176295034,
1.,0.995734176295034,1.,0.995734176295034,1.,0.995734176295034,1.,0.995734176295034,
1.,0.995734176295034,1.,0.995734176295034,1.,0.995734176295034,1.,0.995734176295034,
1.,0.995734176295034,1.,0.995734176295034,1.,0.995734176295034,1.,0.995734176295034,
1.,0.995734176295034,1.,0.995734176295034,1.,0.995734176295034,1.,0.995734176295034,
1.,0.995734176295034,1.,0.995734176295034,1.,0.995734176295034,1.,0.995734176295034,
1.,0.995734176295034,1.,0.995734176295034,1.,0.995734176295034,1.,0.995734176295034,
1.,0.995734176295034,1.,0.995734176295034,1.,0.995734176295034,1.,0.995734176295034,
1.,0.995734176295034,1.,0.995734176295034,1.,0.995734176295034,1.,0.995734176295034,
1.,0.995734176295034,1.,0.995734176295034,1.,0.995734176295034,1.,0.995734176295034,
1.,0.995734176295034,1.,0.995734176295034,1.,0.995734176295034,1.,0.995734176295034,
1.,0.995734176295034,1.,0.995734176295034,1.,0.995734176295034,1.,0.995734176295034,
1.,0.995734176295034,1.,0.995734176295034,1.,0.995734176295034,1.,0.995734176295034,
1.,0.995734176295034,1.,0.995734176295034,1.,0.995734176295034,1.,0.995734176295034,
1.,0.995734176295034,1.,0.995734176295034,1.,0.995734176295034,1.,0.995734176295034,
1.,0.995734176295034,1.,0.995734176295034,1.,0.995734176295034,1.,0.995734176295034,
1.,0.995734176295034,1.,0.995734176295034,1.,0.995734176295034,1.,0.995734176295034,
1.,0.995734176295034,1.,0.995734176295034,1.,0.995734176295034,1.,0.995734176295034,
1.,0.995734176295034,1.,0.995734176295034,1.,0.995734176295034,1.,0.995734176295034,
1.,0.995734176295034,1.,0.995734176295034,1.,0.995734176295034,1.,0.995734176295034,
1.,0.995734176295034,1.,0.995734176295034,1.,0.995734176295034,1.,0.995734176295034,
1.,0.995734176295034,1.,0.995734176295034,1.,0.995734176295034,1.,0.995734176295034,
1.,0.995734176295034,1.,0.995734176295034,1.,0.995734176295034,1.,0.995734176295034,
1.,0.995734176295034,1.,0.995734176295034,1.,0.997201362504479,0.998074874808407)))
REPRESENTATION_ITEM('')
SURFACE()
);
#2505=(
BOUNDED_SURFACE()
B_SPLINE_SURFACE(1,2,((#163107,#163108,#163109,#163110,#163111,#163112,
#163113,#163114,#163115,#163116,#163117,#163118,#163119,#163120,#163121,
#163122,#163123,#163124,#163125,#163126,#163127,#163128,#163129,#163130,
#163131,#163132,#163133,#163134,#163135,#163136,#163137,#163138,#163139,
#163140,#163141,#163142,#163143,#163144,#163145,#163146,#163147,#163148,
#163149,#163150,#163151,#163152,#163153,#163154,#163155,#163156,#163157,
#163158,#163159,#163160,#163161,#163162,#163163,#163164,#163165,#163166,
#163167,#163168,#163169,#163170,#163171,#163172,#163173,#163174,#163175,
#163176,#163177,#163178,#163179,#163180,#163181,#163182,#163183,#163184,
#163185,#163186,#163187,#163188,#163189,#163190,#163191,#163192,#163193,
#163194,#163195,#163196,#163197,#163198,#163199,#163200,#163201,#163202,
#163203,#163204,#163205,#163206,#163207,#163208,#163209,#163210,#163211,
#163212,#163213,#163214,#163215,#163216,#163217,#163218,#163219,#163220,
#163221,#163222,#163223,#163224,#163225,#163226,#163227,#163228,#163229,
#163230,#163231,#163232,#163233,#163234,#163235,#163236,#163237,#163238,
#163239,#163240,#163241,#163242,#163243,#163244,#163245,#163246,#163247,
#163248,#163249,#163250,#163251,#163252,#163253,#163254,#163255,#163256,
#163257,#163258,#163259,#163260,#163261,#163262,#163263,#163264,#163265,
#163266,#163267,#163268,#163269,#163270,#163271,#163272,#163273,#163274,
#163275,#163276,#163277,#163278,#163279,#163280,#163281,#163282,#163283,
#163284,#163285,#163286,#163287,#163288,#163289,#163290,#163291,#163292,
#163293,#163294,#163295,#163296,#163297,#163298,#163299,#163300,#163301,
#163302,#163303,#163304,#163305,#163306,#163307,#163308,#163309,#163310,
#163311,#163312,#163313,#163314,#163315,#163316,#163317,#163318,#163319,
#163320,#163321,#163322,#163323,#163324,#163325,#163326,#163327,#163328,
#163329,#163330,#163331,#163332,#163333,#163334,#163335,#163336,#163337,
#163338,#163339,#163340,#163341,#163342,#163343,#163344,#163345,#163346,
#163347,#163348,#163349,#163350,#163351,#163352,#163353,#163354,#163355,
#163356,#163357,#163358,#163359,#163360,#163361,#163362,#163363,#163364,
#163365,#163366,#163367,#163368,#163369,#163370,#163371,#163372,#163373,
#163374,#163375,#163376,#163377,#163378,#163379,#163380,#163381,#163382,
#163383,#163384,#163385,#163386,#163387,#163388,#163389,#163390,#163391,
#163392,#163393,#163394,#163395,#163396,#163397,#163398,#163399,#163400,
#163401,#163402,#163403,#163404,#163405,#163406,#163407,#163408,#163409,
#163410,#163411,#163412,#163413,#163414,#163415,#163416,#163417,#163418,
#163419,#163420,#163421,#163422,#163423,#163424,#163425,#163426,#163427,
#163428,#163429,#163430,#163431,#163432,#163433,#163434,#163435,#163436,
#163437,#163438,#163439,#163440,#163441,#163442,#163443,#163444,#163445,
#163446,#163447,#163448,#163449,#163450,#163451,#163452,#163453,#163454,
#163455,#163456,#163457,#163458,#163459,#163460,#163461,#163462,#163463,
#163464,#163465,#163466,#163467,#163468,#163469,#163470,#163471,#163472,
#163473,#163474,#163475,#163476,#163477,#163478,#163479,#163480,#163481,
#163482,#163483,#163484,#163485,#163486,#163487,#163488,#163489,#163490,
#163491,#163492,#163493,#163494,#163495,#163496,#163497,#163498,#163499,
#163500,#163501,#163502,#163503,#163504,#163505,#163506,#163507,#163508,
#163509,#163510,#163511,#163512,#163513,#163514,#163515,#163516,#163517,
#163518,#163519,#163520,#163521,#163522,#163523,#163524,#163525,#163526,
#163527,#163528,#163529,#163530,#163531,#163532,#163533,#163534,#163535,
#163536,#163537,#163538,#163539,#163540,#163541,#163542,#163543,#163544,
#163545,#163546,#163547,#163548,#163549,#163550,#163551,#163552,#163553,
#163554,#163555,#163556,#163557,#163558,#163559,#163560,#163561,#163562,
#163563,#163564,#163565,#163566,#163567,#163568,#163569,#163570,#163571,
#163572,#163573,#163574,#163575,#163576,#163577,#163578,#163579,#163580,
#163581,#163582,#163583,#163584,#163585,#163586,#163587,#163588,#163589,
#163590,#163591,#163592,#163593,#163594,#163595,#163596,#163597,#163598,
#163599,#163600,#163601,#163602,#163603,#163604,#163605,#163606,#163607,
#163608,#163609,#163610,#163611,#163612,#163613,#163614,#163615,#163616,
#163617,#163618,#163619,#163620,#163621,#163622,#163623,#163624,#163625,
#163626,#163627,#163628,#163629,#163630,#163631,#163632,#163633,#163634,
#163635,#163636,#163637,#163638,#163639,#163640,#163641,#163642,#163643,
#163644,#163645,#163646,#163647,#163648,#163649,#163650,#163651,#163652,
#163653,#163654,#163655,#163656,#163657,#163658,#163659,#163660,#163661,
#163662,#163663,#163664,#163665,#163666,#163667,#163668,#163669,#163670,
#163671,#163672,#163673,#163674,#163675,#163676,#163677,#163678,#163679,
#163680,#163681,#163682,#163683,#163684,#163685,#163686,#163687,#163688,
#163689,#163690,#163691,#163692,#163693,#163694,#163695,#163696,#163697,
#163698,#163699,#163700,#163701,#163702,#163703,#163704,#163705,#163706,
#163707,#163708,#163709,#163710,#163711,#163712,#163713,#163714,#163715,
#163716,#163717,#163718,#163719,#163720,#163721,#163722,#163723,#163724,
#163725,#163726,#163727,#163728,#163729,#163730,#163731,#163732,#163733,
#163734,#163735,#163736,#163737,#163738,#163739,#163740,#163741,#163742,
#163743,#163744,#163745,#163746,#163747,#163748,#163749,#163750,#163751,
#163752,#163753,#163754,#163755,#163756,#163757,#163758,#163759,#163760,
#163761,#163762,#163763,#163764,#163765,#163766,#163767,#163768,#163769,
#163770,#163771,#163772,#163773,#163774,#163775,#163776,#163777,#163778,
#163779,#163780,#163781,#163782,#163783,#163784,#163785,#163786,#163787,
#163788,#163789,#163790,#163791,#163792,#163793,#163794,#163795,#163796,
#163797,#163798,#163799,#163800,#163801,#163802,#163803,#163804,#163805,
#163806,#163807,#163808,#163809,#163810,#163811,#163812,#163813,#163814,
#163815,#163816,#163817,#163818,#163819,#163820,#163821,#163822,#163823,
#163824,#163825,#163826,#163827,#163828,#163829,#163830,#163831,#163832,
#163833,#163834,#163835,#163836,#163837,#163838,#163839,#163840,#163841,
#163842,#163843,#163844,#163845,#163846,#163847,#163848,#163849,#163850,
#163851,#163852,#163853,#163854,#163855,#163856,#163857,#163858,#163859,
#163860,#163861,#163862,#163863,#163864,#163865,#163866,#163867,#163868,
#163869,#163870,#163871,#163872,#163873,#163874,#163875,#163876,#163877,
#163878,#163879,#163880,#163881,#163882,#163883,#163884,#163885,#163886,
#163887,#163888,#163889,#163890,#163891,#163892,#163893,#163894,#163895,
#163896,#163897,#163898,#163899,#163900,#163901,#163902,#163903,#163904,
#163905,#163906,#163907,#163908,#163909,#163910,#163911,#163912,#163913,
#163914,#163915,#163916,#163917,#163918,#163919,#163920,#163921,#163922,
#163923,#163924,#163925,#163926,#163927,#163928,#163929,#163930,#163931,
#163932,#163933,#163934,#163935,#163936,#163937,#163938,#163939,#163940,
#163941,#163942,#163943,#163944,#163945,#163946,#163947,#163948,#163949,
#163950,#163951,#163952,#163953,#163954,#163955,#163956,#163957,#163958,
#163959,#163960,#163961,#163962,#163963,#163964,#163965,#163966,#163967,
#163968,#163969,#163970,#163971,#163972,#163973,#163974,#163975,#163976,
#163977,#163978,#163979,#163980,#163981,#163982,#163983,#163984,#163985,
#163986,#163987,#163988,#163989,#163990,#163991,#163992,#163993,#163994,
#163995,#163996,#163997,#163998,#163999,#164000,#164001,#164002,#164003,
#164004,#164005,#164006,#164007,#164008,#164009,#164010,#164011,#164012,
#164013,#164014,#164015,#164016,#164017,#164018,#164019,#164020,#164021,
#164022,#164023,#164024,#164025,#164026,#164027,#164028,#164029,#164030,
#164031,#164032,#164033,#164034,#164035,#164036,#164037,#164038,#164039,
#164040,#164041,#164042,#164043,#164044,#164045,#164046,#164047,#164048,
#164049,#164050,#164051,#164052,#164053,#164054,#164055,#164056,#164057,
#164058,#164059,#164060,#164061,#164062,#164063,#164064,#164065,#164066,
#164067,#164068,#164069,#164070,#164071,#164072,#164073,#164074,#164075,
#164076,#164077,#164078,#164079,#164080,#164081,#164082,#164083,#164084,
#164085,#164086,#164087,#164088,#164089,#164090,#164091,#164092,#164093,
#164094,#164095,#164096,#164097,#164098,#164099,#164100,#164101,#164102,
#164103,#164104,#164105,#164106,#164107,#164108,#164109,#164110,#164111,
#164112,#164113,#164114,#164115,#164116,#164117,#164118,#164119,#164120,
#164121,#164122,#164123,#164124,#164125,#164126,#164127,#164128,#164129,
#164130,#164131,#164132,#164133,#164134,#164135,#164136,#164137,#164138,
#164139,#164140,#164141,#164142,#164143,#164144,#164145,#164146,#164147,
#164148,#164149,#164150,#164151,#164152,#164153,#164154,#164155,#164156,
#164157,#164158,#164159,#164160,#164161,#164162,#164163,#164164,#164165,
#164166,#164167,#164168,#164169,#164170,#164171,#164172,#164173,#164174,
#164175,#164176,#164177,#164178,#164179,#164180,#164181,#164182,#164183,
#164184,#164185,#164186,#164187,#164188,#164189,#164190,#164191,#164192,
#164193,#164194,#164195,#164196,#164197,#164198,#164199,#164200,#164201,
#164202,#164203,#164204,#164205,#164206,#164207,#164208,#164209,#164210,
#164211,#164212,#164213,#164214,#164215,#164216,#164217,#164218,#164219,
#164220,#164221,#164222,#164223,#164224,#164225,#164226,#164227,#164228,
#164229,#164230,#164231,#164232,#164233,#164234,#164235,#164236,#164237,
#164238,#164239,#164240,#164241,#164242,#164243,#164244,#164245,#164246,
#164247,#164248,#164249,#164250,#164251,#164252,#164253,#164254,#164255,
#164256,#164257,#164258,#164259,#164260,#164261,#164262,#164263,#164264,
#164265,#164266,#164267,#164268,#164269,#164270,#164271,#164272,#164273,
#164274,#164275,#164276,#164277,#164278,#164279,#164280,#164281,#164282,
#164283,#164284,#164285,#164286,#164287,#164288,#164289,#164290,#164291,
#164292,#164293,#164294,#164295,#164296,#164297,#164298,#164299,#164300,
#164301,#164302,#164303,#164304,#164305,#164306,#164307,#164308,#164309,
#164310,#164311,#164312,#164313,#164314,#164315,#164316,#164317,#164318,
#164319,#164320,#164321,#164322,#164323,#164324,#164325,#164326,#164327,
#164328,#164329,#164330,#164331,#164332,#164333,#164334,#164335,#164336,
#164337,#164338,#164339,#164340,#164341,#164342,#164343,#164344,#164345,
#164346,#164347,#164348,#164349,#164350,#164351,#164352,#164353,#164354,
#164355,#164356,#164357,#164358,#164359,#164360,#164361,#164362,#164363,
#164364,#164365,#164366,#164367,#164368,#164369,#164370,#164371,#164372,
#164373,#164374,#164375,#164376,#164377,#164378,#164379,#164380,#164381,
#164382,#164383,#164384,#164385,#164386,#164387,#164388,#164389,#164390,
#164391,#164392,#164393,#164394,#164395,#164396,#164397,#164398,#164399,
#164400,#164401,#164402,#164403,#164404,#164405,#164406,#164407,#164408,
#164409,#164410,#164411,#164412,#164413,#164414,#164415,#164416,#164417,
#164418,#164419,#164420,#164421,#164422,#164423,#164424,#164425,#164426,
#164427,#164428,#164429,#164430,#164431,#164432,#164433,#164434,#164435,
#164436,#164437,#164438,#164439,#164440,#164441,#164442,#164443,#164444,
#164445,#164446,#164447,#164448,#164449,#164450,#164451,#164452,#164453,
#164454,#164455,#164456,#164457,#164458,#164459,#164460,#164461,#164462,
#164463,#164464,#164465,#164466,#164467,#164468,#164469,#164470,#164471,
#164472,#164473,#164474,#164475,#164476,#164477,#164478,#164479,#164480,
#164481,#164482,#164483,#164484,#164485,#164486,#164487,#164488,#164489,
#164490,#164491,#164492,#164493,#164494,#164495,#164496,#164497,#164498,
#164499,#164500,#164501,#164502,#164503,#164504,#164505,#164506,#164507,
#164508,#164509,#164510,#164511,#164512,#164513,#164514,#164515,#164516,
#164517,#164518,#164519,#164520,#164521,#164522,#164523,#164524,#164525,
#164526,#164527,#164528,#164529,#164530,#164531,#164532,#164533,#164534,
#164535,#164536,#164537,#164538,#164539,#164540,#164541,#164542,#164543,
#164544,#164545,#164546,#164547,#164548,#164549,#164550,#164551,#164552,
#164553,#164554,#164555,#164556,#164557,#164558,#164559,#164560,#164561,
#164562,#164563,#164564,#164565,#164566,#164567,#164568,#164569,#164570,
#164571,#164572,#164573,#164574,#164575,#164576,#164577,#164578,#164579,
#164580,#164581,#164582,#164583,#164584,#164585,#164586,#164587,#164588,
#164589,#164590,#164591,#164592,#164593,#164594,#164595,#164596,#164597,
#164598,#164599,#164600,#164601,#164602,#164603,#164604,#164605,#164606,
#164607,#164608,#164609,#164610,#164611,#164612,#164613,#164614,#164615,
#164616,#164617,#164618,#164619,#164620,#164621,#164622,#164623,#164624,
#164625,#164626,#164627,#164628,#164629,#164630,#164631,#164632,#164633,
#164634,#164635,#164636,#164637,#164638,#164639,#164640,#164641,#164642,
#164643,#164644,#164645,#164646,#164647,#164648,#164649,#164650,#164651,
#164652,#164653,#164654,#164655,#164656,#164657,#164658,#164659,#164660,
#164661,#164662,#164663,#164664,#164665,#164666,#164667,#164668,#164669,
#164670,#164671,#164672,#164673,#164674,#164675,#164676,#164677,#164678,
#164679,#164680,#164681,#164682,#164683,#164684,#164685,#164686,#164687,
#164688,#164689,#164690,#164691,#164692,#164693,#164694,#164695,#164696,
#164697,#164698,#164699,#164700,#164701,#164702,#164703,#164704,#164705,
#164706,#164707,#164708,#164709,#164710,#164711,#164712,#164713,#164714,
#164715,#164716,#164717,#164718,#164719,#164720,#164721,#164722,#164723,
#164724,#164725,#164726,#164727,#164728,#164729,#164730,#164731,#164732,
#164733,#164734,#164735,#164736,#164737,#164738,#164739,#164740,#164741,
#164742,#164743,#164744,#164745,#164746,#164747,#164748,#164749,#164750,
#164751,#164752,#164753,#164754,#164755,#164756,#164757,#164758,#164759,
#164760,#164761,#164762,#164763,#164764,#164765,#164766,#164767,#164768,
#164769,#164770,#164771,#164772,#164773,#164774,#164775,#164776,#164777,
#164778,#164779,#164780,#164781,#164782,#164783,#164784,#164785,#164786,
#164787,#164788,#164789,#164790,#164791,#164792,#164793,#164794,#164795,
#164796,#164797,#164798,#164799,#164800,#164801,#164802,#164803,#164804,
#164805,#164806,#164807,#164808,#164809,#164810,#164811,#164812,#164813,
#164814,#164815,#164816,#164817,#164818,#164819,#164820,#164821,#164822,
#164823,#164824,#164825,#164826,#164827,#164828,#164829,#164830,#164831,
#164832,#164833,#164834,#164835,#164836,#164837,#164838,#164839,#164840,
#164841,#164842,#164843,#164844,#164845,#164846,#164847,#164848,#164849,
#164850,#164851,#164852,#164853,#164854,#164855,#164856,#164857,#164858,
#164859,#164860,#164861,#164862,#164863,#164864,#164865,#164866,#164867,
#164868,#164869,#164870,#164871,#164872,#164873,#164874,#164875,#164876,
#164877,#164878,#164879,#164880,#164881,#164882,#164883,#164884,#164885,
#164886,#164887,#164888,#164889,#164890,#164891,#164892,#164893,#164894,
#164895,#164896,#164897,#164898,#164899,#164900,#164901,#164902,#164903,
#164904,#164905,#164906,#164907,#164908,#164909,#164910,#164911,#164912,
#164913,#164914,#164915,#164916,#164917,#164918,#164919,#164920,#164921,
#164922,#164923,#164924,#164925,#164926,#164927,#164928,#164929,#164930,
#164931,#164932,#164933,#164934,#164935,#164936,#164937,#164938,#164939,
#164940,#164941,#164942,#164943,#164944,#164945,#164946,#164947,#164948,
#164949,#164950,#164951,#164952,#164953,#164954,#164955,#164956,#164957,
#164958,#164959,#164960,#164961,#164962,#164963,#164964,#164965,#164966,
#164967,#164968,#164969,#164970,#164971,#164972,#164973,#164974,#164975,
#164976,#164977,#164978,#164979,#164980,#164981,#164982,#164983,#164984,
#164985,#164986,#164987,#164988,#164989,#164990,#164991,#164992,#164993,
#164994,#164995,#164996,#164997,#164998,#164999,#165000,#165001,#165002,
#165003,#165004,#165005,#165006,#165007,#165008,#165009,#165010,#165011,
#165012,#165013,#165014,#165015,#165016,#165017,#165018,#165019,#165020,
#165021,#165022,#165023,#165024,#165025,#165026,#165027,#165028,#165029,
#165030,#165031,#165032,#165033,#165034,#165035,#165036,#165037,#165038,
#165039,#165040,#165041,#165042,#165043,#165044,#165045,#165046,#165047,
#165048,#165049,#165050,#165051,#165052,#165053,#165054,#165055,#165056,
#165057,#165058,#165059,#165060,#165061,#165062,#165063,#165064,#165065,
#165066,#165067,#165068,#165069,#165070,#165071,#165072,#165073,#165074,
#165075,#165076,#165077,#165078,#165079,#165080,#165081,#165082,#165083,
#165084,#165085,#165086,#165087,#165088,#165089,#165090,#165091,#165092,
#165093,#165094,#165095,#165096,#165097,#165098,#165099,#165100,#165101,
#165102,#165103,#165104,#165105,#165106,#165107,#165108,#165109,#165110,
#165111,#165112,#165113,#165114,#165115,#165116,#165117,#165118,#165119,
#165120,#165121),(#165122,#165123,#165124,#165125,#165126,#165127,#165128,
#165129,#165130,#165131,#165132,#165133,#165134,#165135,#165136,#165137,
#165138,#165139,#165140,#165141,#165142,#165143,#165144,#165145,#165146,
#165147,#165148,#165149,#165150,#165151,#165152,#165153,#165154,#165155,
#165156,#165157,#165158,#165159,#165160,#165161,#165162,#165163,#165164,
#165165,#165166,#165167,#165168,#165169,#165170,#165171,#165172,#165173,
#165174,#165175,#165176,#165177,#165178,#165179,#165180,#165181,#165182,
#165183,#165184,#165185,#165186,#165187,#165188,#165189,#165190,#165191,
#165192,#165193,#165194,#165195,#165196,#165197,#165198,#165199,#165200,
#165201,#165202,#165203,#165204,#165205,#165206,#165207,#165208,#165209,
#165210,#165211,#165212,#165213,#165214,#165215,#165216,#165217,#165218,
#165219,#165220,#165221,#165222,#165223,#165224,#165225,#165226,#165227,
#165228,#165229,#165230,#165231,#165232,#165233,#165234,#165235,#165236,
#165237,#165238,#165239,#165240,#165241,#165242,#165243,#165244,#165245,
#165246,#165247,#165248,#165249,#165250,#165251,#165252,#165253,#165254,
#165255,#165256,#165257,#165258,#165259,#165260,#165261,#165262,#165263,
#165264,#165265,#165266,#165267,#165268,#165269,#165270,#165271,#165272,
#165273,#165274,#165275,#165276,#165277,#165278,#165279,#165280,#165281,
#165282,#165283,#165284,#165285,#165286,#165287,#165288,#165289,#165290,
#165291,#165292,#165293,#165294,#165295,#165296,#165297,#165298,#165299,
#165300,#165301,#165302,#165303,#165304,#165305,#165306,#165307,#165308,
#165309,#165310,#165311,#165312,#165313,#165314,#165315,#165316,#165317,
#165318,#165319,#165320,#165321,#165322,#165323,#165324,#165325,#165326,
#165327,#165328,#165329,#165330,#165331,#165332,#165333,#165334,#165335,
#165336,#165337,#165338,#165339,#165340,#165341,#165342,#165343,#165344,
#165345,#165346,#165347,#165348,#165349,#165350,#165351,#165352,#165353,
#165354,#165355,#165356,#165357,#165358,#165359,#165360,#165361,#165362,
#165363,#165364,#165365,#165366,#165367,#165368,#165369,#165370,#165371,
#165372,#165373,#165374,#165375,#165376,#165377,#165378,#165379,#165380,
#165381,#165382,#165383,#165384,#165385,#165386,#165387,#165388,#165389,
#165390,#165391,#165392,#165393,#165394,#165395,#165396,#165397,#165398,
#165399,#165400,#165401,#165402,#165403,#165404,#165405,#165406,#165407,
#165408,#165409,#165410,#165411,#165412,#165413,#165414,#165415,#165416,
#165417,#165418,#165419,#165420,#165421,#165422,#165423,#165424,#165425,
#165426,#165427,#165428,#165429,#165430,#165431,#165432,#165433,#165434,
#165435,#165436,#165437,#165438,#165439,#165440,#165441,#165442,#165443,
#165444,#165445,#165446,#165447,#165448,#165449,#165450,#165451,#165452,
#165453,#165454,#165455,#165456,#165457,#165458,#165459,#165460,#165461,
#165462,#165463,#165464,#165465,#165466,#165467,#165468,#165469,#165470,
#165471,#165472,#165473,#165474,#165475,#165476,#165477,#165478,#165479,
#165480,#165481,#165482,#165483,#165484,#165485,#165486,#165487,#165488,
#165489,#165490,#165491,#165492,#165493,#165494,#165495,#165496,#165497,
#165498,#165499,#165500,#165501,#165502,#165503,#165504,#165505,#165506,
#165507,#165508,#165509,#165510,#165511,#165512,#165513,#165514,#165515,
#165516,#165517,#165518,#165519,#165520,#165521,#165522,#165523,#165524,
#165525,#165526,#165527,#165528,#165529,#165530,#165531,#165532,#165533,
#165534,#165535,#165536,#165537,#165538,#165539,#165540,#165541,#165542,
#165543,#165544,#165545,#165546,#165547,#165548,#165549,#165550,#165551,
#165552,#165553,#165554,#165555,#165556,#165557,#165558,#165559,#165560,
#165561,#165562,#165563,#165564,#165565,#165566,#165567,#165568,#165569,
#165570,#165571,#165572,#165573,#165574,#165575,#165576,#165577,#165578,
#165579,#165580,#165581,#165582,#165583,#165584,#165585,#165586,#165587,
#165588,#165589,#165590,#165591,#165592,#165593,#165594,#165595,#165596,
#165597,#165598,#165599,#165600,#165601,#165602,#165603,#165604,#165605,
#165606,#165607,#165608,#165609,#165610,#165611,#165612,#165613,#165614,
#165615,#165616,#165617,#165618,#165619,#165620,#165621,#165622,#165623,
#165624,#165625,#165626,#165627,#165628,#165629,#165630,#165631,#165632,
#165633,#165634,#165635,#165636,#165637,#165638,#165639,#165640,#165641,
#165642,#165643,#165644,#165645,#165646,#165647,#165648,#165649,#165650,
#165651,#165652,#165653,#165654,#165655,#165656,#165657,#165658,#165659,
#165660,#165661,#165662,#165663,#165664,#165665,#165666,#165667,#165668,
#165669,#165670,#165671,#165672,#165673,#165674,#165675,#165676,#165677,
#165678,#165679,#165680,#165681,#165682,#165683,#165684,#165685,#165686,
#165687,#165688,#165689,#165690,#165691,#165692,#165693,#165694,#165695,
#165696,#165697,#165698,#165699,#165700,#165701,#165702,#165703,#165704,
#165705,#165706,#165707,#165708,#165709,#165710,#165711,#165712,#165713,
#165714,#165715,#165716,#165717,#165718,#165719,#165720,#165721,#165722,
#165723,#165724,#165725,#165726,#165727,#165728,#165729,#165730,#165731,
#165732,#165733,#165734,#165735,#165736,#165737,#165738,#165739,#165740,
#165741,#165742,#165743,#165744,#165745,#165746,#165747,#165748,#165749,
#165750,#165751,#165752,#165753,#165754,#165755,#165756,#165757,#165758,
#165759,#165760,#165761,#165762,#165763,#165764,#165765,#165766,#165767,
#165768,#165769,#165770,#165771,#165772,#165773,#165774,#165775,#165776,
#165777,#165778,#165779,#165780,#165781,#165782,#165783,#165784,#165785,
#165786,#165787,#165788,#165789,#165790,#165791,#165792,#165793,#165794,
#165795,#165796,#165797,#165798,#165799,#165800,#165801,#165802,#165803,
#165804,#165805,#165806,#165807,#165808,#165809,#165810,#165811,#165812,
#165813,#165814,#165815,#165816,#165817,#165818,#165819,#165820,#165821,
#165822,#165823,#165824,#165825,#165826,#165827,#165828,#165829,#165830,
#165831,#165832,#165833,#165834,#165835,#165836,#165837,#165838,#165839,
#165840,#165841,#165842,#165843,#165844,#165845,#165846,#165847,#165848,
#165849,#165850,#165851,#165852,#165853,#165854,#165855,#165856,#165857,
#165858,#165859,#165860,#165861,#165862,#165863,#165864,#165865,#165866,
#165867,#165868,#165869,#165870,#165871,#165872,#165873,#165874,#165875,
#165876,#165877,#165878,#165879,#165880,#165881,#165882,#165883,#165884,
#165885,#165886,#165887,#165888,#165889,#165890,#165891,#165892,#165893,
#165894,#165895,#165896,#165897,#165898,#165899,#165900,#165901,#165902,
#165903,#165904,#165905,#165906,#165907,#165908,#165909,#165910,#165911,
#165912,#165913,#165914,#165915,#165916,#165917,#165918,#165919,#165920,
#165921,#165922,#165923,#165924,#165925,#165926,#165927,#165928,#165929,
#165930,#165931,#165932,#165933,#165934,#165935,#165936,#165937,#165938,
#165939,#165940,#165941,#165942,#165943,#165944,#165945,#165946,#165947,
#165948,#165949,#165950,#165951,#165952,#165953,#165954,#165955,#165956,
#165957,#165958,#165959,#165960,#165961,#165962,#165963,#165964,#165965,
#165966,#165967,#165968,#165969,#165970,#165971,#165972,#165973,#165974,
#165975,#165976,#165977,#165978,#165979,#165980,#165981,#165982,#165983,
#165984,#165985,#165986,#165987,#165988,#165989,#165990,#165991,#165992,
#165993,#165994,#165995,#165996,#165997,#165998,#165999,#166000,#166001,
#166002,#166003,#166004,#166005,#166006,#166007,#166008,#166009,#166010,
#166011,#166012,#166013,#166014,#166015,#166016,#166017,#166018,#166019,
#166020,#166021,#166022,#166023,#166024,#166025,#166026,#166027,#166028,
#166029,#166030,#166031,#166032,#166033,#166034,#166035,#166036,#166037,
#166038,#166039,#166040,#166041,#166042,#166043,#166044,#166045,#166046,
#166047,#166048,#166049,#166050,#166051,#166052,#166053,#166054,#166055,
#166056,#166057,#166058,#166059,#166060,#166061,#166062,#166063,#166064,
#166065,#166066,#166067,#166068,#166069,#166070,#166071,#166072,#166073,
#166074,#166075,#166076,#166077,#166078,#166079,#166080,#166081,#166082,
#166083,#166084,#166085,#166086,#166087,#166088,#166089,#166090,#166091,
#166092,#166093,#166094,#166095,#166096,#166097,#166098,#166099,#166100,
#166101,#166102,#166103,#166104,#166105,#166106,#166107,#166108,#166109,
#166110,#166111,#166112,#166113,#166114,#166115,#166116,#166117,#166118,
#166119,#166120,#166121,#166122,#166123,#166124,#166125,#166126,#166127,
#166128,#166129,#166130,#166131,#166132,#166133,#166134,#166135,#166136,
#166137,#166138,#166139,#166140,#166141,#166142,#166143,#166144,#166145,
#166146,#166147,#166148,#166149,#166150,#166151,#166152,#166153,#166154,
#166155,#166156,#166157,#166158,#166159,#166160,#166161,#166162,#166163,
#166164,#166165,#166166,#166167,#166168,#166169,#166170,#166171,#166172,
#166173,#166174,#166175,#166176,#166177,#166178,#166179,#166180,#166181,
#166182,#166183,#166184,#166185,#166186,#166187,#166188,#166189,#166190,
#166191,#166192,#166193,#166194,#166195,#166196,#166197,#166198,#166199,
#166200,#166201,#166202,#166203,#166204,#166205,#166206,#166207,#166208,
#166209,#166210,#166211,#166212,#166213,#166214,#166215,#166216,#166217,
#166218,#166219,#166220,#166221,#166222,#166223,#166224,#166225,#166226,
#166227,#166228,#166229,#166230,#166231,#166232,#166233,#166234,#166235,
#166236,#166237,#166238,#166239,#166240,#166241,#166242,#166243,#166244,
#166245,#166246,#166247,#166248,#166249,#166250,#166251,#166252,#166253,
#166254,#166255,#166256,#166257,#166258,#166259,#166260,#166261,#166262,
#166263,#166264,#166265,#166266,#166267,#166268,#166269,#166270,#166271,
#166272,#166273,#166274,#166275,#166276,#166277,#166278,#166279,#166280,
#166281,#166282,#166283,#166284,#166285,#166286,#166287,#166288,#166289,
#166290,#166291,#166292,#166293,#166294,#166295,#166296,#166297,#166298,
#166299,#166300,#166301,#166302,#166303,#166304,#166305,#166306,#166307,
#166308,#166309,#166310,#166311,#166312,#166313,#166314,#166315,#166316,
#166317,#166318,#166319,#166320,#166321,#166322,#166323,#166324,#166325,
#166326,#166327,#166328,#166329,#166330,#166331,#166332,#166333,#166334,
#166335,#166336,#166337,#166338,#166339,#166340,#166341,#166342,#166343,
#166344,#166345,#166346,#166347,#166348,#166349,#166350,#166351,#166352,
#166353,#166354,#166355,#166356,#166357,#166358,#166359,#166360,#166361,
#166362,#166363,#166364,#166365,#166366,#166367,#166368,#166369,#166370,
#166371,#166372,#166373,#166374,#166375,#166376,#166377,#166378,#166379,
#166380,#166381,#166382,#166383,#166384,#166385,#166386,#166387,#166388,
#166389,#166390,#166391,#166392,#166393,#166394,#166395,#166396,#166397,
#166398,#166399,#166400,#166401,#166402,#166403,#166404,#166405,#166406,
#166407,#166408,#166409,#166410,#166411,#166412,#166413,#166414,#166415,
#166416,#166417,#166418,#166419,#166420,#166421,#166422,#166423,#166424,
#166425,#166426,#166427,#166428,#166429,#166430,#166431,#166432,#166433,
#166434,#166435,#166436,#166437,#166438,#166439,#166440,#166441,#166442,
#166443,#166444,#166445,#166446,#166447,#166448,#166449,#166450,#166451,
#166452,#166453,#166454,#166455,#166456,#166457,#166458,#166459,#166460,
#166461,#166462,#166463,#166464,#166465,#166466,#166467,#166468,#166469,
#166470,#166471,#166472,#166473,#166474,#166475,#166476,#166477,#166478,
#166479,#166480,#166481,#166482,#166483,#166484,#166485,#166486,#166487,
#166488,#166489,#166490,#166491,#166492,#166493,#166494,#166495,#166496,
#166497,#166498,#166499,#166500,#166501,#166502,#166503,#166504,#166505,
#166506,#166507,#166508,#166509,#166510,#166511,#166512,#166513,#166514,
#166515,#166516,#166517,#166518,#166519,#166520,#166521,#166522,#166523,
#166524,#166525,#166526,#166527,#166528,#166529,#166530,#166531,#166532,
#166533,#166534,#166535,#166536,#166537,#166538,#166539,#166540,#166541,
#166542,#166543,#166544,#166545,#166546,#166547,#166548,#166549,#166550,
#166551,#166552,#166553,#166554,#166555,#166556,#166557,#166558,#166559,
#166560,#166561,#166562,#166563,#166564,#166565,#166566,#166567,#166568,
#166569,#166570,#166571,#166572,#166573,#166574,#166575,#166576,#166577,
#166578,#166579,#166580,#166581,#166582,#166583,#166584,#166585,#166586,
#166587,#166588,#166589,#166590,#166591,#166592,#166593,#166594,#166595,
#166596,#166597,#166598,#166599,#166600,#166601,#166602,#166603,#166604,
#166605,#166606,#166607,#166608,#166609,#166610,#166611,#166612,#166613,
#166614,#166615,#166616,#166617,#166618,#166619,#166620,#166621,#166622,
#166623,#166624,#166625,#166626,#166627,#166628,#166629,#166630,#166631,
#166632,#166633,#166634,#166635,#166636,#166637,#166638,#166639,#166640,
#166641,#166642,#166643,#166644,#166645,#166646,#166647,#166648,#166649,
#166650,#166651,#166652,#166653,#166654,#166655,#166656,#166657,#166658,
#166659,#166660,#166661,#166662,#166663,#166664,#166665,#166666,#166667,
#166668,#166669,#166670,#166671,#166672,#166673,#166674,#166675,#166676,
#166677,#166678,#166679,#166680,#166681,#166682,#166683,#166684,#166685,
#166686,#166687,#166688,#166689,#166690,#166691,#166692,#166693,#166694,
#166695,#166696,#166697,#166698,#166699,#166700,#166701,#166702,#166703,
#166704,#166705,#166706,#166707,#166708,#166709,#166710,#166711,#166712,
#166713,#166714,#166715,#166716,#166717,#166718,#166719,#166720,#166721,
#166722,#166723,#166724,#166725,#166726,#166727,#166728,#166729,#166730,
#166731,#166732,#166733,#166734,#166735,#166736,#166737,#166738,#166739,
#166740,#166741,#166742,#166743,#166744,#166745,#166746,#166747,#166748,
#166749,#166750,#166751,#166752,#166753,#166754,#166755,#166756,#166757,
#166758,#166759,#166760,#166761,#166762,#166763,#166764,#166765,#166766,
#166767,#166768,#166769,#166770,#166771,#166772,#166773,#166774,#166775,
#166776,#166777,#166778,#166779,#166780,#166781,#166782,#166783,#166784,
#166785,#166786,#166787,#166788,#166789,#166790,#166791,#166792,#166793,
#166794,#166795,#166796,#166797,#166798,#166799,#166800,#166801,#166802,
#166803,#166804,#166805,#166806,#166807,#166808,#166809,#166810,#166811,
#166812,#166813,#166814,#166815,#166816,#166817,#166818,#166819,#166820,
#166821,#166822,#166823,#166824,#166825,#166826,#166827,#166828,#166829,
#166830,#166831,#166832,#166833,#166834,#166835,#166836,#166837,#166838,
#166839,#166840,#166841,#166842,#166843,#166844,#166845,#166846,#166847,
#166848,#166849,#166850,#166851,#166852,#166853,#166854,#166855,#166856,
#166857,#166858,#166859,#166860,#166861,#166862,#166863,#166864,#166865,
#166866,#166867,#166868,#166869,#166870,#166871,#166872,#166873,#166874,
#166875,#166876,#166877,#166878,#166879,#166880,#166881,#166882,#166883,
#166884,#166885,#166886,#166887,#166888,#166889,#166890,#166891,#166892,
#166893,#166894,#166895,#166896,#166897,#166898,#166899,#166900,#166901,
#166902,#166903,#166904,#166905,#166906,#166907,#166908,#166909,#166910,
#166911,#166912,#166913,#166914,#166915,#166916,#166917,#166918,#166919,
#166920,#166921,#166922,#166923,#166924,#166925,#166926,#166927,#166928,
#166929,#166930,#166931,#166932,#166933,#166934,#166935,#166936,#166937,
#166938,#166939,#166940,#166941,#166942,#166943,#166944,#166945,#166946,
#166947,#166948,#166949,#166950,#166951,#166952,#166953,#166954,#166955,
#166956,#166957,#166958,#166959,#166960,#166961,#166962,#166963,#166964,
#166965,#166966,#166967,#166968,#166969,#166970,#166971,#166972,#166973,
#166974,#166975,#166976,#166977,#166978,#166979,#166980,#166981,#166982,
#166983,#166984,#166985,#166986,#166987,#166988,#166989,#166990,#166991,
#166992,#166993,#166994,#166995,#166996,#166997,#166998,#166999,#167000,
#167001,#167002,#167003,#167004,#167005,#167006,#167007,#167008,#167009,
#167010,#167011,#167012,#167013,#167014,#167015,#167016,#167017,#167018,
#167019,#167020,#167021,#167022,#167023,#167024,#167025,#167026,#167027,
#167028,#167029,#167030,#167031,#167032,#167033,#167034,#167035,#167036,
#167037,#167038,#167039,#167040,#167041,#167042,#167043,#167044,#167045,
#167046,#167047,#167048,#167049,#167050,#167051,#167052,#167053,#167054,
#167055,#167056,#167057,#167058,#167059,#167060,#167061,#167062,#167063,
#167064,#167065,#167066,#167067,#167068,#167069,#167070,#167071,#167072,
#167073,#167074,#167075,#167076,#167077,#167078,#167079,#167080,#167081,
#167082,#167083,#167084,#167085,#167086,#167087,#167088,#167089,#167090,
#167091,#167092,#167093,#167094,#167095,#167096,#167097,#167098,#167099,
#167100,#167101,#167102,#167103,#167104,#167105,#167106,#167107,#167108,
#167109,#167110,#167111,#167112,#167113,#167114,#167115,#167116,#167117,
#167118,#167119,#167120,#167121,#167122,#167123,#167124,#167125,#167126,
#167127,#167128,#167129,#167130,#167131,#167132,#167133,#167134,#167135,
#167136)),.UNSPECIFIED.,.F.,.F.,.F.)
B_SPLINE_SURFACE_WITH_KNOTS((2,2),(3,2,2,2,2,2,2,2,2,2,2,2,2,2,2,2,2,2,
2,2,2,2,2,2,2,2,2,2,2,2,2,2,2,2,2,2,2,2,2,2,2,2,2,2,2,2,2,2,2,2,2,2,2,2,
2,2,2,2,2,2,2,2,2,2,2,2,2,2,2,2,2,2,2,2,2,2,2,2,2,2,2,2,2,2,2,2,2,2,2,2,
2,2,2,2,2,2,2,2,2,2,2,2,2,2,2,2,2,2,2,2,2,2,2,2,2,2,2,2,2,2,2,2,2,2,2,2,
2,2,2,2,2,2,2,2,2,2,2,2,2,2,2,2,2,2,2,2,2,2,2,2,2,2,2,2,2,2,2,2,2,2,2,2,
2,2,2,2,2,2,2,2,2,2,2,2,2,2,2,2,2,2,2,2,2,2,2,2,2,2,2,2,2,2,2,2,2,2,2,2,
2,2,2,2,2,2,2,2,2,2,2,2,2,2,2,2,2,2,2,2,2,2,2,2,2,2,2,2,2,2,2,2,2,2,2,2,
2,2,2,2,2,2,2,2,2,2,2,2,2,2,2,2,2,2,2,2,2,2,2,2,2,2,2,2,2,2,2,2,2,2,2,2,
2,2,2,2,2,2,2,2,2,2,2,2,2,2,2,2,2,2,2,2,2,2,2,2,2,2,2,2,2,2,2,2,2,2,2,2,
2,2,2,2,2,2,2,2,2,2,2,2,2,2,2,2,2,2,2,2,2,2,2,2,2,2,2,2,2,2,2,2,2,2,2,2,
2,2,2,2,2,2,2,2,2,2,2,2,2,2,2,2,2,2,2,2,2,2,2,2,2,2,2,2,2,2,2,2,2,2,2,2,
2,2,2,2,2,2,2,2,2,2,2,2,2,2,2,2,2,2,2,2,2,2,2,2,2,2,2,2,2,2,2,2,2,2,2,2,
2,2,2,2,2,2,2,2,2,2,2,2,2,2,2,2,2,2,2,2,2,2,2,2,2,2,2,2,2,2,2,2,2,2,2,2,
2,2,2,2,2,2,2,2,2,2,2,2,2,2,2,2,2,2,2,2,2,2,2,2,2,2,2,2,2,2,2,2,2,2,2,2,
2,2,2,2,2,2,2,2,2,2,2,2,2,2,2,2,2,2,2,2,2,2,2,2,2,2,2,2,2,2,2,2,2,2,2,2,
2,2,2,2,2,2,2,2,2,2,2,2,2,2,2,2,2,2,2,2,2,2,2,2,2,2,2,2,2,2,2,2,2,2,2,2,
2,2,2,2,2,2,2,2,2,2,2,2,2,2,2,2,2,2,2,2,2,2,2,2,2,2,2,2,2,2,2,2,2,2,2,2,
2,2,2,2,2,2,2,2,2,2,2,2,2,2,2,2,2,2,2,2,2,2,2,2,2,2,2,2,2,2,2,2,2,2,2,2,
2,2,2,2,2,2,2,2,2,2,2,2,2,2,2,2,2,2,2,2,2,2,2,2,2,2,2,2,2,2,2,2,2,2,2,2,
2,2,2,2,2,2,2,2,2,2,2,2,2,2,2,2,2,2,2,2,2,2,2,2,2,2,2,2,2,2,2,2,2,2,2,2,
2,2,2,2,2,2,2,2,2,2,2,2,2,2,2,2,2,2,2,2,2,2,2,2,2,2,2,2,2,2,2,2,2,2,2,2,
2,2,2,2,2,2,2,2,2,2,2,2,2,2,2,2,2,2,2,2,2,2,2,2,2,2,2,2,2,2,2,2,2,2,2,2,
2,2,2,2,2,2,2,2,2,2,2,2,2,2,2,2,2,2,2,2,2,2,2,2,2,2,2,2,2,2,2,2,2,2,2,2,
2,2,2,2,2,2,2,2,2,2,2,2,2,2,2,2,2,2,2,2,2,2,2,2,2,2,2,2,2,2,2,2,2,2,2,2,
2,2,2,2,2,2,2,2,2,2,2,2,2,2,2,2,2,2,2,2,2,2,2,2,2,2,2,2,2,2,2,2,2,2,2,2,
2,2,2,2,2,2,2,2,2,2,2,2,2,2,2,2,2,2,2,2,2,2,2,2,2,2,2,2,2,2,2,2,2,2,2,2,
2,2,2,2,2,2,2,2,2,2,2,2,2,2,2,2,2,2,2,2,2,2,2,2,2,2,2,2,2,2,2,2,2,2,2,2,
2,2,2,2,2,2,2,2,2,2,2,2,2,2,2,2,2,2,2,2,2,2,2,2,2,2,2,2,2,2,2,2,2,2,2,2,
2,2,2,2,2,2,2,2,2,2,2,2,2,2,2,2,2,3),(0.,1.),(0.,0.000980392156862745,0.00196078431372549,
0.00294117647058824,0.00392156862745098,0.00490196078431373,0.00588235294117647,
0.00686274509803922,0.00784313725490196,0.00882352941176471,0.00980392156862745,
0.0107843137254902,0.0117647058823529,0.0127450980392157,0.0137254901960784,
0.0147058823529412,0.0156862745098039,0.0166666666666667,0.0176470588235294,
0.0186274509803922,0.0196078431372549,0.0205882352941176,0.0215686274509804,
0.0225490196078431,0.0235294117647059,0.0245098039215686,0.0254901960784314,
0.0264705882352941,0.0274509803921569,0.0284313725490196,0.0294117647058824,
0.0303921568627451,0.0313725490196078,0.0323529411764706,0.0333333333333333,
0.0343137254901961,0.0352941176470588,0.0362745098039216,0.0372549019607843,
0.0382352941176471,0.0392156862745098,0.0401960784313726,0.0411764705882353,
0.042156862745098,0.0431372549019608,0.0441176470588235,0.0450980392156863,
0.046078431372549,0.0470588235294118,0.0480392156862745,0.0490196078431373,
0.05,0.0509803921568627,0.0519607843137255,0.0529411764705882,0.053921568627451,
0.0549019607843137,0.0558823529411765,0.0568627450980392,0.057843137254902,
0.0588235294117647,0.0598039215686275,0.0607843137254902,0.0617647058823529,
0.0627450980392157,0.0637254901960784,0.0647058823529412,0.0656862745098039,
0.0666666666666667,0.0676470588235294,0.0686274509803922,0.0696078431372549,
0.0705882352941176,0.0715686274509804,0.0725490196078431,0.0735294117647059,
0.0745098039215686,0.0754901960784314,0.0764705882352941,0.0774509803921569,
0.0784313725490196,0.0794117647058823,0.0803921568627451,0.0813725490196078,
0.0823529411764706,0.0833333333333333,0.0843137254901961,0.0852941176470588,
0.0862745098039216,0.0872549019607843,0.0882352941176471,0.0892156862745098,
0.0901960784313725,0.0911764705882353,0.092156862745098,0.0931372549019608,
0.0941176470588235,0.0950980392156863,0.096078431372549,0.0970588235294118,
0.0980392156862745,0.0990196078431373,0.1,0.100980392156863,0.101960784313725,
0.102941176470588,0.103921568627451,0.104901960784314,0.105882352941176,
0.106862745098039,0.107843137254902,0.108823529411765,0.109803921568627,
0.11078431372549,0.111764705882353,0.112745098039216,0.113725490196078,
0.114705882352941,0.115686274509804,0.116666666666667,0.117647058823529,
0.118627450980392,0.119607843137255,0.120588235294118,0.12156862745098,
0.122549019607843,0.123529411764706,0.124509803921569,0.125490196078431,
0.126470588235294,0.127450980392157,0.12843137254902,0.129411764705882,
0.130392156862745,0.131372549019608,0.132352941176471,0.133333333333333,
0.134313725490196,0.135294117647059,0.136274509803922,0.137254901960784,
0.138235294117647,0.13921568627451,0.140196078431373,0.141176470588235,
0.142156862745098,0.143137254901961,0.144117647058824,0.145098039215686,
0.146078431372549,0.147058823529412,0.148039215686275,0.149019607843137,
0.15,0.150980392156863,0.151960784313725,0.152941176470588,0.153921568627451,
0.154901960784314,0.155882352941176,0.156862745098039,0.157843137254902,
0.158823529411765,0.159803921568627,0.16078431372549,0.161764705882353,
0.162745098039216,0.163725490196078,0.164705882352941,0.165686274509804,
0.166666666666667,0.167647058823529,0.168627450980392,0.169607843137255,
0.170588235294118,0.17156862745098,0.172549019607843,0.173529411764706,
0.174509803921569,0.175490196078431,0.176470588235294,0.177450980392157,
0.17843137254902,0.179411764705882,0.180392156862745,0.181372549019608,
0.182352941176471,0.183333333333333,0.184313725490196,0.185294117647059,
0.186274509803922,0.187254901960784,0.188235294117647,0.18921568627451,
0.190196078431373,0.191176470588235,0.192156862745098,0.193137254901961,
0.194117647058824,0.195098039215686,0.196078431372549,0.197058823529412,
0.198039215686275,0.199019607843137,0.2,0.200980392156863,0.201960784313725,
0.202941176470588,0.203921568627451,0.204901960784314,0.205882352941176,
0.206862745098039,0.207843137254902,0.208823529411765,0.209803921568627,
0.21078431372549,0.211764705882353,0.212745098039216,0.213725490196078,
0.214705882352941,0.215686274509804,0.216666666666667,0.217647058823529,
0.218627450980392,0.219607843137255,0.220588235294118,0.22156862745098,
0.222549019607843,0.223529411764706,0.224509803921569,0.225490196078431,
0.226470588235294,0.227450980392157,0.22843137254902,0.229411764705882,
0.230392156862745,0.231372549019608,0.232352941176471,0.233333333333333,
0.234313725490196,0.235294117647059,0.236274509803922,0.237254901960784,
0.238235294117647,0.23921568627451,0.240196078431373,0.241176470588235,
0.242156862745098,0.243137254901961,0.244117647058824,0.245098039215686,
0.246078431372549,0.247058823529412,0.248039215686275,0.249019607843137,
0.25,0.250980392156863,0.251960784313725,0.252941176470588,0.253921568627451,
0.254901960784314,0.255882352941176,0.256862745098039,0.257843137254902,
0.258823529411765,0.259803921568627,0.26078431372549,0.261764705882353,
0.262745098039216,0.263725490196078,0.264705882352941,0.265686274509804,
0.266666666666667,0.267647058823529,0.268627450980392,0.269607843137255,
0.270588235294118,0.27156862745098,0.272549019607843,0.273529411764706,
0.274509803921569,0.275490196078431,0.276470588235294,0.277450980392157,
0.27843137254902,0.279411764705882,0.280392156862745,0.281372549019608,
0.282352941176471,0.283333333333333,0.284313725490196,0.285294117647059,
0.286274509803922,0.287254901960784,0.288235294117647,0.28921568627451,
0.290196078431373,0.291176470588235,0.292156862745098,0.293137254901961,
0.294117647058824,0.295098039215686,0.296078431372549,0.297058823529412,
0.298039215686275,0.299019607843137,0.3,0.300980392156863,0.301960784313725,
0.302941176470588,0.303921568627451,0.304901960784314,0.305882352941176,
0.306862745098039,0.307843137254902,0.308823529411765,0.309803921568627,
0.31078431372549,0.311764705882353,0.312745098039216,0.313725490196078,
0.314705882352941,0.315686274509804,0.316666666666667,0.317647058823529,
0.318627450980392,0.319607843137255,0.320588235294118,0.32156862745098,
0.322549019607843,0.323529411764706,0.324509803921569,0.325490196078431,
0.326470588235294,0.327450980392157,0.32843137254902,0.329411764705882,
0.330392156862745,0.331372549019608,0.332352941176471,0.333333333333333,
0.334313725490196,0.335294117647059,0.336274509803922,0.337254901960784,
0.338235294117647,0.33921568627451,0.340196078431373,0.341176470588235,
0.342156862745098,0.343137254901961,0.344117647058824,0.345098039215686,
0.346078431372549,0.347058823529412,0.348039215686274,0.349019607843137,
0.35,0.350980392156863,0.351960784313726,0.352941176470588,0.353921568627451,
0.354901960784314,0.355882352941176,0.356862745098039,0.357843137254902,
0.358823529411765,0.359803921568627,0.36078431372549,0.361764705882353,
0.362745098039216,0.363725490196078,0.364705882352941,0.365686274509804,
0.366666666666667,0.367647058823529,0.368627450980392,0.369607843137255,
0.370588235294118,0.37156862745098,0.372549019607843,0.373529411764706,
0.374509803921569,0.375490196078431,0.376470588235294,0.377450980392157,
0.37843137254902,0.379411764705882,0.380392156862745,0.381372549019608,
0.382352941176471,0.383333333333333,0.384313725490196,0.385294117647059,
0.386274509803922,0.387254901960784,0.388235294117647,0.38921568627451,
0.390196078431373,0.391176470588235,0.392156862745098,0.393137254901961,
0.394117647058824,0.395098039215686,0.396078431372549,0.397058823529412,
0.398039215686274,0.399019607843137,0.4,0.400980392156863,0.401960784313726,
0.402941176470588,0.403921568627451,0.404901960784314,0.405882352941176,
0.406862745098039,0.407843137254902,0.408823529411765,0.409803921568627,
0.41078431372549,0.411764705882353,0.412745098039216,0.413725490196078,
0.414705882352941,0.415686274509804,0.416666666666667,0.417647058823529,
0.418627450980392,0.419607843137255,0.420588235294118,0.42156862745098,
0.422549019607843,0.423529411764706,0.424509803921569,0.425490196078431,
0.426470588235294,0.427450980392157,0.42843137254902,0.429411764705882,
0.430392156862745,0.431372549019608,0.432352941176471,0.433333333333333,
0.434313725490196,0.435294117647059,0.436274509803922,0.437254901960784,
0.438235294117647,0.43921568627451,0.440196078431373,0.441176470588235,
0.442156862745098,0.443137254901961,0.444117647058824,0.445098039215686,
0.446078431372549,0.447058823529412,0.448039215686275,0.449019607843137,
0.45,0.450980392156863,0.451960784313725,0.452941176470588,0.453921568627451,
0.454901960784314,0.455882352941176,0.456862745098039,0.457843137254902,
0.458823529411765,0.459803921568627,0.46078431372549,0.461764705882353,
0.462745098039216,0.463725490196078,0.464705882352941,0.465686274509804,
0.466666666666667,0.467647058823529,0.468627450980392,0.469607843137255,
0.470588235294118,0.47156862745098,0.472549019607843,0.473529411764706,
0.474509803921569,0.475490196078431,0.476470588235294,0.477450980392157,
0.47843137254902,0.479411764705882,0.480392156862745,0.481372549019608,
0.482352941176471,0.483333333333333,0.484313725490196,0.485294117647059,
0.486274509803922,0.487254901960784,0.488235294117647,0.48921568627451,
0.490196078431373,0.491176470588235,0.492156862745098,0.493137254901961,
0.494117647058824,0.495098039215686,0.496078431372549,0.497058823529412,
0.498039215686275,0.499019607843137,0.5,0.500980392156863,0.501960784313725,
0.502941176470588,0.503921568627451,0.504901960784314,0.505882352941176,
0.506862745098039,0.507843137254902,0.508823529411765,0.509803921568627,
0.51078431372549,0.511764705882353,0.512745098039216,0.513725490196078,
0.514705882352941,0.515686274509804,0.516666666666667,0.517647058823529,
0.518627450980392,0.519607843137255,0.520588235294118,0.52156862745098,
0.522549019607843,0.523529411764706,0.524509803921569,0.525490196078431,
0.526470588235294,0.527450980392157,0.52843137254902,0.529411764705882,
0.530392156862745,0.531372549019608,0.532352941176471,0.533333333333333,
0.534313725490196,0.535294117647059,0.536274509803922,0.537254901960784,
0.538235294117647,0.53921568627451,0.540196078431373,0.541176470588235,
0.542156862745098,0.543137254901961,0.544117647058823,0.545098039215686,
0.546078431372549,0.547058823529412,0.548039215686275,0.549019607843137,
0.55,0.550980392156863,0.551960784313726,0.552941176470588,0.553921568627451,
0.554901960784314,0.555882352941176,0.556862745098039,0.557843137254902,
0.558823529411765,0.559803921568627,0.56078431372549,0.561764705882353,
0.562745098039216,0.563725490196078,0.564705882352941,0.565686274509804,
0.566666666666667,0.567647058823529,0.568627450980392,0.569607843137255,
0.570588235294118,0.57156862745098,0.572549019607843,0.573529411764706,
0.574509803921569,0.575490196078431,0.576470588235294,0.577450980392157,
0.57843137254902,0.579411764705882,0.580392156862745,0.581372549019608,
0.582352941176471,0.583333333333333,0.584313725490196,0.585294117647059,
0.586274509803922,0.587254901960784,0.588235294117647,0.58921568627451,
0.590196078431373,0.591176470588235,0.592156862745098,0.593137254901961,
0.594117647058824,0.595098039215686,0.596078431372549,0.597058823529412,
0.598039215686274,0.599019607843137,0.6,0.600980392156863,0.601960784313725,
0.602941176470588,0.603921568627451,0.604901960784314,0.605882352941176,
0.606862745098039,0.607843137254902,0.608823529411765,0.609803921568628,
0.61078431372549,0.611764705882353,0.612745098039216,0.613725490196078,
0.614705882352941,0.615686274509804,0.616666666666667,0.617647058823529,
0.618627450980392,0.619607843137255,0.620588235294118,0.62156862745098,
0.622549019607843,0.623529411764706,0.624509803921569,0.625490196078431,
0.626470588235294,0.627450980392157,0.62843137254902,0.629411764705882,
0.630392156862745,0.631372549019608,0.632352941176471,0.633333333333333,
0.634313725490196,0.635294117647059,0.636274509803922,0.637254901960784,
0.638235294117647,0.63921568627451,0.640196078431372,0.641176470588235,
0.642156862745098,0.643137254901961,0.644117647058824,0.645098039215686,
0.646078431372549,0.647058823529412,0.648039215686275,0.649019607843137,
0.65,0.650980392156863,0.651960784313726,0.652941176470588,0.653921568627451,
0.654901960784314,0.655882352941176,0.656862745098039,0.657843137254902,
0.658823529411765,0.659803921568627,0.66078431372549,0.661764705882353,
0.662745098039216,0.663725490196078,0.664705882352941,0.665686274509804,
0.666666666666667,0.667647058823529,0.668627450980392,0.669607843137255,
0.670588235294118,0.67156862745098,0.672549019607843,0.673529411764706,
0.674509803921569,0.675490196078431,0.676470588235294,0.677450980392157,
0.67843137254902,0.679411764705882,0.680392156862745,0.681372549019608,
0.682352941176471,0.683333333333333,0.684313725490196,0.685294117647059,
0.686274509803922,0.687254901960784,0.688235294117647,0.68921568627451,
0.690196078431373,0.691176470588235,0.692156862745098,0.693137254901961,
0.694117647058824,0.695098039215686,0.696078431372549,0.697058823529412,
0.698039215686274,0.699019607843137,0.7,0.700980392156863,0.701960784313725,
0.702941176470588,0.703921568627451,0.704901960784314,0.705882352941177,
0.706862745098039,0.707843137254902,0.708823529411765,0.709803921568627,
0.71078431372549,0.711764705882353,0.712745098039216,0.713725490196078,
0.714705882352941,0.715686274509804,0.716666666666667,0.717647058823529,
0.718627450980392,0.719607843137255,0.720588235294118,0.72156862745098,
0.722549019607843,0.723529411764706,0.724509803921569,0.725490196078431,
0.726470588235294,0.727450980392157,0.72843137254902,0.729411764705882,
0.730392156862745,0.731372549019608,0.732352941176471,0.733333333333333,
0.734313725490196,0.735294117647059,0.736274509803922,0.737254901960784,
0.738235294117647,0.73921568627451,0.740196078431373,0.741176470588235,
0.742156862745098,0.743137254901961,0.744117647058824,0.745098039215686,
0.746078431372549,0.747058823529412,0.748039215686275,0.749019607843137,
0.75,0.750980392156863,0.751960784313725,0.752941176470588,0.753921568627451,
0.754901960784314,0.755882352941176,0.756862745098039,0.757843137254902,
0.758823529411765,0.759803921568627,0.76078431372549,0.761764705882353,
0.762745098039216,0.763725490196078,0.764705882352941,0.765686274509804,
0.766666666666667,0.767647058823529,0.768627450980392,0.769607843137255,
0.770588235294118,0.77156862745098,0.772549019607843,0.773529411764706,
0.774509803921569,0.775490196078431,0.776470588235294,0.777450980392157,
0.77843137254902,0.779411764705882,0.780392156862745,0.781372549019608,
0.782352941176471,0.783333333333333,0.784313725490196,0.785294117647059,
0.786274509803922,0.787254901960784,0.788235294117647,0.78921568627451,
0.790196078431373,0.791176470588235,0.792156862745098,0.793137254901961,
0.794117647058823,0.795098039215686,0.796078431372549,0.797058823529412,
0.798039215686275,0.799019607843137,0.8,0.800980392156863,0.801960784313726,
0.802941176470588,0.803921568627451,0.804901960784314,0.805882352941176,
0.806862745098039,0.807843137254902,0.808823529411765,0.809803921568627,
0.81078431372549,0.811764705882353,0.812745098039216,0.813725490196078,
0.814705882352941,0.815686274509804,0.816666666666667,0.817647058823529,
0.818627450980392,0.819607843137255,0.820588235294118,0.82156862745098,
0.822549019607843,0.823529411764706,0.824509803921569,0.825490196078431,
0.826470588235294,0.827450980392157,0.82843137254902,0.829411764705882,
0.830392156862745,0.831372549019608,0.832352941176471,0.833333333333333,
0.834313725490196,0.835294117647059,0.836274509803922,0.837254901960784,
0.838235294117647,0.83921568627451,0.840196078431373,0.841176470588235,
0.842156862745098,0.843137254901961,0.844117647058824,0.845098039215686,
0.846078431372549,0.847058823529412,0.848039215686274,0.849019607843137,
0.85,0.850980392156863,0.851960784313725,0.852941176470588,0.853921568627451,
0.854901960784314,0.855882352941176,0.856862745098039,0.857843137254902,
0.858823529411765,0.859803921568628,0.86078431372549,0.861764705882353,
0.862745098039216,0.863725490196078,0.864705882352941,0.865686274509804,
0.866666666666667,0.867647058823529,0.868627450980392,0.869607843137255,
0.870588235294118,0.87156862745098,0.872549019607843,0.873529411764706,
0.874509803921569,0.875490196078431,0.876470588235294,0.877450980392157,
0.87843137254902,0.879411764705882,0.880392156862745,0.881372549019608,
0.882352941176471,0.883333333333333,0.884313725490196,0.885294117647059,
0.886274509803922,0.887254901960784,0.888235294117647,0.88921568627451,
0.890196078431372,0.891176470588235,0.892156862745098,0.893137254901961,
0.894117647058824,0.895098039215686,0.896078431372549,0.897058823529412,
0.898039215686275,0.899019607843137,0.9,0.900980392156863,0.901960784313726,
0.902941176470588,0.903921568627451,0.904901960784314,0.905882352941176,
0.906862745098039,0.907843137254902,0.908823529411765,0.909803921568627,
0.91078431372549,0.911764705882353,0.912745098039216,0.913725490196078,
0.914705882352941,0.915686274509804,0.916666666666667,0.917647058823529,
0.918627450980392,0.919607843137255,0.920588235294118,0.92156862745098,
0.922549019607843,0.923529411764706,0.924509803921569,0.925490196078431,
0.926470588235294,0.927450980392157,0.92843137254902,0.929411764705882,
0.930392156862745,0.931372549019608,0.932352941176471,0.933333333333333,
0.934313725490196,0.935294117647059,0.936274509803922,0.937254901960784,
0.938235294117647,0.93921568627451,0.940196078431373,0.941176470588235,
0.942156862745098,0.943137254901961,0.944117647058824,0.945098039215686,
0.946078431372549,0.947058823529412,0.948039215686274,0.949019607843137,
0.95,0.950980392156863,0.951960784313725,0.952941176470588,0.953921568627451,
0.954901960784314,0.955882352941177,0.956862745098039,0.957843137254902,
0.958823529411765,0.959803921568627,0.96078431372549,0.961764705882353,
0.962745098039216,0.963725490196078,0.964705882352941,0.965686274509804,
0.966666666666667,0.967647058823529,0.968627450980392,0.969607843137255,
0.970588235294118,0.97156862745098,0.972549019607843,0.973529411764706,
0.974509803921569,0.975490196078431,0.976470588235294,0.977450980392157,
0.97843137254902,0.979411764705882,0.980392156862745,0.981372549019608,
0.982352941176471,0.983333333333333,0.984313725490196,0.985294117647059,
0.985937314000278,0.995796687140281),.UNSPECIFIED.)
GEOMETRIC_REPRESENTATION_ITEM()
RATIONAL_B_SPLINE_SURFACE(((1.,0.995734176295034,1.,0.995734176295034,1.,
0.995734176295034,1.,0.995734176295034,1.,0.995734176295034,1.,0.995734176295034,
1.,0.995734176295034,1.,0.995734176295034,1.,0.995734176295034,1.,0.995734176295034,
1.,0.995734176295034,1.,0.995734176295034,1.,0.995734176295034,1.,0.995734176295034,
1.,0.995734176295034,1.,0.995734176295034,1.,0.995734176295034,1.,0.995734176295034,
1.,0.995734176295034,1.,0.995734176295034,1.,0.995734176295034,1.,0.995734176295034,
1.,0.995734176295034,1.,0.995734176295034,1.,0.995734176295034,1.,0.995734176295034,
1.,0.995734176295034,1.,0.995734176295034,1.,0.995734176295034,1.,0.995734176295034,
1.,0.995734176295034,1.,0.995734176295034,1.,0.995734176295034,1.,0.995734176295034,
1.,0.995734176295034,1.,0.995734176295034,1.,0.995734176295034,1.,0.995734176295034,
1.,0.995734176295034,1.,0.995734176295034,1.,0.995734176295034,1.,0.995734176295034,
1.,0.995734176295034,1.,0.995734176295034,1.,0.995734176295034,1.,0.995734176295034,
1.,0.995734176295034,1.,0.995734176295034,1.,0.995734176295034,1.,0.995734176295034,
1.,0.995734176295034,1.,0.995734176295034,1.,0.995734176295034,1.,0.995734176295034,
1.,0.995734176295034,1.,0.995734176295034,1.,0.995734176295034,1.,0.995734176295034,
1.,0.995734176295034,1.,0.995734176295034,1.,0.995734176295034,1.,0.995734176295034,
1.,0.995734176295034,1.,0.995734176295034,1.,0.995734176295034,1.,0.995734176295034,
1.,0.995734176295034,1.,0.995734176295034,1.,0.995734176295034,1.,0.995734176295034,
1.,0.995734176295034,1.,0.995734176295034,1.,0.995734176295034,1.,0.995734176295034,
1.,0.995734176295034,1.,0.995734176295034,1.,0.995734176295034,1.,0.995734176295034,
1.,0.995734176295034,1.,0.995734176295034,1.,0.995734176295034,1.,0.995734176295034,
1.,0.995734176295034,1.,0.995734176295034,1.,0.995734176295034,1.,0.995734176295034,
1.,0.995734176295034,1.,0.995734176295034,1.,0.995734176295034,1.,0.995734176295034,
1.,0.995734176295034,1.,0.995734176295034,1.,0.995734176295034,1.,0.995734176295034,
1.,0.995734176295034,1.,0.995734176295034,1.,0.995734176295034,1.,0.995734176295034,
1.,0.995734176295034,1.,0.995734176295034,1.,0.995734176295034,1.,0.995734176295034,
1.,0.995734176295034,1.,0.995734176295034,1.,0.995734176295034,1.,0.995734176295034,
1.,0.995734176295034,1.,0.995734176295034,1.,0.995734176295034,1.,0.995734176295034,
1.,0.995734176295034,1.,0.995734176295034,1.,0.995734176295034,1.,0.995734176295034,
1.,0.995734176295034,1.,0.995734176295034,1.,0.995734176295034,1.,0.995734176295034,
1.,0.995734176295034,1.,0.995734176295034,1.,0.995734176295034,1.,0.995734176295034,
1.,0.995734176295034,1.,0.995734176295034,1.,0.995734176295034,1.,0.995734176295034,
1.,0.995734176295034,1.,0.995734176295034,1.,0.995734176295034,1.,0.995734176295034,
1.,0.995734176295034,1.,0.995734176295034,1.,0.995734176295034,1.,0.995734176295034,
1.,0.995734176295034,1.,0.995734176295034,1.,0.995734176295034,1.,0.995734176295034,
1.,0.995734176295034,1.,0.995734176295034,1.,0.995734176295034,1.,0.995734176295034,
1.,0.995734176295034,1.,0.995734176295034,1.,0.995734176295034,1.,0.995734176295034,
1.,0.995734176295034,1.,0.995734176295034,1.,0.995734176295034,1.,0.995734176295034,
1.,0.995734176295034,1.,0.995734176295034,1.,0.995734176295034,1.,0.995734176295034,
1.,0.995734176295034,1.,0.995734176295034,1.,0.995734176295034,1.,0.995734176295034,
1.,0.995734176295034,1.,0.995734176295034,1.,0.995734176295034,1.,0.995734176295034,
1.,0.995734176295034,1.,0.995734176295034,1.,0.995734176295034,1.,0.995734176295034,
1.,0.995734176295034,1.,0.995734176295034,1.,0.995734176295034,1.,0.995734176295034,
1.,0.995734176295034,1.,0.995734176295034,1.,0.995734176295034,1.,0.995734176295034,
1.,0.995734176295034,1.,0.995734176295034,1.,0.995734176295034,1.,0.995734176295034,
1.,0.995734176295034,1.,0.995734176295034,1.,0.995734176295034,1.,0.995734176295034,
1.,0.995734176295034,1.,0.995734176295034,1.,0.995734176295034,1.,0.995734176295034,
1.,0.995734176295034,1.,0.995734176295034,1.,0.995734176295034,1.,0.995734176295034,
1.,0.995734176295034,1.,0.995734176295034,1.,0.995734176295034,1.,0.995734176295034,
1.,0.995734176295034,1.,0.995734176295034,1.,0.995734176295034,1.,0.995734176295034,
1.,0.995734176295034,1.,0.995734176295034,1.,0.995734176295034,1.,0.995734176295034,
1.,0.995734176295034,1.,0.995734176295034,1.,0.995734176295034,1.,0.995734176295034,
1.,0.995734176295034,1.,0.995734176295034,1.,0.995734176295034,1.,0.995734176295034,
1.,0.995734176295034,1.,0.995734176295034,1.,0.995734176295034,1.,0.995734176295034,
1.,0.995734176295034,1.,0.995734176295034,1.,0.995734176295034,1.,0.995734176295034,
1.,0.995734176295034,1.,0.995734176295034,1.,0.995734176295034,1.,0.995734176295034,
1.,0.995734176295034,1.,0.995734176295034,1.,0.995734176295034,1.,0.995734176295034,
1.,0.995734176295034,1.,0.995734176295034,1.,0.995734176295034,1.,0.995734176295034,
1.,0.995734176295034,1.,0.995734176295034,1.,0.995734176295034,1.,0.995734176295034,
1.,0.995734176295034,1.,0.995734176295034,1.,0.995734176295034,1.,0.995734176295034,
1.,0.995734176295034,1.,0.995734176295034,1.,0.995734176295034,1.,0.995734176295034,
1.,0.995734176295034,1.,0.995734176295034,1.,0.995734176295034,1.,0.995734176295034,
1.,0.995734176295034,1.,0.995734176295034,1.,0.995734176295034,1.,0.995734176295034,
1.,0.995734176295034,1.,0.995734176295034,1.,0.995734176295034,1.,0.995734176295034,
1.,0.995734176295034,1.,0.995734176295034,1.,0.995734176295034,1.,0.995734176295034,
1.,0.995734176295034,1.,0.995734176295034,1.,0.995734176295034,1.,0.995734176295034,
1.,0.995734176295034,1.,0.995734176295034,1.,0.995734176295034,1.,0.995734176295034,
1.,0.995734176295034,1.,0.995734176295034,1.,0.995734176295034,1.,0.995734176295034,
1.,0.995734176295034,1.,0.995734176295034,1.,0.995734176295034,1.,0.995734176295034,
1.,0.995734176295034,1.,0.995734176295034,1.,0.995734176295034,1.,0.995734176295034,
1.,0.995734176295034,1.,0.995734176295034,1.,0.995734176295034,1.,0.995734176295034,
1.,0.995734176295034,1.,0.995734176295034,1.,0.995734176295034,1.,0.995734176295034,
1.,0.995734176295034,1.,0.995734176295034,1.,0.995734176295034,1.,0.995734176295034,
1.,0.995734176295034,1.,0.995734176295034,1.,0.995734176295034,1.,0.995734176295034,
1.,0.995734176295034,1.,0.995734176295034,1.,0.995734176295034,1.,0.995734176295034,
1.,0.995734176295034,1.,0.995734176295034,1.,0.995734176295034,1.,0.995734176295034,
1.,0.995734176295034,1.,0.995734176295034,1.,0.995734176295034,1.,0.995734176295034,
1.,0.995734176295034,1.,0.995734176295034,1.,0.995734176295034,1.,0.995734176295034,
1.,0.995734176295034,1.,0.995734176295034,1.,0.995734176295034,1.,0.995734176295034,
1.,0.995734176295034,1.,0.995734176295034,1.,0.995734176295034,1.,0.995734176295034,
1.,0.995734176295034,1.,0.995734176295034,1.,0.995734176295034,1.,0.995734176295034,
1.,0.995734176295034,1.,0.995734176295034,1.,0.995734176295034,1.,0.995734176295034,
1.,0.995734176295034,1.,0.995734176295034,1.,0.995734176295034,1.,0.995734176295034,
1.,0.995734176295034,1.,0.995734176295034,1.,0.995734176295034,1.,0.995734176295034,
1.,0.995734176295034,1.,0.995734176295034,1.,0.995734176295034,1.,0.995734176295034,
1.,0.995734176295034,1.,0.995734176295034,1.,0.995734176295034,1.,0.995734176295034,
1.,0.995734176295034,1.,0.995734176295034,1.,0.995734176295034,1.,0.995734176295034,
1.,0.995734176295034,1.,0.995734176295034,1.,0.995734176295034,1.,0.995734176295034,
1.,0.995734176295034,1.,0.995734176295034,1.,0.995734176295034,1.,0.995734176295034,
1.,0.995734176295034,1.,0.995734176295034,1.,0.995734176295034,1.,0.995734176295034,
1.,0.995734176295034,1.,0.995734176295034,1.,0.995734176295034,1.,0.995734176295034,
1.,0.995734176295034,1.,0.995734176295034,1.,0.995734176295034,1.,0.995734176295034,
1.,0.995734176295034,1.,0.995734176295034,1.,0.995734176295034,1.,0.995734176295034,
1.,0.995734176295034,1.,0.995734176295034,1.,0.995734176295034,1.,0.995734176295034,
1.,0.995734176295034,1.,0.995734176295034,1.,0.995734176295034,1.,0.995734176295034,
1.,0.995734176295034,1.,0.995734176295034,1.,0.995734176295034,1.,0.995734176295034,
1.,0.995734176295034,1.,0.995734176295034,1.,0.995734176295034,1.,0.995734176295034,
1.,0.995734176295034,1.,0.995734176295034,1.,0.995734176295034,1.,0.995734176295034,
1.,0.995734176295034,1.,0.995734176295034,1.,0.995734176295034,1.,0.995734176295034,
1.,0.995734176295034,1.,0.995734176295034,1.,0.995734176295034,1.,0.995734176295034,
1.,0.995734176295034,1.,0.995734176295034,1.,0.995734176295034,1.,0.995734176295034,
1.,0.995734176295034,1.,0.995734176295034,1.,0.995734176295034,1.,0.995734176295034,
1.,0.995734176295034,1.,0.995734176295034,1.,0.995734176295034,1.,0.995734176295034,
1.,0.995734176295034,1.,0.995734176295034,1.,0.995734176295034,1.,0.995734176295034,
1.,0.995734176295034,1.,0.995734176295034,1.,0.995734176295034,1.,0.995734176295034,
1.,0.995734176295034,1.,0.995734176295034,1.,0.995734176295034,1.,0.995734176295034,
1.,0.995734176295034,1.,0.995734176295034,1.,0.995734176295034,1.,0.995734176295034,
1.,0.995734176295034,1.,0.995734176295034,1.,0.995734176295034,1.,0.995734176295034,
1.,0.995734176295034,1.,0.995734176295034,1.,0.995734176295034,1.,0.995734176295034,
1.,0.995734176295034,1.,0.995734176295034,1.,0.995734176295034,1.,0.995734176295034,
1.,0.995734176295034,1.,0.995734176295034,1.,0.995734176295034,1.,0.995734176295034,
1.,0.995734176295034,1.,0.995734176295034,1.,0.995734176295034,1.,0.995734176295034,
1.,0.995734176295034,1.,0.995734176295034,1.,0.995734176295034,1.,0.995734176295034,
1.,0.995734176295034,1.,0.995734176295034,1.,0.995734176295034,1.,0.995734176295034,
1.,0.995734176295034,1.,0.995734176295034,1.,0.995734176295034,1.,0.995734176295034,
1.,0.995734176295034,1.,0.995734176295034,1.,0.995734176295034,1.,0.995734176295034,
1.,0.995734176295034,1.,0.995734176295034,1.,0.995734176295034,1.,0.995734176295034,
1.,0.995734176295034,1.,0.995734176295034,1.,0.995734176295034,1.,0.995734176295034,
1.,0.995734176295034,1.,0.995734176295034,1.,0.995734176295034,1.,0.995734176295034,
1.,0.995734176295034,1.,0.995734176295034,1.,0.995734176295034,1.,0.995734176295034,
1.,0.995734176295034,1.,0.995734176295034,1.,0.995734176295034,1.,0.995734176295034,
1.,0.995734176295034,1.,0.995734176295034,1.,0.995734176295034,1.,0.995734176295034,
1.,0.995734176295034,1.,0.995734176295034,1.,0.995734176295034,1.,0.995734176295034,
1.,0.995734176295034,1.,0.995734176295034,1.,0.995734176295034,1.,0.995734176295034,
1.,0.995734176295034,1.,0.995734176295034,1.,0.995734176295034,1.,0.995734176295034,
1.,0.995734176295034,1.,0.995734176295034,1.,0.995734176295034,1.,0.995734176295034,
1.,0.995734176295034,1.,0.995734176295034,1.,0.995734176295034,1.,0.995734176295034,
1.,0.995734176295034,1.,0.995734176295034,1.,0.995734176295034,1.,0.995734176295034,
1.,0.995734176295034,1.,0.995734176295034,1.,0.995734176295034,1.,0.995734176295034,
1.,0.995734176295034,1.,0.995734176295034,1.,0.995734176295034,1.,0.995734176295034,
1.,0.995734176295034,1.,0.995734176295034,1.,0.995734176295034,1.,0.995734176295034,
1.,0.995734176295034,1.,0.995734176295034,1.,0.995734176295034,1.,0.995734176295034,
1.,0.995734176295034,1.,0.995734176295034,1.,0.995734176295034,1.,0.995734176295034,
1.,0.995734176295034,1.,0.995734176295034,1.,0.995734176295034,1.,0.995734176295034,
1.,0.995734176295034,1.,0.995734176295034,1.,0.995734176295034,1.,0.995734176295034,
1.,0.995734176295034,1.,0.995734176295034,1.,0.995734176295034,1.,0.995734176295034,
1.,0.995734176295034,1.,0.995734176295034,1.,0.995734176295034,1.,0.995734176295034,
1.,0.995734176295034,1.,0.995734176295034,1.,0.995734176295034,1.,0.995734176295034,
1.,0.995734176295034,1.,0.995734176295034,1.,0.995734176295034,1.,0.995734176295034,
1.,0.995734176295034,1.,0.995734176295034,1.,0.995734176295034,1.,0.995734176295034,
1.,0.995734176295034,1.,0.995734176295034,1.,0.995734176295034,1.,0.995734176295034,
1.,0.995734176295034,1.,0.995734176295034,1.,0.995734176295034,1.,0.995734176295034,
1.,0.995734176295034,1.,0.995734176295034,1.,0.995734176295034,1.,0.995734176295034,
1.,0.995734176295034,1.,0.995734176295034,1.,0.995734176295034,1.,0.995734176295034,
1.,0.995734176295034,1.,0.995734176295034,1.,0.995734176295034,1.,0.995734176295034,
1.,0.995734176295034,1.,0.995734176295034,1.,0.995734176295034,1.,0.995734176295034,
1.,0.995734176295034,1.,0.995734176295034,1.,0.995734176295034,1.,0.995734176295034,
1.,0.995734176295034,1.,0.995734176295034,1.,0.995734176295034,1.,0.995734176295034,
1.,0.995734176295034,1.,0.995734176295034,1.,0.995734176295034,1.,0.995734176295034,
1.,0.995734176295034,1.,0.995734176295034,1.,0.995734176295034,1.,0.995734176295034,
1.,0.995734176295034,1.,0.995734176295034,1.,0.995734176295034,1.,0.995734176295034,
1.,0.995734176295034,1.,0.995734176295034,1.,0.995734176295034,1.,0.995734176295034,
1.,0.995734176295034,1.,0.995734176295034,1.,0.995734176295034,1.,0.995734176295034,
1.,0.995734176295034,1.,0.995734176295034,1.,0.995734176295034,1.,0.995734176295034,
1.,0.995734176295034,1.,0.995734176295034,1.,0.995734176295034,1.,0.995734176295034,
1.,0.995734176295034,1.,0.995734176295034,1.,0.995734176295034,1.,0.995734176295034,
1.,0.995734176295034,1.,0.995734176295034,1.,0.995734176295034,1.,0.995734176295034,
1.,0.995734176295034,1.,0.995734176295034,1.,0.995734176295034,1.,0.995734176295034,
1.,0.995734176295034,1.,0.995734176295034,1.,0.995734176295034,1.,0.995734176295034,
1.,0.995734176295034,1.,0.995734176295034,1.,0.995734176295034,1.,0.995734176295034,
1.,0.995734176295034,1.,0.995734176295034,1.,0.995734176295034,1.,0.995734176295034,
1.,0.995734176295034,1.,0.995734176295034,1.,0.995734176295034,1.,0.995734176295034,
1.,0.995734176295034,1.,0.995734176295034,1.,0.995734176295034,1.,0.995734176295034,
1.,0.995734176295034,1.,0.995734176295034,1.,0.995734176295034,1.,0.995734176295034,
1.,0.995734176295034,1.,0.995734176295034,1.,0.995734176295034,1.,0.995734176295034,
1.,0.995734176295034,1.,0.995734176295034,1.,0.995734176295034,1.,0.995734176295034,
1.,0.995734176295034,1.,0.995734176295034,1.,0.995734176295034,1.,0.995734176295034,
1.,0.995734176295034,1.,0.995734176295034,1.,0.995734176295034,1.,0.995734176295034,
1.,0.995734176295034,1.,0.995734176295034,1.,0.995734176295034,1.,0.995734176295034,
1.,0.995734176295034,1.,0.995734176295034,1.,0.995734176295034,1.,0.995734176295034,
1.,0.995734176295034,1.,0.995734176295034,1.,0.995734176295034,1.,0.995734176295034,
1.,0.995734176295034,1.,0.995734176295034,1.,0.995734176295034,1.,0.995734176295034,
1.,0.995734176295034,1.,0.995734176295034,1.,0.995734176295034,1.,0.995734176295034,
1.,0.995734176295034,1.,0.995734176295034,1.,0.995734176295034,1.,0.995734176295034,
1.,0.995734176295034,1.,0.995734176295034,1.,0.995734176295034,1.,0.995734176295034,
1.,0.995734176295034,1.,0.995734176295034,1.,0.995734176295034,1.,0.995734176295034,
1.,0.995734176295034,1.,0.995734176295034,1.,0.995734176295034,1.,0.995734176295034,
1.,0.995734176295034,1.,0.995734176295034,1.,0.995734176295034,1.,0.995734176295034,
1.,0.995734176295034,1.,0.995734176295034,1.,0.995734176295034,1.,0.995734176295034,
1.,0.995734176295034,1.,0.995734176295034,1.,0.995734176295034,1.,0.995734176295034,
1.,0.995734176295034,1.,0.995734176295034,1.,0.995734176295034,1.,0.995734176295034,
1.,0.995734176295034,1.,0.995734176295034,1.,0.995734176295034,1.,0.995734176295034,
1.,0.995734176295034,1.,0.995734176295034,1.,0.995734176295034,1.,0.995734176295034,
1.,0.995734176295034,1.,0.995734176295034,1.,0.995734176295034,1.,0.995734176295034,
1.,0.995734176295034,1.,0.995734176295034,1.,0.995734176295034,1.,0.995734176295034,
1.,0.995734176295034,1.,0.995734176295034,1.,0.995734176295034,1.,0.995734176295034,
1.,0.995734176295034,1.,0.995734176295034,1.,0.995734176295034,1.,0.995734176295034,
1.,0.995734176295034,1.,0.995734176295034,1.,0.995734176295034,1.,0.995734176295034,
1.,0.995734176295034,1.,0.995734176295034,1.,0.995734176295034,1.,0.995734176295034,
1.,0.995734176295034,1.,0.995734176295034,1.,0.995734176295034,1.,0.995734176295034,
1.,0.995734176295034,1.,0.995734176295034,1.,0.995734176295034,1.,0.995734176295034,
1.,0.995734176295034,1.,0.995734176295034,1.,0.995734176295034,1.,0.995734176295034,
1.,0.995734176295034,1.,0.995734176295034,1.,0.995734176295034,1.,0.995734176295034,
1.,0.995734176295034,1.,0.995734176295034,1.,0.995734176295034,1.,0.995734176295034,
1.,0.995734176295034,1.,0.995734176295034,1.,0.995734176295034,1.,0.995734176295034,
1.,0.995734176295034,1.,0.995734176295034,1.,0.995734176295034,1.,0.995734176295034,
1.,0.995734176295034,1.,0.995734176295034,1.,0.995734176295034,1.,0.995734176295034,
1.,0.995734176295034,1.,0.995734176295034,1.,0.995734176295034,1.,0.995734176295034,
1.,0.995734176295034,1.,0.995734176295034,1.,0.995734176295034,1.,0.995734176295034,
1.,0.995734176295034,1.,0.995734176295034,1.,0.995734176295034,1.,0.995734176295034,
1.,0.995734176295034,1.,0.995734176295034,1.,0.995734176295034,1.,0.995734176295034,
1.,0.995734176295034,1.,0.995734176295034,1.,0.995734176295034,1.,0.995734176295034,
1.,0.995734176295034,1.,0.995734176295034,1.,0.995734176295034,1.,0.995734176295034,
1.,0.995734176295034,1.,0.995734176295034,1.,0.995734176295034,1.,0.995734176295034,
1.,0.995734176295034,1.,0.995734176295034,1.,0.995734176295034,1.,0.995734176295034,
1.,0.995734176295034,1.,0.995734176295034,1.,0.995734176295034,1.,0.995734176295034,
1.,0.995734176295034,1.,0.995734176295034,1.,0.995734176295034,1.,0.995734176295034,
1.,0.995734176295034,1.,0.995734176295034,1.,0.995734176295034,1.,0.995734176295034,
1.,0.995734176295034,1.,0.995734176295034,1.,0.995734176295034,1.,0.995734176295034,
1.,0.995734176295034,1.,0.995734176295034,1.,0.995734176295034,1.,0.995734176295034,
1.,0.995734176295034,1.,0.995734176295034,1.,0.995734176295034,1.,0.995734176295034,
1.,0.995734176295034,1.,0.995734176295034,1.,0.995734176295034,1.,0.995734176295034,
1.,0.995734176295034,1.,0.995734176295034,1.,0.995734176295034,1.,0.995734176295034,
1.,0.995734176295034,1.,0.995734176295034,1.,0.995734176295034,1.,0.995734176295034,
1.,0.995734176295034,1.,0.995734176295034,1.,0.995734176295034,1.,0.995734176295034,
1.,0.995734176295034,1.,0.995734176295034,1.,0.995734176295034,1.,0.995734176295034,
1.,0.995734176295034,1.,0.995734176295034,1.,0.995734176295034,1.,0.995734176295034,
1.,0.995734176295034,1.,0.995734176295034,1.,0.995734176295034,1.,0.995734176295034,
1.,0.995734176295034,1.,0.995734176295034,1.,0.995734176295034,1.,0.995734176295034,
1.,0.995734176295034,1.,0.995734176295034,1.,0.995734176295034,1.,0.995734176295034,
1.,0.995734176295034,1.,0.995734176295034,1.,0.995734176295034,1.,0.995734176295034,
1.,0.995734176295034,1.,0.995734176295034,1.,0.995734176295034,1.,0.995734176295034,
1.,0.995734176295034,1.,0.995734176295034,1.,0.995734176295034,1.,0.995734176295034,
1.,0.995734176295034,1.,0.995734176295034,1.,0.995734176295034,1.,0.995734176295034,
1.,0.995734176295034,1.,0.995734176295034,1.,0.995734176295034,1.,0.995734176295034,
1.,0.995734176295034,1.,0.995734176295034,1.,0.995734176295034,1.,0.995734176295034,
1.,0.995734176295034,1.,0.995734176295034,1.,0.995734176295034,1.,0.995734176295034,
1.,0.995734176295034,1.,0.995734176295034,1.,0.995734176295034,1.,0.995734176295034,
1.,0.995734176295034,1.,0.995734176295034,1.,0.995734176295034,1.,0.995734176295034,
1.,0.995734176295034,1.,0.995734176295034,1.,0.995734176295034,1.,0.995734176295034,
1.,0.995734176295034,1.,0.995734176295034,1.,0.995734176295034,1.,0.995734176295034,
1.,0.995734176295034,1.,0.995734176295034,1.,0.995734176295034,1.,0.995734176295034,
1.,0.995734176295034,1.,0.995734176295034,1.,0.995734176295034,1.,0.995734176295034,
1.,0.995734176295034,1.,0.995734176295034,1.,0.995734176295034,1.,0.995734176295034,
1.,0.995734176295034,1.,0.995734176295034,1.,0.995734176295034,1.,0.995734176295034,
1.,0.995734176295034,1.,0.995734176295034,1.,0.995734176295034,1.,0.995734176295034,
1.,0.995734176295034,1.,0.995734176295034,1.,0.995734176295034,1.,0.995734176295034,
1.,0.995734176295034,1.,0.995734176295034,1.,0.995734176295034,1.,0.995734176295034,
1.,0.995734176295034,1.,0.995734176295034,1.,0.995734176295034,1.,0.995734176295034,
1.,0.995734176295034,1.,0.995734176295034,1.,0.995734176295034,1.,0.995734176295034,
1.,0.995734176295034,1.,0.995734176295034,1.,0.995734176295034,1.,0.995734176295034,
1.,0.995734176295034,1.,0.995734176295034,1.,0.995734176295034,1.,0.995734176295034,
1.,0.995734176295034,1.,0.995734176295034,1.,0.995734176295034,1.,0.995734176295034,
1.,0.995734176295034,1.,0.995734176295034,1.,0.995734176295034,1.,0.995734176295034,
1.,0.995734176295034,1.,0.995734176295034,1.,0.995734176295034,1.,0.995734176295034,
1.,0.995734176295034,1.,0.995734176295034,1.,0.995734176295034,1.,0.995734176295034,
1.,0.995734176295034,1.,0.995734176295034,1.,0.995734176295034,1.,0.995734176295034,
1.,0.995734176295034,1.,0.995734176295034,1.,0.995734176295034,1.,0.995734176295034,
1.,0.995734176295034,1.,0.995734176295034,1.,0.995734176295034,1.,0.995734176295034,
1.,0.995734176295034,1.,0.995734176295034,1.,0.995734176295034,1.,0.995734176295034,
1.,0.995734176295034,1.,0.995734176295034,1.,0.995734176295034,1.,0.995734176295034,
1.,0.995734176295034,1.,0.995734176295034,1.,0.995734176295034,1.,0.997201362504481,
0.998074874808405,0.998074874808405,0.998074874808405),(1.,0.995734176295034,
1.,0.995734176295034,1.,0.995734176295034,1.,0.995734176295034,1.,0.995734176295034,
1.,0.995734176295034,1.,0.995734176295034,1.,0.995734176295034,1.,0.995734176295034,
1.,0.995734176295034,1.,0.995734176295034,1.,0.995734176295034,1.,0.995734176295034,
1.,0.995734176295034,1.,0.995734176295034,1.,0.995734176295034,1.,0.995734176295034,
1.,0.995734176295034,1.,0.995734176295034,1.,0.995734176295034,1.,0.995734176295034,
1.,0.995734176295034,1.,0.995734176295034,1.,0.995734176295034,1.,0.995734176295034,
1.,0.995734176295034,1.,0.995734176295034,1.,0.995734176295034,1.,0.995734176295034,
1.,0.995734176295034,1.,0.995734176295034,1.,0.995734176295034,1.,0.995734176295034,
1.,0.995734176295034,1.,0.995734176295034,1.,0.995734176295034,1.,0.995734176295034,
1.,0.995734176295034,1.,0.995734176295034,1.,0.995734176295034,1.,0.995734176295034,
1.,0.995734176295034,1.,0.995734176295034,1.,0.995734176295034,1.,0.995734176295034,
1.,0.995734176295034,1.,0.995734176295034,1.,0.995734176295034,1.,0.995734176295034,
1.,0.995734176295034,1.,0.995734176295034,1.,0.995734176295034,1.,0.995734176295034,
1.,0.995734176295034,1.,0.995734176295034,1.,0.995734176295034,1.,0.995734176295034,
1.,0.995734176295034,1.,0.995734176295034,1.,0.995734176295034,1.,0.995734176295034,
1.,0.995734176295034,1.,0.995734176295034,1.,0.995734176295034,1.,0.995734176295034,
1.,0.995734176295034,1.,0.995734176295034,1.,0.995734176295034,1.,0.995734176295034,
1.,0.995734176295034,1.,0.995734176295034,1.,0.995734176295034,1.,0.995734176295034,
1.,0.995734176295034,1.,0.995734176295034,1.,0.995734176295034,1.,0.995734176295034,
1.,0.995734176295034,1.,0.995734176295034,1.,0.995734176295034,1.,0.995734176295034,
1.,0.995734176295034,1.,0.995734176295034,1.,0.995734176295034,1.,0.995734176295034,
1.,0.995734176295034,1.,0.995734176295034,1.,0.995734176295034,1.,0.995734176295034,
1.,0.995734176295034,1.,0.995734176295034,1.,0.995734176295034,1.,0.995734176295034,
1.,0.995734176295034,1.,0.995734176295034,1.,0.995734176295034,1.,0.995734176295034,
1.,0.995734176295034,1.,0.995734176295034,1.,0.995734176295034,1.,0.995734176295034,
1.,0.995734176295034,1.,0.995734176295034,1.,0.995734176295034,1.,0.995734176295034,
1.,0.995734176295034,1.,0.995734176295034,1.,0.995734176295034,1.,0.995734176295034,
1.,0.995734176295034,1.,0.995734176295034,1.,0.995734176295034,1.,0.995734176295034,
1.,0.995734176295034,1.,0.995734176295034,1.,0.995734176295034,1.,0.995734176295034,
1.,0.995734176295034,1.,0.995734176295034,1.,0.995734176295034,1.,0.995734176295034,
1.,0.995734176295034,1.,0.995734176295034,1.,0.995734176295034,1.,0.995734176295034,
1.,0.995734176295034,1.,0.995734176295034,1.,0.995734176295034,1.,0.995734176295034,
1.,0.995734176295034,1.,0.995734176295034,1.,0.995734176295034,1.,0.995734176295034,
1.,0.995734176295034,1.,0.995734176295034,1.,0.995734176295034,1.,0.995734176295034,
1.,0.995734176295034,1.,0.995734176295034,1.,0.995734176295034,1.,0.995734176295034,
1.,0.995734176295034,1.,0.995734176295034,1.,0.995734176295034,1.,0.995734176295034,
1.,0.995734176295034,1.,0.995734176295034,1.,0.995734176295034,1.,0.995734176295034,
1.,0.995734176295034,1.,0.995734176295034,1.,0.995734176295034,1.,0.995734176295034,
1.,0.995734176295034,1.,0.995734176295034,1.,0.995734176295034,1.,0.995734176295034,
1.,0.995734176295034,1.,0.995734176295034,1.,0.995734176295034,1.,0.995734176295034,
1.,0.995734176295034,1.,0.995734176295034,1.,0.995734176295034,1.,0.995734176295034,
1.,0.995734176295034,1.,0.995734176295034,1.,0.995734176295034,1.,0.995734176295034,
1.,0.995734176295034,1.,0.995734176295034,1.,0.995734176295034,1.,0.995734176295034,
1.,0.995734176295034,1.,0.995734176295034,1.,0.995734176295034,1.,0.995734176295034,
1.,0.995734176295034,1.,0.995734176295034,1.,0.995734176295034,1.,0.995734176295034,
1.,0.995734176295034,1.,0.995734176295034,1.,0.995734176295034,1.,0.995734176295034,
1.,0.995734176295034,1.,0.995734176295034,1.,0.995734176295034,1.,0.995734176295034,
1.,0.995734176295034,1.,0.995734176295034,1.,0.995734176295034,1.,0.995734176295034,
1.,0.995734176295034,1.,0.995734176295034,1.,0.995734176295034,1.,0.995734176295034,
1.,0.995734176295034,1.,0.995734176295034,1.,0.995734176295034,1.,0.995734176295034,
1.,0.995734176295034,1.,0.995734176295034,1.,0.995734176295034,1.,0.995734176295034,
1.,0.995734176295034,1.,0.995734176295034,1.,0.995734176295034,1.,0.995734176295034,
1.,0.995734176295034,1.,0.995734176295034,1.,0.995734176295034,1.,0.995734176295034,
1.,0.995734176295034,1.,0.995734176295034,1.,0.995734176295034,1.,0.995734176295034,
1.,0.995734176295034,1.,0.995734176295034,1.,0.995734176295034,1.,0.995734176295034,
1.,0.995734176295034,1.,0.995734176295034,1.,0.995734176295034,1.,0.995734176295034,
1.,0.995734176295034,1.,0.995734176295034,1.,0.995734176295034,1.,0.995734176295034,
1.,0.995734176295034,1.,0.995734176295034,1.,0.995734176295034,1.,0.995734176295034,
1.,0.995734176295034,1.,0.995734176295034,1.,0.995734176295034,1.,0.995734176295034,
1.,0.995734176295034,1.,0.995734176295034,1.,0.995734176295034,1.,0.995734176295034,
1.,0.995734176295034,1.,0.995734176295034,1.,0.995734176295034,1.,0.995734176295034,
1.,0.995734176295034,1.,0.995734176295034,1.,0.995734176295034,1.,0.995734176295034,
1.,0.995734176295034,1.,0.995734176295034,1.,0.995734176295034,1.,0.995734176295034,
1.,0.995734176295034,1.,0.995734176295034,1.,0.995734176295034,1.,0.995734176295034,
1.,0.995734176295034,1.,0.995734176295034,1.,0.995734176295034,1.,0.995734176295034,
1.,0.995734176295034,1.,0.995734176295034,1.,0.995734176295034,1.,0.995734176295034,
1.,0.995734176295034,1.,0.995734176295034,1.,0.995734176295034,1.,0.995734176295034,
1.,0.995734176295034,1.,0.995734176295034,1.,0.995734176295034,1.,0.995734176295034,
1.,0.995734176295034,1.,0.995734176295034,1.,0.995734176295034,1.,0.995734176295034,
1.,0.995734176295034,1.,0.995734176295034,1.,0.995734176295034,1.,0.995734176295034,
1.,0.995734176295034,1.,0.995734176295034,1.,0.995734176295034,1.,0.995734176295034,
1.,0.995734176295034,1.,0.995734176295034,1.,0.995734176295034,1.,0.995734176295034,
1.,0.995734176295034,1.,0.995734176295034,1.,0.995734176295034,1.,0.995734176295034,
1.,0.995734176295034,1.,0.995734176295034,1.,0.995734176295034,1.,0.995734176295034,
1.,0.995734176295034,1.,0.995734176295034,1.,0.995734176295034,1.,0.995734176295034,
1.,0.995734176295034,1.,0.995734176295034,1.,0.995734176295034,1.,0.995734176295034,
1.,0.995734176295034,1.,0.995734176295034,1.,0.995734176295034,1.,0.995734176295034,
1.,0.995734176295034,1.,0.995734176295034,1.,0.995734176295034,1.,0.995734176295034,
1.,0.995734176295034,1.,0.995734176295034,1.,0.995734176295034,1.,0.995734176295034,
1.,0.995734176295034,1.,0.995734176295034,1.,0.995734176295034,1.,0.995734176295034,
1.,0.995734176295034,1.,0.995734176295034,1.,0.995734176295034,1.,0.995734176295034,
1.,0.995734176295034,1.,0.995734176295034,1.,0.995734176295034,1.,0.995734176295034,
1.,0.995734176295034,1.,0.995734176295034,1.,0.995734176295034,1.,0.995734176295034,
1.,0.995734176295034,1.,0.995734176295034,1.,0.995734176295034,1.,0.995734176295034,
1.,0.995734176295034,1.,0.995734176295034,1.,0.995734176295034,1.,0.995734176295034,
1.,0.995734176295034,1.,0.995734176295034,1.,0.995734176295034,1.,0.995734176295034,
1.,0.995734176295034,1.,0.995734176295034,1.,0.995734176295034,1.,0.995734176295034,
1.,0.995734176295034,1.,0.995734176295034,1.,0.995734176295034,1.,0.995734176295034,
1.,0.995734176295034,1.,0.995734176295034,1.,0.995734176295034,1.,0.995734176295034,
1.,0.995734176295034,1.,0.995734176295034,1.,0.995734176295034,1.,0.995734176295034,
1.,0.995734176295034,1.,0.995734176295034,1.,0.995734176295034,1.,0.995734176295034,
1.,0.995734176295034,1.,0.995734176295034,1.,0.995734176295034,1.,0.995734176295034,
1.,0.995734176295034,1.,0.995734176295034,1.,0.995734176295034,1.,0.995734176295034,
1.,0.995734176295034,1.,0.995734176295034,1.,0.995734176295034,1.,0.995734176295034,
1.,0.995734176295034,1.,0.995734176295034,1.,0.995734176295034,1.,0.995734176295034,
1.,0.995734176295034,1.,0.995734176295034,1.,0.995734176295034,1.,0.995734176295034,
1.,0.995734176295034,1.,0.995734176295034,1.,0.995734176295034,1.,0.995734176295034,
1.,0.995734176295034,1.,0.995734176295034,1.,0.995734176295034,1.,0.995734176295034,
1.,0.995734176295034,1.,0.995734176295034,1.,0.995734176295034,1.,0.995734176295034,
1.,0.995734176295034,1.,0.995734176295034,1.,0.995734176295034,1.,0.995734176295034,
1.,0.995734176295034,1.,0.995734176295034,1.,0.995734176295034,1.,0.995734176295034,
1.,0.995734176295034,1.,0.995734176295034,1.,0.995734176295034,1.,0.995734176295034,
1.,0.995734176295034,1.,0.995734176295034,1.,0.995734176295034,1.,0.995734176295034,
1.,0.995734176295034,1.,0.995734176295034,1.,0.995734176295034,1.,0.995734176295034,
1.,0.995734176295034,1.,0.995734176295034,1.,0.995734176295034,1.,0.995734176295034,
1.,0.995734176295034,1.,0.995734176295034,1.,0.995734176295034,1.,0.995734176295034,
1.,0.995734176295034,1.,0.995734176295034,1.,0.995734176295034,1.,0.995734176295034,
1.,0.995734176295034,1.,0.995734176295034,1.,0.995734176295034,1.,0.995734176295034,
1.,0.995734176295034,1.,0.995734176295034,1.,0.995734176295034,1.,0.995734176295034,
1.,0.995734176295034,1.,0.995734176295034,1.,0.995734176295034,1.,0.995734176295034,
1.,0.995734176295034,1.,0.995734176295034,1.,0.995734176295034,1.,0.995734176295034,
1.,0.995734176295034,1.,0.995734176295034,1.,0.995734176295034,1.,0.995734176295034,
1.,0.995734176295034,1.,0.995734176295034,1.,0.995734176295034,1.,0.995734176295034,
1.,0.995734176295034,1.,0.995734176295034,1.,0.995734176295034,1.,0.995734176295034,
1.,0.995734176295034,1.,0.995734176295034,1.,0.995734176295034,1.,0.995734176295034,
1.,0.995734176295034,1.,0.995734176295034,1.,0.995734176295034,1.,0.995734176295034,
1.,0.995734176295034,1.,0.995734176295034,1.,0.995734176295034,1.,0.995734176295034,
1.,0.995734176295034,1.,0.995734176295034,1.,0.995734176295034,1.,0.995734176295034,
1.,0.995734176295034,1.,0.995734176295034,1.,0.995734176295034,1.,0.995734176295034,
1.,0.995734176295034,1.,0.995734176295034,1.,0.995734176295034,1.,0.995734176295034,
1.,0.995734176295034,1.,0.995734176295034,1.,0.995734176295034,1.,0.995734176295034,
1.,0.995734176295034,1.,0.995734176295034,1.,0.995734176295034,1.,0.995734176295034,
1.,0.995734176295034,1.,0.995734176295034,1.,0.995734176295034,1.,0.995734176295034,
1.,0.995734176295034,1.,0.995734176295034,1.,0.995734176295034,1.,0.995734176295034,
1.,0.995734176295034,1.,0.995734176295034,1.,0.995734176295034,1.,0.995734176295034,
1.,0.995734176295034,1.,0.995734176295034,1.,0.995734176295034,1.,0.995734176295034,
1.,0.995734176295034,1.,0.995734176295034,1.,0.995734176295034,1.,0.995734176295034,
1.,0.995734176295034,1.,0.995734176295034,1.,0.995734176295034,1.,0.995734176295034,
1.,0.995734176295034,1.,0.995734176295034,1.,0.995734176295034,1.,0.995734176295034,
1.,0.995734176295034,1.,0.995734176295034,1.,0.995734176295034,1.,0.995734176295034,
1.,0.995734176295034,1.,0.995734176295034,1.,0.995734176295034,1.,0.995734176295034,
1.,0.995734176295034,1.,0.995734176295034,1.,0.995734176295034,1.,0.995734176295034,
1.,0.995734176295034,1.,0.995734176295034,1.,0.995734176295034,1.,0.995734176295034,
1.,0.995734176295034,1.,0.995734176295034,1.,0.995734176295034,1.,0.995734176295034,
1.,0.995734176295034,1.,0.995734176295034,1.,0.995734176295034,1.,0.995734176295034,
1.,0.995734176295034,1.,0.995734176295034,1.,0.995734176295034,1.,0.995734176295034,
1.,0.995734176295034,1.,0.995734176295034,1.,0.995734176295034,1.,0.995734176295034,
1.,0.995734176295034,1.,0.995734176295034,1.,0.995734176295034,1.,0.995734176295034,
1.,0.995734176295034,1.,0.995734176295034,1.,0.995734176295034,1.,0.995734176295034,
1.,0.995734176295034,1.,0.995734176295034,1.,0.995734176295034,1.,0.995734176295034,
1.,0.995734176295034,1.,0.995734176295034,1.,0.995734176295034,1.,0.995734176295034,
1.,0.995734176295034,1.,0.995734176295034,1.,0.995734176295034,1.,0.995734176295034,
1.,0.995734176295034,1.,0.995734176295034,1.,0.995734176295034,1.,0.995734176295034,
1.,0.995734176295034,1.,0.995734176295034,1.,0.995734176295034,1.,0.995734176295034,
1.,0.995734176295034,1.,0.995734176295034,1.,0.995734176295034,1.,0.995734176295034,
1.,0.995734176295034,1.,0.995734176295034,1.,0.995734176295034,1.,0.995734176295034,
1.,0.995734176295034,1.,0.995734176295034,1.,0.995734176295034,1.,0.995734176295034,
1.,0.995734176295034,1.,0.995734176295034,1.,0.995734176295034,1.,0.995734176295034,
1.,0.995734176295034,1.,0.995734176295034,1.,0.995734176295034,1.,0.995734176295034,
1.,0.995734176295034,1.,0.995734176295034,1.,0.995734176295034,1.,0.995734176295034,
1.,0.995734176295034,1.,0.995734176295034,1.,0.995734176295034,1.,0.995734176295034,
1.,0.995734176295034,1.,0.995734176295034,1.,0.995734176295034,1.,0.995734176295034,
1.,0.995734176295034,1.,0.995734176295034,1.,0.995734176295034,1.,0.995734176295034,
1.,0.995734176295034,1.,0.995734176295034,1.,0.995734176295034,1.,0.995734176295034,
1.,0.995734176295034,1.,0.995734176295034,1.,0.995734176295034,1.,0.995734176295034,
1.,0.995734176295034,1.,0.995734176295034,1.,0.995734176295034,1.,0.995734176295034,
1.,0.995734176295034,1.,0.995734176295034,1.,0.995734176295034,1.,0.995734176295034,
1.,0.995734176295034,1.,0.995734176295034,1.,0.995734176295034,1.,0.995734176295034,
1.,0.995734176295034,1.,0.995734176295034,1.,0.995734176295034,1.,0.995734176295034,
1.,0.995734176295034,1.,0.995734176295034,1.,0.995734176295034,1.,0.995734176295034,
1.,0.995734176295034,1.,0.995734176295034,1.,0.995734176295034,1.,0.995734176295034,
1.,0.995734176295034,1.,0.995734176295034,1.,0.995734176295034,1.,0.995734176295034,
1.,0.995734176295034,1.,0.995734176295034,1.,0.995734176295034,1.,0.995734176295034,
1.,0.995734176295034,1.,0.995734176295034,1.,0.995734176295034,1.,0.995734176295034,
1.,0.995734176295034,1.,0.995734176295034,1.,0.995734176295034,1.,0.995734176295034,
1.,0.995734176295034,1.,0.995734176295034,1.,0.995734176295034,1.,0.995734176295034,
1.,0.995734176295034,1.,0.995734176295034,1.,0.995734176295034,1.,0.995734176295034,
1.,0.995734176295034,1.,0.995734176295034,1.,0.995734176295034,1.,0.995734176295034,
1.,0.995734176295034,1.,0.995734176295034,1.,0.995734176295034,1.,0.995734176295034,
1.,0.995734176295034,1.,0.995734176295034,1.,0.995734176295034,1.,0.995734176295034,
1.,0.995734176295034,1.,0.995734176295034,1.,0.995734176295034,1.,0.995734176295034,
1.,0.995734176295034,1.,0.995734176295034,1.,0.995734176295034,1.,0.995734176295034,
1.,0.995734176295034,1.,0.995734176295034,1.,0.995734176295034,1.,0.995734176295034,
1.,0.995734176295034,1.,0.995734176295034,1.,0.995734176295034,1.,0.995734176295034,
1.,0.995734176295034,1.,0.995734176295034,1.,0.995734176295034,1.,0.995734176295034,
1.,0.995734176295034,1.,0.995734176295034,1.,0.995734176295034,1.,0.995734176295034,
1.,0.995734176295034,1.,0.995734176295034,1.,0.995734176295034,1.,0.995734176295034,
1.,0.995734176295034,1.,0.995734176295034,1.,0.995734176295034,1.,0.995734176295034,
1.,0.995734176295034,1.,0.995734176295034,1.,0.995734176295034,1.,0.995734176295034,
1.,0.995734176295034,1.,0.995734176295034,1.,0.995734176295034,1.,0.995734176295034,
1.,0.995734176295034,1.,0.995734176295034,1.,0.995734176295034,1.,0.995734176295034,
1.,0.995734176295034,1.,0.995734176295034,1.,0.995734176295034,1.,0.995734176295034,
1.,0.995734176295034,1.,0.995734176295034,1.,0.995734176295034,1.,0.995734176295034,
1.,0.995734176295034,1.,0.995734176295034,1.,0.995734176295034,1.,0.995734176295034,
1.,0.995734176295034,1.,0.995734176295034,1.,0.995734176295034,1.,0.995734176295034,
1.,0.995734176295034,1.,0.995734176295034,1.,0.995734176295034,1.,0.995734176295034,
1.,0.995734176295034,1.,0.995734176295034,1.,0.995734176295034,1.,0.995734176295034,
1.,0.995734176295034,1.,0.995734176295034,1.,0.995734176295034,1.,0.995734176295034,
1.,0.995734176295034,1.,0.995734176295034,1.,0.995734176295034,1.,0.995734176295034,
1.,0.995734176295034,1.,0.995734176295034,1.,0.995734176295034,1.,0.995734176295034,
1.,0.995734176295034,1.,0.995734176295034,1.,0.995734176295034,1.,0.995734176295034,
1.,0.995734176295034,1.,0.995734176295034,1.,0.995734176295034,1.,0.995734176295034,
1.,0.995734176295034,1.,0.995734176295034,1.,0.995734176295034,1.,0.995734176295034,
1.,0.995734176295034,1.,0.995734176295034,1.,0.995734176295034,1.,0.995734176295034,
1.,0.995734176295034,1.,0.995734176295034,1.,0.995734176295034,1.,0.995734176295034,
1.,0.995734176295034,1.,0.995734176295034,1.,0.995734176295034,1.,0.995734176295034,
1.,0.995734176295034,1.,0.995734176295034,1.,0.995734176295034,1.,0.995734176295034,
1.,0.995734176295034,1.,0.995734176295034,1.,0.995734176295034,1.,0.995734176295034,
1.,0.995734176295034,1.,0.995734176295034,1.,0.995734176295034,1.,0.995734176295034,
1.,0.995734176295034,1.,0.995734176295034,1.,0.995734176295034,1.,0.995734176295034,
1.,0.995734176295034,1.,0.995734176295034,1.,0.995734176295034,1.,0.995734176295034,
1.,0.995734176295034,1.,0.995734176295034,1.,0.995734176295034,1.,0.995734176295034,
1.,0.995734176295034,1.,0.995734176295034,1.,0.995734176295034,1.,0.995734176295034,
1.,0.995734176295034,1.,0.995734176295034,1.,0.995734176295034,1.,0.995734176295034,
1.,0.995734176295034,1.,0.995734176295034,1.,0.995734176295034,1.,0.995734176295034,
1.,0.995734176295034,1.,0.995734176295034,1.,0.995734176295034,1.,0.995734176295034,
1.,0.995734176295034,1.,0.995734176295034,1.,0.995734176295034,1.,0.995734176295034,
1.,0.995734176295034,1.,0.995734176295034,1.,0.995734176295034,1.,0.995734176295034,
1.,0.995734176295034,1.,0.995734176295034,1.,0.995734176295034,1.,0.995734176295034,
1.,0.995734176295034,1.,0.995734176295034,1.,0.995734176295034,1.,0.995734176295034,
1.,0.995734176295034,1.,0.995734176295034,1.,0.995734176295034,1.,0.995734176295034,
1.,0.995734176295034,1.,0.995734176295034,1.,0.995734176295034,1.,0.995734176295034,
1.,0.995734176295034,1.,0.995734176295034,1.,0.995734176295034,1.,0.995734176295034,
1.,0.995734176295034,1.,0.995734176295034,1.,0.995734176295034,1.,0.995734176295034,
1.,0.995734176295034,1.,0.995734176295034,1.,0.995734176295034,1.,0.995734176295034,
1.,0.995734176295034,1.,0.995734176295034,1.,0.995734176295034,1.,0.995734176295034,
1.,0.995734176295034,1.,0.995734176295034,1.,0.995734176295034,1.,0.995734176295034,
1.,0.995734176295034,1.,0.995734176295034,1.,0.995734176295034,1.,0.995734176295034,
1.,0.995734176295034,1.,0.995734176295034,1.,0.995734176295034,1.,0.995734176295034,
1.,0.995734176295034,1.,0.995734176295034,1.,0.995734176295034,1.,0.995734176295034,
1.,0.995734176295034,1.,0.995734176295034,1.,0.995734176295034,1.,0.995734176295034,
1.,0.995734176295034,1.,0.995734176295034,1.,0.995734176295034,1.,0.995734176295034,
1.,0.995734176295034,1.,0.995734176295034,1.,0.995734176295034,1.,0.995734176295034,
1.,0.995734176295034,1.,0.995734176295034,1.,0.995734176295034,1.,0.995734176295034,
1.,0.995734176295034,1.,0.995734176295034,1.,0.995734176295034,1.,0.995734176295034,
1.,0.995734176295034,1.,0.995734176295034,1.,0.995734176295034,1.,0.995734176295034,
1.,0.995734176295034,1.,0.995734176295034,1.,0.995734176295034,1.,0.995734176295034,
1.,0.995734176295034,1.,0.995734176295034,1.,0.995734176295034,1.,0.995734176295034,
1.,0.995734176295034,1.,0.995734176295034,1.,0.995734176295034,1.,0.995734176295034,
1.,0.995734176295034,1.,0.995734176295034,1.,0.995734176295034,1.,0.995734176295034,
1.,0.995734176295034,1.,0.995734176295034,1.,0.995734176295034,1.,0.995734176295034,
1.,0.995734176295034,1.,0.995734176295034,1.,0.995734176295034,1.,0.995734176295034,
1.,0.995734176295034,1.,0.995734176295034,1.,0.995734176295034,1.,0.995734176295034,
1.,0.995734176295034,1.,0.995734176295034,1.,0.995734176295034,1.,0.995734176295034,
1.,0.995734176295034,1.,0.995734176295034,1.,0.995734176295034,1.,0.995734176295034,
1.,0.995734176295034,1.,0.995734176295034,1.,0.995734176295034,1.,0.995734176295034,
1.,0.995734176295034,1.,0.995734176295034,1.,0.995734176295034,1.,0.995734176295034,
1.,0.995734176295034,1.,0.995734176295034,1.,0.995734176295034,1.,0.995734176295034,
1.,0.995734176295034,1.,0.995734176295034,1.,0.995734176295034,1.,0.995734176295034,
1.,0.995734176295034,1.,0.995734176295034,1.,0.995734176295034,1.,0.995734176295034,
1.,0.995734176295034,1.,0.995734176295034,1.,0.995734176295034,1.,0.995734176295034,
1.,0.995734176295034,1.,0.995734176295034,1.,0.995734176295034,1.,0.995734176295034,
1.,0.995734176295034,1.,0.995734176295034,1.,0.995734176295034,1.,0.995734176295034,
1.,0.995734176295034,1.,0.995734176295034,1.,0.995734176295034,1.,0.995734176295034,
1.,0.995734176295034,1.,0.995734176295034,1.,0.995734176295034,1.,0.995734176295034,
1.,0.995734176295034,1.,0.995734176295034,1.,0.995734176295034,1.,0.995734176295034,
1.,0.995734176295034,1.,0.995734176295034,1.,0.995734176295034,1.,0.995734176295034,
1.,0.995734176295034,1.,0.995734176295034,1.,0.995734176295034,1.,0.995734176295034,
1.,0.995734176295034,1.,0.995734176295034,1.,0.995734176295034,1.,0.995734176295034,
1.,0.995734176295034,1.,0.995734176295034,1.,0.995734176295034,1.,0.995734176295034,
1.,0.995734176295034,1.,0.995734176295034,1.,0.995734176295034,1.,0.995734176295034,
1.,0.997201362504481,0.998074874808405,0.998074874808405,0.998074874808405)))
REPRESENTATION_ITEM('')
SURFACE()
);
#4065=(
BOUNDED_CURVE()
B_SPLINE_CURVE(2,(#143197,#143198,#143199,#143200,#143201,#143202,#143203,
#143204,#143205,#143206,#143207,#143208,#143209,#143210,#143211,#143212,
#143213,#143214,#143215,#143216,#143217,#143218,#143219,#143220,#143221,
#143222,#143223,#143224,#143225,#143226,#143227,#143228,#143229,#143230,
#143231),.UNSPECIFIED.,.F.,.F.)
B_SPLINE_CURVE_WITH_KNOTS((3,2,2,2,2,2,2,2,2,2,2,2,2,2,2,2,2,3),(0.,0.000980392156862745,
0.00196078431372549,0.00294117647058824,0.00392156862745098,0.00490196078431373,
0.00588235294117647,0.00686274509803922,0.00784313725490196,0.00882352941176471,
0.00980392156862745,0.0107843137254902,0.0117647058823529,0.0127450980392157,
0.0137254901960784,0.0147058823529412,0.0156862745098039,0.0166666666666667),
 .UNSPECIFIED.)
CURVE()
GEOMETRIC_REPRESENTATION_ITEM()
RATIONAL_B_SPLINE_CURVE((1.,0.995734176295034,1.,0.995734176295034,1.,0.995734176295034,
1.,0.995734176295034,1.,0.995734176295034,1.,0.995734176295034,1.,0.995734176295034,
1.,0.995734176295034,1.,0.995734176295034,1.,0.995734176295034,1.,0.995734176295034,
1.,0.995734176295034,1.,0.995734176295034,1.,0.995734176295034,1.,0.995734176295034,
1.,0.995734176295034,1.,0.995734176295034,1.))
REPRESENTATION_ITEM('')
);
#4066=(
BOUNDED_CURVE()
B_SPLINE_CURVE(2,(#143234,#143235,#143236,#143237,#143238,#143239,#143240,
#143241,#143242,#143243,#143244,#143245,#143246,#143247,#143248,#143249,
#143250,#143251,#143252,#143253,#143254,#143255,#143256,#143257,#143258,
#143259,#143260,#143261,#143262,#143263,#143264,#143265,#143266,#143267,
#143268),.UNSPECIFIED.,.F.,.F.)
B_SPLINE_CURVE_WITH_KNOTS((3,2,2,2,2,2,2,2,2,2,2,2,2,2,2,2,2,3),(0.,0.000994375769093022,
0.00198875153818604,0.00298312730727906,0.00397750307637209,0.00497187884546511,
0.00596625461455813,0.00696063038365115,0.00795500615274417,0.00894938192183719,
0.00994375769093021,0.0109381334600232,0.0119325092291163,0.0129268849982093,
0.0139212607673023,0.0149156365363953,0.0159100123054883,0.0169043880745814),
 .UNSPECIFIED.)
CURVE()
GEOMETRIC_REPRESENTATION_ITEM()
RATIONAL_B_SPLINE_CURVE((1.,0.995734176295034,1.,0.995734176295034,1.,0.995734176295034,
1.,0.995734176295034,1.,0.995734176295034,1.,0.995734176295034,1.,0.995734176295034,
1.,0.995734176295034,1.,0.995734176295034,1.,0.995734176295034,1.,0.995734176295034,
1.,0.995734176295034,1.,0.995734176295034,1.,0.995734176295034,1.,0.995734176295034,
1.,0.995734176295034,1.,0.995734176295034,1.))
REPRESENTATION_ITEM('')
);
#4067=(
BOUNDED_CURVE()
B_SPLINE_CURVE(2,(#143273,#143274,#143275,#143276,#143277,#143278,#143279,
#143280,#143281,#143282,#143283,#143284,#143285,#143286,#143287,#143288,
#143289,#143290,#143291,#143292,#143293,#143294,#143295,#143296,#143297,
#143298,#143299,#143300,#143301,#143302,#143303,#143304,#143305,#143306,
#143307,#143308,#143309,#143310,#143311,#143312,#143313,#143314,#143315,
#143316,#143317,#143318,#143319,#143320,#143321,#143322,#143323,#143324,
#143325,#143326,#143327,#143328,#143329,#143330,#143331,#143332,#143333,
#143334,#143335,#143336,#143337,#143338,#143339,#143340,#143341),
 .UNSPECIFIED.,.F.,.F.)
B_SPLINE_CURVE_WITH_KNOTS((3,2,2,2,2,2,2,2,2,2,2,2,2,2,2,2,2,2,2,2,2,2,
2,2,2,2,2,2,2,2,2,2,2,2,3),(0.0166666666666667,0.0176470588235294,0.0186274509803922,
0.0196078431372549,0.0205882352941176,0.0215686274509804,0.0225490196078431,
0.0235294117647059,0.0245098039215686,0.0254901960784314,0.0264705882352941,
0.0274509803921569,0.0284313725490196,0.0294117647058824,0.0303921568627451,
0.0313725490196078,0.0323529411764706,0.0333333333333333,0.0343137254901961,
0.0352941176470588,0.0362745098039216,0.0372549019607843,0.0382352941176471,
0.0392156862745098,0.0401960784313726,0.0411764705882353,0.042156862745098,
0.0431372549019608,0.0441176470588235,0.0450980392156863,0.046078431372549,
0.0470588235294118,0.0480392156862745,0.0490196078431373,0.05),
 .UNSPECIFIED.)
CURVE()
GEOMETRIC_REPRESENTATION_ITEM()
RATIONAL_B_SPLINE_CURVE((1.,0.995734176295034,1.,0.995734176295034,1.,0.995734176295034,
1.,0.995734176295034,1.,0.995734176295034,1.,0.995734176295034,1.,0.995734176295034,
1.,0.995734176295034,1.,0.995734176295034,1.,0.995734176295034,1.,0.995734176295034,
1.,0.995734176295034,1.,0.995734176295034,1.,0.995734176295034,1.,0.995734176295034,
1.,0.995734176295034,1.,0.995734176295034,1.,0.995734176295034,1.,0.995734176295034,
1.,0.995734176295034,1.,0.995734176295034,1.,0.995734176295034,1.,0.995734176295034,
1.,0.995734176295034,1.,0.995734176295034,1.,0.995734176295034,1.,0.995734176295034,
1.,0.995734176295034,1.,0.995734176295034,1.,0.995734176295034,1.,0.995734176295034,
1.,0.995734176295034,1.,0.995734176295034,1.,0.995734176295034,1.))
REPRESENTATION_ITEM('')
);
#4068=(
BOUNDED_CURVE()
B_SPLINE_CURVE(2,(#143342,#143343,#143344,#143345,#143346,#143347,#143348,
#143349,#143350,#143351,#143352,#143353,#143354,#143355,#143356,#143357,
#143358,#143359,#143360,#143361,#143362,#143363,#143364,#143365,#143366,
#143367,#143368,#143369,#143370,#143371,#143372,#143373,#143374,#143375,
#143376,#143377,#143378,#143379,#143380,#143381,#143382,#143383,#143384,
#143385,#143386,#143387,#143388,#143389,#143390,#143391,#143392,#143393,
#143394,#143395,#143396,#143397,#143398,#143399,#143400,#143401,#143402,
#143403,#143404,#143405,#143406,#143407,#143408,#143409,#143410),
 .UNSPECIFIED.,.F.,.F.)
B_SPLINE_CURVE_WITH_KNOTS((3,2,2,2,2,2,2,2,2,2,2,2,2,2,2,2,2,2,2,2,2,2,
2,2,2,2,2,2,2,2,2,2,2,2,3),(0.0169043880745814,0.0178987638436744,0.0188931396127674,
0.0198875153818604,0.0208818911509534,0.0218762669200465,0.0228706426891395,
0.0238650184582325,0.0248593942273255,0.0258537699964186,0.0268481457655116,
0.0278425215346046,0.0288368973036976,0.0298312730727906,0.0308256488418837,
0.0318200246109767,0.0328144003800697,0.0338087761491627,0.0348031519182558,
0.0357975276873488,0.0367919034564418,0.0377862792255348,0.0387806549946278,
0.0397750307637209,0.0407694065328139,0.0417637823019069,0.0427581580709999,
0.0437525338400929,0.044746909609186,0.045741285378279,0.046735661147372,
0.047730036916465,0.048724412685558,0.0497187884546511,0.0507131642237441),
 .UNSPECIFIED.)
CURVE()
GEOMETRIC_REPRESENTATION_ITEM()
RATIONAL_B_SPLINE_CURVE((1.,0.995734176295034,1.,0.995734176295034,1.,0.995734176295034,
1.,0.995734176295034,1.,0.995734176295034,1.,0.995734176295034,1.,0.995734176295034,
1.,0.995734176295034,1.,0.995734176295034,1.,0.995734176295034,1.,0.995734176295034,
1.,0.995734176295034,1.,0.995734176295034,1.,0.995734176295034,1.,0.995734176295034,
1.,0.995734176295034,1.,0.995734176295034,1.,0.995734176295034,1.,0.995734176295034,
1.,0.995734176295034,1.,0.995734176295034,1.,0.995734176295034,1.,0.995734176295034,
1.,0.995734176295034,1.,0.995734176295034,1.,0.995734176295034,1.,0.995734176295034,
1.,0.995734176295034,1.,0.995734176295034,1.,0.995734176295034,1.,0.995734176295034,
1.,0.995734176295034,1.,0.995734176295034,1.,0.995734176295034,1.))
REPRESENTATION_ITEM('')
);
#4069=(
BOUNDED_CURVE()
B_SPLINE_CURVE(2,(#143415,#143416,#143417,#143418,#143419,#143420,#143421,
#143422,#143423,#143424,#143425,#143426,#143427,#143428,#143429,#143430,
#143431,#143432,#143433,#143434,#143435,#143436,#143437,#143438,#143439,
#143440,#143441,#143442,#143443,#143444,#143445,#143446,#143447,#143448,
#143449,#143450,#143451,#143452,#143453,#143454,#143455,#143456,#143457,
#143458,#143459,#143460,#143461,#143462,#143463,#143464,#143465,#143466,
#143467,#143468,#143469,#143470,#143471,#143472,#143473,#143474,#143475,
#143476,#143477,#143478,#143479,#143480,#143481,#143482,#143483),
 .UNSPECIFIED.,.F.,.F.)
B_SPLINE_CURVE_WITH_KNOTS((3,2,2,2,2,2,2,2,2,2,2,2,2,2,2,2,2,2,2,2,2,2,
2,2,2,2,2,2,2,2,2,2,2,2,3),(0.05,0.0509803921568627,0.0519607843137255,
0.0529411764705882,0.053921568627451,0.0549019607843137,0.0558823529411765,
0.0568627450980392,0.057843137254902,0.0588235294117647,0.0598039215686275,
0.0607843137254902,0.061764705882353,0.0627450980392157,0.0637254901960784,
0.0647058823529412,0.0656862745098039,0.0666666666666667,0.0676470588235294,
0.0686274509803922,0.0696078431372549,0.0705882352941176,0.0715686274509804,
0.0725490196078431,0.0735294117647059,0.0745098039215686,0.0754901960784314,
0.0764705882352941,0.0774509803921569,0.0784313725490196,0.0794117647058823,
0.0803921568627451,0.0813725490196078,0.0823529411764706,0.0833333333333333),
 .UNSPECIFIED.)
CURVE()
GEOMETRIC_REPRESENTATION_ITEM()
RATIONAL_B_SPLINE_CURVE((1.,0.995734176295034,1.,0.995734176295034,1.,0.995734176295034,
1.,0.995734176295034,1.,0.995734176295034,1.,0.995734176295034,1.,0.995734176295034,
1.,0.995734176295034,1.,0.995734176295034,1.,0.995734176295034,1.,0.995734176295034,
1.,0.995734176295034,1.,0.995734176295034,1.,0.995734176295034,1.,0.995734176295034,
1.,0.995734176295034,1.,0.995734176295034,1.,0.995734176295034,1.,0.995734176295034,
1.,0.995734176295034,1.,0.995734176295034,1.,0.995734176295034,1.,0.995734176295034,
1.,0.995734176295034,1.,0.995734176295034,1.,0.995734176295034,1.,0.995734176295034,
1.,0.995734176295034,1.,0.995734176295034,1.,0.995734176295034,1.,0.995734176295034,
1.,0.995734176295034,1.,0.995734176295034,1.,0.995734176295034,1.))
REPRESENTATION_ITEM('')
);
#4070=(
BOUNDED_CURVE()
B_SPLINE_CURVE(2,(#143484,#143485,#143486,#143487,#143488,#143489,#143490,
#143491,#143492,#143493,#143494,#143495,#143496,#143497,#143498,#143499,
#143500,#143501,#143502,#143503,#143504,#143505,#143506,#143507,#143508,
#143509,#143510,#143511,#143512,#143513,#143514,#143515,#143516,#143517,
#143518,#143519,#143520,#143521,#143522,#143523,#143524,#143525,#143526,
#143527,#143528,#143529,#143530,#143531,#143532,#143533,#143534,#143535,
#143536,#143537,#143538,#143539,#143540,#143541,#143542,#143543,#143544,
#143545,#143546,#143547,#143548,#143549,#143550,#143551,#143552),
 .UNSPECIFIED.,.F.,.F.)
B_SPLINE_CURVE_WITH_KNOTS((3,2,2,2,2,2,2,2,2,2,2,2,2,2,2,2,2,2,2,2,2,2,
2,2,2,2,2,2,2,2,2,2,2,2,3),(0.0507131642237441,0.0517075399928371,0.0527019157619301,
0.0536962915310232,0.0546906673001162,0.0556850430692092,0.0566794188383022,
0.0576737946073952,0.0586681703764883,0.0596625461455813,0.0606569219146743,
0.0616512976837673,0.0626456734528604,0.0636400492219534,0.0646344249910464,
0.0656288007601394,0.0666231765292324,0.0676175522983255,0.0686119280674185,
0.0696063038365115,0.0706006796056045,0.0715950553746975,0.0725894311437906,
0.0735838069128836,0.0745781826819766,0.0755725584510696,0.0765669342201626,
0.0775613099892557,0.0785556857583487,0.0795500615274417,0.0805444372965347,
0.0815388130656278,0.0825331888347208,0.0835275646038138,0.0845219403729068),
 .UNSPECIFIED.)
CURVE()
GEOMETRIC_REPRESENTATION_ITEM()
RATIONAL_B_SPLINE_CURVE((1.,0.995734176295034,1.,0.995734176295034,1.,0.995734176295034,
1.,0.995734176295034,1.,0.995734176295034,1.,0.995734176295034,1.,0.995734176295034,
1.,0.995734176295034,1.,0.995734176295034,1.,0.995734176295034,1.,0.995734176295034,
1.,0.995734176295034,1.,0.995734176295034,1.,0.995734176295034,1.,0.995734176295034,
1.,0.995734176295034,1.,0.995734176295034,1.,0.995734176295034,1.,0.995734176295034,
1.,0.995734176295034,1.,0.995734176295034,1.,0.995734176295034,1.,0.995734176295034,
1.,0.995734176295034,1.,0.995734176295034,1.,0.995734176295034,1.,0.995734176295034,
1.,0.995734176295034,1.,0.995734176295034,1.,0.995734176295034,1.,0.995734176295034,
1.,0.995734176295034,1.,0.995734176295034,1.,0.995734176295034,1.))
REPRESENTATION_ITEM('')
);
#4071=(
BOUNDED_CURVE()
B_SPLINE_CURVE(2,(#143557,#143558,#143559,#143560,#143561,#143562,#143563,
#143564,#143565,#143566,#143567,#143568,#143569,#143570,#143571,#143572,
#143573,#143574,#143575,#143576,#143577,#143578,#143579,#143580,#143581,
#143582,#143583,#143584,#143585,#143586,#143587,#143588,#143589,#143590,
#143591,#143592,#143593,#143594,#143595,#143596,#143597,#143598,#143599,
#143600,#143601,#143602,#143603,#143604,#143605,#143606,#143607,#143608,
#143609,#143610,#143611,#143612,#143613,#143614,#143615,#143616,#143617,
#143618,#143619,#143620,#143621,#143622,#143623,#143624,#143625),
 .UNSPECIFIED.,.F.,.F.)
B_SPLINE_CURVE_WITH_KNOTS((3,2,2,2,2,2,2,2,2,2,2,2,2,2,2,2,2,2,2,2,2,2,
2,2,2,2,2,2,2,2,2,2,2,2,3),(0.0833333333333333,0.0843137254901961,0.0852941176470588,
0.0862745098039216,0.0872549019607843,0.0882352941176471,0.0892156862745098,
0.0901960784313725,0.0911764705882353,0.092156862745098,0.0931372549019608,
0.0941176470588235,0.0950980392156863,0.096078431372549,0.0970588235294118,
0.0980392156862745,0.0990196078431373,0.1,0.100980392156863,0.101960784313725,
0.102941176470588,0.103921568627451,0.104901960784314,0.105882352941176,
0.106862745098039,0.107843137254902,0.108823529411765,0.109803921568627,
0.11078431372549,0.111764705882353,0.112745098039216,0.113725490196078,
0.114705882352941,0.115686274509804,0.116666666666667),.UNSPECIFIED.)
CURVE()
GEOMETRIC_REPRESENTATION_ITEM()
RATIONAL_B_SPLINE_CURVE((1.,0.995734176295034,1.,0.995734176295034,1.,0.995734176295034,
1.,0.995734176295034,1.,0.995734176295034,1.,0.995734176295034,1.,0.995734176295034,
1.,0.995734176295034,1.,0.995734176295034,1.,0.995734176295034,1.,0.995734176295034,
1.,0.995734176295034,1.,0.995734176295034,1.,0.995734176295034,1.,0.995734176295034,
1.,0.995734176295034,1.,0.995734176295034,1.,0.995734176295034,1.,0.995734176295034,
1.,0.995734176295034,1.,0.995734176295034,1.,0.995734176295034,1.,0.995734176295034,
1.,0.995734176295034,1.,0.995734176295034,1.,0.995734176295034,1.,0.995734176295034,
1.,0.995734176295034,1.,0.995734176295034,1.,0.995734176295034,1.,0.995734176295034,
1.,0.995734176295034,1.,0.995734176295034,1.,0.995734176295034,1.))
REPRESENTATION_ITEM('')
);
#4072=(
BOUNDED_CURVE()
B_SPLINE_CURVE(2,(#143626,#143627,#143628,#143629,#143630,#143631,#143632,
#143633,#143634,#143635,#143636,#143637,#143638,#143639,#143640,#143641,
#143642,#143643,#143644,#143645,#143646,#143647,#143648,#143649,#143650,
#143651,#143652,#143653,#143654,#143655,#143656,#143657,#143658,#143659,
#143660,#143661,#143662,#143663,#143664,#143665,#143666,#143667,#143668,
#143669,#143670,#143671,#143672,#143673,#143674,#143675,#143676,#143677,
#143678,#143679,#143680,#143681,#143682,#143683,#143684,#143685,#143686,
#143687,#143688,#143689,#143690,#143691,#143692,#143693,#143694),
 .UNSPECIFIED.,.F.,.F.)
B_SPLINE_CURVE_WITH_KNOTS((3,2,2,2,2,2,2,2,2,2,2,2,2,2,2,2,2,2,2,2,2,2,
2,2,2,2,2,2,2,2,2,2,2,2,3),(0.0845219403729068,0.0855163161419998,0.0865106919110929,
0.0875050676801859,0.0884994434492789,0.0894938192183719,0.090488194987465,
0.091482570756558,0.092476946525651,0.093471322294744,0.094465698063837,
0.0954600738329301,0.0964544496020231,0.0974488253711161,0.0984432011402091,
0.0994375769093021,0.100431952678395,0.101426328447488,0.102420704216581,
0.103415079985674,0.104409455754767,0.10540383152386,0.106398207292953,
0.107392583062046,0.108386958831139,0.109381334600232,0.110375710369325,
0.111370086138418,0.112364461907511,0.113358837676604,0.114353213445697,
0.11534758921479,0.116341964983883,0.117336340752977,0.11833071652207),
 .UNSPECIFIED.)
CURVE()
GEOMETRIC_REPRESENTATION_ITEM()
RATIONAL_B_SPLINE_CURVE((1.,0.995734176295034,1.,0.995734176295034,1.,0.995734176295034,
1.,0.995734176295034,1.,0.995734176295034,1.,0.995734176295034,1.,0.995734176295034,
1.,0.995734176295034,1.,0.995734176295034,1.,0.995734176295034,1.,0.995734176295034,
1.,0.995734176295034,1.,0.995734176295034,1.,0.995734176295034,1.,0.995734176295034,
1.,0.995734176295034,1.,0.995734176295034,1.,0.995734176295034,1.,0.995734176295034,
1.,0.995734176295034,1.,0.995734176295034,1.,0.995734176295034,1.,0.995734176295034,
1.,0.995734176295034,1.,0.995734176295034,1.,0.995734176295034,1.,0.995734176295034,
1.,0.995734176295034,1.,0.995734176295034,1.,0.995734176295034,1.,0.995734176295034,
1.,0.995734176295034,1.,0.995734176295034,1.,0.995734176295034,1.))
REPRESENTATION_ITEM('')
);
#4073=(
BOUNDED_CURVE()
B_SPLINE_CURVE(2,(#143699,#143700,#143701,#143702,#143703,#143704,#143705,
#143706,#143707,#143708,#143709,#143710,#143711,#143712,#143713,#143714,
#143715,#143716,#143717,#143718,#143719,#143720,#143721,#143722,#143723,
#143724,#143725,#143726,#143727,#143728,#143729,#143730,#143731,#143732,
#143733,#143734,#143735,#143736,#143737,#143738,#143739,#143740,#143741,
#143742,#143743,#143744,#143745,#143746,#143747,#143748,#143749,#143750,
#143751,#143752,#143753,#143754,#143755,#143756,#143757,#143758,#143759,
#143760,#143761,#143762,#143763,#143764,#143765,#143766,#143767),
 .UNSPECIFIED.,.F.,.F.)
B_SPLINE_CURVE_WITH_KNOTS((3,2,2,2,2,2,2,2,2,2,2,2,2,2,2,2,2,2,2,2,2,2,
2,2,2,2,2,2,2,2,2,2,2,2,3),(0.116666666666667,0.117647058823529,0.118627450980392,
0.119607843137255,0.120588235294118,0.12156862745098,0.122549019607843,
0.123529411764706,0.124509803921569,0.125490196078431,0.126470588235294,
0.127450980392157,0.12843137254902,0.129411764705882,0.130392156862745,
0.131372549019608,0.132352941176471,0.133333333333333,0.134313725490196,
0.135294117647059,0.136274509803922,0.137254901960784,0.138235294117647,
0.13921568627451,0.140196078431373,0.141176470588235,0.142156862745098,
0.143137254901961,0.144117647058824,0.145098039215686,0.146078431372549,
0.147058823529412,0.148039215686275,0.149019607843137,0.15),
 .UNSPECIFIED.)
CURVE()
GEOMETRIC_REPRESENTATION_ITEM()
RATIONAL_B_SPLINE_CURVE((1.,0.995734176295034,1.,0.995734176295034,1.,0.995734176295034,
1.,0.995734176295034,1.,0.995734176295034,1.,0.995734176295034,1.,0.995734176295034,
1.,0.995734176295034,1.,0.995734176295034,1.,0.995734176295034,1.,0.995734176295034,
1.,0.995734176295034,1.,0.995734176295034,1.,0.995734176295034,1.,0.995734176295034,
1.,0.995734176295034,1.,0.995734176295034,1.,0.995734176295034,1.,0.995734176295034,
1.,0.995734176295034,1.,0.995734176295034,1.,0.995734176295034,1.,0.995734176295034,
1.,0.995734176295034,1.,0.995734176295034,1.,0.995734176295034,1.,0.995734176295034,
1.,0.995734176295034,1.,0.995734176295034,1.,0.995734176295034,1.,0.995734176295034,
1.,0.995734176295034,1.,0.995734176295034,1.,0.995734176295034,1.))
REPRESENTATION_ITEM('')
);
#4074=(
BOUNDED_CURVE()
B_SPLINE_CURVE(2,(#143768,#143769,#143770,#143771,#143772,#143773,#143774,
#143775,#143776,#143777,#143778,#143779,#143780,#143781,#143782,#143783,
#143784,#143785,#143786,#143787,#143788,#143789,#143790,#143791,#143792,
#143793,#143794,#143795,#143796,#143797,#143798,#143799,#143800,#143801,
#143802,#143803,#143804,#143805,#143806,#143807,#143808,#143809,#143810,
#143811,#143812,#143813,#143814,#143815,#143816,#143817,#143818,#143819,
#143820,#143821,#143822,#143823,#143824,#143825,#143826,#143827,#143828,
#143829,#143830,#143831,#143832,#143833,#143834,#143835,#143836),
 .UNSPECIFIED.,.F.,.F.)
B_SPLINE_CURVE_WITH_KNOTS((3,2,2,2,2,2,2,2,2,2,2,2,2,2,2,2,2,2,2,2,2,2,
2,2,2,2,2,2,2,2,2,2,2,2,3),(0.11833071652207,0.119325092291163,0.120319468060256,
0.121313843829349,0.122308219598442,0.123302595367535,0.124296971136628,
0.125291346905721,0.126285722674814,0.127280098443907,0.128274474213,0.129268849982093,
0.130263225751186,0.131257601520279,0.132251977289372,0.133246353058465,
0.134240728827558,0.135235104596651,0.136229480365744,0.137223856134837,
0.13821823190393,0.139212607673023,0.140206983442116,0.141201359211209,
0.142195734980302,0.143190110749395,0.144184486518488,0.145178862287581,
0.146173238056674,0.147167613825767,0.14816198959486,0.149156365363953,
0.150150741133046,0.151145116902139,0.152139492671232),.UNSPECIFIED.)
CURVE()
GEOMETRIC_REPRESENTATION_ITEM()
RATIONAL_B_SPLINE_CURVE((1.,0.995734176295034,1.,0.995734176295034,1.,0.995734176295034,
1.,0.995734176295034,1.,0.995734176295034,1.,0.995734176295034,1.,0.995734176295034,
1.,0.995734176295034,1.,0.995734176295034,1.,0.995734176295034,1.,0.995734176295034,
1.,0.995734176295034,1.,0.995734176295034,1.,0.995734176295034,1.,0.995734176295034,
1.,0.995734176295034,1.,0.995734176295034,1.,0.995734176295034,1.,0.995734176295034,
1.,0.995734176295034,1.,0.995734176295034,1.,0.995734176295034,1.,0.995734176295034,
1.,0.995734176295034,1.,0.995734176295034,1.,0.995734176295034,1.,0.995734176295034,
1.,0.995734176295034,1.,0.995734176295034,1.,0.995734176295034,1.,0.995734176295034,
1.,0.995734176295034,1.,0.995734176295034,1.,0.995734176295034,1.))
REPRESENTATION_ITEM('')
);
#4075=(
BOUNDED_CURVE()
B_SPLINE_CURVE(2,(#143841,#143842,#143843,#143844,#143845,#143846,#143847,
#143848,#143849,#143850,#143851,#143852,#143853,#143854,#143855,#143856,
#143857,#143858,#143859,#143860,#143861,#143862,#143863,#143864,#143865,
#143866,#143867,#143868,#143869,#143870,#143871,#143872,#143873,#143874,
#143875,#143876,#143877,#143878,#143879,#143880,#143881,#143882,#143883,
#143884,#143885,#143886,#143887,#143888,#143889,#143890,#143891,#143892,
#143893,#143894,#143895,#143896,#143897,#143898,#143899,#143900,#143901,
#143902,#143903,#143904,#143905,#143906,#143907,#143908,#143909),
 .UNSPECIFIED.,.F.,.F.)
B_SPLINE_CURVE_WITH_KNOTS((3,2,2,2,2,2,2,2,2,2,2,2,2,2,2,2,2,2,2,2,2,2,
2,2,2,2,2,2,2,2,2,2,2,2,3),(0.15,0.150980392156863,0.151960784313725,0.152941176470588,
0.153921568627451,0.154901960784314,0.155882352941176,0.156862745098039,
0.157843137254902,0.158823529411765,0.159803921568627,0.16078431372549,
0.161764705882353,0.162745098039216,0.163725490196078,0.164705882352941,
0.165686274509804,0.166666666666667,0.167647058823529,0.168627450980392,
0.169607843137255,0.170588235294118,0.17156862745098,0.172549019607843,
0.173529411764706,0.174509803921569,0.175490196078431,0.176470588235294,
0.177450980392157,0.17843137254902,0.179411764705882,0.180392156862745,
0.181372549019608,0.182352941176471,0.183333333333333),.UNSPECIFIED.)
CURVE()
GEOMETRIC_REPRESENTATION_ITEM()
RATIONAL_B_SPLINE_CURVE((1.,0.995734176295034,1.,0.995734176295034,1.,0.995734176295034,
1.,0.995734176295034,1.,0.995734176295034,1.,0.995734176295034,1.,0.995734176295034,
1.,0.995734176295034,1.,0.995734176295034,1.,0.995734176295034,1.,0.995734176295034,
1.,0.995734176295034,1.,0.995734176295034,1.,0.995734176295034,1.,0.995734176295034,
1.,0.995734176295034,1.,0.995734176295034,1.,0.995734176295034,1.,0.995734176295034,
1.,0.995734176295034,1.,0.995734176295034,1.,0.995734176295034,1.,0.995734176295034,
1.,0.995734176295034,1.,0.995734176295034,1.,0.995734176295034,1.,0.995734176295034,
1.,0.995734176295034,1.,0.995734176295034,1.,0.995734176295034,1.,0.995734176295034,
1.,0.995734176295034,1.,0.995734176295034,1.,0.995734176295034,1.))
REPRESENTATION_ITEM('')
);
#4076=(
BOUNDED_CURVE()
B_SPLINE_CURVE(2,(#143910,#143911,#143912,#143913,#143914,#143915,#143916,
#143917,#143918,#143919,#143920,#143921,#143922,#143923,#143924,#143925,
#143926,#143927,#143928,#143929,#143930,#143931,#143932,#143933,#143934,
#143935,#143936,#143937,#143938,#143939,#143940,#143941,#143942,#143943,
#143944,#143945,#143946,#143947,#143948,#143949,#143950,#143951,#143952,
#143953,#143954,#143955,#143956,#143957,#143958,#143959,#143960,#143961,
#143962,#143963,#143964,#143965,#143966,#143967,#143968,#143969,#143970,
#143971,#143972,#143973,#143974,#143975,#143976,#143977,#143978),
 .UNSPECIFIED.,.F.,.F.)
B_SPLINE_CURVE_WITH_KNOTS((3,2,2,2,2,2,2,2,2,2,2,2,2,2,2,2,2,2,2,2,2,2,
2,2,2,2,2,2,2,2,2,2,2,2,3),(0.152139492671232,0.153133868440325,0.154128244209418,
0.155122619978511,0.156116995747604,0.157111371516697,0.15810574728579,
0.159100123054883,0.160094498823976,0.161088874593069,0.162083250362162,
0.163077626131256,0.164072001900349,0.165066377669442,0.166060753438535,
0.167055129207628,0.168049504976721,0.169043880745814,0.170038256514907,
0.171032632284,0.172027008053093,0.173021383822186,0.174015759591279,0.175010135360372,
0.176004511129465,0.176998886898558,0.177993262667651,0.178987638436744,
0.179982014205837,0.18097638997493,0.181970765744023,0.182965141513116,
0.183959517282209,0.184953893051302,0.185948268820395),.UNSPECIFIED.)
CURVE()
GEOMETRIC_REPRESENTATION_ITEM()
RATIONAL_B_SPLINE_CURVE((1.,0.995734176295034,1.,0.995734176295034,1.,0.995734176295034,
1.,0.995734176295034,1.,0.995734176295034,1.,0.995734176295034,1.,0.995734176295034,
1.,0.995734176295034,1.,0.995734176295034,1.,0.995734176295034,1.,0.995734176295034,
1.,0.995734176295034,1.,0.995734176295034,1.,0.995734176295034,1.,0.995734176295034,
1.,0.995734176295034,1.,0.995734176295034,1.,0.995734176295034,1.,0.995734176295034,
1.,0.995734176295034,1.,0.995734176295034,1.,0.995734176295034,1.,0.995734176295034,
1.,0.995734176295034,1.,0.995734176295034,1.,0.995734176295034,1.,0.995734176295034,
1.,0.995734176295034,1.,0.995734176295034,1.,0.995734176295034,1.,0.995734176295034,
1.,0.995734176295034,1.,0.995734176295034,1.,0.995734176295034,1.))
REPRESENTATION_ITEM('')
);
#4077=(
BOUNDED_CURVE()
B_SPLINE_CURVE(2,(#143983,#143984,#143985,#143986,#143987,#143988,#143989,
#143990,#143991,#143992,#143993,#143994,#143995,#143996,#143997,#143998,
#143999,#144000,#144001,#144002,#144003,#144004,#144005,#144006,#144007,
#144008,#144009,#144010,#144011,#144012,#144013,#144014,#144015,#144016,
#144017,#144018,#144019,#144020,#144021,#144022,#144023,#144024,#144025,
#144026,#144027,#144028,#144029,#144030,#144031,#144032,#144033,#144034,
#144035,#144036,#144037,#144038,#144039,#144040,#144041,#144042,#144043,
#144044,#144045,#144046,#144047,#144048,#144049,#144050,#144051),
 .UNSPECIFIED.,.F.,.F.)
B_SPLINE_CURVE_WITH_KNOTS((3,2,2,2,2,2,2,2,2,2,2,2,2,2,2,2,2,2,2,2,2,2,
2,2,2,2,2,2,2,2,2,2,2,2,3),(0.183333333333333,0.184313725490196,0.185294117647059,
0.186274509803922,0.187254901960784,0.188235294117647,0.18921568627451,
0.190196078431373,0.191176470588235,0.192156862745098,0.193137254901961,
0.194117647058824,0.195098039215686,0.196078431372549,0.197058823529412,
0.198039215686275,0.199019607843137,0.2,0.200980392156863,0.201960784313725,
0.202941176470588,0.203921568627451,0.204901960784314,0.205882352941176,
0.206862745098039,0.207843137254902,0.208823529411765,0.209803921568627,
0.21078431372549,0.211764705882353,0.212745098039216,0.213725490196078,
0.214705882352941,0.215686274509804,0.216666666666667),.UNSPECIFIED.)
CURVE()
GEOMETRIC_REPRESENTATION_ITEM()
RATIONAL_B_SPLINE_CURVE((1.,0.995734176295034,1.,0.995734176295034,1.,0.995734176295034,
1.,0.995734176295034,1.,0.995734176295034,1.,0.995734176295034,1.,0.995734176295034,
1.,0.995734176295034,1.,0.995734176295034,1.,0.995734176295034,1.,0.995734176295034,
1.,0.995734176295034,1.,0.995734176295034,1.,0.995734176295034,1.,0.995734176295034,
1.,0.995734176295034,1.,0.995734176295034,1.,0.995734176295034,1.,0.995734176295034,
1.,0.995734176295034,1.,0.995734176295034,1.,0.995734176295034,1.,0.995734176295034,
1.,0.995734176295034,1.,0.995734176295034,1.,0.995734176295034,1.,0.995734176295034,
1.,0.995734176295034,1.,0.995734176295034,1.,0.995734176295034,1.,0.995734176295034,
1.,0.995734176295034,1.,0.995734176295034,1.,0.995734176295034,1.))
REPRESENTATION_ITEM('')
);
#4078=(
BOUNDED_CURVE()
B_SPLINE_CURVE(2,(#144052,#144053,#144054,#144055,#144056,#144057,#144058,
#144059,#144060,#144061,#144062,#144063,#144064,#144065,#144066,#144067,
#144068,#144069,#144070,#144071,#144072,#144073,#144074,#144075,#144076,
#144077,#144078,#144079,#144080,#144081,#144082,#144083,#144084,#144085,
#144086,#144087,#144088,#144089,#144090,#144091,#144092,#144093,#144094,
#144095,#144096,#144097,#144098,#144099,#144100,#144101,#144102,#144103,
#144104,#144105,#144106,#144107,#144108,#144109,#144110,#144111,#144112,
#144113,#144114,#144115,#144116,#144117,#144118,#144119,#144120),
 .UNSPECIFIED.,.F.,.F.)
B_SPLINE_CURVE_WITH_KNOTS((3,2,2,2,2,2,2,2,2,2,2,2,2,2,2,2,2,2,2,2,2,2,
2,2,2,2,2,2,2,2,2,2,2,2,3),(0.185948268820395,0.186942644589488,0.187937020358581,
0.188931396127674,0.189925771896767,0.19092014766586,0.191914523434953,
0.192908899204046,0.193903274973139,0.194897650742232,0.195892026511325,
0.196886402280418,0.197880778049511,0.198875153818604,0.199869529587697,
0.20086390535679,0.201858281125883,0.202852656894976,0.203847032664069,
0.204841408433162,0.205835784202255,0.206830159971348,0.207824535740441,
0.208818911509534,0.209813287278627,0.210807663047721,0.211802038816814,
0.212796414585907,0.213790790355,0.214785166124093,0.215779541893186,0.216773917662279,
0.217768293431372,0.218762669200465,0.219757044969558),.UNSPECIFIED.)
CURVE()
GEOMETRIC_REPRESENTATION_ITEM()
RATIONAL_B_SPLINE_CURVE((1.,0.995734176295034,1.,0.995734176295034,1.,0.995734176295034,
1.,0.995734176295034,1.,0.995734176295034,1.,0.995734176295034,1.,0.995734176295034,
1.,0.995734176295034,1.,0.995734176295034,1.,0.995734176295034,1.,0.995734176295034,
1.,0.995734176295034,1.,0.995734176295034,1.,0.995734176295034,1.,0.995734176295034,
1.,0.995734176295034,1.,0.995734176295034,1.,0.995734176295034,1.,0.995734176295034,
1.,0.995734176295034,1.,0.995734176295034,1.,0.995734176295034,1.,0.995734176295034,
1.,0.995734176295034,1.,0.995734176295034,1.,0.995734176295034,1.,0.995734176295034,
1.,0.995734176295034,1.,0.995734176295034,1.,0.995734176295034,1.,0.995734176295034,
1.,0.995734176295034,1.,0.995734176295034,1.,0.995734176295034,1.))
REPRESENTATION_ITEM('')
);
#4079=(
BOUNDED_CURVE()
B_SPLINE_CURVE(2,(#144125,#144126,#144127,#144128,#144129,#144130,#144131,
#144132,#144133,#144134,#144135,#144136,#144137,#144138,#144139,#144140,
#144141,#144142,#144143,#144144,#144145,#144146,#144147,#144148,#144149,
#144150,#144151,#144152,#144153,#144154,#144155,#144156,#144157,#144158,
#144159,#144160,#144161,#144162,#144163,#144164,#144165,#144166,#144167,
#144168,#144169,#144170,#144171,#144172,#144173,#144174,#144175,#144176,
#144177,#144178,#144179,#144180,#144181,#144182,#144183,#144184,#144185,
#144186,#144187,#144188,#144189,#144190,#144191,#144192,#144193),
 .UNSPECIFIED.,.F.,.F.)
B_SPLINE_CURVE_WITH_KNOTS((3,2,2,2,2,2,2,2,2,2,2,2,2,2,2,2,2,2,2,2,2,2,
2,2,2,2,2,2,2,2,2,2,2,2,3),(0.216666666666667,0.217647058823529,0.218627450980392,
0.219607843137255,0.220588235294118,0.22156862745098,0.222549019607843,
0.223529411764706,0.224509803921569,0.225490196078431,0.226470588235294,
0.227450980392157,0.22843137254902,0.229411764705882,0.230392156862745,
0.231372549019608,0.232352941176471,0.233333333333333,0.234313725490196,
0.235294117647059,0.236274509803922,0.237254901960784,0.238235294117647,
0.23921568627451,0.240196078431373,0.241176470588235,0.242156862745098,
0.243137254901961,0.244117647058824,0.245098039215686,0.246078431372549,
0.247058823529412,0.248039215686275,0.249019607843137,0.25),
 .UNSPECIFIED.)
CURVE()
GEOMETRIC_REPRESENTATION_ITEM()
RATIONAL_B_SPLINE_CURVE((1.,0.995734176295034,1.,0.995734176295034,1.,0.995734176295034,
1.,0.995734176295034,1.,0.995734176295034,1.,0.995734176295034,1.,0.995734176295034,
1.,0.995734176295034,1.,0.995734176295034,1.,0.995734176295034,1.,0.995734176295034,
1.,0.995734176295034,1.,0.995734176295034,1.,0.995734176295034,1.,0.995734176295034,
1.,0.995734176295034,1.,0.995734176295034,1.,0.995734176295034,1.,0.995734176295034,
1.,0.995734176295034,1.,0.995734176295034,1.,0.995734176295034,1.,0.995734176295034,
1.,0.995734176295034,1.,0.995734176295034,1.,0.995734176295034,1.,0.995734176295034,
1.,0.995734176295034,1.,0.995734176295034,1.,0.995734176295034,1.,0.995734176295034,
1.,0.995734176295034,1.,0.995734176295034,1.,0.995734176295034,1.))
REPRESENTATION_ITEM('')
);
#4080=(
BOUNDED_CURVE()
B_SPLINE_CURVE(2,(#144194,#144195,#144196,#144197,#144198,#144199,#144200,
#144201,#144202,#144203,#144204,#144205,#144206,#144207,#144208,#144209,
#144210,#144211,#144212,#144213,#144214,#144215,#144216,#144217,#144218,
#144219,#144220,#144221,#144222,#144223,#144224,#144225,#144226,#144227,
#144228,#144229,#144230,#144231,#144232,#144233,#144234,#144235,#144236,
#144237,#144238,#144239,#144240,#144241,#144242,#144243,#144244,#144245,
#144246,#144247,#144248,#144249,#144250,#144251,#144252,#144253,#144254,
#144255,#144256,#144257,#144258,#144259,#144260,#144261,#144262),
 .UNSPECIFIED.,.F.,.F.)
B_SPLINE_CURVE_WITH_KNOTS((3,2,2,2,2,2,2,2,2,2,2,2,2,2,2,2,2,2,2,2,2,2,
2,2,2,2,2,2,2,2,2,2,2,2,3),(0.219757044969558,0.220751420738651,0.221745796507744,
0.222740172276837,0.22373454804593,0.224728923815023,0.225723299584116,
0.226717675353209,0.227712051122302,0.228706426891395,0.229700802660488,
0.230695178429581,0.231689554198674,0.232683929967767,0.23367830573686,
0.234672681505953,0.235667057275046,0.236661433044139,0.237655808813232,
0.238650184582325,0.239644560351418,0.240638936120511,0.241633311889604,
0.242627687658697,0.24362206342779,0.244616439196883,0.245610814965976,
0.246605190735069,0.247599566504162,0.248593942273255,0.249588318042348,
0.250582693811441,0.251577069580534,0.252571445349627,0.25356582111872),
 .UNSPECIFIED.)
CURVE()
GEOMETRIC_REPRESENTATION_ITEM()
RATIONAL_B_SPLINE_CURVE((1.,0.995734176295034,1.,0.995734176295034,1.,0.995734176295034,
1.,0.995734176295034,1.,0.995734176295034,1.,0.995734176295034,1.,0.995734176295034,
1.,0.995734176295034,1.,0.995734176295034,1.,0.995734176295034,1.,0.995734176295034,
1.,0.995734176295034,1.,0.995734176295034,1.,0.995734176295034,1.,0.995734176295034,
1.,0.995734176295034,1.,0.995734176295034,1.,0.995734176295034,1.,0.995734176295034,
1.,0.995734176295034,1.,0.995734176295034,1.,0.995734176295034,1.,0.995734176295034,
1.,0.995734176295034,1.,0.995734176295034,1.,0.995734176295034,1.,0.995734176295034,
1.,0.995734176295034,1.,0.995734176295034,1.,0.995734176295034,1.,0.995734176295034,
1.,0.995734176295034,1.,0.995734176295034,1.,0.995734176295034,1.))
REPRESENTATION_ITEM('')
);
#4081=(
BOUNDED_CURVE()
B_SPLINE_CURVE(2,(#149844,#149845,#149846,#149847,#149848,#149849,#149850,
#149851,#149852,#149853,#149854,#149855,#149856,#149857,#149858,#149859,
#149860,#149861,#149862,#149863,#149864,#149865,#149866,#149867,#149868,
#149869,#149870,#149871,#149872,#149873,#149874,#149875,#149876,#149877,
#149878,#149879,#149880,#149881,#149882,#149883,#149884,#149885,#149886,
#149887,#149888,#149889,#149890,#149891,#149892,#149893,#149894,#149895,
#149896,#149897,#149898,#149899,#149900,#149901,#149902,#149903,#149904,
#149905,#149906,#149907,#149908,#149909,#149910,#149911,#149912,#149913,
#149914,#149915,#149916,#149917,#149918,#149919,#149920,#149921,#149922,
#149923,#149924,#149925,#149926,#149927,#149928,#149929,#149930,#149931,
#149932,#149933,#149934,#149935,#149936,#149937,#149938,#149939,#149940,
#149941,#149942,#149943,#149944,#149945,#149946,#149947,#149948,#149949,
#149950,#149951,#149952,#149953,#149954,#149955,#149956,#149957,#149958,
#149959,#149960,#149961,#149962,#149963,#149964,#149965,#149966,#149967,
#149968,#149969,#149970,#149971,#149972,#149973,#149974,#149975,#149976,
#149977,#149978,#149979,#149980,#149981,#149982,#149983,#149984,#149985,
#149986,#149987,#149988,#149989,#149990,#149991,#149992,#149993,#149994,
#149995,#149996,#149997,#149998,#149999,#150000,#150001,#150002,#150003,
#150004,#150005,#150006,#150007,#150008,#150009,#150010,#150011,#150012,
#150013,#150014,#150015,#150016,#150017,#150018,#150019,#150020,#150021,
#150022,#150023,#150024,#150025,#150026,#150027,#150028,#150029,#150030,
#150031,#150032,#150033,#150034,#150035,#150036,#150037,#150038,#150039,
#150040,#150041,#150042,#150043,#150044,#150045,#150046,#150047,#150048,
#150049,#150050,#150051,#150052,#150053,#150054,#150055,#150056,#150057,
#150058,#150059,#150060,#150061,#150062,#150063,#150064,#150065,#150066,
#150067,#150068,#150069,#150070,#150071,#150072,#150073,#150074,#150075,
#150076,#150077,#150078,#150079,#150080,#150081,#150082,#150083,#150084,
#150085,#150086,#150087,#150088,#150089,#150090,#150091,#150092,#150093,
#150094,#150095,#150096,#150097,#150098,#150099,#150100,#150101,#150102,
#150103,#150104,#150105,#150106,#150107,#150108,#150109,#150110,#150111,
#150112,#150113,#150114,#150115,#150116,#150117,#150118,#150119,#150120,
#150121,#150122,#150123,#150124,#150125,#150126,#150127,#150128,#150129,
#150130,#150131,#150132,#150133,#150134,#150135,#150136,#150137,#150138,
#150139,#150140,#150141,#150142,#150143,#150144,#150145,#150146,#150147,
#150148,#150149,#150150,#150151,#150152,#150153,#150154,#150155,#150156,
#150157,#150158,#150159,#150160,#150161,#150162,#150163,#150164,#150165,
#150166,#150167,#150168,#150169,#150170,#150171,#150172,#150173,#150174,
#150175,#150176,#150177,#150178,#150179,#150180,#150181,#150182,#150183,
#150184,#150185,#150186,#150187,#150188,#150189,#150190,#150191,#150192,
#150193,#150194,#150195,#150196,#150197,#150198,#150199,#150200,#150201,
#150202,#150203,#150204,#150205,#150206,#150207,#150208,#150209,#150210,
#150211,#150212,#150213,#150214,#150215,#150216,#150217,#150218,#150219,
#150220,#150221,#150222,#150223,#150224,#150225,#150226,#150227,#150228,
#150229,#150230,#150231,#150232,#150233,#150234,#150235,#150236,#150237,
#150238,#150239,#150240,#150241,#150242,#150243,#150244,#150245,#150246,
#150247,#150248,#150249,#150250,#150251,#150252,#150253,#150254,#150255,
#150256,#150257,#150258,#150259,#150260,#150261,#150262,#150263,#150264,
#150265,#150266,#150267,#150268,#150269,#150270,#150271,#150272,#150273,
#150274,#150275,#150276,#150277,#150278,#150279,#150280,#150281,#150282,
#150283,#150284,#150285,#150286,#150287,#150288,#150289,#150290,#150291,
#150292,#150293,#150294,#150295,#150296,#150297,#150298,#150299,#150300,
#150301,#150302,#150303,#150304,#150305,#150306,#150307,#150308,#150309,
#150310,#150311,#150312,#150313,#150314,#150315,#150316,#150317,#150318,
#150319,#150320,#150321,#150322,#150323,#150324,#150325,#150326,#150327,
#150328,#150329,#150330,#150331,#150332,#150333,#150334,#150335,#150336,
#150337,#150338,#150339,#150340,#150341,#150342,#150343,#150344,#150345,
#150346,#150347,#150348,#150349,#150350,#150351,#150352,#150353,#150354,
#150355,#150356,#150357,#150358,#150359,#150360,#150361,#150362,#150363,
#150364,#150365,#150366,#150367,#150368,#150369,#150370,#150371,#150372,
#150373,#150374,#150375,#150376,#150377,#150378,#150379,#150380,#150381,
#150382,#150383,#150384,#150385,#150386),.UNSPECIFIED.,.F.,.F.)
B_SPLINE_CURVE_WITH_KNOTS((3,2,2,2,2,2,2,2,2,2,2,2,2,2,2,2,2,2,2,2,2,2,
2,2,2,2,2,2,2,2,2,2,2,2,2,2,2,2,2,2,2,2,2,2,2,2,2,2,2,2,2,2,2,2,2,2,2,2,
2,2,2,2,2,2,2,2,2,2,2,2,2,2,2,2,2,2,2,2,2,2,2,2,2,2,2,2,2,2,2,2,2,2,2,2,
2,2,2,2,2,2,2,2,2,2,2,2,2,2,2,2,2,2,2,2,2,2,2,2,2,2,2,2,2,2,2,2,2,2,2,2,
2,2,2,2,2,2,2,2,2,2,2,2,2,2,2,2,2,2,2,2,2,2,2,2,2,2,2,2,2,2,2,2,2,2,2,2,
2,2,2,2,2,2,2,2,2,2,2,2,2,2,2,2,2,2,2,2,2,2,2,2,2,2,2,2,2,2,2,2,2,2,2,2,
2,2,2,2,2,2,2,2,2,2,2,2,2,2,2,2,2,2,2,2,2,2,2,2,2,2,2,2,2,2,2,2,2,2,2,2,
2,2,2,2,2,2,2,2,2,2,2,2,2,2,2,2,2,2,2,2,2,2,2,2,2,2,2,2,2,2,2,2,2,3),(0.,
0.0009943756807032,0.0019887513614064,0.0029831270421096,0.0039775027228128,
0.004971878403516,0.0059662540842192,0.0069606297649224,0.0079550054456256,
0.0089493811263288,0.009943756807032,0.0109381324877352,0.0119325081684384,
0.0129268838491416,0.0139212595298448,0.014915635210548,0.0159100108912512,
0.0169043865719544,0.0178987622526576,0.0188931379333608,0.019887513614064,
0.0208818892947672,0.0218762649754704,0.0228706406561736,0.0238650163368768,
0.02485939201758,0.0258537676982832,0.0268481433789864,0.0278425190596896,
0.0288368947403928,0.029831270421096,0.0308256461017992,0.0318200217825024,
0.0328143974632056,0.0338087731439088,0.034803148824612,0.0357975245053152,
0.0367919001860184,0.0377862758667216,0.0387806515474248,0.039775027228128,
0.0407694029088312,0.0417637785895344,0.0427581542702376,0.0437525299509408,
0.044746905631644,0.0457412813123472,0.0467356569930504,0.0477300326737536,
0.0487244083544568,0.04971878403516,0.0507131597158632,0.0517075353965664,
0.0527019110772696,0.0536962867579728,0.054690662438676,0.0556850381193792,
0.0566794138000824,0.0576737894807856,0.0586681651614888,0.059662540842192,
0.0606569165228952,0.0616512922035984,0.0626456678843016,0.0636400435650048,
0.064634419245708,0.0656287949264112,0.0666231706071144,0.0676175462878176,
0.0686119219685208,0.069606297649224,0.0706006733299272,0.0715950490106304,
0.0725894246913336,0.0735838003720368,0.07457817605274,0.0755725517334432,
0.0765669274141464,0.0775613030948496,0.0785556787755528,0.079550054456256,
0.0805444301369592,0.0815388058176624,0.0825331814983656,0.0835275571790688,
0.084521932859772,0.0855163085404752,0.0865106842211784,0.0875050599018816,
0.0884994355825848,0.089493811263288,0.0904881869439912,0.0914825626246944,
0.0924769383053976,0.0934713139861008,0.094465689666804,0.0954600653475072,
0.0964544410282104,0.0974488167089136,0.0984431923896168,0.09943756807032,
0.100431943751023,0.101426319431726,0.10242069511243,0.103415070793133,
0.104409446473836,0.105403822154539,0.106398197835242,0.107392573515946,
0.108386949196649,0.109381324877352,0.110375700558055,0.111370076238758,
0.112364451919462,0.113358827600165,0.114353203280868,0.115347578961571,
0.116341954642274,0.117336330322978,0.118330706003681,0.119325081684384,
0.120319457365087,0.12131383304579,0.122308208726494,0.123302584407197,
0.1242969600879,0.125291335768603,0.126285711449306,0.12728008713001,0.128274462810713,
0.129268838491416,0.130263214172119,0.131257589852822,0.132251965533526,
0.133246341214229,0.134240716894932,0.135235092575635,0.136229468256338,
0.137223843937042,0.138218219617745,0.139212595298448,0.140206970979151,
0.141201346659854,0.142195722340558,0.143190098021261,0.144184473701964,
0.145178849382667,0.14617322506337,0.147167600744074,0.148161976424777,
0.14915635210548,0.150150727786183,0.151145103466886,0.15213947914759,0.153133854828293,
0.154128230508996,0.155122606189699,0.156116981870402,0.157111357551106,
0.158105733231809,0.159100108912512,0.160094484593215,0.161088860273918,
0.162083235954622,0.163077611635325,0.164071987316028,0.165066362996731,
0.166060738677434,0.167055114358138,0.168049490038841,0.169043865719544,
0.170038241400247,0.17103261708095,0.172026992761654,0.173021368442357,
0.17401574412306,0.175010119803763,0.176004495484466,0.17699887116517,0.177993246845873,
0.178987622526576,0.179981998207279,0.180976373887982,0.181970749568686,
0.182965125249389,0.183959500930092,0.184953876610795,0.185948252291498,
0.186942627972202,0.187937003652905,0.188931379333608,0.189925755014311,
0.190920130695014,0.191914506375718,0.192908882056421,0.193903257737124,
0.194897633417827,0.19589200909853,0.196886384779234,0.197880760459937,
0.19887513614064,0.199869511821343,0.200863887502046,0.20185826318275,0.202852638863453,
0.203847014544156,0.204841390224859,0.205835765905562,0.206830141586266,
0.207824517266969,0.208818892947672,0.209813268628375,0.210807644309078,
0.211802019989782,0.212796395670485,0.213790771351188,0.214785147031891,
0.215779522712594,0.216773898393298,0.217768274074001,0.218762649754704,
0.219757025435407,0.22075140111611,0.221745776796814,0.222740152477517,
0.22373452815822,0.224728903838923,0.225723279519626,0.22671765520033,0.227712030881033,
0.228706406561736,0.229700782242439,0.230695157923142,0.231689533603846,
0.232683909284549,0.233678284965252,0.234672660645955,0.235667036326658,
0.236661412007362,0.237655787688065,0.238650163368768,0.239644539049471,
0.240638914730174,0.241633290410878,0.242627666091581,0.243622041772284,
0.244616417452987,0.24561079313369,0.246605168814394,0.247599544495097,
0.2485939201758,0.249588295856503,0.250582671537206,0.25157704721791,0.252571422898613,
0.253565798579316,0.254560174260019,0.255554549940722,0.256548925621426,
0.257543301302129,0.258537676982832,0.259532052663535,0.260526428344238,
0.261520804024942,0.262515179705645,0.263509555386348,0.264503931067051,
0.265498306747754,0.266492682428458,0.267487058109161,0.268481433789864,
0.268969065897308),.UNSPECIFIED.)
CURVE()
GEOMETRIC_REPRESENTATION_ITEM()
RATIONAL_B_SPLINE_CURVE((1.,0.995734176295034,1.,0.995734176295034,1.,0.995734176295034,
1.,0.995734176295034,1.,0.995734176295034,1.,0.995734176295034,1.,0.995734176295034,
1.,0.995734176295034,1.,0.995734176295034,1.,0.995734176295034,1.,0.995734176295034,
1.,0.995734176295034,1.,0.995734176295034,1.,0.995734176295034,1.,0.995734176295034,
1.,0.995734176295034,1.,0.995734176295034,1.,0.995734176295034,1.,0.995734176295034,
1.,0.995734176295034,1.,0.995734176295034,1.,0.995734176295034,1.,0.995734176295034,
1.,0.995734176295034,1.,0.995734176295034,1.,0.995734176295034,1.,0.995734176295034,
1.,0.995734176295034,1.,0.995734176295034,1.,0.995734176295034,1.,0.995734176295034,
1.,0.995734176295034,1.,0.995734176295034,1.,0.995734176295034,1.,0.995734176295034,
1.,0.995734176295034,1.,0.995734176295034,1.,0.995734176295034,1.,0.995734176295034,
1.,0.995734176295034,1.,0.995734176295034,1.,0.995734176295034,1.,0.995734176295034,
1.,0.995734176295034,1.,0.995734176295034,1.,0.995734176295034,1.,0.995734176295034,
1.,0.995734176295034,1.,0.995734176295034,1.,0.995734176295034,1.,0.995734176295034,
1.,0.995734176295034,1.,0.995734176295034,1.,0.995734176295034,1.,0.995734176295034,
1.,0.995734176295034,1.,0.995734176295034,1.,0.995734176295034,1.,0.995734176295034,
1.,0.995734176295034,1.,0.995734176295034,1.,0.995734176295034,1.,0.995734176295034,
1.,0.995734176295034,1.,0.995734176295034,1.,0.995734176295034,1.,0.995734176295034,
1.,0.995734176295034,1.,0.995734176295034,1.,0.995734176295034,1.,0.995734176295034,
1.,0.995734176295034,1.,0.995734176295034,1.,0.995734176295034,1.,0.995734176295034,
1.,0.995734176295034,1.,0.995734176295034,1.,0.995734176295034,1.,0.995734176295034,
1.,0.995734176295034,1.,0.995734176295034,1.,0.995734176295034,1.,0.995734176295034,
1.,0.995734176295034,1.,0.995734176295034,1.,0.995734176295034,1.,0.995734176295034,
1.,0.995734176295034,1.,0.995734176295034,1.,0.995734176295034,1.,0.995734176295034,
1.,0.995734176295034,1.,0.995734176295034,1.,0.995734176295034,1.,0.995734176295034,
1.,0.995734176295034,1.,0.995734176295034,1.,0.995734176295034,1.,0.995734176295034,
1.,0.995734176295034,1.,0.995734176295034,1.,0.995734176295034,1.,0.995734176295034,
1.,0.995734176295034,1.,0.995734176295034,1.,0.995734176295034,1.,0.995734176295034,
1.,0.995734176295034,1.,0.995734176295034,1.,0.995734176295034,1.,0.995734176295034,
1.,0.995734176295034,1.,0.995734176295034,1.,0.995734176295034,1.,0.995734176295034,
1.,0.995734176295034,1.,0.995734176295034,1.,0.995734176295034,1.,0.995734176295034,
1.,0.995734176295034,1.,0.995734176295034,1.,0.995734176295034,1.,0.995734176295034,
1.,0.995734176295034,1.,0.995734176295034,1.,0.995734176295034,1.,0.995734176295034,
1.,0.995734176295034,1.,0.995734176295034,1.,0.995734176295034,1.,0.995734176295034,
1.,0.995734176295034,1.,0.995734176295034,1.,0.995734176295034,1.,0.995734176295034,
1.,0.995734176295034,1.,0.995734176295034,1.,0.995734176295034,1.,0.995734176295034,
1.,0.995734176295034,1.,0.995734176295034,1.,0.995734176295034,1.,0.995734176295034,
1.,0.995734176295034,1.,0.995734176295034,1.,0.995734176295034,1.,0.995734176295034,
1.,0.995734176295034,1.,0.995734176295034,1.,0.995734176295034,1.,0.995734176295034,
1.,0.995734176295034,1.,0.995734176295034,1.,0.995734176295034,1.,0.995734176295034,
1.,0.995734176295034,1.,0.995734176295034,1.,0.995734176295034,1.,0.995734176295034,
1.,0.995734176295034,1.,0.995734176295034,1.,0.995734176295034,1.,0.995734176295034,
1.,0.995734176295034,1.,0.995734176295034,1.,0.995734176295034,1.,0.995734176295034,
1.,0.995734176295034,1.,0.995734176295034,1.,0.995734176295034,1.,0.995734176295034,
1.,0.995734176295034,1.,0.995734176295034,1.,0.995734176295034,1.,0.995734176295034,
1.,0.995734176295034,1.,0.995734176295034,1.,0.995734176295034,1.,0.995734176295034,
1.,0.995734176295034,1.,0.995734176295034,1.,0.995734176295034,1.,0.995734176295034,
1.,0.995734176295034,1.,0.995734176295034,1.,0.995734176295034,1.,0.995734176295034,
1.,0.995734176295034,1.,0.995734176295034,1.,0.995734176295034,1.,0.995734176295034,
1.,0.995734176295034,1.,0.995734176295034,1.,0.995734176295034,1.,0.995734176295034,
1.,0.995734176295034,1.,0.995734176295034,1.,0.995734176295034,1.,0.995734176295034,
1.,0.995734176295034,1.,0.995734176295034,1.,0.995734176295034,1.,0.995734176295034,
1.,0.995734176295034,1.,0.995734176295034,1.,0.995734176295034,1.,0.995734176295034,
1.,0.995734176295034,1.,0.995734176295034,1.,0.995734176295034,1.,0.995734176295034,
1.,0.995734176295034,1.,0.995734176295034,1.,0.995734176295034,1.,0.995734176295034,
1.,0.995734176295034,1.,0.995734176295034,1.,0.995734176295034,1.,0.995734176295034,
1.,0.995734176295034,1.,0.995734176295034,1.,0.995734176295034,1.,0.995734176295034,
1.,0.995734176295034,1.,0.995734176295034,1.,0.995734176295034,1.,0.995734176295034,
1.,0.995734176295034,1.,0.995734176295034,1.,0.995734176295034,1.,0.995734176295034,
1.,0.995734176295034,1.,0.995734176295034,1.,0.995734176295034,1.,0.995734176295034,
1.,0.995734176295034,1.,0.995734176295034,1.,0.995734176295034,1.,0.995734176295034,
1.,0.995734176295034,1.,0.995734176295034,1.,0.995734176295034,1.,0.995734176295034,
1.,0.995734176295034,1.,0.995734176295034,1.,0.995734176295034,1.,0.995734176295034,
1.,0.995734176295034,1.,0.995734176295034,1.,0.995734176295034,1.,0.995734176295034,
1.,0.995734176295034,1.,0.995734176295034,1.,0.995734176295034,1.,0.995734176295034,
1.,0.995734176295034,1.,0.995734176295034,1.,0.995734176295034,1.,0.995734176295034,
1.,0.995734176295034,1.,0.995734176295034,1.,0.995734176295034,1.,0.995734176295034,
1.,0.995734176295034,1.,0.995734176295034,1.,0.995734176295034,1.,0.995734176295034,
1.,0.995734176295034,1.,0.995734176295034,1.,0.995734176295034,1.,0.997908081780755,
0.997867876027224))
REPRESENTATION_ITEM('')
);
#4082=(
BOUNDED_CURVE()
B_SPLINE_CURVE(2,(#154422,#154423,#154424,#154425,#154426,#154427,#154428,
#154429,#154430,#154431,#154432,#154433,#154434,#154435,#154436,#154437,
#154438,#154439,#154440,#154441,#154442,#154443,#154444,#154445,#154446,
#154447,#154448,#154449,#154450,#154451,#154452,#154453,#154454,#154455,
#154456,#154457,#154458),.UNSPECIFIED.,.F.,.F.)
B_SPLINE_CURVE_WITH_KNOTS((3,2,2,2,2,2,2,2,2,2,2,2,2,2,2,2,2,2,3),(0.25,
0.250980392156863,0.251960784313725,0.252941176470588,0.253921568627451,
0.254901960784314,0.255882352941176,0.256862745098039,0.257843137254902,
0.258823529411765,0.259803921568627,0.26078431372549,0.261764705882353,
0.262745098039216,0.263725490196078,0.264705882352941,0.265686274509804,
0.266666666666667,0.26668268661721),.UNSPECIFIED.)
CURVE()
GEOMETRIC_REPRESENTATION_ITEM()
RATIONAL_B_SPLINE_CURVE((1.,0.995734176295034,1.,0.995734176295034,1.,0.995734176295034,
1.,0.995734176295034,1.,0.995734176295034,1.,0.995734176295034,1.,0.995734176295034,
1.,0.995734176295034,1.,0.995734176295034,1.,0.995734176295034,1.,0.995734176295034,
1.,0.995734176295034,1.,0.995734176295034,1.,0.995734176295034,1.,0.995734176295034,
1.,0.995734176295034,1.,0.995734176295034,1.,0.999930294949526,0.999862867908832))
REPRESENTATION_ITEM('')
);
#4083=(
BOUNDED_CURVE()
B_SPLINE_CURVE(2,(#158491,#158492,#158493,#158494,#158495,#158496,#158497,
#158498,#158499,#158500,#158501,#158502,#158503,#158504,#158505,#158506,
#158507,#158508,#158509,#158510,#158511,#158512,#158513,#158514,#158515,
#158516,#158517,#158518,#158519,#158520,#158521,#158522,#158523,#158524,
#158525,#158526,#158527),.UNSPECIFIED.,.F.,.F.)
B_SPLINE_CURVE_WITH_KNOTS((3,2,2,2,2,2,2,2,2,2,2,2,2,2,2,2,2,2,3),(0.25356582111872,
0.254560196887814,0.255554572656907,0.256548948426,0.257543324195093,0.258537699964186,
0.259532075733279,0.260526451502372,0.261520827271465,0.262515203040558,
0.263509578809651,0.264503954578744,0.265498330347837,0.26649270611693,
0.267487081886023,0.268481457655116,0.269475833424209,0.270470209193302,
0.27052030629005),.UNSPECIFIED.)
CURVE()
GEOMETRIC_REPRESENTATION_ITEM()
RATIONAL_B_SPLINE_CURVE((1.,0.995734176295034,1.,0.995734176295034,1.,0.995734176295034,
1.,0.995734176295034,1.,0.995734176295034,1.,0.995734176295034,1.,0.995734176295034,
1.,0.995734176295034,1.,0.995734176295034,1.,0.995734176295034,1.,0.995734176295034,
1.,0.995734176295034,1.,0.995734176295034,1.,0.995734176295034,1.,0.995734176295034,
1.,0.995734176295034,1.,0.995734176295034,1.,0.999785085890563,0.999591826719365))
REPRESENTATION_ITEM('')
);
#4084=(
BOUNDED_CURVE()
B_SPLINE_CURVE(2,(#162564,#162565,#162566,#162567,#162568,#162569,#162570,
#162571,#162572,#162573,#162574,#162575,#162576,#162577,#162578,#162579,
#162580,#162581,#162582,#162583,#162584,#162585,#162586,#162587,#162588,
#162589,#162590,#162591,#162592,#162593,#162594,#162595,#162596,#162597,
#162598,#162599,#162600,#162601,#162602,#162603,#162604,#162605,#162606,
#162607,#162608,#162609,#162610,#162611,#162612,#162613,#162614,#162615,
#162616,#162617,#162618,#162619,#162620,#162621,#162622,#162623,#162624,
#162625,#162626,#162627,#162628,#162629,#162630,#162631,#162632,#162633,
#162634,#162635,#162636,#162637,#162638,#162639,#162640,#162641,#162642,
#162643,#162644,#162645,#162646,#162647,#162648,#162649,#162650,#162651,
#162652,#162653,#162654,#162655,#162656,#162657,#162658,#162659,#162660,
#162661,#162662,#162663,#162664,#162665,#162666,#162667,#162668,#162669,
#162670,#162671,#162672,#162673,#162674,#162675,#162676,#162677,#162678,
#162679,#162680,#162681,#162682,#162683,#162684,#162685,#162686,#162687,
#162688,#162689,#162690,#162691,#162692,#162693,#162694,#162695,#162696,
#162697,#162698,#162699,#162700,#162701,#162702,#162703,#162704,#162705,
#162706,#162707,#162708,#162709,#162710,#162711,#162712,#162713,#162714,
#162715,#162716,#162717,#162718,#162719,#162720,#162721,#162722,#162723,
#162724,#162725,#162726,#162727,#162728,#162729,#162730,#162731,#162732,
#162733,#162734,#162735,#162736,#162737,#162738,#162739,#162740,#162741,
#162742,#162743,#162744,#162745,#162746,#162747,#162748,#162749,#162750,
#162751,#162752,#162753,#162754,#162755,#162756,#162757,#162758,#162759,
#162760,#162761,#162762,#162763,#162764,#162765,#162766,#162767,#162768,
#162769,#162770,#162771,#162772,#162773,#162774,#162775,#162776,#162777,
#162778,#162779,#162780,#162781,#162782,#162783,#162784,#162785,#162786,
#162787,#162788,#162789,#162790,#162791,#162792,#162793,#162794,#162795,
#162796,#162797,#162798,#162799,#162800,#162801,#162802,#162803,#162804,
#162805,#162806,#162807,#162808,#162809,#162810,#162811,#162812,#162813,
#162814,#162815,#162816,#162817,#162818,#162819,#162820,#162821,#162822,
#162823,#162824,#162825,#162826,#162827,#162828,#162829,#162830,#162831,
#162832,#162833,#162834,#162835,#162836,#162837,#162838,#162839,#162840,
#162841,#162842,#162843,#162844,#162845,#162846,#162847,#162848,#162849,
#162850,#162851,#162852,#162853,#162854,#162855,#162856,#162857,#162858,
#162859,#162860,#162861,#162862,#162863,#162864,#162865,#162866,#162867,
#162868,#162869,#162870,#162871,#162872,#162873,#162874,#162875,#162876,
#162877,#162878,#162879,#162880,#162881,#162882,#162883,#162884,#162885,
#162886,#162887,#162888,#162889,#162890,#162891,#162892,#162893,#162894,
#162895,#162896,#162897,#162898,#162899,#162900,#162901,#162902,#162903,
#162904,#162905,#162906,#162907,#162908,#162909,#162910,#162911,#162912,
#162913,#162914,#162915,#162916,#162917,#162918,#162919,#162920,#162921,
#162922,#162923,#162924,#162925,#162926,#162927,#162928,#162929,#162930,
#162931,#162932,#162933,#162934,#162935,#162936,#162937,#162938,#162939,
#162940,#162941,#162942,#162943,#162944,#162945,#162946,#162947,#162948,
#162949,#162950,#162951,#162952,#162953,#162954,#162955,#162956,#162957,
#162958,#162959,#162960,#162961,#162962,#162963,#162964,#162965,#162966,
#162967,#162968,#162969,#162970,#162971,#162972,#162973,#162974,#162975,
#162976,#162977,#162978,#162979,#162980,#162981,#162982,#162983,#162984,
#162985,#162986,#162987,#162988,#162989,#162990,#162991,#162992,#162993,
#162994,#162995,#162996,#162997,#162998,#162999,#163000,#163001,#163002,
#163003,#163004,#163005,#163006,#163007,#163008,#163009,#163010,#163011,
#163012,#163013,#163014,#163015,#163016,#163017,#163018,#163019,#163020,
#163021,#163022,#163023,#163024,#163025,#163026,#163027,#163028,#163029,
#163030,#163031,#163032,#163033,#163034,#163035,#163036,#163037,#163038,
#163039,#163040,#163041,#163042,#163043,#163044,#163045,#163046,#163047,
#163048,#163049,#163050,#163051,#163052,#163053,#163054,#163055,#163056,
#163057,#163058,#163059,#163060,#163061,#163062,#163063,#163064,#163065,
#163066,#163067,#163068,#163069,#163070,#163071,#163072,#163073,#163074,
#163075,#163076,#163077,#163078,#163079,#163080,#163081,#163082,#163083,
#163084,#163085,#163086,#163087,#163088,#163089,#163090,#163091,#163092,
#163093,#163094,#163095,#163096,#163097,#163098,#163099,#163100,#163101,
#163102,#163103,#163104,#163105,#163106),.UNSPECIFIED.,.F.,.F.)
B_SPLINE_CURVE_WITH_KNOTS((3,2,2,2,2,2,2,2,2,2,2,2,2,2,2,2,2,2,2,2,2,2,
2,2,2,2,2,2,2,2,2,2,2,2,2,2,2,2,2,2,2,2,2,2,2,2,2,2,2,2,2,2,2,2,2,2,2,2,
2,2,2,2,2,2,2,2,2,2,2,2,2,2,2,2,2,2,2,2,2,2,2,2,2,2,2,2,2,2,2,2,2,2,2,2,
2,2,2,2,2,2,2,2,2,2,2,2,2,2,2,2,2,2,2,2,2,2,2,2,2,2,2,2,2,2,2,2,2,2,2,2,
2,2,2,2,2,2,2,2,2,2,2,2,2,2,2,2,2,2,2,2,2,2,2,2,2,2,2,2,2,2,2,2,2,2,2,2,
2,2,2,2,2,2,2,2,2,2,2,2,2,2,2,2,2,2,2,2,2,2,2,2,2,2,2,2,2,2,2,2,2,2,2,2,
2,2,2,2,2,2,2,2,2,2,2,2,2,2,2,2,2,2,2,2,2,2,2,2,2,2,2,2,2,2,2,2,2,2,2,2,
2,2,2,2,2,2,2,2,2,2,2,2,2,2,2,2,2,2,2,2,2,2,2,2,2,2,2,2,2,2,2,2,2,3),(0.,
0.000980392156862745,0.00196078431372549,0.00294117647058824,0.00392156862745098,
0.00490196078431373,0.00588235294117647,0.00686274509803922,0.00784313725490196,
0.00882352941176471,0.00980392156862745,0.0107843137254902,0.0117647058823529,
0.0127450980392157,0.0137254901960784,0.0147058823529412,0.0156862745098039,
0.0166666666666667,0.0176470588235294,0.0186274509803922,0.0196078431372549,
0.0205882352941176,0.0215686274509804,0.0225490196078431,0.0235294117647059,
0.0245098039215686,0.0254901960784314,0.0264705882352941,0.0274509803921569,
0.0284313725490196,0.0294117647058824,0.0303921568627451,0.0313725490196078,
0.0323529411764706,0.0333333333333333,0.0343137254901961,0.0352941176470588,
0.0362745098039216,0.0372549019607843,0.0382352941176471,0.0392156862745098,
0.0401960784313726,0.0411764705882353,0.042156862745098,0.0431372549019608,
0.0441176470588235,0.0450980392156863,0.046078431372549,0.0470588235294118,
0.0480392156862745,0.0490196078431373,0.05,0.0509803921568627,0.0519607843137255,
0.0529411764705882,0.053921568627451,0.0549019607843137,0.0558823529411765,
0.0568627450980392,0.057843137254902,0.0588235294117647,0.0598039215686275,
0.0607843137254902,0.0617647058823529,0.0627450980392157,0.0637254901960784,
0.0647058823529412,0.0656862745098039,0.0666666666666667,0.0676470588235294,
0.0686274509803922,0.0696078431372549,0.0705882352941176,0.0715686274509804,
0.0725490196078431,0.0735294117647059,0.0745098039215686,0.0754901960784314,
0.0764705882352941,0.0774509803921569,0.0784313725490196,0.0794117647058823,
0.0803921568627451,0.0813725490196078,0.0823529411764706,0.0833333333333333,
0.0843137254901961,0.0852941176470588,0.0862745098039216,0.0872549019607843,
0.0882352941176471,0.0892156862745098,0.0901960784313725,0.0911764705882353,
0.092156862745098,0.0931372549019608,0.0941176470588235,0.0950980392156863,
0.096078431372549,0.0970588235294118,0.0980392156862745,0.0990196078431373,
0.1,0.100980392156863,0.101960784313725,0.102941176470588,0.103921568627451,
0.104901960784314,0.105882352941176,0.106862745098039,0.107843137254902,
0.108823529411765,0.109803921568627,0.11078431372549,0.111764705882353,
0.112745098039216,0.113725490196078,0.114705882352941,0.115686274509804,
0.116666666666667,0.117647058823529,0.118627450980392,0.119607843137255,
0.120588235294118,0.12156862745098,0.122549019607843,0.123529411764706,
0.124509803921569,0.125490196078431,0.126470588235294,0.127450980392157,
0.12843137254902,0.129411764705882,0.130392156862745,0.131372549019608,
0.132352941176471,0.133333333333333,0.134313725490196,0.135294117647059,
0.136274509803922,0.137254901960784,0.138235294117647,0.13921568627451,
0.140196078431373,0.141176470588235,0.142156862745098,0.143137254901961,
0.144117647058824,0.145098039215686,0.146078431372549,0.147058823529412,
0.148039215686275,0.149019607843137,0.15,0.150980392156863,0.151960784313725,
0.152941176470588,0.153921568627451,0.154901960784314,0.155882352941176,
0.156862745098039,0.157843137254902,0.158823529411765,0.159803921568627,
0.16078431372549,0.161764705882353,0.162745098039216,0.163725490196078,
0.164705882352941,0.165686274509804,0.166666666666667,0.167647058823529,
0.168627450980392,0.169607843137255,0.170588235294118,0.17156862745098,
0.172549019607843,0.173529411764706,0.174509803921569,0.175490196078431,
0.176470588235294,0.177450980392157,0.17843137254902,0.179411764705882,
0.180392156862745,0.181372549019608,0.182352941176471,0.183333333333333,
0.184313725490196,0.185294117647059,0.186274509803922,0.187254901960784,
0.188235294117647,0.18921568627451,0.190196078431373,0.191176470588235,
0.192156862745098,0.193137254901961,0.194117647058824,0.195098039215686,
0.196078431372549,0.197058823529412,0.198039215686275,0.199019607843137,
0.2,0.200980392156863,0.201960784313725,0.202941176470588,0.203921568627451,
0.204901960784314,0.205882352941176,0.206862745098039,0.207843137254902,
0.208823529411765,0.209803921568627,0.21078431372549,0.211764705882353,
0.212745098039216,0.213725490196078,0.214705882352941,0.215686274509804,
0.216666666666667,0.217647058823529,0.218627450980392,0.219607843137255,
0.220588235294118,0.22156862745098,0.222549019607843,0.223529411764706,
0.224509803921569,0.225490196078431,0.226470588235294,0.227450980392157,
0.22843137254902,0.229411764705882,0.230392156862745,0.231372549019608,
0.232352941176471,0.233333333333333,0.234313725490196,0.235294117647059,
0.236274509803922,0.237254901960784,0.238235294117647,0.23921568627451,
0.240196078431373,0.241176470588235,0.242156862745098,0.243137254901961,
0.244117647058824,0.245098039215686,0.246078431372549,0.247058823529412,
0.248039215686275,0.249019607843137,0.25,0.250980392156863,0.251960784313725,
0.252941176470588,0.253921568627451,0.254901960784314,0.255882352941176,
0.256862745098039,0.257843137254902,0.258823529411765,0.259803921568627,
0.26078431372549,0.261764705882353,0.262745098039216,0.263725490196078,
0.264705882352941,0.265153469650551),.UNSPECIFIED.)
CURVE()
GEOMETRIC_REPRESENTATION_ITEM()
RATIONAL_B_SPLINE_CURVE((1.,0.995734176295034,1.,0.995734176295034,1.,0.995734176295034,
1.,0.995734176295034,1.,0.995734176295034,1.,0.995734176295034,1.,0.995734176295034,
1.,0.995734176295034,1.,0.995734176295034,1.,0.995734176295034,1.,0.995734176295034,
1.,0.995734176295034,1.,0.995734176295034,1.,0.995734176295034,1.,0.995734176295034,
1.,0.995734176295034,1.,0.995734176295034,1.,0.995734176295034,1.,0.995734176295034,
1.,0.995734176295034,1.,0.995734176295034,1.,0.995734176295034,1.,0.995734176295034,
1.,0.995734176295034,1.,0.995734176295034,1.,0.995734176295034,1.,0.995734176295034,
1.,0.995734176295034,1.,0.995734176295034,1.,0.995734176295034,1.,0.995734176295034,
1.,0.995734176295034,1.,0.995734176295034,1.,0.995734176295034,1.,0.995734176295034,
1.,0.995734176295034,1.,0.995734176295034,1.,0.995734176295034,1.,0.995734176295034,
1.,0.995734176295034,1.,0.995734176295034,1.,0.995734176295034,1.,0.995734176295034,
1.,0.995734176295034,1.,0.995734176295034,1.,0.995734176295034,1.,0.995734176295034,
1.,0.995734176295034,1.,0.995734176295034,1.,0.995734176295034,1.,0.995734176295034,
1.,0.995734176295034,1.,0.995734176295034,1.,0.995734176295034,1.,0.995734176295034,
1.,0.995734176295034,1.,0.995734176295034,1.,0.995734176295034,1.,0.995734176295034,
1.,0.995734176295034,1.,0.995734176295034,1.,0.995734176295034,1.,0.995734176295034,
1.,0.995734176295034,1.,0.995734176295034,1.,0.995734176295034,1.,0.995734176295034,
1.,0.995734176295034,1.,0.995734176295034,1.,0.995734176295034,1.,0.995734176295034,
1.,0.995734176295034,1.,0.995734176295034,1.,0.995734176295034,1.,0.995734176295034,
1.,0.995734176295034,1.,0.995734176295034,1.,0.995734176295034,1.,0.995734176295034,
1.,0.995734176295034,1.,0.995734176295034,1.,0.995734176295034,1.,0.995734176295034,
1.,0.995734176295034,1.,0.995734176295034,1.,0.995734176295034,1.,0.995734176295034,
1.,0.995734176295034,1.,0.995734176295034,1.,0.995734176295034,1.,0.995734176295034,
1.,0.995734176295034,1.,0.995734176295034,1.,0.995734176295034,1.,0.995734176295034,
1.,0.995734176295034,1.,0.995734176295034,1.,0.995734176295034,1.,0.995734176295034,
1.,0.995734176295034,1.,0.995734176295034,1.,0.995734176295034,1.,0.995734176295034,
1.,0.995734176295034,1.,0.995734176295034,1.,0.995734176295034,1.,0.995734176295034,
1.,0.995734176295034,1.,0.995734176295034,1.,0.995734176295034,1.,0.995734176295034,
1.,0.995734176295034,1.,0.995734176295034,1.,0.995734176295034,1.,0.995734176295034,
1.,0.995734176295034,1.,0.995734176295034,1.,0.995734176295034,1.,0.995734176295034,
1.,0.995734176295034,1.,0.995734176295034,1.,0.995734176295034,1.,0.995734176295034,
1.,0.995734176295034,1.,0.995734176295034,1.,0.995734176295034,1.,0.995734176295034,
1.,0.995734176295034,1.,0.995734176295034,1.,0.995734176295034,1.,0.995734176295034,
1.,0.995734176295034,1.,0.995734176295034,1.,0.995734176295034,1.,0.995734176295034,
1.,0.995734176295034,1.,0.995734176295034,1.,0.995734176295034,1.,0.995734176295034,
1.,0.995734176295034,1.,0.995734176295034,1.,0.995734176295034,1.,0.995734176295034,
1.,0.995734176295034,1.,0.995734176295034,1.,0.995734176295034,1.,0.995734176295034,
1.,0.995734176295034,1.,0.995734176295034,1.,0.995734176295034,1.,0.995734176295034,
1.,0.995734176295034,1.,0.995734176295034,1.,0.995734176295034,1.,0.995734176295034,
1.,0.995734176295034,1.,0.995734176295034,1.,0.995734176295034,1.,0.995734176295034,
1.,0.995734176295034,1.,0.995734176295034,1.,0.995734176295034,1.,0.995734176295034,
1.,0.995734176295034,1.,0.995734176295034,1.,0.995734176295034,1.,0.995734176295034,
1.,0.995734176295034,1.,0.995734176295034,1.,0.995734176295034,1.,0.995734176295034,
1.,0.995734176295034,1.,0.995734176295034,1.,0.995734176295034,1.,0.995734176295034,
1.,0.995734176295034,1.,0.995734176295034,1.,0.995734176295034,1.,0.995734176295034,
1.,0.995734176295034,1.,0.995734176295034,1.,0.995734176295034,1.,0.995734176295034,
1.,0.995734176295034,1.,0.995734176295034,1.,0.995734176295034,1.,0.995734176295034,
1.,0.995734176295034,1.,0.995734176295034,1.,0.995734176295034,1.,0.995734176295034,
1.,0.995734176295034,1.,0.995734176295034,1.,0.995734176295034,1.,0.995734176295034,
1.,0.995734176295034,1.,0.995734176295034,1.,0.995734176295034,1.,0.995734176295034,
1.,0.995734176295034,1.,0.995734176295034,1.,0.995734176295034,1.,0.995734176295034,
1.,0.995734176295034,1.,0.995734176295034,1.,0.995734176295034,1.,0.995734176295034,
1.,0.995734176295034,1.,0.995734176295034,1.,0.995734176295034,1.,0.995734176295034,
1.,0.995734176295034,1.,0.995734176295034,1.,0.995734176295034,1.,0.995734176295034,
1.,0.995734176295034,1.,0.995734176295034,1.,0.995734176295034,1.,0.995734176295034,
1.,0.995734176295034,1.,0.995734176295034,1.,0.995734176295034,1.,0.995734176295034,
1.,0.995734176295034,1.,0.995734176295034,1.,0.995734176295034,1.,0.995734176295034,
1.,0.995734176295034,1.,0.995734176295034,1.,0.995734176295034,1.,0.995734176295034,
1.,0.995734176295034,1.,0.995734176295034,1.,0.995734176295034,1.,0.995734176295034,
1.,0.995734176295034,1.,0.995734176295034,1.,0.995734176295034,1.,0.995734176295034,
1.,0.995734176295034,1.,0.995734176295034,1.,0.995734176295034,1.,0.995734176295034,
1.,0.995734176295034,1.,0.995734176295034,1.,0.995734176295034,1.,0.995734176295034,
1.,0.995734176295034,1.,0.995734176295034,1.,0.995734176295034,1.,0.995734176295034,
1.,0.995734176295034,1.,0.995734176295034,1.,0.995734176295034,1.,0.995734176295034,
1.,0.995734176295034,1.,0.995734176295034,1.,0.995734176295034,1.,0.995734176295034,
1.,0.995734176295034,1.,0.995734176295034,1.,0.995734176295034,1.,0.995734176295034,
1.,0.995734176295034,1.,0.995734176295034,1.,0.995734176295034,1.,0.995734176295034,
1.,0.995734176295034,1.,0.995734176295034,1.,0.995734176295034,1.,0.998052484925732,
0.997883203190121))
REPRESENTATION_ITEM('')
);
#4173=B_SPLINE_CURVE_WITH_KNOTS('',3,(#142867,#142868,#142869,#142870,#142871,
#142872,#142873,#142874,#142875,#142876,#142877,#142878,#142879,#142880,
#142881,#142882,#142883,#142884),.UNSPECIFIED.,.F.,.F.,(4,2,2,2,2,2,2,2,
4),(-1.58055055147889,-1.3828040290386,-1.18505750659832,-0.987666391168882,
-0.790275275739446,-0.59288416031001,-0.395493044880575,-0.197746522440287,
0.),.UNSPECIFIED.);
#4174=B_SPLINE_CURVE_WITH_KNOTS('',3,(#142888,#142889,#142890,#142891,#142892,
#142893,#142894,#142895,#142896,#142897,#142898,#142899,#142900,#142901,
#142902,#142903,#142904,#142905),.UNSPECIFIED.,.F.,.F.,(4,2,2,2,2,2,2,2,
4),(0.,0.200360130478694,0.400720260957388,0.600044505959735,0.799368750962083,
0.99869299596443,1.19801724096678,1.39837737144547,1.59873750192417),
 .UNSPECIFIED.);
#4175=B_SPLINE_CURVE_WITH_KNOTS('',3,(#142906,#142907,#142908,#142909,#142910,
#142911,#142912,#142913,#142914,#142915,#142916,#142917,#142918,#142919,
#142920,#142921,#142922,#142923),.UNSPECIFIED.,.F.,.F.,(4,2,2,2,2,2,2,2,
4),(-1.59873750192417,-1.39837737144547,-1.19801724096678,-0.99869299596443,
-0.799368750962083,-0.600044505959736,-0.400720260957388,-0.200360130478694,
0.),.UNSPECIFIED.);
#4176=B_SPLINE_CURVE_WITH_KNOTS('',3,(#142924,#142925,#142926,#142927,#142928,
#142929,#142930,#142931,#142932,#142933,#142934,#142935,#142936,#142937,
#142938,#142939,#142940,#142941),.UNSPECIFIED.,.F.,.F.,(4,2,2,2,2,2,2,2,
4),(0.,0.197746522440287,0.395493044880574,0.59288416031001,0.790275275739446,
0.987666391168882,1.18505750659832,1.3828040290386,1.58055055147889),
 .UNSPECIFIED.);
#4177=B_SPLINE_CURVE_WITH_KNOTS('',3,(#142945,#142946,#142947,#142948,#142949,
#142950,#142951,#142952,#142953,#142954,#142955,#142956,#142957,#142958,
#142959,#142960,#142961,#142962),.UNSPECIFIED.,.F.,.F.,(4,2,2,2,2,2,2,2,
4),(1.59873750192417,1.79909763240286,1.99945776288156,2.1987820078839,
2.39810625288625,2.5974304978886,2.79675474289095,2.99711487336964,3.19747500384833),
 .UNSPECIFIED.);
#4178=B_SPLINE_CURVE_WITH_KNOTS('',3,(#142966,#142967,#142968,#142969,#142970,
#142971,#142972,#142973,#142974,#142975,#142976,#142977,#142978,#142979,
#142980,#142981,#142982,#142983),.UNSPECIFIED.,.F.,.F.,(4,2,2,2,2,2,2,2,
4),(3.16110110295778,3.35884762539807,3.55659414783836,3.75398526326779,
3.95137637869723,4.14876749412666,4.3461586095561,4.54390513199639,4.74165165443667),
 .UNSPECIFIED.);
#4179=B_SPLINE_CURVE_WITH_KNOTS('',3,(#142984,#142985,#142986,#142987,#142988,
#142989,#142990,#142991,#142992,#142993,#142994,#142995,#142996,#142997,
#142998,#142999,#143000,#143001),.UNSPECIFIED.,.F.,.F.,(4,2,2,2,2,2,2,2,
4),(1.58055055147889,1.77829707391918,1.97604359635947,2.1734347117889,
2.37082582721834,2.56821694264777,2.76560805807721,2.9633545805175,3.16110110295778),
 .UNSPECIFIED.);
#4180=B_SPLINE_CURVE_WITH_KNOTS('',3,(#143002,#143003,#143004,#143005,#143006,
#143007,#143008,#143009,#143010,#143011,#143012,#143013,#143014,#143015,
#143016,#143017,#143018,#143019),.UNSPECIFIED.,.F.,.F.,(4,2,2,2,2,2,2,2,
4),(3.19747500384833,3.39783513432703,3.59819526480572,3.79751950980807,
3.99684375481042,4.19616799981276,4.39549224481511,4.59585237529381,4.7962125057725),
 .UNSPECIFIED.);
#4181=B_SPLINE_CURVE_WITH_KNOTS('',3,(#143023,#143024,#143025,#143026,#143027,
#143028,#143029,#143030,#143031,#143032,#143033,#143034,#143035,#143036,
#143037,#143038,#143039,#143040,#143041),.UNSPECIFIED.,.F.,.F.,(4,2,2,2,
3,2,2,2,4),(-0.790275275739451,-0.592884160310013,-0.395493044880575,-0.197746522440287,
0.,0.197746522440287,0.395493044880575,0.592884160310013,0.790275275739451),
 .UNSPECIFIED.);
#4182=B_SPLINE_CURVE_WITH_KNOTS('',3,(#143045,#143046,#143047,#143048,#143049,
#143050,#143051,#143052,#143053,#143054,#143055,#143056,#143057,#143058,
#143059,#143060,#143061,#143062,#143063),.UNSPECIFIED.,.F.,.F.,(4,2,2,2,
3,2,2,2,4),(-0.799368750962089,-0.600044505959739,-0.400720260957389,-0.200360130478695,
0.,0.200360130478694,0.400720260957389,0.600044505959739,0.799368750962089),
 .UNSPECIFIED.);
#4183=B_SPLINE_CURVE_WITH_KNOTS('',3,(#143064,#143065,#143066,#143067,#143068,
#143069,#143070,#143071,#143072,#143073,#143074,#143075,#143076,#143077,
#143078,#143079,#143080,#143081),.UNSPECIFIED.,.F.,.F.,(4,2,2,2,2,2,2,2,
4),(-2.39810625288627,-2.19878200788392,-1.99945776288157,-1.79909763240287,
-1.59873750192418,-1.39837737144548,-1.19801724096679,-0.998692995964438,
-0.799368750962089),.UNSPECIFIED.);
#4184=B_SPLINE_CURVE_WITH_KNOTS('',3,(#143082,#143083,#143084,#143085,#143086,
#143087,#143088,#143089,#143090,#143091,#143092,#143093,#143094,#143095,
#143096,#143097,#143098,#143099),.UNSPECIFIED.,.F.,.F.,(4,2,2,2,2,2,2,2,
4),(0.790275275739451,0.987666391168889,1.18505750659833,1.38280402903861,
1.5805505514789,1.77829707391919,1.97604359635948,2.17343471178891,2.37082582721835),
 .UNSPECIFIED.);
#4185=B_SPLINE_CURVE_WITH_KNOTS('',3,(#143103,#143104,#143105,#143106,#143107,
#143108,#143109,#143110,#143111,#143112,#143113,#143114,#143115,#143116,
#143117,#143118,#143119,#143120,#143121),.UNSPECIFIED.,.F.,.F.,(4,2,2,2,
3,2,2,2,4),(2.39810625288627,2.59743049788862,2.79675474289097,2.99711487336966,
3.19747500384836,3.39783513432705,3.59819526480574,3.79751950980809,3.99684375481044),
 .UNSPECIFIED.);
#4186=B_SPLINE_CURVE_WITH_KNOTS('',3,(#143125,#143126,#143127,#143128,#143129,
#143130,#143131,#143132,#143133,#143134,#143135,#143136,#143137,#143138,
#143139,#143140,#143141,#143142,#143143),.UNSPECIFIED.,.F.,.F.,(4,2,2,2,
3,2,2,2,4),(2.37082582721835,2.56821694264779,2.76560805807723,2.96335458051752,
3.1611011029578,3.35884762539809,3.55659414783838,3.75398526326782,3.95137637869726),
 .UNSPECIFIED.);
#4187=B_SPLINE_CURVE_WITH_KNOTS('',3,(#143144,#143145,#143146,#143147,#143148,
#143149,#143150,#143151,#143152,#143153,#143154,#143155,#143156,#143157,
#143158,#143159,#143160,#143161),.UNSPECIFIED.,.F.,.F.,(4,2,2,2,2,2,2,2,
4),(0.790275275739451,0.987666391168889,1.18505750659833,1.38280402903861,
1.5805505514789,1.77829707391919,1.97604359635948,2.17343471178892,2.37082582721835),
 .UNSPECIFIED.);
#4188=B_SPLINE_CURVE_WITH_KNOTS('',3,(#143162,#143163,#143164,#143165,#143166,
#143167,#143168,#143169,#143170,#143171,#143172,#143173,#143174,#143175,
#143176,#143177,#143178,#143179),.UNSPECIFIED.,.F.,.F.,(4,2,2,2,2,2,2,2,
4),(3.99684375481044,4.19616799981279,4.39549224481514,4.59585237529384,
4.79621250577253,4.99657263625123,5.19693276672992,5.39625701173227,5.59558125673462),
 .UNSPECIFIED.);
#4189=B_SPLINE_CURVE_WITH_KNOTS('',3,(#144268,#144269,#144270,#144271,#144272,
#144273,#144274,#144275,#144276,#144277,#144278,#144279,#144280,#144281,
#144282,#144283,#144284,#144285,#144286,#144287,#144288,#144289,#144290,
#144291,#144292,#144293),.UNSPECIFIED.,.F.,.F.,(4,2,2,2,2,2,2,2,2,2,2,2,
4),(-13.8814766639242,-12.963099391817,-11.6984193910095,-10.4333774964113,
-9.16809598401541,-7.90278570433247,-6.63757145246671,-5.37278587819109,
-4.10915141819608,-2.84701293295869,-1.58416264486531,-0.792436008190626,
0.),.UNSPECIFIED.);
#4190=B_SPLINE_CURVE_WITH_KNOTS('',3,(#144299,#144300,#144301,#144302,#144303,
#144304,#144305,#144306,#144307,#144308,#144309,#144310,#144311,#144312,
#144313,#144314,#144315,#144316),.UNSPECIFIED.,.F.,.F.,(4,2,2,2,2,2,2,2,
4),(0.784365106334379,0.980404435697066,1.17644376505975,1.37258698886426,
1.56873021266876,1.76487343647326,1.96101666027776,2.15705598964045,2.35309531900314),
 .UNSPECIFIED.);
#4191=B_SPLINE_CURVE_WITH_KNOTS('',3,(#144319,#144320,#144321,#144322,#144323,
#144324,#144325,#144326,#144327,#144328,#144329,#144330,#144331,#144332,
#144333,#144334,#144335,#144336),.UNSPECIFIED.,.F.,.F.,(4,2,2,2,2,2,2,2,
4),(1.56873021266875,1.76487343647325,1.96101666027775,2.15705598964044,
2.35309531900312,2.54913464836581,2.74517397772849,2.94131720153299,3.1374604253375),
 .UNSPECIFIED.);
#4192=B_SPLINE_CURVE_WITH_KNOTS('',3,(#144337,#144338,#144339,#144340,#144341,
#144342,#144343,#144344,#144345,#144346,#144347,#144348,#144349,#144350,
#144351,#144352,#144353,#144354),.UNSPECIFIED.,.F.,.F.,(4,2,2,2,2,2,2,2,
4),(3.1374604253375,3.333603649142,3.5297468729465,3.72578620230918,3.92182553167187,
4.11786486103455,4.31390419039724,4.51004741420174,4.70619063800624),
 .UNSPECIFIED.);
#4193=B_SPLINE_CURVE_WITH_KNOTS('',3,(#144357,#144358,#144359,#144360,#144361,
#144362,#144363,#144364,#144365,#144366,#144367,#144368,#144369,#144370,
#144371,#144372,#144373,#144374),.UNSPECIFIED.,.F.,.F.,(4,2,2,2,2,2,2,2,
4),(-1.56873021266875,-1.37258698886425,-1.17644376505974,-0.980404435697059,
-0.784365106334374,-0.588325776971689,-0.392286447609003,-0.196143223804502,
0.),.UNSPECIFIED.);
#4194=B_SPLINE_CURVE_WITH_KNOTS('',3,(#144375,#144376,#144377,#144378,#144379,
#144380,#144381,#144382,#144383,#144384,#144385,#144386,#144387,#144388,
#144389,#144390,#144391,#144392),.UNSPECIFIED.,.F.,.F.,(4,2,2,2,2,2,2,2,
4),(0.,0.196143223804502,0.392286447609004,0.588325776971689,0.784365106334374,
0.980404435697059,1.17644376505974,1.37258698886425,1.56873021266875),
 .UNSPECIFIED.);
#4195=B_SPLINE_CURVE_WITH_KNOTS('',3,(#144397,#144398,#144399,#144400,#144401,
#144402,#144403,#144404,#144405,#144406,#144407,#144408,#144409,#144410,
#144411,#144412,#144413,#144414,#144415,#144416,#144417,#144418,#144419,
#144420,#144421,#144422),.UNSPECIFIED.,.F.,.F.,(4,2,2,2,2,2,2,2,2,2,2,2,
4),(-27.7692554578402,-26.8737799915245,-25.608769554275,-24.3432221416514,
-23.0773813467393,-21.8113780103894,-20.5453898616053,-19.2795959206261,
-18.014467770055,-16.7509292170372,-15.4895459533869,-14.2270583969213,
-13.8814766639242),.UNSPECIFIED.);
#4196=B_SPLINE_CURVE_WITH_KNOTS('',3,(#144423,#144424,#144425,#144426,#144427,
#144428,#144429,#144430,#144431,#144432,#144433,#144434,#144435,#144436,
#144437,#144438,#144439,#144440,#144441),.UNSPECIFIED.,.F.,.F.,(4,2,2,2,
3,2,2,2,4),(2.35309531900314,2.54913464836582,2.74517397772851,2.94131720153301,
3.13746042533751,3.33360364914202,3.52974687294652,3.72578620230921,3.92182553167189),
 .UNSPECIFIED.);
#4197=B_SPLINE_CURVE_WITH_KNOTS('',3,(#144442,#144443,#144444,#144445,#144446,
#144447,#144448,#144449,#144450,#144451,#144452,#144453,#144454,#144455,
#144456,#144457,#144458,#144459,#144460,#144461,#144462,#144463,#144464,
#144465,#144466,#144467),.UNSPECIFIED.,.F.,.F.,(4,2,2,2,2,2,2,2,2,2,2,2,
4),(-104.015874542983,-103.240957296345,-102.466440663735,-101.207072089471,
-99.9489235979378,-98.6882843547007,-97.425630439723,-96.1620642931025,
-94.8981892506107,-93.6342617969183,-92.3704234079043,-91.1068430913151,
-90.1604031166725),.UNSPECIFIED.);
#4198=B_SPLINE_CURVE_WITH_KNOTS('',3,(#144470,#144471,#144472,#144473,#144474,
#144475,#144476,#144477,#144478,#144479,#144480,#144481,#144482,#144483,
#144484,#144485,#144486,#144487,#144488),.UNSPECIFIED.,.F.,.F.,(4,2,2,2,
3,2,2,2,4),(-0.784365106334379,-0.588325776971691,-0.392286447609004,-0.196143223804502,
0.,0.196143223804502,0.392286447609004,0.588325776971692,0.784365106334379),
 .UNSPECIFIED.);
#4199=B_SPLINE_CURVE_WITH_KNOTS('',3,(#144489,#144490,#144491,#144492,#144493,
#144494,#144495,#144496,#144497,#144498,#144499,#144500,#144501,#144502,
#144503,#144504,#144505,#144506),.UNSPECIFIED.,.F.,.F.,(4,2,2,2,2,2,2,2,
4),(0.784365106334379,0.980404435697066,1.17644376505975,1.37258698886426,
1.56873021266876,1.76487343647326,1.96101666027776,2.15705598964045,2.35309531900314),
 .UNSPECIFIED.);
#4200=B_SPLINE_CURVE_WITH_KNOTS('',3,(#144511,#144512,#144513,#144514,#144515,
#144516,#144517,#144518,#144519,#144520,#144521,#144522,#144523,#144524,
#144525,#144526,#144527,#144528,#144529,#144530,#144531,#144532,#144533,
#144534,#144535,#144536),.UNSPECIFIED.,.F.,.F.,(4,2,2,2,2,2,2,2,2,2,2,2,
4),(-41.6372629980801,-40.7664022234293,-39.5041738810512,-38.2411203720136,
-36.9776617236179,-35.7139513451538,-34.4501697796324,-33.1864522471623,
-31.9230767454262,-30.6606810056365,-29.3994174888209,-28.1376783293277,
-27.7692554578402),.UNSPECIFIED.);
#4201=B_SPLINE_CURVE_WITH_KNOTS('',3,(#144537,#144538,#144539,#144540,#144541,
#144542,#144543,#144544,#144545,#144546,#144547,#144548,#144549,#144550,
#144551,#144552,#144553,#144554,#144555,#144556,#144557,#144558,#144559,
#144560,#144561,#144562),.UNSPECIFIED.,.F.,.F.,(4,2,2,2,2,2,2,2,2,2,2,2,
4),(-90.1604031166725,-89.8436895134744,-88.5814107402185,-87.3208827048715,
-86.0612546066959,-84.7998510025023,-83.537157629253,-82.2739624099999,
-81.0106422304456,-79.7473270963416,-78.4842338503542,-77.2214744103415,
-76.2990316115284),.UNSPECIFIED.);
#4202=B_SPLINE_CURVE_WITH_KNOTS('',3,(#144567,#144568,#144569,#144570,#144571,
#144572,#144573,#144574,#144575,#144576,#144577,#144578,#144579,#144580,
#144581,#144582,#144583,#144584,#144585,#144586,#144587,#144588,#144589,
#144590,#144591,#144592),.UNSPECIFIED.,.F.,.F.,(4,2,2,2,2,2,2,2,2,2,2,2,
4),(-55.4993512071467,-54.6513921073566,-53.3902342683282,-52.1278116316948,
-50.8647759569511,-49.6014201273275,-48.3378604563596,-47.0743011025923,
-45.8108853500451,-44.5480169787744,-43.2865230918552,-42.0269684623869,
-41.6372629980801),.UNSPECIFIED.);
#4203=B_SPLINE_CURVE_WITH_KNOTS('',3,(#144593,#144594,#144595,#144596,#144597,
#144598,#144599,#144600,#144601,#144602,#144603,#144604,#144605,#144606,
#144607,#144608,#144609,#144610,#144611,#144612,#144613,#144614,#144615,
#144616,#144617,#144618),.UNSPECIFIED.,.F.,.F.,(4,2,2,2,2,2,2,2,2,2,2,2,
4),(-76.2990316115284,-75.9593645087416,-74.6985903757287,-73.4389646676771,
-72.177047042093,-70.9133659385421,-69.6489198280436,-68.3842346083183,
-67.1195201876227,-65.85493675867,-64.5906295488055,-63.3268076944692,-62.4266886913099),
 .UNSPECIFIED.);
#4204=B_SPLINE_CURVE_WITH_KNOTS('',3,(#144623,#144624,#144625,#144626,#144627,
#144628,#144629,#144630,#144631,#144632,#144633,#144634,#144635,#144636,
#144637,#144638,#144639,#144640,#144641,#144642,#144643,#144644,#144645,
#144646,#144647,#144648),.UNSPECIFIED.,.F.,.F.,(4,2,2,2,2,2,2,2,2,2,2,2,
4),(-69.3801191133633,-68.5536951873574,-67.292001693102,-66.0284301208769,
-64.7639112991888,-63.4989332139754,-62.2336870563708,-60.9683277594848,
-59.7030069572755,-58.4379539740317,-57.1737276963798,-55.9113714686727,
-55.4993512071467),.UNSPECIFIED.);
#4205=B_SPLINE_CURVE_WITH_KNOTS('',3,(#144649,#144650,#144651,#144652,#144653,
#144654,#144655,#144656,#144657,#144658,#144659,#144660,#144661,#144662,
#144663,#144664,#144665,#144666,#144667,#144668,#144669,#144670,#144671,
#144672,#144673,#144674),.UNSPECIFIED.,.F.,.F.,(4,2,2,2,2,2,2,2,2,2,2,2,
4),(-62.4266886913099,-62.0639896504061,-60.8031471476672,-59.5429544790536,
-58.281360404511,-57.0186615159492,-55.7555575129026,-54.4923663240911,
-53.2292146600348,-51.9663050678705,-50.7032610542343,-49.4407596448874,
-48.5661368651097),.UNSPECIFIED.);
#4206=B_SPLINE_CURVE_WITH_KNOTS('',3,(#144679,#144680,#144681,#144682,#144683,
#144684,#144685,#144686,#144687,#144688,#144689,#144690,#144691,#144692,
#144693,#144694,#144695,#144696,#144697,#144698,#144699,#144700,#144701,
#144702,#144703,#144704),.UNSPECIFIED.,.F.,.F.,(4,2,2,2,2,2,2,2,2,2,2,2,
4),(-83.2500328628607,-82.4481533960685,-81.1876171552324,-79.9253065699082,
-78.6617065326316,-77.3976049520614,-76.1333785891597,-74.8691703087574,
-73.6049410691841,-72.3408142660145,-71.0771325954068,-69.8146334354338,
-69.3801191133633),.UNSPECIFIED.);
#4207=B_SPLINE_CURVE_WITH_KNOTS('',3,(#144705,#144706,#144707,#144708,#144709,
#144710,#144711,#144712,#144713,#144714,#144715,#144716,#144717,#144718,
#144719,#144720,#144721,#144722,#144723,#144724,#144725,#144726,#144727,
#144728,#144729,#144730),.UNSPECIFIED.,.F.,.F.,(4,2,2,2,2,2,2,2,2,2,2,2,
4),(-48.5661368651097,-48.1796237958336,-46.9204103396194,-45.6601967379575,
-44.3983128950498,-43.1355993319228,-41.8724786857766,-40.6091057824071,
-39.3456599380502,-38.082276908884,-36.8192324431946,-35.5571606562185,
-34.7056572650582),.UNSPECIFIED.);
#4208=B_SPLINE_CURVE_WITH_KNOTS('',3,(#144735,#144736,#144737,#144738,#144739,
#144740,#144741,#144742,#144743,#144744,#144745,#144746,#144747,#144748,
#144749,#144750,#144751,#144752,#144753,#144754,#144755,#144756,#144757,
#144758,#144759,#144760),.UNSPECIFIED.,.F.,.F.,(4,2,2,2,2,2,2,2,2,2,2,2,
4),(-97.1232537091924,-96.3443719127046,-95.0853105232451,-93.8237579151547,
-92.5601908545606,-91.295711898233,-90.0309243056691,-88.7660844304284,
-87.5013339520407,-86.2368418327317,-84.9727770982929,-83.7095885668981,
-83.2500328628607),.UNSPECIFIED.);
#4209=B_SPLINE_CURVE_WITH_KNOTS('',3,(#144761,#144762,#144763,#144764,#144765,
#144766,#144767,#144768,#144769,#144770,#144771,#144772,#144773,#144774,
#144775,#144776,#144777,#144778,#144779,#144780,#144781,#144782,#144783,
#144784,#144785,#144786),.UNSPECIFIED.,.F.,.F.,(4,2,2,2,2,2,2,2,2,2,2,2,
4),(-34.7056572650582,-34.2962056922594,-33.0347847958924,-31.771194527919,
-30.5064860259869,-29.2412375641598,-27.9756947285637,-26.7099875939099,
-25.4442949200012,-24.1787940187062,-22.9139533339695,-21.6506922260116,
-20.8210363596471),.UNSPECIFIED.);
#4210=B_SPLINE_CURVE_WITH_KNOTS('',3,(#144791,#144792,#144793,#144794,#144795,
#144796,#144797,#144798,#144799,#144800,#144801,#144802,#144803,#144804,
#144805,#144806,#144807,#144808,#144809,#144810,#144811,#144812,#144813,
#144814,#144815,#144816),.UNSPECIFIED.,.F.,.F.,(4,2,2,2,2,2,2,2,2,2,2,2,
4),(-110.967977009243,-109.972570106527,-108.957916406404,-107.699758598375,
-106.439527248507,-105.177806722715,-103.915475803826,-102.652974563524,
-101.390465164933,-100.128136116833,-98.8661109187615,-97.6046537650016,
-97.1232537091924),.UNSPECIFIED.);
#4211=B_SPLINE_CURVE_WITH_KNOTS('',3,(#144817,#144818,#144819,#144820,#144821,
#144822,#144823,#144824,#144825,#144826,#144827,#144828,#144829,#144830,
#144831,#144832,#144833,#144834,#144835,#144836,#144837,#144838,#144839,
#144840,#144841,#144842),.UNSPECIFIED.,.F.,.F.,(4,2,2,2,2,2,2,2,2,2,2,2,
4),(-20.8210363596471,-20.3895782821617,-19.1273626285183,-17.863667873144,
-16.5992480081042,-15.3344646086074,-14.0694411584903,-12.8043870765627,
-11.5394274728486,-10.2748924628399,-9.01150060417685,-7.74958849211455,
-6.94140314827258),.UNSPECIFIED.);
#4212=B_SPLINE_CURVE_WITH_KNOTS('',3,(#144848,#144849,#144850,#144851,#144852,
#144853,#144854,#144855,#144856,#144857,#144858,#144859,#144860,#144861,
#144862,#144863,#144864,#144865,#144866,#144867,#144868,#144869,#144870,
#144871,#144872,#144873),.UNSPECIFIED.,.F.,.F.,(4,2,2,2,2,2,2,2,2,2,2,2,
4),(192.908593634536,193.053216493834,194.838241605474,196.624309799068,
198.409265218689,200.19376370034,201.978838598696,203.764512861769,205.549513185926,
207.334220267435,209.119842173418,210.904778060657,212.697004771953),
 .UNSPECIFIED.);
#4213=B_SPLINE_CURVE_WITH_KNOTS('',3,(#144876,#144877,#144878,#144879,#144880,
#144881,#144882,#144883,#144884,#144885,#144886,#144887,#144888,#144889,
#144890,#144891,#144892,#144893,#144894,#144895,#144896,#144897,#144898,
#144899),.UNSPECIFIED.,.F.,.F.,(4,2,2,2,2,2,2,2,2,2,2,4),(9.99999989108212E-7,
1.6769694808229,3.35394573760072,5.14001215222226,6.92611120726754,8.71152346455622,
10.4972993356259,12.2838558739946,14.0693244115025,15.8542458178252,17.6397062809234,
18.9650896985654),.UNSPECIFIED.);
#4214=B_SPLINE_CURVE_WITH_KNOTS('',3,(#144904,#144905,#144906,#144907,#144908,
#144909,#144910,#144911,#144912,#144913,#144914,#144915,#144916,#144917,
#144918,#144919,#144920,#144921,#144922,#144923,#144924,#144925,#144926,
#144927,#144928,#144929,#144930,#144931,#144932,#144933,#144934,#144935),
 .UNSPECIFIED.,.F.,.F.,(4,2,2,2,2,2,2,2,2,2,2,2,2,2,2,4),(166.298715258511,
168.062704889159,169.846980296724,171.632329207268,173.416900833311,175.201110861311,
176.986013726065,178.770866342029,180.555131335309,182.339939547942,184.126158497811,
185.911539890777,187.696514469877,189.482090107986,191.267970458966,192.908593634536),
 .UNSPECIFIED.);
#4215=B_SPLINE_CURVE_WITH_KNOTS('',3,(#144936,#144937,#144938,#144939,#144940,
#144941,#144942,#144943,#144944,#144945,#144946,#144947,#144948,#144949,
#144950,#144951,#144952,#144953,#144954,#144955,#144956,#144957,#144958,
#144959,#144960,#144961,#144962,#144963,#144964,#144965,#144966,#144967,
#144968,#144969),.UNSPECIFIED.,.F.,.F.,(4,2,2,2,2,2,2,2,2,2,2,2,2,2,2,2,
4),(18.9650896985654,19.425618542153,21.2106941659649,22.996095123781,24.7822019761817,
26.5675394095681,28.3523130129014,30.137572813644,31.9237070575206,33.7088671994476,
35.4942868404638,37.2803639611839,39.0659738961904,40.850996381668,42.6364531786856,
44.4232157048341,45.5834444085454),.UNSPECIFIED.);
#4216=B_SPLINE_CURVE_WITH_KNOTS('',3,(#144974,#144975,#144976,#144977,#144978,
#144979,#144980,#144981,#144982,#144983,#144984,#144985,#144986,#144987,
#144988,#144989,#144990,#144991,#144992,#144993,#144994,#144995,#144996,
#144997,#144998,#144999,#145000,#145001,#145002,#145003,#145004,#145005,
#145006,#145007),.UNSPECIFIED.,.F.,.F.,(4,2,2,2,2,2,2,2,2,2,2,2,2,2,2,2,
4),(139.698460362937,141.298680190492,143.082542874683,144.866993668424,
146.651898927764,148.436148802202,150.220142419869,152.00511492784,153.789195633697,
155.572792685623,157.35695409508,159.141871394973,160.926086686371,162.709978269322,
164.494712074918,166.278976729113,166.298715258511),.UNSPECIFIED.);
#4217=B_SPLINE_CURVE_WITH_KNOTS('',3,(#145008,#145009,#145010,#145011,#145012,
#145013,#145014,#145015,#145016,#145017,#145018,#145019,#145020,#145021,
#145022,#145023,#145024,#145025,#145026,#145027,#145028,#145029,#145030,
#145031,#145032,#145033,#145034,#145035,#145036,#145037,#145038,#145039,
#145040,#145041),.UNSPECIFIED.,.F.,.F.,(4,2,2,2,2,2,2,2,2,2,2,2,2,2,2,2,
4),(45.5834444085454,46.2088841699579,47.9947463716619,49.7812231812246,
51.5675223476345,53.3532100307112,55.1392838945247,56.9261710618272,58.7117996117417,
60.496884827521,62.2825356237994,64.0684233445439,65.853549939962,67.6390203919217,
69.4252366706261,71.2113397224562,72.2052309313631),.UNSPECIFIED.);
#4218=B_SPLINE_CURVE_WITH_KNOTS('',3,(#145046,#145047,#145048,#145049,#145050,
#145051,#145052,#145053,#145054,#145055,#145056,#145057,#145058,#145059,
#145060,#145061,#145062,#145063,#145064,#145065,#145066,#145067,#145068,
#145069,#145070,#145071,#145072,#145073,#145074,#145075,#145076,#145077,
#145078,#145079),.UNSPECIFIED.,.F.,.F.,(4,2,2,2,2,2,2,2,2,2,2,2,2,2,2,2,
4),(113.09235101392,114.52775166222,116.312097574426,118.096101456626,119.880872306608,
121.665388745755,123.449342109569,125.23383862757,127.019578752594,128.804508600531,
130.589054425226,132.374213279577,134.15953667438,135.944247806099,137.728767737168,
139.514385601497,139.698460362937),.UNSPECIFIED.);
#4219=B_SPLINE_CURVE_WITH_KNOTS('',3,(#145080,#145081,#145082,#145083,#145084,
#145085,#145086,#145087,#145088,#145089,#145090,#145091,#145092,#145093,
#145094,#145095,#145096,#145097,#145098,#145099,#145100,#145101,#145102,
#145103,#145104,#145105,#145106,#145107,#145108,#145109,#145110,#145111,
#145112,#145113),.UNSPECIFIED.,.F.,.F.,(4,2,2,2,2,2,2,2,2,2,2,2,2,2,2,2,
4),(72.2052309313631,72.9965317100158,74.7812420564402,76.5665180619611,
78.3525368904608,80.1378568580769,81.9228543667527,83.7087009217182,85.49405960617,
87.2788837652769,89.0642560350252,90.8506881535951,92.6363455201069,94.421642900023,
96.2076402994364,97.9935690491882,98.8223876750889),.UNSPECIFIED.);
#4220=B_SPLINE_CURVE_WITH_KNOTS('',3,(#145118,#145119,#145120,#145121,#145122,
#145123,#145124,#145125,#145126,#145127,#145128,#145129,#145130,#145131,
#145132,#145133,#145134,#145135,#145136,#145137,#145138,#145139,#145140,
#145141,#145142,#145143,#145144,#145145,#145146,#145147,#145148,#145149,
#145150,#145151),.UNSPECIFIED.,.F.,.F.,(4,2,2,2,2,2,2,2,2,2,2,2,2,2,2,2,
4),(86.4916057697223,87.7620179914404,89.5470742844118,91.3314954032844,
93.1156939706259,94.9009319839527,96.6850691658659,98.4687482426107,100.253002836542,
102.037864510603,103.822051617035,105.605943517478,107.390746196952,109.174874371702,
110.958491782147,112.74266354629,113.09235101392),.UNSPECIFIED.);
#4221=B_SPLINE_CURVE_WITH_KNOTS('',3,(#145152,#145153,#145154,#145155,#145156,
#145157,#145158,#145159,#145160,#145161,#145162,#145163,#145164,#145165,
#145166,#145167,#145168,#145169,#145170,#145171,#145172,#145173,#145174,
#145175,#145176,#145177,#145178,#145179,#145180,#145181,#145182,#145183,
#145184,#145185),.UNSPECIFIED.,.F.,.F.,(4,2,2,2,2,2,2,2,2,2,2,2,2,2,2,2,
4),(98.8223876750889,99.778911980072,101.564798285203,103.352080954802,
105.138527824139,106.924569725461,108.711214082261,110.498150768372,112.284454663544,
114.070540322883,115.857674832274,117.643677117955,119.429224455379,121.215349595913,
123.002061348891,124.78810032242,125.451829625253),.UNSPECIFIED.);
#4222=B_SPLINE_CURVE_WITH_KNOTS('',3,(#145190,#145191,#145192,#145193,#145194,
#145195,#145196,#145197,#145198,#145199,#145200,#145201,#145202,#145203,
#145204,#145205,#145206,#145207,#145208,#145209,#145210,#145211,#145212,
#145213,#145214,#145215,#145216,#145217,#145218,#145219,#145220,#145221,
#145222,#145223),.UNSPECIFIED.,.F.,.F.,(4,2,2,2,2,2,2,2,2,2,2,2,2,2,2,2,
4),(59.8786188341278,60.9848711462809,62.7699607377911,64.5544747957343,
66.3394477240105,68.1255174331873,69.9105484752843,71.695958346319,73.4810053395191,
75.2667414148746,77.0524382847678,78.8375459582976,80.6224879685026,82.408578192017,
84.1931300109447,85.9772739287588,86.4916057697223),.UNSPECIFIED.);
#4223=B_SPLINE_CURVE_WITH_KNOTS('',3,(#145224,#145225,#145226,#145227,#145228,
#145229,#145230,#145231,#145232,#145233,#145234,#145235,#145236,#145237,
#145238,#145239,#145240,#145241,#145242,#145243,#145244,#145245,#145246,
#145247,#145248,#145249,#145250,#145251,#145252,#145253,#145254,#145255,
#145256,#145257),.UNSPECIFIED.,.F.,.F.,(4,2,2,2,2,2,2,2,2,2,2,2,2,2,2,2,
4),(125.451829625253,126.573849309195,128.360519589848,130.146485042424,
131.931942914064,133.71795694799,135.504866056864,137.29103750207,139.076869212986,
140.863479157537,142.64980507424,144.435570928966,146.221880827012,148.009412023174,
149.796136365143,151.582479454181,152.081568540232),.UNSPECIFIED.);
#4224=B_SPLINE_CURVE_WITH_KNOTS('',3,(#145262,#145263,#145264,#145265,#145266,
#145267,#145268,#145269,#145270,#145271,#145272,#145273,#145274,#145275,
#145276,#145277,#145278,#145279,#145280,#145281,#145282,#145283,#145284,
#145285,#145286,#145287,#145288,#145289,#145290,#145291,#145292,#145293,
#145294,#145295),.UNSPECIFIED.,.F.,.F.,(4,2,2,2,2,2,2,2,2,2,2,2,2,2,2,2,
4),(33.2649250020999,34.2056820368628,35.9922701244673,37.777610445128,
39.5624073988762,41.3477682347804,43.1333791648598,44.9182243539491,46.7034121380009,
48.4893432713056,50.2743542552732,52.0588108074829,53.8437789249438,55.6294173890104,
57.4141460993981,59.1991709946284,59.8786188341278),.UNSPECIFIED.);
#4225=B_SPLINE_CURVE_WITH_KNOTS('',3,(#145296,#145297,#145298,#145299,#145300,
#145301,#145302,#145303,#145304,#145305,#145306,#145307,#145308,#145309,
#145310,#145311,#145312,#145313,#145314,#145315,#145316,#145317,#145318,
#145319,#145320,#145321,#145322,#145323,#145324,#145325,#145326,#145327,
#145328,#145329),.UNSPECIFIED.,.F.,.F.,(4,2,2,2,2,2,2,2,2,2,2,2,2,2,2,2,
4),(152.081568540232,153.369447222936,155.156550264893,156.943043698927,
158.729349687956,160.516762242765,162.3028195186,164.088447986099,165.874666880246,
167.661320055741,169.44732000726,171.233068513856,173.019805839672,174.80562058442,
176.590954903103,178.376855652217,178.710809555564),.UNSPECIFIED.);
#4226=B_SPLINE_CURVE_WITH_KNOTS('',3,(#145334,#145335,#145336,#145337,#145338,
#145339,#145340,#145341,#145342,#145343,#145344,#145345,#145346,#145347,
#145348,#145349,#145350,#145351,#145352,#145353,#145354,#145355,#145356,
#145357,#145358,#145359,#145360,#145361,#145362,#145363,#145364,#145365,
#145366,#145367),.UNSPECIFIED.,.F.,.F.,(4,2,2,2,2,2,2,2,2,2,2,2,2,2,2,2,
4),(6.64837408914975,7.42331429784298,9.20825051621213,10.9940744495241,
12.7789203869486,14.5640234744708,16.3497826803808,18.135084081717,19.9197973552195,
21.7049432734423,23.491408467138,25.2767763535493,27.0623361352787,28.8485089624496,
30.6345131361714,32.4199052440002,33.2649250020999),.UNSPECIFIED.);
#4227=B_SPLINE_CURVE_WITH_KNOTS('',3,(#145368,#145369,#145370,#145371,#145372,
#145373,#145374,#145375,#145376,#145377,#145378,#145379,#145380,#145381,
#145382,#145383,#145384,#145385,#145386,#145387,#145388,#145389,#145390,
#145391,#145392,#145393,#145394,#145395,#145396,#145397,#145398,#145399,
#145400,#145401),.UNSPECIFIED.,.F.,.F.,(4,2,2,2,2,2,2,2,2,2,2,2,2,2,2,2,
4),(178.710809555564,180.163491400479,181.949430198385,183.7350472835,185.521517466646,
187.307488583991,189.092926368585,190.878912779111,192.665950859082,194.452215734871,
196.238121590287,198.024731740104,199.81126223008,201.597207998778,203.383697238931,
205.171574228893,205.339933575319),.UNSPECIFIED.);
#4228=B_SPLINE_CURVE_WITH_KNOTS('',3,(#145406,#145407,#145408,#145409,#145410,
#145411,#145412,#145413,#145414,#145415,#145416,#145417,#145418,#145419,
#145420,#145421,#145422,#145423),.UNSPECIFIED.,.F.,.F.,(4,2,2,2,2,2,2,2,
4),(0.,0.197658290162167,0.395316580324333,0.59263683604877,0.789957091773207,
0.987277347497643,1.18459760322208,1.38225589338425,1.57991418354641),
 .UNSPECIFIED.);
#4229=B_SPLINE_CURVE_WITH_KNOTS('',3,(#145424,#145425,#145426,#145427,#145428,
#145429,#145430,#145431,#145432,#145433,#145434,#145435,#145436,#145437,
#145438,#145439,#145440,#145441),.UNSPECIFIED.,.F.,.F.,(4,2,2,2,2,2,2,2,
4),(-1.57991418354641,-1.38225589338425,-1.18459760322208,-0.987277347497643,
-0.789957091773207,-0.59263683604877,-0.395316580324333,-0.197658290162167,
0.),.UNSPECIFIED.);
#4230=B_SPLINE_CURVE_WITH_KNOTS('',3,(#145445,#145446,#145447,#145448,#145449,
#145450,#145451,#145452,#145453,#145454,#145455,#145456,#145457,#145458,
#145459,#145460,#145461,#145462),.UNSPECIFIED.,.F.,.F.,(4,2,2,2,2,2,2,2,
4),(1.57991418354641,1.77757247370858,1.97523076387075,2.17255101959518,
2.36987127531962,2.56719153104406,2.76451178676849,2.96217007693066,3.15982836709283),
 .UNSPECIFIED.);
#4231=B_SPLINE_CURVE_WITH_KNOTS('',3,(#145464,#145465,#145466,#145467,#145468,
#145469,#145470,#145471,#145472,#145473,#145474,#145475,#145476,#145477,
#145478,#145479,#145480,#145481),.UNSPECIFIED.,.F.,.F.,(4,2,2,2,2,2,2,2,
4),(3.15982836709283,3.357486657255,3.55514494741716,3.7524652031416,3.94978545886604,
4.14710571459047,4.34442597031491,4.54208426047708,4.73974255063924),
 .UNSPECIFIED.);
#4232=B_SPLINE_CURVE_WITH_KNOTS('',3,(#145486,#145487,#145488,#145489,#145490,
#145491,#145492,#145493,#145494,#145495,#145496,#145497,#145498,#145499,
#145500,#145501,#145502,#145503,#145504),.UNSPECIFIED.,.F.,.F.,(4,2,2,2,
3,2,2,2,4),(-0.789957091773212,-0.592636836048773,-0.395316580324334,-0.197658290162167,
0.,0.197658290162167,0.395316580324334,0.592636836048773,0.789957091773212),
 .UNSPECIFIED.);
#4233=B_SPLINE_CURVE_WITH_KNOTS('',3,(#145505,#145506,#145507,#145508,#145509,
#145510,#145511,#145512,#145513,#145514,#145515,#145516,#145517,#145518,
#145519,#145520,#145521,#145522),.UNSPECIFIED.,.F.,.F.,(4,2,2,2,2,2,2,2,
4),(-2.36987127531964,-2.1725510195952,-1.97523076387076,-1.77757247370859,
-1.57991418354642,-1.38225589338426,-1.18459760322209,-0.987277347497651,
-0.789957091773212),.UNSPECIFIED.);
#4234=B_SPLINE_CURVE_WITH_KNOTS('',3,(#145526,#145527,#145528,#145529,#145530,
#145531,#145532,#145533,#145534,#145535,#145536,#145537,#145538,#145539,
#145540,#145541,#145542,#145543,#145544),.UNSPECIFIED.,.F.,.F.,(4,2,2,2,
3,2,2,2,4),(2.36987127531964,2.56719153104407,2.76451178676851,2.96217007693068,
3.15982836709285,3.35748665725501,3.55514494741718,3.75246520314162,3.94978545886606),
 .UNSPECIFIED.);
#4235=B_SPLINE_CURVE_WITH_KNOTS('',3,(#145546,#145547,#145548,#145549,#145550,
#145551,#145552,#145553,#145554,#145555,#145556,#145557,#145558,#145559,
#145560,#145561,#145562,#145563),.UNSPECIFIED.,.F.,.F.,(4,2,2,2,2,2,2,2,
4),(3.94978545886606,4.1471057145905,4.34442597031494,4.5420842604771,4.73974255063927,
4.93740084080144,5.13505913096361,5.33237938668804,5.52969964241248),
 .UNSPECIFIED.);
#4236=B_SPLINE_CURVE_WITH_KNOTS('',3,(#145566,#145567,#145568,#145569,#145570,
#145571,#145572,#145573,#145574,#145575),.UNSPECIFIED.,.F.,.F.,(4,2,2,2,
4),(205.339933575319,206.958616507017,208.745254927296,210.371885430349,
211.997838068529),.UNSPECIFIED.);
#4237=B_SPLINE_CURVE_WITH_KNOTS('',3,(#145578,#145579,#145580,#145581,#145582,
#145583,#145584,#145585,#145586,#145587,#145588,#145589),.UNSPECIFIED.,
 .F.,.F.,(4,2,2,2,2,4),(0.,1.03389160214753,2.06807064969959,3.85384635032225,
5.6388625243884,6.64837408914975),.UNSPECIFIED.);
#4238=B_SPLINE_CURVE_WITH_KNOTS('',3,(#145592,#145593,#145594,#145595,#145596,
#145597,#145598,#145599,#145600,#145601,#145602,#145603,#145604,#145605,
#145606,#145607),.UNSPECIFIED.,.F.,.F.,(4,2,2,2,2,2,2,4),(-6.94140314827258,
-6.4869752748672,-5.22243205186437,-3.95691169732814,-2.69091834975448,
-1.42465254456224,-0.71276813162599,0.),.UNSPECIFIED.);
#4239=B_SPLINE_CURVE_WITH_KNOTS('',3,(#145609,#145610,#145611,#145612,#145613,
#145614,#145615,#145616,#145617,#145618,#145619,#145620,#145621,#145622,
#145623,#145624,#145625,#145626,#145627,#145628,#145629,#145630,#145631,
#145632,#145633,#145634,#145635,#145636,#145637,#145638,#145639,#145640,
#145641,#145642,#145643,#145644,#145645,#145646,#145647,#145648,#145649,
#145650,#145651,#145652,#145653,#145654,#145655,#145656,#145657,#145658,
#145659,#145660,#145661,#145662,#145663,#145664,#145665,#145666,#145667,
#145668,#145669,#145670,#145671,#145672,#145673,#145674,#145675,#145676,
#145677,#145678,#145679,#145680,#145681,#145682,#145683,#145684,#145685,
#145686,#145687,#145688,#145689,#145690,#145691,#145692,#145693,#145694,
#145695,#145696,#145697,#145698,#145699,#145700,#145701,#145702,#145703,
#145704,#145705,#145706,#145707,#145708,#145709,#145710,#145711,#145712,
#145713,#145714,#145715,#145716,#145717,#145718,#145719,#145720,#145721,
#145722,#145723,#145724,#145725,#145726,#145727,#145728,#145729,#145730,
#145731,#145732,#145733,#145734,#145735,#145736,#145737,#145738,#145739,
#145740,#145741,#145742,#145743,#145744,#145745,#145746,#145747,#145748,
#145749,#145750,#145751,#145752,#145753,#145754,#145755,#145756,#145757,
#145758,#145759,#145760,#145761,#145762,#145763,#145764,#145765,#145766,
#145767,#145768,#145769,#145770,#145771,#145772,#145773,#145774,#145775,
#145776,#145777,#145778,#145779,#145780,#145781,#145782,#145783,#145784,
#145785,#145786,#145787,#145788,#145789,#145790,#145791,#145792,#145793,
#145794,#145795,#145796,#145797,#145798,#145799,#145800,#145801),
 .UNSPECIFIED.,.F.,.F.,(4,3,3,3,3,3,3,3,3,3,3,3,3,3,3,3,3,3,3,3,3,3,3,3,
3,3,3,3,3,3,3,3,3,3,3,3,3,3,3,3,3,3,3,3,3,3,3,3,3,3,3,3,3,3,3,3,3,3,3,3,
3,3,3,3,4),(0.25356579115215,0.253868242204076,0.254170595365822,0.254472068163607,
0.254559994575927,0.254862017366658,0.255174497215665,0.255486977064673,
0.25555456294769,0.25584417182401,0.256133884295542,0.256422820807404,0.256548943572741,
0.256837945950334,0.257127769386952,0.257408162977196,0.257543416604553,
0.257823699925624,0.258104255128538,0.258384192910332,0.258537766343908,
0.258817699141702,0.259098358149039,0.259329348889719,0.25953227603482,
0.259805885422422,0.260079864682975,0.260353333221958,0.260526494633499,
0.260800011386373,0.261074159864624,0.261250534802241,0.26152110805456,
0.261790065895994,0.262059439700215,0.262328354529141,0.262515160885892,
0.262784212260444,0.263053826468364,0.263171720714764,0.263438131643026,
0.263509893617797,0.263775819121753,0.264042173628218,0.264308080258592,
0.264503796454098,0.264769929002005,0.26503658597714,0.265092906627287,
0.265357824185491,0.265498626097877,0.265762894912191,0.266027586277107,
0.266291815112806,0.266492429976106,0.266757448196561,0.26701409253981,
0.267278657447202,0.267487309531408,0.267751167693691,0.268015432145765,
0.268279206795948,0.268481085740995,0.268745635122929,0.268935278452333),
 .UNSPECIFIED.);
#4240=B_SPLINE_CURVE_WITH_KNOTS('',3,(#145804,#145805,#145806,#145807),
 .UNSPECIFIED.,.F.,.F.,(4,4),(-110.988356064082,-110.967977009243),
 .UNSPECIFIED.);
#4241=B_SPLINE_CURVE_WITH_KNOTS('',3,(#154415,#154416,#154417,#154418,#154419,
#154420),.UNSPECIFIED.,.F.,.F.,(4,2,4),(9.99999997214368E-7,1.050385970465,
2.09906864072777),.UNSPECIFIED.);
#4242=B_SPLINE_CURVE_WITH_KNOTS('',3,(#162556,#162557,#162558,#162559,#162560,
#162561),.UNSPECIFIED.,.F.,.F.,(4,2,4),(0.,0.152399999790679,0.304800000000001),
 .UNSPECIFIED.);
#5461=SHAPE_REPRESENTATION_RELATIONSHIP('SRR','None',#276489,#5467);
#5467=ADVANCED_BREP_SHAPE_REPRESENTATION('',(#5502,#5503),#276457);
#5473=STYLED_ITEM('',(#276528),#5502);
#5474=STYLED_ITEM('',(#276528),#5503);
#5502=MANIFOLD_SOLID_BREP('Body1',#98698);
#5503=MANIFOLD_SOLID_BREP('Body2',#98699);
#5533=TOROIDAL_SURFACE('',#98876,9.25400000000018,0.254);
#5534=TOROIDAL_SURFACE('',#98881,11.0630000000002,0.254);
#6333=FACE_BOUND('',#13785,.T.);
#6334=FACE_BOUND('',#13786,.T.);
#6335=FACE_BOUND('',#13787,.T.);
#6336=FACE_BOUND('',#13789,.T.);
#6337=FACE_BOUND('',#13790,.T.);
#6338=FACE_BOUND('',#13791,.T.);
#6339=FACE_BOUND('',#13793,.T.);
#6340=FACE_BOUND('',#13795,.T.);
#6341=FACE_BOUND('',#13805,.T.);
#6342=FACE_BOUND('',#13806,.T.);
#6343=FACE_BOUND('',#13808,.T.);
#6344=FACE_BOUND('',#13830,.T.);
#6345=FACE_BOUND('',#13831,.T.);
#6346=FACE_BOUND('',#13832,.T.);
#6347=FACE_BOUND('',#13841,.T.);
#6348=FACE_BOUND('',#13843,.T.);
#6473=PLANE('',#98894);
#6474=PLANE('',#98895);
#6475=PLANE('',#98936);
#6476=PLANE('',#98937);
#6477=PLANE('',#98938);
#7657=FACE_OUTER_BOUND('',#13778,.T.);
#7658=FACE_OUTER_BOUND('',#13779,.T.);
#7659=FACE_OUTER_BOUND('',#13780,.T.);
#7660=FACE_OUTER_BOUND('',#13781,.T.);
#7661=FACE_OUTER_BOUND('',#13782,.T.);
#7662=FACE_OUTER_BOUND('',#13783,.T.);
#7663=FACE_OUTER_BOUND('',#13784,.T.);
#7664=FACE_OUTER_BOUND('',#13788,.T.);
#7665=FACE_OUTER_BOUND('',#13792,.T.);
#7666=FACE_OUTER_BOUND('',#13794,.T.);
#7667=FACE_OUTER_BOUND('',#13796,.T.);
#7668=FACE_OUTER_BOUND('',#13797,.T.);
#7669=FACE_OUTER_BOUND('',#13798,.T.);
#7670=FACE_OUTER_BOUND('',#13799,.T.);
#7671=FACE_OUTER_BOUND('',#13800,.T.);
#7672=FACE_OUTER_BOUND('',#13801,.T.);
#7673=FACE_OUTER_BOUND('',#13802,.T.);
#7674=FACE_OUTER_BOUND('',#13803,.T.);
#7675=FACE_OUTER_BOUND('',#13804,.T.);
#7676=FACE_OUTER_BOUND('',#13807,.T.);
#7677=FACE_OUTER_BOUND('',#13809,.T.);
#7678=FACE_OUTER_BOUND('',#13810,.T.);
#7679=FACE_OUTER_BOUND('',#13811,.T.);
#7680=FACE_OUTER_BOUND('',#13812,.T.);
#7681=FACE_OUTER_BOUND('',#13813,.T.);
#7682=FACE_OUTER_BOUND('',#13814,.T.);
#7683=FACE_OUTER_BOUND('',#13815,.T.);
#7684=FACE_OUTER_BOUND('',#13816,.T.);
#7685=FACE_OUTER_BOUND('',#13817,.T.);
#7686=FACE_OUTER_BOUND('',#13818,.T.);
#7687=FACE_OUTER_BOUND('',#13819,.T.);
#7688=FACE_OUTER_BOUND('',#13820,.T.);
#7689=FACE_OUTER_BOUND('',#13821,.T.);
#7690=FACE_OUTER_BOUND('',#13822,.T.);
#7691=FACE_OUTER_BOUND('',#13823,.T.);
#7692=FACE_OUTER_BOUND('',#13824,.T.);
#7693=FACE_OUTER_BOUND('',#13825,.T.);
#7694=FACE_OUTER_BOUND('',#13826,.T.);
#7695=FACE_OUTER_BOUND('',#13827,.T.);
#7696=FACE_OUTER_BOUND('',#13828,.T.);
#7697=FACE_OUTER_BOUND('',#13829,.T.);
#7698=FACE_OUTER_BOUND('',#13833,.T.);
#7699=FACE_OUTER_BOUND('',#13834,.T.);
#7700=FACE_OUTER_BOUND('',#13835,.T.);
#7701=FACE_OUTER_BOUND('',#13836,.T.);
#7702=FACE_OUTER_BOUND('',#13837,.T.);
#7703=FACE_OUTER_BOUND('',#13838,.T.);
#7704=FACE_OUTER_BOUND('',#13839,.T.);
#7705=FACE_OUTER_BOUND('',#13840,.T.);
#7706=FACE_OUTER_BOUND('',#13842,.T.);
#13778=EDGE_LOOP('',(#60625,#60626,#60627,#60628,#60629));
#13779=EDGE_LOOP('',(#60630,#60631,#60632,#60633,#60634));
#13780=EDGE_LOOP('',(#60635,#60636,#60637,#60638,#60639,#60640));
#13781=EDGE_LOOP('',(#60641,#60642,#60643,#60644,#60645,#60646));
#13782=EDGE_LOOP('',(#60647,#60648,#60649,#60650,#60651,#60652));
#13783=EDGE_LOOP('',(#60653,#60654,#60655,#60656,#60657,#60658));
#13784=EDGE_LOOP('',(#60659,#60660,#60661,#60662,#60663,#60664,#60665,#60666,
#60667));
#13785=EDGE_LOOP('',(#60668,#60669));
#13786=EDGE_LOOP('',(#60670,#60671));
#13787=EDGE_LOOP('',(#60672,#60673));
#13788=EDGE_LOOP('',(#60674,#60675,#60676,#60677,#60678,#60679,#60680,#60681,
#60682));
#13789=EDGE_LOOP('',(#60683,#60684));
#13790=EDGE_LOOP('',(#60685,#60686));
#13791=EDGE_LOOP('',(#60687,#60688));
#13792=EDGE_LOOP('',(#60689));
#13793=EDGE_LOOP('',(#60690));
#13794=EDGE_LOOP('',(#60691));
#13795=EDGE_LOOP('',(#60692));
#13796=EDGE_LOOP('',(#60693,#60694,#60695,#60696));
#13797=EDGE_LOOP('',(#60697,#60698,#60699,#60700));
#13798=EDGE_LOOP('',(#60701,#60702,#60703,#60704));
#13799=EDGE_LOOP('',(#60705,#60706,#60707,#60708));
#13800=EDGE_LOOP('',(#60709,#60710,#60711,#60712));
#13801=EDGE_LOOP('',(#60713,#60714,#60715,#60716));
#13802=EDGE_LOOP('',(#60717,#60718,#60719,#60720));
#13803=EDGE_LOOP('',(#60721,#60722,#60723,#60724));
#13804=EDGE_LOOP('',(#60725,#60726,#60727,#60728,#60729,#60730));
#13805=EDGE_LOOP('',(#60731,#60732));
#13806=EDGE_LOOP('',(#60733,#60734));
#13807=EDGE_LOOP('',(#60735,#60736,#60737,#60738,#60739,#60740));
#13808=EDGE_LOOP('',(#60741,#60742));
#13809=EDGE_LOOP('',(#60743,#60744,#60745,#60746));
#13810=EDGE_LOOP('',(#60747,#60748,#60749,#60750));
#13811=EDGE_LOOP('',(#60751,#60752,#60753,#60754));
#13812=EDGE_LOOP('',(#60755,#60756,#60757,#60758));
#13813=EDGE_LOOP('',(#60759,#60760,#60761,#60762));
#13814=EDGE_LOOP('',(#60763,#60764,#60765,#60766));
#13815=EDGE_LOOP('',(#60767,#60768,#60769,#60770));
#13816=EDGE_LOOP('',(#60771,#60772,#60773,#60774));
#13817=EDGE_LOOP('',(#60775,#60776,#60777,#60778));
#13818=EDGE_LOOP('',(#60779,#60780,#60781,#60782));
#13819=EDGE_LOOP('',(#60783,#60784,#60785,#60786));
#13820=EDGE_LOOP('',(#60787,#60788,#60789,#60790));
#13821=EDGE_LOOP('',(#60791,#60792,#60793,#60794));
#13822=EDGE_LOOP('',(#60795,#60796,#60797,#60798));
#13823=EDGE_LOOP('',(#60799,#60800,#60801,#60802,#60803,#60804));
#13824=EDGE_LOOP('',(#60805,#60806,#60807,#60808,#60809,#60810));
#13825=EDGE_LOOP('',(#60811,#60812,#60813,#60814,#60815,#60816));
#13826=EDGE_LOOP('',(#60817,#60818,#60819,#60820,#60821,#60822));
#13827=EDGE_LOOP('',(#60823,#60824,#60825,#60826));
#13828=EDGE_LOOP('',(#60827,#60828,#60829,#60830,#60831));
#13829=EDGE_LOOP('',(#60832,#60833,#60834,#60835,#60836,#60837,#60838,#60839));
#13830=EDGE_LOOP('',(#60840,#60841));
#13831=EDGE_LOOP('',(#60842,#60843));
#13832=EDGE_LOOP('',(#60844,#60845));
#13833=EDGE_LOOP('',(#60846,#60847,#60848,#60849,#60850,#60851,#60852,#60853,
#60854,#60855,#60856,#60857));
#13834=EDGE_LOOP('',(#60858,#60859,#60860,#60861,#60862,#60863,#60864,#60865,
#60866,#60867,#60868,#60869,#60870,#60871,#60872,#60873,#60874,#60875,#60876,
#60877));
#13835=EDGE_LOOP('',(#60878,#60879,#60880,#60881,#60882,#60883,#60884,#60885,
#60886,#60887,#60888,#60889,#60890,#60891,#60892,#60893,#60894,#60895,#60896,
#60897));
#13836=EDGE_LOOP('',(#60898,#60899,#60900,#60901,#60902,#60903,#60904,#60905,
#60906,#60907,#60908,#60909));
#13837=EDGE_LOOP('',(#60910,#60911,#60912,#60913));
#13838=EDGE_LOOP('',(#60914,#60915,#60916,#60917));
#13839=EDGE_LOOP('',(#60918,#60919,#60920,#60921,#60922,#60923,#60924,#60925));
#13840=EDGE_LOOP('',(#60926));
#13841=EDGE_LOOP('',(#60927));
#13842=EDGE_LOOP('',(#60928,#60929,#60930,#60931,#60932,#60933,#60934,#60935));
#13843=EDGE_LOOP('',(#60936));
#20030=LINE('',#142886,#25257);
#20031=LINE('',#142964,#25258);
#20032=LINE('',#143043,#25259);
#20033=LINE('',#143123,#25260);
#20034=LINE('',#143183,#25261);
#20035=LINE('',#143184,#25262);
#20036=LINE('',#143186,#25263);
#20037=LINE('',#143188,#25264);
#20038=LINE('',#143195,#25265);
#20039=LINE('',#143233,#25266);
#20040=LINE('',#143272,#25267);
#20041=LINE('',#143414,#25268);
#20042=LINE('',#143556,#25269);
#20043=LINE('',#143698,#25270);
#20044=LINE('',#143840,#25271);
#20045=LINE('',#143982,#25272);
#20046=LINE('',#144124,#25273);
#20047=LINE('',#144266,#25274);
#20048=LINE('',#144296,#25275);
#20049=LINE('',#144298,#25276);
#20050=LINE('',#144396,#25277);
#20051=LINE('',#144510,#25278);
#20052=LINE('',#144566,#25279);
#20053=LINE('',#144622,#25280);
#20054=LINE('',#144678,#25281);
#20055=LINE('',#144734,#25282);
#20056=LINE('',#144790,#25283);
#20057=LINE('',#144846,#25284);
#20058=LINE('',#144903,#25285);
#20059=LINE('',#144973,#25286);
#20060=LINE('',#145045,#25287);
#20061=LINE('',#145117,#25288);
#20062=LINE('',#145189,#25289);
#20063=LINE('',#145261,#25290);
#20064=LINE('',#145333,#25291);
#20065=LINE('',#145404,#25292);
#20066=LINE('',#145463,#25293);
#20067=LINE('',#145484,#25294);
#20068=LINE('',#145545,#25295);
#20069=LINE('',#145577,#25296);
#20070=LINE('',#145811,#25297);
#20071=LINE('',#145813,#25298);
#20072=LINE('',#150387,#25299);
#20073=LINE('',#154421,#25300);
#20074=LINE('',#158490,#25301);
#20075=LINE('',#158528,#25302);
#20076=LINE('',#162563,#25303);
#20077=LINE('',#167138,#25304);
#25257=VECTOR('',#111915,5.15937500000002);
#25258=VECTOR('',#111918,5.15937500000002);
#25259=VECTOR('',#111921,5.15937500000008);
#25260=VECTOR('',#111924,5.15937500000008);
#25261=VECTOR('',#111929,11.3170000000002);
#25262=VECTOR('',#111930,11.3170000000002);
#25263=VECTOR('',#111933,9.00000000000018);
#25264=VECTOR('',#111934,9.00000000000018);
#25265=VECTOR('',#111943,18.0480000000001);
#25266=VECTOR('',#111944,10.);
#25267=VECTOR('',#111947,18.0480000000001);
#25268=VECTOR('',#111950,18.0480000000001);
#25269=VECTOR('',#111953,18.0480000000001);
#25270=VECTOR('',#111956,18.0480000000001);
#25271=VECTOR('',#111959,18.0480000000001);
#25272=VECTOR('',#111962,18.0480000000001);
#25273=VECTOR('',#111965,18.0480000000001);
#25274=VECTOR('',#111968,15.);
#25275=VECTOR('',#111971,10.);
#25276=VECTOR('',#111972,15.);
#25277=VECTOR('',#111975,15.);
#25278=VECTOR('',#111978,15.);
#25279=VECTOR('',#111981,15.);
#25280=VECTOR('',#111984,15.);
#25281=VECTOR('',#111987,15.);
#25282=VECTOR('',#111990,15.);
#25283=VECTOR('',#111993,15.);
#25284=VECTOR('',#111996,39.);
#25285=VECTOR('',#112001,39.);
#25286=VECTOR('',#112004,39.);
#25287=VECTOR('',#112007,39.);
#25288=VECTOR('',#112010,39.);
#25289=VECTOR('',#112013,39.);
#25290=VECTOR('',#112016,39.);
#25291=VECTOR('',#112019,39.);
#25292=VECTOR('',#112022,5.15937500000002);
#25293=VECTOR('',#112025,5.15937500000002);
#25294=VECTOR('',#112028,5.15937500000008);
#25295=VECTOR('',#112031,5.15937500000008);
#25296=VECTOR('',#112034,1000.);
#25297=VECTOR('',#112043,11.444);
#25298=VECTOR('',#112044,11.444);
#25299=VECTOR('',#112049,10.);
#25300=VECTOR('',#112050,10.);
#25301=VECTOR('',#112051,10.);
#25302=VECTOR('',#112052,10.);
#25303=VECTOR('',#112053,10.);
#25304=VECTOR('',#112056,10.);
#30440=CIRCLE('',#98877,9.00000000000018);
#30441=CIRCLE('',#98878,9.00000000000018);
#30442=CIRCLE('',#98879,0.254);
#30443=CIRCLE('',#98880,9.25400000000018);
#30444=CIRCLE('',#98882,11.0630000000002);
#30445=CIRCLE('',#98883,0.254);
#30446=CIRCLE('',#98884,11.3170000000002);
#30447=CIRCLE('',#98885,11.3170000000002);
#30448=CIRCLE('',#98891,11.3170000000002);
#30449=CIRCLE('',#98893,9.00000000000017);
#30450=CIRCLE('',#98905,15.0000000000002);
#30451=CIRCLE('',#98914,39.);
#30452=CIRCLE('',#98928,15.);
#30453=CIRCLE('',#98930,11.4440000000002);
#30454=CIRCLE('',#98931,11.444);
#30455=CIRCLE('',#98933,18.0480155876192);
#36619=VERTEX_POINT('',#142849);
#36620=VERTEX_POINT('',#142850);
#36621=VERTEX_POINT('',#142853);
#36622=VERTEX_POINT('',#142857);
#36623=VERTEX_POINT('',#142859);
#36624=VERTEX_POINT('',#142861);
#36625=VERTEX_POINT('',#142865);
#36626=VERTEX_POINT('',#142866);
#36627=VERTEX_POINT('',#142885);
#36628=VERTEX_POINT('',#142887);
#36629=VERTEX_POINT('',#142943);
#36630=VERTEX_POINT('',#142944);
#36631=VERTEX_POINT('',#142963);
#36632=VERTEX_POINT('',#142965);
#36633=VERTEX_POINT('',#143021);
#36634=VERTEX_POINT('',#143022);
#36635=VERTEX_POINT('',#143042);
#36636=VERTEX_POINT('',#143044);
#36637=VERTEX_POINT('',#143101);
#36638=VERTEX_POINT('',#143102);
#36639=VERTEX_POINT('',#143122);
#36640=VERTEX_POINT('',#143124);
#36641=VERTEX_POINT('',#143181);
#36642=VERTEX_POINT('',#143187);
#36643=VERTEX_POINT('',#143193);
#36644=VERTEX_POINT('',#143194);
#36645=VERTEX_POINT('',#143196);
#36646=VERTEX_POINT('',#143232);
#36647=VERTEX_POINT('',#143270);
#36648=VERTEX_POINT('',#143271);
#36649=VERTEX_POINT('',#143412);
#36650=VERTEX_POINT('',#143413);
#36651=VERTEX_POINT('',#143554);
#36652=VERTEX_POINT('',#143555);
#36653=VERTEX_POINT('',#143696);
#36654=VERTEX_POINT('',#143697);
#36655=VERTEX_POINT('',#143838);
#36656=VERTEX_POINT('',#143839);
#36657=VERTEX_POINT('',#143980);
#36658=VERTEX_POINT('',#143981);
#36659=VERTEX_POINT('',#144122);
#36660=VERTEX_POINT('',#144123);
#36661=VERTEX_POINT('',#144264);
#36662=VERTEX_POINT('',#144265);
#36663=VERTEX_POINT('',#144267);
#36664=VERTEX_POINT('',#144295);
#36665=VERTEX_POINT('',#144297);
#36666=VERTEX_POINT('',#144317);
#36667=VERTEX_POINT('',#144318);
#36668=VERTEX_POINT('',#144355);
#36669=VERTEX_POINT('',#144356);
#36670=VERTEX_POINT('',#144394);
#36671=VERTEX_POINT('',#144395);
#36672=VERTEX_POINT('',#144468);
#36673=VERTEX_POINT('',#144469);
#36674=VERTEX_POINT('',#144508);
#36675=VERTEX_POINT('',#144509);
#36676=VERTEX_POINT('',#144564);
#36677=VERTEX_POINT('',#144565);
#36678=VERTEX_POINT('',#144620);
#36679=VERTEX_POINT('',#144621);
#36680=VERTEX_POINT('',#144676);
#36681=VERTEX_POINT('',#144677);
#36682=VERTEX_POINT('',#144732);
#36683=VERTEX_POINT('',#144733);
#36684=VERTEX_POINT('',#144788);
#36685=VERTEX_POINT('',#144789);
#36686=VERTEX_POINT('',#144844);
#36687=VERTEX_POINT('',#144845);
#36688=VERTEX_POINT('',#144847);
#36689=VERTEX_POINT('',#144874);
#36690=VERTEX_POINT('',#144901);
#36691=VERTEX_POINT('',#144902);
#36692=VERTEX_POINT('',#144971);
#36693=VERTEX_POINT('',#144972);
#36694=VERTEX_POINT('',#145043);
#36695=VERTEX_POINT('',#145044);
#36696=VERTEX_POINT('',#145115);
#36697=VERTEX_POINT('',#145116);
#36698=VERTEX_POINT('',#145187);
#36699=VERTEX_POINT('',#145188);
#36700=VERTEX_POINT('',#145259);
#36701=VERTEX_POINT('',#145260);
#36702=VERTEX_POINT('',#145331);
#36703=VERTEX_POINT('',#145332);
#36704=VERTEX_POINT('',#145403);
#36705=VERTEX_POINT('',#145405);
#36706=VERTEX_POINT('',#145443);
#36707=VERTEX_POINT('',#145444);
#36708=VERTEX_POINT('',#145483);
#36709=VERTEX_POINT('',#145485);
#36710=VERTEX_POINT('',#145524);
#36711=VERTEX_POINT('',#145525);
#36712=VERTEX_POINT('',#145565);
#36713=VERTEX_POINT('',#145576);
#36714=VERTEX_POINT('',#145591);
#36715=VERTEX_POINT('',#145608);
#36716=VERTEX_POINT('',#145802);
#36717=VERTEX_POINT('',#145809);
#36718=VERTEX_POINT('',#145812);
#36719=VERTEX_POINT('',#149841);
#36720=VERTEX_POINT('',#149843);
#36721=VERTEX_POINT('',#154414);
#36722=VERTEX_POINT('',#158489);
#36723=VERTEX_POINT('',#162555);
#36724=VERTEX_POINT('',#162562);
#45591=EDGE_CURVE('',#36619,#36620,#30440,.T.);
#45592=EDGE_CURVE('',#36620,#36619,#30441,.T.);
#45593=EDGE_CURVE('',#36620,#36621,#30442,.T.);
#45594=EDGE_CURVE('',#36621,#36621,#30443,.T.);
#45595=EDGE_CURVE('',#36622,#36622,#30444,.T.);
#45596=EDGE_CURVE('',#36622,#36623,#30445,.T.);
#45597=EDGE_CURVE('',#36624,#36623,#30446,.T.);
#45598=EDGE_CURVE('',#36623,#36624,#30447,.T.);
#45599=EDGE_CURVE('',#36625,#36626,#4173,.T.);
#45600=EDGE_CURVE('',#36626,#36627,#20030,.T.);
#45601=EDGE_CURVE('',#36627,#36628,#4174,.T.);
#45602=EDGE_CURVE('',#36628,#36627,#4175,.T.);
#45603=EDGE_CURVE('',#36626,#36625,#4176,.T.);
#45604=EDGE_CURVE('',#36629,#36630,#4177,.T.);
#45605=EDGE_CURVE('',#36630,#36631,#20031,.T.);
#45606=EDGE_CURVE('',#36631,#36632,#4178,.T.);
#45607=EDGE_CURVE('',#36632,#36631,#4179,.T.);
#45608=EDGE_CURVE('',#36630,#36629,#4180,.T.);
#45609=EDGE_CURVE('',#36633,#36634,#4181,.T.);
#45610=EDGE_CURVE('',#36634,#36635,#20032,.T.);
#45611=EDGE_CURVE('',#36635,#36636,#4182,.T.);
#45612=EDGE_CURVE('',#36636,#36635,#4183,.T.);
#45613=EDGE_CURVE('',#36634,#36633,#4184,.T.);
#45614=EDGE_CURVE('',#36637,#36638,#4185,.T.);
#45615=EDGE_CURVE('',#36638,#36639,#20033,.T.);
#45616=EDGE_CURVE('',#36639,#36640,#4186,.T.);
#45617=EDGE_CURVE('',#36640,#36639,#4187,.T.);
#45618=EDGE_CURVE('',#36638,#36637,#4188,.T.);
#45619=EDGE_CURVE('',#36641,#36641,#30448,.T.);
#45620=EDGE_CURVE('',#36641,#36640,#20034,.T.);
#45621=EDGE_CURVE('',#36639,#36624,#20035,.T.);
#45622=EDGE_CURVE('',#36619,#36638,#20036,.T.);
#45623=EDGE_CURVE('',#36637,#36642,#20037,.T.);
#45624=EDGE_CURVE('',#36642,#36642,#30449,.T.);
#45625=EDGE_CURVE('',#36643,#36644,#20038,.T.);
#45626=EDGE_CURVE('',#36645,#36643,#4065,.T.);
#45627=EDGE_CURVE('',#36646,#36645,#20039,.T.);
#45628=EDGE_CURVE('',#36646,#36644,#4066,.T.);
#45629=EDGE_CURVE('',#36647,#36648,#20040,.T.);
#45630=EDGE_CURVE('',#36643,#36647,#4067,.T.);
#45631=EDGE_CURVE('',#36644,#36648,#4068,.T.);
#45632=EDGE_CURVE('',#36649,#36650,#20041,.T.);
#45633=EDGE_CURVE('',#36647,#36649,#4069,.T.);
#45634=EDGE_CURVE('',#36648,#36650,#4070,.T.);
#45635=EDGE_CURVE('',#36651,#36652,#20042,.T.);
#45636=EDGE_CURVE('',#36649,#36651,#4071,.T.);
#45637=EDGE_CURVE('',#36650,#36652,#4072,.T.);
#45638=EDGE_CURVE('',#36653,#36654,#20043,.T.);
#45639=EDGE_CURVE('',#36651,#36653,#4073,.T.);
#45640=EDGE_CURVE('',#36652,#36654,#4074,.T.);
#45641=EDGE_CURVE('',#36655,#36656,#20044,.T.);
#45642=EDGE_CURVE('',#36653,#36655,#4075,.T.);
#45643=EDGE_CURVE('',#36654,#36656,#4076,.T.);
#45644=EDGE_CURVE('',#36657,#36658,#20045,.T.);
#45645=EDGE_CURVE('',#36655,#36657,#4077,.T.);
#45646=EDGE_CURVE('',#36656,#36658,#4078,.T.);
#45647=EDGE_CURVE('',#36659,#36660,#20046,.T.);
#45648=EDGE_CURVE('',#36657,#36659,#4079,.T.);
#45649=EDGE_CURVE('',#36658,#36660,#4080,.T.);
#45650=EDGE_CURVE('',#36661,#36662,#20047,.T.);
#45651=EDGE_CURVE('',#36663,#36661,#4189,.F.);
#45652=EDGE_CURVE('',#36663,#36663,#30450,.T.);
#45653=EDGE_CURVE('',#36664,#36663,#20048,.T.);
#45654=EDGE_CURVE('',#36665,#36664,#20049,.T.);
#45655=EDGE_CURVE('',#36662,#36665,#4190,.T.);
#45656=EDGE_CURVE('',#36666,#36667,#4191,.T.);
#45657=EDGE_CURVE('',#36667,#36666,#4192,.T.);
#45658=EDGE_CURVE('',#36668,#36669,#4193,.T.);
#45659=EDGE_CURVE('',#36669,#36668,#4194,.T.);
#45660=EDGE_CURVE('',#36670,#36671,#20050,.T.);
#45661=EDGE_CURVE('',#36661,#36670,#4195,.F.);
#45662=EDGE_CURVE('',#36665,#36662,#4196,.T.);
#45663=EDGE_CURVE('',#36664,#36671,#4197,.T.);
#45664=EDGE_CURVE('',#36672,#36673,#4198,.T.);
#45665=EDGE_CURVE('',#36673,#36672,#4199,.T.);
#45666=EDGE_CURVE('',#36674,#36675,#20051,.T.);
#45667=EDGE_CURVE('',#36670,#36674,#4200,.F.);
#45668=EDGE_CURVE('',#36671,#36675,#4201,.T.);
#45669=EDGE_CURVE('',#36676,#36677,#20052,.T.);
#45670=EDGE_CURVE('',#36674,#36676,#4202,.F.);
#45671=EDGE_CURVE('',#36675,#36677,#4203,.T.);
#45672=EDGE_CURVE('',#36678,#36679,#20053,.T.);
#45673=EDGE_CURVE('',#36676,#36678,#4204,.F.);
#45674=EDGE_CURVE('',#36677,#36679,#4205,.T.);
#45675=EDGE_CURVE('',#36680,#36681,#20054,.T.);
#45676=EDGE_CURVE('',#36678,#36680,#4206,.F.);
#45677=EDGE_CURVE('',#36679,#36681,#4207,.T.);
#45678=EDGE_CURVE('',#36682,#36683,#20055,.T.);
#45679=EDGE_CURVE('',#36680,#36682,#4208,.F.);
#45680=EDGE_CURVE('',#36681,#36683,#4209,.T.);
#45681=EDGE_CURVE('',#36684,#36685,#20056,.T.);
#45682=EDGE_CURVE('',#36682,#36684,#4210,.F.);
#45683=EDGE_CURVE('',#36683,#36685,#4211,.T.);
#45684=EDGE_CURVE('',#36686,#36687,#20057,.T.);
#45685=EDGE_CURVE('',#36686,#36688,#4212,.T.);
#45686=EDGE_CURVE('',#36689,#36688,#30451,.T.);
#45687=EDGE_CURVE('',#36689,#36687,#4213,.T.);
#45688=EDGE_CURVE('',#36690,#36691,#20058,.T.);
#45689=EDGE_CURVE('',#36690,#36686,#4214,.T.);
#45690=EDGE_CURVE('',#36687,#36691,#4215,.T.);
#45691=EDGE_CURVE('',#36692,#36693,#20059,.T.);
#45692=EDGE_CURVE('',#36692,#36690,#4216,.T.);
#45693=EDGE_CURVE('',#36691,#36693,#4217,.T.);
#45694=EDGE_CURVE('',#36694,#36695,#20060,.T.);
#45695=EDGE_CURVE('',#36694,#36692,#4218,.T.);
#45696=EDGE_CURVE('',#36693,#36695,#4219,.T.);
#45697=EDGE_CURVE('',#36696,#36697,#20061,.T.);
#45698=EDGE_CURVE('',#36696,#36694,#4220,.T.);
#45699=EDGE_CURVE('',#36695,#36697,#4221,.T.);
#45700=EDGE_CURVE('',#36698,#36699,#20062,.T.);
#45701=EDGE_CURVE('',#36698,#36696,#4222,.T.);
#45702=EDGE_CURVE('',#36697,#36699,#4223,.T.);
#45703=EDGE_CURVE('',#36700,#36701,#20063,.T.);
#45704=EDGE_CURVE('',#36700,#36698,#4224,.T.);
#45705=EDGE_CURVE('',#36699,#36701,#4225,.T.);
#45706=EDGE_CURVE('',#36702,#36703,#20064,.T.);
#45707=EDGE_CURVE('',#36702,#36700,#4226,.T.);
#45708=EDGE_CURVE('',#36701,#36703,#4227,.T.);
#45709=EDGE_CURVE('',#36669,#36704,#20065,.T.);
#45710=EDGE_CURVE('',#36704,#36705,#4228,.T.);
#45711=EDGE_CURVE('',#36705,#36704,#4229,.T.);
#45712=EDGE_CURVE('',#36706,#36707,#4230,.T.);
#45713=EDGE_CURVE('',#36707,#36667,#20066,.T.);
#45714=EDGE_CURVE('',#36707,#36706,#4231,.T.);
#45715=EDGE_CURVE('',#36673,#36708,#20067,.T.);
#45716=EDGE_CURVE('',#36708,#36709,#4232,.T.);
#45717=EDGE_CURVE('',#36709,#36708,#4233,.T.);
#45718=EDGE_CURVE('',#36710,#36711,#4234,.T.);
#45719=EDGE_CURVE('',#36711,#36665,#20068,.T.);
#45720=EDGE_CURVE('',#36711,#36710,#4235,.T.);
#45721=EDGE_CURVE('',#36703,#36712,#4236,.T.);
#45722=EDGE_CURVE('',#36713,#36712,#20069,.T.);
#45723=EDGE_CURVE('',#36713,#36702,#4237,.T.);
#45724=EDGE_CURVE('',#36685,#36714,#4238,.T.);
#45725=EDGE_CURVE('',#36714,#36715,#4239,.T.);
#45726=EDGE_CURVE('',#36715,#36716,#30452,.T.);
#45727=EDGE_CURVE('',#36684,#36716,#4240,.F.);
#45728=EDGE_CURVE('',#36717,#36717,#30453,.T.);
#45729=EDGE_CURVE('',#36717,#36711,#20070,.T.);
#45730=EDGE_CURVE('',#36710,#36718,#20071,.T.);
#45731=EDGE_CURVE('',#36718,#36718,#30454,.T.);
#45732=EDGE_CURVE('',#36719,#36689,#336,.T.);
#45733=EDGE_CURVE('',#36720,#36719,#4081,.T.);
#45734=EDGE_CURVE('',#36712,#36720,#20072,.T.);
#45735=EDGE_CURVE('',#36688,#36721,#4241,.T.);
#45736=EDGE_CURVE('',#36645,#36713,#20073,.T.);
#45737=EDGE_CURVE('',#36659,#36721,#4082,.T.);
#45738=EDGE_CURVE('',#36722,#36716,#20074,.T.);
#45739=EDGE_CURVE('',#36660,#36722,#4083,.T.);
#45740=EDGE_CURVE('',#36663,#36646,#20075,.T.);
#45741=EDGE_CURVE('',#36715,#36723,#4242,.T.);
#45742=EDGE_CURVE('',#36724,#36664,#20076,.T.);
#45743=EDGE_CURVE('',#36724,#36723,#4084,.T.);
#45744=EDGE_CURVE('',#36723,#36719,#30455,.T.);
#45745=EDGE_CURVE('',#36720,#36724,#20077,.T.);
#45746=EDGE_CURVE('',#36721,#36722,#337,.T.);
#60625=ORIENTED_EDGE('',*,*,#45591,.F.);
#60626=ORIENTED_EDGE('',*,*,#45592,.F.);
#60627=ORIENTED_EDGE('',*,*,#45593,.T.);
#60628=ORIENTED_EDGE('',*,*,#45594,.F.);
#60629=ORIENTED_EDGE('',*,*,#45593,.F.);
#60630=ORIENTED_EDGE('',*,*,#45595,.F.);
#60631=ORIENTED_EDGE('',*,*,#45596,.T.);
#60632=ORIENTED_EDGE('',*,*,#45597,.F.);
#60633=ORIENTED_EDGE('',*,*,#45598,.F.);
#60634=ORIENTED_EDGE('',*,*,#45596,.F.);
#60635=ORIENTED_EDGE('',*,*,#45599,.T.);
#60636=ORIENTED_EDGE('',*,*,#45600,.T.);
#60637=ORIENTED_EDGE('',*,*,#45601,.T.);
#60638=ORIENTED_EDGE('',*,*,#45602,.T.);
#60639=ORIENTED_EDGE('',*,*,#45600,.F.);
#60640=ORIENTED_EDGE('',*,*,#45603,.T.);
#60641=ORIENTED_EDGE('',*,*,#45604,.T.);
#60642=ORIENTED_EDGE('',*,*,#45605,.T.);
#60643=ORIENTED_EDGE('',*,*,#45606,.T.);
#60644=ORIENTED_EDGE('',*,*,#45607,.T.);
#60645=ORIENTED_EDGE('',*,*,#45605,.F.);
#60646=ORIENTED_EDGE('',*,*,#45608,.T.);
#60647=ORIENTED_EDGE('',*,*,#45609,.T.);
#60648=ORIENTED_EDGE('',*,*,#45610,.T.);
#60649=ORIENTED_EDGE('',*,*,#45611,.T.);
#60650=ORIENTED_EDGE('',*,*,#45612,.T.);
#60651=ORIENTED_EDGE('',*,*,#45610,.F.);
#60652=ORIENTED_EDGE('',*,*,#45613,.T.);
#60653=ORIENTED_EDGE('',*,*,#45614,.T.);
#60654=ORIENTED_EDGE('',*,*,#45615,.T.);
#60655=ORIENTED_EDGE('',*,*,#45616,.T.);
#60656=ORIENTED_EDGE('',*,*,#45617,.T.);
#60657=ORIENTED_EDGE('',*,*,#45615,.F.);
#60658=ORIENTED_EDGE('',*,*,#45618,.T.);
#60659=ORIENTED_EDGE('',*,*,#45619,.F.);
#60660=ORIENTED_EDGE('',*,*,#45620,.T.);
#60661=ORIENTED_EDGE('',*,*,#45616,.F.);
#60662=ORIENTED_EDGE('',*,*,#45621,.T.);
#60663=ORIENTED_EDGE('',*,*,#45597,.T.);
#60664=ORIENTED_EDGE('',*,*,#45598,.T.);
#60665=ORIENTED_EDGE('',*,*,#45621,.F.);
#60666=ORIENTED_EDGE('',*,*,#45617,.F.);
#60667=ORIENTED_EDGE('',*,*,#45620,.F.);
#60668=ORIENTED_EDGE('',*,*,#45609,.F.);
#60669=ORIENTED_EDGE('',*,*,#45613,.F.);
#60670=ORIENTED_EDGE('',*,*,#45599,.F.);
#60671=ORIENTED_EDGE('',*,*,#45603,.F.);
#60672=ORIENTED_EDGE('',*,*,#45607,.F.);
#60673=ORIENTED_EDGE('',*,*,#45606,.F.);
#60674=ORIENTED_EDGE('',*,*,#45591,.T.);
#60675=ORIENTED_EDGE('',*,*,#45592,.T.);
#60676=ORIENTED_EDGE('',*,*,#45622,.T.);
#60677=ORIENTED_EDGE('',*,*,#45614,.F.);
#60678=ORIENTED_EDGE('',*,*,#45623,.T.);
#60679=ORIENTED_EDGE('',*,*,#45624,.T.);
#60680=ORIENTED_EDGE('',*,*,#45623,.F.);
#60681=ORIENTED_EDGE('',*,*,#45618,.F.);
#60682=ORIENTED_EDGE('',*,*,#45622,.F.);
#60683=ORIENTED_EDGE('',*,*,#45612,.F.);
#60684=ORIENTED_EDGE('',*,*,#45611,.F.);
#60685=ORIENTED_EDGE('',*,*,#45604,.F.);
#60686=ORIENTED_EDGE('',*,*,#45608,.F.);
#60687=ORIENTED_EDGE('',*,*,#45602,.F.);
#60688=ORIENTED_EDGE('',*,*,#45601,.F.);
#60689=ORIENTED_EDGE('',*,*,#45595,.T.);
#60690=ORIENTED_EDGE('',*,*,#45594,.T.);
#60691=ORIENTED_EDGE('',*,*,#45619,.T.);
#60692=ORIENTED_EDGE('',*,*,#45624,.F.);
#60693=ORIENTED_EDGE('',*,*,#45625,.F.);
#60694=ORIENTED_EDGE('',*,*,#45626,.F.);
#60695=ORIENTED_EDGE('',*,*,#45627,.F.);
#60696=ORIENTED_EDGE('',*,*,#45628,.T.);
#60697=ORIENTED_EDGE('',*,*,#45629,.F.);
#60698=ORIENTED_EDGE('',*,*,#45630,.F.);
#60699=ORIENTED_EDGE('',*,*,#45625,.T.);
#60700=ORIENTED_EDGE('',*,*,#45631,.T.);
#60701=ORIENTED_EDGE('',*,*,#45632,.F.);
#60702=ORIENTED_EDGE('',*,*,#45633,.F.);
#60703=ORIENTED_EDGE('',*,*,#45629,.T.);
#60704=ORIENTED_EDGE('',*,*,#45634,.T.);
#60705=ORIENTED_EDGE('',*,*,#45635,.F.);
#60706=ORIENTED_EDGE('',*,*,#45636,.F.);
#60707=ORIENTED_EDGE('',*,*,#45632,.T.);
#60708=ORIENTED_EDGE('',*,*,#45637,.T.);
#60709=ORIENTED_EDGE('',*,*,#45638,.F.);
#60710=ORIENTED_EDGE('',*,*,#45639,.F.);
#60711=ORIENTED_EDGE('',*,*,#45635,.T.);
#60712=ORIENTED_EDGE('',*,*,#45640,.T.);
#60713=ORIENTED_EDGE('',*,*,#45641,.F.);
#60714=ORIENTED_EDGE('',*,*,#45642,.F.);
#60715=ORIENTED_EDGE('',*,*,#45638,.T.);
#60716=ORIENTED_EDGE('',*,*,#45643,.T.);
#60717=ORIENTED_EDGE('',*,*,#45644,.F.);
#60718=ORIENTED_EDGE('',*,*,#45645,.F.);
#60719=ORIENTED_EDGE('',*,*,#45641,.T.);
#60720=ORIENTED_EDGE('',*,*,#45646,.T.);
#60721=ORIENTED_EDGE('',*,*,#45647,.F.);
#60722=ORIENTED_EDGE('',*,*,#45648,.F.);
#60723=ORIENTED_EDGE('',*,*,#45644,.T.);
#60724=ORIENTED_EDGE('',*,*,#45649,.T.);
#60725=ORIENTED_EDGE('',*,*,#45650,.F.);
#60726=ORIENTED_EDGE('',*,*,#45651,.F.);
#60727=ORIENTED_EDGE('',*,*,#45652,.T.);
#60728=ORIENTED_EDGE('',*,*,#45653,.F.);
#60729=ORIENTED_EDGE('',*,*,#45654,.F.);
#60730=ORIENTED_EDGE('',*,*,#45655,.F.);
#60731=ORIENTED_EDGE('',*,*,#45656,.F.);
#60732=ORIENTED_EDGE('',*,*,#45657,.F.);
#60733=ORIENTED_EDGE('',*,*,#45658,.F.);
#60734=ORIENTED_EDGE('',*,*,#45659,.F.);
#60735=ORIENTED_EDGE('',*,*,#45660,.F.);
#60736=ORIENTED_EDGE('',*,*,#45661,.F.);
#60737=ORIENTED_EDGE('',*,*,#45650,.T.);
#60738=ORIENTED_EDGE('',*,*,#45662,.F.);
#60739=ORIENTED_EDGE('',*,*,#45654,.T.);
#60740=ORIENTED_EDGE('',*,*,#45663,.T.);
#60741=ORIENTED_EDGE('',*,*,#45664,.F.);
#60742=ORIENTED_EDGE('',*,*,#45665,.F.);
#60743=ORIENTED_EDGE('',*,*,#45666,.F.);
#60744=ORIENTED_EDGE('',*,*,#45667,.F.);
#60745=ORIENTED_EDGE('',*,*,#45660,.T.);
#60746=ORIENTED_EDGE('',*,*,#45668,.T.);
#60747=ORIENTED_EDGE('',*,*,#45669,.F.);
#60748=ORIENTED_EDGE('',*,*,#45670,.F.);
#60749=ORIENTED_EDGE('',*,*,#45666,.T.);
#60750=ORIENTED_EDGE('',*,*,#45671,.T.);
#60751=ORIENTED_EDGE('',*,*,#45672,.F.);
#60752=ORIENTED_EDGE('',*,*,#45673,.F.);
#60753=ORIENTED_EDGE('',*,*,#45669,.T.);
#60754=ORIENTED_EDGE('',*,*,#45674,.T.);
#60755=ORIENTED_EDGE('',*,*,#45675,.F.);
#60756=ORIENTED_EDGE('',*,*,#45676,.F.);
#60757=ORIENTED_EDGE('',*,*,#45672,.T.);
#60758=ORIENTED_EDGE('',*,*,#45677,.T.);
#60759=ORIENTED_EDGE('',*,*,#45678,.F.);
#60760=ORIENTED_EDGE('',*,*,#45679,.F.);
#60761=ORIENTED_EDGE('',*,*,#45675,.T.);
#60762=ORIENTED_EDGE('',*,*,#45680,.T.);
#60763=ORIENTED_EDGE('',*,*,#45681,.F.);
#60764=ORIENTED_EDGE('',*,*,#45682,.F.);
#60765=ORIENTED_EDGE('',*,*,#45678,.T.);
#60766=ORIENTED_EDGE('',*,*,#45683,.T.);
#60767=ORIENTED_EDGE('',*,*,#45684,.F.);
#60768=ORIENTED_EDGE('',*,*,#45685,.T.);
#60769=ORIENTED_EDGE('',*,*,#45686,.F.);
#60770=ORIENTED_EDGE('',*,*,#45687,.T.);
#60771=ORIENTED_EDGE('',*,*,#45688,.F.);
#60772=ORIENTED_EDGE('',*,*,#45689,.T.);
#60773=ORIENTED_EDGE('',*,*,#45684,.T.);
#60774=ORIENTED_EDGE('',*,*,#45690,.T.);
#60775=ORIENTED_EDGE('',*,*,#45691,.F.);
#60776=ORIENTED_EDGE('',*,*,#45692,.T.);
#60777=ORIENTED_EDGE('',*,*,#45688,.T.);
#60778=ORIENTED_EDGE('',*,*,#45693,.T.);
#60779=ORIENTED_EDGE('',*,*,#45694,.F.);
#60780=ORIENTED_EDGE('',*,*,#45695,.T.);
#60781=ORIENTED_EDGE('',*,*,#45691,.T.);
#60782=ORIENTED_EDGE('',*,*,#45696,.T.);
#60783=ORIENTED_EDGE('',*,*,#45697,.F.);
#60784=ORIENTED_EDGE('',*,*,#45698,.T.);
#60785=ORIENTED_EDGE('',*,*,#45694,.T.);
#60786=ORIENTED_EDGE('',*,*,#45699,.T.);
#60787=ORIENTED_EDGE('',*,*,#45700,.F.);
#60788=ORIENTED_EDGE('',*,*,#45701,.T.);
#60789=ORIENTED_EDGE('',*,*,#45697,.T.);
#60790=ORIENTED_EDGE('',*,*,#45702,.T.);
#60791=ORIENTED_EDGE('',*,*,#45703,.F.);
#60792=ORIENTED_EDGE('',*,*,#45704,.T.);
#60793=ORIENTED_EDGE('',*,*,#45700,.T.);
#60794=ORIENTED_EDGE('',*,*,#45705,.T.);
#60795=ORIENTED_EDGE('',*,*,#45706,.F.);
#60796=ORIENTED_EDGE('',*,*,#45707,.T.);
#60797=ORIENTED_EDGE('',*,*,#45703,.T.);
#60798=ORIENTED_EDGE('',*,*,#45708,.T.);
#60799=ORIENTED_EDGE('',*,*,#45658,.T.);
#60800=ORIENTED_EDGE('',*,*,#45709,.T.);
#60801=ORIENTED_EDGE('',*,*,#45710,.T.);
#60802=ORIENTED_EDGE('',*,*,#45711,.T.);
#60803=ORIENTED_EDGE('',*,*,#45709,.F.);
#60804=ORIENTED_EDGE('',*,*,#45659,.T.);
#60805=ORIENTED_EDGE('',*,*,#45712,.T.);
#60806=ORIENTED_EDGE('',*,*,#45713,.T.);
#60807=ORIENTED_EDGE('',*,*,#45657,.T.);
#60808=ORIENTED_EDGE('',*,*,#45656,.T.);
#60809=ORIENTED_EDGE('',*,*,#45713,.F.);
#60810=ORIENTED_EDGE('',*,*,#45714,.T.);
#60811=ORIENTED_EDGE('',*,*,#45664,.T.);
#60812=ORIENTED_EDGE('',*,*,#45715,.T.);
#60813=ORIENTED_EDGE('',*,*,#45716,.T.);
#60814=ORIENTED_EDGE('',*,*,#45717,.T.);
#60815=ORIENTED_EDGE('',*,*,#45715,.F.);
#60816=ORIENTED_EDGE('',*,*,#45665,.T.);
#60817=ORIENTED_EDGE('',*,*,#45718,.T.);
#60818=ORIENTED_EDGE('',*,*,#45719,.T.);
#60819=ORIENTED_EDGE('',*,*,#45662,.T.);
#60820=ORIENTED_EDGE('',*,*,#45655,.T.);
#60821=ORIENTED_EDGE('',*,*,#45719,.F.);
#60822=ORIENTED_EDGE('',*,*,#45720,.T.);
#60823=ORIENTED_EDGE('',*,*,#45706,.T.);
#60824=ORIENTED_EDGE('',*,*,#45721,.T.);
#60825=ORIENTED_EDGE('',*,*,#45722,.F.);
#60826=ORIENTED_EDGE('',*,*,#45723,.T.);
#60827=ORIENTED_EDGE('',*,*,#45681,.T.);
#60828=ORIENTED_EDGE('',*,*,#45724,.T.);
#60829=ORIENTED_EDGE('',*,*,#45725,.T.);
#60830=ORIENTED_EDGE('',*,*,#45726,.T.);
#60831=ORIENTED_EDGE('',*,*,#45727,.F.);
#60832=ORIENTED_EDGE('',*,*,#45728,.F.);
#60833=ORIENTED_EDGE('',*,*,#45729,.T.);
#60834=ORIENTED_EDGE('',*,*,#45718,.F.);
#60835=ORIENTED_EDGE('',*,*,#45730,.T.);
#60836=ORIENTED_EDGE('',*,*,#45731,.T.);
#60837=ORIENTED_EDGE('',*,*,#45730,.F.);
#60838=ORIENTED_EDGE('',*,*,#45720,.F.);
#60839=ORIENTED_EDGE('',*,*,#45729,.F.);
#60840=ORIENTED_EDGE('',*,*,#45717,.F.);
#60841=ORIENTED_EDGE('',*,*,#45716,.F.);
#60842=ORIENTED_EDGE('',*,*,#45712,.F.);
#60843=ORIENTED_EDGE('',*,*,#45714,.F.);
#60844=ORIENTED_EDGE('',*,*,#45711,.F.);
#60845=ORIENTED_EDGE('',*,*,#45710,.F.);
#60846=ORIENTED_EDGE('',*,*,#45732,.F.);
#60847=ORIENTED_EDGE('',*,*,#45733,.F.);
#60848=ORIENTED_EDGE('',*,*,#45734,.F.);
#60849=ORIENTED_EDGE('',*,*,#45721,.F.);
#60850=ORIENTED_EDGE('',*,*,#45708,.F.);
#60851=ORIENTED_EDGE('',*,*,#45705,.F.);
#60852=ORIENTED_EDGE('',*,*,#45702,.F.);
#60853=ORIENTED_EDGE('',*,*,#45699,.F.);
#60854=ORIENTED_EDGE('',*,*,#45696,.F.);
#60855=ORIENTED_EDGE('',*,*,#45693,.F.);
#60856=ORIENTED_EDGE('',*,*,#45690,.F.);
#60857=ORIENTED_EDGE('',*,*,#45687,.F.);
#60858=ORIENTED_EDGE('',*,*,#45735,.F.);
#60859=ORIENTED_EDGE('',*,*,#45685,.F.);
#60860=ORIENTED_EDGE('',*,*,#45689,.F.);
#60861=ORIENTED_EDGE('',*,*,#45692,.F.);
#60862=ORIENTED_EDGE('',*,*,#45695,.F.);
#60863=ORIENTED_EDGE('',*,*,#45698,.F.);
#60864=ORIENTED_EDGE('',*,*,#45701,.F.);
#60865=ORIENTED_EDGE('',*,*,#45704,.F.);
#60866=ORIENTED_EDGE('',*,*,#45707,.F.);
#60867=ORIENTED_EDGE('',*,*,#45723,.F.);
#60868=ORIENTED_EDGE('',*,*,#45736,.F.);
#60869=ORIENTED_EDGE('',*,*,#45626,.T.);
#60870=ORIENTED_EDGE('',*,*,#45630,.T.);
#60871=ORIENTED_EDGE('',*,*,#45633,.T.);
#60872=ORIENTED_EDGE('',*,*,#45636,.T.);
#60873=ORIENTED_EDGE('',*,*,#45639,.T.);
#60874=ORIENTED_EDGE('',*,*,#45642,.T.);
#60875=ORIENTED_EDGE('',*,*,#45645,.T.);
#60876=ORIENTED_EDGE('',*,*,#45648,.T.);
#60877=ORIENTED_EDGE('',*,*,#45737,.T.);
#60878=ORIENTED_EDGE('',*,*,#45738,.F.);
#60879=ORIENTED_EDGE('',*,*,#45739,.F.);
#60880=ORIENTED_EDGE('',*,*,#45649,.F.);
#60881=ORIENTED_EDGE('',*,*,#45646,.F.);
#60882=ORIENTED_EDGE('',*,*,#45643,.F.);
#60883=ORIENTED_EDGE('',*,*,#45640,.F.);
#60884=ORIENTED_EDGE('',*,*,#45637,.F.);
#60885=ORIENTED_EDGE('',*,*,#45634,.F.);
#60886=ORIENTED_EDGE('',*,*,#45631,.F.);
#60887=ORIENTED_EDGE('',*,*,#45628,.F.);
#60888=ORIENTED_EDGE('',*,*,#45740,.F.);
#60889=ORIENTED_EDGE('',*,*,#45651,.T.);
#60890=ORIENTED_EDGE('',*,*,#45661,.T.);
#60891=ORIENTED_EDGE('',*,*,#45667,.T.);
#60892=ORIENTED_EDGE('',*,*,#45670,.T.);
#60893=ORIENTED_EDGE('',*,*,#45673,.T.);
#60894=ORIENTED_EDGE('',*,*,#45676,.T.);
#60895=ORIENTED_EDGE('',*,*,#45679,.T.);
#60896=ORIENTED_EDGE('',*,*,#45682,.T.);
#60897=ORIENTED_EDGE('',*,*,#45727,.T.);
#60898=ORIENTED_EDGE('',*,*,#45741,.F.);
#60899=ORIENTED_EDGE('',*,*,#45725,.F.);
#60900=ORIENTED_EDGE('',*,*,#45724,.F.);
#60901=ORIENTED_EDGE('',*,*,#45683,.F.);
#60902=ORIENTED_EDGE('',*,*,#45680,.F.);
#60903=ORIENTED_EDGE('',*,*,#45677,.F.);
#60904=ORIENTED_EDGE('',*,*,#45674,.F.);
#60905=ORIENTED_EDGE('',*,*,#45671,.F.);
#60906=ORIENTED_EDGE('',*,*,#45668,.F.);
#60907=ORIENTED_EDGE('',*,*,#45663,.F.);
#60908=ORIENTED_EDGE('',*,*,#45742,.F.);
#60909=ORIENTED_EDGE('',*,*,#45743,.T.);
#60910=ORIENTED_EDGE('',*,*,#45744,.F.);
#60911=ORIENTED_EDGE('',*,*,#45743,.F.);
#60912=ORIENTED_EDGE('',*,*,#45745,.F.);
#60913=ORIENTED_EDGE('',*,*,#45733,.T.);
#60914=ORIENTED_EDGE('',*,*,#45647,.T.);
#60915=ORIENTED_EDGE('',*,*,#45739,.T.);
#60916=ORIENTED_EDGE('',*,*,#45746,.F.);
#60917=ORIENTED_EDGE('',*,*,#45737,.F.);
#60918=ORIENTED_EDGE('',*,*,#45736,.T.);
#60919=ORIENTED_EDGE('',*,*,#45722,.T.);
#60920=ORIENTED_EDGE('',*,*,#45734,.T.);
#60921=ORIENTED_EDGE('',*,*,#45745,.T.);
#60922=ORIENTED_EDGE('',*,*,#45742,.T.);
#60923=ORIENTED_EDGE('',*,*,#45653,.T.);
#60924=ORIENTED_EDGE('',*,*,#45740,.T.);
#60925=ORIENTED_EDGE('',*,*,#45627,.T.);
#60926=ORIENTED_EDGE('',*,*,#45652,.F.);
#60927=ORIENTED_EDGE('',*,*,#45728,.T.);
#60928=ORIENTED_EDGE('',*,*,#45732,.T.);
#60929=ORIENTED_EDGE('',*,*,#45686,.T.);
#60930=ORIENTED_EDGE('',*,*,#45735,.T.);
#60931=ORIENTED_EDGE('',*,*,#45746,.T.);
#60932=ORIENTED_EDGE('',*,*,#45738,.T.);
#60933=ORIENTED_EDGE('',*,*,#45726,.F.);
#60934=ORIENTED_EDGE('',*,*,#45741,.T.);
#60935=ORIENTED_EDGE('',*,*,#45744,.T.);
#60936=ORIENTED_EDGE('',*,*,#45731,.F.);
#90305=CYLINDRICAL_SURFACE('',#98886,5.15937500000002);
#90306=CYLINDRICAL_SURFACE('',#98887,5.15937500000002);
#90307=CYLINDRICAL_SURFACE('',#98888,5.15937500000008);
#90308=CYLINDRICAL_SURFACE('',#98889,5.15937500000008);
#90309=CYLINDRICAL_SURFACE('',#98890,11.3170000000002);
#90310=CYLINDRICAL_SURFACE('',#98892,9.00000000000018);
#90311=CYLINDRICAL_SURFACE('',#98896,18.0480000000001);
#90312=CYLINDRICAL_SURFACE('',#98897,18.0480000000001);
#90313=CYLINDRICAL_SURFACE('',#98898,18.0480000000001);
#90314=CYLINDRICAL_SURFACE('',#98899,18.0480000000001);
#90315=CYLINDRICAL_SURFACE('',#98900,18.0480000000001);
#90316=CYLINDRICAL_SURFACE('',#98901,18.0480000000001);
#90317=CYLINDRICAL_SURFACE('',#98902,18.0480000000001);
#90318=CYLINDRICAL_SURFACE('',#98903,18.0480000000001);
#90319=CYLINDRICAL_SURFACE('',#98904,15.);
#90320=CYLINDRICAL_SURFACE('',#98906,15.);
#90321=CYLINDRICAL_SURFACE('',#98907,15.);
#90322=CYLINDRICAL_SURFACE('',#98908,15.);
#90323=CYLINDRICAL_SURFACE('',#98909,15.);
#90324=CYLINDRICAL_SURFACE('',#98910,15.);
#90325=CYLINDRICAL_SURFACE('',#98911,15.);
#90326=CYLINDRICAL_SURFACE('',#98912,15.);
#90327=CYLINDRICAL_SURFACE('',#98913,39.);
#90328=CYLINDRICAL_SURFACE('',#98915,39.);
#90329=CYLINDRICAL_SURFACE('',#98916,39.);
#90330=CYLINDRICAL_SURFACE('',#98917,39.);
#90331=CYLINDRICAL_SURFACE('',#98918,39.);
#90332=CYLINDRICAL_SURFACE('',#98919,39.);
#90333=CYLINDRICAL_SURFACE('',#98920,39.);
#90334=CYLINDRICAL_SURFACE('',#98921,39.);
#90335=CYLINDRICAL_SURFACE('',#98922,5.15937500000002);
#90336=CYLINDRICAL_SURFACE('',#98923,5.15937500000002);
#90337=CYLINDRICAL_SURFACE('',#98924,5.15937500000008);
#90338=CYLINDRICAL_SURFACE('',#98925,5.15937500000008);
#90339=CYLINDRICAL_SURFACE('',#98926,39.);
#90340=CYLINDRICAL_SURFACE('',#98927,15.);
#90341=CYLINDRICAL_SURFACE('',#98929,11.444);
#90342=CYLINDRICAL_SURFACE('',#98934,18.0480000000001);
#92630=ADVANCED_FACE('',(#7657),#5533,.T.);
#92631=ADVANCED_FACE('',(#7658),#5534,.T.);
#92632=ADVANCED_FACE('',(#7659),#90305,.F.);
#92633=ADVANCED_FACE('',(#7660),#90306,.F.);
#92634=ADVANCED_FACE('',(#7661),#90307,.F.);
#92635=ADVANCED_FACE('',(#7662),#90308,.F.);
#92636=ADVANCED_FACE('',(#7663,#6333,#6334,#6335),#90309,.T.);
#92637=ADVANCED_FACE('',(#7664,#6336,#6337,#6338),#90310,.F.);
#92638=ADVANCED_FACE('',(#7665,#6339),#6473,.T.);
#92639=ADVANCED_FACE('',(#7666,#6340),#6474,.T.);
#92640=ADVANCED_FACE('',(#7667),#90311,.T.);
#92641=ADVANCED_FACE('',(#7668),#90312,.T.);
#92642=ADVANCED_FACE('',(#7669),#90313,.T.);
#92643=ADVANCED_FACE('',(#7670),#90314,.T.);
#92644=ADVANCED_FACE('',(#7671),#90315,.T.);
#92645=ADVANCED_FACE('',(#7672),#90316,.T.);
#92646=ADVANCED_FACE('',(#7673),#90317,.T.);
#92647=ADVANCED_FACE('',(#7674),#90318,.T.);
#92648=ADVANCED_FACE('',(#7675,#6341,#6342),#90319,.T.);
#92649=ADVANCED_FACE('',(#7676,#6343),#90320,.T.);
#92650=ADVANCED_FACE('',(#7677),#90321,.T.);
#92651=ADVANCED_FACE('',(#7678),#90322,.T.);
#92652=ADVANCED_FACE('',(#7679),#90323,.T.);
#92653=ADVANCED_FACE('',(#7680),#90324,.T.);
#92654=ADVANCED_FACE('',(#7681),#90325,.T.);
#92655=ADVANCED_FACE('',(#7682),#90326,.T.);
#92656=ADVANCED_FACE('',(#7683),#90327,.T.);
#92657=ADVANCED_FACE('',(#7684),#90328,.T.);
#92658=ADVANCED_FACE('',(#7685),#90329,.T.);
#92659=ADVANCED_FACE('',(#7686),#90330,.T.);
#92660=ADVANCED_FACE('',(#7687),#90331,.T.);
#92661=ADVANCED_FACE('',(#7688),#90332,.T.);
#92662=ADVANCED_FACE('',(#7689),#90333,.T.);
#92663=ADVANCED_FACE('',(#7690),#90334,.T.);
#92664=ADVANCED_FACE('',(#7691),#90335,.F.);
#92665=ADVANCED_FACE('',(#7692),#90336,.F.);
#92666=ADVANCED_FACE('',(#7693),#90337,.F.);
#92667=ADVANCED_FACE('',(#7694),#90338,.F.);
#92668=ADVANCED_FACE('',(#7695),#90339,.T.);
#92669=ADVANCED_FACE('',(#7696),#90340,.T.);
#92670=ADVANCED_FACE('',(#7697,#6344,#6345,#6346),#90341,.F.);
#92671=ADVANCED_FACE('',(#7698),#2501,.F.);
#92672=ADVANCED_FACE('',(#7699),#2502,.F.);
#92673=ADVANCED_FACE('',(#7700),#2503,.F.);
#92674=ADVANCED_FACE('',(#7701),#2504,.F.);
#92675=ADVANCED_FACE('',(#7702),#2505,.F.);
#92676=ADVANCED_FACE('',(#7703),#90342,.T.);
#92677=ADVANCED_FACE('',(#7704),#6475,.T.);
#92678=ADVANCED_FACE('',(#7705,#6347),#6476,.T.);
#92679=ADVANCED_FACE('',(#7706,#6348),#6477,.T.);
#98698=CLOSED_SHELL('',(#92630,#92631,#92632,#92633,#92634,#92635,#92636,
#92637,#92638,#92639));
#98699=CLOSED_SHELL('',(#92640,#92641,#92642,#92643,#92644,#92645,#92646,
#92647,#92648,#92649,#92650,#92651,#92652,#92653,#92654,#92655,#92656,#92657,
#92658,#92659,#92660,#92661,#92662,#92663,#92664,#92665,#92666,#92667,#92668,
#92669,#92670,#92671,#92672,#92673,#92674,#92675,#92676,#92677,#92678,#92679));
#98875=AXIS2_PLACEMENT_3D('',#142847,#111891,#111892);
#98876=AXIS2_PLACEMENT_3D('',#142848,#111893,#111894);
#98877=AXIS2_PLACEMENT_3D('',#142851,#111895,#111896);
#98878=AXIS2_PLACEMENT_3D('',#142852,#111897,#111898);
#98879=AXIS2_PLACEMENT_3D('',#142854,#111899,#111900);
#98880=AXIS2_PLACEMENT_3D('',#142855,#111901,#111902);
#98881=AXIS2_PLACEMENT_3D('',#142856,#111903,#111904);
#98882=AXIS2_PLACEMENT_3D('',#142858,#111905,#111906);
#98883=AXIS2_PLACEMENT_3D('',#142860,#111907,#111908);
#98884=AXIS2_PLACEMENT_3D('',#142862,#111909,#111910);
#98885=AXIS2_PLACEMENT_3D('',#142863,#111911,#111912);
#98886=AXIS2_PLACEMENT_3D('',#142864,#111913,#111914);
#98887=AXIS2_PLACEMENT_3D('',#142942,#111916,#111917);
#98888=AXIS2_PLACEMENT_3D('',#143020,#111919,#111920);
#98889=AXIS2_PLACEMENT_3D('',#143100,#111922,#111923);
#98890=AXIS2_PLACEMENT_3D('',#143180,#111925,#111926);
#98891=AXIS2_PLACEMENT_3D('',#143182,#111927,#111928);
#98892=AXIS2_PLACEMENT_3D('',#143185,#111931,#111932);
#98893=AXIS2_PLACEMENT_3D('',#143189,#111935,#111936);
#98894=AXIS2_PLACEMENT_3D('',#143190,#111937,#111938);
#98895=AXIS2_PLACEMENT_3D('',#143191,#111939,#111940);
#98896=AXIS2_PLACEMENT_3D('',#143192,#111941,#111942);
#98897=AXIS2_PLACEMENT_3D('',#143269,#111945,#111946);
#98898=AXIS2_PLACEMENT_3D('',#143411,#111948,#111949);
#98899=AXIS2_PLACEMENT_3D('',#143553,#111951,#111952);
#98900=AXIS2_PLACEMENT_3D('',#143695,#111954,#111955);
#98901=AXIS2_PLACEMENT_3D('',#143837,#111957,#111958);
#98902=AXIS2_PLACEMENT_3D('',#143979,#111960,#111961);
#98903=AXIS2_PLACEMENT_3D('',#144121,#111963,#111964);
#98904=AXIS2_PLACEMENT_3D('',#144263,#111966,#111967);
#98905=AXIS2_PLACEMENT_3D('',#144294,#111969,#111970);
#98906=AXIS2_PLACEMENT_3D('',#144393,#111973,#111974);
#98907=AXIS2_PLACEMENT_3D('',#144507,#111976,#111977);
#98908=AXIS2_PLACEMENT_3D('',#144563,#111979,#111980);
#98909=AXIS2_PLACEMENT_3D('',#144619,#111982,#111983);
#98910=AXIS2_PLACEMENT_3D('',#144675,#111985,#111986);
#98911=AXIS2_PLACEMENT_3D('',#144731,#111988,#111989);
#98912=AXIS2_PLACEMENT_3D('',#144787,#111991,#111992);
#98913=AXIS2_PLACEMENT_3D('',#144843,#111994,#111995);
#98914=AXIS2_PLACEMENT_3D('',#144875,#111997,#111998);
#98915=AXIS2_PLACEMENT_3D('',#144900,#111999,#112000);
#98916=AXIS2_PLACEMENT_3D('',#144970,#112002,#112003);
#98917=AXIS2_PLACEMENT_3D('',#145042,#112005,#112006);
#98918=AXIS2_PLACEMENT_3D('',#145114,#112008,#112009);
#98919=AXIS2_PLACEMENT_3D('',#145186,#112011,#112012);
#98920=AXIS2_PLACEMENT_3D('',#145258,#112014,#112015);
#98921=AXIS2_PLACEMENT_3D('',#145330,#112017,#112018);
#98922=AXIS2_PLACEMENT_3D('',#145402,#112020,#112021);
#98923=AXIS2_PLACEMENT_3D('',#145442,#112023,#112024);
#98924=AXIS2_PLACEMENT_3D('',#145482,#112026,#112027);
#98925=AXIS2_PLACEMENT_3D('',#145523,#112029,#112030);
#98926=AXIS2_PLACEMENT_3D('',#145564,#112032,#112033);
#98927=AXIS2_PLACEMENT_3D('',#145590,#112035,#112036);
#98928=AXIS2_PLACEMENT_3D('',#145803,#112037,#112038);
#98929=AXIS2_PLACEMENT_3D('',#145808,#112039,#112040);
#98930=AXIS2_PLACEMENT_3D('',#145810,#112041,#112042);
#98931=AXIS2_PLACEMENT_3D('',#145814,#112045,#112046);
#98932=AXIS2_PLACEMENT_3D('',#149842,#112047,#112048);
#98933=AXIS2_PLACEMENT_3D('',#167137,#112054,#112055);
#98934=AXIS2_PLACEMENT_3D('',#167139,#112057,#112058);
#98935=AXIS2_PLACEMENT_3D('',#167140,#112059,#112060);
#98936=AXIS2_PLACEMENT_3D('',#167141,#112061,#112062);
#98937=AXIS2_PLACEMENT_3D('',#167142,#112063,#112064);
#98938=AXIS2_PLACEMENT_3D('',#167143,#112065,#112066);
#111891=DIRECTION('axis',(0.,0.,1.));
#111892=DIRECTION('refdir',(1.,0.,0.));
#111893=DIRECTION('center_axis',(0.,-1.21968337170492E-16,1.));
#111894=DIRECTION('ref_axis',(0.,-1.,0.));
#111895=DIRECTION('center_axis',(0.,-1.21968337170492E-16,1.));
#111896=DIRECTION('ref_axis',(0.,-1.,-1.21968337170492E-16));
#111897=DIRECTION('center_axis',(0.,-1.21968337170492E-16,1.));
#111898=DIRECTION('ref_axis',(0.,-1.,-1.21968337170492E-16));
#111899=DIRECTION('center_axis',(-1.,-1.22464679914735E-16,-1.49368133713168E-32));
#111900=DIRECTION('ref_axis',(-1.22464679914735E-16,1.,0.));
#111901=DIRECTION('center_axis',(0.,1.21968337170492E-16,-1.));
#111902=DIRECTION('ref_axis',(0.,-1.,-1.21968337170492E-16));
#111903=DIRECTION('center_axis',(0.,-1.21968337170492E-16,1.));
#111904=DIRECTION('ref_axis',(0.,-1.,0.));
#111905=DIRECTION('center_axis',(0.,-1.21968337170492E-16,1.));
#111906=DIRECTION('ref_axis',(0.,-1.,-1.21968337170492E-16));
#111907=DIRECTION('center_axis',(-1.,-1.22464679914735E-16,-1.49368133713168E-32));
#111908=DIRECTION('ref_axis',(-1.22464679914735E-16,1.,0.));
#111909=DIRECTION('center_axis',(0.,1.21968337170492E-16,-1.));
#111910=DIRECTION('ref_axis',(0.,-1.,-1.21968337170492E-16));
#111911=DIRECTION('center_axis',(0.,1.21968337170492E-16,-1.));
#111912=DIRECTION('ref_axis',(0.,-1.,-1.21968337170492E-16));
#111913=DIRECTION('center_axis',(1.,-6.08557808619092E-15,0.));
#111914=DIRECTION('ref_axis',(6.08557808619092E-15,1.,0.));
#111915=DIRECTION('',(1.,-6.08557808619092E-15,0.));
#111916=DIRECTION('center_axis',(1.,-6.08557808619092E-15,0.));
#111917=DIRECTION('ref_axis',(6.08557808619092E-15,1.,0.));
#111918=DIRECTION('',(1.,-6.08557808619092E-15,0.));
#111919=DIRECTION('center_axis',(0.,-1.,0.));
#111920=DIRECTION('ref_axis',(0.,0.,-1.));
#111921=DIRECTION('',(0.,-1.,0.));
#111922=DIRECTION('center_axis',(0.,-1.,0.));
#111923=DIRECTION('ref_axis',(0.,0.,-1.));
#111924=DIRECTION('',(0.,-1.,0.));
#111925=DIRECTION('center_axis',(0.,1.21968337170492E-16,-1.));
#111926=DIRECTION('ref_axis',(0.,1.,1.21968337170492E-16));
#111927=DIRECTION('center_axis',(0.,1.21968337170492E-16,-1.));
#111928=DIRECTION('ref_axis',(0.,1.,1.21968337170492E-16));
#111929=DIRECTION('',(0.,-1.21968337170492E-16,1.));
#111930=DIRECTION('',(0.,-1.21968337170492E-16,1.));
#111931=DIRECTION('center_axis',(0.,1.21968337170492E-16,-1.));
#111932=DIRECTION('ref_axis',(0.,1.,1.21968337170492E-16));
#111933=DIRECTION('',(0.,1.21968337170492E-16,-1.));
#111934=DIRECTION('',(0.,1.21968337170492E-16,-1.));
#111935=DIRECTION('center_axis',(0.,1.21968337170492E-16,-1.));
#111936=DIRECTION('ref_axis',(0.,1.,1.21968337170492E-16));
#111937=DIRECTION('center_axis',(0.,-1.21968337170492E-16,1.));
#111938=DIRECTION('ref_axis',(0.,-1.,-1.21968337170492E-16));
#111939=DIRECTION('center_axis',(0.,1.21968337170492E-16,-1.));
#111940=DIRECTION('ref_axis',(0.,1.,1.21968337170492E-16));
#111941=DIRECTION('center_axis',(0.,0.,1.));
#111942=DIRECTION('ref_axis',(-2.97930117404573E-15,-1.,0.));
#111943=DIRECTION('',(0.,0.,1.));
#111944=DIRECTION('',(0.,0.,-1.));
#111945=DIRECTION('center_axis',(0.,0.,1.));
#111946=DIRECTION('ref_axis',(-2.97930117404573E-15,-1.,0.));
#111947=DIRECTION('',(0.,0.,1.));
#111948=DIRECTION('center_axis',(0.,0.,1.));
#111949=DIRECTION('ref_axis',(-2.97930117404573E-15,-1.,0.));
#111950=DIRECTION('',(0.,0.,1.));
#111951=DIRECTION('center_axis',(0.,0.,1.));
#111952=DIRECTION('ref_axis',(-2.97930117404573E-15,-1.,0.));
#111953=DIRECTION('',(0.,0.,1.));
#111954=DIRECTION('center_axis',(0.,0.,1.));
#111955=DIRECTION('ref_axis',(-2.97930117404573E-15,-1.,0.));
#111956=DIRECTION('',(0.,0.,1.));
#111957=DIRECTION('center_axis',(0.,0.,1.));
#111958=DIRECTION('ref_axis',(-2.97930117404573E-15,-1.,0.));
#111959=DIRECTION('',(0.,0.,1.));
#111960=DIRECTION('center_axis',(0.,0.,1.));
#111961=DIRECTION('ref_axis',(-2.97930117404573E-15,-1.,0.));
#111962=DIRECTION('',(0.,0.,1.));
#111963=DIRECTION('center_axis',(0.,0.,1.));
#111964=DIRECTION('ref_axis',(-2.97930117404573E-15,-1.,0.));
#111965=DIRECTION('',(0.,0.,1.));
#111966=DIRECTION('center_axis',(0.,1.21968337170492E-16,-1.));
#111967=DIRECTION('ref_axis',(0.,1.,1.21968337170492E-16));
#111968=DIRECTION('',(0.,-1.21968337170492E-16,1.));
#111969=DIRECTION('center_axis',(0.,1.21968337170492E-16,-1.));
#111970=DIRECTION('ref_axis',(0.,1.,1.21968337170492E-16));
#111971=DIRECTION('',(0.,-1.9115651027667E-14,1.));
#111972=DIRECTION('',(0.,-1.21968337170492E-16,1.));
#111973=DIRECTION('center_axis',(0.,1.21968337170492E-16,-1.));
#111974=DIRECTION('ref_axis',(0.,1.,1.21968337170492E-16));
#111975=DIRECTION('',(0.,-1.21968337170492E-16,1.));
#111976=DIRECTION('center_axis',(0.,1.21968337170492E-16,-1.));
#111977=DIRECTION('ref_axis',(0.,1.,1.21968337170492E-16));
#111978=DIRECTION('',(0.,-1.21968337170492E-16,1.));
#111979=DIRECTION('center_axis',(0.,1.21968337170492E-16,-1.));
#111980=DIRECTION('ref_axis',(0.,1.,1.21968337170492E-16));
#111981=DIRECTION('',(0.,-1.21968337170492E-16,1.));
#111982=DIRECTION('center_axis',(0.,1.21968337170492E-16,-1.));
#111983=DIRECTION('ref_axis',(0.,1.,1.21968337170492E-16));
#111984=DIRECTION('',(0.,-1.21968337170492E-16,1.));
#111985=DIRECTION('center_axis',(0.,1.21968337170492E-16,-1.));
#111986=DIRECTION('ref_axis',(0.,1.,1.21968337170492E-16));
#111987=DIRECTION('',(0.,-1.21968337170492E-16,1.));
#111988=DIRECTION('center_axis',(0.,1.21968337170492E-16,-1.));
#111989=DIRECTION('ref_axis',(0.,1.,1.21968337170492E-16));
#111990=DIRECTION('',(0.,-1.21968337170492E-16,1.));
#111991=DIRECTION('center_axis',(0.,1.21968337170492E-16,-1.));
#111992=DIRECTION('ref_axis',(0.,1.,1.21968337170492E-16));
#111993=DIRECTION('',(0.,-1.21968337170492E-16,1.));
#111994=DIRECTION('center_axis',(0.,0.,1.));
#111995=DIRECTION('ref_axis',(1.,0.,0.));
#111996=DIRECTION('',(0.,0.,-1.));
#111997=DIRECTION('center_axis',(0.,0.,-1.));
#111998=DIRECTION('ref_axis',(-1.,0.,0.));
#111999=DIRECTION('center_axis',(0.,0.,1.));
#112000=DIRECTION('ref_axis',(1.,0.,0.));
#112001=DIRECTION('',(0.,0.,-1.));
#112002=DIRECTION('center_axis',(0.,0.,1.));
#112003=DIRECTION('ref_axis',(1.,0.,0.));
#112004=DIRECTION('',(0.,0.,-1.));
#112005=DIRECTION('center_axis',(0.,0.,1.));
#112006=DIRECTION('ref_axis',(1.,0.,0.));
#112007=DIRECTION('',(0.,0.,-1.));
#112008=DIRECTION('center_axis',(0.,0.,1.));
#112009=DIRECTION('ref_axis',(1.,0.,0.));
#112010=DIRECTION('',(0.,0.,-1.));
#112011=DIRECTION('center_axis',(0.,0.,1.));
#112012=DIRECTION('ref_axis',(1.,0.,0.));
#112013=DIRECTION('',(0.,0.,-1.));
#112014=DIRECTION('center_axis',(0.,0.,1.));
#112015=DIRECTION('ref_axis',(1.,0.,0.));
#112016=DIRECTION('',(0.,0.,-1.));
#112017=DIRECTION('center_axis',(0.,0.,1.));
#112018=DIRECTION('ref_axis',(1.,0.,0.));
#112019=DIRECTION('',(0.,0.,-1.));
#112020=DIRECTION('center_axis',(1.,-6.08557808619092E-15,0.));
#112021=DIRECTION('ref_axis',(6.08557808619092E-15,1.,0.));
#112022=DIRECTION('',(1.,-6.08557808619092E-15,0.));
#112023=DIRECTION('center_axis',(1.,-6.08557808619092E-15,0.));
#112024=DIRECTION('ref_axis',(6.08557808619092E-15,1.,0.));
#112025=DIRECTION('',(1.,-6.08557808619092E-15,0.));
#112026=DIRECTION('center_axis',(0.,-1.,0.));
#112027=DIRECTION('ref_axis',(0.,0.,-1.));
#112028=DIRECTION('',(0.,-1.,0.));
#112029=DIRECTION('center_axis',(0.,-1.,0.));
#112030=DIRECTION('ref_axis',(0.,0.,-1.));
#112031=DIRECTION('',(0.,-1.,0.));
#112032=DIRECTION('center_axis',(0.,0.,1.));
#112033=DIRECTION('ref_axis',(1.,0.,0.));
#112034=DIRECTION('',(0.,0.,-1.));
#112035=DIRECTION('center_axis',(0.,1.21968337170492E-16,-1.));
#112036=DIRECTION('ref_axis',(0.,1.,1.21968337170492E-16));
#112037=DIRECTION('center_axis',(0.,0.,1.));
#112038=DIRECTION('ref_axis',(-1.,0.,0.));
#112039=DIRECTION('center_axis',(0.,1.21968337170492E-16,-1.));
#112040=DIRECTION('ref_axis',(0.,1.,1.21968337170492E-16));
#112041=DIRECTION('center_axis',(0.,1.21968337170492E-16,-1.));
#112042=DIRECTION('ref_axis',(0.,1.,1.21968337170492E-16));
#112043=DIRECTION('',(0.,1.21968337170492E-16,-1.));
#112044=DIRECTION('',(0.,1.21968337170492E-16,-1.));
#112045=DIRECTION('center_axis',(0.,0.,-1.));
#112046=DIRECTION('ref_axis',(-1.,0.,0.));
#112047=DIRECTION('center_axis',(-1.33967923098245E-7,-2.70052261735722E-8,
-0.999999999999991));
#112048=DIRECTION('ref_axis',(0.526776707081478,0.850003706389793,-9.352572372367E-8));
#112049=DIRECTION('',(0.,0.999447421660403,-0.0332393040897854));
#112050=DIRECTION('',(0.,-0.999447421660403,-0.0332393040897854));
#112051=DIRECTION('',(0.00929884004822234,0.99995676485224,0.));
#112052=DIRECTION('',(0.,-1.,0.));
#112053=DIRECTION('',(0.,1.,0.));
#112054=DIRECTION('center_axis',(-4.45046801311947E-10,1.54454672436889E-9,
-1.));
#112055=DIRECTION('ref_axis',(-0.292280983426921,0.956332487541332,1.60717892779798E-9));
#112056=DIRECTION('',(0.,0.,-1.));
#112057=DIRECTION('center_axis',(0.,0.,1.));
#112058=DIRECTION('ref_axis',(-2.97930117404573E-15,-1.,0.));
#112059=DIRECTION('center_axis',(2.58127960627592E-11,3.98865904338256E-9,
-1.));
#112060=DIRECTION('ref_axis',(0.00677738398148346,0.999977033269448,3.98874238015561E-9));
#112061=DIRECTION('center_axis',(1.,0.,0.));
#112062=DIRECTION('ref_axis',(0.,0.,-1.));
#112063=DIRECTION('center_axis',(0.,-1.21968337170492E-16,1.));
#112064=DIRECTION('ref_axis',(0.,-1.,-1.21968337170492E-16));
#112065=DIRECTION('center_axis',(0.,0.,-1.));
#112066=DIRECTION('ref_axis',(-1.,0.,0.));
#142847=CARTESIAN_POINT('',(0.,0.,0.));
#142848=CARTESIAN_POINT('Origin',(0.,-1.83525269067091E-13,1504.696));
#142849=CARTESIAN_POINT('',(1.10218211923264E-15,-9.00000000000036,1504.696));
#142850=CARTESIAN_POINT('',(-1.10218211923264E-15,8.99999999999999,1504.696));
#142851=CARTESIAN_POINT('Origin',(0.,-1.83525269067091E-13,1504.696));
#142852=CARTESIAN_POINT('Origin',(0.,-1.83525269067091E-13,1504.696));
#142853=CARTESIAN_POINT('',(-1.13328814793098E-15,9.254,1504.95));
#142854=CARTESIAN_POINT('Origin',(-1.13328814793098E-15,9.254,1504.696));
#142855=CARTESIAN_POINT('Origin',(0.,-1.83556249024732E-13,1504.95));
#142856=CARTESIAN_POINT('Origin',(0.,-1.83525269067091E-13,1504.696));
#142857=CARTESIAN_POINT('',(-1.35482675389674E-15,11.063,1504.95));
#142858=CARTESIAN_POINT('Origin',(0.,-1.83556249024732E-13,1504.95));
#142859=CARTESIAN_POINT('',(-1.38593278259508E-15,11.317,1504.696));
#142860=CARTESIAN_POINT('Origin',(-1.35482675389674E-15,11.063,1504.696));
#142861=CARTESIAN_POINT('',(1.38593278259508E-15,-11.3170000000004,1504.696));
#142862=CARTESIAN_POINT('Origin',(0.,-1.83525269067091E-13,1504.696));
#142863=CARTESIAN_POINT('Origin',(0.,-1.83525269067091E-13,1504.696));
#142864=CARTESIAN_POINT('Origin',(-51.0189817055138,1.6136547197417E-13,
1492.25));
#142865=CARTESIAN_POINT('',(-10.0725040883277,5.15937499999993,1492.25));
#142866=CARTESIAN_POINT('',(-10.0725040883278,-5.15937500000011,1492.25));
#142867=CARTESIAN_POINT('Ctrl Pts',(-10.0725040883277,5.15937499999994,
1492.25));
#142868=CARTESIAN_POINT('Ctrl Pts',(-10.0725040883277,5.15937499999994,
1491.5908449252));
#142869=CARTESIAN_POINT('Ctrl Pts',(-10.1440843535216,5.02564501462724,
1490.8958794792));
#142870=CARTESIAN_POINT('Ctrl Pts',(-10.3894819155763,4.4964667402695,1489.62844582463));
#142871=CARTESIAN_POINT('Ctrl Pts',(-10.5585230349077,4.10136924643432,
1489.05491114807));
#142872=CARTESIAN_POINT('Ctrl Pts',(-10.866877089651,3.19590327436256,1488.14944517599));
#142873=CARTESIAN_POINT('Ctrl Pts',(-11.0278903257137,2.62207755819461,
1487.75374024113));
#142874=CARTESIAN_POINT('Ctrl Pts',(-11.254236928579,1.35344266229487,1487.22408350872));
#142875=CARTESIAN_POINT('Ctrl Pts',(-11.3170000000002,0.657970384764705,
1487.090625));
#142876=CARTESIAN_POINT('Ctrl Pts',(-11.3170000000002,-0.657970384764866,
1487.090625));
#142877=CARTESIAN_POINT('Ctrl Pts',(-11.254236928579,-1.35344266229482,
1487.22408350872));
#142878=CARTESIAN_POINT('Ctrl Pts',(-11.0278903257138,-2.62207755819449,
1487.75374024113));
#142879=CARTESIAN_POINT('Ctrl Pts',(-10.866877089651,-3.19590327436272,
1488.14944517599));
#142880=CARTESIAN_POINT('Ctrl Pts',(-10.5585230349078,-4.10136924643449,
1489.05491114807));
#142881=CARTESIAN_POINT('Ctrl Pts',(-10.3894819155764,-4.49646674026967,
1489.62844582463));
#142882=CARTESIAN_POINT('Ctrl Pts',(-10.1440843535217,-5.02564501462741,
1490.8958794792));
#142883=CARTESIAN_POINT('Ctrl Pts',(-10.0725040883278,-5.15937500000011,
1491.5908449252));
#142884=CARTESIAN_POINT('Ctrl Pts',(-10.0725040883278,-5.15937500000011,
1492.25));
#142885=CARTESIAN_POINT('',(-7.37433723187231,-5.15937500000013,1492.25));
#142886=CARTESIAN_POINT('',(-51.0189817055139,-5.15937499999986,1492.25));
#142887=CARTESIAN_POINT('',(-7.37433723187225,5.15937499999992,1492.25));
#142888=CARTESIAN_POINT('Ctrl Pts',(-7.37433723187237,-5.1593750000001,
1492.25));
#142889=CARTESIAN_POINT('Ctrl Pts',(-7.37433723187237,-5.15937500000011,
1491.5821328984));
#142890=CARTESIAN_POINT('Ctrl Pts',(-7.47468272092302,-5.0226214370987,
1490.88541735607));
#142891=CARTESIAN_POINT('Ctrl Pts',(-7.80496687696187,-4.49222528611439,
1489.62155204094));
#142892=CARTESIAN_POINT('Ctrl Pts',(-8.02760290754501,-4.09885081991491,
1489.05239272155));
#142893=CARTESIAN_POINT('Ctrl Pts',(-8.42620218982163,-3.19993704609044,
1488.15347894772));
#142894=CARTESIAN_POINT('Ctrl Pts',(-8.63162196667481,-2.63009169102994,
1487.75845526816));
#142895=CARTESIAN_POINT('Ctrl Pts',(-8.91992322022013,-1.36280970424654,
1487.22664378595));
#142896=CARTESIAN_POINT('Ctrl Pts',(-9.00000000000018,-0.664414150007918,
1487.090625));
#142897=CARTESIAN_POINT('Ctrl Pts',(-9.00000000000017,0.664414150007731,
1487.090625));
#142898=CARTESIAN_POINT('Ctrl Pts',(-8.9199232202201,1.36280970424636,1487.22664378595));
#142899=CARTESIAN_POINT('Ctrl Pts',(-8.63162196667476,2.63009169102975,
1487.75845526816));
#142900=CARTESIAN_POINT('Ctrl Pts',(-8.42620218982157,3.19993704609025,
1488.15347894772));
#142901=CARTESIAN_POINT('Ctrl Pts',(-8.02760290754492,4.09885081991471,
1489.05239272155));
#142902=CARTESIAN_POINT('Ctrl Pts',(-7.80496687696178,4.49222528611418,
1489.62155204094));
#142903=CARTESIAN_POINT('Ctrl Pts',(-7.47468272092292,5.02262143709849,
1490.88541735607));
#142904=CARTESIAN_POINT('Ctrl Pts',(-7.37433723187224,5.15937499999992,
1491.5821328984));
#142905=CARTESIAN_POINT('Ctrl Pts',(-7.37433723187224,5.15937499999992,
1492.25));
#142906=CARTESIAN_POINT('Ctrl Pts',(-7.37433723187225,5.15937499999991,
1492.25));
#142907=CARTESIAN_POINT('Ctrl Pts',(-7.37433723187225,5.15937499999991,
1492.9178671016));
#142908=CARTESIAN_POINT('Ctrl Pts',(-7.47468272092287,5.02262143709855,
1493.61458264393));
#142909=CARTESIAN_POINT('Ctrl Pts',(-7.80496687696175,4.49222528611424,
1494.87844795906));
#142910=CARTESIAN_POINT('Ctrl Pts',(-8.02760290754492,4.09885081991471,
1495.44760727845));
#142911=CARTESIAN_POINT('Ctrl Pts',(-8.42620218982157,3.19993704609025,
1496.34652105228));
#142912=CARTESIAN_POINT('Ctrl Pts',(-8.63162196667476,2.63009169102975,
1496.74154473184));
#142913=CARTESIAN_POINT('Ctrl Pts',(-8.9199232202201,1.36280970424635,1497.27335621405));
#142914=CARTESIAN_POINT('Ctrl Pts',(-9.00000000000017,0.664414150007731,
1497.409375));
#142915=CARTESIAN_POINT('Ctrl Pts',(-9.00000000000018,-0.664414150007918,
1497.409375));
#142916=CARTESIAN_POINT('Ctrl Pts',(-8.9199232202201,-1.36280970424675,
1497.27335621405));
#142917=CARTESIAN_POINT('Ctrl Pts',(-8.63162196667478,-2.63009169103002,
1496.74154473184));
#142918=CARTESIAN_POINT('Ctrl Pts',(-8.42620218982163,-3.19993704609044,
1496.34652105228));
#142919=CARTESIAN_POINT('Ctrl Pts',(-8.02760290754501,-4.09885081991491,
1495.44760727845));
#142920=CARTESIAN_POINT('Ctrl Pts',(-7.80496687696187,-4.49222528611439,
1494.87844795906));
#142921=CARTESIAN_POINT('Ctrl Pts',(-7.47468272092302,-5.0226214370987,
1493.61458264393));
#142922=CARTESIAN_POINT('Ctrl Pts',(-7.37433723187236,-5.15937500000012,
1492.9178671016));
#142923=CARTESIAN_POINT('Ctrl Pts',(-7.37433723187236,-5.15937500000012,
1492.25));
#142924=CARTESIAN_POINT('Ctrl Pts',(-10.0725040883278,-5.1593750000001,
1492.25));
#142925=CARTESIAN_POINT('Ctrl Pts',(-10.0725040883278,-5.1593750000001,
1492.9091550748));
#142926=CARTESIAN_POINT('Ctrl Pts',(-10.1440843535217,-5.02564501462741,
1493.6041205208));
#142927=CARTESIAN_POINT('Ctrl Pts',(-10.3894819155764,-4.49646674026967,
1494.87155417537));
#142928=CARTESIAN_POINT('Ctrl Pts',(-10.5585230349078,-4.10136924643449,
1495.44508885193));
#142929=CARTESIAN_POINT('Ctrl Pts',(-10.866877089651,-3.19590327436273,
1496.35055482401));
#142930=CARTESIAN_POINT('Ctrl Pts',(-11.0278903257138,-2.62207755819477,
1496.74625975887));
#142931=CARTESIAN_POINT('Ctrl Pts',(-11.254236928579,-1.35344266229503,
1497.27591649128));
#142932=CARTESIAN_POINT('Ctrl Pts',(-11.3170000000002,-0.657970384764865,
1497.409375));
#142933=CARTESIAN_POINT('Ctrl Pts',(-11.3170000000002,0.657970384764708,
1497.409375));
#142934=CARTESIAN_POINT('Ctrl Pts',(-11.254236928579,1.35344266229487,1497.27591649128));
#142935=CARTESIAN_POINT('Ctrl Pts',(-11.0278903257137,2.62207755819461,
1496.74625975887));
#142936=CARTESIAN_POINT('Ctrl Pts',(-10.866877089651,3.19590327436256,1496.35055482401));
#142937=CARTESIAN_POINT('Ctrl Pts',(-10.5585230349077,4.10136924643432,
1495.44508885193));
#142938=CARTESIAN_POINT('Ctrl Pts',(-10.3894819155763,4.4964667402695,1494.87155417537));
#142939=CARTESIAN_POINT('Ctrl Pts',(-10.1440843535216,5.02564501462724,
1493.6041205208));
#142940=CARTESIAN_POINT('Ctrl Pts',(-10.0725040883277,5.15937499999996,
1492.9091550748));
#142941=CARTESIAN_POINT('Ctrl Pts',(-10.0725040883277,5.15937499999996,
1492.25));
#142942=CARTESIAN_POINT('Origin',(-51.0189817055138,1.6136547197417E-13,
1492.25));
#142943=CARTESIAN_POINT('',(7.37433723187231,5.15937499999983,1492.25));
#142944=CARTESIAN_POINT('',(7.37433723187222,-5.15937500000021,1492.25));
#142945=CARTESIAN_POINT('Ctrl Pts',(7.37433723187231,5.15937499999983,1492.25));
#142946=CARTESIAN_POINT('Ctrl Pts',(7.3743372318723,5.15937499999983,1491.5821328984));
#142947=CARTESIAN_POINT('Ctrl Pts',(7.47468272092298,5.0226214370984,1490.88541735607));
#142948=CARTESIAN_POINT('Ctrl Pts',(7.80496687696183,4.49222528611409,1489.62155204094));
#142949=CARTESIAN_POINT('Ctrl Pts',(8.02760290754497,4.09885081991462,1489.05239272155));
#142950=CARTESIAN_POINT('Ctrl Pts',(8.42620218982161,3.19993704609015,1488.15347894772));
#142951=CARTESIAN_POINT('Ctrl Pts',(8.63162196667479,2.63009169102964,1487.75845526816));
#142952=CARTESIAN_POINT('Ctrl Pts',(8.91992322022012,1.36280970424625,1487.22664378595));
#142953=CARTESIAN_POINT('Ctrl Pts',(9.00000000000018,0.664414150007621,
1487.090625));
#142954=CARTESIAN_POINT('Ctrl Pts',(9.00000000000018,-0.664414150008029,
1487.090625));
#142955=CARTESIAN_POINT('Ctrl Pts',(8.91992322022011,-1.36280970424665,
1487.22664378595));
#142956=CARTESIAN_POINT('Ctrl Pts',(8.63162196667478,-2.63009169103005,
1487.75845526816));
#142957=CARTESIAN_POINT('Ctrl Pts',(8.4262021898216,-3.19993704609055,1488.15347894772));
#142958=CARTESIAN_POINT('Ctrl Pts',(8.02760290754496,-4.09885081991501,
1489.05239272155));
#142959=CARTESIAN_POINT('Ctrl Pts',(7.80496687696182,-4.49222528611448,
1489.62155204094));
#142960=CARTESIAN_POINT('Ctrl Pts',(7.47468272092296,-5.02262143709879,
1490.88541735607));
#142961=CARTESIAN_POINT('Ctrl Pts',(7.3743372318723,-5.1593750000002,1491.5821328984));
#142962=CARTESIAN_POINT('Ctrl Pts',(7.3743372318723,-5.15937500000019,1492.25));
#142963=CARTESIAN_POINT('',(10.0725040883277,-5.15937500000024,1492.25));
#142964=CARTESIAN_POINT('',(-51.0189817055139,-5.15937499999986,1492.25));
#142965=CARTESIAN_POINT('',(10.0725040883277,5.15937499999981,1492.25));
#142966=CARTESIAN_POINT('Ctrl Pts',(10.0725040883277,-5.15937500000025,
1492.25));
#142967=CARTESIAN_POINT('Ctrl Pts',(10.0725040883277,-5.15937500000025,
1491.5908449252));
#142968=CARTESIAN_POINT('Ctrl Pts',(10.1440843535216,-5.02564501462754,
1490.8958794792));
#142969=CARTESIAN_POINT('Ctrl Pts',(10.3894819155763,-4.4964667402698,1489.62844582463));
#142970=CARTESIAN_POINT('Ctrl Pts',(10.5585230349078,-4.10136924643461,
1489.05491114807));
#142971=CARTESIAN_POINT('Ctrl Pts',(10.866877089651,-3.19590327436286,1488.14944517599));
#142972=CARTESIAN_POINT('Ctrl Pts',(11.0278903257137,-2.62207755819491,
1487.75374024113));
#142973=CARTESIAN_POINT('Ctrl Pts',(11.254236928579,-1.35344266229517,1487.22408350872));
#142974=CARTESIAN_POINT('Ctrl Pts',(11.3170000000002,-0.657970384765003,
1487.090625));
#142975=CARTESIAN_POINT('Ctrl Pts',(11.3170000000002,0.657970384764568,
1487.090625));
#142976=CARTESIAN_POINT('Ctrl Pts',(11.254236928579,1.35344266229473,1487.22408350872));
#142977=CARTESIAN_POINT('Ctrl Pts',(11.0278903257137,2.62207755819447,1487.75374024113));
#142978=CARTESIAN_POINT('Ctrl Pts',(10.866877089651,3.19590327436243,1488.14944517599));
#142979=CARTESIAN_POINT('Ctrl Pts',(10.5585230349078,4.10136924643419,1489.05491114807));
#142980=CARTESIAN_POINT('Ctrl Pts',(10.3894819155764,4.49646674026938,1489.62844582463));
#142981=CARTESIAN_POINT('Ctrl Pts',(10.1440843535216,5.02564501462711,1490.8958794792));
#142982=CARTESIAN_POINT('Ctrl Pts',(10.0725040883277,5.15937499999981,1491.5908449252));
#142983=CARTESIAN_POINT('Ctrl Pts',(10.0725040883277,5.15937499999981,1492.25));
#142984=CARTESIAN_POINT('Ctrl Pts',(10.0725040883277,5.15937499999983,1492.25));
#142985=CARTESIAN_POINT('Ctrl Pts',(10.0725040883277,5.15937499999983,1492.9091550748));
#142986=CARTESIAN_POINT('Ctrl Pts',(10.1440843535216,5.02564501462711,1493.6041205208));
#142987=CARTESIAN_POINT('Ctrl Pts',(10.3894819155764,4.49646674026938,1494.87155417537));
#142988=CARTESIAN_POINT('Ctrl Pts',(10.5585230349078,4.10136924643419,1495.44508885193));
#142989=CARTESIAN_POINT('Ctrl Pts',(10.866877089651,3.19590327436243,1496.35055482401));
#142990=CARTESIAN_POINT('Ctrl Pts',(11.0278903257137,2.62207755819446,1496.74625975887));
#142991=CARTESIAN_POINT('Ctrl Pts',(11.254236928579,1.35344266229473,1497.27591649128));
#142992=CARTESIAN_POINT('Ctrl Pts',(11.3170000000002,0.657970384764568,
1497.409375));
#142993=CARTESIAN_POINT('Ctrl Pts',(11.3170000000002,-0.657970384765003,
1497.409375));
#142994=CARTESIAN_POINT('Ctrl Pts',(11.254236928579,-1.35344266229517,1497.27591649128));
#142995=CARTESIAN_POINT('Ctrl Pts',(11.0278903257137,-2.62207755819491,
1496.74625975887));
#142996=CARTESIAN_POINT('Ctrl Pts',(10.866877089651,-3.19590327436286,1496.35055482401));
#142997=CARTESIAN_POINT('Ctrl Pts',(10.5585230349078,-4.10136924643461,
1495.44508885193));
#142998=CARTESIAN_POINT('Ctrl Pts',(10.3894819155763,-4.4964667402698,1494.87155417537));
#142999=CARTESIAN_POINT('Ctrl Pts',(10.1440843535216,-5.02564501462754,
1493.6041205208));
#143000=CARTESIAN_POINT('Ctrl Pts',(10.0725040883277,-5.15937500000024,
1492.9091550748));
#143001=CARTESIAN_POINT('Ctrl Pts',(10.0725040883277,-5.15937500000024,
1492.25));
#143002=CARTESIAN_POINT('Ctrl Pts',(7.37433723187228,-5.15937500000022,
1492.25));
#143003=CARTESIAN_POINT('Ctrl Pts',(7.37433723187228,-5.15937500000023,
1492.9178671016));
#143004=CARTESIAN_POINT('Ctrl Pts',(7.47468272092296,-5.02262143709879,
1493.61458264393));
#143005=CARTESIAN_POINT('Ctrl Pts',(7.80496687696182,-4.49222528611448,
1494.87844795906));
#143006=CARTESIAN_POINT('Ctrl Pts',(8.02760290754496,-4.09885081991501,
1495.44760727845));
#143007=CARTESIAN_POINT('Ctrl Pts',(8.4262021898216,-3.19993704609055,1496.34652105228));
#143008=CARTESIAN_POINT('Ctrl Pts',(8.63162196667478,-2.63009169103005,
1496.74154473184));
#143009=CARTESIAN_POINT('Ctrl Pts',(8.91992322022011,-1.36280970424665,
1497.27335621405));
#143010=CARTESIAN_POINT('Ctrl Pts',(9.00000000000018,-0.664414150008027,
1497.409375));
#143011=CARTESIAN_POINT('Ctrl Pts',(9.00000000000018,0.664414150007622,
1497.409375));
#143012=CARTESIAN_POINT('Ctrl Pts',(8.91992322022012,1.36280970424625,1497.27335621405));
#143013=CARTESIAN_POINT('Ctrl Pts',(8.63162196667479,2.63009169102964,1496.74154473184));
#143014=CARTESIAN_POINT('Ctrl Pts',(8.42620218982161,3.19993704609015,1496.34652105228));
#143015=CARTESIAN_POINT('Ctrl Pts',(8.02760290754497,4.09885081991462,1495.44760727845));
#143016=CARTESIAN_POINT('Ctrl Pts',(7.80496687696183,4.49222528611409,1494.87844795906));
#143017=CARTESIAN_POINT('Ctrl Pts',(7.47468272092298,5.0226214370984,1493.61458264393));
#143018=CARTESIAN_POINT('Ctrl Pts',(7.37433723187231,5.15937499999982,1492.9178671016));
#143019=CARTESIAN_POINT('Ctrl Pts',(7.37433723187231,5.15937499999982,1492.25));
#143020=CARTESIAN_POINT('Origin',(0.,50.8013494805973,1441.45));
#143021=CARTESIAN_POINT('',(1.84349851574185E-21,11.317,1436.290625));
#143022=CARTESIAN_POINT('',(-6.31841207935097E-16,11.317,1446.609375));
#143023=CARTESIAN_POINT('Ctrl Pts',(-2.24820162486594E-14,11.317,1436.290625));
#143024=CARTESIAN_POINT('Ctrl Pts',(-0.657970384764816,11.317,1436.290625));
#143025=CARTESIAN_POINT('Ctrl Pts',(-1.35344266229499,11.2542369285788,
1436.42408350872));
#143026=CARTESIAN_POINT('Ctrl Pts',(-2.62207755819474,11.0278903257136,
1436.95374024113));
#143027=CARTESIAN_POINT('Ctrl Pts',(-3.19590327436269,10.8668770896508,
1437.34944517599));
#143028=CARTESIAN_POINT('Ctrl Pts',(-4.10136924643445,10.5585230349076,
1438.25491114807));
#143029=CARTESIAN_POINT('Ctrl Pts',(-4.49646674026965,10.3894819155762,
1438.82844582463));
#143030=CARTESIAN_POINT('Ctrl Pts',(-5.02564501462738,10.1440843535214,
1440.0958794792));
#143031=CARTESIAN_POINT('Ctrl Pts',(-5.15937500000008,10.0725040883275,
1440.7908449252));
#143032=CARTESIAN_POINT('Ctrl Pts',(-5.15937500000008,10.0725040883275,
1441.45));
#143033=CARTESIAN_POINT('Ctrl Pts',(-5.15937500000008,10.0725040883275,
1442.1091550748));
#143034=CARTESIAN_POINT('Ctrl Pts',(-5.02564501462738,10.1440843535214,
1442.8041205208));
#143035=CARTESIAN_POINT('Ctrl Pts',(-4.49646674026965,10.3894819155762,
1444.07155417537));
#143036=CARTESIAN_POINT('Ctrl Pts',(-4.10136924643444,10.5585230349076,
1444.64508885193));
#143037=CARTESIAN_POINT('Ctrl Pts',(-3.19590327436268,10.8668770896508,
1445.55055482401));
#143038=CARTESIAN_POINT('Ctrl Pts',(-2.62207755819474,11.0278903257136,
1445.94625975887));
#143039=CARTESIAN_POINT('Ctrl Pts',(-1.35344266229499,11.2542369285788,
1446.47591649128));
#143040=CARTESIAN_POINT('Ctrl Pts',(-0.657970384764796,11.317,1446.609375));
#143041=CARTESIAN_POINT('Ctrl Pts',(-3.7470027081099E-15,11.317,1446.609375));
#143042=CARTESIAN_POINT('',(-4.2017011901556E-15,9.,1446.609375));
#143043=CARTESIAN_POINT('',(-6.31841207935097E-16,50.8013494805973,1446.609375));
#143044=CARTESIAN_POINT('',(-1.55306990715387E-27,9.,1436.290625));
#143045=CARTESIAN_POINT('Ctrl Pts',(-1.11022302462516E-15,9.,1446.609375));
#143046=CARTESIAN_POINT('Ctrl Pts',(-0.664414150007834,9.,1446.609375));
#143047=CARTESIAN_POINT('Ctrl Pts',(-1.36280970424649,8.91992322021993,
1446.47335621405));
#143048=CARTESIAN_POINT('Ctrl Pts',(-2.6300916910299,8.6316219666746,1445.94154473184));
#143049=CARTESIAN_POINT('Ctrl Pts',(-3.19993704609039,8.42620218982141,
1445.54652105228));
#143050=CARTESIAN_POINT('Ctrl Pts',(-4.09885081991486,8.02760290754477,
1444.64760727845));
#143051=CARTESIAN_POINT('Ctrl Pts',(-4.49222528611435,7.80496687696161,
1444.07844795906));
#143052=CARTESIAN_POINT('Ctrl Pts',(-5.02262143709865,7.47468272092276,
1442.81458264393));
#143053=CARTESIAN_POINT('Ctrl Pts',(-5.15937500000008,7.37433723187208,
1442.1178671016));
#143054=CARTESIAN_POINT('Ctrl Pts',(-5.15937500000008,7.37433723187208,
1441.45));
#143055=CARTESIAN_POINT('Ctrl Pts',(-5.15937500000008,7.37433723187208,
1440.7821328984));
#143056=CARTESIAN_POINT('Ctrl Pts',(-5.02262143709865,7.47468272092276,
1440.08541735607));
#143057=CARTESIAN_POINT('Ctrl Pts',(-4.49222528611435,7.80496687696161,
1438.82155204094));
#143058=CARTESIAN_POINT('Ctrl Pts',(-4.09885081991486,8.02760290754477,
1438.25239272155));
#143059=CARTESIAN_POINT('Ctrl Pts',(-3.19993704609039,8.42620218982141,
1437.35347894772));
#143060=CARTESIAN_POINT('Ctrl Pts',(-2.63009169102989,8.6316219666746,1436.95845526816));
#143061=CARTESIAN_POINT('Ctrl Pts',(-1.36280970424649,8.91992322021993,
1436.42664378595));
#143062=CARTESIAN_POINT('Ctrl Pts',(-0.664414150007838,9.,1436.290625));
#143063=CARTESIAN_POINT('Ctrl Pts',(-5.48172618408671E-15,9.,1436.290625));
#143064=CARTESIAN_POINT('Ctrl Pts',(-2.91433543964104E-15,9.00000000000001,
1436.290625));
#143065=CARTESIAN_POINT('Ctrl Pts',(0.66441415000783,9.00000000000001,1436.290625));
#143066=CARTESIAN_POINT('Ctrl Pts',(1.36280970424649,8.91992322021993,1436.42664378595));
#143067=CARTESIAN_POINT('Ctrl Pts',(2.6300916910299,8.6316219666746,1436.95845526816));
#143068=CARTESIAN_POINT('Ctrl Pts',(3.19993704609039,8.42620218982141,1437.35347894772));
#143069=CARTESIAN_POINT('Ctrl Pts',(4.09885081991486,8.02760290754477,1438.25239272155));
#143070=CARTESIAN_POINT('Ctrl Pts',(4.49222528611408,7.80496687696178,1438.82155204094));
#143071=CARTESIAN_POINT('Ctrl Pts',(5.02262143709853,7.47468272092284,1440.08541735607));
#143072=CARTESIAN_POINT('Ctrl Pts',(5.15937500000008,7.37433723187208,1440.7821328984));
#143073=CARTESIAN_POINT('Ctrl Pts',(5.15937500000008,7.37433723187208,1442.1178671016));
#143074=CARTESIAN_POINT('Ctrl Pts',(5.02262143709865,7.47468272092276,1442.81458264393));
#143075=CARTESIAN_POINT('Ctrl Pts',(4.49222528611435,7.80496687696161,1444.07844795906));
#143076=CARTESIAN_POINT('Ctrl Pts',(4.09885081991486,8.02760290754477,1444.64760727845));
#143077=CARTESIAN_POINT('Ctrl Pts',(3.19993704609039,8.42620218982141,1445.54652105228));
#143078=CARTESIAN_POINT('Ctrl Pts',(2.63009169102989,8.6316219666746,1445.94154473184));
#143079=CARTESIAN_POINT('Ctrl Pts',(1.36280970424649,8.91992322021993,1446.47335621405));
#143080=CARTESIAN_POINT('Ctrl Pts',(0.664414150007821,9.,1446.609375));
#143081=CARTESIAN_POINT('Ctrl Pts',(-1.15879528195251E-14,9.,1446.609375));
#143082=CARTESIAN_POINT('Ctrl Pts',(6.10622663543836E-15,11.317,1446.609375));
#143083=CARTESIAN_POINT('Ctrl Pts',(0.6579703847648,11.317,1446.609375));
#143084=CARTESIAN_POINT('Ctrl Pts',(1.35344266229499,11.2542369285788,1446.47591649128));
#143085=CARTESIAN_POINT('Ctrl Pts',(2.62207755819474,11.0278903257136,1445.94625975887));
#143086=CARTESIAN_POINT('Ctrl Pts',(3.19590327436269,10.8668770896508,1445.55055482401));
#143087=CARTESIAN_POINT('Ctrl Pts',(4.10136924643444,10.5585230349076,1444.64508885193));
#143088=CARTESIAN_POINT('Ctrl Pts',(4.49646674026965,10.3894819155762,1444.07155417537));
#143089=CARTESIAN_POINT('Ctrl Pts',(5.02564501462738,10.1440843535214,1442.8041205208));
#143090=CARTESIAN_POINT('Ctrl Pts',(5.15937500000008,10.0725040883275,1442.1091550748));
#143091=CARTESIAN_POINT('Ctrl Pts',(5.15937500000008,10.0725040883275,1440.7908449252));
#143092=CARTESIAN_POINT('Ctrl Pts',(5.02564501462738,10.1440843535214,1440.0958794792));
#143093=CARTESIAN_POINT('Ctrl Pts',(4.49646674026965,10.3894819155762,1438.82844582463));
#143094=CARTESIAN_POINT('Ctrl Pts',(4.10136924643445,10.5585230349076,1438.25491114807));
#143095=CARTESIAN_POINT('Ctrl Pts',(3.19590327436269,10.8668770896508,1437.34944517599));
#143096=CARTESIAN_POINT('Ctrl Pts',(2.62207755819474,11.0278903257136,1436.95374024113));
#143097=CARTESIAN_POINT('Ctrl Pts',(1.35344266229499,11.2542369285788,1436.42408350872));
#143098=CARTESIAN_POINT('Ctrl Pts',(0.657970384764793,11.317,1436.290625));
#143099=CARTESIAN_POINT('Ctrl Pts',(1.38777878078145E-16,11.317,1436.290625));
#143100=CARTESIAN_POINT('Origin',(0.,50.8013494805973,1441.45));
#143101=CARTESIAN_POINT('',(-5.72393189099081E-15,-9.00000000000036,1436.290625));
#143102=CARTESIAN_POINT('',(-3.68128414736255E-15,-9.00000000000036,1446.609375));
#143103=CARTESIAN_POINT('Ctrl Pts',(4.30211422042248E-15,-9.00000000000036,
1436.290625));
#143104=CARTESIAN_POINT('Ctrl Pts',(-0.664414150007829,-9.00000000000036,
1436.290625));
#143105=CARTESIAN_POINT('Ctrl Pts',(-1.36280970424649,-8.91992322022029,
1436.42664378595));
#143106=CARTESIAN_POINT('Ctrl Pts',(-2.6300916910299,-8.63162196667495,
1436.95845526816));
#143107=CARTESIAN_POINT('Ctrl Pts',(-3.19993704609039,-8.42620218982176,
1437.35347894772));
#143108=CARTESIAN_POINT('Ctrl Pts',(-4.09885081991486,-8.02760290754512,
1438.25239272155));
#143109=CARTESIAN_POINT('Ctrl Pts',(-4.49222528611435,-7.80496687696196,
1438.82155204094));
#143110=CARTESIAN_POINT('Ctrl Pts',(-5.02262143709865,-7.47468272092311,
1440.08541735607));
#143111=CARTESIAN_POINT('Ctrl Pts',(-5.15937500000008,-7.37433723187243,
1440.7821328984));
#143112=CARTESIAN_POINT('Ctrl Pts',(-5.15937500000008,-7.37433723187243,
1441.45));
#143113=CARTESIAN_POINT('Ctrl Pts',(-5.15937500000008,-7.37433723187243,
1442.1178671016));
#143114=CARTESIAN_POINT('Ctrl Pts',(-5.02262143709865,-7.47468272092311,
1442.81458264393));
#143115=CARTESIAN_POINT('Ctrl Pts',(-4.49222528611435,-7.80496687696197,
1444.07844795906));
#143116=CARTESIAN_POINT('Ctrl Pts',(-4.09885081991486,-8.02760290754512,
1444.64760727845));
#143117=CARTESIAN_POINT('Ctrl Pts',(-3.19993704609039,-8.42620218982176,
1445.54652105228));
#143118=CARTESIAN_POINT('Ctrl Pts',(-2.63009169102989,-8.63162196667495,
1445.94154473184));
#143119=CARTESIAN_POINT('Ctrl Pts',(-1.36280970424649,-8.91992322022029,
1446.47335621405));
#143120=CARTESIAN_POINT('Ctrl Pts',(-0.664414150007844,-9.00000000000035,
1446.609375));
#143121=CARTESIAN_POINT('Ctrl Pts',(-1.09634523681734E-14,-9.00000000000035,
1446.609375));
#143122=CARTESIAN_POINT('',(-6.31841207935097E-16,-11.3170000000004,1446.609375));
#143123=CARTESIAN_POINT('',(-6.31841207935097E-16,50.8013494805973,1446.609375));
#143124=CARTESIAN_POINT('',(2.00906028488723E-14,-11.3170000000004,1436.290625));
#143125=CARTESIAN_POINT('Ctrl Pts',(-1.04083408558608E-14,-11.3170000000004,
1446.609375));
#143126=CARTESIAN_POINT('Ctrl Pts',(-0.657970384764804,-11.3170000000004,
1446.609375));
#143127=CARTESIAN_POINT('Ctrl Pts',(-1.35344266229499,-11.2542369285791,
1446.47591649128));
#143128=CARTESIAN_POINT('Ctrl Pts',(-2.62207755819474,-11.0278903257139,
1445.94625975887));
#143129=CARTESIAN_POINT('Ctrl Pts',(-3.19590327436269,-10.8668770896512,
1445.55055482401));
#143130=CARTESIAN_POINT('Ctrl Pts',(-4.10136924643444,-10.5585230349079,
1444.64508885193));
#143131=CARTESIAN_POINT('Ctrl Pts',(-4.49646674026965,-10.3894819155765,
1444.07155417537));
#143132=CARTESIAN_POINT('Ctrl Pts',(-5.02564501462738,-10.1440843535218,
1442.8041205208));
#143133=CARTESIAN_POINT('Ctrl Pts',(-5.15937500000008,-10.0725040883279,
1442.1091550748));
#143134=CARTESIAN_POINT('Ctrl Pts',(-5.15937500000008,-10.0725040883279,
1441.45));
#143135=CARTESIAN_POINT('Ctrl Pts',(-5.15937500000008,-10.0725040883279,
1440.7908449252));
#143136=CARTESIAN_POINT('Ctrl Pts',(-5.02564501462738,-10.1440843535218,
1440.0958794792));
#143137=CARTESIAN_POINT('Ctrl Pts',(-4.49646674026965,-10.3894819155765,
1438.82844582463));
#143138=CARTESIAN_POINT('Ctrl Pts',(-4.10136924643445,-10.5585230349079,
1438.25491114807));
#143139=CARTESIAN_POINT('Ctrl Pts',(-3.19590327436269,-10.8668770896512,
1437.34944517599));
#143140=CARTESIAN_POINT('Ctrl Pts',(-2.62207755819474,-11.0278903257139,
1436.95374024113));
#143141=CARTESIAN_POINT('Ctrl Pts',(-1.35344266229499,-11.2542369285791,
1436.42408350872));
#143142=CARTESIAN_POINT('Ctrl Pts',(-0.657970384764801,-11.3170000000004,
1436.290625));
#143143=CARTESIAN_POINT('Ctrl Pts',(-6.66133814775094E-15,-11.3170000000004,
1436.290625));
#143144=CARTESIAN_POINT('Ctrl Pts',(2.23432383705813E-14,-11.3170000000004,
1436.290625));
#143145=CARTESIAN_POINT('Ctrl Pts',(0.657970384764816,-11.3170000000004,
1436.290625));
#143146=CARTESIAN_POINT('Ctrl Pts',(1.35344266229499,-11.2542369285791,
1436.42408350872));
#143147=CARTESIAN_POINT('Ctrl Pts',(2.62207755819474,-11.0278903257139,
1436.95374024113));
#143148=CARTESIAN_POINT('Ctrl Pts',(3.19590327436269,-10.8668770896512,
1437.34944517599));
#143149=CARTESIAN_POINT('Ctrl Pts',(4.10136924643445,-10.5585230349079,
1438.25491114807));
#143150=CARTESIAN_POINT('Ctrl Pts',(4.49646674026965,-10.3894819155765,
1438.82844582463));
#143151=CARTESIAN_POINT('Ctrl Pts',(5.02564501462738,-10.1440843535218,
1440.0958794792));
#143152=CARTESIAN_POINT('Ctrl Pts',(5.15937500000008,-10.0725040883279,
1440.7908449252));
#143153=CARTESIAN_POINT('Ctrl Pts',(5.15937500000008,-10.0725040883279,
1442.1091550748));
#143154=CARTESIAN_POINT('Ctrl Pts',(5.02564501462738,-10.1440843535218,
1442.8041205208));
#143155=CARTESIAN_POINT('Ctrl Pts',(4.49646674026965,-10.3894819155765,
1444.07155417537));
#143156=CARTESIAN_POINT('Ctrl Pts',(4.10136924643444,-10.5585230349079,
1444.64508885193));
#143157=CARTESIAN_POINT('Ctrl Pts',(3.19590327436268,-10.8668770896512,
1445.55055482401));
#143158=CARTESIAN_POINT('Ctrl Pts',(2.62207755819474,-11.0278903257139,
1445.94625975887));
#143159=CARTESIAN_POINT('Ctrl Pts',(1.35344266229499,-11.2542369285791,
1446.47591649128));
#143160=CARTESIAN_POINT('Ctrl Pts',(0.657970384764803,-11.3170000000004,
1446.609375));
#143161=CARTESIAN_POINT('Ctrl Pts',(9.36750677027476E-15,-11.3170000000004,
1446.609375));
#143162=CARTESIAN_POINT('Ctrl Pts',(-5.55111512312578E-16,-9.00000000000036,
1446.609375));
#143163=CARTESIAN_POINT('Ctrl Pts',(0.664414150007831,-9.00000000000036,
1446.609375));
#143164=CARTESIAN_POINT('Ctrl Pts',(1.36280970424649,-8.91992322022029,
1446.47335621405));
#143165=CARTESIAN_POINT('Ctrl Pts',(2.63009169102989,-8.63162196667495,
1445.94154473184));
#143166=CARTESIAN_POINT('Ctrl Pts',(3.19993704609039,-8.42620218982176,
1445.54652105228));
#143167=CARTESIAN_POINT('Ctrl Pts',(4.09885081991486,-8.02760290754512,
1444.64760727845));
#143168=CARTESIAN_POINT('Ctrl Pts',(4.49222528611435,-7.80496687696197,
1444.07844795906));
#143169=CARTESIAN_POINT('Ctrl Pts',(5.02262143709865,-7.47468272092311,
1442.81458264393));
#143170=CARTESIAN_POINT('Ctrl Pts',(5.15937500000008,-7.37433723187243,
1442.1178671016));
#143171=CARTESIAN_POINT('Ctrl Pts',(5.15937500000008,-7.37433723187243,
1440.7821328984));
#143172=CARTESIAN_POINT('Ctrl Pts',(5.02262143709865,-7.47468272092311,
1440.08541735607));
#143173=CARTESIAN_POINT('Ctrl Pts',(4.49222528611435,-7.80496687696196,
1438.82155204094));
#143174=CARTESIAN_POINT('Ctrl Pts',(4.09885081991486,-8.02760290754512,
1438.25239272155));
#143175=CARTESIAN_POINT('Ctrl Pts',(3.19993704609039,-8.42620218982176,
1437.35347894772));
#143176=CARTESIAN_POINT('Ctrl Pts',(2.6300916910299,-8.63162196667495,1436.95845526816));
#143177=CARTESIAN_POINT('Ctrl Pts',(1.36280970424649,-8.91992322022029,
1436.42664378595));
#143178=CARTESIAN_POINT('Ctrl Pts',(0.664414150007828,-9.00000000000036,
1436.290625));
#143179=CARTESIAN_POINT('Ctrl Pts',(-4.71844785465692E-15,-9.00000000000036,
1436.290625));
#143180=CARTESIAN_POINT('Origin',(0.,0.,0.));
#143181=CARTESIAN_POINT('',(-1.38593278259508E-15,-11.3170000000004,1428.75));
#143182=CARTESIAN_POINT('Origin',(0.,-1.74262261732341E-13,1428.75));
#143183=CARTESIAN_POINT('',(-1.38593278259508E-15,-11.3170000000002,-1.38031567175848E-15));
#143184=CARTESIAN_POINT('',(-1.38593278259508E-15,-11.3170000000002,-1.38031567175848E-15));
#143185=CARTESIAN_POINT('Origin',(0.,0.,0.));
#143186=CARTESIAN_POINT('',(-1.10218211923264E-15,-9.00000000000018,-1.09771503453445E-15));
#143187=CARTESIAN_POINT('',(-1.10218211923264E-15,-9.00000000000035,1428.75));
#143188=CARTESIAN_POINT('',(-1.10218211923264E-15,-9.00000000000018,-1.09771503453445E-15));
#143189=CARTESIAN_POINT('Origin',(0.,-1.74262261732341E-13,1428.75));
#143190=CARTESIAN_POINT('Origin',(0.,11.317,1504.95));
#143191=CARTESIAN_POINT('Origin',(0.,11.317,1428.75));
#143192=CARTESIAN_POINT('Origin',(5.37704275891775E-14,4.44089209850063E-14,
1504.8993152933));
#143193=CARTESIAN_POINT('',(5.15601850460762E-14,18.048,1454.04863058659));
#143194=CARTESIAN_POINT('',(5.15601850460762E-14,18.048,1454.15));
#143195=CARTESIAN_POINT('',(1.05330612635254E-13,18.0480000000001,1504.8993152933));
#143196=CARTESIAN_POINT('',(0.,-18.048,1504.84863058659));
#143197=CARTESIAN_POINT('Ctrl Pts',(0.,-18.048,1504.84863058659));
#143198=CARTESIAN_POINT('Ctrl Pts',(-1.6723934873761,-18.048,1503.35451293953));
#143199=CARTESIAN_POINT('Ctrl Pts',(-3.31631129755346,-17.7406985030951,
1501.86039529247));
#143200=CARTESIAN_POINT('Ctrl Pts',(-4.96022910773077,-17.4333970061901,
1500.36627764542));
#143201=CARTESIAN_POINT('Ctrl Pts',(-6.51968959134574,-16.8292587962898,
1498.87215999836));
#143202=CARTESIAN_POINT('Ctrl Pts',(-8.07915007496071,-16.2251205863895,
1497.3780423513));
#143203=CARTESIAN_POINT('Ctrl Pts',(-9.50104767561052,-15.3447188656481,
1495.88392470424));
#143204=CARTESIAN_POINT('Ctrl Pts',(-10.9229452762603,-14.4643171449067,
1494.38980705718));
#143205=CARTESIAN_POINT('Ctrl Pts',(-12.1588589765331,-13.3376329379985,
1492.89568941012));
#143206=CARTESIAN_POINT('Ctrl Pts',(-13.3947726768058,-12.2109487310903,
1491.40157176306));
#143207=CARTESIAN_POINT('Ctrl Pts',(-14.4026149179538,-10.8763499173728,
1489.907454116));
#143208=CARTESIAN_POINT('Ctrl Pts',(-15.4104571591017,-9.54175110365538,
1488.41333646895));
#143209=CARTESIAN_POINT('Ctrl Pts',(-16.1559070823762,-8.04468584505497,
1486.91921882189));
#143210=CARTESIAN_POINT('Ctrl Pts',(-16.9013570056506,-6.54762058645456,
1485.42510117483));
#143211=CARTESIAN_POINT('Ctrl Pts',(-17.3590292079831,-4.93906964482095,
1483.93098352777));
#143212=CARTESIAN_POINT('Ctrl Pts',(-17.8167014103155,-3.33051870318735,
1482.43686588071));
#143213=CARTESIAN_POINT('Ctrl Pts',(-17.9710104137728,-1.66525935159368,
1480.94274823365));
#143214=CARTESIAN_POINT('Ctrl Pts',(-18.1253194172301,-1.10985572039171E-15,
1479.44863058659));
#143215=CARTESIAN_POINT('Ctrl Pts',(-17.9710104137728,1.66525935159367,
1477.95451293953));
#143216=CARTESIAN_POINT('Ctrl Pts',(-17.8167014103155,3.33051870318735,
1476.46039529247));
#143217=CARTESIAN_POINT('Ctrl Pts',(-17.3590292079831,4.93906964482096,
1474.96627764542));
#143218=CARTESIAN_POINT('Ctrl Pts',(-16.9013570056506,6.54762058645456,
1473.47215999836));
#143219=CARTESIAN_POINT('Ctrl Pts',(-16.1559070823762,8.04468584505497,
1471.9780423513));
#143220=CARTESIAN_POINT('Ctrl Pts',(-15.4104571591017,9.54175110365538,
1470.48392470424));
#143221=CARTESIAN_POINT('Ctrl Pts',(-14.4026149179538,10.8763499173728,
1468.98980705718));
#143222=CARTESIAN_POINT('Ctrl Pts',(-13.3947726768058,12.2109487310903,
1467.49568941012));
#143223=CARTESIAN_POINT('Ctrl Pts',(-12.1588589765331,13.3376329379985,
1466.00157176306));
#143224=CARTESIAN_POINT('Ctrl Pts',(-10.9229452762603,14.4643171449067,
1464.507454116));
#143225=CARTESIAN_POINT('Ctrl Pts',(-9.50104767561052,15.3447188656481,
1463.01333646895));
#143226=CARTESIAN_POINT('Ctrl Pts',(-8.07915007496071,16.2251205863895,
1461.51921882189));
#143227=CARTESIAN_POINT('Ctrl Pts',(-6.51968959134574,16.8292587962898,
1460.02510117483));
#143228=CARTESIAN_POINT('Ctrl Pts',(-4.96022910773078,17.4333970061901,
1458.53098352777));
#143229=CARTESIAN_POINT('Ctrl Pts',(-3.31631129755346,17.7406985030951,
1457.03686588071));
#143230=CARTESIAN_POINT('Ctrl Pts',(-1.67239348737615,18.048,1455.54274823365));
#143231=CARTESIAN_POINT('Ctrl Pts',(-2.21024254310115E-15,18.048,1454.04863058659));
#143232=CARTESIAN_POINT('',(0.,-18.048,1504.95));
#143233=CARTESIAN_POINT('',(0.,-18.048,1504.95));
#143234=CARTESIAN_POINT('Ctrl Pts',(0.,-18.048,1504.95));
#143235=CARTESIAN_POINT('Ctrl Pts',(-1.67239348737621,-18.048,1503.45588235294));
#143236=CARTESIAN_POINT('Ctrl Pts',(-3.31631129755346,-17.7406985030951,
1501.96176470588));
#143237=CARTESIAN_POINT('Ctrl Pts',(-4.96022910773077,-17.4333970061901,
1500.46764705882));
#143238=CARTESIAN_POINT('Ctrl Pts',(-6.51968959134574,-16.8292587962898,
1498.97352941176));
#143239=CARTESIAN_POINT('Ctrl Pts',(-8.07915007496071,-16.2251205863895,
1497.47941176471));
#143240=CARTESIAN_POINT('Ctrl Pts',(-9.50104767561052,-15.3447188656481,
1495.98529411765));
#143241=CARTESIAN_POINT('Ctrl Pts',(-10.9229452762603,-14.4643171449067,
1494.49117647059));
#143242=CARTESIAN_POINT('Ctrl Pts',(-12.1588589765331,-13.3376329379985,
1492.99705882353));
#143243=CARTESIAN_POINT('Ctrl Pts',(-13.3947726768058,-12.2109487310903,
1491.50294117647));
#143244=CARTESIAN_POINT('Ctrl Pts',(-14.4026149179538,-10.8763499173728,
1490.00882352941));
#143245=CARTESIAN_POINT('Ctrl Pts',(-15.4104571591017,-9.54175110365538,
1488.51470588235));
#143246=CARTESIAN_POINT('Ctrl Pts',(-16.1559070823762,-8.04468584505497,
1487.02058823529));
#143247=CARTESIAN_POINT('Ctrl Pts',(-16.9013570056506,-6.54762058645456,
1485.52647058824));
#143248=CARTESIAN_POINT('Ctrl Pts',(-17.3590292079831,-4.93906964482095,
1484.03235294118));
#143249=CARTESIAN_POINT('Ctrl Pts',(-17.8167014103155,-3.33051870318735,
1482.53823529412));
#143250=CARTESIAN_POINT('Ctrl Pts',(-17.9710104137728,-1.66525935159368,
1481.04411764706));
#143251=CARTESIAN_POINT('Ctrl Pts',(-18.1253194172301,-1.10985572039171E-15,
1479.55));
#143252=CARTESIAN_POINT('Ctrl Pts',(-17.9710104137728,1.66525935159367,
1478.05588235294));
#143253=CARTESIAN_POINT('Ctrl Pts',(-17.8167014103155,3.33051870318735,
1476.56176470588));
#143254=CARTESIAN_POINT('Ctrl Pts',(-17.3590292079831,4.93906964482096,
1475.06764705882));
#143255=CARTESIAN_POINT('Ctrl Pts',(-16.9013570056506,6.54762058645456,
1473.57352941176));
#143256=CARTESIAN_POINT('Ctrl Pts',(-16.1559070823762,8.04468584505497,
1472.07941176471));
#143257=CARTESIAN_POINT('Ctrl Pts',(-15.4104571591017,9.54175110365538,
1470.58529411765));
#143258=CARTESIAN_POINT('Ctrl Pts',(-14.4026149179538,10.8763499173728,
1469.09117647059));
#143259=CARTESIAN_POINT('Ctrl Pts',(-13.3947726768058,12.2109487310903,
1467.59705882353));
#143260=CARTESIAN_POINT('Ctrl Pts',(-12.1588589765331,13.3376329379985,
1466.10294117647));
#143261=CARTESIAN_POINT('Ctrl Pts',(-10.9229452762603,14.4643171449067,
1464.60882352941));
#143262=CARTESIAN_POINT('Ctrl Pts',(-9.50104767561052,15.3447188656481,
1463.11470588235));
#143263=CARTESIAN_POINT('Ctrl Pts',(-8.07915007496071,16.2251205863895,
1461.62058823529));
#143264=CARTESIAN_POINT('Ctrl Pts',(-6.51968959134574,16.8292587962898,
1460.12647058824));
#143265=CARTESIAN_POINT('Ctrl Pts',(-4.96022910773078,17.4333970061901,
1458.63235294118));
#143266=CARTESIAN_POINT('Ctrl Pts',(-3.31631129755346,17.7406985030951,
1457.13823529412));
#143267=CARTESIAN_POINT('Ctrl Pts',(-1.67239348737615,18.048,1455.64411764706));
#143268=CARTESIAN_POINT('Ctrl Pts',(-2.21024254310115E-15,18.048,1454.15));
#143269=CARTESIAN_POINT('Origin',(5.37704275891775E-14,4.44089209850063E-14,
1504.8993152933));
#143270=CARTESIAN_POINT('',(5.15601850460762E-14,18.048,1352.44863058659));
#143271=CARTESIAN_POINT('',(5.15601850460762E-14,18.048,1352.55));
#143272=CARTESIAN_POINT('',(1.05330612635254E-13,18.0480000000001,1504.8993152933));
#143273=CARTESIAN_POINT('Ctrl Pts',(-2.21024254310115E-15,18.048,1454.04863058659));
#143274=CARTESIAN_POINT('Ctrl Pts',(1.67239348737616,18.048,1452.55451293953));
#143275=CARTESIAN_POINT('Ctrl Pts',(3.31631129755346,17.7406985030951,1451.06039529247));
#143276=CARTESIAN_POINT('Ctrl Pts',(4.96022910773077,17.4333970061901,1449.56627764542));
#143277=CARTESIAN_POINT('Ctrl Pts',(6.51968959134575,16.8292587962898,1448.07215999836));
#143278=CARTESIAN_POINT('Ctrl Pts',(8.07915007496071,16.2251205863895,1446.5780423513));
#143279=CARTESIAN_POINT('Ctrl Pts',(9.50104767561053,15.3447188656481,1445.08392470424));
#143280=CARTESIAN_POINT('Ctrl Pts',(10.9229452762603,14.4643171449067,1443.58980705718));
#143281=CARTESIAN_POINT('Ctrl Pts',(12.1588589765331,13.3376329379985,1442.09568941012));
#143282=CARTESIAN_POINT('Ctrl Pts',(13.3947726768058,12.2109487310903,1440.60157176306));
#143283=CARTESIAN_POINT('Ctrl Pts',(14.4026149179538,10.8763499173728,1439.107454116));
#143284=CARTESIAN_POINT('Ctrl Pts',(15.4104571591017,9.54175110365539,1437.61333646895));
#143285=CARTESIAN_POINT('Ctrl Pts',(16.1559070823762,8.04468584505496,1436.11921882189));
#143286=CARTESIAN_POINT('Ctrl Pts',(16.9013570056506,6.54762058645456,1434.62510117483));
#143287=CARTESIAN_POINT('Ctrl Pts',(17.3590292079831,4.93906964482096,1433.13098352777));
#143288=CARTESIAN_POINT('Ctrl Pts',(17.8167014103155,3.33051870318735,1431.63686588071));
#143289=CARTESIAN_POINT('Ctrl Pts',(17.9710104137728,1.66525935159367,1430.14274823365));
#143290=CARTESIAN_POINT('Ctrl Pts',(18.1253194172301,3.32956716117513E-15,
1428.64863058659));
#143291=CARTESIAN_POINT('Ctrl Pts',(17.9710104137728,-1.66525935159367,
1427.15451293953));
#143292=CARTESIAN_POINT('Ctrl Pts',(17.8167014103155,-3.33051870318736,
1425.66039529247));
#143293=CARTESIAN_POINT('Ctrl Pts',(17.3590292079831,-4.93906964482095,
1424.16627764542));
#143294=CARTESIAN_POINT('Ctrl Pts',(16.9013570056506,-6.54762058645456,
1422.67215999836));
#143295=CARTESIAN_POINT('Ctrl Pts',(16.1559070823762,-8.04468584505497,
1421.1780423513));
#143296=CARTESIAN_POINT('Ctrl Pts',(15.4104571591017,-9.54175110365538,
1419.68392470424));
#143297=CARTESIAN_POINT('Ctrl Pts',(14.4026149179538,-10.8763499173728,
1418.18980705718));
#143298=CARTESIAN_POINT('Ctrl Pts',(13.3947726768058,-12.2109487310903,
1416.69568941012));
#143299=CARTESIAN_POINT('Ctrl Pts',(12.1588589765331,-13.3376329379985,
1415.20157176306));
#143300=CARTESIAN_POINT('Ctrl Pts',(10.9229452762603,-14.4643171449067,
1413.707454116));
#143301=CARTESIAN_POINT('Ctrl Pts',(9.50104767561053,-15.3447188656481,
1412.21333646895));
#143302=CARTESIAN_POINT('Ctrl Pts',(8.07915007496071,-16.2251205863895,
1410.71921882189));
#143303=CARTESIAN_POINT('Ctrl Pts',(6.51968959134574,-16.8292587962898,
1409.22510117483));
#143304=CARTESIAN_POINT('Ctrl Pts',(4.96022910773078,-17.4333970061901,
1407.73098352777));
#143305=CARTESIAN_POINT('Ctrl Pts',(3.31631129755346,-17.7406985030951,
1406.23686588071));
#143306=CARTESIAN_POINT('Ctrl Pts',(1.67239348737615,-18.048,1404.74274823365));
#143307=CARTESIAN_POINT('Ctrl Pts',(0.,-18.048,1403.24863058659));
#143308=CARTESIAN_POINT('Ctrl Pts',(-1.67239348737615,-18.048,1401.75451293953));
#143309=CARTESIAN_POINT('Ctrl Pts',(-3.31631129755346,-17.7406985030951,
1400.26039529247));
#143310=CARTESIAN_POINT('Ctrl Pts',(-4.96022910773077,-17.4333970061901,
1398.76627764542));
#143311=CARTESIAN_POINT('Ctrl Pts',(-6.51968959134574,-16.8292587962898,
1397.27215999836));
#143312=CARTESIAN_POINT('Ctrl Pts',(-8.07915007496071,-16.2251205863895,
1395.7780423513));
#143313=CARTESIAN_POINT('Ctrl Pts',(-9.50104767561052,-15.3447188656481,
1394.28392470424));
#143314=CARTESIAN_POINT('Ctrl Pts',(-10.9229452762603,-14.4643171449067,
1392.78980705718));
#143315=CARTESIAN_POINT('Ctrl Pts',(-12.1588589765331,-13.3376329379985,
1391.29568941012));
#143316=CARTESIAN_POINT('Ctrl Pts',(-13.3947726768058,-12.2109487310903,
1389.80157176306));
#143317=CARTESIAN_POINT('Ctrl Pts',(-14.4026149179538,-10.8763499173728,
1388.307454116));
#143318=CARTESIAN_POINT('Ctrl Pts',(-15.4104571591017,-9.54175110365538,
1386.81333646895));
#143319=CARTESIAN_POINT('Ctrl Pts',(-16.1559070823762,-8.04468584505497,
1385.31921882189));
#143320=CARTESIAN_POINT('Ctrl Pts',(-16.9013570056506,-6.54762058645456,
1383.82510117483));
#143321=CARTESIAN_POINT('Ctrl Pts',(-17.3590292079831,-4.93906964482095,
1382.33098352777));
#143322=CARTESIAN_POINT('Ctrl Pts',(-17.8167014103155,-3.33051870318735,
1380.83686588071));
#143323=CARTESIAN_POINT('Ctrl Pts',(-17.9710104137728,-1.66525935159368,
1379.34274823365));
#143324=CARTESIAN_POINT('Ctrl Pts',(-18.1253194172301,-1.10985572039171E-15,
1377.84863058659));
#143325=CARTESIAN_POINT('Ctrl Pts',(-17.9710104137728,1.66525935159367,
1376.35451293953));
#143326=CARTESIAN_POINT('Ctrl Pts',(-17.8167014103155,3.33051870318735,
1374.86039529247));
#143327=CARTESIAN_POINT('Ctrl Pts',(-17.3590292079831,4.93906964482096,
1373.36627764542));
#143328=CARTESIAN_POINT('Ctrl Pts',(-16.9013570056506,6.54762058645456,
1371.87215999836));
#143329=CARTESIAN_POINT('Ctrl Pts',(-16.1559070823762,8.04468584505497,
1370.3780423513));
#143330=CARTESIAN_POINT('Ctrl Pts',(-15.4104571591017,9.54175110365538,
1368.88392470424));
#143331=CARTESIAN_POINT('Ctrl Pts',(-14.4026149179538,10.8763499173728,
1367.38980705718));
#143332=CARTESIAN_POINT('Ctrl Pts',(-13.3947726768058,12.2109487310903,
1365.89568941012));
#143333=CARTESIAN_POINT('Ctrl Pts',(-12.1588589765331,13.3376329379985,
1364.40157176306));
#143334=CARTESIAN_POINT('Ctrl Pts',(-10.9229452762603,14.4643171449067,
1362.907454116));
#143335=CARTESIAN_POINT('Ctrl Pts',(-9.50104767561052,15.3447188656481,
1361.41333646895));
#143336=CARTESIAN_POINT('Ctrl Pts',(-8.07915007496071,16.2251205863895,
1359.91921882189));
#143337=CARTESIAN_POINT('Ctrl Pts',(-6.51968959134574,16.8292587962898,
1358.42510117483));
#143338=CARTESIAN_POINT('Ctrl Pts',(-4.96022910773078,17.4333970061901,
1356.93098352777));
#143339=CARTESIAN_POINT('Ctrl Pts',(-3.31631129755346,17.7406985030951,
1355.43686588071));
#143340=CARTESIAN_POINT('Ctrl Pts',(-1.67239348737615,18.048,1353.94274823365));
#143341=CARTESIAN_POINT('Ctrl Pts',(-2.21024254310115E-15,18.048,1352.44863058659));
#143342=CARTESIAN_POINT('Ctrl Pts',(-2.21024254310115E-15,18.048,1454.15));
#143343=CARTESIAN_POINT('Ctrl Pts',(1.67239348737616,18.048,1452.65588235294));
#143344=CARTESIAN_POINT('Ctrl Pts',(3.31631129755346,17.7406985030951,1451.16176470588));
#143345=CARTESIAN_POINT('Ctrl Pts',(4.96022910773077,17.4333970061901,1449.66764705882));
#143346=CARTESIAN_POINT('Ctrl Pts',(6.51968959134575,16.8292587962898,1448.17352941177));
#143347=CARTESIAN_POINT('Ctrl Pts',(8.07915007496071,16.2251205863895,1446.67941176471));
#143348=CARTESIAN_POINT('Ctrl Pts',(9.50104767561053,15.3447188656481,1445.18529411765));
#143349=CARTESIAN_POINT('Ctrl Pts',(10.9229452762603,14.4643171449067,1443.69117647059));
#143350=CARTESIAN_POINT('Ctrl Pts',(12.1588589765331,13.3376329379985,1442.19705882353));
#143351=CARTESIAN_POINT('Ctrl Pts',(13.3947726768058,12.2109487310903,1440.70294117647));
#143352=CARTESIAN_POINT('Ctrl Pts',(14.4026149179538,10.8763499173728,1439.20882352941));
#143353=CARTESIAN_POINT('Ctrl Pts',(15.4104571591017,9.54175110365539,1437.71470588235));
#143354=CARTESIAN_POINT('Ctrl Pts',(16.1559070823762,8.04468584505496,1436.22058823529));
#143355=CARTESIAN_POINT('Ctrl Pts',(16.9013570056506,6.54762058645456,1434.72647058824));
#143356=CARTESIAN_POINT('Ctrl Pts',(17.3590292079831,4.93906964482096,1433.23235294118));
#143357=CARTESIAN_POINT('Ctrl Pts',(17.8167014103155,3.33051870318735,1431.73823529412));
#143358=CARTESIAN_POINT('Ctrl Pts',(17.9710104137728,1.66525935159367,1430.24411764706));
#143359=CARTESIAN_POINT('Ctrl Pts',(18.1253194172301,3.32956716117513E-15,
1428.75));
#143360=CARTESIAN_POINT('Ctrl Pts',(17.9710104137728,-1.66525935159367,
1427.25588235294));
#143361=CARTESIAN_POINT('Ctrl Pts',(17.8167014103155,-3.33051870318736,
1425.76176470588));
#143362=CARTESIAN_POINT('Ctrl Pts',(17.3590292079831,-4.93906964482095,
1424.26764705882));
#143363=CARTESIAN_POINT('Ctrl Pts',(16.9013570056506,-6.54762058645456,
1422.77352941176));
#143364=CARTESIAN_POINT('Ctrl Pts',(16.1559070823762,-8.04468584505497,
1421.27941176471));
#143365=CARTESIAN_POINT('Ctrl Pts',(15.4104571591017,-9.54175110365538,
1419.78529411765));
#143366=CARTESIAN_POINT('Ctrl Pts',(14.4026149179538,-10.8763499173728,
1418.29117647059));
#143367=CARTESIAN_POINT('Ctrl Pts',(13.3947726768058,-12.2109487310903,
1416.79705882353));
#143368=CARTESIAN_POINT('Ctrl Pts',(12.1588589765331,-13.3376329379985,
1415.30294117647));
#143369=CARTESIAN_POINT('Ctrl Pts',(10.9229452762603,-14.4643171449067,
1413.80882352941));
#143370=CARTESIAN_POINT('Ctrl Pts',(9.50104767561053,-15.3447188656481,
1412.31470588235));
#143371=CARTESIAN_POINT('Ctrl Pts',(8.07915007496071,-16.2251205863895,
1410.82058823529));
#143372=CARTESIAN_POINT('Ctrl Pts',(6.51968959134574,-16.8292587962898,
1409.32647058824));
#143373=CARTESIAN_POINT('Ctrl Pts',(4.96022910773078,-17.4333970061901,
1407.83235294118));
#143374=CARTESIAN_POINT('Ctrl Pts',(3.31631129755346,-17.7406985030951,
1406.33823529412));
#143375=CARTESIAN_POINT('Ctrl Pts',(1.67239348737615,-18.048,1404.84411764706));
#143376=CARTESIAN_POINT('Ctrl Pts',(0.,-18.048,1403.35));
#143377=CARTESIAN_POINT('Ctrl Pts',(-1.67239348737615,-18.048,1401.85588235294));
#143378=CARTESIAN_POINT('Ctrl Pts',(-3.31631129755346,-17.7406985030951,
1400.36176470588));
#143379=CARTESIAN_POINT('Ctrl Pts',(-4.96022910773077,-17.4333970061901,
1398.86764705882));
#143380=CARTESIAN_POINT('Ctrl Pts',(-6.51968959134574,-16.8292587962898,
1397.37352941176));
#143381=CARTESIAN_POINT('Ctrl Pts',(-8.07915007496071,-16.2251205863895,
1395.87941176471));
#143382=CARTESIAN_POINT('Ctrl Pts',(-9.50104767561052,-15.3447188656481,
1394.38529411765));
#143383=CARTESIAN_POINT('Ctrl Pts',(-10.9229452762603,-14.4643171449067,
1392.89117647059));
#143384=CARTESIAN_POINT('Ctrl Pts',(-12.1588589765331,-13.3376329379985,
1391.39705882353));
#143385=CARTESIAN_POINT('Ctrl Pts',(-13.3947726768058,-12.2109487310903,
1389.90294117647));
#143386=CARTESIAN_POINT('Ctrl Pts',(-14.4026149179538,-10.8763499173728,
1388.40882352941));
#143387=CARTESIAN_POINT('Ctrl Pts',(-15.4104571591017,-9.54175110365538,
1386.91470588235));
#143388=CARTESIAN_POINT('Ctrl Pts',(-16.1559070823762,-8.04468584505497,
1385.42058823529));
#143389=CARTESIAN_POINT('Ctrl Pts',(-16.9013570056506,-6.54762058645456,
1383.92647058824));
#143390=CARTESIAN_POINT('Ctrl Pts',(-17.3590292079831,-4.93906964482095,
1382.43235294118));
#143391=CARTESIAN_POINT('Ctrl Pts',(-17.8167014103155,-3.33051870318735,
1380.93823529412));
#143392=CARTESIAN_POINT('Ctrl Pts',(-17.9710104137728,-1.66525935159368,
1379.44411764706));
#143393=CARTESIAN_POINT('Ctrl Pts',(-18.1253194172301,-1.10985572039171E-15,
1377.95));
#143394=CARTESIAN_POINT('Ctrl Pts',(-17.9710104137728,1.66525935159367,
1376.45588235294));
#143395=CARTESIAN_POINT('Ctrl Pts',(-17.8167014103155,3.33051870318735,
1374.96176470588));
#143396=CARTESIAN_POINT('Ctrl Pts',(-17.3590292079831,4.93906964482096,
1373.46764705882));
#143397=CARTESIAN_POINT('Ctrl Pts',(-16.9013570056506,6.54762058645456,
1371.97352941176));
#143398=CARTESIAN_POINT('Ctrl Pts',(-16.1559070823762,8.04468584505497,
1370.47941176471));
#143399=CARTESIAN_POINT('Ctrl Pts',(-15.4104571591017,9.54175110365538,
1368.98529411765));
#143400=CARTESIAN_POINT('Ctrl Pts',(-14.4026149179538,10.8763499173728,
1367.49117647059));
#143401=CARTESIAN_POINT('Ctrl Pts',(-13.3947726768058,12.2109487310903,
1365.99705882353));
#143402=CARTESIAN_POINT('Ctrl Pts',(-12.1588589765331,13.3376329379985,
1364.50294117647));
#143403=CARTESIAN_POINT('Ctrl Pts',(-10.9229452762603,14.4643171449067,
1363.00882352941));
#143404=CARTESIAN_POINT('Ctrl Pts',(-9.50104767561052,15.3447188656481,
1361.51470588235));
#143405=CARTESIAN_POINT('Ctrl Pts',(-8.07915007496071,16.2251205863895,
1360.02058823529));
#143406=CARTESIAN_POINT('Ctrl Pts',(-6.51968959134574,16.8292587962898,
1358.52647058824));
#143407=CARTESIAN_POINT('Ctrl Pts',(-4.96022910773078,17.4333970061901,
1357.03235294118));
#143408=CARTESIAN_POINT('Ctrl Pts',(-3.31631129755346,17.7406985030951,
1355.53823529412));
#143409=CARTESIAN_POINT('Ctrl Pts',(-1.67239348737615,18.048,1354.04411764706));
#143410=CARTESIAN_POINT('Ctrl Pts',(-2.21024254310115E-15,18.048,1352.55));
#143411=CARTESIAN_POINT('Origin',(5.37704275891775E-14,4.44089209850063E-14,
1504.8993152933));
#143412=CARTESIAN_POINT('',(5.15601850460762E-14,18.048,1250.84863058659));
#143413=CARTESIAN_POINT('',(5.15601850460762E-14,18.048,1250.95));
#143414=CARTESIAN_POINT('',(1.05330612635254E-13,18.0480000000001,1504.8993152933));
#143415=CARTESIAN_POINT('Ctrl Pts',(-2.21024254310115E-15,18.048,1352.44863058659));
#143416=CARTESIAN_POINT('Ctrl Pts',(1.67239348737616,18.048,1350.95451293953));
#143417=CARTESIAN_POINT('Ctrl Pts',(3.31631129755346,17.7406985030951,1349.46039529247));
#143418=CARTESIAN_POINT('Ctrl Pts',(4.96022910773077,17.4333970061901,1347.96627764542));
#143419=CARTESIAN_POINT('Ctrl Pts',(6.51968959134575,16.8292587962898,1346.47215999836));
#143420=CARTESIAN_POINT('Ctrl Pts',(8.07915007496071,16.2251205863895,1344.9780423513));
#143421=CARTESIAN_POINT('Ctrl Pts',(9.50104767561053,15.3447188656481,1343.48392470424));
#143422=CARTESIAN_POINT('Ctrl Pts',(10.9229452762603,14.4643171449067,1341.98980705718));
#143423=CARTESIAN_POINT('Ctrl Pts',(12.1588589765331,13.3376329379985,1340.49568941012));
#143424=CARTESIAN_POINT('Ctrl Pts',(13.3947726768058,12.2109487310903,1339.00157176306));
#143425=CARTESIAN_POINT('Ctrl Pts',(14.4026149179538,10.8763499173728,1337.507454116));
#143426=CARTESIAN_POINT('Ctrl Pts',(15.4104571591017,9.54175110365539,1336.01333646895));
#143427=CARTESIAN_POINT('Ctrl Pts',(16.1559070823762,8.04468584505496,1334.51921882189));
#143428=CARTESIAN_POINT('Ctrl Pts',(16.9013570056506,6.54762058645456,1333.02510117483));
#143429=CARTESIAN_POINT('Ctrl Pts',(17.3590292079831,4.93906964482096,1331.53098352777));
#143430=CARTESIAN_POINT('Ctrl Pts',(17.8167014103155,3.33051870318735,1330.03686588071));
#143431=CARTESIAN_POINT('Ctrl Pts',(17.9710104137728,1.66525935159367,1328.54274823365));
#143432=CARTESIAN_POINT('Ctrl Pts',(18.1253194172301,3.32956716117513E-15,
1327.04863058659));
#143433=CARTESIAN_POINT('Ctrl Pts',(17.9710104137728,-1.66525935159367,
1325.55451293953));
#143434=CARTESIAN_POINT('Ctrl Pts',(17.8167014103155,-3.33051870318736,
1324.06039529247));
#143435=CARTESIAN_POINT('Ctrl Pts',(17.3590292079831,-4.93906964482095,
1322.56627764542));
#143436=CARTESIAN_POINT('Ctrl Pts',(16.9013570056506,-6.54762058645456,
1321.07215999836));
#143437=CARTESIAN_POINT('Ctrl Pts',(16.1559070823762,-8.04468584505497,
1319.5780423513));
#143438=CARTESIAN_POINT('Ctrl Pts',(15.4104571591017,-9.54175110365538,
1318.08392470424));
#143439=CARTESIAN_POINT('Ctrl Pts',(14.4026149179538,-10.8763499173728,
1316.58980705718));
#143440=CARTESIAN_POINT('Ctrl Pts',(13.3947726768058,-12.2109487310903,
1315.09568941012));
#143441=CARTESIAN_POINT('Ctrl Pts',(12.1588589765331,-13.3376329379985,
1313.60157176306));
#143442=CARTESIAN_POINT('Ctrl Pts',(10.9229452762603,-14.4643171449067,
1312.107454116));
#143443=CARTESIAN_POINT('Ctrl Pts',(9.50104767561053,-15.3447188656481,
1310.61333646895));
#143444=CARTESIAN_POINT('Ctrl Pts',(8.07915007496071,-16.2251205863895,
1309.11921882189));
#143445=CARTESIAN_POINT('Ctrl Pts',(6.51968959134574,-16.8292587962898,
1307.62510117483));
#143446=CARTESIAN_POINT('Ctrl Pts',(4.96022910773078,-17.4333970061901,
1306.13098352777));
#143447=CARTESIAN_POINT('Ctrl Pts',(3.31631129755346,-17.7406985030951,
1304.63686588071));
#143448=CARTESIAN_POINT('Ctrl Pts',(1.67239348737615,-18.048,1303.14274823365));
#143449=CARTESIAN_POINT('Ctrl Pts',(0.,-18.048,1301.64863058659));
#143450=CARTESIAN_POINT('Ctrl Pts',(-1.67239348737615,-18.048,1300.15451293953));
#143451=CARTESIAN_POINT('Ctrl Pts',(-3.31631129755346,-17.7406985030951,
1298.66039529247));
#143452=CARTESIAN_POINT('Ctrl Pts',(-4.96022910773077,-17.4333970061901,
1297.16627764542));
#143453=CARTESIAN_POINT('Ctrl Pts',(-6.51968959134574,-16.8292587962898,
1295.67215999836));
#143454=CARTESIAN_POINT('Ctrl Pts',(-8.07915007496071,-16.2251205863895,
1294.1780423513));
#143455=CARTESIAN_POINT('Ctrl Pts',(-9.50104767561052,-15.3447188656481,
1292.68392470424));
#143456=CARTESIAN_POINT('Ctrl Pts',(-10.9229452762603,-14.4643171449067,
1291.18980705718));
#143457=CARTESIAN_POINT('Ctrl Pts',(-12.1588589765331,-13.3376329379985,
1289.69568941012));
#143458=CARTESIAN_POINT('Ctrl Pts',(-13.3947726768058,-12.2109487310903,
1288.20157176306));
#143459=CARTESIAN_POINT('Ctrl Pts',(-14.4026149179538,-10.8763499173728,
1286.707454116));
#143460=CARTESIAN_POINT('Ctrl Pts',(-15.4104571591017,-9.54175110365538,
1285.21333646895));
#143461=CARTESIAN_POINT('Ctrl Pts',(-16.1559070823762,-8.04468584505497,
1283.71921882189));
#143462=CARTESIAN_POINT('Ctrl Pts',(-16.9013570056506,-6.54762058645456,
1282.22510117483));
#143463=CARTESIAN_POINT('Ctrl Pts',(-17.3590292079831,-4.93906964482095,
1280.73098352777));
#143464=CARTESIAN_POINT('Ctrl Pts',(-17.8167014103155,-3.33051870318735,
1279.23686588071));
#143465=CARTESIAN_POINT('Ctrl Pts',(-17.9710104137728,-1.66525935159368,
1277.74274823365));
#143466=CARTESIAN_POINT('Ctrl Pts',(-18.1253194172301,-1.10985572039171E-15,
1276.24863058659));
#143467=CARTESIAN_POINT('Ctrl Pts',(-17.9710104137728,1.66525935159367,
1274.75451293953));
#143468=CARTESIAN_POINT('Ctrl Pts',(-17.8167014103155,3.33051870318735,
1273.26039529247));
#143469=CARTESIAN_POINT('Ctrl Pts',(-17.3590292079831,4.93906964482096,
1271.76627764542));
#143470=CARTESIAN_POINT('Ctrl Pts',(-16.9013570056506,6.54762058645456,
1270.27215999836));
#143471=CARTESIAN_POINT('Ctrl Pts',(-16.1559070823762,8.04468584505497,
1268.7780423513));
#143472=CARTESIAN_POINT('Ctrl Pts',(-15.4104571591017,9.54175110365538,
1267.28392470424));
#143473=CARTESIAN_POINT('Ctrl Pts',(-14.4026149179538,10.8763499173728,
1265.78980705718));
#143474=CARTESIAN_POINT('Ctrl Pts',(-13.3947726768058,12.2109487310903,
1264.29568941012));
#143475=CARTESIAN_POINT('Ctrl Pts',(-12.1588589765331,13.3376329379985,
1262.80157176306));
#143476=CARTESIAN_POINT('Ctrl Pts',(-10.9229452762603,14.4643171449067,
1261.307454116));
#143477=CARTESIAN_POINT('Ctrl Pts',(-9.50104767561052,15.3447188656481,
1259.81333646895));
#143478=CARTESIAN_POINT('Ctrl Pts',(-8.07915007496071,16.2251205863895,
1258.31921882189));
#143479=CARTESIAN_POINT('Ctrl Pts',(-6.51968959134574,16.8292587962898,
1256.82510117483));
#143480=CARTESIAN_POINT('Ctrl Pts',(-4.96022910773078,17.4333970061901,
1255.33098352777));
#143481=CARTESIAN_POINT('Ctrl Pts',(-3.31631129755346,17.7406985030951,
1253.83686588071));
#143482=CARTESIAN_POINT('Ctrl Pts',(-1.67239348737615,18.048,1252.34274823365));
#143483=CARTESIAN_POINT('Ctrl Pts',(-2.21024254310115E-15,18.048,1250.84863058659));
#143484=CARTESIAN_POINT('Ctrl Pts',(-2.21024254310115E-15,18.048,1352.55));
#143485=CARTESIAN_POINT('Ctrl Pts',(1.67239348737616,18.048,1351.05588235294));
#143486=CARTESIAN_POINT('Ctrl Pts',(3.31631129755346,17.7406985030951,1349.56176470588));
#143487=CARTESIAN_POINT('Ctrl Pts',(4.96022910773077,17.4333970061901,1348.06764705882));
#143488=CARTESIAN_POINT('Ctrl Pts',(6.51968959134575,16.8292587962898,1346.57352941176));
#143489=CARTESIAN_POINT('Ctrl Pts',(8.07915007496071,16.2251205863895,1345.07941176471));
#143490=CARTESIAN_POINT('Ctrl Pts',(9.50104767561053,15.3447188656481,1343.58529411765));
#143491=CARTESIAN_POINT('Ctrl Pts',(10.9229452762603,14.4643171449067,1342.09117647059));
#143492=CARTESIAN_POINT('Ctrl Pts',(12.1588589765331,13.3376329379985,1340.59705882353));
#143493=CARTESIAN_POINT('Ctrl Pts',(13.3947726768058,12.2109487310903,1339.10294117647));
#143494=CARTESIAN_POINT('Ctrl Pts',(14.4026149179538,10.8763499173728,1337.60882352941));
#143495=CARTESIAN_POINT('Ctrl Pts',(15.4104571591017,9.54175110365539,1336.11470588235));
#143496=CARTESIAN_POINT('Ctrl Pts',(16.1559070823762,8.04468584505496,1334.62058823529));
#143497=CARTESIAN_POINT('Ctrl Pts',(16.9013570056506,6.54762058645456,1333.12647058824));
#143498=CARTESIAN_POINT('Ctrl Pts',(17.3590292079831,4.93906964482096,1331.63235294118));
#143499=CARTESIAN_POINT('Ctrl Pts',(17.8167014103155,3.33051870318735,1330.13823529412));
#143500=CARTESIAN_POINT('Ctrl Pts',(17.9710104137728,1.66525935159367,1328.64411764706));
#143501=CARTESIAN_POINT('Ctrl Pts',(18.1253194172301,3.32956716117513E-15,
1327.15));
#143502=CARTESIAN_POINT('Ctrl Pts',(17.9710104137728,-1.66525935159367,
1325.65588235294));
#143503=CARTESIAN_POINT('Ctrl Pts',(17.8167014103155,-3.33051870318736,
1324.16176470588));
#143504=CARTESIAN_POINT('Ctrl Pts',(17.3590292079831,-4.93906964482095,
1322.66764705882));
#143505=CARTESIAN_POINT('Ctrl Pts',(16.9013570056506,-6.54762058645456,
1321.17352941176));
#143506=CARTESIAN_POINT('Ctrl Pts',(16.1559070823762,-8.04468584505497,
1319.67941176471));
#143507=CARTESIAN_POINT('Ctrl Pts',(15.4104571591017,-9.54175110365538,
1318.18529411765));
#143508=CARTESIAN_POINT('Ctrl Pts',(14.4026149179538,-10.8763499173728,
1316.69117647059));
#143509=CARTESIAN_POINT('Ctrl Pts',(13.3947726768058,-12.2109487310903,
1315.19705882353));
#143510=CARTESIAN_POINT('Ctrl Pts',(12.1588589765331,-13.3376329379985,
1313.70294117647));
#143511=CARTESIAN_POINT('Ctrl Pts',(10.9229452762603,-14.4643171449067,
1312.20882352941));
#143512=CARTESIAN_POINT('Ctrl Pts',(9.50104767561053,-15.3447188656481,
1310.71470588235));
#143513=CARTESIAN_POINT('Ctrl Pts',(8.07915007496071,-16.2251205863895,
1309.22058823529));
#143514=CARTESIAN_POINT('Ctrl Pts',(6.51968959134574,-16.8292587962898,
1307.72647058824));
#143515=CARTESIAN_POINT('Ctrl Pts',(4.96022910773078,-17.4333970061901,
1306.23235294118));
#143516=CARTESIAN_POINT('Ctrl Pts',(3.31631129755346,-17.7406985030951,
1304.73823529412));
#143517=CARTESIAN_POINT('Ctrl Pts',(1.67239348737615,-18.048,1303.24411764706));
#143518=CARTESIAN_POINT('Ctrl Pts',(0.,-18.048,1301.75));
#143519=CARTESIAN_POINT('Ctrl Pts',(-1.67239348737615,-18.048,1300.25588235294));
#143520=CARTESIAN_POINT('Ctrl Pts',(-3.31631129755346,-17.7406985030951,
1298.76176470588));
#143521=CARTESIAN_POINT('Ctrl Pts',(-4.96022910773077,-17.4333970061901,
1297.26764705882));
#143522=CARTESIAN_POINT('Ctrl Pts',(-6.51968959134574,-16.8292587962898,
1295.77352941176));
#143523=CARTESIAN_POINT('Ctrl Pts',(-8.07915007496071,-16.2251205863895,
1294.27941176471));
#143524=CARTESIAN_POINT('Ctrl Pts',(-9.50104767561052,-15.3447188656481,
1292.78529411765));
#143525=CARTESIAN_POINT('Ctrl Pts',(-10.9229452762603,-14.4643171449067,
1291.29117647059));
#143526=CARTESIAN_POINT('Ctrl Pts',(-12.1588589765331,-13.3376329379985,
1289.79705882353));
#143527=CARTESIAN_POINT('Ctrl Pts',(-13.3947726768058,-12.2109487310903,
1288.30294117647));
#143528=CARTESIAN_POINT('Ctrl Pts',(-14.4026149179538,-10.8763499173728,
1286.80882352941));
#143529=CARTESIAN_POINT('Ctrl Pts',(-15.4104571591017,-9.54175110365538,
1285.31470588235));
#143530=CARTESIAN_POINT('Ctrl Pts',(-16.1559070823762,-8.04468584505497,
1283.82058823529));
#143531=CARTESIAN_POINT('Ctrl Pts',(-16.9013570056506,-6.54762058645456,
1282.32647058824));
#143532=CARTESIAN_POINT('Ctrl Pts',(-17.3590292079831,-4.93906964482095,
1280.83235294118));
#143533=CARTESIAN_POINT('Ctrl Pts',(-17.8167014103155,-3.33051870318735,
1279.33823529412));
#143534=CARTESIAN_POINT('Ctrl Pts',(-17.9710104137728,-1.66525935159368,
1277.84411764706));
#143535=CARTESIAN_POINT('Ctrl Pts',(-18.1253194172301,-1.10985572039171E-15,
1276.35));
#143536=CARTESIAN_POINT('Ctrl Pts',(-17.9710104137728,1.66525935159367,
1274.85588235294));
#143537=CARTESIAN_POINT('Ctrl Pts',(-17.8167014103155,3.33051870318735,
1273.36176470588));
#143538=CARTESIAN_POINT('Ctrl Pts',(-17.3590292079831,4.93906964482096,
1271.86764705882));
#143539=CARTESIAN_POINT('Ctrl Pts',(-16.9013570056506,6.54762058645456,
1270.37352941176));
#143540=CARTESIAN_POINT('Ctrl Pts',(-16.1559070823762,8.04468584505497,
1268.87941176471));
#143541=CARTESIAN_POINT('Ctrl Pts',(-15.4104571591017,9.54175110365538,
1267.38529411765));
#143542=CARTESIAN_POINT('Ctrl Pts',(-14.4026149179538,10.8763499173728,
1265.89117647059));
#143543=CARTESIAN_POINT('Ctrl Pts',(-13.3947726768058,12.2109487310903,
1264.39705882353));
#143544=CARTESIAN_POINT('Ctrl Pts',(-12.1588589765331,13.3376329379985,
1262.90294117647));
#143545=CARTESIAN_POINT('Ctrl Pts',(-10.9229452762603,14.4643171449067,
1261.40882352941));
#143546=CARTESIAN_POINT('Ctrl Pts',(-9.50104767561052,15.3447188656481,
1259.91470588235));
#143547=CARTESIAN_POINT('Ctrl Pts',(-8.07915007496071,16.2251205863895,
1258.42058823529));
#143548=CARTESIAN_POINT('Ctrl Pts',(-6.51968959134574,16.8292587962898,
1256.92647058824));
#143549=CARTESIAN_POINT('Ctrl Pts',(-4.96022910773078,17.4333970061901,
1255.43235294118));
#143550=CARTESIAN_POINT('Ctrl Pts',(-3.31631129755346,17.7406985030951,
1253.93823529412));
#143551=CARTESIAN_POINT('Ctrl Pts',(-1.67239348737615,18.048,1252.44411764706));
#143552=CARTESIAN_POINT('Ctrl Pts',(-2.21024254310115E-15,18.048,1250.95));
#143553=CARTESIAN_POINT('Origin',(5.37704275891775E-14,4.44089209850063E-14,
1504.8993152933));
#143554=CARTESIAN_POINT('',(5.15601850460762E-14,18.048,1149.24863058659));
#143555=CARTESIAN_POINT('',(5.15601850460762E-14,18.048,1149.35));
#143556=CARTESIAN_POINT('',(1.05330612635254E-13,18.0480000000001,1504.8993152933));
#143557=CARTESIAN_POINT('Ctrl Pts',(-2.21024254310115E-15,18.048,1250.84863058659));
#143558=CARTESIAN_POINT('Ctrl Pts',(1.67239348737616,18.048,1249.35451293953));
#143559=CARTESIAN_POINT('Ctrl Pts',(3.31631129755346,17.7406985030951,1247.86039529247));
#143560=CARTESIAN_POINT('Ctrl Pts',(4.96022910773077,17.4333970061901,1246.36627764542));
#143561=CARTESIAN_POINT('Ctrl Pts',(6.51968959134575,16.8292587962898,1244.87215999836));
#143562=CARTESIAN_POINT('Ctrl Pts',(8.07915007496071,16.2251205863895,1243.3780423513));
#143563=CARTESIAN_POINT('Ctrl Pts',(9.50104767561053,15.3447188656481,1241.88392470424));
#143564=CARTESIAN_POINT('Ctrl Pts',(10.9229452762603,14.4643171449067,1240.38980705718));
#143565=CARTESIAN_POINT('Ctrl Pts',(12.1588589765331,13.3376329379985,1238.89568941012));
#143566=CARTESIAN_POINT('Ctrl Pts',(13.3947726768058,12.2109487310903,1237.40157176306));
#143567=CARTESIAN_POINT('Ctrl Pts',(14.4026149179538,10.8763499173728,1235.907454116));
#143568=CARTESIAN_POINT('Ctrl Pts',(15.4104571591017,9.54175110365539,1234.41333646895));
#143569=CARTESIAN_POINT('Ctrl Pts',(16.1559070823762,8.04468584505496,1232.91921882189));
#143570=CARTESIAN_POINT('Ctrl Pts',(16.9013570056506,6.54762058645456,1231.42510117483));
#143571=CARTESIAN_POINT('Ctrl Pts',(17.3590292079831,4.93906964482096,1229.93098352777));
#143572=CARTESIAN_POINT('Ctrl Pts',(17.8167014103155,3.33051870318735,1228.43686588071));
#143573=CARTESIAN_POINT('Ctrl Pts',(17.9710104137728,1.66525935159367,1226.94274823365));
#143574=CARTESIAN_POINT('Ctrl Pts',(18.1253194172301,3.32956716117513E-15,
1225.44863058659));
#143575=CARTESIAN_POINT('Ctrl Pts',(17.9710104137728,-1.66525935159367,
1223.95451293953));
#143576=CARTESIAN_POINT('Ctrl Pts',(17.8167014103155,-3.33051870318736,
1222.46039529247));
#143577=CARTESIAN_POINT('Ctrl Pts',(17.3590292079831,-4.93906964482095,
1220.96627764542));
#143578=CARTESIAN_POINT('Ctrl Pts',(16.9013570056506,-6.54762058645456,
1219.47215999836));
#143579=CARTESIAN_POINT('Ctrl Pts',(16.1559070823762,-8.04468584505497,
1217.9780423513));
#143580=CARTESIAN_POINT('Ctrl Pts',(15.4104571591017,-9.54175110365538,
1216.48392470424));
#143581=CARTESIAN_POINT('Ctrl Pts',(14.4026149179538,-10.8763499173728,
1214.98980705718));
#143582=CARTESIAN_POINT('Ctrl Pts',(13.3947726768058,-12.2109487310903,
1213.49568941012));
#143583=CARTESIAN_POINT('Ctrl Pts',(12.1588589765331,-13.3376329379985,
1212.00157176306));
#143584=CARTESIAN_POINT('Ctrl Pts',(10.9229452762603,-14.4643171449067,
1210.507454116));
#143585=CARTESIAN_POINT('Ctrl Pts',(9.50104767561053,-15.3447188656481,
1209.01333646895));
#143586=CARTESIAN_POINT('Ctrl Pts',(8.07915007496071,-16.2251205863895,
1207.51921882189));
#143587=CARTESIAN_POINT('Ctrl Pts',(6.51968959134574,-16.8292587962898,
1206.02510117483));
#143588=CARTESIAN_POINT('Ctrl Pts',(4.96022910773078,-17.4333970061901,
1204.53098352777));
#143589=CARTESIAN_POINT('Ctrl Pts',(3.31631129755346,-17.7406985030951,
1203.03686588071));
#143590=CARTESIAN_POINT('Ctrl Pts',(1.67239348737615,-18.048,1201.54274823365));
#143591=CARTESIAN_POINT('Ctrl Pts',(0.,-18.048,1200.04863058659));
#143592=CARTESIAN_POINT('Ctrl Pts',(-1.67239348737615,-18.048,1198.55451293953));
#143593=CARTESIAN_POINT('Ctrl Pts',(-3.31631129755346,-17.7406985030951,
1197.06039529247));
#143594=CARTESIAN_POINT('Ctrl Pts',(-4.96022910773077,-17.4333970061901,
1195.56627764542));
#143595=CARTESIAN_POINT('Ctrl Pts',(-6.51968959134574,-16.8292587962898,
1194.07215999836));
#143596=CARTESIAN_POINT('Ctrl Pts',(-8.07915007496071,-16.2251205863895,
1192.5780423513));
#143597=CARTESIAN_POINT('Ctrl Pts',(-9.50104767561052,-15.3447188656481,
1191.08392470424));
#143598=CARTESIAN_POINT('Ctrl Pts',(-10.9229452762603,-14.4643171449067,
1189.58980705718));
#143599=CARTESIAN_POINT('Ctrl Pts',(-12.1588589765331,-13.3376329379985,
1188.09568941012));
#143600=CARTESIAN_POINT('Ctrl Pts',(-13.3947726768058,-12.2109487310903,
1186.60157176306));
#143601=CARTESIAN_POINT('Ctrl Pts',(-14.4026149179538,-10.8763499173728,
1185.107454116));
#143602=CARTESIAN_POINT('Ctrl Pts',(-15.4104571591017,-9.54175110365538,
1183.61333646895));
#143603=CARTESIAN_POINT('Ctrl Pts',(-16.1559070823762,-8.04468584505497,
1182.11921882189));
#143604=CARTESIAN_POINT('Ctrl Pts',(-16.9013570056506,-6.54762058645456,
1180.62510117483));
#143605=CARTESIAN_POINT('Ctrl Pts',(-17.3590292079831,-4.93906964482095,
1179.13098352777));
#143606=CARTESIAN_POINT('Ctrl Pts',(-17.8167014103155,-3.33051870318735,
1177.63686588071));
#143607=CARTESIAN_POINT('Ctrl Pts',(-17.9710104137728,-1.66525935159368,
1176.14274823365));
#143608=CARTESIAN_POINT('Ctrl Pts',(-18.1253194172301,-1.10985572039171E-15,
1174.64863058659));
#143609=CARTESIAN_POINT('Ctrl Pts',(-17.9710104137728,1.66525935159367,
1173.15451293953));
#143610=CARTESIAN_POINT('Ctrl Pts',(-17.8167014103155,3.33051870318735,
1171.66039529247));
#143611=CARTESIAN_POINT('Ctrl Pts',(-17.3590292079831,4.93906964482096,
1170.16627764542));
#143612=CARTESIAN_POINT('Ctrl Pts',(-16.9013570056506,6.54762058645456,
1168.67215999836));
#143613=CARTESIAN_POINT('Ctrl Pts',(-16.1559070823762,8.04468584505497,
1167.1780423513));
#143614=CARTESIAN_POINT('Ctrl Pts',(-15.4104571591017,9.54175110365538,
1165.68392470424));
#143615=CARTESIAN_POINT('Ctrl Pts',(-14.4026149179538,10.8763499173728,
1164.18980705718));
#143616=CARTESIAN_POINT('Ctrl Pts',(-13.3947726768058,12.2109487310903,
1162.69568941012));
#143617=CARTESIAN_POINT('Ctrl Pts',(-12.1588589765331,13.3376329379985,
1161.20157176306));
#143618=CARTESIAN_POINT('Ctrl Pts',(-10.9229452762603,14.4643171449067,
1159.707454116));
#143619=CARTESIAN_POINT('Ctrl Pts',(-9.50104767561052,15.3447188656481,
1158.21333646895));
#143620=CARTESIAN_POINT('Ctrl Pts',(-8.07915007496071,16.2251205863895,
1156.71921882189));
#143621=CARTESIAN_POINT('Ctrl Pts',(-6.51968959134574,16.8292587962898,
1155.22510117483));
#143622=CARTESIAN_POINT('Ctrl Pts',(-4.96022910773078,17.4333970061901,
1153.73098352777));
#143623=CARTESIAN_POINT('Ctrl Pts',(-3.31631129755346,17.7406985030951,
1152.23686588071));
#143624=CARTESIAN_POINT('Ctrl Pts',(-1.67239348737615,18.048,1150.74274823365));
#143625=CARTESIAN_POINT('Ctrl Pts',(-2.21024254310115E-15,18.048,1149.24863058659));
#143626=CARTESIAN_POINT('Ctrl Pts',(-2.21024254310115E-15,18.048,1250.95));
#143627=CARTESIAN_POINT('Ctrl Pts',(1.67239348737616,18.048,1249.45588235294));
#143628=CARTESIAN_POINT('Ctrl Pts',(3.31631129755346,17.7406985030951,1247.96176470588));
#143629=CARTESIAN_POINT('Ctrl Pts',(4.96022910773077,17.4333970061901,1246.46764705882));
#143630=CARTESIAN_POINT('Ctrl Pts',(6.51968959134575,16.8292587962898,1244.97352941176));
#143631=CARTESIAN_POINT('Ctrl Pts',(8.07915007496071,16.2251205863895,1243.47941176471));
#143632=CARTESIAN_POINT('Ctrl Pts',(9.50104767561053,15.3447188656481,1241.98529411765));
#143633=CARTESIAN_POINT('Ctrl Pts',(10.9229452762603,14.4643171449067,1240.49117647059));
#143634=CARTESIAN_POINT('Ctrl Pts',(12.1588589765331,13.3376329379985,1238.99705882353));
#143635=CARTESIAN_POINT('Ctrl Pts',(13.3947726768058,12.2109487310903,1237.50294117647));
#143636=CARTESIAN_POINT('Ctrl Pts',(14.4026149179538,10.8763499173728,1236.00882352941));
#143637=CARTESIAN_POINT('Ctrl Pts',(15.4104571591017,9.54175110365539,1234.51470588235));
#143638=CARTESIAN_POINT('Ctrl Pts',(16.1559070823762,8.04468584505496,1233.02058823529));
#143639=CARTESIAN_POINT('Ctrl Pts',(16.9013570056506,6.54762058645456,1231.52647058824));
#143640=CARTESIAN_POINT('Ctrl Pts',(17.3590292079831,4.93906964482096,1230.03235294118));
#143641=CARTESIAN_POINT('Ctrl Pts',(17.8167014103155,3.33051870318735,1228.53823529412));
#143642=CARTESIAN_POINT('Ctrl Pts',(17.9710104137728,1.66525935159367,1227.04411764706));
#143643=CARTESIAN_POINT('Ctrl Pts',(18.1253194172301,3.32956716117513E-15,
1225.55));
#143644=CARTESIAN_POINT('Ctrl Pts',(17.9710104137728,-1.66525935159367,
1224.05588235294));
#143645=CARTESIAN_POINT('Ctrl Pts',(17.8167014103155,-3.33051870318736,
1222.56176470588));
#143646=CARTESIAN_POINT('Ctrl Pts',(17.3590292079831,-4.93906964482095,
1221.06764705882));
#143647=CARTESIAN_POINT('Ctrl Pts',(16.9013570056506,-6.54762058645456,
1219.57352941176));
#143648=CARTESIAN_POINT('Ctrl Pts',(16.1559070823762,-8.04468584505497,
1218.07941176471));
#143649=CARTESIAN_POINT('Ctrl Pts',(15.4104571591017,-9.54175110365538,
1216.58529411765));
#143650=CARTESIAN_POINT('Ctrl Pts',(14.4026149179538,-10.8763499173728,
1215.09117647059));
#143651=CARTESIAN_POINT('Ctrl Pts',(13.3947726768058,-12.2109487310903,
1213.59705882353));
#143652=CARTESIAN_POINT('Ctrl Pts',(12.1588589765331,-13.3376329379985,
1212.10294117647));
#143653=CARTESIAN_POINT('Ctrl Pts',(10.9229452762603,-14.4643171449067,
1210.60882352941));
#143654=CARTESIAN_POINT('Ctrl Pts',(9.50104767561053,-15.3447188656481,
1209.11470588235));
#143655=CARTESIAN_POINT('Ctrl Pts',(8.07915007496071,-16.2251205863895,
1207.62058823529));
#143656=CARTESIAN_POINT('Ctrl Pts',(6.51968959134574,-16.8292587962898,
1206.12647058824));
#143657=CARTESIAN_POINT('Ctrl Pts',(4.96022910773078,-17.4333970061901,
1204.63235294118));
#143658=CARTESIAN_POINT('Ctrl Pts',(3.31631129755346,-17.7406985030951,
1203.13823529412));
#143659=CARTESIAN_POINT('Ctrl Pts',(1.67239348737615,-18.048,1201.64411764706));
#143660=CARTESIAN_POINT('Ctrl Pts',(0.,-18.048,1200.15));
#143661=CARTESIAN_POINT('Ctrl Pts',(-1.67239348737615,-18.048,1198.65588235294));
#143662=CARTESIAN_POINT('Ctrl Pts',(-3.31631129755346,-17.7406985030951,
1197.16176470588));
#143663=CARTESIAN_POINT('Ctrl Pts',(-4.96022910773077,-17.4333970061901,
1195.66764705882));
#143664=CARTESIAN_POINT('Ctrl Pts',(-6.51968959134574,-16.8292587962898,
1194.17352941176));
#143665=CARTESIAN_POINT('Ctrl Pts',(-8.07915007496071,-16.2251205863895,
1192.67941176471));
#143666=CARTESIAN_POINT('Ctrl Pts',(-9.50104767561052,-15.3447188656481,
1191.18529411765));
#143667=CARTESIAN_POINT('Ctrl Pts',(-10.9229452762603,-14.4643171449067,
1189.69117647059));
#143668=CARTESIAN_POINT('Ctrl Pts',(-12.1588589765331,-13.3376329379985,
1188.19705882353));
#143669=CARTESIAN_POINT('Ctrl Pts',(-13.3947726768058,-12.2109487310903,
1186.70294117647));
#143670=CARTESIAN_POINT('Ctrl Pts',(-14.4026149179538,-10.8763499173728,
1185.20882352941));
#143671=CARTESIAN_POINT('Ctrl Pts',(-15.4104571591017,-9.54175110365538,
1183.71470588235));
#143672=CARTESIAN_POINT('Ctrl Pts',(-16.1559070823762,-8.04468584505497,
1182.22058823529));
#143673=CARTESIAN_POINT('Ctrl Pts',(-16.9013570056506,-6.54762058645456,
1180.72647058824));
#143674=CARTESIAN_POINT('Ctrl Pts',(-17.3590292079831,-4.93906964482095,
1179.23235294118));
#143675=CARTESIAN_POINT('Ctrl Pts',(-17.8167014103155,-3.33051870318735,
1177.73823529412));
#143676=CARTESIAN_POINT('Ctrl Pts',(-17.9710104137728,-1.66525935159368,
1176.24411764706));
#143677=CARTESIAN_POINT('Ctrl Pts',(-18.1253194172301,-1.10985572039171E-15,
1174.75));
#143678=CARTESIAN_POINT('Ctrl Pts',(-17.9710104137728,1.66525935159367,
1173.25588235294));
#143679=CARTESIAN_POINT('Ctrl Pts',(-17.8167014103155,3.33051870318735,
1171.76176470588));
#143680=CARTESIAN_POINT('Ctrl Pts',(-17.3590292079831,4.93906964482096,
1170.26764705882));
#143681=CARTESIAN_POINT('Ctrl Pts',(-16.9013570056506,6.54762058645456,
1168.77352941176));
#143682=CARTESIAN_POINT('Ctrl Pts',(-16.1559070823762,8.04468584505497,
1167.27941176471));
#143683=CARTESIAN_POINT('Ctrl Pts',(-15.4104571591017,9.54175110365538,
1165.78529411765));
#143684=CARTESIAN_POINT('Ctrl Pts',(-14.4026149179538,10.8763499173728,
1164.29117647059));
#143685=CARTESIAN_POINT('Ctrl Pts',(-13.3947726768058,12.2109487310903,
1162.79705882353));
#143686=CARTESIAN_POINT('Ctrl Pts',(-12.1588589765331,13.3376329379985,
1161.30294117647));
#143687=CARTESIAN_POINT('Ctrl Pts',(-10.9229452762603,14.4643171449067,
1159.80882352941));
#143688=CARTESIAN_POINT('Ctrl Pts',(-9.50104767561052,15.3447188656481,
1158.31470588235));
#143689=CARTESIAN_POINT('Ctrl Pts',(-8.07915007496071,16.2251205863895,
1156.82058823529));
#143690=CARTESIAN_POINT('Ctrl Pts',(-6.51968959134574,16.8292587962898,
1155.32647058824));
#143691=CARTESIAN_POINT('Ctrl Pts',(-4.96022910773078,17.4333970061901,
1153.83235294118));
#143692=CARTESIAN_POINT('Ctrl Pts',(-3.31631129755346,17.7406985030951,
1152.33823529412));
#143693=CARTESIAN_POINT('Ctrl Pts',(-1.67239348737615,18.048,1150.84411764706));
#143694=CARTESIAN_POINT('Ctrl Pts',(-2.21024254310115E-15,18.048,1149.35));
#143695=CARTESIAN_POINT('Origin',(5.37704275891775E-14,4.44089209850063E-14,
1504.8993152933));
#143696=CARTESIAN_POINT('',(5.15601850460762E-14,18.048,1047.64863058659));
#143697=CARTESIAN_POINT('',(5.15601850460762E-14,18.048,1047.75));
#143698=CARTESIAN_POINT('',(1.05330612635254E-13,18.0480000000001,1504.8993152933));
#143699=CARTESIAN_POINT('Ctrl Pts',(-2.21024254310115E-15,18.048,1149.24863058659));
#143700=CARTESIAN_POINT('Ctrl Pts',(1.67239348737616,18.048,1147.75451293953));
#143701=CARTESIAN_POINT('Ctrl Pts',(3.31631129755346,17.7406985030951,1146.26039529247));
#143702=CARTESIAN_POINT('Ctrl Pts',(4.96022910773077,17.4333970061901,1144.76627764542));
#143703=CARTESIAN_POINT('Ctrl Pts',(6.51968959134575,16.8292587962898,1143.27215999836));
#143704=CARTESIAN_POINT('Ctrl Pts',(8.07915007496071,16.2251205863895,1141.7780423513));
#143705=CARTESIAN_POINT('Ctrl Pts',(9.50104767561053,15.3447188656481,1140.28392470424));
#143706=CARTESIAN_POINT('Ctrl Pts',(10.9229452762603,14.4643171449067,1138.78980705718));
#143707=CARTESIAN_POINT('Ctrl Pts',(12.1588589765331,13.3376329379985,1137.29568941012));
#143708=CARTESIAN_POINT('Ctrl Pts',(13.3947726768058,12.2109487310903,1135.80157176306));
#143709=CARTESIAN_POINT('Ctrl Pts',(14.4026149179538,10.8763499173728,1134.307454116));
#143710=CARTESIAN_POINT('Ctrl Pts',(15.4104571591017,9.54175110365539,1132.81333646895));
#143711=CARTESIAN_POINT('Ctrl Pts',(16.1559070823762,8.04468584505496,1131.31921882189));
#143712=CARTESIAN_POINT('Ctrl Pts',(16.9013570056506,6.54762058645456,1129.82510117483));
#143713=CARTESIAN_POINT('Ctrl Pts',(17.3590292079831,4.93906964482096,1128.33098352777));
#143714=CARTESIAN_POINT('Ctrl Pts',(17.8167014103155,3.33051870318735,1126.83686588071));
#143715=CARTESIAN_POINT('Ctrl Pts',(17.9710104137728,1.66525935159367,1125.34274823365));
#143716=CARTESIAN_POINT('Ctrl Pts',(18.1253194172301,3.32956716117513E-15,
1123.84863058659));
#143717=CARTESIAN_POINT('Ctrl Pts',(17.9710104137728,-1.66525935159367,
1122.35451293953));
#143718=CARTESIAN_POINT('Ctrl Pts',(17.8167014103155,-3.33051870318736,
1120.86039529247));
#143719=CARTESIAN_POINT('Ctrl Pts',(17.3590292079831,-4.93906964482095,
1119.36627764542));
#143720=CARTESIAN_POINT('Ctrl Pts',(16.9013570056506,-6.54762058645456,
1117.87215999836));
#143721=CARTESIAN_POINT('Ctrl Pts',(16.1559070823762,-8.04468584505497,
1116.3780423513));
#143722=CARTESIAN_POINT('Ctrl Pts',(15.4104571591017,-9.54175110365538,
1114.88392470424));
#143723=CARTESIAN_POINT('Ctrl Pts',(14.4026149179538,-10.8763499173728,
1113.38980705718));
#143724=CARTESIAN_POINT('Ctrl Pts',(13.3947726768058,-12.2109487310903,
1111.89568941012));
#143725=CARTESIAN_POINT('Ctrl Pts',(12.1588589765331,-13.3376329379985,
1110.40157176306));
#143726=CARTESIAN_POINT('Ctrl Pts',(10.9229452762603,-14.4643171449067,
1108.907454116));
#143727=CARTESIAN_POINT('Ctrl Pts',(9.50104767561053,-15.3447188656481,
1107.41333646895));
#143728=CARTESIAN_POINT('Ctrl Pts',(8.07915007496071,-16.2251205863895,
1105.91921882189));
#143729=CARTESIAN_POINT('Ctrl Pts',(6.51968959134574,-16.8292587962898,
1104.42510117483));
#143730=CARTESIAN_POINT('Ctrl Pts',(4.96022910773078,-17.4333970061901,
1102.93098352777));
#143731=CARTESIAN_POINT('Ctrl Pts',(3.31631129755346,-17.7406985030951,
1101.43686588071));
#143732=CARTESIAN_POINT('Ctrl Pts',(1.67239348737615,-18.048,1099.94274823365));
#143733=CARTESIAN_POINT('Ctrl Pts',(0.,-18.048,1098.44863058659));
#143734=CARTESIAN_POINT('Ctrl Pts',(-1.67239348737615,-18.048,1096.95451293953));
#143735=CARTESIAN_POINT('Ctrl Pts',(-3.31631129755346,-17.7406985030951,
1095.46039529247));
#143736=CARTESIAN_POINT('Ctrl Pts',(-4.96022910773077,-17.4333970061901,
1093.96627764542));
#143737=CARTESIAN_POINT('Ctrl Pts',(-6.51968959134574,-16.8292587962898,
1092.47215999836));
#143738=CARTESIAN_POINT('Ctrl Pts',(-8.07915007496071,-16.2251205863895,
1090.9780423513));
#143739=CARTESIAN_POINT('Ctrl Pts',(-9.50104767561052,-15.3447188656481,
1089.48392470424));
#143740=CARTESIAN_POINT('Ctrl Pts',(-10.9229452762603,-14.4643171449067,
1087.98980705718));
#143741=CARTESIAN_POINT('Ctrl Pts',(-12.1588589765331,-13.3376329379985,
1086.49568941012));
#143742=CARTESIAN_POINT('Ctrl Pts',(-13.3947726768058,-12.2109487310903,
1085.00157176306));
#143743=CARTESIAN_POINT('Ctrl Pts',(-14.4026149179538,-10.8763499173728,
1083.507454116));
#143744=CARTESIAN_POINT('Ctrl Pts',(-15.4104571591017,-9.54175110365538,
1082.01333646895));
#143745=CARTESIAN_POINT('Ctrl Pts',(-16.1559070823762,-8.04468584505497,
1080.51921882189));
#143746=CARTESIAN_POINT('Ctrl Pts',(-16.9013570056506,-6.54762058645456,
1079.02510117483));
#143747=CARTESIAN_POINT('Ctrl Pts',(-17.3590292079831,-4.93906964482095,
1077.53098352777));
#143748=CARTESIAN_POINT('Ctrl Pts',(-17.8167014103155,-3.33051870318735,
1076.03686588071));
#143749=CARTESIAN_POINT('Ctrl Pts',(-17.9710104137728,-1.66525935159368,
1074.54274823365));
#143750=CARTESIAN_POINT('Ctrl Pts',(-18.1253194172301,-1.10985572039171E-15,
1073.04863058659));
#143751=CARTESIAN_POINT('Ctrl Pts',(-17.9710104137728,1.66525935159367,
1071.55451293953));
#143752=CARTESIAN_POINT('Ctrl Pts',(-17.8167014103155,3.33051870318735,
1070.06039529247));
#143753=CARTESIAN_POINT('Ctrl Pts',(-17.3590292079831,4.93906964482096,
1068.56627764542));
#143754=CARTESIAN_POINT('Ctrl Pts',(-16.9013570056506,6.54762058645456,
1067.07215999836));
#143755=CARTESIAN_POINT('Ctrl Pts',(-16.1559070823762,8.04468584505497,
1065.5780423513));
#143756=CARTESIAN_POINT('Ctrl Pts',(-15.4104571591017,9.54175110365538,
1064.08392470424));
#143757=CARTESIAN_POINT('Ctrl Pts',(-14.4026149179538,10.8763499173728,
1062.58980705718));
#143758=CARTESIAN_POINT('Ctrl Pts',(-13.3947726768058,12.2109487310903,
1061.09568941012));
#143759=CARTESIAN_POINT('Ctrl Pts',(-12.1588589765331,13.3376329379985,
1059.60157176306));
#143760=CARTESIAN_POINT('Ctrl Pts',(-10.9229452762603,14.4643171449067,
1058.107454116));
#143761=CARTESIAN_POINT('Ctrl Pts',(-9.50104767561052,15.3447188656481,
1056.61333646895));
#143762=CARTESIAN_POINT('Ctrl Pts',(-8.07915007496071,16.2251205863895,
1055.11921882189));
#143763=CARTESIAN_POINT('Ctrl Pts',(-6.51968959134574,16.8292587962898,
1053.62510117483));
#143764=CARTESIAN_POINT('Ctrl Pts',(-4.96022910773078,17.4333970061901,
1052.13098352777));
#143765=CARTESIAN_POINT('Ctrl Pts',(-3.31631129755346,17.7406985030951,
1050.63686588071));
#143766=CARTESIAN_POINT('Ctrl Pts',(-1.67239348737615,18.048,1049.14274823365));
#143767=CARTESIAN_POINT('Ctrl Pts',(-2.21024254310115E-15,18.048,1047.64863058659));
#143768=CARTESIAN_POINT('Ctrl Pts',(-2.21024254310115E-15,18.048,1149.35));
#143769=CARTESIAN_POINT('Ctrl Pts',(1.67239348737616,18.048,1147.85588235294));
#143770=CARTESIAN_POINT('Ctrl Pts',(3.31631129755346,17.7406985030951,1146.36176470588));
#143771=CARTESIAN_POINT('Ctrl Pts',(4.96022910773077,17.4333970061901,1144.86764705882));
#143772=CARTESIAN_POINT('Ctrl Pts',(6.51968959134575,16.8292587962898,1143.37352941176));
#143773=CARTESIAN_POINT('Ctrl Pts',(8.07915007496071,16.2251205863895,1141.87941176471));
#143774=CARTESIAN_POINT('Ctrl Pts',(9.50104767561053,15.3447188656481,1140.38529411765));
#143775=CARTESIAN_POINT('Ctrl Pts',(10.9229452762603,14.4643171449067,1138.89117647059));
#143776=CARTESIAN_POINT('Ctrl Pts',(12.1588589765331,13.3376329379985,1137.39705882353));
#143777=CARTESIAN_POINT('Ctrl Pts',(13.3947726768058,12.2109487310903,1135.90294117647));
#143778=CARTESIAN_POINT('Ctrl Pts',(14.4026149179538,10.8763499173728,1134.40882352941));
#143779=CARTESIAN_POINT('Ctrl Pts',(15.4104571591017,9.54175110365539,1132.91470588235));
#143780=CARTESIAN_POINT('Ctrl Pts',(16.1559070823762,8.04468584505496,1131.42058823529));
#143781=CARTESIAN_POINT('Ctrl Pts',(16.9013570056506,6.54762058645456,1129.92647058824));
#143782=CARTESIAN_POINT('Ctrl Pts',(17.3590292079831,4.93906964482096,1128.43235294118));
#143783=CARTESIAN_POINT('Ctrl Pts',(17.8167014103155,3.33051870318735,1126.93823529412));
#143784=CARTESIAN_POINT('Ctrl Pts',(17.9710104137728,1.66525935159367,1125.44411764706));
#143785=CARTESIAN_POINT('Ctrl Pts',(18.1253194172301,3.32956716117513E-15,
1123.95));
#143786=CARTESIAN_POINT('Ctrl Pts',(17.9710104137728,-1.66525935159367,
1122.45588235294));
#143787=CARTESIAN_POINT('Ctrl Pts',(17.8167014103155,-3.33051870318736,
1120.96176470588));
#143788=CARTESIAN_POINT('Ctrl Pts',(17.3590292079831,-4.93906964482095,
1119.46764705882));
#143789=CARTESIAN_POINT('Ctrl Pts',(16.9013570056506,-6.54762058645456,
1117.97352941176));
#143790=CARTESIAN_POINT('Ctrl Pts',(16.1559070823762,-8.04468584505497,
1116.47941176471));
#143791=CARTESIAN_POINT('Ctrl Pts',(15.4104571591017,-9.54175110365538,
1114.98529411765));
#143792=CARTESIAN_POINT('Ctrl Pts',(14.4026149179538,-10.8763499173728,
1113.49117647059));
#143793=CARTESIAN_POINT('Ctrl Pts',(13.3947726768058,-12.2109487310903,
1111.99705882353));
#143794=CARTESIAN_POINT('Ctrl Pts',(12.1588589765331,-13.3376329379985,
1110.50294117647));
#143795=CARTESIAN_POINT('Ctrl Pts',(10.9229452762603,-14.4643171449067,
1109.00882352941));
#143796=CARTESIAN_POINT('Ctrl Pts',(9.50104767561053,-15.3447188656481,
1107.51470588235));
#143797=CARTESIAN_POINT('Ctrl Pts',(8.07915007496071,-16.2251205863895,
1106.02058823529));
#143798=CARTESIAN_POINT('Ctrl Pts',(6.51968959134574,-16.8292587962898,
1104.52647058824));
#143799=CARTESIAN_POINT('Ctrl Pts',(4.96022910773078,-17.4333970061901,
1103.03235294118));
#143800=CARTESIAN_POINT('Ctrl Pts',(3.31631129755346,-17.7406985030951,
1101.53823529412));
#143801=CARTESIAN_POINT('Ctrl Pts',(1.67239348737615,-18.048,1100.04411764706));
#143802=CARTESIAN_POINT('Ctrl Pts',(0.,-18.048,1098.55));
#143803=CARTESIAN_POINT('Ctrl Pts',(-1.67239348737615,-18.048,1097.05588235294));
#143804=CARTESIAN_POINT('Ctrl Pts',(-3.31631129755346,-17.7406985030951,
1095.56176470588));
#143805=CARTESIAN_POINT('Ctrl Pts',(-4.96022910773077,-17.4333970061901,
1094.06764705882));
#143806=CARTESIAN_POINT('Ctrl Pts',(-6.51968959134574,-16.8292587962898,
1092.57352941176));
#143807=CARTESIAN_POINT('Ctrl Pts',(-8.07915007496071,-16.2251205863895,
1091.07941176471));
#143808=CARTESIAN_POINT('Ctrl Pts',(-9.50104767561052,-15.3447188656481,
1089.58529411765));
#143809=CARTESIAN_POINT('Ctrl Pts',(-10.9229452762603,-14.4643171449067,
1088.09117647059));
#143810=CARTESIAN_POINT('Ctrl Pts',(-12.1588589765331,-13.3376329379985,
1086.59705882353));
#143811=CARTESIAN_POINT('Ctrl Pts',(-13.3947726768058,-12.2109487310903,
1085.10294117647));
#143812=CARTESIAN_POINT('Ctrl Pts',(-14.4026149179538,-10.8763499173728,
1083.60882352941));
#143813=CARTESIAN_POINT('Ctrl Pts',(-15.4104571591017,-9.54175110365538,
1082.11470588235));
#143814=CARTESIAN_POINT('Ctrl Pts',(-16.1559070823762,-8.04468584505497,
1080.62058823529));
#143815=CARTESIAN_POINT('Ctrl Pts',(-16.9013570056506,-6.54762058645456,
1079.12647058824));
#143816=CARTESIAN_POINT('Ctrl Pts',(-17.3590292079831,-4.93906964482095,
1077.63235294118));
#143817=CARTESIAN_POINT('Ctrl Pts',(-17.8167014103155,-3.33051870318735,
1076.13823529412));
#143818=CARTESIAN_POINT('Ctrl Pts',(-17.9710104137728,-1.66525935159368,
1074.64411764706));
#143819=CARTESIAN_POINT('Ctrl Pts',(-18.1253194172301,-1.10985572039171E-15,
1073.15));
#143820=CARTESIAN_POINT('Ctrl Pts',(-17.9710104137728,1.66525935159367,
1071.65588235294));
#143821=CARTESIAN_POINT('Ctrl Pts',(-17.8167014103155,3.33051870318735,
1070.16176470588));
#143822=CARTESIAN_POINT('Ctrl Pts',(-17.3590292079831,4.93906964482096,
1068.66764705882));
#143823=CARTESIAN_POINT('Ctrl Pts',(-16.9013570056506,6.54762058645456,
1067.17352941176));
#143824=CARTESIAN_POINT('Ctrl Pts',(-16.1559070823762,8.04468584505497,
1065.67941176471));
#143825=CARTESIAN_POINT('Ctrl Pts',(-15.4104571591017,9.54175110365538,
1064.18529411765));
#143826=CARTESIAN_POINT('Ctrl Pts',(-14.4026149179538,10.8763499173728,
1062.69117647059));
#143827=CARTESIAN_POINT('Ctrl Pts',(-13.3947726768058,12.2109487310903,
1061.19705882353));
#143828=CARTESIAN_POINT('Ctrl Pts',(-12.1588589765331,13.3376329379985,
1059.70294117647));
#143829=CARTESIAN_POINT('Ctrl Pts',(-10.9229452762603,14.4643171449067,
1058.20882352941));
#143830=CARTESIAN_POINT('Ctrl Pts',(-9.50104767561052,15.3447188656481,
1056.71470588235));
#143831=CARTESIAN_POINT('Ctrl Pts',(-8.07915007496071,16.2251205863895,
1055.22058823529));
#143832=CARTESIAN_POINT('Ctrl Pts',(-6.51968959134574,16.8292587962898,
1053.72647058824));
#143833=CARTESIAN_POINT('Ctrl Pts',(-4.96022910773078,17.4333970061901,
1052.23235294118));
#143834=CARTESIAN_POINT('Ctrl Pts',(-3.31631129755346,17.7406985030951,
1050.73823529412));
#143835=CARTESIAN_POINT('Ctrl Pts',(-1.67239348737615,18.048,1049.24411764706));
#143836=CARTESIAN_POINT('Ctrl Pts',(-2.21024254310115E-15,18.048,1047.75));
#143837=CARTESIAN_POINT('Origin',(5.37704275891775E-14,4.44089209850063E-14,
1504.8993152933));
#143838=CARTESIAN_POINT('',(5.15601850460762E-14,18.048,946.048630586592));
#143839=CARTESIAN_POINT('',(5.15601850460762E-14,18.048,946.15));
#143840=CARTESIAN_POINT('',(1.05330612635254E-13,18.0480000000001,1504.8993152933));
#143841=CARTESIAN_POINT('Ctrl Pts',(-2.21024254310115E-15,18.048,1047.64863058659));
#143842=CARTESIAN_POINT('Ctrl Pts',(1.67239348737616,18.048,1046.15451293953));
#143843=CARTESIAN_POINT('Ctrl Pts',(3.31631129755346,17.7406985030951,1044.66039529247));
#143844=CARTESIAN_POINT('Ctrl Pts',(4.96022910773077,17.4333970061901,1043.16627764542));
#143845=CARTESIAN_POINT('Ctrl Pts',(6.51968959134575,16.8292587962898,1041.67215999836));
#143846=CARTESIAN_POINT('Ctrl Pts',(8.07915007496071,16.2251205863895,1040.1780423513));
#143847=CARTESIAN_POINT('Ctrl Pts',(9.50104767561053,15.3447188656481,1038.68392470424));
#143848=CARTESIAN_POINT('Ctrl Pts',(10.9229452762603,14.4643171449067,1037.18980705718));
#143849=CARTESIAN_POINT('Ctrl Pts',(12.1588589765331,13.3376329379985,1035.69568941012));
#143850=CARTESIAN_POINT('Ctrl Pts',(13.3947726768058,12.2109487310903,1034.20157176306));
#143851=CARTESIAN_POINT('Ctrl Pts',(14.4026149179538,10.8763499173728,1032.707454116));
#143852=CARTESIAN_POINT('Ctrl Pts',(15.4104571591017,9.54175110365539,1031.21333646895));
#143853=CARTESIAN_POINT('Ctrl Pts',(16.1559070823762,8.04468584505496,1029.71921882189));
#143854=CARTESIAN_POINT('Ctrl Pts',(16.9013570056506,6.54762058645456,1028.22510117483));
#143855=CARTESIAN_POINT('Ctrl Pts',(17.3590292079831,4.93906964482096,1026.73098352777));
#143856=CARTESIAN_POINT('Ctrl Pts',(17.8167014103155,3.33051870318735,1025.23686588071));
#143857=CARTESIAN_POINT('Ctrl Pts',(17.9710104137728,1.66525935159367,1023.74274823365));
#143858=CARTESIAN_POINT('Ctrl Pts',(18.1253194172301,3.32956716117513E-15,
1022.24863058659));
#143859=CARTESIAN_POINT('Ctrl Pts',(17.9710104137728,-1.66525935159367,
1020.75451293953));
#143860=CARTESIAN_POINT('Ctrl Pts',(17.8167014103155,-3.33051870318736,
1019.26039529247));
#143861=CARTESIAN_POINT('Ctrl Pts',(17.3590292079831,-4.93906964482095,
1017.76627764542));
#143862=CARTESIAN_POINT('Ctrl Pts',(16.9013570056506,-6.54762058645456,
1016.27215999836));
#143863=CARTESIAN_POINT('Ctrl Pts',(16.1559070823762,-8.04468584505497,
1014.7780423513));
#143864=CARTESIAN_POINT('Ctrl Pts',(15.4104571591017,-9.54175110365538,
1013.28392470424));
#143865=CARTESIAN_POINT('Ctrl Pts',(14.4026149179538,-10.8763499173728,
1011.78980705718));
#143866=CARTESIAN_POINT('Ctrl Pts',(13.3947726768058,-12.2109487310903,
1010.29568941012));
#143867=CARTESIAN_POINT('Ctrl Pts',(12.1588589765331,-13.3376329379985,
1008.80157176306));
#143868=CARTESIAN_POINT('Ctrl Pts',(10.9229452762603,-14.4643171449067,
1007.307454116));
#143869=CARTESIAN_POINT('Ctrl Pts',(9.50104767561053,-15.3447188656481,
1005.81333646895));
#143870=CARTESIAN_POINT('Ctrl Pts',(8.07915007496071,-16.2251205863895,
1004.31921882189));
#143871=CARTESIAN_POINT('Ctrl Pts',(6.51968959134574,-16.8292587962898,
1002.82510117483));
#143872=CARTESIAN_POINT('Ctrl Pts',(4.96022910773078,-17.4333970061901,
1001.33098352777));
#143873=CARTESIAN_POINT('Ctrl Pts',(3.31631129755346,-17.7406985030951,
999.83686588071));
#143874=CARTESIAN_POINT('Ctrl Pts',(1.67239348737615,-18.048,998.342748233651));
#143875=CARTESIAN_POINT('Ctrl Pts',(0.,-18.048,996.848630586592));
#143876=CARTESIAN_POINT('Ctrl Pts',(-1.67239348737615,-18.048,995.354512939534));
#143877=CARTESIAN_POINT('Ctrl Pts',(-3.31631129755346,-17.7406985030951,
993.860395292475));
#143878=CARTESIAN_POINT('Ctrl Pts',(-4.96022910773077,-17.4333970061901,
992.366277645416));
#143879=CARTESIAN_POINT('Ctrl Pts',(-6.51968959134574,-16.8292587962898,
990.872159998357));
#143880=CARTESIAN_POINT('Ctrl Pts',(-8.07915007496071,-16.2251205863895,
989.378042351298));
#143881=CARTESIAN_POINT('Ctrl Pts',(-9.50104767561052,-15.3447188656481,
987.883924704239));
#143882=CARTESIAN_POINT('Ctrl Pts',(-10.9229452762603,-14.4643171449067,
986.389807057181));
#143883=CARTESIAN_POINT('Ctrl Pts',(-12.1588589765331,-13.3376329379985,
984.895689410122));
#143884=CARTESIAN_POINT('Ctrl Pts',(-13.3947726768058,-12.2109487310903,
983.401571763063));
#143885=CARTESIAN_POINT('Ctrl Pts',(-14.4026149179538,-10.8763499173728,
981.907454116004));
#143886=CARTESIAN_POINT('Ctrl Pts',(-15.4104571591017,-9.54175110365538,
980.413336468945));
#143887=CARTESIAN_POINT('Ctrl Pts',(-16.1559070823762,-8.04468584505497,
978.919218821886));
#143888=CARTESIAN_POINT('Ctrl Pts',(-16.9013570056506,-6.54762058645456,
977.425101174828));
#143889=CARTESIAN_POINT('Ctrl Pts',(-17.3590292079831,-4.93906964482095,
975.930983527769));
#143890=CARTESIAN_POINT('Ctrl Pts',(-17.8167014103155,-3.33051870318735,
974.43686588071));
#143891=CARTESIAN_POINT('Ctrl Pts',(-17.9710104137728,-1.66525935159368,
972.942748233651));
#143892=CARTESIAN_POINT('Ctrl Pts',(-18.1253194172301,-1.10985572039171E-15,
971.448630586592));
#143893=CARTESIAN_POINT('Ctrl Pts',(-17.9710104137728,1.66525935159367,
969.954512939534));
#143894=CARTESIAN_POINT('Ctrl Pts',(-17.8167014103155,3.33051870318735,
968.460395292475));
#143895=CARTESIAN_POINT('Ctrl Pts',(-17.3590292079831,4.93906964482096,
966.966277645416));
#143896=CARTESIAN_POINT('Ctrl Pts',(-16.9013570056506,6.54762058645456,
965.472159998357));
#143897=CARTESIAN_POINT('Ctrl Pts',(-16.1559070823762,8.04468584505497,
963.978042351298));
#143898=CARTESIAN_POINT('Ctrl Pts',(-15.4104571591017,9.54175110365538,
962.483924704239));
#143899=CARTESIAN_POINT('Ctrl Pts',(-14.4026149179538,10.8763499173728,
960.989807057181));
#143900=CARTESIAN_POINT('Ctrl Pts',(-13.3947726768058,12.2109487310903,
959.495689410122));
#143901=CARTESIAN_POINT('Ctrl Pts',(-12.1588589765331,13.3376329379985,
958.001571763063));
#143902=CARTESIAN_POINT('Ctrl Pts',(-10.9229452762603,14.4643171449067,
956.507454116004));
#143903=CARTESIAN_POINT('Ctrl Pts',(-9.50104767561052,15.3447188656481,
955.013336468945));
#143904=CARTESIAN_POINT('Ctrl Pts',(-8.07915007496071,16.2251205863895,
953.519218821887));
#143905=CARTESIAN_POINT('Ctrl Pts',(-6.51968959134574,16.8292587962898,
952.025101174828));
#143906=CARTESIAN_POINT('Ctrl Pts',(-4.96022910773078,17.4333970061901,
950.530983527769));
#143907=CARTESIAN_POINT('Ctrl Pts',(-3.31631129755346,17.7406985030951,
949.03686588071));
#143908=CARTESIAN_POINT('Ctrl Pts',(-1.67239348737615,18.048,947.542748233651));
#143909=CARTESIAN_POINT('Ctrl Pts',(-2.21024254310115E-15,18.048,946.048630586592));
#143910=CARTESIAN_POINT('Ctrl Pts',(-2.21024254310115E-15,18.048,1047.75));
#143911=CARTESIAN_POINT('Ctrl Pts',(1.67239348737616,18.048,1046.25588235294));
#143912=CARTESIAN_POINT('Ctrl Pts',(3.31631129755346,17.7406985030951,1044.76176470588));
#143913=CARTESIAN_POINT('Ctrl Pts',(4.96022910773077,17.4333970061901,1043.26764705882));
#143914=CARTESIAN_POINT('Ctrl Pts',(6.51968959134575,16.8292587962898,1041.77352941176));
#143915=CARTESIAN_POINT('Ctrl Pts',(8.07915007496071,16.2251205863895,1040.27941176471));
#143916=CARTESIAN_POINT('Ctrl Pts',(9.50104767561053,15.3447188656481,1038.78529411765));
#143917=CARTESIAN_POINT('Ctrl Pts',(10.9229452762603,14.4643171449067,1037.29117647059));
#143918=CARTESIAN_POINT('Ctrl Pts',(12.1588589765331,13.3376329379985,1035.79705882353));
#143919=CARTESIAN_POINT('Ctrl Pts',(13.3947726768058,12.2109487310903,1034.30294117647));
#143920=CARTESIAN_POINT('Ctrl Pts',(14.4026149179538,10.8763499173728,1032.80882352941));
#143921=CARTESIAN_POINT('Ctrl Pts',(15.4104571591017,9.54175110365539,1031.31470588235));
#143922=CARTESIAN_POINT('Ctrl Pts',(16.1559070823762,8.04468584505496,1029.82058823529));
#143923=CARTESIAN_POINT('Ctrl Pts',(16.9013570056506,6.54762058645456,1028.32647058824));
#143924=CARTESIAN_POINT('Ctrl Pts',(17.3590292079831,4.93906964482096,1026.83235294118));
#143925=CARTESIAN_POINT('Ctrl Pts',(17.8167014103155,3.33051870318735,1025.33823529412));
#143926=CARTESIAN_POINT('Ctrl Pts',(17.9710104137728,1.66525935159367,1023.84411764706));
#143927=CARTESIAN_POINT('Ctrl Pts',(18.1253194172301,3.32956716117513E-15,
1022.35));
#143928=CARTESIAN_POINT('Ctrl Pts',(17.9710104137728,-1.66525935159367,
1020.85588235294));
#143929=CARTESIAN_POINT('Ctrl Pts',(17.8167014103155,-3.33051870318736,
1019.36176470588));
#143930=CARTESIAN_POINT('Ctrl Pts',(17.3590292079831,-4.93906964482095,
1017.86764705882));
#143931=CARTESIAN_POINT('Ctrl Pts',(16.9013570056506,-6.54762058645456,
1016.37352941176));
#143932=CARTESIAN_POINT('Ctrl Pts',(16.1559070823762,-8.04468584505497,
1014.87941176471));
#143933=CARTESIAN_POINT('Ctrl Pts',(15.4104571591017,-9.54175110365538,
1013.38529411765));
#143934=CARTESIAN_POINT('Ctrl Pts',(14.4026149179538,-10.8763499173728,
1011.89117647059));
#143935=CARTESIAN_POINT('Ctrl Pts',(13.3947726768058,-12.2109487310903,
1010.39705882353));
#143936=CARTESIAN_POINT('Ctrl Pts',(12.1588589765331,-13.3376329379985,
1008.90294117647));
#143937=CARTESIAN_POINT('Ctrl Pts',(10.9229452762603,-14.4643171449067,
1007.40882352941));
#143938=CARTESIAN_POINT('Ctrl Pts',(9.50104767561053,-15.3447188656481,
1005.91470588235));
#143939=CARTESIAN_POINT('Ctrl Pts',(8.07915007496071,-16.2251205863895,
1004.42058823529));
#143940=CARTESIAN_POINT('Ctrl Pts',(6.51968959134574,-16.8292587962898,
1002.92647058824));
#143941=CARTESIAN_POINT('Ctrl Pts',(4.96022910773078,-17.4333970061901,
1001.43235294118));
#143942=CARTESIAN_POINT('Ctrl Pts',(3.31631129755346,-17.7406985030951,
999.938235294118));
#143943=CARTESIAN_POINT('Ctrl Pts',(1.67239348737615,-18.048,998.444117647059));
#143944=CARTESIAN_POINT('Ctrl Pts',(0.,-18.048,996.95));
#143945=CARTESIAN_POINT('Ctrl Pts',(-1.67239348737615,-18.048,995.455882352941));
#143946=CARTESIAN_POINT('Ctrl Pts',(-3.31631129755346,-17.7406985030951,
993.961764705882));
#143947=CARTESIAN_POINT('Ctrl Pts',(-4.96022910773077,-17.4333970061901,
992.467647058824));
#143948=CARTESIAN_POINT('Ctrl Pts',(-6.51968959134574,-16.8292587962898,
990.973529411765));
#143949=CARTESIAN_POINT('Ctrl Pts',(-8.07915007496071,-16.2251205863895,
989.479411764706));
#143950=CARTESIAN_POINT('Ctrl Pts',(-9.50104767561052,-15.3447188656481,
987.985294117647));
#143951=CARTESIAN_POINT('Ctrl Pts',(-10.9229452762603,-14.4643171449067,
986.491176470588));
#143952=CARTESIAN_POINT('Ctrl Pts',(-12.1588589765331,-13.3376329379985,
984.997058823529));
#143953=CARTESIAN_POINT('Ctrl Pts',(-13.3947726768058,-12.2109487310903,
983.502941176471));
#143954=CARTESIAN_POINT('Ctrl Pts',(-14.4026149179538,-10.8763499173728,
982.008823529412));
#143955=CARTESIAN_POINT('Ctrl Pts',(-15.4104571591017,-9.54175110365538,
980.514705882353));
#143956=CARTESIAN_POINT('Ctrl Pts',(-16.1559070823762,-8.04468584505497,
979.020588235294));
#143957=CARTESIAN_POINT('Ctrl Pts',(-16.9013570056506,-6.54762058645456,
977.526470588235));
#143958=CARTESIAN_POINT('Ctrl Pts',(-17.3590292079831,-4.93906964482095,
976.032352941177));
#143959=CARTESIAN_POINT('Ctrl Pts',(-17.8167014103155,-3.33051870318735,
974.538235294118));
#143960=CARTESIAN_POINT('Ctrl Pts',(-17.9710104137728,-1.66525935159368,
973.044117647059));
#143961=CARTESIAN_POINT('Ctrl Pts',(-18.1253194172301,-1.10985572039171E-15,
971.55));
#143962=CARTESIAN_POINT('Ctrl Pts',(-17.9710104137728,1.66525935159367,
970.055882352941));
#143963=CARTESIAN_POINT('Ctrl Pts',(-17.8167014103155,3.33051870318735,
968.561764705883));
#143964=CARTESIAN_POINT('Ctrl Pts',(-17.3590292079831,4.93906964482096,
967.067647058824));
#143965=CARTESIAN_POINT('Ctrl Pts',(-16.9013570056506,6.54762058645456,
965.573529411765));
#143966=CARTESIAN_POINT('Ctrl Pts',(-16.1559070823762,8.04468584505497,
964.079411764706));
#143967=CARTESIAN_POINT('Ctrl Pts',(-15.4104571591017,9.54175110365538,
962.585294117647));
#143968=CARTESIAN_POINT('Ctrl Pts',(-14.4026149179538,10.8763499173728,
961.091176470588));
#143969=CARTESIAN_POINT('Ctrl Pts',(-13.3947726768058,12.2109487310903,
959.59705882353));
#143970=CARTESIAN_POINT('Ctrl Pts',(-12.1588589765331,13.3376329379985,
958.102941176471));
#143971=CARTESIAN_POINT('Ctrl Pts',(-10.9229452762603,14.4643171449067,
956.608823529412));
#143972=CARTESIAN_POINT('Ctrl Pts',(-9.50104767561052,15.3447188656481,
955.114705882353));
#143973=CARTESIAN_POINT('Ctrl Pts',(-8.07915007496071,16.2251205863895,
953.620588235294));
#143974=CARTESIAN_POINT('Ctrl Pts',(-6.51968959134574,16.8292587962898,
952.126470588235));
#143975=CARTESIAN_POINT('Ctrl Pts',(-4.96022910773078,17.4333970061901,
950.632352941177));
#143976=CARTESIAN_POINT('Ctrl Pts',(-3.31631129755346,17.7406985030951,
949.138235294118));
#143977=CARTESIAN_POINT('Ctrl Pts',(-1.67239348737615,18.048,947.644117647059));
#143978=CARTESIAN_POINT('Ctrl Pts',(-2.21024254310115E-15,18.048,946.15));
#143979=CARTESIAN_POINT('Origin',(5.37704275891775E-14,4.44089209850063E-14,
1504.8993152933));
#143980=CARTESIAN_POINT('',(5.15601850460762E-14,18.048,844.448630586592));
#143981=CARTESIAN_POINT('',(5.15601850460762E-14,18.048,844.55));
#143982=CARTESIAN_POINT('',(1.05330612635254E-13,18.0480000000001,1504.8993152933));
#143983=CARTESIAN_POINT('Ctrl Pts',(-2.21024254310115E-15,18.048,946.048630586592));
#143984=CARTESIAN_POINT('Ctrl Pts',(1.67239348737616,18.048,944.554512939534));
#143985=CARTESIAN_POINT('Ctrl Pts',(3.31631129755346,17.7406985030951,943.060395292475));
#143986=CARTESIAN_POINT('Ctrl Pts',(4.96022910773077,17.4333970061901,941.566277645416));
#143987=CARTESIAN_POINT('Ctrl Pts',(6.51968959134575,16.8292587962898,940.072159998357));
#143988=CARTESIAN_POINT('Ctrl Pts',(8.07915007496071,16.2251205863895,938.578042351298));
#143989=CARTESIAN_POINT('Ctrl Pts',(9.50104767561053,15.3447188656481,937.083924704239));
#143990=CARTESIAN_POINT('Ctrl Pts',(10.9229452762603,14.4643171449067,935.589807057181));
#143991=CARTESIAN_POINT('Ctrl Pts',(12.1588589765331,13.3376329379985,934.095689410122));
#143992=CARTESIAN_POINT('Ctrl Pts',(13.3947726768058,12.2109487310903,932.601571763063));
#143993=CARTESIAN_POINT('Ctrl Pts',(14.4026149179538,10.8763499173728,931.107454116004));
#143994=CARTESIAN_POINT('Ctrl Pts',(15.4104571591017,9.54175110365539,929.613336468945));
#143995=CARTESIAN_POINT('Ctrl Pts',(16.1559070823762,8.04468584505496,928.119218821886));
#143996=CARTESIAN_POINT('Ctrl Pts',(16.9013570056506,6.54762058645456,926.625101174828));
#143997=CARTESIAN_POINT('Ctrl Pts',(17.3590292079831,4.93906964482096,925.130983527769));
#143998=CARTESIAN_POINT('Ctrl Pts',(17.8167014103155,3.33051870318735,923.63686588071));
#143999=CARTESIAN_POINT('Ctrl Pts',(17.9710104137728,1.66525935159367,922.142748233651));
#144000=CARTESIAN_POINT('Ctrl Pts',(18.1253194172301,3.32956716117513E-15,
920.648630586592));
#144001=CARTESIAN_POINT('Ctrl Pts',(17.9710104137728,-1.66525935159367,
919.154512939534));
#144002=CARTESIAN_POINT('Ctrl Pts',(17.8167014103155,-3.33051870318736,
917.660395292475));
#144003=CARTESIAN_POINT('Ctrl Pts',(17.3590292079831,-4.93906964482095,
916.166277645416));
#144004=CARTESIAN_POINT('Ctrl Pts',(16.9013570056506,-6.54762058645456,
914.672159998357));
#144005=CARTESIAN_POINT('Ctrl Pts',(16.1559070823762,-8.04468584505497,
913.178042351298));
#144006=CARTESIAN_POINT('Ctrl Pts',(15.4104571591017,-9.54175110365538,
911.683924704239));
#144007=CARTESIAN_POINT('Ctrl Pts',(14.4026149179538,-10.8763499173728,
910.18980705718));
#144008=CARTESIAN_POINT('Ctrl Pts',(13.3947726768058,-12.2109487310903,
908.695689410122));
#144009=CARTESIAN_POINT('Ctrl Pts',(12.1588589765331,-13.3376329379985,
907.201571763063));
#144010=CARTESIAN_POINT('Ctrl Pts',(10.9229452762603,-14.4643171449067,
905.707454116004));
#144011=CARTESIAN_POINT('Ctrl Pts',(9.50104767561053,-15.3447188656481,
904.213336468945));
#144012=CARTESIAN_POINT('Ctrl Pts',(8.07915007496071,-16.2251205863895,
902.719218821886));
#144013=CARTESIAN_POINT('Ctrl Pts',(6.51968959134574,-16.8292587962898,
901.225101174828));
#144014=CARTESIAN_POINT('Ctrl Pts',(4.96022910773078,-17.4333970061901,
899.730983527769));
#144015=CARTESIAN_POINT('Ctrl Pts',(3.31631129755346,-17.7406985030951,
898.23686588071));
#144016=CARTESIAN_POINT('Ctrl Pts',(1.67239348737615,-18.048,896.742748233651));
#144017=CARTESIAN_POINT('Ctrl Pts',(0.,-18.048,895.248630586592));
#144018=CARTESIAN_POINT('Ctrl Pts',(-1.67239348737615,-18.048,893.754512939534));
#144019=CARTESIAN_POINT('Ctrl Pts',(-3.31631129755346,-17.7406985030951,
892.260395292475));
#144020=CARTESIAN_POINT('Ctrl Pts',(-4.96022910773077,-17.4333970061901,
890.766277645416));
#144021=CARTESIAN_POINT('Ctrl Pts',(-6.51968959134574,-16.8292587962898,
889.272159998357));
#144022=CARTESIAN_POINT('Ctrl Pts',(-8.07915007496071,-16.2251205863895,
887.778042351298));
#144023=CARTESIAN_POINT('Ctrl Pts',(-9.50104767561052,-15.3447188656481,
886.283924704239));
#144024=CARTESIAN_POINT('Ctrl Pts',(-10.9229452762603,-14.4643171449067,
884.789807057181));
#144025=CARTESIAN_POINT('Ctrl Pts',(-12.1588589765331,-13.3376329379985,
883.295689410122));
#144026=CARTESIAN_POINT('Ctrl Pts',(-13.3947726768058,-12.2109487310903,
881.801571763063));
#144027=CARTESIAN_POINT('Ctrl Pts',(-14.4026149179538,-10.8763499173728,
880.307454116004));
#144028=CARTESIAN_POINT('Ctrl Pts',(-15.4104571591017,-9.54175110365538,
878.813336468945));
#144029=CARTESIAN_POINT('Ctrl Pts',(-16.1559070823762,-8.04468584505497,
877.319218821886));
#144030=CARTESIAN_POINT('Ctrl Pts',(-16.9013570056506,-6.54762058645456,
875.825101174828));
#144031=CARTESIAN_POINT('Ctrl Pts',(-17.3590292079831,-4.93906964482095,
874.330983527769));
#144032=CARTESIAN_POINT('Ctrl Pts',(-17.8167014103155,-3.33051870318735,
872.83686588071));
#144033=CARTESIAN_POINT('Ctrl Pts',(-17.9710104137728,-1.66525935159368,
871.342748233651));
#144034=CARTESIAN_POINT('Ctrl Pts',(-18.1253194172301,-1.10985572039171E-15,
869.848630586592));
#144035=CARTESIAN_POINT('Ctrl Pts',(-17.9710104137728,1.66525935159367,
868.354512939534));
#144036=CARTESIAN_POINT('Ctrl Pts',(-17.8167014103155,3.33051870318735,
866.860395292475));
#144037=CARTESIAN_POINT('Ctrl Pts',(-17.3590292079831,4.93906964482096,
865.366277645416));
#144038=CARTESIAN_POINT('Ctrl Pts',(-16.9013570056506,6.54762058645456,
863.872159998357));
#144039=CARTESIAN_POINT('Ctrl Pts',(-16.1559070823762,8.04468584505497,
862.378042351298));
#144040=CARTESIAN_POINT('Ctrl Pts',(-15.4104571591017,9.54175110365538,
860.883924704239));
#144041=CARTESIAN_POINT('Ctrl Pts',(-14.4026149179538,10.8763499173728,
859.389807057181));
#144042=CARTESIAN_POINT('Ctrl Pts',(-13.3947726768058,12.2109487310903,
857.895689410122));
#144043=CARTESIAN_POINT('Ctrl Pts',(-12.1588589765331,13.3376329379985,
856.401571763063));
#144044=CARTESIAN_POINT('Ctrl Pts',(-10.9229452762603,14.4643171449067,
854.907454116004));
#144045=CARTESIAN_POINT('Ctrl Pts',(-9.50104767561052,15.3447188656481,
853.413336468945));
#144046=CARTESIAN_POINT('Ctrl Pts',(-8.07915007496071,16.2251205863895,
851.919218821886));
#144047=CARTESIAN_POINT('Ctrl Pts',(-6.51968959134574,16.8292587962898,
850.425101174828));
#144048=CARTESIAN_POINT('Ctrl Pts',(-4.96022910773078,17.4333970061901,
848.930983527769));
#144049=CARTESIAN_POINT('Ctrl Pts',(-3.31631129755346,17.7406985030951,
847.43686588071));
#144050=CARTESIAN_POINT('Ctrl Pts',(-1.67239348737615,18.048,845.942748233651));
#144051=CARTESIAN_POINT('Ctrl Pts',(-2.21024254310115E-15,18.048,844.448630586592));
#144052=CARTESIAN_POINT('Ctrl Pts',(-2.21024254310115E-15,18.048,946.15));
#144053=CARTESIAN_POINT('Ctrl Pts',(1.67239348737616,18.048,944.655882352941));
#144054=CARTESIAN_POINT('Ctrl Pts',(3.31631129755346,17.7406985030951,943.161764705882));
#144055=CARTESIAN_POINT('Ctrl Pts',(4.96022910773077,17.4333970061901,941.667647058824));
#144056=CARTESIAN_POINT('Ctrl Pts',(6.51968959134575,16.8292587962898,940.173529411765));
#144057=CARTESIAN_POINT('Ctrl Pts',(8.07915007496071,16.2251205863895,938.679411764706));
#144058=CARTESIAN_POINT('Ctrl Pts',(9.50104767561053,15.3447188656481,937.185294117647));
#144059=CARTESIAN_POINT('Ctrl Pts',(10.9229452762603,14.4643171449067,935.691176470589));
#144060=CARTESIAN_POINT('Ctrl Pts',(12.1588589765331,13.3376329379985,934.19705882353));
#144061=CARTESIAN_POINT('Ctrl Pts',(13.3947726768058,12.2109487310903,932.702941176471));
#144062=CARTESIAN_POINT('Ctrl Pts',(14.4026149179538,10.8763499173728,931.208823529412));
#144063=CARTESIAN_POINT('Ctrl Pts',(15.4104571591017,9.54175110365539,929.714705882353));
#144064=CARTESIAN_POINT('Ctrl Pts',(16.1559070823762,8.04468584505496,928.220588235294));
#144065=CARTESIAN_POINT('Ctrl Pts',(16.9013570056506,6.54762058645456,926.726470588235));
#144066=CARTESIAN_POINT('Ctrl Pts',(17.3590292079831,4.93906964482096,925.232352941176));
#144067=CARTESIAN_POINT('Ctrl Pts',(17.8167014103155,3.33051870318735,923.738235294118));
#144068=CARTESIAN_POINT('Ctrl Pts',(17.9710104137728,1.66525935159367,922.244117647059));
#144069=CARTESIAN_POINT('Ctrl Pts',(18.1253194172301,3.32956716117513E-15,
920.75));
#144070=CARTESIAN_POINT('Ctrl Pts',(17.9710104137728,-1.66525935159367,
919.255882352941));
#144071=CARTESIAN_POINT('Ctrl Pts',(17.8167014103155,-3.33051870318736,
917.761764705882));
#144072=CARTESIAN_POINT('Ctrl Pts',(17.3590292079831,-4.93906964482095,
916.267647058824));
#144073=CARTESIAN_POINT('Ctrl Pts',(16.9013570056506,-6.54762058645456,
914.773529411765));
#144074=CARTESIAN_POINT('Ctrl Pts',(16.1559070823762,-8.04468584505497,
913.279411764706));
#144075=CARTESIAN_POINT('Ctrl Pts',(15.4104571591017,-9.54175110365538,
911.785294117647));
#144076=CARTESIAN_POINT('Ctrl Pts',(14.4026149179538,-10.8763499173728,
910.291176470588));
#144077=CARTESIAN_POINT('Ctrl Pts',(13.3947726768058,-12.2109487310903,
908.79705882353));
#144078=CARTESIAN_POINT('Ctrl Pts',(12.1588589765331,-13.3376329379985,
907.302941176471));
#144079=CARTESIAN_POINT('Ctrl Pts',(10.9229452762603,-14.4643171449067,
905.808823529412));
#144080=CARTESIAN_POINT('Ctrl Pts',(9.50104767561053,-15.3447188656481,
904.314705882353));
#144081=CARTESIAN_POINT('Ctrl Pts',(8.07915007496071,-16.2251205863895,
902.820588235294));
#144082=CARTESIAN_POINT('Ctrl Pts',(6.51968959134574,-16.8292587962898,
901.326470588235));
#144083=CARTESIAN_POINT('Ctrl Pts',(4.96022910773078,-17.4333970061901,
899.832352941177));
#144084=CARTESIAN_POINT('Ctrl Pts',(3.31631129755346,-17.7406985030951,
898.338235294118));
#144085=CARTESIAN_POINT('Ctrl Pts',(1.67239348737615,-18.048,896.844117647059));
#144086=CARTESIAN_POINT('Ctrl Pts',(0.,-18.048,895.35));
#144087=CARTESIAN_POINT('Ctrl Pts',(-1.67239348737615,-18.048,893.855882352941));
#144088=CARTESIAN_POINT('Ctrl Pts',(-3.31631129755346,-17.7406985030951,
892.361764705882));
#144089=CARTESIAN_POINT('Ctrl Pts',(-4.96022910773077,-17.4333970061901,
890.867647058824));
#144090=CARTESIAN_POINT('Ctrl Pts',(-6.51968959134574,-16.8292587962898,
889.373529411765));
#144091=CARTESIAN_POINT('Ctrl Pts',(-8.07915007496071,-16.2251205863895,
887.879411764706));
#144092=CARTESIAN_POINT('Ctrl Pts',(-9.50104767561052,-15.3447188656481,
886.385294117647));
#144093=CARTESIAN_POINT('Ctrl Pts',(-10.9229452762603,-14.4643171449067,
884.891176470588));
#144094=CARTESIAN_POINT('Ctrl Pts',(-12.1588589765331,-13.3376329379985,
883.39705882353));
#144095=CARTESIAN_POINT('Ctrl Pts',(-13.3947726768058,-12.2109487310903,
881.902941176471));
#144096=CARTESIAN_POINT('Ctrl Pts',(-14.4026149179538,-10.8763499173728,
880.408823529412));
#144097=CARTESIAN_POINT('Ctrl Pts',(-15.4104571591017,-9.54175110365538,
878.914705882353));
#144098=CARTESIAN_POINT('Ctrl Pts',(-16.1559070823762,-8.04468584505497,
877.420588235294));
#144099=CARTESIAN_POINT('Ctrl Pts',(-16.9013570056506,-6.54762058645456,
875.926470588235));
#144100=CARTESIAN_POINT('Ctrl Pts',(-17.3590292079831,-4.93906964482095,
874.432352941177));
#144101=CARTESIAN_POINT('Ctrl Pts',(-17.8167014103155,-3.33051870318735,
872.938235294118));
#144102=CARTESIAN_POINT('Ctrl Pts',(-17.9710104137728,-1.66525935159368,
871.444117647059));
#144103=CARTESIAN_POINT('Ctrl Pts',(-18.1253194172301,-1.10985572039171E-15,
869.95));
#144104=CARTESIAN_POINT('Ctrl Pts',(-17.9710104137728,1.66525935159367,
868.455882352941));
#144105=CARTESIAN_POINT('Ctrl Pts',(-17.8167014103155,3.33051870318735,
866.961764705882));
#144106=CARTESIAN_POINT('Ctrl Pts',(-17.3590292079831,4.93906964482096,
865.467647058824));
#144107=CARTESIAN_POINT('Ctrl Pts',(-16.9013570056506,6.54762058645456,
863.973529411765));
#144108=CARTESIAN_POINT('Ctrl Pts',(-16.1559070823762,8.04468584505497,
862.479411764706));
#144109=CARTESIAN_POINT('Ctrl Pts',(-15.4104571591017,9.54175110365538,
860.985294117647));
#144110=CARTESIAN_POINT('Ctrl Pts',(-14.4026149179538,10.8763499173728,
859.491176470588));
#144111=CARTESIAN_POINT('Ctrl Pts',(-13.3947726768058,12.2109487310903,
857.99705882353));
#144112=CARTESIAN_POINT('Ctrl Pts',(-12.1588589765331,13.3376329379985,
856.502941176471));
#144113=CARTESIAN_POINT('Ctrl Pts',(-10.9229452762603,14.4643171449067,
855.008823529412));
#144114=CARTESIAN_POINT('Ctrl Pts',(-9.50104767561052,15.3447188656481,
853.514705882353));
#144115=CARTESIAN_POINT('Ctrl Pts',(-8.07915007496071,16.2251205863895,
852.020588235294));
#144116=CARTESIAN_POINT('Ctrl Pts',(-6.51968959134574,16.8292587962898,
850.526470588235));
#144117=CARTESIAN_POINT('Ctrl Pts',(-4.96022910773078,17.4333970061901,
849.032352941177));
#144118=CARTESIAN_POINT('Ctrl Pts',(-3.31631129755346,17.7406985030951,
847.538235294118));
#144119=CARTESIAN_POINT('Ctrl Pts',(-1.67239348737615,18.048,846.044117647059));
#144120=CARTESIAN_POINT('Ctrl Pts',(-2.21024254310115E-15,18.048,844.55));
#144121=CARTESIAN_POINT('Origin',(5.37704275891775E-14,4.44089209850063E-14,
1504.8993152933));
#144122=CARTESIAN_POINT('',(5.15601850460762E-14,18.048,742.848630586592));
#144123=CARTESIAN_POINT('',(5.15601850460762E-14,18.048,742.95));
#144124=CARTESIAN_POINT('',(1.05330612635254E-13,18.0480000000001,1504.8993152933));
#144125=CARTESIAN_POINT('Ctrl Pts',(-2.21024254310115E-15,18.048,844.448630586592));
#144126=CARTESIAN_POINT('Ctrl Pts',(1.67239348737616,18.048,842.954512939534));
#144127=CARTESIAN_POINT('Ctrl Pts',(3.31631129755346,17.7406985030951,841.460395292475));
#144128=CARTESIAN_POINT('Ctrl Pts',(4.96022910773077,17.4333970061901,839.966277645416));
#144129=CARTESIAN_POINT('Ctrl Pts',(6.51968959134575,16.8292587962898,838.472159998357));
#144130=CARTESIAN_POINT('Ctrl Pts',(8.07915007496071,16.2251205863895,836.978042351298));
#144131=CARTESIAN_POINT('Ctrl Pts',(9.50104767561053,15.3447188656481,835.483924704239));
#144132=CARTESIAN_POINT('Ctrl Pts',(10.9229452762603,14.4643171449067,833.989807057181));
#144133=CARTESIAN_POINT('Ctrl Pts',(12.1588589765331,13.3376329379985,832.495689410122));
#144134=CARTESIAN_POINT('Ctrl Pts',(13.3947726768058,12.2109487310903,831.001571763063));
#144135=CARTESIAN_POINT('Ctrl Pts',(14.4026149179538,10.8763499173728,829.507454116004));
#144136=CARTESIAN_POINT('Ctrl Pts',(15.4104571591017,9.54175110365539,828.013336468945));
#144137=CARTESIAN_POINT('Ctrl Pts',(16.1559070823762,8.04468584505496,826.519218821886));
#144138=CARTESIAN_POINT('Ctrl Pts',(16.9013570056506,6.54762058645456,825.025101174828));
#144139=CARTESIAN_POINT('Ctrl Pts',(17.3590292079831,4.93906964482096,823.530983527769));
#144140=CARTESIAN_POINT('Ctrl Pts',(17.8167014103155,3.33051870318735,822.03686588071));
#144141=CARTESIAN_POINT('Ctrl Pts',(17.9710104137728,1.66525935159367,820.542748233651));
#144142=CARTESIAN_POINT('Ctrl Pts',(18.1253194172301,3.32956716117513E-15,
819.048630586592));
#144143=CARTESIAN_POINT('Ctrl Pts',(17.9710104137728,-1.66525935159367,
817.554512939533));
#144144=CARTESIAN_POINT('Ctrl Pts',(17.8167014103155,-3.33051870318736,
816.060395292475));
#144145=CARTESIAN_POINT('Ctrl Pts',(17.3590292079831,-4.93906964482095,
814.566277645416));
#144146=CARTESIAN_POINT('Ctrl Pts',(16.9013570056506,-6.54762058645456,
813.072159998357));
#144147=CARTESIAN_POINT('Ctrl Pts',(16.1559070823762,-8.04468584505497,
811.578042351298));
#144148=CARTESIAN_POINT('Ctrl Pts',(15.4104571591017,-9.54175110365538,
810.083924704239));
#144149=CARTESIAN_POINT('Ctrl Pts',(14.4026149179538,-10.8763499173728,
808.589807057181));
#144150=CARTESIAN_POINT('Ctrl Pts',(13.3947726768058,-12.2109487310903,
807.095689410122));
#144151=CARTESIAN_POINT('Ctrl Pts',(12.1588589765331,-13.3376329379985,
805.601571763063));
#144152=CARTESIAN_POINT('Ctrl Pts',(10.9229452762603,-14.4643171449067,
804.107454116004));
#144153=CARTESIAN_POINT('Ctrl Pts',(9.50104767561053,-15.3447188656481,
802.613336468945));
#144154=CARTESIAN_POINT('Ctrl Pts',(8.07915007496071,-16.2251205863895,
801.119218821887));
#144155=CARTESIAN_POINT('Ctrl Pts',(6.51968959134574,-16.8292587962898,
799.625101174828));
#144156=CARTESIAN_POINT('Ctrl Pts',(4.96022910773078,-17.4333970061901,
798.130983527769));
#144157=CARTESIAN_POINT('Ctrl Pts',(3.31631129755346,-17.7406985030951,
796.63686588071));
#144158=CARTESIAN_POINT('Ctrl Pts',(1.67239348737615,-18.048,795.142748233651));
#144159=CARTESIAN_POINT('Ctrl Pts',(0.,-18.048,793.648630586592));
#144160=CARTESIAN_POINT('Ctrl Pts',(-1.67239348737615,-18.048,792.154512939534));
#144161=CARTESIAN_POINT('Ctrl Pts',(-3.31631129755346,-17.7406985030951,
790.660395292475));
#144162=CARTESIAN_POINT('Ctrl Pts',(-4.96022910773077,-17.4333970061901,
789.166277645416));
#144163=CARTESIAN_POINT('Ctrl Pts',(-6.51968959134574,-16.8292587962898,
787.672159998357));
#144164=CARTESIAN_POINT('Ctrl Pts',(-8.07915007496071,-16.2251205863895,
786.178042351298));
#144165=CARTESIAN_POINT('Ctrl Pts',(-9.50104767561052,-15.3447188656481,
784.683924704239));
#144166=CARTESIAN_POINT('Ctrl Pts',(-10.9229452762603,-14.4643171449067,
783.189807057181));
#144167=CARTESIAN_POINT('Ctrl Pts',(-12.1588589765331,-13.3376329379985,
781.695689410122));
#144168=CARTESIAN_POINT('Ctrl Pts',(-13.3947726768058,-12.2109487310903,
780.201571763063));
#144169=CARTESIAN_POINT('Ctrl Pts',(-14.4026149179538,-10.8763499173728,
778.707454116004));
#144170=CARTESIAN_POINT('Ctrl Pts',(-15.4104571591017,-9.54175110365538,
777.213336468945));
#144171=CARTESIAN_POINT('Ctrl Pts',(-16.1559070823762,-8.04468584505497,
775.719218821886));
#144172=CARTESIAN_POINT('Ctrl Pts',(-16.9013570056506,-6.54762058645456,
774.225101174828));
#144173=CARTESIAN_POINT('Ctrl Pts',(-17.3590292079831,-4.93906964482095,
772.730983527769));
#144174=CARTESIAN_POINT('Ctrl Pts',(-17.8167014103155,-3.33051870318735,
771.23686588071));
#144175=CARTESIAN_POINT('Ctrl Pts',(-17.9710104137728,-1.66525935159368,
769.742748233651));
#144176=CARTESIAN_POINT('Ctrl Pts',(-18.1253194172301,-1.10985572039171E-15,
768.248630586592));
#144177=CARTESIAN_POINT('Ctrl Pts',(-17.9710104137728,1.66525935159367,
766.754512939533));
#144178=CARTESIAN_POINT('Ctrl Pts',(-17.8167014103155,3.33051870318735,
765.260395292475));
#144179=CARTESIAN_POINT('Ctrl Pts',(-17.3590292079831,4.93906964482096,
763.766277645416));
#144180=CARTESIAN_POINT('Ctrl Pts',(-16.9013570056506,6.54762058645456,
762.272159998357));
#144181=CARTESIAN_POINT('Ctrl Pts',(-16.1559070823762,8.04468584505497,
760.778042351298));
#144182=CARTESIAN_POINT('Ctrl Pts',(-15.4104571591017,9.54175110365538,
759.283924704239));
#144183=CARTESIAN_POINT('Ctrl Pts',(-14.4026149179538,10.8763499173728,
757.78980705718));
#144184=CARTESIAN_POINT('Ctrl Pts',(-13.3947726768058,12.2109487310903,
756.295689410122));
#144185=CARTESIAN_POINT('Ctrl Pts',(-12.1588589765331,13.3376329379985,
754.801571763063));
#144186=CARTESIAN_POINT('Ctrl Pts',(-10.9229452762603,14.4643171449067,
753.307454116004));
#144187=CARTESIAN_POINT('Ctrl Pts',(-9.50104767561052,15.3447188656481,
751.813336468945));
#144188=CARTESIAN_POINT('Ctrl Pts',(-8.07915007496071,16.2251205863895,
750.319218821886));
#144189=CARTESIAN_POINT('Ctrl Pts',(-6.51968959134574,16.8292587962898,
748.825101174828));
#144190=CARTESIAN_POINT('Ctrl Pts',(-4.96022910773078,17.4333970061901,
747.330983527769));
#144191=CARTESIAN_POINT('Ctrl Pts',(-3.31631129755346,17.7406985030951,
745.83686588071));
#144192=CARTESIAN_POINT('Ctrl Pts',(-1.67239348737615,18.048,744.342748233651));
#144193=CARTESIAN_POINT('Ctrl Pts',(-2.21024254310115E-15,18.048,742.848630586592));
#144194=CARTESIAN_POINT('Ctrl Pts',(-2.21024254310115E-15,18.048,844.55));
#144195=CARTESIAN_POINT('Ctrl Pts',(1.67239348737616,18.048,843.055882352941));
#144196=CARTESIAN_POINT('Ctrl Pts',(3.31631129755346,17.7406985030951,841.561764705883));
#144197=CARTESIAN_POINT('Ctrl Pts',(4.96022910773077,17.4333970061901,840.067647058824));
#144198=CARTESIAN_POINT('Ctrl Pts',(6.51968959134575,16.8292587962898,838.573529411765));
#144199=CARTESIAN_POINT('Ctrl Pts',(8.07915007496071,16.2251205863895,837.079411764706));
#144200=CARTESIAN_POINT('Ctrl Pts',(9.50104767561053,15.3447188656481,835.585294117647));
#144201=CARTESIAN_POINT('Ctrl Pts',(10.9229452762603,14.4643171449067,834.091176470588));
#144202=CARTESIAN_POINT('Ctrl Pts',(12.1588589765331,13.3376329379985,832.597058823529));
#144203=CARTESIAN_POINT('Ctrl Pts',(13.3947726768058,12.2109487310903,831.102941176471));
#144204=CARTESIAN_POINT('Ctrl Pts',(14.4026149179538,10.8763499173728,829.608823529412));
#144205=CARTESIAN_POINT('Ctrl Pts',(15.4104571591017,9.54175110365539,828.114705882353));
#144206=CARTESIAN_POINT('Ctrl Pts',(16.1559070823762,8.04468584505496,826.620588235294));
#144207=CARTESIAN_POINT('Ctrl Pts',(16.9013570056506,6.54762058645456,825.126470588235));
#144208=CARTESIAN_POINT('Ctrl Pts',(17.3590292079831,4.93906964482096,823.632352941177));
#144209=CARTESIAN_POINT('Ctrl Pts',(17.8167014103155,3.33051870318735,822.138235294118));
#144210=CARTESIAN_POINT('Ctrl Pts',(17.9710104137728,1.66525935159367,820.644117647059));
#144211=CARTESIAN_POINT('Ctrl Pts',(18.1253194172301,3.32956716117513E-15,
819.15));
#144212=CARTESIAN_POINT('Ctrl Pts',(17.9710104137728,-1.66525935159367,
817.655882352941));
#144213=CARTESIAN_POINT('Ctrl Pts',(17.8167014103155,-3.33051870318736,
816.161764705882));
#144214=CARTESIAN_POINT('Ctrl Pts',(17.3590292079831,-4.93906964482095,
814.667647058824));
#144215=CARTESIAN_POINT('Ctrl Pts',(16.9013570056506,-6.54762058645456,
813.173529411765));
#144216=CARTESIAN_POINT('Ctrl Pts',(16.1559070823762,-8.04468584505497,
811.679411764706));
#144217=CARTESIAN_POINT('Ctrl Pts',(15.4104571591017,-9.54175110365538,
810.185294117647));
#144218=CARTESIAN_POINT('Ctrl Pts',(14.4026149179538,-10.8763499173728,
808.691176470588));
#144219=CARTESIAN_POINT('Ctrl Pts',(13.3947726768058,-12.2109487310903,
807.19705882353));
#144220=CARTESIAN_POINT('Ctrl Pts',(12.1588589765331,-13.3376329379985,
805.702941176471));
#144221=CARTESIAN_POINT('Ctrl Pts',(10.9229452762603,-14.4643171449067,
804.208823529412));
#144222=CARTESIAN_POINT('Ctrl Pts',(9.50104767561053,-15.3447188656481,
802.714705882353));
#144223=CARTESIAN_POINT('Ctrl Pts',(8.07915007496071,-16.2251205863895,
801.220588235294));
#144224=CARTESIAN_POINT('Ctrl Pts',(6.51968959134574,-16.8292587962898,
799.726470588235));
#144225=CARTESIAN_POINT('Ctrl Pts',(4.96022910773078,-17.4333970061901,
798.232352941177));
#144226=CARTESIAN_POINT('Ctrl Pts',(3.31631129755346,-17.7406985030951,
796.738235294118));
#144227=CARTESIAN_POINT('Ctrl Pts',(1.67239348737615,-18.048,795.244117647059));
#144228=CARTESIAN_POINT('Ctrl Pts',(0.,-18.048,793.75));
#144229=CARTESIAN_POINT('Ctrl Pts',(-1.67239348737615,-18.048,792.255882352941));
#144230=CARTESIAN_POINT('Ctrl Pts',(-3.31631129755346,-17.7406985030951,
790.761764705882));
#144231=CARTESIAN_POINT('Ctrl Pts',(-4.96022910773077,-17.4333970061901,
789.267647058824));
#144232=CARTESIAN_POINT('Ctrl Pts',(-6.51968959134574,-16.8292587962898,
787.773529411765));
#144233=CARTESIAN_POINT('Ctrl Pts',(-8.07915007496071,-16.2251205863895,
786.279411764706));
#144234=CARTESIAN_POINT('Ctrl Pts',(-9.50104767561052,-15.3447188656481,
784.785294117647));
#144235=CARTESIAN_POINT('Ctrl Pts',(-10.9229452762603,-14.4643171449067,
783.291176470588));
#144236=CARTESIAN_POINT('Ctrl Pts',(-12.1588589765331,-13.3376329379985,
781.797058823529));
#144237=CARTESIAN_POINT('Ctrl Pts',(-13.3947726768058,-12.2109487310903,
780.302941176471));
#144238=CARTESIAN_POINT('Ctrl Pts',(-14.4026149179538,-10.8763499173728,
778.808823529412));
#144239=CARTESIAN_POINT('Ctrl Pts',(-15.4104571591017,-9.54175110365538,
777.314705882353));
#144240=CARTESIAN_POINT('Ctrl Pts',(-16.1559070823762,-8.04468584505497,
775.820588235294));
#144241=CARTESIAN_POINT('Ctrl Pts',(-16.9013570056506,-6.54762058645456,
774.326470588235));
#144242=CARTESIAN_POINT('Ctrl Pts',(-17.3590292079831,-4.93906964482095,
772.832352941177));
#144243=CARTESIAN_POINT('Ctrl Pts',(-17.8167014103155,-3.33051870318735,
771.338235294118));
#144244=CARTESIAN_POINT('Ctrl Pts',(-17.9710104137728,-1.66525935159368,
769.844117647059));
#144245=CARTESIAN_POINT('Ctrl Pts',(-18.1253194172301,-1.10985572039171E-15,
768.35));
#144246=CARTESIAN_POINT('Ctrl Pts',(-17.9710104137728,1.66525935159367,
766.855882352941));
#144247=CARTESIAN_POINT('Ctrl Pts',(-17.8167014103155,3.33051870318735,
765.361764705882));
#144248=CARTESIAN_POINT('Ctrl Pts',(-17.3590292079831,4.93906964482096,
763.867647058824));
#144249=CARTESIAN_POINT('Ctrl Pts',(-16.9013570056506,6.54762058645456,
762.373529411765));
#144250=CARTESIAN_POINT('Ctrl Pts',(-16.1559070823762,8.04468584505497,
760.879411764706));
#144251=CARTESIAN_POINT('Ctrl Pts',(-15.4104571591017,9.54175110365538,
759.385294117647));
#144252=CARTESIAN_POINT('Ctrl Pts',(-14.4026149179538,10.8763499173728,
757.891176470588));
#144253=CARTESIAN_POINT('Ctrl Pts',(-13.3947726768058,12.2109487310903,
756.39705882353));
#144254=CARTESIAN_POINT('Ctrl Pts',(-12.1588589765331,13.3376329379985,
754.902941176471));
#144255=CARTESIAN_POINT('Ctrl Pts',(-10.9229452762603,14.4643171449067,
753.408823529412));
#144256=CARTESIAN_POINT('Ctrl Pts',(-9.50104767561052,15.3447188656481,
751.914705882353));
#144257=CARTESIAN_POINT('Ctrl Pts',(-8.07915007496071,16.2251205863895,
750.420588235294));
#144258=CARTESIAN_POINT('Ctrl Pts',(-6.51968959134574,16.8292587962898,
748.926470588235));
#144259=CARTESIAN_POINT('Ctrl Pts',(-4.96022910773078,17.4333970061901,
747.432352941177));
#144260=CARTESIAN_POINT('Ctrl Pts',(-3.31631129755346,17.7406985030951,
745.938235294118));
#144261=CARTESIAN_POINT('Ctrl Pts',(-1.67239348737615,18.048,744.444117647059));
#144262=CARTESIAN_POINT('Ctrl Pts',(-2.21024254310115E-15,18.048,742.95));
#144263=CARTESIAN_POINT('Origin',(0.,0.,0.));
#144264=CARTESIAN_POINT('',(2.57009189155355E-10,-15.0000000000002,1403.35000000055));
#144265=CARTESIAN_POINT('',(1.83781454274905E-15,-15.0000000000002,1436.290625));
#144266=CARTESIAN_POINT('',(-1.83697019872103E-15,-15.,-1.82952505755738E-15));
#144267=CARTESIAN_POINT('',(0.,-15.0000000000001,1504.95));
#144268=CARTESIAN_POINT('Ctrl Pts',(5.13986631034413E-10,-15.0000000000002,
1403.35000000055));
#144269=CARTESIAN_POINT('Ctrl Pts',(2.07827945901844,-14.9999999999289,
1405.58402534592));
#144270=CARTESIAN_POINT('Ctrl Pts',(4.13908692185227,-14.5684603429543,
1407.81020920318));
#144271=CARTESIAN_POINT('Ctrl Pts',(8.68689829398006,-12.5629931687572,
1413.17009322386));
#144272=CARTESIAN_POINT('Ctrl Pts',(10.9344652135011,-10.6646060820942,
1416.21094592123));
#144273=CARTESIAN_POINT('Ctrl Pts',(14.1072706803958,-5.85542612428411,
1422.42816851589));
#144274=CARTESIAN_POINT('Ctrl Pts',(14.9683604747762,-3.04195026298039,
1425.46607790158));
#144275=CARTESIAN_POINT('Ctrl Pts',(15.029933794911,2.72204213970847,1431.68856689381));
#144276=CARTESIAN_POINT('Ctrl Pts',(14.2291832910922,5.55329976428186,1434.72524170703));
#144277=CARTESIAN_POINT('Ctrl Pts',(11.1573566374657,10.4318055046907,1440.94870782112));
#144278=CARTESIAN_POINT('Ctrl Pts',(8.94969556395685,12.3777406823635,1443.98680513831));
#144279=CARTESIAN_POINT('Ctrl Pts',(3.72577049390288,14.8129297813082,1450.20684436425));
#144280=CARTESIAN_POINT('Ctrl Pts',(0.815546969962605,15.2523333509076,
1453.24820170673));
#144281=CARTESIAN_POINT('Ctrl Pts',(-4.89155833830842,14.4694790480348,
1459.46097488352));
#144282=CARTESIAN_POINT('Ctrl Pts',(-7.57588543252332,13.2625961079929,
1462.50715168045));
#144283=CARTESIAN_POINT('Ctrl Pts',(-11.9461394121487,9.51657316639935,
1468.70916033785));
#144284=CARTESIAN_POINT('Ctrl Pts',(-13.5495708516033,7.04921298326686,
1471.76148533607));
#144285=CARTESIAN_POINT('Ctrl Pts',(-15.1953740827798,1.53729692049363,
1477.95185674073));
#144286=CARTESIAN_POINT('Ctrl Pts',(-15.2079313081015,-1.40536021411593,
1481.01043271643));
#144287=CARTESIAN_POINT('Ctrl Pts',(-13.6115405479348,-6.92758911761814,
1487.19191578933));
#144288=CARTESIAN_POINT('Ctrl Pts',(-12.0318291094507,-9.40666760558364,
1490.2455169837));
#144289=CARTESIAN_POINT('Ctrl Pts',(-8.51254032736959,-12.4811631175375,
1495.2775465698));
#144290=CARTESIAN_POINT('Ctrl Pts',(-6.95318389069969,-13.4120759382215,
1497.21026935134));
#144291=CARTESIAN_POINT('Ctrl Pts',(-3.58613197332224,-14.6756940642514,
1501.07970655087));
#144292=CARTESIAN_POINT('Ctrl Pts',(-1.79915829322707,-15.0000000000001,
1503.01601310958));
#144293=CARTESIAN_POINT('Ctrl Pts',(-4.413136522885E-14,-15.0000000000002,
1504.95));
#144294=CARTESIAN_POINT('Origin',(0.,-1.83556249024732E-13,1504.95));
#144295=CARTESIAN_POINT('',(0.,-15.,1500.1875));
#144296=CARTESIAN_POINT('',(0.,-15.,1500.1875));
#144297=CARTESIAN_POINT('',(-6.31841207935097E-16,-15.0000000000002,1446.609375));
#144298=CARTESIAN_POINT('',(-1.83697019872103E-15,-15.,-1.82952505755738E-15));
#144299=CARTESIAN_POINT('Ctrl Pts',(1.31838984174237E-15,-15.0000000000002,
1436.290625));
#144300=CARTESIAN_POINT('Ctrl Pts',(0.65346443120896,-15.0000000000002,
1436.290625));
#144301=CARTESIAN_POINT('Ctrl Pts',(1.34693085135696,-14.9531257199513,
1436.42230514128));
#144302=CARTESIAN_POINT('Ctrl Pts',(2.61662608066102,-14.7838918918852,
1436.95053274143));
#144303=CARTESIAN_POINT('Ctrl Pts',(3.19325594296631,-14.6636670624435,
1437.3467978446));
#144304=CARTESIAN_POINT('Ctrl Pts',(4.10344327628912,-14.4354425556451,
1438.25698517792));
#144305=CARTESIAN_POINT('Ctrl Pts',(4.49952313800711,-14.3119470704814,
1438.8335196808));
#144306=CARTESIAN_POINT('Ctrl Pts',(5.02761209168826,-14.1350860668278,
1440.10285875835));
#144307=CARTESIAN_POINT('Ctrl Pts',(5.15937500000008,-14.0847736797358,
1440.79618925399));
#144308=CARTESIAN_POINT('Ctrl Pts',(5.15937500000008,-14.0847736797358,
1442.10381074602));
#144309=CARTESIAN_POINT('Ctrl Pts',(5.02761209168842,-14.1350860668278,
1442.79714124165));
#144310=CARTESIAN_POINT('Ctrl Pts',(4.49952313800732,-14.3119470704813,
1444.0664803192));
#144311=CARTESIAN_POINT('Ctrl Pts',(4.10344327628912,-14.4354425556451,
1444.64301482208));
#144312=CARTESIAN_POINT('Ctrl Pts',(3.19325594296631,-14.6636670624435,
1445.5532021554));
#144313=CARTESIAN_POINT('Ctrl Pts',(2.61662608066126,-14.7838918918852,
1445.94946725857));
#144314=CARTESIAN_POINT('Ctrl Pts',(1.34693085135724,-14.9531257199512,
1446.47769485872));
#144315=CARTESIAN_POINT('Ctrl Pts',(0.653464431208942,-15.0000000000002,
1446.609375));
#144316=CARTESIAN_POINT('Ctrl Pts',(-1.69309011255336E-14,-15.0000000000002,
1446.609375));
#144317=CARTESIAN_POINT('',(14.0847736797357,5.15937499999978,1492.25));
#144318=CARTESIAN_POINT('',(14.0847736797356,-5.15937500000027,1492.25));
#144319=CARTESIAN_POINT('Ctrl Pts',(14.0847736797357,5.15937499999978,1492.25));
#144320=CARTESIAN_POINT('Ctrl Pts',(14.0847736797357,5.15937499999977,1492.90381074601));
#144321=CARTESIAN_POINT('Ctrl Pts',(14.1350860668277,5.02761209168797,1493.59714124165));
#144322=CARTESIAN_POINT('Ctrl Pts',(14.3119470704813,4.49952313800681,1494.8664803192));
#144323=CARTESIAN_POINT('Ctrl Pts',(14.4354425556449,4.10344327628884,1495.44301482208));
#144324=CARTESIAN_POINT('Ctrl Pts',(14.6636670624433,3.19325594296603,1496.3532021554));
#144325=CARTESIAN_POINT('Ctrl Pts',(14.7838918918851,2.61662608066068,1496.74946725857));
#144326=CARTESIAN_POINT('Ctrl Pts',(14.9531257199511,1.34693085135664,1497.27769485872));
#144327=CARTESIAN_POINT('Ctrl Pts',(15.,0.653464431208711,1497.409375));
#144328=CARTESIAN_POINT('Ctrl Pts',(15.,-0.653464431209192,1497.409375));
#144329=CARTESIAN_POINT('Ctrl Pts',(14.9531257199511,-1.34693085135711,
1497.27769485872));
#144330=CARTESIAN_POINT('Ctrl Pts',(14.783891891885,-2.61662608066116,1496.74946725857));
#144331=CARTESIAN_POINT('Ctrl Pts',(14.6636670624433,-3.1932559429665,1496.3532021554));
#144332=CARTESIAN_POINT('Ctrl Pts',(14.4354425556449,-4.10344327628932,
1495.44301482208));
#144333=CARTESIAN_POINT('Ctrl Pts',(14.3119470704812,-4.49952313800728,
1494.8664803192));
#144334=CARTESIAN_POINT('Ctrl Pts',(14.1350860668277,-5.02761209168844,
1493.59714124165));
#144335=CARTESIAN_POINT('Ctrl Pts',(14.0847736797356,-5.15937500000027,
1492.90381074601));
#144336=CARTESIAN_POINT('Ctrl Pts',(14.0847736797356,-5.15937500000027,
1492.25));
#144337=CARTESIAN_POINT('Ctrl Pts',(14.0847736797356,-5.15937500000027,
1492.25));
#144338=CARTESIAN_POINT('Ctrl Pts',(14.0847736797356,-5.15937500000028,
1491.59618925398));
#144339=CARTESIAN_POINT('Ctrl Pts',(14.1350860668277,-5.02761209168844,
1490.90285875835));
#144340=CARTESIAN_POINT('Ctrl Pts',(14.3119470704812,-4.49952313800728,
1489.6335196808));
#144341=CARTESIAN_POINT('Ctrl Pts',(14.4354425556449,-4.10344327628932,
1489.05698517792));
#144342=CARTESIAN_POINT('Ctrl Pts',(14.6636670624433,-3.1932559429665,1488.1467978446));
#144343=CARTESIAN_POINT('Ctrl Pts',(14.783891891885,-2.61662608066116,1487.75053274143));
#144344=CARTESIAN_POINT('Ctrl Pts',(14.9531257199511,-1.34693085135711,
1487.22230514128));
#144345=CARTESIAN_POINT('Ctrl Pts',(15.,-0.653464431209191,1487.090625));
#144346=CARTESIAN_POINT('Ctrl Pts',(15.,0.65346443120871,1487.090625));
#144347=CARTESIAN_POINT('Ctrl Pts',(14.9531257199511,1.34693085135663,1487.22230514128));
#144348=CARTESIAN_POINT('Ctrl Pts',(14.7838918918851,2.61662608066068,1487.75053274143));
#144349=CARTESIAN_POINT('Ctrl Pts',(14.6636670624433,3.19325594296603,1488.1467978446));
#144350=CARTESIAN_POINT('Ctrl Pts',(14.4354425556449,4.10344327628884,1489.05698517792));
#144351=CARTESIAN_POINT('Ctrl Pts',(14.3119470704813,4.49952313800681,1489.6335196808));
#144352=CARTESIAN_POINT('Ctrl Pts',(14.1350860668277,5.02761209168797,1490.90285875835));
#144353=CARTESIAN_POINT('Ctrl Pts',(14.0847736797357,5.15937499999978,1491.59618925399));
#144354=CARTESIAN_POINT('Ctrl Pts',(14.0847736797357,5.15937499999978,1492.25));
#144355=CARTESIAN_POINT('',(-14.0847736797356,5.15937499999996,1492.25));
#144356=CARTESIAN_POINT('',(-14.0847736797357,-5.1593750000001,1492.25));
#144357=CARTESIAN_POINT('Ctrl Pts',(-14.0847736797356,5.15937499999994,
1492.25));
#144358=CARTESIAN_POINT('Ctrl Pts',(-14.0847736797356,5.15937499999995,
1491.59618925398));
#144359=CARTESIAN_POINT('Ctrl Pts',(-14.1350860668276,5.02761209168814,
1490.90285875835));
#144360=CARTESIAN_POINT('Ctrl Pts',(-14.3119470704812,4.49952313800698,
1489.6335196808));
#144361=CARTESIAN_POINT('Ctrl Pts',(-14.4354425556449,4.10344327628902,
1489.05698517792));
#144362=CARTESIAN_POINT('Ctrl Pts',(-14.6636670624433,3.1932559429662,1488.1467978446));
#144363=CARTESIAN_POINT('Ctrl Pts',(-14.783891891885,2.61662608066086,1487.75053274143));
#144364=CARTESIAN_POINT('Ctrl Pts',(-14.9531257199511,1.34693085135682,
1487.22230514128));
#144365=CARTESIAN_POINT('Ctrl Pts',(-15.,0.653464431208892,1487.090625));
#144366=CARTESIAN_POINT('Ctrl Pts',(-15.,-0.653464431209009,1487.090625));
#144367=CARTESIAN_POINT('Ctrl Pts',(-14.9531257199511,-1.34693085135693,
1487.22230514128));
#144368=CARTESIAN_POINT('Ctrl Pts',(-14.7838918918851,-2.61662608066098,
1487.75053274143));
#144369=CARTESIAN_POINT('Ctrl Pts',(-14.6636670624433,-3.19325594296632,
1488.1467978446));
#144370=CARTESIAN_POINT('Ctrl Pts',(-14.4354425556449,-4.10344327628914,
1489.05698517792));
#144371=CARTESIAN_POINT('Ctrl Pts',(-14.3119470704813,-4.49952313800711,
1489.6335196808));
#144372=CARTESIAN_POINT('Ctrl Pts',(-14.1350860668277,-5.02761209168827,
1490.90285875835));
#144373=CARTESIAN_POINT('Ctrl Pts',(-14.0847736797357,-5.15937500000011,
1491.59618925398));
#144374=CARTESIAN_POINT('Ctrl Pts',(-14.0847736797357,-5.1593750000001,
1492.25));
#144375=CARTESIAN_POINT('Ctrl Pts',(-14.0847736797357,-5.1593750000001,
1492.25));
#144376=CARTESIAN_POINT('Ctrl Pts',(-14.0847736797357,-5.15937500000009,
1492.90381074602));
#144377=CARTESIAN_POINT('Ctrl Pts',(-14.1350860668277,-5.02761209168827,
1493.59714124165));
#144378=CARTESIAN_POINT('Ctrl Pts',(-14.3119470704813,-4.49952313800711,
1494.8664803192));
#144379=CARTESIAN_POINT('Ctrl Pts',(-14.4354425556449,-4.10344327628914,
1495.44301482208));
#144380=CARTESIAN_POINT('Ctrl Pts',(-14.6636670624433,-3.19325594296633,
1496.3532021554));
#144381=CARTESIAN_POINT('Ctrl Pts',(-14.7838918918851,-2.61662608066098,
1496.74946725857));
#144382=CARTESIAN_POINT('Ctrl Pts',(-14.9531257199511,-1.34693085135693,
1497.27769485872));
#144383=CARTESIAN_POINT('Ctrl Pts',(-15.,-0.653464431209007,1497.409375));
#144384=CARTESIAN_POINT('Ctrl Pts',(-15.,0.653464431208894,1497.409375));
#144385=CARTESIAN_POINT('Ctrl Pts',(-14.9531257199511,1.34693085135682,
1497.27769485872));
#144386=CARTESIAN_POINT('Ctrl Pts',(-14.783891891885,2.61662608066086,1496.74946725857));
#144387=CARTESIAN_POINT('Ctrl Pts',(-14.6636670624433,3.1932559429662,1496.3532021554));
#144388=CARTESIAN_POINT('Ctrl Pts',(-14.4354425556449,4.10344327628902,
1495.44301482208));
#144389=CARTESIAN_POINT('Ctrl Pts',(-14.3119470704812,4.49952313800698,
1494.8664803192));
#144390=CARTESIAN_POINT('Ctrl Pts',(-14.1350860668276,5.02761209168814,
1493.59714124165));
#144391=CARTESIAN_POINT('Ctrl Pts',(-14.0847736797356,5.15937499999995,
1492.90381074601));
#144392=CARTESIAN_POINT('Ctrl Pts',(-14.0847736797356,5.15937499999995,
1492.25));
#144393=CARTESIAN_POINT('Origin',(0.,0.,0.));
#144394=CARTESIAN_POINT('',(5.36664099495454E-10,-15.0000000000002,1301.75000000115));
#144395=CARTESIAN_POINT('',(5.89150092069277E-11,-15.0000000000002,1398.58750000013));
#144396=CARTESIAN_POINT('',(-1.83697019872103E-15,-15.,-1.82952505755738E-15));
#144397=CARTESIAN_POINT('Ctrl Pts',(1.07339914734439E-9,-15.0000000000002,
1301.75000000115));
#144398=CARTESIAN_POINT('Ctrl Pts',(2.02543822040446,-14.9999999998552,
1303.92722419444));
#144399=CARTESIAN_POINT('Ctrl Pts',(4.03516631768684,-14.5900202019492,
1306.0994090624));
#144400=CARTESIAN_POINT('Ctrl Pts',(8.55354940935205,-12.6538998087048,
1311.3974852079));
#144401=CARTESIAN_POINT('Ctrl Pts',(10.8207722409004,-10.779571491316,1314.44081265877));
#144402=CARTESIAN_POINT('Ctrl Pts',(14.0433921586252,-6.00653378080796,
1320.65317208807));
#144403=CARTESIAN_POINT('Ctrl Pts',(14.9346560888454,-3.20260822987993,
1323.69264040189));
#144404=CARTESIAN_POINT('Ctrl Pts',(15.0584371310492,2.55890057198171,1329.91244823535));
#144405=CARTESIAN_POINT('Ctrl Pts',(14.2885008909213,5.39870928526927,1332.94964058359));
#144406=CARTESIAN_POINT('Ctrl Pts',(11.2699281285619,10.3101005421185,1339.17302602159));
#144407=CARTESIAN_POINT('Ctrl Pts',(9.08384366129597,12.2797340197557,1342.21000829538));
#144408=CARTESIAN_POINT('Ctrl Pts',(3.88567321836983,14.7719134699867,1348.4325824966));
#144409=CARTESIAN_POINT('Ctrl Pts',(0.980539852744524,15.2427566439719,
1351.47179820227));
#144410=CARTESIAN_POINT('Ctrl Pts',(-4.73667751952996,14.5211716925833,
1357.68933833136));
#144411=CARTESIAN_POINT('Ctrl Pts',(-7.43379822914247,13.3429445600174,
1360.73247180874));
#144412=CARTESIAN_POINT('Ctrl Pts',(-11.8458131267598,9.6417587937456,1366.94128753384));
#144413=CARTESIAN_POINT('Ctrl Pts',(-13.4750877044247,7.19090259561012,
1369.98980741048));
#144414=CARTESIAN_POINT('Ctrl Pts',(-15.1787035856865,1.69505586624364,
1376.18654827176));
#144415=CARTESIAN_POINT('Ctrl Pts',(-15.2225085183137,-1.24681598994607,
1379.24168501291));
#144416=CARTESIAN_POINT('Ctrl Pts',(-13.6819345669464,-6.78643951579951,
1385.42572949408));
#144417=CARTESIAN_POINT('Ctrl Pts',(-12.1270137088126,-9.28387784012087,
1388.48363239768));
#144418=CARTESIAN_POINT('Ctrl Pts',(-7.83615501145688,-13.1096904546586,
1394.66915124053));
#144419=CARTESIAN_POINT('Ctrl Pts',(-5.17881657278763,-14.3680357852792,
1397.72013525724));
#144420=CARTESIAN_POINT('Ctrl Pts',(-1.56277020429806,-14.9390998255564,
1401.66404994413));
#144421=CARTESIAN_POINT('Ctrl Pts',(-0.78204833489024,-15.000000000027,
1402.50934510429));
#144422=CARTESIAN_POINT('Ctrl Pts',(5.14190356959432E-10,-15.0000000000002,
1403.35000000055));
#144423=CARTESIAN_POINT('Ctrl Pts',(6.38378239159465E-15,-15.0000000000002,
1446.609375));
#144424=CARTESIAN_POINT('Ctrl Pts',(-0.653464431208952,-15.0000000000002,
1446.609375));
#144425=CARTESIAN_POINT('Ctrl Pts',(-1.34693085135696,-14.9531257199513,
1446.47769485872));
#144426=CARTESIAN_POINT('Ctrl Pts',(-2.61662608066102,-14.7838918918852,
1445.94946725857));
#144427=CARTESIAN_POINT('Ctrl Pts',(-3.19325594296631,-14.6636670624435,
1445.5532021554));
#144428=CARTESIAN_POINT('Ctrl Pts',(-4.10344327628912,-14.4354425556451,
1444.64301482208));
#144429=CARTESIAN_POINT('Ctrl Pts',(-4.49952313800711,-14.3119470704814,
1444.0664803192));
#144430=CARTESIAN_POINT('Ctrl Pts',(-5.02761209168826,-14.1350860668278,
1442.79714124165));
#144431=CARTESIAN_POINT('Ctrl Pts',(-5.15937500000008,-14.0847736797358,
1442.10381074602));
#144432=CARTESIAN_POINT('Ctrl Pts',(-5.15937500000008,-14.0847736797358,
1441.45));
#144433=CARTESIAN_POINT('Ctrl Pts',(-5.15937500000008,-14.0847736797358,
1440.79618925399));
#144434=CARTESIAN_POINT('Ctrl Pts',(-5.02761209168826,-14.1350860668278,
1440.10285875835));
#144435=CARTESIAN_POINT('Ctrl Pts',(-4.49952313800711,-14.3119470704814,
1438.8335196808));
#144436=CARTESIAN_POINT('Ctrl Pts',(-4.10344327628912,-14.4354425556451,
1438.25698517792));
#144437=CARTESIAN_POINT('Ctrl Pts',(-3.19325594296631,-14.6636670624435,
1437.3467978446));
#144438=CARTESIAN_POINT('Ctrl Pts',(-2.61662608066102,-14.7838918918852,
1436.95053274143));
#144439=CARTESIAN_POINT('Ctrl Pts',(-1.34693085135696,-14.9531257199513,
1436.42230514128));
#144440=CARTESIAN_POINT('Ctrl Pts',(-0.653464431208967,-15.0000000000002,
1436.290625));
#144441=CARTESIAN_POINT('Ctrl Pts',(-8.88178419700125E-15,-15.0000000000002,
1436.290625));
#144442=CARTESIAN_POINT('Ctrl Pts',(-3.21964677141295E-14,-15.0000000000002,
1500.1875));
#144443=CARTESIAN_POINT('Ctrl Pts',(-1.76742229229486,-15.0000000000002,
1498.28762740068));
#144444=CARTESIAN_POINT('Ctrl Pts',(-3.52305311160152,-14.6871041937304,
1496.38607439147));
#144445=CARTESIAN_POINT('Ctrl Pts',(-6.83900014078546,-13.4665430518641,
1492.58242152618));
#144446=CARTESIAN_POINT('Ctrl Pts',(-8.37850025940737,-12.5669392521719,
1490.68632496464));
#144447=CARTESIAN_POINT('Ctrl Pts',(-11.9141329007694,-9.5562284284336,
1485.68171169807));
#144448=CARTESIAN_POINT('Ctrl Pts',(-13.5248067380123,-7.09592658651337,
1482.63269613729));
#144449=CARTESIAN_POINT('Ctrl Pts',(-15.1894805082896,-1.59255519695219,
1476.44356712209));
#144450=CARTESIAN_POINT('Ctrl Pts',(-15.2127708569242,1.34762269085022,
1473.38707582416));
#144451=CARTESIAN_POINT('Ctrl Pts',(-13.6380720372901,6.87605632801695,
1467.2078061325));
#144452=CARTESIAN_POINT('Ctrl Pts',(-12.0663282125807,9.36278073914447,
1464.15025536866));
#144453=CARTESIAN_POINT('Ctrl Pts',(-7.74812761957123,13.1624797736,1457.95817034909));
#144454=CARTESIAN_POINT('Ctrl Pts',(-5.08002271936798,14.4039629815762,
1454.90758866529));
#144455=CARTESIAN_POINT('Ctrl Pts',(0.613086311585234,15.2616144348726,
1448.70241026148));
#144456=CARTESIAN_POINT('Ctrl Pts',(3.52888509754822,14.860811034796,1445.65764851361));
#144457=CARTESIAN_POINT('Ctrl Pts',(8.78291544086862,12.4964470149111,1439.44259712957));
#144458=CARTESIAN_POINT('Ctrl Pts',(11.0166930867714,10.580104205331,1436.40226353964));
#144459=CARTESIAN_POINT('Ctrl Pts',(14.1532167714079,5.74397732306138,1430.18092697203));
#144460=CARTESIAN_POINT('Ctrl Pts',(14.9921131886098,2.92336609792222,1427.14340515978));
#144461=CARTESIAN_POINT('Ctrl Pts',(15.0077755460274,-2.84165960585207,
1420.91980067256));
#144462=CARTESIAN_POINT('Ctrl Pts',(14.1844363389502,-5.66644694002087,
1417.8829764111));
#144463=CARTESIAN_POINT('Ctrl Pts',(11.0746670298407,-10.519278170437,1411.66151250116));
#144464=CARTESIAN_POINT('Ctrl Pts',(8.85220915139545,-12.4473699157053,
1408.62298180108));
#144465=CARTESIAN_POINT('Ctrl Pts',(4.26917589575086,-14.5406277074722,
1403.18681607211));
#144466=CARTESIAN_POINT('Ctrl Pts',(2.1447555437566,-14.9999999999999,1400.89298313642));
#144467=CARTESIAN_POINT('Ctrl Pts',(1.17759552109575E-10,-15.0000000000001,
1398.58750000013));
#144468=CARTESIAN_POINT('',(-8.4434420636672E-19,14.9999999999998,1436.290625));
#144469=CARTESIAN_POINT('',(-6.31841207935097E-16,14.9999999999998,1446.609375));
#144470=CARTESIAN_POINT('Ctrl Pts',(-8.46545056276682E-15,14.9999999999998,
1436.290625));
#144471=CARTESIAN_POINT('Ctrl Pts',(-0.653464431208967,14.9999999999998,
1436.290625));
#144472=CARTESIAN_POINT('Ctrl Pts',(-1.34693085135696,14.9531257199509,
1436.42230514128));
#144473=CARTESIAN_POINT('Ctrl Pts',(-2.61662608066102,14.7838918918849,
1436.95053274143));
#144474=CARTESIAN_POINT('Ctrl Pts',(-3.19325594296631,14.6636670624431,
1437.3467978446));
#144475=CARTESIAN_POINT('Ctrl Pts',(-4.10344327628912,14.4354425556447,
1438.25698517792));
#144476=CARTESIAN_POINT('Ctrl Pts',(-4.49952313800711,14.3119470704811,
1438.8335196808));
#144477=CARTESIAN_POINT('Ctrl Pts',(-5.02761209168826,14.1350860668275,
1440.10285875835));
#144478=CARTESIAN_POINT('Ctrl Pts',(-5.15937500000008,14.0847736797355,
1440.79618925399));
#144479=CARTESIAN_POINT('Ctrl Pts',(-5.15937500000008,14.0847736797355,
1441.45));
#144480=CARTESIAN_POINT('Ctrl Pts',(-5.15937500000008,14.0847736797355,
1442.10381074602));
#144481=CARTESIAN_POINT('Ctrl Pts',(-5.02761209168826,14.1350860668275,
1442.79714124165));
#144482=CARTESIAN_POINT('Ctrl Pts',(-4.49952313800711,14.3119470704811,
1444.0664803192));
#144483=CARTESIAN_POINT('Ctrl Pts',(-4.10344327628912,14.4354425556447,
1444.64301482208));
#144484=CARTESIAN_POINT('Ctrl Pts',(-3.19325594296631,14.6636670624431,
1445.5532021554));
#144485=CARTESIAN_POINT('Ctrl Pts',(-2.61662608066101,14.7838918918849,
1445.94946725857));
#144486=CARTESIAN_POINT('Ctrl Pts',(-1.34693085135696,14.9531257199509,
1446.47769485872));
#144487=CARTESIAN_POINT('Ctrl Pts',(-0.653464431208951,14.9999999999998,
1446.609375));
#144488=CARTESIAN_POINT('Ctrl Pts',(6.24500451351651E-15,14.9999999999998,
1446.609375));
#144489=CARTESIAN_POINT('Ctrl Pts',(7.63278329429795E-16,14.9999999999998,
1446.609375));
#144490=CARTESIAN_POINT('Ctrl Pts',(0.65346443120896,14.9999999999998,1446.609375));
#144491=CARTESIAN_POINT('Ctrl Pts',(1.34693085135724,14.9531257199509,1446.47769485872));
#144492=CARTESIAN_POINT('Ctrl Pts',(2.61662608066126,14.7838918918848,1445.94946725857));
#144493=CARTESIAN_POINT('Ctrl Pts',(3.19325594296631,14.6636670624431,1445.5532021554));
#144494=CARTESIAN_POINT('Ctrl Pts',(4.10344327628912,14.4354425556447,1444.64301482208));
#144495=CARTESIAN_POINT('Ctrl Pts',(4.49952313800732,14.311947070481,1444.0664803192));
#144496=CARTESIAN_POINT('Ctrl Pts',(5.02761209168842,14.1350860668274,1442.79714124165));
#144497=CARTESIAN_POINT('Ctrl Pts',(5.15937500000008,14.0847736797355,1442.10381074602));
#144498=CARTESIAN_POINT('Ctrl Pts',(5.15937500000008,14.0847736797355,1440.79618925399));
#144499=CARTESIAN_POINT('Ctrl Pts',(5.02761209168819,14.1350860668275,1440.10285875835));
#144500=CARTESIAN_POINT('Ctrl Pts',(4.49952313800696,14.3119470704811,1438.8335196808));
#144501=CARTESIAN_POINT('Ctrl Pts',(4.10344327628912,14.4354425556447,1438.25698517792));
#144502=CARTESIAN_POINT('Ctrl Pts',(3.19325594296631,14.6636670624431,1437.3467978446));
#144503=CARTESIAN_POINT('Ctrl Pts',(2.61662608066102,14.7838918918849,1436.95053274143));
#144504=CARTESIAN_POINT('Ctrl Pts',(1.34693085135696,14.9531257199509,1436.42230514128));
#144505=CARTESIAN_POINT('Ctrl Pts',(0.653464431208971,14.9999999999998,
1436.290625));
#144506=CARTESIAN_POINT('Ctrl Pts',(1.2490009027033E-14,14.9999999999998,
1436.290625));
#144507=CARTESIAN_POINT('Origin',(0.,0.,0.));
#144508=CARTESIAN_POINT('',(8.79825987290161E-10,-15.0000000000001,1200.15000000189));
#144509=CARTESIAN_POINT('',(2.06320846743069E-10,-15.0000000000002,1296.98750000044));
#144510=CARTESIAN_POINT('',(-1.83697019872103E-15,-15.,-1.82952505755738E-15));
#144511=CARTESIAN_POINT('Ctrl Pts',(1.75979453231889E-9,-15.0000000000001,
1200.15000000189));
#144512=CARTESIAN_POINT('Ctrl Pts',(1.97399358436651,-14.9999999997686,
1202.27192430669));
#144513=CARTESIAN_POINT('Ctrl Pts',(3.93352370368442,-14.6105361002977,
1204.39131264898));
#144514=CARTESIAN_POINT('Ctrl Pts',(8.42209926513274,-12.7415093717001,
1209.62829861148));
#144515=CARTESIAN_POINT('Ctrl Pts',(10.708157128334,-10.8909829112263,1212.67455397258));
#144516=CARTESIAN_POINT('Ctrl Pts',(13.9790171867833,-6.15435157868962,
1218.88091311306));
#144517=CARTESIAN_POINT('Ctrl Pts',(14.8997625697908,-3.36022939188954,
1221.92248126964));
#144518=CARTESIAN_POINT('Ctrl Pts',(15.0847894150078,2.39760634805479,1228.13832386759));
#144519=CARTESIAN_POINT('Ctrl Pts',(14.3453595870873,5.2454463407763,1231.17665534719));
#144520=CARTESIAN_POINT('Ctrl Pts',(11.3801811105094,10.1881713863212,1237.39845607226));
#144521=CARTESIAN_POINT('Ctrl Pts',(9.21562980893118,12.1811613315997,1240.43522159905));
#144522=CARTESIAN_POINT('Ctrl Pts',(4.04428599820379,14.7293316556033,1246.65881387988));
#144523=CARTESIAN_POINT('Ctrl Pts',(1.14467164290646,15.2314208312659,1249.69649554128));
#144524=CARTESIAN_POINT('Ctrl Pts',(-4.58141563311257,14.5710755535568,
1255.91747033129));
#144525=CARTESIAN_POINT('Ctrl Pts',(-7.29089458762112,13.4217383032652,
1258.95810002799));
#144526=CARTESIAN_POINT('Ctrl Pts',(-11.7438326680798,9.76617145395712,
1265.17249253716));
#144527=CARTESIAN_POINT('Ctrl Pts',(-13.398827027713,7.33236029579112,1268.2176697433));
#144528=CARTESIAN_POINT('Ctrl Pts',(-15.1608221842952,1.85167160060532,
1274.42191838725));
#144529=CARTESIAN_POINT('Ctrl Pts',(-15.2346745109395,-1.09014303455582,
1277.47301604798));
#144530=CARTESIAN_POINT('Ctrl Pts',(-13.7499080930685,-6.64897693704802,
1283.66637557301));
#144531=CARTESIAN_POINT('Ctrl Pts',(-12.2192777208826,-9.16225557399221,
1286.72502342585));
#144532=CARTESIAN_POINT('Ctrl Pts',(-7.96708294002146,-13.0303297743241,
1292.90472764945));
#144533=CARTESIAN_POINT('Ctrl Pts',(-5.32321122148986,-14.3146286300458,
1295.95959992813));
#144534=CARTESIAN_POINT('Ctrl Pts',(-1.66486260240058,-14.9308817487195,
1299.95348817526));
#144535=CARTESIAN_POINT('Ctrl Pts',(-0.833320165543613,-15.0000000000598,
1300.85423097193));
#144536=CARTESIAN_POINT('Ctrl Pts',(1.07344951901075E-9,-15.0000000000002,
1301.75000000115));
#144537=CARTESIAN_POINT('Ctrl Pts',(1.17824847101211E-10,-15.0000000000002,
1398.58750000013));
#144538=CARTESIAN_POINT('Ctrl Pts',(-0.71771403817806,-15.0000000000003,
1397.81600060157));
#144539=CARTESIAN_POINT('Ctrl Pts',(-1.43458366106872,-14.9486793604924,
1397.04029696054));
#144540=CARTESIAN_POINT('Ctrl Pts',(-4.99620392819751,-14.4331061176049,
1393.16041437585));
#144541=CARTESIAN_POINT('Ctrl Pts',(-7.66995212336838,-13.2079060285185,
1390.11373050036));
#144542=CARTESIAN_POINT('Ctrl Pts',(-12.0093941122352,-9.43548920412243,
1383.92109513407));
#144543=CARTESIAN_POINT('Ctrl Pts',(-13.5950655942685,-6.95995628694869,
1380.86842290804));
#144544=CARTESIAN_POINT('Ctrl Pts',(-15.2045078947381,-1.44150614914692,
1374.68565391779));
#144545=CARTESIAN_POINT('Ctrl Pts',(-15.1988282304223,1.50118033788765,
1371.62706038024));
#144546=CARTESIAN_POINT('Ctrl Pts',(-13.5667033566612,7.0161084865984,1365.43899111184));
#144547=CARTESIAN_POINT('Ctrl Pts',(-11.9693212941103,9.48724026705885,
1362.38571456362));
#144548=CARTESIAN_POINT('Ctrl Pts',(-7.60893334399002,13.2436188010555,
1356.185468396));
#144549=CARTESIAN_POINT('Ctrl Pts',(-4.92765696827631,14.4571536279501,
1353.1385064468));
#144550=CARTESIAN_POINT('Ctrl Pts',(0.77691088707214,15.2543139944877,1346.92703588305));
#144551=CARTESIAN_POINT('Ctrl Pts',(3.68825684256168,14.8222754834421,1343.88509349636));
#144552=CARTESIAN_POINT('Ctrl Pts',(8.91805348489406,12.4005263563624,1337.66584740671));
#144553=CARTESIAN_POINT('Ctrl Pts',(11.130730801771,10.4601942654857,1334.62739603187));
#144554=CARTESIAN_POINT('Ctrl Pts',(14.2149626350962,5.58959776446285,1328.40413944157));
#144555=CARTESIAN_POINT('Ctrl Pts',(15.0229610734552,2.7603694750373,1325.36744297579));
#144556=CARTESIAN_POINT('Ctrl Pts',(14.9760496486665,-3.00400024173918,
1319.14454665604));
#144557=CARTESIAN_POINT('Ctrl Pts',(14.1221027053062,-5.81966903139119,
1316.1069172253));
#144558=CARTESIAN_POINT('Ctrl Pts',(10.9611608397889,-10.6372410828221,
1309.88873413739));
#144559=CARTESIAN_POINT('Ctrl Pts',(8.71830137524085,-12.5412811976424,
1306.84838787216));
#144560=CARTESIAN_POINT('Ctrl Pts',(4.16368759723579,-14.5632693044744,
1301.47398043358));
#144561=CARTESIAN_POINT('Ctrl Pts',(2.09082327762966,-14.9999999999426,
1299.23500919603));
#144562=CARTESIAN_POINT('Ctrl Pts',(4.12767042767825E-10,-15.0000000000002,
1296.98750000044));
#144563=CARTESIAN_POINT('Origin',(0.,0.,0.));
#144564=CARTESIAN_POINT('',(9.52135784329144E-10,-15.0000000000001,1098.55000000205));
#144565=CARTESIAN_POINT('',(4.61706142986984E-10,-15.0000000000001,1195.38750000099));
#144566=CARTESIAN_POINT('',(-1.83697019872103E-15,-15.,-1.82952505755738E-15));
#144567=CARTESIAN_POINT('Ctrl Pts',(1.90432308810884E-9,-15.0000000000001,
1098.55000000205));
#144568=CARTESIAN_POINT('Ctrl Pts',(1.92202320191745,-14.9999999997561,
1100.61605927318));
#144569=CARTESIAN_POINT('Ctrl Pts',(3.83162991280002,-14.6307194546823,
1102.68313352437));
#144570=CARTESIAN_POINT('Ctrl Pts',(8.29048688497464,-12.8272881628003,
1107.85983619282));
#144571=CARTESIAN_POINT('Ctrl Pts',(10.5948484305959,-11.0006774132446,
1110.90947698597));
#144572=CARTESIAN_POINT('Ctrl Pts',(13.9131826583481,-6.30124214664866,
1117.10867571733));
#144573=CARTESIAN_POINT('Ctrl Pts',(14.8631643120297,-3.51733684258962,
1120.15287671185));
#144574=CARTESIAN_POINT('Ctrl Pts',(15.1094439039152,2.23563536119488,1126.36346890381));
#144575=CARTESIAN_POINT('Ctrl Pts',(14.4006802897054,5.09109066860144,1129.40354120608));
#144576=CARTESIAN_POINT('Ctrl Pts',(11.4898658308363,10.064093992546,1135.62223731496));
#144577=CARTESIAN_POINT('Ctrl Pts',(9.34710505755872,12.0804849622448,1138.65972306586));
#144578=CARTESIAN_POINT('Ctrl Pts',(4.20410894919187,14.6845033463582,1144.88279479004));
#144579=CARTESIAN_POINT('Ctrl Pts',(1.31050196415145,15.218120096428,1147.91956278325));
#144580=CARTESIAN_POINT('Ctrl Pts',(-4.42330682574351,14.6199503152763,
1154.14264456888));
#144581=CARTESIAN_POINT('Ctrl Pts',(-7.14491054562634,13.5001672047438,
1157.18131185169));
#144582=CARTESIAN_POINT('Ctrl Pts',(-11.6385345751432,9.8917585283482,1163.40007537353));
#144583=CARTESIAN_POINT('Ctrl Pts',(-13.3195217540098,7.47578682138226,
1166.44236284484));
#144584=CARTESIAN_POINT('Ctrl Pts',(-15.1407775212644,2.01164521892566,
1172.65306468181));
#144585=CARTESIAN_POINT('Ctrl Pts',(-15.2454755863158,-0.929573713222222,
1175.70048315408));
#144586=CARTESIAN_POINT('Ctrl Pts',(-13.8187694358849,-6.50478376461115,
1181.89970327795));
#144587=CARTESIAN_POINT('Ctrl Pts',(-12.315292405085,-9.03405822125963,
1184.95352856043));
#144588=CARTESIAN_POINT('Ctrl Pts',(-8.10107486955481,-12.9471147882967,
1191.14027521031));
#144589=CARTESIAN_POINT('Ctrl Pts',(-5.46767650788743,-14.2603922672436,
1194.19890607217));
#144590=CARTESIAN_POINT('Ctrl Pts',(-1.76443889312882,-14.922363100848,
1198.24560113117));
#144591=CARTESIAN_POINT('Ctrl Pts',(-0.883351399577367,-15.0000000001038,
1199.20045040626));
#144592=CARTESIAN_POINT('Ctrl Pts',(1.75977386471601E-9,-15.0000000000001,
1200.15000000189));
#144593=CARTESIAN_POINT('Ctrl Pts',(4.12697515050908E-10,-15.0000000000002,
1296.98750000044));
#144594=CARTESIAN_POINT('Ctrl Pts',(-0.769894768051591,-15.0000000000213,
1296.15990945723));
#144595=CARTESIAN_POINT('Ctrl Pts',(-1.53856172628175,-14.9409719495836,
1295.32775907935));
#144596=CARTESIAN_POINT('Ctrl Pts',(-5.14443979608549,-14.380495004843,
1291.39582925936));
#144597=CARTESIAN_POINT('Ctrl Pts',(-7.80491977416643,-13.1283632101541,
1288.34570821307));
#144598=CARTESIAN_POINT('Ctrl Pts',(-12.105104901342,-9.31246842067276,
1282.15860694432));
#144599=CARTESIAN_POINT('Ctrl Pts',(-13.6654892130908,-6.81929030932275,
1279.10135175935));
#144600=CARTESIAN_POINT('Ctrl Pts',(-15.2193804718104,-1.28406273702655,
1272.91933040514));
#144601=CARTESIAN_POINT('Ctrl Pts',(-15.1827094895822,1.65774377668617,
1269.86317053524));
#144602=CARTESIAN_POINT('Ctrl Pts',(-13.4930535609753,7.15705228474937,
1263.66838894451));
#144603=CARTESIAN_POINT('Ctrl Pts',(-11.8699457523811,9.61190395378373,
1260.61900038051));
#144604=CARTESIAN_POINT('Ctrl Pts',(-7.46783838915637,13.3238782986591,
1254.41170121311));
#144605=CARTESIAN_POINT('Ctrl Pts',(-4.77373574858607,14.5089779731568,
1251.36788828749));
#144606=CARTESIAN_POINT('Ctrl Pts',(0.941176728315708,15.2452064662291,
1245.15136717061));
#144607=CARTESIAN_POINT('Ctrl Pts',(3.84756728011627,14.7818617551212,1242.11169395613));
#144608=CARTESIAN_POINT('Ctrl Pts',(9.05198286843481,12.3032191192182,1235.88959848178));
#144609=CARTESIAN_POINT('Ctrl Pts',(11.2432367200937,10.3392060353596,1232.852409349));
#144610=CARTESIAN_POINT('Ctrl Pts',(14.2745479122127,5.43554174545849,1226.62887674805));
#144611=CARTESIAN_POINT('Ctrl Pts',(15.0518224439408,2.59773028908131,1223.59186666104));
#144612=CARTESIAN_POINT('Ctrl Pts',(14.9428235958911,-3.16448362300977,
1217.37129762939));
#144613=CARTESIAN_POINT('Ctrl Pts',(14.0587097698017,-5.97071514542203,
1214.33225324628));
#144614=CARTESIAN_POINT('Ctrl Pts',(10.8478515048654,-10.7524187323543,
1208.11862409471));
#144615=CARTESIAN_POINT('Ctrl Pts',(8.5852522919524,-12.6324748082145,1205.07593148621));
#144616=CARTESIAN_POINT('Ctrl Pts',(4.05979577078787,-14.5849641361676,
1199.76314315456));
#144617=CARTESIAN_POINT('Ctrl Pts',(2.0379397774467,-14.9999999998747,1197.57816261591));
#144618=CARTESIAN_POINT('Ctrl Pts',(9.23458105710732E-10,-15.0000000000001,
1195.38750000099));
#144619=CARTESIAN_POINT('Origin',(0.,0.,0.));
#144620=CARTESIAN_POINT('',(1.12804740017511E-11,-15.0000000000001,996.950000000024));
#144621=CARTESIAN_POINT('',(8.43148104337132E-10,-15.0000000000001,1093.78750000181));
#144622=CARTESIAN_POINT('',(-1.83697019872103E-15,-15.,-1.82952505755738E-15));
#144623=CARTESIAN_POINT('Ctrl Pts',(2.24431584427975E-11,-15.0000000000001,
996.950000000024));
#144624=CARTESIAN_POINT('Ctrl Pts',(1.8730160222366,-15.0000000000001,998.963379504291));
#144625=CARTESIAN_POINT('Ctrl Pts',(3.73260476096043,-14.6497110398557,
1000.97830003658));
#144626=CARTESIAN_POINT('Ctrl Pts',(8.16125115437788,-12.9096787385466,
1006.09530088561));
#144627=CARTESIAN_POINT('Ctrl Pts',(10.4830299559481,-11.1066322977705,
1009.14867930291));
#144628=CARTESIAN_POINT('Ctrl Pts',(13.8472105025231,-6.44441945178535,
1015.33976831645));
#144629=CARTESIAN_POINT('Ctrl Pts',(14.8256060144153,-3.67095044645471,
1018.38704391883));
#144630=CARTESIAN_POINT('Ctrl Pts',(15.1319727650807,2.07612182853235,1024.59126687234));
#144631=CARTESIAN_POINT('Ctrl Pts',(14.4534309549069,4.9386110172691,1027.633609537));
#144632=CARTESIAN_POINT('Ctrl Pts',(11.5968074887327,9.94040367199438,1033.84793273401));
#144633=CARTESIAN_POINT('Ctrl Pts',(9.47586063211703,11.9795942956902,1036.8867496228));
#144634=CARTESIAN_POINT('Ctrl Pts',(4.36222498638682,14.6382077696174,1043.10771916763));
#144635=CARTESIAN_POINT('Ctrl Pts',(1.47462240033404,15.2030775705206,1046.14464154482));
#144636=CARTESIAN_POINT('Ctrl Pts',(-4.26538892408494,14.6668340844614,
1052.3682223371));
#144637=CARTESIAN_POINT('Ctrl Pts',(-6.99866059986271,13.576672237868,1055.40554621383));
#144638=CARTESIAN_POINT('Ctrl Pts',(-11.5319057810387,10.0160832097434,
1061.62733309336));
#144639=CARTESIAN_POINT('Ctrl Pts',(-13.2386493056426,7.61838119872912,
1064.66728246334));
#144640=CARTESIAN_POINT('Ctrl Pts',(-15.1188894104588,2.17192003957943,
1070.8831888708));
#144641=CARTESIAN_POINT('Ctrl Pts',(-15.2546242876952,-0.768179479350522,
1073.92740266756));
#144642=CARTESIAN_POINT('Ctrl Pts',(-13.8859768100344,-6.36101200390849,
1080.13380626064));
#144643=CARTESIAN_POINT('Ctrl Pts',(-12.4083713615784,-8.90603998351183,
1083.18370155585));
#144644=CARTESIAN_POINT('Ctrl Pts',(-8.2334486591165,-12.8635554275619,
1089.37733866998));
#144645=CARTESIAN_POINT('Ctrl Pts',(-5.61463438468432,-14.2040034671046,
1092.4340911989));
#144646=CARTESIAN_POINT('Ctrl Pts',(-1.86492777684583,-14.9132117530754,
1096.53706165363));
#144647=CARTESIAN_POINT('Ctrl Pts',(-0.933904123582952,-15.0000000001187,
1097.54610927026));
#144648=CARTESIAN_POINT('Ctrl Pts',(1.90427969863687E-9,-15.0000000000001,
1098.55000000205));
#144649=CARTESIAN_POINT('Ctrl Pts',(9.23458105710732E-10,-15.0000000000001,
1195.38750000099));
#144650=CARTESIAN_POINT('Ctrl Pts',(-0.821178976272775,-15.0000000000507,
1194.50478201972));
#144651=CARTESIAN_POINT('Ctrl Pts',(-1.64069188092298,-14.9328745854408,
1193.6171687484));
#144652=CARTESIAN_POINT('Ctrl Pts',(-5.28911085923903,-14.327398555011,
1189.63502775005));
#144653=CARTESIAN_POINT('Ctrl Pts',(-7.93620275077505,-13.049206807507,
1186.58111164689));
#144654=CARTESIAN_POINT('Ctrl Pts',(-12.1975161535311,-9.1911476248741,
1180.4000672537));
#144655=CARTESIAN_POINT('Ctrl Pts',(-13.7339933049332,-6.68144215564515,
1177.34148343405));
#144656=CARTESIAN_POINT('Ctrl Pts',(-15.2319436817764,-1.12717518048759,
1171.1503549189));
#144657=CARTESIAN_POINT('Ctrl Pts',(-15.1651986962582,1.81470064774139,
1168.09834177543));
#144658=CARTESIAN_POINT('Ctrl Pts',(-13.4169527219817,7.29905964381786,
1161.89576029855));
#144659=CARTESIAN_POINT('Ctrl Pts',(-11.7680056471831,9.7369333162655,1158.84983893944));
#144660=CARTESIAN_POINT('Ctrl Pts',(-7.32463102653318,13.4033178858974,
1152.63664761051));
#144661=CARTESIAN_POINT('Ctrl Pts',(-4.61802494538421,14.5594801028764,
1149.59547813664));
#144662=CARTESIAN_POINT('Ctrl Pts',(1.10608557067634,15.2342487988229,1143.37519155904));
#144663=CARTESIAN_POINT('Ctrl Pts',(4.00703668296603,14.7395020205243,1140.33720438905));
#144664=CARTESIAN_POINT('Ctrl Pts',(9.18481444702779,12.2044224110096,1134.11369371611));
#144665=CARTESIAN_POINT('Ctrl Pts',(11.3544041109852,10.2169309128655,1131.07700218978));
#144666=CARTESIAN_POINT('Ctrl Pts',(14.3321826275215,5.2814322920117,1124.85467352815));
#144667=CARTESIAN_POINT('Ctrl Pts',(15.0787707297665,2.43543683555569,1121.81666357999));
#144668=CARTESIAN_POINT('Ctrl Pts',(14.9080518871194,-3.32452031727013,
1115.59853082145));
#144669=CARTESIAN_POINT('Ctrl Pts',(13.9934828338927,-6.12205439404753,
1112.55627793874));
#144670=CARTESIAN_POINT('Ctrl Pts',(10.7312074299843,-10.868816474941,1106.34549903581));
#144671=CARTESIAN_POINT('Ctrl Pts',(8.44741452093267,-12.7251674847629,
1103.29812611831));
#144672=CARTESIAN_POINT('Ctrl Pts',(3.95184186519944,-14.6068799135907,
1098.04827409019));
#144673=CARTESIAN_POINT('Ctrl Pts',(1.98322361516975,-14.9999999997772,
1095.91934603433));
#144674=CARTESIAN_POINT('Ctrl Pts',(1.68617259044268E-9,-15.0000000000001,
1093.78750000181));
#144675=CARTESIAN_POINT('Origin',(0.,0.,0.));
#144676=CARTESIAN_POINT('',(-3.39412889236257E-10,-15.0000000000001,895.34999999927));
#144677=CARTESIAN_POINT('',(1.18621812117655E-9,-15.0000000000001,992.18750000255));
#144678=CARTESIAN_POINT('',(-1.83697019872103E-15,-15.,-1.82952505755738E-15));
#144679=CARTESIAN_POINT('Ctrl Pts',(-6.78717360091952E-10,-15.0000000000001,
895.34999999927));
#144680=CARTESIAN_POINT('Ctrl Pts',(1.81530776265467,-15.0000000000822,
897.301346598161));
#144681=CARTESIAN_POINT('Ctrl Pts',(3.61819325598204,-14.6713763119832,
899.254859370096));
#144682=CARTESIAN_POINT('Ctrl Pts',(8.01267924322565,-13.0019991669338,
904.310990328089));
#144683=CARTESIAN_POINT('Ctrl Pts',(10.3575355933915,-11.2240553804396,
907.369583455908));
#144684=CARTESIAN_POINT('Ctrl Pts',(13.7748779118175,-6.59802740400891,
913.557672489966));
#144685=CARTESIAN_POINT('Ctrl Pts',(14.7841893814279,-3.83407757460096,
916.610940848539));
#144686=CARTESIAN_POINT('Ctrl Pts',(15.1540025554497,1.90932507552399,922.811202277));
#144687=CARTESIAN_POINT('Ctrl Pts',(14.5065334548264,4.78033466882151,925.858157433005));
#144688=CARTESIAN_POINT('Ctrl Pts',(11.7048007290421,9.81301866781119,932.069639374599));
#144689=CARTESIAN_POINT('Ctrl Pts',(9.60550431941437,11.8759162278827,935.111576652667));
#144690=CARTESIAN_POINT('Ctrl Pts',(4.52118877587782,14.5898454704389,941.33082980798));
#144691=CARTESIAN_POINT('Ctrl Pts',(1.63932192043573,15.1862259714449,944.369278023895));
#144692=CARTESIAN_POINT('Ctrl Pts',(-4.10612417080342,14.7121834621567,
950.592505158305));
#144693=CARTESIAN_POINT('Ctrl Pts',(-6.85077495090437,13.6519489150702,
953.629170558023));
#144694=CARTESIAN_POINT('Ctrl Pts',(-11.4229070225234,10.1403302346103,
959.85259962067));
#144695=CARTESIAN_POINT('Ctrl Pts',(-13.155411596351,7.76147412577686,962.890777822469));
#144696=CARTESIAN_POINT('Ctrl Pts',(-15.0949074247572,2.33404345680181,
969.110635615743));
#144697=CARTESIAN_POINT('Ctrl Pts',(-15.2621496783219,-0.604415026600302,
972.152129000351));
#144698=CARTESIAN_POINT('Ctrl Pts',(-13.9527222770561,-6.21403477228019,
978.364599340677));
#144699=CARTESIAN_POINT('Ctrl Pts',(-12.5018017555402,-8.77468893311663,
981.410960060362));
#144700=CARTESIAN_POINT('Ctrl Pts',(-8.36628607719189,-12.7781047944913,
987.612556095191));
#144701=CARTESIAN_POINT('Ctrl Pts',(-5.76074314579896,-14.145524343791,
990.665104924394));
#144702=CARTESIAN_POINT('Ctrl Pts',(-1.9673848809929,-14.903369644354,994.8277692865));
#144703=CARTESIAN_POINT('Ctrl Pts',(-0.984787905444944,-15.0000000000001,
995.891412266977));
#144704=CARTESIAN_POINT('Ctrl Pts',(2.24911755886126E-11,-15.0000000000001,
996.950000000024));
#144705=CARTESIAN_POINT('Ctrl Pts',(1.68611037020101E-9,-15.0000000000001,
1093.78750000181));
#144706=CARTESIAN_POINT('Ctrl Pts',(-0.876425657055577,-15.0000000000986,
1092.84539516268));
#144707=CARTESIAN_POINT('Ctrl Pts',(-1.75065812745964,-14.9235720281569,
1091.89803504357));
#144708=CARTESIAN_POINT('Ctrl Pts',(-5.44814057417547,-14.2679091189493,
1087.85815476261));
#144709=CARTESIAN_POINT('Ctrl Pts',(-8.08330603931329,-12.9581831528988,
1084.79952847719));
#144710=CARTESIAN_POINT('Ctrl Pts',(-12.3011322074853,-9.05260244348057,
1078.6161215134));
#144711=CARTESIAN_POINT('Ctrl Pts',(-13.807366164627,-6.52782291760142,
1075.56391360973));
#144712=CARTESIAN_POINT('Ctrl Pts',(-15.2432587189879,-0.959580395540722,
1069.37026490581));
#144713=CARTESIAN_POINT('Ctrl Pts',(-15.1445654985297,1.97993033575274,
1066.32396755525));
#144714=CARTESIAN_POINT('Ctrl Pts',(-13.3365580323199,7.44480340050893,
1060.1176959226));
#144715=CARTESIAN_POINT('Ctrl Pts',(-11.6620142236278,9.86363973510192,
1057.07609626137));
#144716=CARTESIAN_POINT('Ctrl Pts',(-7.17920077957322,13.4817799027032,
1050.86031498226));
#144717=CARTESIAN_POINT('Ctrl Pts',(-4.46113110936773,14.6082956535718,
1047.8219642932));
#144718=CARTESIAN_POINT('Ctrl Pts',(1.27006225544689,15.2215062214116,1041.60019575181));
#144719=CARTESIAN_POINT('Ctrl Pts',(4.16501214688111,14.6956178083694,1038.56342494792));
#144720=CARTESIAN_POINT('Ctrl Pts',(9.31529759896216,12.1051517549074,1032.33983033606));
#144721=CARTESIAN_POINT('Ctrl Pts',(11.4636677038208,10.0940979652688,1029.30216497423));
#144722=CARTESIAN_POINT('Ctrl Pts',(14.3881591190903,5.12704029501961,1023.08115335682));
#144723=CARTESIAN_POINT('Ctrl Pts',(15.1042014134289,2.27230308855386,1020.04055336436));
#144724=CARTESIAN_POINT('Ctrl Pts',(14.8713083193167,-3.48425063619731,
1013.82609475946));
#144725=CARTESIAN_POINT('Ctrl Pts',(13.9268335217246,-6.2717978451629,1010.78095898351));
#144726=CARTESIAN_POINT('Ctrl Pts',(10.6156269806208,-10.9812493468169,
1004.57661759013));
#144727=CARTESIAN_POINT('Ctrl Pts',(8.31276114991967,-12.8133439752483,
1001.52557122028));
#144728=CARTESIAN_POINT('Ctrl Pts',(3.84726626553424,-14.627690881467,996.337201344411));
#144729=CARTESIAN_POINT('Ctrl Pts',(1.92979839330253,-14.9999999996949,
994.261917136008));
#144730=CARTESIAN_POINT('Ctrl Pts',(2.37242503420276E-9,-15.0000000000001,
992.18750000255));
#144731=CARTESIAN_POINT('Origin',(0.,0.,0.));
#144732=CARTESIAN_POINT('',(-7.10644545762562E-10,-15.0000000000001,793.749999998472));
#144733=CARTESIAN_POINT('',(5.08855987370824E-11,-15.0000000000001,890.587500000109));
#144734=CARTESIAN_POINT('',(-1.83697019872103E-15,-15.,-1.82952505755738E-15));
#144735=CARTESIAN_POINT('Ctrl Pts',(-1.4212352516319E-9,-15.0000000000001,
793.749999998472));
#144736=CARTESIAN_POINT('Ctrl Pts',(1.76519122070185,-15.0000000001673,
795.647474331607));
#144737=CARTESIAN_POINT('Ctrl Pts',(3.51901863713381,-14.6893233616095,
797.546580864287));
#144738=CARTESIAN_POINT('Ctrl Pts',(7.88307933530167,-13.0810399035321,
802.553071209357));
#144739=CARTESIAN_POINT('Ctrl Pts',(10.2433978333917,-11.327723059795,805.609567012152));
#144740=CARTESIAN_POINT('Ctrl Pts',(13.7061245965917,-6.7393853876843,811.788854396085));
#144741=CARTESIAN_POINT('Ctrl Pts',(14.7433308821365,-3.98649793084226,
814.846396219982));
#144742=CARTESIAN_POINT('Ctrl Pts',(15.1731391053388,1.7493469424941,821.038498688545));
#144743=CARTESIAN_POINT('Ctrl Pts',(14.5559111691972,4.62668927378638,824.089072661046));
#144744=CARTESIAN_POINT('Ctrl Pts',(11.8093560737853,9.68668515431755,830.294264904198));
#144745=CARTESIAN_POINT('Ctrl Pts',(9.73230183022213,11.7719603645367,833.339020465625));
#144746=CARTESIAN_POINT('Ctrl Pts',(4.67917428517377,14.5398118424006,839.554081593592));
#144747=CARTESIAN_POINT('Ctrl Pts',(1.8037345722074,15.1674876194237,842.594410804555));
#144748=CARTESIAN_POINT('Ctrl Pts',(-3.94574904241249,14.7559442362928,
848.815752630463));
#144749=CARTESIAN_POINT('Ctrl Pts',(-6.70217019283721,13.7255397948671,
851.853272124192));
#144750=CARTESIAN_POINT('Ctrl Pts',(-11.3121227246376,10.263733864938,858.076876602063));
#144751=CARTESIAN_POINT('Ctrl Pts',(-13.0701273279823,7.90434178378963,
861.113701837503));
#144752=CARTESIAN_POINT('Ctrl Pts',(-15.0685969374762,2.49816738752234,
867.335160491185));
#144753=CARTESIAN_POINT('Ctrl Pts',(-15.2678536303296,-0.437331223543642,
870.373694270458));
#144754=CARTESIAN_POINT('Ctrl Pts',(-14.0198829821495,-6.06101357079894,
876.588896410459));
#144755=CARTESIAN_POINT('Ctrl Pts',(-12.5977171160585,-8.6362950379507,
879.63079255184));
#144756=CARTESIAN_POINT('Ctrl Pts',(-8.50671645746886,-12.6851234777784,
885.83624334546));
#144757=CARTESIAN_POINT('Ctrl Pts',(-5.91766454505476,-14.0804183360584,
888.882933729287));
#144758=CARTESIAN_POINT('Ctrl Pts',(-2.07890783483043,-14.8920661724229,
893.10863180637));
#144759=CARTESIAN_POINT('Ctrl Pts',(-1.04034966888609,-14.999999999953,
894.231686715025));
#144760=CARTESIAN_POINT('Ctrl Pts',(-6.7874927900391E-10,-15.0000000000001,
895.34999999927));
#144761=CARTESIAN_POINT('Ctrl Pts',(2.37243471590498E-9,-15.0000000000001,
992.18750000255));
#144762=CARTESIAN_POINT('Ctrl Pts',(-0.927957530816727,-15.0000000001469,
991.190001499619));
#144763=CARTESIAN_POINT('Ctrl Pts',(-1.85296309005188,-14.9143294957641,
990.187315211522));
#144764=CARTESIAN_POINT('Ctrl Pts',(-5.59527262211916,-14.2111492040552,
986.093806251726));
#144765=CARTESIAN_POINT('Ctrl Pts',(-8.21361976692825,-12.8756124686143,
983.03887894798));
#144766=CARTESIAN_POINT('Ctrl Pts',(-12.3917472570646,-8.92848976450734,
976.851202299565));
#144767=CARTESIAN_POINT('Ctrl Pts',(-13.873061125772,-6.38810058370437,
973.80261370812));
#144768=CARTESIAN_POINT('Ctrl Pts',(-15.2525780670412,-0.801972300954369,
967.60116828226));
#144769=CARTESIAN_POINT('Ctrl Pts',(-15.1235572878471,2.13685845381269,
964.557803828508));
#144770=CARTESIAN_POINT('Ctrl Pts',(-13.2574509380886,7.58519758337838,
958.345518804266));
#144771=CARTESIAN_POINT('Ctrl Pts',(-11.5573269768786,9.98642922314981,
955.306025368043));
#144772=CARTESIAN_POINT('Ctrl Pts',(-7.0346793751524,13.5579395357593,949.086263182288));
#144773=CARTESIAN_POINT('Ctrl Pts',(-4.30463460409252,14.6552860177948,
946.049059359286));
#144774=CARTESIAN_POINT('Ctrl Pts',(1.43374846857219,15.2070315904723,939.825684710236));
#144775=CARTESIAN_POINT('Ctrl Pts',(4.32303749816315,14.6498960878069,936.788713098054));
#144776=CARTESIAN_POINT('Ctrl Pts',(9.44483642742651,12.0042902169801,930.566113997223));
#144777=CARTESIAN_POINT('Ctrl Pts',(11.5716088123676,9.97000556149205,927.526923347156));
#144778=CARTESIAN_POINT('Ctrl Pts',(14.4419093540699,4.97311569195438,921.309327379516));
#144779=CARTESIAN_POINT('Ctrl Pts',(15.1274586611398,2.11082613967822,918.266231736795));
#144780=CARTESIAN_POINT('Ctrl Pts',(14.8335136101058,-3.64057867511896,
912.057331611732));
#144781=CARTESIAN_POINT('Ctrl Pts',(13.8599399514386,-6.41788133803346,
909.008860498642));
#144782=CARTESIAN_POINT('Ctrl Pts',(10.5014564938674,-11.0898991083664,
902.812009755185));
#144783=CARTESIAN_POINT('Ctrl Pts',(8.18043380872852,-12.8980569953977,
899.75693072865));
#144784=CARTESIAN_POINT('Ctrl Pts',(3.74578459492545,-14.6471922085484,
894.629748667918));
#144785=CARTESIAN_POINT('Ctrl Pts',(1.87950880952251,-14.9999999999999,
892.607858859883));
#144786=CARTESIAN_POINT('Ctrl Pts',(1.01686159492687E-10,-15.,890.587500000109));
#144787=CARTESIAN_POINT('Origin',(0.,0.,0.));
#144788=CARTESIAN_POINT('',(-1.80332313813543E-12,-15.0000000000001,692.149999999996));
#144789=CARTESIAN_POINT('',(-2.4458388347729E-10,-15.0000000000001,788.987499999474));
#144790=CARTESIAN_POINT('',(-1.83697019872103E-15,-15.,-1.82952505755738E-15));
#144791=CARTESIAN_POINT('Ctrl Pts',(-3.5241254359164E-12,-15.0000000000001,
692.149999999996));
#144792=CARTESIAN_POINT('Ctrl Pts',(2.27103459580004,-15.0000000000006,
694.591225517793));
#144793=CARTESIAN_POINT('Ctrl Pts',(4.51291959281525,-14.4846707381985,
697.011788622728));
#144794=CARTESIAN_POINT('Ctrl Pts',(8.64315435316608,-12.4767767750544,
701.96930729735));
#144795=CARTESIAN_POINT('Ctrl Pts',(10.4683168716844,-10.9901223189493,
704.442659371204));
#144796=CARTESIAN_POINT('Ctrl Pts',(13.6358594810391,-6.87878566199796,
710.026361856284));
#144797=CARTESIAN_POINT('Ctrl Pts',(14.70182367816,-4.13630823077973,713.084669264574));
#144798=CARTESIAN_POINT('Ctrl Pts',(15.1901873421449,1.5931409972409,719.26986734642));
#144799=CARTESIAN_POINT('Ctrl Pts',(14.602480182245,4.47613423322987,722.324420568784));
#144800=CARTESIAN_POINT('Ctrl Pts',(11.9104277463035,9.56187576526177,728.522269143782));
#144801=CARTESIAN_POINT('Ctrl Pts',(9.85546654182256,11.6686743298856,731.570297221167));
#144802=CARTESIAN_POINT('Ctrl Pts',(4.8340096828692,14.4889113802708,737.779960433601));
#144803=CARTESIAN_POINT('Ctrl Pts',(1.96533794957528,15.1472381812194,740.82271390217));
#144804=CARTESIAN_POINT('Ctrl Pts',(-3.78684542770849,14.7974126041612,
747.040810232922));
#144805=CARTESIAN_POINT('Ctrl Pts',(-6.55447001096606,13.7966352145626,
750.079776453113));
#144806=CARTESIAN_POINT('Ctrl Pts',(-11.2011708624236,10.384705053829,756.302591703863));
#144807=CARTESIAN_POINT('Ctrl Pts',(-12.9845668664545,8.04427576340637,
759.339471318412));
#144808=CARTESIAN_POINT('Ctrl Pts',(-15.0411951245362,2.65883896988886,
765.562735066766));
#144809=CARTESIAN_POINT('Ctrl Pts',(-15.2718217246421,-0.274436759551656,
768.600049449871));
#144810=CARTESIAN_POINT('Ctrl Pts',(-14.0831511308341,-5.91309660484774,
774.819382059842));
#144811=CARTESIAN_POINT('Ctrl Pts',(-12.6880307450419,-8.50343061672422,
777.859110474772));
#144812=CARTESIAN_POINT('Ctrl Pts',(-8.63749803694922,-12.5968495674121,
784.07070355884));
#144813=CARTESIAN_POINT('Ctrl Pts',(-6.06246619700213,-14.0189147492482,
787.11441114891));
#144814=CARTESIAN_POINT('Ctrl Pts',(-2.1806435024888,-14.8812351916921,
791.399796387356));
#144815=CARTESIAN_POINT('Ctrl Pts',(-1.0910039980068,-14.9999999998967,
792.577236359633));
#144816=CARTESIAN_POINT('Ctrl Pts',(-1.421166517801E-9,-15.0000000000001,
793.749999998472));
#144817=CARTESIAN_POINT('Ctrl Pts',(1.01688518716614E-10,-15.0000000000002,
890.587500000109));
#144818=CARTESIAN_POINT('Ctrl Pts',(-0.977428461994903,-15.0000000000003,
889.536823225789));
#144819=CARTESIAN_POINT('Ctrl Pts',(-1.95255362472441,-14.9048231302732,
888.481098490165));
#144820=CARTESIAN_POINT('Ctrl Pts',(-5.73749331040952,-14.1545187708565,
884.329403256852));
#144821=CARTESIAN_POINT('Ctrl Pts',(-8.34325300287303,-12.7925966847513,
881.27836923249));
#144822=CARTESIAN_POINT('Ctrl Pts',(-12.4834370889708,-8.80020283642223,
875.082171224733));
#144823=CARTESIAN_POINT('Ctrl Pts',(-13.9388522127874,-6.24418165447485,
872.036841463946));
#144824=CARTESIAN_POINT('Ctrl Pts',(-15.2604165047268,-0.640780879139956,
865.828562924129));
#144825=CARTESIAN_POINT('Ctrl Pts',(-15.1003526217916,2.29686927308867,
862.787680347582));
#144826=CARTESIAN_POINT('Ctrl Pts',(-13.1753791252392,7.72725137941694,
856.570514872512));
#144827=CARTESIAN_POINT('Ctrl Pts',(-11.449446160624,10.1101637037372,853.532588444096));
#144828=CARTESIAN_POINT('Ctrl Pts',(-6.88731259235128,13.6335360655616,
847.310126440447));
#144829=CARTESIAN_POINT('Ctrl Pts',(-4.1455159194855,14.7011388963839,844.273449042886));
#144830=CARTESIAN_POINT('Ctrl Pts',(1.59873478344331,15.1905640636383,838.049974645588));
#144831=CARTESIAN_POINT('Ctrl Pts',(4.48211981955633,14.6019231598022,835.011896556154));
#144832=CARTESIAN_POINT('Ctrl Pts',(9.57397060596606,11.9014034615129,828.791814175797));
#144833=CARTESIAN_POINT('Ctrl Pts',(11.6787211549985,9.84410097360831,825.75048940482));
#144834=CARTESIAN_POINT('Ctrl Pts',(14.4940300860886,4.81833720724832,819.537643727229));
#144835=CARTESIAN_POINT('Ctrl Pts',(15.1489947663658,1.94897957664842,816.491511094136));
#144836=CARTESIAN_POINT('Ctrl Pts',(14.7940850656901,-3.79613331868855,
810.289403379063));
#144837=CARTESIAN_POINT('Ctrl Pts',(13.79175459564,-6.56276165432192,807.237132215546));
#144838=CARTESIAN_POINT('Ctrl Pts',(10.385580112573,-11.1983334067647,801.046630210449));
#144839=CARTESIAN_POINT('Ctrl Pts',(8.04509568799686,-12.9820150209759,
797.988053372213));
#144840=CARTESIAN_POINT('Ctrl Pts',(3.64287626884949,-14.66683091111,792.919331437006));
#144841=CARTESIAN_POINT('Ctrl Pts',(1.82776494649211,-15.0000000000597,
790.952237321105));
#144842=CARTESIAN_POINT('Ctrl Pts',(-4.89162321759551E-10,-15.0000000000001,
788.987499999474));
#144843=CARTESIAN_POINT('Origin',(0.,0.,-11.4051836540916));
#144844=CARTESIAN_POINT('',(-39.,3.56961574259503E-12,767.551815642455));
#144845=CARTESIAN_POINT('',(-39.,-1.80076817690714E-11,764.385684357557));
#144846=CARTESIAN_POINT('',(-39.,-4.77612251667468E-15,-11.4051836540916));
#144847=CARTESIAN_POINT('',(1.56487907968316,-38.9685918845674,692.));
#144848=CARTESIAN_POINT('Ctrl Pts',(-39.,7.1880001950575E-12,767.551815642455));
#144849=CARTESIAN_POINT('Ctrl Pts',(-39.,0.444599787572262,767.367213541182));
#144850=CARTESIAN_POINT('Ctrl Pts',(-38.992397846984,0.889538753063548,
767.182470609977));
#144851=CARTESIAN_POINT('Ctrl Pts',(-38.7890284837619,6.82867978239275,
764.716482221239));
#144852=CARTESIAN_POINT('Ctrl Pts',(-37.4402879297879,12.2245802425215,
762.458043468178));
#144853=CARTESIAN_POINT('Ctrl Pts',(-32.6014351065545,22.0997120942476,
757.90889018916));
#144854=CARTESIAN_POINT('Ctrl Pts',(-29.1621326216746,26.4734173647096,
755.64917874153));
#144855=CARTESIAN_POINT('Ctrl Pts',(-20.7028282263121,33.5056264037719,
751.086638313621));
#144856=CARTESIAN_POINT('Ctrl Pts',(-15.7768863592026,36.0878204316542,
748.834245115048));
#144857=CARTESIAN_POINT('Ctrl Pts',(-5.18442159666645,39.0428894729064,
744.268269289717));
#144858=CARTESIAN_POINT('Ctrl Pts',(0.365808868099208,39.383788448861,742.015279419795));
#144859=CARTESIAN_POINT('Ctrl Pts',(11.2391673468008,37.748076109223,737.457150275462));
#144860=CARTESIAN_POINT('Ctrl Pts',(16.4443409752546,35.7884046024072,735.199214991829));
#144861=CARTESIAN_POINT('Ctrl Pts',(25.6986365833266,29.8467189665087,730.646129090551));
#144862=CARTESIAN_POINT('Ctrl Pts',(29.6484851419845,25.927241388788,728.3887560339));
#144863=CARTESIAN_POINT('Ctrl Pts',(35.6615894594247,16.7177367431117,723.823289708095));
#144864=CARTESIAN_POINT('Ctrl Pts',(37.6604489060644,11.5291626374632,721.572274339719));
#144865=CARTESIAN_POINT('Ctrl Pts',(39.3798653450543,0.668787227458401,
717.008539998774));
#144866=CARTESIAN_POINT('Ctrl Pts',(39.0813650471648,-4.88478403069311,
714.751600946893));
#144867=CARTESIAN_POINT('Ctrl Pts',(36.2080678936678,-15.4990648548602,
710.200272791918));
#144868=CARTESIAN_POINT('Ctrl Pts',(33.6630934166401,-20.4463943747878,
707.941434691088));
#144869=CARTESIAN_POINT('Ctrl Pts',(26.6958917991014,-28.9579870927979,
703.380807166622));
#144870=CARTESIAN_POINT('Ctrl Pts',(22.3503480195058,-32.4300148760212,
701.127610053241));
#144871=CARTESIAN_POINT('Ctrl Pts',(12.4910508591148,-37.3559251748377,
696.551440503674));
#144872=CARTESIAN_POINT('Ctrl Pts',(7.08162027719987,-38.7470536541486,
694.289319896425));
#144873=CARTESIAN_POINT('Ctrl Pts',(1.56487907968316,-38.9685918845674,
692.000000000001));
#144874=CARTESIAN_POINT('',(9.11627411387425,-37.91956679975,692.));
#144875=CARTESIAN_POINT('Origin',(0.,0.,692.));
#144876=CARTESIAN_POINT('Ctrl Pts',(9.1162741138742,-37.9195667997501,692.));
#144877=CARTESIAN_POINT('Ctrl Pts',(14.1364514273045,-36.7126618598502,
694.141991806554));
#144878=CARTESIAN_POINT('Ctrl Pts',(18.8687364296366,-34.5200872168667,
696.25895288502));
#144879=CARTESIAN_POINT('Ctrl Pts',(27.2024632672717,-28.4199203974411,
700.546668576892));
#144880=CARTESIAN_POINT('Ctrl Pts',(30.7225562439626,-24.5721582467486,
702.661883267291));
#144881=CARTESIAN_POINT('Ctrl Pts',(36.2324554963202,-15.4420798166754,
707.089320277153));
#144882=CARTESIAN_POINT('Ctrl Pts',(38.0466274529669,-10.1829991503243,
709.344111975511));
#144883=CARTESIAN_POINT('Ctrl Pts',(39.3789466567602,0.734164630120643,
713.901490499695));
#144884=CARTESIAN_POINT('Ctrl Pts',(38.8826514753387,6.27508587776081,716.159640762425));
#144885=CARTESIAN_POINT('Ctrl Pts',(35.6324146729093,16.7793046237023,720.714080390645));
#144886=CARTESIAN_POINT('Ctrl Pts',(32.9140276449878,21.6307625893325,722.969013463136));
#144887=CARTESIAN_POINT('Ctrl Pts',(25.6512770191788,29.8872448531897,727.534034394676));
#144888=CARTESIAN_POINT('Ctrl Pts',(21.1864018163163,33.2019407361348,729.785369990551));
#144889=CARTESIAN_POINT('Ctrl Pts',(11.1789157366835,37.7662650004625,734.349697976576));
#144890=CARTESIAN_POINT('Ctrl Pts',(5.74390122675569,38.9648870548074,736.609589868737));
#144891=CARTESIAN_POINT('Ctrl Pts',(-5.25341170921003,39.0335708226067,
741.158932569111));
#144892=CARTESIAN_POINT('Ctrl Pts',(-10.6985856030828,37.9048715375236,
743.417488861358));
#144893=CARTESIAN_POINT('Ctrl Pts',(-20.7607467890849,33.4695665217669,
747.978260294979));
#144894=CARTESIAN_POINT('Ctrl Pts',(-25.2673353820903,30.2124000190225,
750.23016450274));
#144895=CARTESIAN_POINT('Ctrl Pts',(-32.63599301526,22.0485276733406,754.796393500793));
#144896=CARTESIAN_POINT('Ctrl Pts',(-35.4166106518228,17.2308001327554,
757.050113502379));
#144897=CARTESIAN_POINT('Ctrl Pts',(-38.3641920260956,8.1148275827748,761.021668280858));
#144898=CARTESIAN_POINT('Ctrl Pts',(-39.0000000000038,4.06368217415025,
762.698404495439));
#144899=CARTESIAN_POINT('Ctrl Pts',(-39.,-3.61188856601302E-11,764.385684357557));
#144900=CARTESIAN_POINT('Origin',(0.,0.,-11.4051836540916));
#144901=CARTESIAN_POINT('',(-39.,-4.02744219736708E-14,869.151815642458));
#144902=CARTESIAN_POINT('',(-39.,-8.91515698045976E-11,865.985684357616));
#144903=CARTESIAN_POINT('',(-39.,-4.77612251667468E-15,-11.4051836540916));
#144904=CARTESIAN_POINT('Ctrl Pts',(-39.,5.88418203051333E-14,869.151815642458));
#144905=CARTESIAN_POINT('Ctrl Pts',(-39.,5.43573553489539,866.894846049194));
#144906=CARTESIAN_POINT('Ctrl Pts',(-37.8631212524949,10.8138469940783,
864.667660265692));
#144907=CARTESIAN_POINT('Ctrl Pts',(-33.4370296592246,20.8135523395336,
860.132186162968));
#144908=CARTESIAN_POINT('Ctrl Pts',(-30.1721615248585,25.3151904067071,
857.873657366882));
#144909=CARTESIAN_POINT('Ctrl Pts',(-21.9967696512043,32.6710375348237,
853.324209146));
#144910=CARTESIAN_POINT('Ctrl Pts',(-17.1720111301126,35.4454630157482,
851.064390556249));
#144911=CARTESIAN_POINT('Ctrl Pts',(-6.70052089744381,38.8115381378829,
846.500025433587));
#144912=CARTESIAN_POINT('Ctrl Pts',(-1.16770832885968,39.3684107232863,
844.248705172239));
#144913=CARTESIAN_POINT('Ctrl Pts',(9.76154258437761,38.1567207763231,839.683712548098));
#144914=CARTESIAN_POINT('Ctrl Pts',(15.0383962019526,36.4013826067875,837.428730640023));
#144915=CARTESIAN_POINT('Ctrl Pts',(24.51549939447,30.8257647944294,832.874370577483));
#144916=CARTESIAN_POINT('Ctrl Pts',(28.6141467064143,27.0642110841891,830.616212538848));
#144917=CARTESIAN_POINT('Ctrl Pts',(34.981969791075,18.096988705713,826.058741973881));
#144918=CARTESIAN_POINT('Ctrl Pts',(37.1828994118403,12.9877066390436,823.803998730174));
#144919=CARTESIAN_POINT('Ctrl Pts',(39.3241345362518,2.20024120607044,819.237839384974));
#144920=CARTESIAN_POINT('Ctrl Pts',(39.2420353216892,-3.35949143992115,
816.986391935878));
#144921=CARTESIAN_POINT('Ctrl Pts',(36.7838234711582,-14.0780771294997,
812.424161558999));
#144922=CARTESIAN_POINT('Ctrl Pts',(34.4343093017528,-19.1178375038457,
810.16482214988));
#144923=CARTESIAN_POINT('Ctrl Pts',(27.8063368808782,-27.893884243463,805.617939454984));
#144924=CARTESIAN_POINT('Ctrl Pts',(23.5963270574983,-31.5352943432299,
803.356306298561));
#144925=CARTESIAN_POINT('Ctrl Pts',(13.9552638353624,-36.8304721490037,
798.792907898438));
#144926=CARTESIAN_POINT('Ctrl Pts',(8.62872741855903,-38.4289357163304,
796.541140708907));
#144927=CARTESIAN_POINT('Ctrl Pts',(-2.3319679143772,-39.3164874371797,
791.975565719672));
#144928=CARTESIAN_POINT('Ctrl Pts',(-7.8460057578923,-38.5960507447532,
789.721660590033));
#144929=CARTESIAN_POINT('Ctrl Pts',(-18.2099342535552,-34.9232527989276,
785.165399093187));
#144930=CARTESIAN_POINT('Ctrl Pts',(-22.9483474087012,-32.0094593548667,
782.907430332298));
#144931=CARTESIAN_POINT('Ctrl Pts',(-30.9042815915061,-24.4165483955361,
778.352121306444));
#144932=CARTESIAN_POINT('Ctrl Pts',(-34.0365945401134,-19.8182183286086,
776.096150894115));
#144933=CARTESIAN_POINT('Ctrl Pts',(-38.021049427416,-10.0464108930014,
771.715153884756));
#144934=CARTESIAN_POINT('Ctrl Pts',(-39.,-5.04360596152766,769.645969271254));
#144935=CARTESIAN_POINT('Ctrl Pts',(-39.,7.16232628761304E-12,767.551815642455));
#144936=CARTESIAN_POINT('Ctrl Pts',(-39.,-3.61427554551597E-11,764.385684357557));
#144937=CARTESIAN_POINT('Ctrl Pts',(-38.9999999999987,-1.41200103218787,
764.971960745502));
#144938=CARTESIAN_POINT('Ctrl Pts',(-38.9233013074596,-2.82623296434554,
765.557781691743));
#144939=CARTESIAN_POINT('Ctrl Pts',(-38.1722588338924,-9.70013164892058,
768.420594268634));
#144940=CARTESIAN_POINT('Ctrl Pts',(-36.4255115393919,-14.9801180847204,
770.676769353789));
#144941=CARTESIAN_POINT('Ctrl Pts',(-30.8647629112545,-24.4662881566758,
775.241027877367));
#144942=CARTESIAN_POINT('Ctrl Pts',(-27.1116891258472,-28.5690135328132,
777.49208368091));
#144943=CARTESIAN_POINT('Ctrl Pts',(-18.1545878659332,-34.9523543053397,
782.057206704967));
#144944=CARTESIAN_POINT('Ctrl Pts',(-13.0472248932953,-37.1620661313272,
784.315434277579));
#144945=CARTESIAN_POINT('Ctrl Pts',(-2.26362020088496,-39.3204680063181,
788.867220301099));
#144946=CARTESIAN_POINT('Ctrl Pts',(3.29737917386447,-39.2474740090443,
791.125283740846));
#144947=CARTESIAN_POINT('Ctrl Pts',(14.0188203721114,-36.8061204904945,
795.68439528666));
#144948=CARTESIAN_POINT('Ctrl Pts',(19.0626052570436,-34.4651011006093,
797.936948847296));
#144949=CARTESIAN_POINT('Ctrl Pts',(27.8486672076749,-27.8512893435151,
802.503067329164));
#144950=CARTESIAN_POINT('Ctrl Pts',(31.4942080166653,-23.6505762003017,
804.755886017233));
#144951=CARTESIAN_POINT('Ctrl Pts',(36.8068355358466,-14.018608246568,809.317379629089));
#144952=CARTESIAN_POINT('Ctrl Pts',(38.4147344977359,-8.69228539662842,
811.576563989154));
#144953=CARTESIAN_POINT('Ctrl Pts',(39.3201679817139,2.26694917916401,816.126943426164));
#144954=CARTESIAN_POINT('Ctrl Pts',(38.6088754210609,7.78300555017287,818.384528116055));
#144955=CARTESIAN_POINT('Ctrl Pts',(34.9528871370198,18.1528208293289,822.947789636676));
#144956=CARTESIAN_POINT('Ctrl Pts',(32.0482572340742,22.8941072466728,825.198840226943));
#144957=CARTESIAN_POINT('Ctrl Pts',(24.4682514825065,30.8635363641544,829.764524896469));
#144958=CARTESIAN_POINT('Ctrl Pts',(19.8747124247098,34.0035355777327,832.021254263112));
#144959=CARTESIAN_POINT('Ctrl Pts',(9.69813407717675,38.1729616484813,836.575344807772));
#144960=CARTESIAN_POINT('Ctrl Pts',(4.22398187768683,39.1585705743747,838.833253131089));
#144961=CARTESIAN_POINT('Ctrl Pts',(-6.76575577782906,38.8000042504229,
843.39056952592));
#144962=CARTESIAN_POINT('Ctrl Pts',(-12.1627992121961,37.4605290148405,
845.643944977488));
#144963=CARTESIAN_POINT('Ctrl Pts',(-22.045652839921,32.6378433627528,850.209765718567));
#144964=CARTESIAN_POINT('Ctrl Pts',(-26.4229593532984,29.2072045838926,
852.461859088474));
#144965=CARTESIAN_POINT('Ctrl Pts',(-33.4707468218834,20.76022457522,857.025202485842));
#144966=CARTESIAN_POINT('Ctrl Pts',(-36.0620133214413,15.8361821387683,
859.285407332465));
#144967=CARTESIAN_POINT('Ctrl Pts',(-38.5138914172955,7.10187197100778,
863.037292523889));
#144968=CARTESIAN_POINT('Ctrl Pts',(-39.0000000000163,3.554560955032,864.50979651469));
#144969=CARTESIAN_POINT('Ctrl Pts',(-39.,-1.78223547031564E-10,865.985684357616));
#144970=CARTESIAN_POINT('Origin',(0.,0.,-11.4051836540916));
#144971=CARTESIAN_POINT('',(-39.,-1.05587355240895E-11,970.751815642467));
#144972=CARTESIAN_POINT('',(-39.,-1.22179591926513E-11,967.585684357552));
#144973=CARTESIAN_POINT('',(-39.,-4.77612251667468E-15,-11.4051836540916));
#144974=CARTESIAN_POINT('Ctrl Pts',(-39.,-2.11605732935993E-11,970.751815642467));
#144975=CARTESIAN_POINT('Ctrl Pts',(-39.0000000000027,4.92045984381282,
968.708793464306));
#144976=CARTESIAN_POINT('Ctrl Pts',(-38.0680720015819,9.80530383712027,
966.688880125693));
#144977=CARTESIAN_POINT('Ctrl Pts',(-34.2201085718197,19.4989496685401,
962.358617547347));
#144978=CARTESIAN_POINT('Ctrl Pts',(-31.1327799735451,24.1239656923328,
960.105203795389));
#144979=CARTESIAN_POINT('Ctrl Pts',(-23.2507510474625,31.7905365139141,
955.547965852891));
#144980=CARTESIAN_POINT('Ctrl Pts',(-18.5404717310421,34.7488123608543,
953.290056619791));
#144981=CARTESIAN_POINT('Ctrl Pts',(-8.20992752944213,38.5206638305759,
948.735872244936));
#144982=CARTESIAN_POINT('Ctrl Pts',(-2.69967510934749,39.2933179652049,
946.479202197762));
#144983=CARTESIAN_POINT('Ctrl Pts',(8.27075550201749,38.5074729519727,941.913498726737));
#144984=CARTESIAN_POINT('Ctrl Pts',(13.6110658153455,36.9590035688653,939.662442975147));
#144985=CARTESIAN_POINT('Ctrl Pts',(23.2975428355124,31.7560210478991,935.099228184755));
#144986=CARTESIAN_POINT('Ctrl Pts',(27.5383720174836,28.1576417514627,932.841580577787));
#144987=CARTESIAN_POINT('Ctrl Pts',(34.250086087367,19.4468375978943,928.291292528354));
#144988=CARTESIAN_POINT('Ctrl Pts',(36.6487984492457,14.4267332905264,926.032071881529));
#144989=CARTESIAN_POINT('Ctrl Pts',(39.2088126415577,3.72878507586251,921.470497515674));
#144990=CARTESIAN_POINT('Ctrl Pts',(39.3432049830526,-1.8315782015685,919.217712942267));
#144991=CARTESIAN_POINT('Ctrl Pts',(37.3029756255119,-12.637803275991,914.651603230416));
#144992=CARTESIAN_POINT('Ctrl Pts',(35.1513049600264,-17.7652326337268,
912.399018510629));
#144993=CARTESIAN_POINT('Ctrl Pts',(28.8703393170326,-26.790676818201,907.839979854173));
#144994=CARTESIAN_POINT('Ctrl Pts',(24.8088327264741,-30.5899530438165,
905.581929779443));
#144995=CARTESIAN_POINT('Ctrl Pts',(15.3839930471174,-36.2571617911556,
901.030043861947));
#144996=CARTESIAN_POINT('Ctrl Pts',(10.1204684588554,-38.0635275467779,
898.771882771897));
#144997=CARTESIAN_POINT('Ctrl Pts',(-0.799685057268203,-39.3775662049388,
894.206730309309));
#144998=CARTESIAN_POINT('Ctrl Pts',(-6.33707553182674,-38.8725380651309,
891.95568238689));
#144999=CARTESIAN_POINT('Ctrl Pts',(-16.8364085685143,-35.605577080513,
887.391460074885));
#145000=CARTESIAN_POINT('Ctrl Pts',(-21.6836447425657,-32.8790733233354,
885.135228979051));
#145001=CARTESIAN_POINT('Ctrl Pts',(-29.9284323367762,-25.6033471660073,
880.582834717982));
#145002=CARTESIAN_POINT('Ctrl Pts',(-33.2374777722068,-21.1310829147382,
878.324314875799));
#145003=CARTESIAN_POINT('Ctrl Pts',(-37.7845490861634,-11.1159588568865,
873.76472521789));
#145004=CARTESIAN_POINT('Ctrl Pts',(-38.9738384760769,-5.6820241810347,
871.5110466467));
#145005=CARTESIAN_POINT('Ctrl Pts',(-38.9998577080699,-0.121656064835777,
869.202328408837));
#145006=CARTESIAN_POINT('Ctrl Pts',(-39.,-0.0608242949889622,869.177070473831));
#145007=CARTESIAN_POINT('Ctrl Pts',(-39.,-2.5360886051307E-15,869.151815642458));
#145008=CARTESIAN_POINT('Ctrl Pts',(-39.,-1.78279613294308E-10,865.985684357616));
#145009=CARTESIAN_POINT('Ctrl Pts',(-38.9999999999912,-1.91614269570151,
866.781285205448));
#145010=CARTESIAN_POINT('Ctrl Pts',(-38.8586492523547,-3.83569992409224,
867.574718006289));
#145011=CARTESIAN_POINT('Ctrl Pts',(-37.7660819373123,-11.1780366895091,
870.654775329797));
#145012=CARTESIAN_POINT('Ctrl Pts',(-35.8156431428152,-16.3850268959936,
872.906032745858));
#145013=CARTESIAN_POINT('Ctrl Pts',(-29.8889018752433,-25.6496346055645,
877.472074254061));
#145014=CARTESIAN_POINT('Ctrl Pts',(-25.9764906847373,-29.6051152359186,
879.72747839053));
#145015=CARTESIAN_POINT('Ctrl Pts',(-16.7779944725433,-35.6333243471609,
884.283725350576));
#145016=CARTESIAN_POINT('Ctrl Pts',(-11.5901967615144,-37.641764954479,
886.54181709808));
#145017=CARTESIAN_POINT('Ctrl Pts',(-0.732831366644527,-39.3786413109767,
891.097209752753));
#145018=CARTESIAN_POINT('Ctrl Pts',(4.82065298608422,-39.089449133969,893.351573189743));
#145019=CARTESIAN_POINT('Ctrl Pts',(15.4396725026777,-36.2333177596016,
897.916911861676));
#145020=CARTESIAN_POINT('Ctrl Pts',(20.3888906201009,-33.6975651182713,
900.168458710607));
#145021=CARTESIAN_POINT('Ctrl Pts',(28.9126401245583,-26.74545823846,904.732309528255));
#145022=CARTESIAN_POINT('Ctrl Pts',(32.394104696192,-22.4026799003182,906.993115408434));
#145023=CARTESIAN_POINT('Ctrl Pts',(37.3249232093689,-12.5724135651128,
911.541156287731));
#145024=CARTESIAN_POINT('Ctrl Pts',(38.7238464068962,-7.19056169986337,
913.80009408905));
#145025=CARTESIAN_POINT('Ctrl Pts',(39.2022363161185,3.79561924881892,918.361661918849));
#145026=CARTESIAN_POINT('Ctrl Pts',(38.2771142429207,9.27849894774687,920.613301618383));
#145027=CARTESIAN_POINT('Ctrl Pts',(34.2196133974516,19.5003906151297,925.179514617699));
#145028=CARTESIAN_POINT('Ctrl Pts',(31.1308192063526,24.1269579025388,927.433762820568));
#145029=CARTESIAN_POINT('Ctrl Pts',(23.2455746018107,31.7944851846347,931.992193752191));
#145030=CARTESIAN_POINT('Ctrl Pts',(18.5339271312125,34.7524557069582,934.250471010959));
#145031=CARTESIAN_POINT('Ctrl Pts',(8.20428422704431,38.5214691152723,938.80397296253));
#145032=CARTESIAN_POINT('Ctrl Pts',(2.69680821024608,39.2931256125301,941.059490457559));
#145033=CARTESIAN_POINT('Ctrl Pts',(-8.27114295907375,38.5074321825743,
945.624163024791));
#145034=CARTESIAN_POINT('Ctrl Pts',(-13.611727879551,36.9588039026025,947.875340054341));
#145035=CARTESIAN_POINT('Ctrl Pts',(-23.3013168801336,31.7538378152413,
952.440078615087));
#145036=CARTESIAN_POINT('Ctrl Pts',(-27.5442735200595,28.1525304217482,
954.699138598242));
#145037=CARTESIAN_POINT('Ctrl Pts',(-34.2556024106436,19.4371253352674,
959.250730670246));
#145038=CARTESIAN_POINT('Ctrl Pts',(-36.6529021409899,14.4163237958122,
961.509989737668));
#145039=CARTESIAN_POINT('Ctrl Pts',(-38.6433191435739,6.08814410720707,
965.060909914876));
#145040=CARTESIAN_POINT('Ctrl Pts',(-39.0000000000019,3.04469482380837,
966.3214978286));
#145041=CARTESIAN_POINT('Ctrl Pts',(-39.,-2.44598785670291E-11,967.585684357552));
#145042=CARTESIAN_POINT('Origin',(0.,0.,-11.4051836540916));
#145043=CARTESIAN_POINT('',(-39.,-1.20381251188915E-10,1072.35181564256));
#145044=CARTESIAN_POINT('',(-39.,3.32285671526687E-12,1069.18568435754));
#145045=CARTESIAN_POINT('',(-39.,-4.77612251667468E-15,-11.4051836540916));
#145046=CARTESIAN_POINT('Ctrl Pts',(-39.,-2.40734654433084E-10,1072.35181564256));
#145047=CARTESIAN_POINT('Ctrl Pts',(-39.0000000000272,4.40669534644803,
1070.52211341727));
#145048=CARTESIAN_POINT('Ctrl Pts',(-38.2519218970919,8.79514383817135,
1068.7075610424));
#145049=CARTESIAN_POINT('Ctrl Pts',(-34.95323281987,18.1522402513944,1064.58998699583));
#145050=CARTESIAN_POINT('Ctrl Pts',(-32.0485147457729,22.8938143039188,
1062.3388216931));
#145051=CARTESIAN_POINT('Ctrl Pts',(-24.4702653485043,30.86144123232,1057.77418130979));
#145052=CARTESIAN_POINT('Ctrl Pts',(-19.8794677561395,34.0003032109931,
1055.51861143013));
#145053=CARTESIAN_POINT('Ctrl Pts',(-9.70545079215384,38.1712465858339,
1050.96519208669));
#145054=CARTESIAN_POINT('Ctrl Pts',(-4.23045115476902,39.1580106813823,
1048.70690006653));
#145055=CARTESIAN_POINT('Ctrl Pts',(6.76233223196223,38.8008860452023,1044.14837968156));
#145056=CARTESIAN_POINT('Ctrl Pts',(12.1614862664044,37.4612506269753,1041.89417657098));
#145057=CARTESIAN_POINT('Ctrl Pts',(22.0451309758311,32.6380171285112,1037.32796040776));
#145058=CARTESIAN_POINT('Ctrl Pts',(26.4216655732491,29.2081754381505,1035.07630071444));
#145059=CARTESIAN_POINT('Ctrl Pts',(33.4671612900492,20.7651016180944,1030.51479696608));
#145060=CARTESIAN_POINT('Ctrl Pts',(36.0577483833216,15.8446981587664,1028.25589378643));
#145061=CARTESIAN_POINT('Ctrl Pts',(39.0335483194285,5.25736747886637,1023.7077446547));
#145062=CARTESIAN_POINT('Ctrl Pts',(39.3849169238395,-0.297496027210565,
1021.44701543651));
#145063=CARTESIAN_POINT('Ctrl Pts',(37.7664474293011,-11.1771274820797,
1016.88312363906));
#145064=CARTESIAN_POINT('Ctrl Pts',(35.8158523018511,-16.3847920769605,
1014.63159586748));
#145065=CARTESIAN_POINT('Ctrl Pts',(29.8899703813292,-25.6478722084131,
1010.06628145815));
#145066=CARTESIAN_POINT('Ctrl Pts',(25.9796475946162,-29.6018969664766,
1007.81187290831));
#145067=CARTESIAN_POINT('Ctrl Pts',(16.784203177988,-35.630403856542,1003.25656263356));
#145068=CARTESIAN_POINT('Ctrl Pts',(11.5967237879651,-37.639755608264,1000.99845840472));
#145069=CARTESIAN_POINT('Ctrl Pts',(0.737286909422714,-39.3788926554812,
996.442122710503));
#145070=CARTESIAN_POINT('Ctrl Pts',(-4.81870463978068,-39.0900264694501,
994.186770501551));
#145071=CARTESIAN_POINT('Ctrl Pts',(-15.4393561983312,-36.2333495478132,
989.620718069404));
#145072=CARTESIAN_POINT('Ctrl Pts',(-20.3879904968142,-33.6979990799886,
987.369448125984));
#145073=CARTESIAN_POINT('Ctrl Pts',(-28.9085862874412,-26.7490646841177,
982.807436091745));
#145074=CARTESIAN_POINT('Ctrl Pts',(-32.3884041854296,-22.4099933719744,
980.548212396911));
#145075=CARTESIAN_POINT('Ctrl Pts',(-37.3223319393225,-12.5816239153753,
976.000161533641));
#145076=CARTESIAN_POINT('Ctrl Pts',(-38.7232174803287,-7.19658426606107,
973.73990653827));
#145077=CARTESIAN_POINT('Ctrl Pts',(-38.9876796771853,-1.13252041238029,
971.222048993232));
#145078=CARTESIAN_POINT('Ctrl Pts',(-38.9999999999997,-0.566005030289253,
970.986826366361));
#145079=CARTESIAN_POINT('Ctrl Pts',(-39.,-2.11239359337867E-11,970.751815642467));
#145080=CARTESIAN_POINT('Ctrl Pts',(-39.,-2.45281572830436E-11,967.585684357552));
#145081=CARTESIAN_POINT('Ctrl Pts',(-38.9999999999985,-2.42407756834171,
968.592184642248));
#145082=CARTESIAN_POINT('Ctrl Pts',(-38.7738086935458,-4.85115479483614,
969.595638499149));
#145083=CARTESIAN_POINT('Ctrl Pts',(-37.2993818336415,-12.6484040123052,
972.890497539515));
#145084=CARTESIAN_POINT('Ctrl Pts',(-35.1462500049703,-17.7752282487208,
975.143115035084));
#145085=CARTESIAN_POINT('Ctrl Pts',(-28.8627288744489,-26.7988743877845,
979.70207752624));
#145086=CARTESIAN_POINT('Ctrl Pts',(-24.8001245103406,-30.5970173517883,
981.960114319475));
#145087=CARTESIAN_POINT('Ctrl Pts',(-15.3736672565857,-36.2615382735034,
986.51210400875));
#145088=CARTESIAN_POINT('Ctrl Pts',(-10.1096591876265,-38.0663982542976,
988.770196174658));
#145089=CARTESIAN_POINT('Ctrl Pts',(0.810854819229557,-39.3773377218996,
993.335378945768));
#145090=CARTESIAN_POINT('Ctrl Pts',(6.34808589841638,-38.8707401479934,
995.586418997613));
#145091=CARTESIAN_POINT('Ctrl Pts',(16.8464795008,-35.6008123867018,1000.15060324527));
#145092=CARTESIAN_POINT('Ctrl Pts',(21.6929555690272,-32.8729312097374,
1002.40689298906));
#145093=CARTESIAN_POINT('Ctrl Pts',(29.935698723851,-25.5948553290272,1006.9591977836));
#145094=CARTESIAN_POINT('Ctrl Pts',(33.2434856325897,-21.121642604465,1009.21774126761));
#145095=CARTESIAN_POINT('Ctrl Pts',(37.7877155770828,-11.1051856131721,
1013.77742081939));
#145096=CARTESIAN_POINT('Ctrl Pts',(38.9754514576547,-5.67093770419533,
1016.03105656495));
#145097=CARTESIAN_POINT('Ctrl Pts',(39.0237879021348,5.32646418474255,1020.59728343689));
#145098=CARTESIAN_POINT('Ctrl Pts',(37.8846828359875,10.7689854040637,1022.84923656495));
#145099=CARTESIAN_POINT('Ctrl Pts',(33.4311239339301,20.8230342782236,1027.40987077843));
#145100=CARTESIAN_POINT('Ctrl Pts',(30.1649685930785,25.3237652473569,1029.66837156485));
#145101=CARTESIAN_POINT('Ctrl Pts',(21.9874860148398,32.6772820623094,1034.21792943879));
#145102=CARTESIAN_POINT('Ctrl Pts',(17.1619696342435,35.4503243055008,1036.47767198415));
#145103=CARTESIAN_POINT('Ctrl Pts',(6.68953916182195,38.8134322237963,1041.04207544429));
#145104=CARTESIAN_POINT('Ctrl Pts',(1.1565875492231,39.3687375276673,1043.2933800649));
#145105=CARTESIAN_POINT('Ctrl Pts',(-9.77230555535638,38.1539649824231,
1047.85834285374));
#145106=CARTESIAN_POINT('Ctrl Pts',(-15.0486747245861,36.3971342631628,
1050.11337594687));
#145107=CARTESIAN_POINT('Ctrl Pts',(-24.5242177640814,30.8188324763402,
1054.66765286728));
#145108=CARTESIAN_POINT('Ctrl Pts',(-28.6218089207113,27.0561169484875,
1056.92581964375));
#145109=CARTESIAN_POINT('Ctrl Pts',(-34.9871035270197,18.0870581421282,
1061.48338582739));
#145110=CARTESIAN_POINT('Ctrl Pts',(-37.186573660034,12.9771776024501,1063.73807891462));
#145111=CARTESIAN_POINT('Ctrl Pts',(-38.752066982733,5.07858103950625,1067.08124972354));
#145112=CARTESIAN_POINT('Ctrl Pts',(-39.,2.53802064523472,1068.13187381312));
#145113=CARTESIAN_POINT('Ctrl Pts',(-39.,6.6818772737065E-12,1069.18568435754));
#145114=CARTESIAN_POINT('Origin',(0.,0.,-11.4051836540916));
#145115=CARTESIAN_POINT('',(-39.,-1.9327470101175E-12,1173.95181564246));
#145116=CARTESIAN_POINT('',(-39.,7.6522481211573E-11,1170.78568435748));
#145117=CARTESIAN_POINT('',(-39.,-4.77612251667468E-15,-11.4051836540916));
#145118=CARTESIAN_POINT('Ctrl Pts',(-39.,-3.89355214736042E-12,1173.95181564246));
#145119=CARTESIAN_POINT('Ctrl Pts',(-39.0000000000004,3.89628960201103,
1172.33403878377));
#145120=CARTESIAN_POINT('Ctrl Pts',(-38.4156384927199,7.78182406127406,
1170.72444552087));
#145121=CARTESIAN_POINT('Ctrl Pts',(-35.6349007362537,16.7748741585694,
1166.825507846));
#145122=CARTESIAN_POINT('Ctrl Pts',(-32.9156592349078,21.6289390011343,
1164.56950248956));
#145123=CARTESIAN_POINT('Ctrl Pts',(-25.6514842461451,29.8869780371979,
1160.00360544265));
#145124=CARTESIAN_POINT('Ctrl Pts',(-21.1870597913509,33.2014408747266,
1157.75246707764));
#145125=CARTESIAN_POINT('Ctrl Pts',(-11.183414353962,37.7644129148115,1153.18981684574));
#145126=CARTESIAN_POINT('Ctrl Pts',(-5.75222980330756,38.9631534505373,
1150.93141990017));
#145127=CARTESIAN_POINT('Ctrl Pts',(5.24445745961987,39.0351938236361,1146.38220728312));
#145128=CARTESIAN_POINT('Ctrl Pts',(10.6928461412629,37.9069188122571,1144.12252328313));
#145129=CARTESIAN_POINT('Ctrl Pts',(20.7591961881651,33.4707320654403,1139.5600317458));
#145130=CARTESIAN_POINT('Ctrl Pts',(25.2669350996321,30.2129607232191,1137.30761951472));
#145131=CARTESIAN_POINT('Ctrl Pts',(32.635081188955,22.0494206969798,1132.74163557832));
#145132=CARTESIAN_POINT('Ctrl Pts',(35.4150168873858,17.2334918475209,1130.488667703));
#145133=CARTESIAN_POINT('Ctrl Pts',(38.7992588732006,6.77153421948918,1125.93049079934));
#145134=CARTESIAN_POINT('Ctrl Pts',(39.3661250868372,1.23866868789697,1123.6725517893));
#145135=CARTESIAN_POINT('Ctrl Pts',(38.1742261404252,-9.69407731506407,
1119.1195268412));
#145136=CARTESIAN_POINT('Ctrl Pts',(36.4271546111516,-14.9772160932738,
1116.86211424447));
#145137=CARTESIAN_POINT('Ctrl Pts',(30.8650369918341,-24.4659196034356,
1112.29666213713));
#145138=CARTESIAN_POINT('Ctrl Pts',(27.1120874699223,-28.5686160683228,
1110.04564776162));
#145139=CARTESIAN_POINT('Ctrl Pts',(18.1577692119097,-34.950200646368,1105.48188630413));
#145140=CARTESIAN_POINT('Ctrl Pts',(13.0537483440062,-37.1593035688508,
1103.22498482583));
#145141=CARTESIAN_POINT('Ctrl Pts',(2.27187987206591,-39.3202697017892,
1098.67360080778));
#145142=CARTESIAN_POINT('Ctrl Pts',(-3.29118271115233,-39.2482698618276,
1096.41478130458));
#145143=CARTESIAN_POINT('Ctrl Pts',(-14.0163937440488,-36.807287473383,
1091.85420641104));
#145144=CARTESIAN_POINT('Ctrl Pts',(-19.0618186421746,-34.4657956797521,
1089.60098559052));
#145145=CARTESIAN_POINT('Ctrl Pts',(-27.8479269337317,-27.851744166451,
1085.03479176213));
#145146=CARTESIAN_POINT('Ctrl Pts',(-31.4926544757299,-23.6523090805093,
1082.78256529372));
#145147=CARTESIAN_POINT('Ctrl Pts',(-36.8043276295087,-14.0242385086279,
1078.22265613395));
#145148=CARTESIAN_POINT('Ctrl Pts',(-38.4124932907264,-8.70063483893357,
1075.96440277947));
#145149=CARTESIAN_POINT('Ctrl Pts',(-38.955687170905,-2.14833127284238,
1073.24382341729));
#145150=CARTESIAN_POINT('Ctrl Pts',(-38.9999999999934,-1.07354426693828,
1072.7975615313));
#145151=CARTESIAN_POINT('Ctrl Pts',(-39.,-2.40743813773037E-10,1072.35181564256));
#145152=CARTESIAN_POINT('Ctrl Pts',(-39.,6.7390537594747E-12,1069.18568435754));
#145153=CARTESIAN_POINT('Ctrl Pts',(-39.,-2.92908286305145,1070.40186769016));
#145154=CARTESIAN_POINT('Ctrl Pts',(-38.6698735170771,-5.85801370569777,
1071.61450745359));
#145155=CARTESIAN_POINT('Ctrl Pts',(-36.7798486915294,-14.0884527735446,
1075.1178764091));
#145156=CARTESIAN_POINT('Ctrl Pts',(-34.42890930272,-19.1275658806115,1077.37717345445));
#145157=CARTESIAN_POINT('Ctrl Pts',(-27.7984595898942,-27.9017290234602,
1081.92417113998));
#145158=CARTESIAN_POINT('Ctrl Pts',(-23.5874503239633,-31.5419326682777,
1084.18572159625));
#145159=CARTESIAN_POINT('Ctrl Pts',(-13.9449101522654,-36.8343930863333,
1088.74916602945));
#145160=CARTESIAN_POINT('Ctrl Pts',(-8.61794438291774,-38.4313537265566,
1091.0009100477));
#145161=CARTESIAN_POINT('Ctrl Pts',(2.3429835031869,-39.3158318656711,1095.56646343224));
#145162=CARTESIAN_POINT('Ctrl Pts',(7.85682919037316,-38.5938481919951,
1097.82041211834));
#145163=CARTESIAN_POINT('Ctrl Pts',(18.2197211130999,-34.9181476162326,
1102.37658946879));
#145164=CARTESIAN_POINT('Ctrl Pts',(22.9573494361813,-32.0030078391976,
1104.63456736523));
#145165=CARTESIAN_POINT('Ctrl Pts',(30.9111507093045,-24.4078483224121,
1109.1899697186));
#145166=CARTESIAN_POINT('Ctrl Pts',(34.0421550841879,-19.8086620493969,
1111.44588305573));
#145167=CARTESIAN_POINT('Ctrl Pts',(38.1919195816138,-9.6232672276592,1116.01180423757));
#145168=CARTESIAN_POINT('Ctrl Pts',(39.166468806553,-4.14905254858988,1118.26295789616));
#145169=CARTESIAN_POINT('Ctrl Pts',(38.7871156041852,6.83953168245799,1122.82552359188));
#145170=CARTESIAN_POINT('Ctrl Pts',(37.4368627370235,12.2350688954627,1125.08403118664));
#145171=CARTESIAN_POINT('Ctrl Pts',(32.595228404851,22.1088711917865,1129.63308690113));
#145172=CARTESIAN_POINT('Ctrl Pts',(29.1546851162566,26.4816299228362,1131.89284389154));
#145173=CARTESIAN_POINT('Ctrl Pts',(20.6933554732093,33.5114768607126,1136.45546432974));
#145174=CARTESIAN_POINT('Ctrl Pts',(15.7667043480505,36.0922683185844,1138.7078265675));
#145175=CARTESIAN_POINT('Ctrl Pts',(5.17342299714505,39.0443477133479,1143.27378879888));
#145176=CARTESIAN_POINT('Ctrl Pts',(-0.37691182012992,39.3836826504988,
1145.52681502005));
#145177=CARTESIAN_POINT('Ctrl Pts',(-11.2497965798242,37.7449090321416,
1150.08486559052));
#145178=CARTESIAN_POINT('Ctrl Pts',(-16.4544474528643,35.7837625096039,
1152.34279527611));
#145179=CARTESIAN_POINT('Ctrl Pts',(-25.7070652977076,29.8394562917062,
1156.89598098112));
#145180=CARTESIAN_POINT('Ctrl Pts',(-29.6557870721231,25.9188866020372,
1159.1532894125));
#145181=CARTESIAN_POINT('Ctrl Pts',(-35.6662892255865,16.7077054790432,
1163.71877878532));
#145182=CARTESIAN_POINT('Ctrl Pts',(-37.6636877096582,11.5185699648607,
1165.96979605541));
#145183=CARTESIAN_POINT('Ctrl Pts',(-38.8408829296079,4.06949041451221,
1169.09987601447));
#145184=CARTESIAN_POINT('Ctrl Pts',(-38.9999999999999,2.032982257003,1169.94157060178));
#145185=CARTESIAN_POINT('Ctrl Pts',(-39.,1.53110857326055E-10,1170.78568435748));
#145186=CARTESIAN_POINT('Origin',(0.,0.,-11.4051836540916));
#145187=CARTESIAN_POINT('',(-39.,-6.92868819070596E-11,1275.55181564252));
#145188=CARTESIAN_POINT('',(-39.,7.90570704135022E-14,1272.38568435754));
#145189=CARTESIAN_POINT('',(-39.,-4.77612251667468E-15,-11.4051836540916));
#145190=CARTESIAN_POINT('Ctrl Pts',(-39.,-1.38611622180207E-10,1275.55181564252));
#145191=CARTESIAN_POINT('Ctrl Pts',(-39.0000000000121,3.39009799570675,
1274.14421439965));
#145192=CARTESIAN_POINT('Ctrl Pts',(-38.5578414158399,6.77504194114251,
1272.74016932084));
#145193=CARTESIAN_POINT('Ctrl Pts',(-36.2593020322943,15.3782008352702,
1269.0535111035));
#145194=CARTESIAN_POINT('Ctrl Pts',(-33.7316775642524,20.3324889403378,
1266.79557053843));
#145195=CARTESIAN_POINT('Ctrl Pts',(-26.7960837422303,28.8649715059958,
1262.23737458539));
#145196=CARTESIAN_POINT('Ctrl Pts',(-22.463919094978,32.3511642572694,1259.98441546151));
#145197=CARTESIAN_POINT('Ctrl Pts',(-12.6439735093029,37.3010853753511,
1255.4184283221));
#145198=CARTESIAN_POINT('Ctrl Pts',(-7.2636870838922,38.7101148932136,1253.16600845434));
#145199=CARTESIAN_POINT('Ctrl Pts',(3.72546313492805,39.2095936708073,1248.6035364724));
#145200=CARTESIAN_POINT('Ctrl Pts',(9.21344617495873,38.2931199921262,1246.34386337045));
#145201=CARTESIAN_POINT('Ctrl Pts',(19.441245138911,34.2527873764992,1241.79462707815));
#145202=CARTESIAN_POINT('Ctrl Pts',(24.0724262610235,31.1727116195146,1239.53624680028));
#145203=CARTESIAN_POINT('Ctrl Pts',(31.7520139165969,23.3032636376238,1234.97338516403));
#145204=CARTESIAN_POINT('Ctrl Pts',(34.7175002768481,18.5992083269852,1232.72205531739));
#145205=CARTESIAN_POINT('Ctrl Pts',(38.5061843592954,8.27628254398474,1228.15704489311));
#145206=CARTESIAN_POINT('Ctrl Pts',(39.2879009775359,2.77035504833265,1225.90209366215));
#145207=CARTESIAN_POINT('Ctrl Pts',(38.5229871029467,-8.198586862572,1221.34768364638));
#145208=CARTESIAN_POINT('Ctrl Pts',(36.983616651298,-13.5444717146089,1219.08953055696));
#145209=CARTESIAN_POINT('Ctrl Pts',(31.7965405177819,-23.242618137828,1214.5321177159));
#145210=CARTESIAN_POINT('Ctrl Pts',(28.2046521619375,-27.4908386398366,
1212.27734410354));
#145211=CARTESIAN_POINT('Ctrl Pts',(19.5036771475858,-34.2174696969444,
1207.71118909283));
#145212=CARTESIAN_POINT('Ctrl Pts',(14.4906255946235,-36.6230170530299,
1205.45975193439));
#145213=CARTESIAN_POINT('Ctrl Pts',(3.8025676904283,-39.2015111663801,1200.89838937249));
#145214=CARTESIAN_POINT('Ctrl Pts',(-1.75779254886071,-39.3462572065711,
1198.63834207664));
#145215=CARTESIAN_POINT('Ctrl Pts',(-12.5684694905614,-37.3268034371924,
1194.09142647996));
#145216=CARTESIAN_POINT('Ctrl Pts',(-17.7036431989977,-35.183323529683,
1191.83054903452));
#145217=CARTESIAN_POINT('Ctrl Pts',(-26.7439367605968,-28.9135770053946,
1187.2662842232));
#145218=CARTESIAN_POINT('Ctrl Pts',(-30.5497675463814,-24.8585963968017,
1185.01450274688));
#145219=CARTESIAN_POINT('Ctrl Pts',(-36.2314872565174,-15.4435624601413,
1180.44891476071));
#145220=CARTESIAN_POINT('Ctrl Pts',(-38.0452931856009,-10.1867875622354,
1178.19503602378));
#145221=CARTESIAN_POINT('Ctrl Pts',(-38.904245474371,-3.15764135812629,
1175.26062781204));
#145222=CARTESIAN_POINT('Ctrl Pts',(-38.9999999999998,-1.57742956945571,
1174.6067795477));
#145223=CARTESIAN_POINT('Ctrl Pts',(-39.,-3.85858012208473E-12,1173.95181564246));
#145224=CARTESIAN_POINT('Ctrl Pts',(-39.,1.53028145710721E-10,1170.78568435748));
#145225=CARTESIAN_POINT('Ctrl Pts',(-39.0000000000002,-3.43671147175983,
1172.21263996323));
#145226=CARTESIAN_POINT('Ctrl Pts',(-38.5455980291902,-6.86767714357309,
1173.63607290253));
#145227=CARTESIAN_POINT('Ctrl Pts',(-36.2037036727293,-15.5092640042679,
1177.34172285394));
#145228=CARTESIAN_POINT('Ctrl Pts',(-33.6573303360208,-20.4558930289092,
1179.60059198728));
#145229=CARTESIAN_POINT('Ctrl Pts',(-26.6876907218572,-28.9655440023475,
1184.16130566822));
#145230=CARTESIAN_POINT('Ctrl Pts',(-22.3411840840882,-32.4363266018347,
1186.41446414357));
#145231=CARTESIAN_POINT('Ctrl Pts',(-12.5020145840668,-37.3487112574047,
1190.98064938005));
#145232=CARTESIAN_POINT('Ctrl Pts',(-7.11759788381116,-38.7370446357954,
1193.23292212716));
#145233=CARTESIAN_POINT('Ctrl Pts',(3.86889336978166,-39.1952716515687,
1197.79271440655));
#145234=CARTESIAN_POINT('Ctrl Pts',(9.35082466511408,-38.2594188534342,
1200.05093475405));
#145235=CARTESIAN_POINT('Ctrl Pts',(19.5648565769327,-34.1828573801283,
1204.60175915323));
#145236=CARTESIAN_POINT('Ctrl Pts',(24.1875101948081,-31.0841055881524,
1206.86063323524));
#145237=CARTESIAN_POINT('Ctrl Pts',(31.8397140269745,-23.1832893296027,
1211.42546008912));
#145238=CARTESIAN_POINT('Ctrl Pts',(34.7873038977391,-18.4682792629896,
1213.67660659029));
#145239=CARTESIAN_POINT('Ctrl Pts',(38.5370384484279,-8.13136021947425,
1218.24119272561));
#145240=CARTESIAN_POINT('Ctrl Pts',(39.2980535938245,-2.62237187735175,
1220.49685037152));
#145241=CARTESIAN_POINT('Ctrl Pts',(38.4918215306549,8.34385191811939,1225.05013179966));
#145242=CARTESIAN_POINT('Ctrl Pts',(36.9323013274488,13.6840218885835,1227.30844969847));
#145243=CARTESIAN_POINT('Ctrl Pts',(31.7082793287542,23.3628496115169,1231.86711830015));
#145244=CARTESIAN_POINT('Ctrl Pts',(28.1005812757189,27.5971767593091,1234.12124709457));
#145245=CARTESIAN_POINT('Ctrl Pts',(19.3744690646522,34.2907832826383,1238.68746778651));
#145246=CARTESIAN_POINT('Ctrl Pts',(14.3523225347968,36.6774118726178,1240.93916141839));
#145247=CARTESIAN_POINT('Ctrl Pts',(3.65283329393246,39.2160289927788,1245.50055806714));
#145248=CARTESIAN_POINT('Ctrl Pts',(-1.90654130622282,39.3393075310152,
1247.75940496865));
#145249=CARTESIAN_POINT('Ctrl Pts',(-12.709415220828,37.2790572970399,1252.30773360844));
#145250=CARTESIAN_POINT('Ctrl Pts',(-17.8375195708604,35.1152800961424,
1254.56833596046));
#145251=CARTESIAN_POINT('Ctrl Pts',(-26.8522956797519,28.8129642019199,
1259.1322952039));
#145252=CARTESIAN_POINT('Ctrl Pts',(-30.6426963934833,24.7439215570187,
1261.38379193086));
#145253=CARTESIAN_POINT('Ctrl Pts',(-36.2890196037476,15.3078623613554,
1265.94906526269));
#145254=CARTESIAN_POINT('Ctrl Pts',(-38.0831767765695,10.0442011135505,
1268.20354950298));
#145255=CARTESIAN_POINT('Ctrl Pts',(-38.9100499980652,3.06047839876306,
1271.11697111921));
#145256=CARTESIAN_POINT('Ctrl Pts',(-39.,1.52893054872031,1271.75085771145));
#145257=CARTESIAN_POINT('Ctrl Pts',(-39.,2.20101714631937E-13,1272.38568435754));
#145258=CARTESIAN_POINT('Origin',(0.,0.,-11.4051836540916));
#145259=CARTESIAN_POINT('',(-39.,-1.43281722098234E-12,1377.15181564246));
#145260=CARTESIAN_POINT('',(-39.,1.04944080121118E-10,1373.98568435745));
#145261=CARTESIAN_POINT('',(-39.,-4.77612251667468E-15,-11.4051836540916));
#145262=CARTESIAN_POINT('Ctrl Pts',(-39.,-2.82135426132868E-12,1377.15181564246));
#145263=CARTESIAN_POINT('Ctrl Pts',(-39.0000000000002,2.88041777647212,
1375.95583852112));
#145264=CARTESIAN_POINT('Ctrl Pts',(-38.6807435490783,5.76111009139163,
1374.76337209935));
#145265=CARTESIAN_POINT('Ctrl Pts',(-36.8318578925542,13.9525788639201,
1371.27904717011));
#145266=CARTESIAN_POINT('Ctrl Pts',(-34.4972202638612,19.0052537775258,
1369.01829870079));
#145267=CARTESIAN_POINT('Ctrl Pts',(-27.8971802064615,27.8022114893361,
1364.47017676853));
#145268=CARTESIAN_POINT('Ctrl Pts',(-23.7038291806506,31.4542341225288,
1362.21126493798));
#145269=CARTESIAN_POINT('Ctrl Pts',(-14.0837403213775,36.7813840979505,
1357.64974505296));
#145270=CARTESIAN_POINT('Ctrl Pts',(-8.76363186995282,38.3982647036319,
1355.3980904166));
#145271=CARTESIAN_POINT('Ctrl Pts',(2.19501292647189,39.3246614391287,1350.83187501784));
#145272=CARTESIAN_POINT('Ctrl Pts',(7.71346452394935,38.6230551216481,1348.57766059682));
#145273=CARTESIAN_POINT('Ctrl Pts',(18.0926794494128,34.9843013980631,1344.01916268284));
#145274=CARTESIAN_POINT('Ctrl Pts',(22.8413040626638,32.0860501965724,1341.76087443117));
#145275=CARTESIAN_POINT('Ctrl Pts',(30.8210535135947,24.5209404045838,1337.20743429205));
#145276=CARTESIAN_POINT('Ctrl Pts',(33.967642327505,19.9354390322161,1334.9518776128));
#145277=CARTESIAN_POINT('Ctrl Pts',(38.1552177008476,9.76797933073579,1330.38722910559));
#145278=CARTESIAN_POINT('Ctrl Pts',(39.150558748526,4.29721574010371,1328.13606088376));
#145279=CARTESIAN_POINT('Ctrl Pts',(38.8125265088509,-6.69666200815592,
1323.57129726886));
#145280=CARTESIAN_POINT('Ctrl Pts',(37.4811251675765,-12.1002914500509,
1321.31228975546));
#145281=CARTESIAN_POINT('Ctrl Pts',(32.6740393585401,-21.9915389253384,
1316.76166173402));
#145282=CARTESIAN_POINT('Ctrl Pts',(29.2510655423101,-26.3744760051109,
1314.50340324433));
#145283=CARTESIAN_POINT('Ctrl Pts',(20.8195296146921,-33.4330110139997,
1309.94347646719));
#145284=CARTESIAN_POINT('Ctrl Pts',(15.9037342957803,-36.0319016450438,
1307.69125692304));
#145285=CARTESIAN_POINT('Ctrl Pts',(5.32145177615644,-39.0246868645341,
1303.12506187543));
#145286=CARTESIAN_POINT('Ctrl Pts',(-0.229142101628406,-39.3850633927897,
1300.87183155197));
#145287=CARTESIAN_POINT('Ctrl Pts',(-11.1117677761475,-37.7860696001166,
1296.31127770666));
#145288=CARTESIAN_POINT('Ctrl Pts',(-16.3250416871503,-35.8432420952935,
1294.05246556515));
#145289=CARTESIAN_POINT('Ctrl Pts',(-25.5977941436226,-29.9327097697844,
1289.50105926183));
#145290=CARTESIAN_POINT('Ctrl Pts',(-29.5588628263736,-26.0287293417693,
1287.2441727584));
#145291=CARTESIAN_POINT('Ctrl Pts',(-35.6025966941331,-16.8429885383189,
1282.68040050665));
#145292=CARTESIAN_POINT('Ctrl Pts',(-37.6196980955947,-11.6614777857802,
1280.42938649254));
#145293=CARTESIAN_POINT('Ctrl Pts',(-38.8330920305166,-4.16786431624148,
1277.27836870029));
#145294=CARTESIAN_POINT('Ctrl Pts',(-38.9999999999926,-2.08216040212245,
1276.41634863633));
#145295=CARTESIAN_POINT('Ctrl Pts',(-39.,-1.38562772367123E-10,1275.55181564252));
#145296=CARTESIAN_POINT('Ctrl Pts',(-39.,2.647881913731E-13,1272.38568435754));
#145297=CARTESIAN_POINT('Ctrl Pts',(-39.,-3.94534185592291,1274.0238281831));
#145298=CARTESIAN_POINT('Ctrl Pts',(-38.4007569452698,-7.87952769446106,
1275.65311463225));
#145299=CARTESIAN_POINT('Ctrl Pts',(-35.5715404036943,-16.9087570846571,
1279.57333127736));
#145300=CARTESIAN_POINT('Ctrl Pts',(-32.8342767055597,-21.7522446139334,
1281.82859776841));
#145301=CARTESIAN_POINT('Ctrl Pts',(-25.5393666793081,-29.98282822353,1286.39466764876));
#145302=CARTESIAN_POINT('Ctrl Pts',(-21.0625296728186,-33.2805482709015,
1288.64595911512));
#145303=CARTESIAN_POINT('Ctrl Pts',(-11.0421380925384,-37.8059505035515,
1293.20788033371));
#145304=CARTESIAN_POINT('Ctrl Pts',(-5.60631950711533,-38.9844311981042,
1295.46722018366));
#145305=CARTESIAN_POINT('Ctrl Pts',(5.39098520885725,-39.0152716393876,
1300.01510968091));
#145306=CARTESIAN_POINT('Ctrl Pts',(10.8354276405026,-37.8665138835699,
1302.27544940074));
#145307=CARTESIAN_POINT('Ctrl Pts',(20.8855354501616,-33.3920330986026,
1306.83899128012));
#145308=CARTESIAN_POINT('Ctrl Pts',(25.3806943553124,-30.1174311355258,
1309.09101442429));
#145309=CARTESIAN_POINT('Ctrl Pts',(32.7178846802067,-21.926349624505,1313.65679019088));
#145310=CARTESIAN_POINT('Ctrl Pts',(35.4797105811817,-17.0998751609009,
1315.91026833225));
#145311=CARTESIAN_POINT('Ctrl Pts',(38.8244745123745,-6.62538734318276,
1320.46737521405));
#145312=CARTESIAN_POINT('Ctrl Pts',(39.3705647181445,-1.08999955230238,
1322.7252872927));
#145313=CARTESIAN_POINT('Ctrl Pts',(38.1372954002353,9.83823489768537,1327.27962723063));
#145314=CARTESIAN_POINT('Ctrl Pts',(36.3704386297287,15.1143662728797,1329.53619924304));
#145315=CARTESIAN_POINT('Ctrl Pts',(30.7727670954361,24.5818543154064,1334.10193326534));
#145316=CARTESIAN_POINT('Ctrl Pts',(27.0044017377237,28.6703866293253,1336.35299830247));
#145317=CARTESIAN_POINT('Ctrl Pts',(18.0264084499264,35.0181220236859,1340.91613461669));
#145318=CARTESIAN_POINT('Ctrl Pts',(12.913961529755,37.2081229471099,1343.17388755452));
#145319=CARTESIAN_POINT('Ctrl Pts',(2.12369724136763,39.3285926079057,1347.72402300653));
#145320=CARTESIAN_POINT('Ctrl Pts',(-3.43930503697113,39.2356616772837,
1349.9833053519));
#145321=CARTESIAN_POINT('Ctrl Pts',(-14.155752083824,36.7539032180833,1354.54501354965));
#145322=CARTESIAN_POINT('Ctrl Pts',(-19.1919795822001,34.3934611066868,
1356.79774204446));
#145323=CARTESIAN_POINT('Ctrl Pts',(-27.9528668502543,27.746409001408,1361.36383642538));
#145324=CARTESIAN_POINT('Ctrl Pts',(-31.5817648869465,23.5331615977101,
1363.61647367641));
#145325=CARTESIAN_POINT('Ctrl Pts',(-36.8569517582067,13.88531067212,1368.17539050311));
#145326=CARTESIAN_POINT('Ctrl Pts',(-38.4451521731786,8.55535292592722,
1370.43341966595));
#145327=CARTESIAN_POINT('Ctrl Pts',(-38.9596487804728,2.05002493395998,
1373.13449431865));
#145328=CARTESIAN_POINT('Ctrl Pts',(-38.9999999999999,1.02442168325448,
1373.56033463717));
#145329=CARTESIAN_POINT('Ctrl Pts',(-39.,2.09992717659091E-10,1373.98568435745));
#145330=CARTESIAN_POINT('Origin',(0.,0.,-11.4051836540916));
#145331=CARTESIAN_POINT('',(-39.,1.80311138088147E-11,1478.75181564244));
#145332=CARTESIAN_POINT('',(-39.,7.02754413066815E-12,1475.58568435754));
#145333=CARTESIAN_POINT('',(-39.,-4.77612251667468E-15,-11.4051836540916));
#145334=CARTESIAN_POINT('Ctrl Pts',(-39.,3.61144447680317E-11,1478.75181564244));
#145335=CARTESIAN_POINT('Ctrl Pts',(-39.,2.37441675948014,1477.76593500248));
#145336=CARTESIAN_POINT('Ctrl Pts',(-38.7829742622338,4.75198370846709,
1476.78303645826));
#145337=CARTESIAN_POINT('Ctrl Pts',(-37.347229177159,12.5070764604314,1473.50833436143));
#145338=CARTESIAN_POINT('Ctrl Pts',(-35.2129213102348,17.6432711332436,
1471.25554123724));
#145339=CARTESIAN_POINT('Ctrl Pts',(-28.9606169290237,26.6935870925475,
1466.69398715833));
#145340=CARTESIAN_POINT('Ctrl Pts',(-24.9101561368435,30.5078998124061,
1464.43477569376));
#145341=CARTESIAN_POINT('Ctrl Pts',(-15.5045799938302,36.2052856351559,
1459.88446463748));
#145342=CARTESIAN_POINT('Ctrl Pts',(-10.2501188711739,38.0283506563109,
1457.6268328815));
#145343=CARTESIAN_POINT('Ctrl Pts',(0.661883501075245,39.3800839171634,
1453.06360630778));
#145344=CARTESIAN_POINT('Ctrl Pts',(6.20091300299922,38.894467021419,1450.8125518839));
#145345=CARTESIAN_POINT('Ctrl Pts',(16.7141980976748,35.6635485592597,1446.24685311034));
#145346=CARTESIAN_POINT('Ctrl Pts',(21.5730610713052,32.9522007088133,1443.99016817262));
#145347=CARTESIAN_POINT('Ctrl Pts',(29.8429570127381,25.7026634234135,1439.43600737227));
#145348=CARTESIAN_POINT('Ctrl Pts',(33.1661994321955,21.2423835839676,1437.17809842454));
#145349=CARTESIAN_POINT('Ctrl Pts',(37.7458046507818,11.2458863025301,1432.620840729));
#145350=CARTESIAN_POINT('Ctrl Pts',(38.953532270286,5.81783508378545,1430.36743663771));
#145351=CARTESIAN_POINT('Ctrl Pts',(39.0438479909382,-5.1785588031054,1425.80162829789));
#145352=CARTESIAN_POINT('Ctrl Pts',(37.9251153602865,-10.6263433292262,
1423.54955488541));
#145353=CARTESIAN_POINT('Ctrl Pts',(33.5072026416274,-20.7013434890943,
1418.98615553982));
#145354=CARTESIAN_POINT('Ctrl Pts',(30.2553113772127,-25.216458746652,1416.72591321134));
#145355=CARTESIAN_POINT('Ctrl Pts',(22.1036478741556,-32.5982400550239,
1412.17783801107));
#145356=CARTESIAN_POINT('Ctrl Pts',(17.2911749160037,-35.386920041304,1409.91863180754));
#145357=CARTESIAN_POINT('Ctrl Pts',(6.83547549740724,-38.7879054736836,
1405.35660612111));
#145358=CARTESIAN_POINT('Ctrl Pts',(1.30509855894386,-39.3640200220915,
1403.10533935717));
#145359=CARTESIAN_POINT('Ctrl Pts',(-9.63023925437765,-38.1904256013885,
1398.53928964146));
#145360=CARTESIAN_POINT('Ctrl Pts',(-14.9152855697462,-36.4523671333016,
1396.28392440178));
#145361=CARTESIAN_POINT('Ctrl Pts',(-24.4127757610747,-30.9071429022493,
1391.72761197885));
#145362=CARTESIAN_POINT('Ctrl Pts',(-28.5238375105124,-27.1592675983071,
1389.46950898569));
#145363=CARTESIAN_POINT('Ctrl Pts',(-34.9199771510344,-18.2156415998711,
1384.91417895116));
#145364=CARTESIAN_POINT('Ctrl Pts',(-37.1375385041311,-13.1159035068419,
1382.65978177388));
#145365=CARTESIAN_POINT('Ctrl Pts',(-38.7423587002407,-5.17687524663117,
1379.2971087506));
#145366=CARTESIAN_POINT('Ctrl Pts',(-38.9999999999998,-2.58728858011592,
1378.22608270656));
#145367=CARTESIAN_POINT('Ctrl Pts',(-39.,-2.84605672362659E-12,1377.15181564246));
#145368=CARTESIAN_POINT('Ctrl Pts',(-39.0000000000001,2.09855327559794E-10,
1373.98568435745));
#145369=CARTESIAN_POINT('Ctrl Pts',(-39.0000000000004,-4.45618022580496,
1375.83593317984));
#145370=CARTESIAN_POINT('Ctrl Pts',(-38.2350734620249,-8.8927699197193,
1377.6702641004));
#145371=CARTESIAN_POINT('Ctrl Pts',(-34.8846175646687,-18.2837541637938,
1381.80872310428));
#145372=CARTESIAN_POINT('Ctrl Pts',(-31.9621762762703,-23.0141664573471,
1384.05975861463));
#145373=CARTESIAN_POINT('Ctrl Pts',(-24.3541829842684,-30.9531169708647,
1388.62391993159));
#145374=CARTESIAN_POINT('Ctrl Pts',(-19.7514891007839,-34.0748091144117,
1390.8802448956));
#145375=CARTESIAN_POINT('Ctrl Pts',(-9.56160343469945,-38.2075719539005,
1395.43249606781));
#145376=CARTESIAN_POINT('Ctrl Pts',(-4.08276794280321,-39.1737724321858,
1397.69105399931));
#145377=CARTESIAN_POINT('Ctrl Pts',(6.90909010052654,-38.7750050144413,
1402.25078717627));
#145378=CARTESIAN_POINT('Ctrl Pts',(12.3028022100999,-37.4150548403148,
1404.50439747286));
#145379=CARTESIAN_POINT('Ctrl Pts',(22.1679831917244,-32.554688309711,1409.07062342063));
#145380=CARTESIAN_POINT('Ctrl Pts',(26.5316025562092,-29.1083189220235,
1411.32259173001));
#145381=CARTESIAN_POINT('Ctrl Pts',(33.5450503237739,-20.6390004187557,
1415.883183882));
#145382=CARTESIAN_POINT('Ctrl Pts',(36.1172600369038,-15.708662448361,1418.14166822648));
#145383=CARTESIAN_POINT('Ctrl Pts',(39.0530359196965,-5.11023800956806,
1422.69129154581));
#145384=CARTESIAN_POINT('Ctrl Pts',(39.383501308142,0.445475200229383,1424.95098876778));
#145385=CARTESIAN_POINT('Ctrl Pts',(37.7242291732344,11.3187887239687,1429.51541498531));
#145386=CARTESIAN_POINT('Ctrl Pts',(35.7541933445629,16.5188612851454,1431.7667104148));
#145387=CARTESIAN_POINT('Ctrl Pts',(29.793792131418,25.7595209126659,1436.33165519177));
#145388=CARTESIAN_POINT('Ctrl Pts',(25.8685919165449,29.6989887557016,1438.58671904772));
#145389=CARTESIAN_POINT('Ctrl Pts',(16.6504672755713,35.6931331713202,1443.14094612052));
#145390=CARTESIAN_POINT('Ctrl Pts',(11.4554285550858,37.6830845947796,1445.39911843335));
#145391=CARTESIAN_POINT('Ctrl Pts',(0.589091599192387,39.3813659275958,
1449.95674167307));
#145392=CARTESIAN_POINT('Ctrl Pts',(-4.96540523733698,39.0716402290369,
1452.21140492066));
#145393=CARTESIAN_POINT('Ctrl Pts',(-15.5750437562469,36.1752198940577,
1456.77757513838));
#145394=CARTESIAN_POINT('Ctrl Pts',(-20.5141684009702,33.6213054232799,
1459.02905048086));
#145395=CARTESIAN_POINT('Ctrl Pts',(-29.0101491441578,26.639311686823,1463.59117855446));
#145396=CARTESIAN_POINT('Ctrl Pts',(-32.4723478199063,22.2881206444973,
1465.85045056518));
#145397=CARTESIAN_POINT('Ctrl Pts',(-37.3695418329642,12.4409805236918,
1470.39751689979));
#145398=CARTESIAN_POINT('Ctrl Pts',(-38.7501977411297,7.0486479464448,1472.65901804226));
#145399=CARTESIAN_POINT('Ctrl Pts',(-38.9897218108706,1.0343759573043,1475.15620152699));
#145400=CARTESIAN_POINT('Ctrl Pts',(-39.,0.516968414109846,1475.37103410757));
#145401=CARTESIAN_POINT('Ctrl Pts',(-39.,1.41471556691641E-11,1475.58568435754));
#145402=CARTESIAN_POINT('Origin',(-51.0189817055138,1.6136547197417E-13,
1492.25));
#145403=CARTESIAN_POINT('',(-10.2149882823905,-5.15937500000011,1492.25));
#145404=CARTESIAN_POINT('',(-51.0189817055139,-5.15937499999986,1492.25));
#145405=CARTESIAN_POINT('',(-10.2149882823904,5.15937499999993,1492.25));
#145406=CARTESIAN_POINT('Ctrl Pts',(-10.2149882823905,-5.15937500000011,
1492.25));
#145407=CARTESIAN_POINT('Ctrl Pts',(-10.2149882823905,-5.15937500000011,
1491.59113903279));
#145408=CARTESIAN_POINT('Ctrl Pts',(-10.2855048387883,-5.02575113964846,
1490.89625255689));
#145409=CARTESIAN_POINT('Ctrl Pts',(-10.5275891593601,-4.49662578128932,
1489.62870790392));
#145410=CARTESIAN_POINT('Ctrl Pts',(-10.6944718935536,-4.10147232415352,
1489.05501422578));
#145411=CARTESIAN_POINT('Ctrl Pts',(-10.9990970108091,-3.1957609090983,
1488.14930281073));
#145412=CARTESIAN_POINT('Ctrl Pts',(-11.1582376083003,-2.62178859469202,
1487.7535702398));
#145413=CARTESIAN_POINT('Ctrl Pts',(-11.3819664861004,-1.35310050851121,
1487.22399004237));
#145414=CARTESIAN_POINT('Ctrl Pts',(-11.444,-0.657734185748201,1487.090625));
#145415=CARTESIAN_POINT('Ctrl Pts',(-11.444,0.657734185748043,1487.090625));
#145416=CARTESIAN_POINT('Ctrl Pts',(-11.3819664861004,1.35310050851105,
1487.22399004237));
#145417=CARTESIAN_POINT('Ctrl Pts',(-11.1582376083003,2.62178859469186,
1487.7535702398));
#145418=CARTESIAN_POINT('Ctrl Pts',(-10.999097010809,3.19576090909814,1488.14930281073));
#145419=CARTESIAN_POINT('Ctrl Pts',(-10.6944718935536,4.10147232415335,
1489.05501422578));
#145420=CARTESIAN_POINT('Ctrl Pts',(-10.52758915936,4.49662578128915,1489.62870790392));
#145421=CARTESIAN_POINT('Ctrl Pts',(-10.2855048387882,5.02575113964829,
1490.89625255689));
#145422=CARTESIAN_POINT('Ctrl Pts',(-10.2149882823904,5.15937499999993,
1491.59113903279));
#145423=CARTESIAN_POINT('Ctrl Pts',(-10.2149882823904,5.15937499999993,
1492.25));
#145424=CARTESIAN_POINT('Ctrl Pts',(-10.2149882823904,5.15937499999994,
1492.25));
#145425=CARTESIAN_POINT('Ctrl Pts',(-10.2149882823904,5.15937499999994,
1492.90886096721));
#145426=CARTESIAN_POINT('Ctrl Pts',(-10.2855048387882,5.02575113964829,
1493.60374744311));
#145427=CARTESIAN_POINT('Ctrl Pts',(-10.52758915936,4.49662578128915,1494.87129209608));
#145428=CARTESIAN_POINT('Ctrl Pts',(-10.6944718935536,4.10147232415335,
1495.44498577422));
#145429=CARTESIAN_POINT('Ctrl Pts',(-10.999097010809,3.19576090909814,1496.35069718927));
#145430=CARTESIAN_POINT('Ctrl Pts',(-11.1582376083003,2.62178859469186,
1496.7464297602));
#145431=CARTESIAN_POINT('Ctrl Pts',(-11.3819664861004,1.35310050851105,
1497.27600995763));
#145432=CARTESIAN_POINT('Ctrl Pts',(-11.444,0.657734185748043,1497.409375));
#145433=CARTESIAN_POINT('Ctrl Pts',(-11.444,-0.657734185748201,1497.409375));
#145434=CARTESIAN_POINT('Ctrl Pts',(-11.3819664861004,-1.35310050851147,
1497.27600995763));
#145435=CARTESIAN_POINT('Ctrl Pts',(-11.1582376083003,-2.62178859469227,
1496.7464297602));
#145436=CARTESIAN_POINT('Ctrl Pts',(-10.9990970108091,-3.1957609090983,
1496.35069718927));
#145437=CARTESIAN_POINT('Ctrl Pts',(-10.6944718935536,-4.10147232415352,
1495.44498577422));
#145438=CARTESIAN_POINT('Ctrl Pts',(-10.5275891593601,-4.49662578128932,
1494.87129209608));
#145439=CARTESIAN_POINT('Ctrl Pts',(-10.2855048387883,-5.02575113964846,
1493.60374744311));
#145440=CARTESIAN_POINT('Ctrl Pts',(-10.2149882823905,-5.1593750000001,
1492.90886096721));
#145441=CARTESIAN_POINT('Ctrl Pts',(-10.2149882823905,-5.15937500000009,
1492.25));
#145442=CARTESIAN_POINT('Origin',(-51.0189817055138,1.6136547197417E-13,
1492.25));
#145443=CARTESIAN_POINT('',(10.2149882823905,5.15937499999981,1492.25));
#145444=CARTESIAN_POINT('',(10.2149882823904,-5.15937500000023,1492.25));
#145445=CARTESIAN_POINT('Ctrl Pts',(10.2149882823905,5.15937499999981,1492.25));
#145446=CARTESIAN_POINT('Ctrl Pts',(10.2149882823905,5.15937499999981,1491.59113903279));
#145447=CARTESIAN_POINT('Ctrl Pts',(10.2855048387883,5.02575113964801,1490.89625255689));
#145448=CARTESIAN_POINT('Ctrl Pts',(10.5275891593602,4.49662578128873,1489.62870790392));
#145449=CARTESIAN_POINT('Ctrl Pts',(10.6944718935536,4.10147232415322,1489.05501422578));
#145450=CARTESIAN_POINT('Ctrl Pts',(10.9990970108091,3.19576090909801,1488.14930281073));
#145451=CARTESIAN_POINT('Ctrl Pts',(11.1582376083003,2.6217885946917,1487.7535702398));
#145452=CARTESIAN_POINT('Ctrl Pts',(11.3819664861004,1.35310050851075,1487.22399004237));
#145453=CARTESIAN_POINT('Ctrl Pts',(11.444,0.657734185747904,1487.090625));
#145454=CARTESIAN_POINT('Ctrl Pts',(11.444,-0.657734185748342,1487.090625));
#145455=CARTESIAN_POINT('Ctrl Pts',(11.3819664861004,-1.35310050851134,
1487.22399004237));
#145456=CARTESIAN_POINT('Ctrl Pts',(11.1582376083003,-2.62178859469216,
1487.7535702398));
#145457=CARTESIAN_POINT('Ctrl Pts',(10.999097010809,-3.19576090909844,1488.14930281073));
#145458=CARTESIAN_POINT('Ctrl Pts',(10.6944718935536,-4.10147232415365,
1489.05501422578));
#145459=CARTESIAN_POINT('Ctrl Pts',(10.5275891593601,-4.49662578128945,
1489.62870790392));
#145460=CARTESIAN_POINT('Ctrl Pts',(10.2855048387882,-5.02575113964858,
1490.89625255689));
#145461=CARTESIAN_POINT('Ctrl Pts',(10.2149882823905,-5.15937500000024,
1491.59113903279));
#145462=CARTESIAN_POINT('Ctrl Pts',(10.2149882823905,-5.15937500000024,
1492.25));
#145463=CARTESIAN_POINT('',(-51.0189817055139,-5.15937499999986,1492.25));
#145464=CARTESIAN_POINT('Ctrl Pts',(10.2149882823905,-5.15937500000024,
1492.25));
#145465=CARTESIAN_POINT('Ctrl Pts',(10.2149882823905,-5.15937500000024,
1492.90886096721));
#145466=CARTESIAN_POINT('Ctrl Pts',(10.2855048387882,-5.02575113964858,
1493.60374744311));
#145467=CARTESIAN_POINT('Ctrl Pts',(10.5275891593601,-4.49662578128945,
1494.87129209608));
#145468=CARTESIAN_POINT('Ctrl Pts',(10.6944718935536,-4.10147232415365,
1495.44498577422));
#145469=CARTESIAN_POINT('Ctrl Pts',(10.999097010809,-3.19576090909844,1496.35069718927));
#145470=CARTESIAN_POINT('Ctrl Pts',(11.1582376083003,-2.62178859469216,
1496.7464297602));
#145471=CARTESIAN_POINT('Ctrl Pts',(11.3819664861004,-1.35310050851134,
1497.27600995763));
#145472=CARTESIAN_POINT('Ctrl Pts',(11.444,-0.657734185748339,1497.409375));
#145473=CARTESIAN_POINT('Ctrl Pts',(11.444,0.657734185747905,1497.409375));
#145474=CARTESIAN_POINT('Ctrl Pts',(11.3819664861004,1.35310050851086,1497.27600995763));
#145475=CARTESIAN_POINT('Ctrl Pts',(11.1582376083003,2.62178859469168,1496.7464297602));
#145476=CARTESIAN_POINT('Ctrl Pts',(10.9990970108091,3.195760909098,1496.35069718927));
#145477=CARTESIAN_POINT('Ctrl Pts',(10.6944718935536,4.10147232415322,1495.44498577422));
#145478=CARTESIAN_POINT('Ctrl Pts',(10.5275891593601,4.49662578128903,1494.87129209608));
#145479=CARTESIAN_POINT('Ctrl Pts',(10.2855048387882,5.02575113964816,1493.60374744311));
#145480=CARTESIAN_POINT('Ctrl Pts',(10.2149882823905,5.15937499999979,1492.90886096721));
#145481=CARTESIAN_POINT('Ctrl Pts',(10.2149882823905,5.1593749999998,1492.25));
#145482=CARTESIAN_POINT('Origin',(0.,50.8013494805973,1441.45));
#145483=CARTESIAN_POINT('',(1.0718581768139E-15,11.4439999999998,1446.609375));
#145484=CARTESIAN_POINT('',(-6.31841207935097E-16,50.8013494805973,1446.609375));
#145485=CARTESIAN_POINT('',(-2.60620079334573E-21,11.4439999999998,1436.290625));
#145486=CARTESIAN_POINT('Ctrl Pts',(-3.19189119579733E-15,11.4439999999998,
1446.609375));
#145487=CARTESIAN_POINT('Ctrl Pts',(-0.657734185748133,11.4439999999998,
1446.609375));
#145488=CARTESIAN_POINT('Ctrl Pts',(-1.35310050851117,11.3819664861002,
1446.47600995763));
#145489=CARTESIAN_POINT('Ctrl Pts',(-2.62178859469199,11.1582376083001,
1445.9464297602));
#145490=CARTESIAN_POINT('Ctrl Pts',(-3.19576090909826,10.9990970108089,
1445.55069718927));
#145491=CARTESIAN_POINT('Ctrl Pts',(-4.10147232415348,10.6944718935534,
1444.64498577422));
#145492=CARTESIAN_POINT('Ctrl Pts',(-4.4966257812893,10.5275891593599,1444.07129209608));
#145493=CARTESIAN_POINT('Ctrl Pts',(-5.02575113964843,10.285504838788,1442.80374744311));
#145494=CARTESIAN_POINT('Ctrl Pts',(-5.15937500000008,10.2149882823903,
1442.10886096721));
#145495=CARTESIAN_POINT('Ctrl Pts',(-5.15937500000008,10.2149882823903,
1441.45));
#145496=CARTESIAN_POINT('Ctrl Pts',(-5.15937500000008,10.2149882823903,
1440.79113903279));
#145497=CARTESIAN_POINT('Ctrl Pts',(-5.02575113964843,10.285504838788,1440.09625255689));
#145498=CARTESIAN_POINT('Ctrl Pts',(-4.4966257812893,10.5275891593599,1438.82870790392));
#145499=CARTESIAN_POINT('Ctrl Pts',(-4.10147232415348,10.6944718935534,
1438.25501422579));
#145500=CARTESIAN_POINT('Ctrl Pts',(-3.19576090909827,10.9990970108089,
1437.34930281073));
#145501=CARTESIAN_POINT('Ctrl Pts',(-2.621788594692,11.1582376083001,1436.9535702398));
#145502=CARTESIAN_POINT('Ctrl Pts',(-1.35310050851117,11.3819664861002,
1436.42399004237));
#145503=CARTESIAN_POINT('Ctrl Pts',(-0.657734185748142,11.4439999999998,
1436.290625));
#145504=CARTESIAN_POINT('Ctrl Pts',(-1.08246744900953E-14,11.4439999999998,
1436.290625));
#145505=CARTESIAN_POINT('Ctrl Pts',(3.33066907387547E-15,11.4439999999998,
1436.290625));
#145506=CARTESIAN_POINT('Ctrl Pts',(0.657734185748133,11.4439999999998,
1436.290625));
#145507=CARTESIAN_POINT('Ctrl Pts',(1.35310050851117,11.3819664861002,1436.42399004237));
#145508=CARTESIAN_POINT('Ctrl Pts',(2.621788594692,11.1582376083001,1436.9535702398));
#145509=CARTESIAN_POINT('Ctrl Pts',(3.19576090909826,10.9990970108089,1437.34930281073));
#145510=CARTESIAN_POINT('Ctrl Pts',(4.10147232415348,10.6944718935534,1438.25501422579));
#145511=CARTESIAN_POINT('Ctrl Pts',(4.496625781289,10.52758915936,1438.82870790392));
#145512=CARTESIAN_POINT('Ctrl Pts',(5.02575113964828,10.2855048387881,1440.09625255689));
#145513=CARTESIAN_POINT('Ctrl Pts',(5.15937500000008,10.2149882823903,1440.79113903279));
#145514=CARTESIAN_POINT('Ctrl Pts',(5.15937500000008,10.2149882823903,1442.10886096721));
#145515=CARTESIAN_POINT('Ctrl Pts',(5.02575113964848,10.285504838788,1442.80374744311));
#145516=CARTESIAN_POINT('Ctrl Pts',(4.4966257812895,10.5275891593598,1444.07129209608));
#145517=CARTESIAN_POINT('Ctrl Pts',(4.10147232415348,10.6944718935534,1444.64498577422));
#145518=CARTESIAN_POINT('Ctrl Pts',(3.19576090909826,10.9990970108089,1445.55069718927));
#145519=CARTESIAN_POINT('Ctrl Pts',(2.62178859469199,11.1582376083001,1445.9464297602));
#145520=CARTESIAN_POINT('Ctrl Pts',(1.35310050851117,11.3819664861002,1446.47600995763));
#145521=CARTESIAN_POINT('Ctrl Pts',(0.657734185748116,11.4439999999998,
1446.609375));
#145522=CARTESIAN_POINT('Ctrl Pts',(-1.40165656858926E-14,11.4439999999998,
1446.609375));
#145523=CARTESIAN_POINT('Origin',(0.,50.8013494805973,1441.45));
#145524=CARTESIAN_POINT('',(-2.27105430665522E-14,-11.4440000000002,1436.290625));
#145525=CARTESIAN_POINT('',(4.40252725068937E-15,-11.4440000000002,1446.609375));
#145526=CARTESIAN_POINT('Ctrl Pts',(-8.32667268468867E-16,-11.4440000000002,
1436.290625));
#145527=CARTESIAN_POINT('Ctrl Pts',(-0.657734185748132,-11.4440000000002,
1436.290625));
#145528=CARTESIAN_POINT('Ctrl Pts',(-1.35310050851117,-11.3819664861006,
1436.42399004237));
#145529=CARTESIAN_POINT('Ctrl Pts',(-2.621788594692,-11.1582376083005,1436.9535702398));
#145530=CARTESIAN_POINT('Ctrl Pts',(-3.19576090909827,-10.9990970108092,
1437.34930281073));
#145531=CARTESIAN_POINT('Ctrl Pts',(-4.10147232415348,-10.6944718935538,
1438.25501422579));
#145532=CARTESIAN_POINT('Ctrl Pts',(-4.4966257812893,-10.5275891593602,
1438.82870790392));
#145533=CARTESIAN_POINT('Ctrl Pts',(-5.02575113964843,-10.2855048387884,
1440.09625255689));
#145534=CARTESIAN_POINT('Ctrl Pts',(-5.15937500000008,-10.2149882823906,
1440.79113903279));
#145535=CARTESIAN_POINT('Ctrl Pts',(-5.15937500000008,-10.2149882823906,
1441.45));
#145536=CARTESIAN_POINT('Ctrl Pts',(-5.15937500000008,-10.2149882823906,
1442.10886096721));
#145537=CARTESIAN_POINT('Ctrl Pts',(-5.02575113964843,-10.2855048387884,
1442.80374744311));
#145538=CARTESIAN_POINT('Ctrl Pts',(-4.4966257812893,-10.5275891593602,
1444.07129209608));
#145539=CARTESIAN_POINT('Ctrl Pts',(-4.10147232415348,-10.6944718935538,
1444.64498577422));
#145540=CARTESIAN_POINT('Ctrl Pts',(-3.19576090909826,-10.9990970108092,
1445.55069718927));
#145541=CARTESIAN_POINT('Ctrl Pts',(-2.62178859469199,-11.1582376083005,
1445.9464297602));
#145542=CARTESIAN_POINT('Ctrl Pts',(-1.35310050851117,-11.3819664861006,
1446.47600995763));
#145543=CARTESIAN_POINT('Ctrl Pts',(-0.657734185748134,-11.4440000000002,
1446.609375));
#145544=CARTESIAN_POINT('Ctrl Pts',(-3.7470027081099E-15,-11.4440000000002,
1446.609375));
#145545=CARTESIAN_POINT('',(-6.31841207935097E-16,50.8013494805973,1446.609375));
#145546=CARTESIAN_POINT('Ctrl Pts',(4.71844785465692E-15,-11.4440000000002,
1446.609375));
#145547=CARTESIAN_POINT('Ctrl Pts',(0.657734185748135,-11.4440000000002,
1446.609375));
#145548=CARTESIAN_POINT('Ctrl Pts',(1.35310050851117,-11.3819664861006,
1446.47600995763));
#145549=CARTESIAN_POINT('Ctrl Pts',(2.62178859469199,-11.1582376083005,
1445.9464297602));
#145550=CARTESIAN_POINT('Ctrl Pts',(3.19576090909826,-10.9990970108092,
1445.55069718927));
#145551=CARTESIAN_POINT('Ctrl Pts',(4.10147232415348,-10.6944718935538,
1444.64498577422));
#145552=CARTESIAN_POINT('Ctrl Pts',(4.4966257812893,-10.5275891593602,1444.07129209608));
#145553=CARTESIAN_POINT('Ctrl Pts',(5.02575113964843,-10.2855048387884,
1442.80374744311));
#145554=CARTESIAN_POINT('Ctrl Pts',(5.15937500000008,-10.2149882823906,
1442.10886096721));
#145555=CARTESIAN_POINT('Ctrl Pts',(5.15937500000008,-10.2149882823906,
1440.79113903279));
#145556=CARTESIAN_POINT('Ctrl Pts',(5.02575113964838,-10.2855048387884,
1440.09625255689));
#145557=CARTESIAN_POINT('Ctrl Pts',(4.4966257812891,-10.5275891593603,1438.82870790392));
#145558=CARTESIAN_POINT('Ctrl Pts',(4.10147232415348,-10.6944718935538,
1438.25501422578));
#145559=CARTESIAN_POINT('Ctrl Pts',(3.19576090909826,-10.9990970108092,
1437.34930281073));
#145560=CARTESIAN_POINT('Ctrl Pts',(2.62178859469186,-11.1582376083005,
1436.9535702398));
#145561=CARTESIAN_POINT('Ctrl Pts',(1.353100508511,-11.3819664861006,1436.42399004237));
#145562=CARTESIAN_POINT('Ctrl Pts',(0.657734185748139,-11.4440000000002,
1436.290625));
#145563=CARTESIAN_POINT('Ctrl Pts',(9.85322934354826E-15,-11.4440000000002,
1436.290625));
#145564=CARTESIAN_POINT('Origin',(0.,0.,-11.4051836540916));
#145565=CARTESIAN_POINT('',(0.,-39.,1500.98568435754));
#145566=CARTESIAN_POINT('Ctrl Pts',(-39.,1.41056610836188E-11,1475.58568435754));
#145567=CARTESIAN_POINT('Ctrl Pts',(-39.,-4.970368238445,1477.64942898041));
#145568=CARTESIAN_POINT('Ctrl Pts',(-38.0491535857389,-9.90306272484582,
1479.68930691437));
#145569=CARTESIAN_POINT('Ctrl Pts',(-34.1464428607401,-19.6276492723476,
1484.03976045586));
#145570=CARTESIAN_POINT('Ctrl Pts',(-31.0416401501891,-24.2411102676192,
1486.29373534575));
#145571=CARTESIAN_POINT('Ctrl Pts',(-23.4863841819941,-31.5346631935602,
1490.64510860141));
#145572=CARTESIAN_POINT('Ctrl Pts',(-19.247643648964,-34.2867807694761,
1492.70674499341));
#145573=CARTESIAN_POINT('Ctrl Pts',(-9.96719072828815,-38.035369756234,
1496.84987692723));
#145574=CARTESIAN_POINT('Ctrl Pts',(-5.00616845072917,-39.,1498.9159421232));
#145575=CARTESIAN_POINT('Ctrl Pts',(-4.88498130835069E-14,-39.,1500.98568435754));
#145576=CARTESIAN_POINT('',(0.,-39.,1504.15181564246));
#145577=CARTESIAN_POINT('',(0.,-39.,-11.4051836540916));
#145578=CARTESIAN_POINT('Ctrl Pts',(-1.77635683940025E-14,-39.,1504.15181564246));
#145579=CARTESIAN_POINT('Ctrl Pts',(-3.18484312075356,-39.,1502.83507922385));
#145580=CARTESIAN_POINT('Ctrl Pts',(-6.35799498342694,-38.6098072039276,
1501.51747455921));
#145581=CARTESIAN_POINT('Ctrl Pts',(-12.5382317252814,-37.0666925628971,
1498.8739996287));
#145582=CARTESIAN_POINT('Ctrl Pts',(-15.5230464279844,-35.9191078993228,
1497.55933873559));
#145583=CARTESIAN_POINT('Ctrl Pts',(-23.1893713136726,-31.8356576757199,
1493.95417215531));
#145584=CARTESIAN_POINT('Ctrl Pts',(-27.4446869642291,-28.2495705127348,
1491.69599437198));
#145585=CARTESIAN_POINT('Ctrl Pts',(-34.1852574911453,-19.5599468650915,
1487.14413355563));
#145586=CARTESIAN_POINT('Ctrl Pts',(-36.5996966347151,-14.5498824765313,
1484.8860801759));
#145587=CARTESIAN_POINT('Ctrl Pts',(-38.6318850891163,-6.18454031151119,
1481.31680557566));
#145588=CARTESIAN_POINT('Ctrl Pts',(-39.,-3.09314338229533,1480.03611847813));
#145589=CARTESIAN_POINT('Ctrl Pts',(-39.,3.61204122167891E-11,1478.75181564244));
#145590=CARTESIAN_POINT('Origin',(0.,0.,0.));
#145591=CARTESIAN_POINT('',(7.57979930842467E-5,14.9999999998085,738.1874185217));
#145592=CARTESIAN_POINT('Ctrl Pts',(-4.89098483935635E-10,-15.0000000000001,
788.987499999474));
#145593=CARTESIAN_POINT('Ctrl Pts',(-1.02771888238626,-14.9999999999666,
787.882764050382));
#145594=CARTESIAN_POINT('Ctrl Pts',(-2.05351531366403,-14.8946888393821,
786.773272543722));
#145595=CARTESIAN_POINT('Ctrl Pts',(-5.88144240218294,-14.0955300452956,
782.56250888796));
#145596=CARTESIAN_POINT('Ctrl Pts',(-8.47391997558319,-12.7069392000974,
779.515000164681));
#145597=CARTESIAN_POINT('Ctrl Pts',(-12.5749111849436,-8.66937272960075,
773.311268120249));
#145598=CARTESIAN_POINT('Ctrl Pts',(-14.0037987885581,-6.09791553059049,
770.2687459843));
#145599=CARTESIAN_POINT('Ctrl Pts',(-15.2665815114232,-0.478165236301349,
764.054778185987));
#145600=CARTESIAN_POINT('Ctrl Pts',(-15.0751907911456,2.45782223945693,
761.015845209898));
#145601=CARTESIAN_POINT('Ctrl Pts',(-13.0914001141734,7.86899513846603,
754.795079275443));
#145602=CARTESIAN_POINT('Ctrl Pts',(-11.3397878890973,10.2331405877126,
751.758113120992));
#145603=CARTESIAN_POINT('Ctrl Pts',(-7.74651260584957,12.9467120513458,
746.897151285694));
#145604=CARTESIAN_POINT('Ctrl Pts',(-6.30365555683432,13.7072852422168,
745.165589145661));
#145605=CARTESIAN_POINT('Ctrl Pts',(-3.22895029994973,14.7379152250953,
741.668537470621));
#145606=CARTESIAN_POINT('Ctrl Pts',(-1.61820297783865,15.000008177294,739.92697163094));
#145607=CARTESIAN_POINT('Ctrl Pts',(7.57979930842463E-5,14.9999999998084,
738.1874185217));
#145608=CARTESIAN_POINT('',(4.22080283094658,-14.3939161961195,692.000039859602));
#145609=CARTESIAN_POINT('Ctrl Pts',(7.57979930842468E-5,14.9999999998085,
738.1874185217));
#145610=CARTESIAN_POINT('Ctrl Pts',(0.281550833006751,14.999999286898,737.884849656782));
#145611=CARTESIAN_POINT('Ctrl Pts',(0.563038542676674,14.9920711836477,
737.581477601275));
#145612=CARTESIAN_POINT('Ctrl Pts',(0.843973186420159,14.9762396678864,
737.27791284127));
#145613=CARTESIAN_POINT('Ctrl Pts',(1.12481690390502,14.9604132760944,736.974446331903));
#145614=CARTESIAN_POINT('Ctrl Pts',(1.40510753881479,14.9366886541256,736.67078765209));
#145615=CARTESIAN_POINT('Ctrl Pts',(1.68428629575425,14.905141382265,736.367544974865));
#145616=CARTESIAN_POINT('Ctrl Pts',(1.96265216582003,14.8736859668319,736.065185251611));
#145617=CARTESIAN_POINT('Ctrl Pts',(2.23991227258382,14.8344535235122,735.763239502357));
#145618=CARTESIAN_POINT('Ctrl Pts',(2.51552447619478,14.787568766651,735.462302903552));
#145619=CARTESIAN_POINT('Ctrl Pts',(2.5959084857406,14.7738945363604,735.374532876992));
#145620=CARTESIAN_POINT('Ctrl Pts',(2.67615241441217,14.7595696908977,735.286848621306));
#145621=CARTESIAN_POINT('Ctrl Pts',(2.75624306674878,14.7445980974433,735.199264705882));
#145622=CARTESIAN_POINT('Ctrl Pts',(3.03135041722587,14.693171429193,734.898418374712));
#145623=CARTESIAN_POINT('Ctrl Pts',(3.30536110980185,14.6339768655788,734.596415852432));
#145624=CARTESIAN_POINT('Ctrl Pts',(3.57772157299117,14.5670840383446,734.293852494505));
#145625=CARTESIAN_POINT('Ctrl Pts',(3.85951208359147,14.497875153468,733.980813362023));
#145626=CARTESIAN_POINT('Ctrl Pts',(4.13953565571147,14.420425401538,733.667174273596));
#145627=CARTESIAN_POINT('Ctrl Pts',(4.41718621299959,14.3348692038643,733.353604256735));
#145628=CARTESIAN_POINT('Ctrl Pts',(4.6948367702877,14.2493130061907,733.040034239875));
#145629=CARTESIAN_POINT('Ctrl Pts',(4.97011387588181,14.1556504467663,732.726533773015));
#145630=CARTESIAN_POINT('Ctrl Pts',(5.24242510239044,14.054073405876,732.413774701343));
#145631=CARTESIAN_POINT('Ctrl Pts',(5.3013229633486,14.0321034323732,732.346128425599));
#145632=CARTESIAN_POINT('Ctrl Pts',(5.36005824713267,14.0097723288205,732.278544270074));
#145633=CARTESIAN_POINT('Ctrl Pts',(5.41862499612807,13.9870834496368,732.211029411765));
#145634=CARTESIAN_POINT('Ctrl Pts',(5.6695864337698,13.8898604718194,731.921724879855));
#145635=CARTESIAN_POINT('Ctrl Pts',(5.91807648535088,13.7858223151936,731.631529191763));
#145636=CARTESIAN_POINT('Ctrl Pts',(6.16359696334797,13.6751626241441,731.341016961021));
#145637=CARTESIAN_POINT('Ctrl Pts',(6.40920526581501,13.5644633493141,731.050400811931));
#145638=CARTESIAN_POINT('Ctrl Pts',(6.65184148726155,13.4471379709317,730.75946834466));
#145639=CARTESIAN_POINT('Ctrl Pts',(6.89102818973086,13.3234278919885,730.468797102226));
#145640=CARTESIAN_POINT('Ctrl Pts',(7.12957425966607,13.2000491554675,730.178904387413));
#145641=CARTESIAN_POINT('Ctrl Pts',(7.36468892711074,13.0703201158073,729.889271942079));
#145642=CARTESIAN_POINT('Ctrl Pts',(7.59592512409975,12.9345244117713,729.600468284286));
#145643=CARTESIAN_POINT('Ctrl Pts',(7.69686130700828,12.8752486573728,729.474403510659));
#145644=CARTESIAN_POINT('Ctrl Pts',(7.79705886486056,12.8148175183969,729.348496556582));
#145645=CARTESIAN_POINT('Ctrl Pts',(7.89648244705168,12.7532570422289,729.222794117647));
#145646=CARTESIAN_POINT('Ctrl Pts',(8.12430532712643,12.6121950861993,728.934754891545));
#145647=CARTESIAN_POINT('Ctrl Pts',(8.3486274609939,12.4648505962549,728.645644306878));
#145648=CARTESIAN_POINT('Ctrl Pts',(8.56898524697153,12.311478059254,728.356027316226));
#145649=CARTESIAN_POINT('Ctrl Pts',(8.78996907191286,12.1576697891399,728.065587520427));
#145650=CARTESIAN_POINT('Ctrl Pts',(9.00696561094669,11.997799342883,727.774638876241));
#145651=CARTESIAN_POINT('Ctrl Pts',(9.21953296179767,11.8321685296063,727.483758428849));
#145652=CARTESIAN_POINT('Ctrl Pts',(9.4251841105422,11.6719267667887,727.202342219286));
#145653=CARTESIAN_POINT('Ctrl Pts',(9.62668945470535,11.5062938109494,726.920990246791));
#145654=CARTESIAN_POINT('Ctrl Pts',(9.82367643067417,11.3355803369513,726.640225589426));
#145655=CARTESIAN_POINT('Ctrl Pts',(9.91869715856878,11.2532331742471,726.504792970195));
#145656=CARTESIAN_POINT('Ctrl Pts',(10.0126295933473,11.1697367600015,726.36955024063));
#145657=CARTESIAN_POINT('Ctrl Pts',(10.105434659685,11.0851337637799,726.234558823529));
#145658=CARTESIAN_POINT('Ctrl Pts',(10.2977526973862,10.9098127079468,725.954818875402));
#145659=CARTESIAN_POINT('Ctrl Pts',(10.4856902898329,10.7293149967496,725.674134857072));
#145660=CARTESIAN_POINT('Ctrl Pts',(10.6688588721195,10.5439769826085,725.393057705533));
#145661=CARTESIAN_POINT('Ctrl Pts',(10.85220513252,10.3584591859501,725.111707902115));
#145662=CARTESIAN_POINT('Ctrl Pts',(11.0307727964269,10.1680919790287,724.829964671725));
#145663=CARTESIAN_POINT('Ctrl Pts',(11.2042076602919,9.97325077005239,724.548385119335));
#145664=CARTESIAN_POINT('Ctrl Pts',(11.3772608440206,9.77883835040691,724.267425242365));
#145665=CARTESIAN_POINT('Ctrl Pts',(11.5452035346936,9.57997194837157,723.98662879142));
#145666=CARTESIAN_POINT('Ctrl Pts',(11.707723575922,9.37705757861438,723.706546708871));
#145667=CARTESIAN_POINT('Ctrl Pts',(11.7968818188589,9.26573906960191,723.552894112124));
#145668=CARTESIAN_POINT('Ctrl Pts',(11.884408780843,9.1532028338603,723.399456426814));
#145669=CARTESIAN_POINT('Ctrl Pts',(11.9702584125853,9.03951954824237,723.246323529412));
#145670=CARTESIAN_POINT('Ctrl Pts',(12.1267446422907,8.83229828956197,722.967193738496));
#145671=CARTESIAN_POINT('Ctrl Pts',(12.2780314854468,8.62076607850108,722.687061998882));
#145672=CARTESIAN_POINT('Ctrl Pts',(12.4237935186084,8.40531704755474,722.406475004631));
#145673=CARTESIAN_POINT('Ctrl Pts',(12.5699336917389,8.18930909266857,722.125160103703));
#145674=CARTESIAN_POINT('Ctrl Pts',(12.7105200582298,7.96936429288088,721.843388047227));
#145675=CARTESIAN_POINT('Ctrl Pts',(12.8452656387393,7.74591186917703,721.561715887111));
#145676=CARTESIAN_POINT('Ctrl Pts',(12.95616527364,7.56200385443744,721.329891291452));
#145677=CARTESIAN_POINT('Ctrl Pts',(13.0631091840619,7.37572053594736,721.098134595532));
#145678=CARTESIAN_POINT('Ctrl Pts',(13.165960058574,7.18731491838453,720.866756054193));
#145679=CARTESIAN_POINT('Ctrl Pts',(13.2563153441342,7.02179913199209,720.663488223225));
#145680=CARTESIAN_POINT('Ctrl Pts',(13.3435057150174,6.85465692241973,720.460526227376));
#145681=CARTESIAN_POINT('Ctrl Pts',(13.427449370526,6.6860753367475,720.258088235294));
#145682=CARTESIAN_POINT('Ctrl Pts',(13.5406317255301,6.45877452692322,719.985138379259));
#145683=CARTESIAN_POINT('Ctrl Pts',(13.6481759951956,6.22832192582482,719.711214507562));
#145684=CARTESIAN_POINT('Ctrl Pts',(13.7498401916303,5.99515593932086,719.436852309226));
#145685=CARTESIAN_POINT('Ctrl Pts',(13.8516418206169,5.76167475240564,719.162119220267));
#145686=CARTESIAN_POINT('Ctrl Pts',(13.9475472454033,5.52547322797553,718.886947097059));
#145687=CARTESIAN_POINT('Ctrl Pts',(14.0373597882222,5.28701524906024,718.611879605197));
#145688=CARTESIAN_POINT('Ctrl Pts',(14.1270049125188,5.04900177690535,718.337324863465));
#145689=CARTESIAN_POINT('Ctrl Pts',(14.2105797159508,4.80874068116805,718.062874844367));
#145690=CARTESIAN_POINT('Ctrl Pts',(14.2879373390108,4.56671070908823,717.789068748523));
#145691=CARTESIAN_POINT('Ctrl Pts',(14.3369205063337,4.41345632832305,717.615693594579));
#145692=CARTESIAN_POINT('Ctrl Pts',(14.3834118976418,4.2594930507057,717.442576567067));
#145693=CARTESIAN_POINT('Ctrl Pts',(14.4273846515339,4.10494485220273,717.269852941177));
#145694=CARTESIAN_POINT('Ctrl Pts',(14.4968417248649,3.86082856185289,716.997027691729));
#145695=CARTESIAN_POINT('Ctrl Pts',(14.5601755404354,3.61467881023674,716.723259252437));
#145696=CARTESIAN_POINT('Ctrl Pts',(14.6172331099927,3.36697139101017,716.449082865871));
#145697=CARTESIAN_POINT('Ctrl Pts',(14.674422462025,3.11869185668948,716.174273230412));
#145698=CARTESIAN_POINT('Ctrl Pts',(14.7253063946445,2.86884787430016,715.899054239511));
#145699=CARTESIAN_POINT('Ctrl Pts',(14.7697809208011,2.61793271182503,715.623969958683));
#145700=CARTESIAN_POINT('Ctrl Pts',(14.7983938528386,2.45650505623126,715.44699296731));
#145701=CARTESIAN_POINT('Ctrl Pts',(14.8243549155049,2.29463430283197,715.270071817007));
#145702=CARTESIAN_POINT('Ctrl Pts',(14.8476476804061,2.13245362629643,715.093351086719));
#145703=CARTESIAN_POINT('Ctrl Pts',(14.8833806436034,1.88365550505326,714.822247360802));
#145704=CARTESIAN_POINT('Ctrl Pts',(14.9128478753549,1.63401309449245,714.551490612981));
#145705=CARTESIAN_POINT('Ctrl Pts',(14.936012647393,1.38402539222435,714.281617647059));
#145706=CARTESIAN_POINT('Ctrl Pts',(14.9590391181592,1.13553019836948,714.013355911083));
#145707=CARTESIAN_POINT('Ctrl Pts',(14.9758914132006,0.886119743165234,
713.744106109306));
#145708=CARTESIAN_POINT('Ctrl Pts',(14.986498794157,0.636281385739037,713.474394367854));
#145709=CARTESIAN_POINT('Ctrl Pts',(14.9971225801966,0.386056635191933,
713.204265497653));
#145710=CARTESIAN_POINT('Ctrl Pts',(15.001482045022,0.135403105453872,712.933673741051));
#145711=CARTESIAN_POINT('Ctrl Pts',(14.9995577562733,-0.115183625524045,
712.663154096745));
#145712=CARTESIAN_POINT('Ctrl Pts',(14.9976367462435,-0.365343391752358,
712.393095380086));
#145713=CARTESIAN_POINT('Ctrl Pts',(14.9894534009396,-0.615436134420939,
712.123109018403));
#145714=CARTESIAN_POINT('Ctrl Pts',(14.9750401577341,-0.864969637016497,
711.853726381551));
#145715=CARTESIAN_POINT('Ctrl Pts',(14.9650277479948,-1.03831241879351,
711.666595053899));
#145716=CARTESIAN_POINT('Ctrl Pts',(14.9520101078572,-1.2113853461834,711.479755046204));
#145717=CARTESIAN_POINT('Ctrl Pts',(14.9360126519092,-1.38402539264299,
711.293382352941));
#145718=CARTESIAN_POINT('Ctrl Pts',(14.9129720146043,-1.63267347191893,
711.024955570398));
#145719=CARTESIAN_POINT('Ctrl Pts',(14.8836946574883,-1.88099800592914,
710.755634970035));
#145720=CARTESIAN_POINT('Ctrl Pts',(14.8482138789356,-2.12850765735087,
710.485948546402));
#145721=CARTESIAN_POINT('Ctrl Pts',(14.8126588775094,-2.3765350786264,710.21569796093));
#145722=CARTESIAN_POINT('Ctrl Pts',(14.7708744994095,-2.62374375064837,
709.945080506721));
#145723=CARTESIAN_POINT('Ctrl Pts',(14.722945983439,-2.86964488842252,709.674631773074));
#145724=CARTESIAN_POINT('Ctrl Pts',(14.7019882738472,-2.97717011697189,
709.55637261348));
#145725=CARTESIAN_POINT('Ctrl Pts',(14.679856436388,-3.08444545163411,709.4381457253));
#145726=CARTESIAN_POINT('Ctrl Pts',(14.656560656033,-3.19143070180115,709.319995777693));
#145727=CARTESIAN_POINT('Ctrl Pts',(14.6039181339553,-3.43319008088539,
709.053007029918));
#145728=CARTESIAN_POINT('Ctrl Pts',(14.5452834571176,-3.67367460155924,
708.786182476552));
#145729=CARTESIAN_POINT('Ctrl Pts',(14.480781628501,-3.91241147646642,708.520048618717));
#145730=CARTESIAN_POINT('Ctrl Pts',(14.4634070462039,-3.97671900959168,
708.448361277224));
#145731=CARTESIAN_POINT('Ctrl Pts',(14.4456070353278,-4.0408998169529,708.376724021998));
#145732=CARTESIAN_POINT('Ctrl Pts',(14.427384651626,-4.10494485222909,708.305147058823));
#145733=CARTESIAN_POINT('Ctrl Pts',(14.3598586870102,-4.34227399953762,
708.039907145005));
#145734=CARTESIAN_POINT('Ctrl Pts',(14.2863747232897,-4.57827959615286,
707.773676097403));
#145735=CARTESIAN_POINT('Ctrl Pts',(14.2070397540541,-4.81248600453167,
707.506974439535));
#145736=CARTESIAN_POINT('Ctrl Pts',(14.1275767982191,-5.04707024480546,
707.239842527032));
#145737=CARTESIAN_POINT('Ctrl Pts',(14.0422440323164,-5.2798490384921,706.972238970869));
#145738=CARTESIAN_POINT('Ctrl Pts',(13.9511993147848,-5.5103573213283,706.704693487103));
#145739=CARTESIAN_POINT('Ctrl Pts',(13.860307689284,-5.74047800363047,706.437597882061));
#145740=CARTESIAN_POINT('Ctrl Pts',(13.763723489821,-5.96833538710859,706.170560646299));
#145741=CARTESIAN_POINT('Ctrl Pts',(13.6616518215246,-6.19348606661768,
705.904108117904));
#145742=CARTESIAN_POINT('Ctrl Pts',(13.5865236513097,-6.35920451578658,
705.70799012315));
#145743=CARTESIAN_POINT('Ctrl Pts',(13.5084236875781,-6.52345699766309,
705.512188908077));
#145744=CARTESIAN_POINT('Ctrl Pts',(13.4274493751688,-6.68607533905936,
705.316911764706));
#145745=CARTESIAN_POINT('Ctrl Pts',(13.3173414711156,-6.90720181977887,
705.051376234656));
#145746=CARTESIAN_POINT('Ctrl Pts',(13.2016653434899,-7.12581135822056,
704.784986412623));
#145747=CARTESIAN_POINT('Ctrl Pts',(13.080631160973,-7.34146365485426,704.518265866849));
#145748=CARTESIAN_POINT('Ctrl Pts',(12.9593584746677,-7.55754090490723,
704.251019735167));
#145749=CARTESIAN_POINT('Ctrl Pts',(12.8327067931809,-7.77064883360974,
703.983442066405));
#145750=CARTESIAN_POINT('Ctrl Pts',(12.7009334371162,-7.98036903689955,
703.71606312886));
#145751=CARTESIAN_POINT('Ctrl Pts',(12.6731015715451,-8.02466406496766,
703.65958999295));
#145752=CARTESIAN_POINT('Ctrl Pts',(12.6450413858188,-8.06880806697079,
703.603125719969));
#145753=CARTESIAN_POINT('Ctrl Pts',(12.6167555513653,-8.11279726641198,
703.546675294356));
#145754=CARTESIAN_POINT('Ctrl Pts',(12.4837064090762,-8.31971091660871,
703.281147306415));
#145755=CARTESIAN_POINT('Ctrl Pts',(12.3455131459612,-8.52342765962367,
703.015630151262));
#145756=CARTESIAN_POINT('Ctrl Pts',(12.2024496090295,-8.72354421217255,
702.750649610741));
#145757=CARTESIAN_POINT('Ctrl Pts',(12.1264122948955,-8.82990482296075,
702.609814223674));
#145758=CARTESIAN_POINT('Ctrl Pts',(12.048999936094,-8.93524891659357,702.46913039669));
#145759=CARTESIAN_POINT('Ctrl Pts',(11.9702584108949,-9.03951954696603,
702.328676470588));
#145760=CARTESIAN_POINT('Ctrl Pts',(11.8224697257209,-9.23522339352024,
702.065060786061));
#145761=CARTESIAN_POINT('Ctrl Pts',(11.6696609069418,-9.42758811617559,
701.800457965802));
#145762=CARTESIAN_POINT('Ctrl Pts',(11.5121019326805,-9.61621074689837,
701.535385846013));
#145763=CARTESIAN_POINT('Ctrl Pts',(11.3542910307001,-9.8051349743366,701.269889891181));
#145764=CARTESIAN_POINT('Ctrl Pts',(11.1917150167255,-9.99030474597149,
701.003923622989));
#145765=CARTESIAN_POINT('Ctrl Pts',(11.0246874612152,-10.1713453586207,
700.738014032166));
#145766=CARTESIAN_POINT('Ctrl Pts',(10.8579517744045,-10.3520696157557,
700.472569099323));
#145767=CARTESIAN_POINT('Ctrl Pts',(10.6867804145302,-10.528678809136,700.207181139665));
#145768=CARTESIAN_POINT('Ctrl Pts',(10.5115231038306,-10.7008355773604,
699.942373645533));
#145769=CARTESIAN_POINT('Ctrl Pts',(10.3784595745027,-10.8315450301425,
699.741319437745));
#145770=CARTESIAN_POINT('Ctrl Pts',(10.2430414898439,-10.9596885536914,
699.540599879091));
#145771=CARTESIAN_POINT('Ctrl Pts',(10.1054346550857,-11.0851337587347,
699.340441176471));
#145772=CARTESIAN_POINT('Ctrl Pts',(9.92365192039655,-11.2508506176865,
699.076025557885));
#145773=CARTESIAN_POINT('Ctrl Pts',(9.73763449665069,-11.4122344480125,
698.810780717394));
#145774=CARTESIAN_POINT('Ctrl Pts',(9.54773966847933,-11.5689527290905,
698.545230782436));
#145775=CARTESIAN_POINT('Ctrl Pts',(9.36384501633439,-11.7207191255803,
698.28807152546));
#145776=CARTESIAN_POINT('Ctrl Pts',(9.17631459608406,-11.8681100780542,
698.030626608508));
#145777=CARTESIAN_POINT('Ctrl Pts',(8.9855029746898,-12.0108591004051,697.773374857605));
#145778=CARTESIAN_POINT('Ctrl Pts',(8.78880252026194,-12.1580136466555,
697.508183796729));
#145779=CARTESIAN_POINT('Ctrl Pts',(8.58837255017628,-12.3004165090796,
697.242871083569));
#145780=CARTESIAN_POINT('Ctrl Pts',(8.38460658247155,-12.4377800472919,
696.977962862677));
#145781=CARTESIAN_POINT('Ctrl Pts',(8.22390426457572,-12.5461133437386,
696.769040020425));
#145782=CARTESIAN_POINT('Ctrl Pts',(8.06112772889969,-12.6513129929349,
696.560368909545));
#145783=CARTESIAN_POINT('Ctrl Pts',(7.8964824440045,-12.7532570373073,696.352205882353));
#145784=CARTESIAN_POINT('Ctrl Pts',(7.68827459184559,-12.882173881374,696.088966173921));
#145785=CARTESIAN_POINT('Ctrl Pts',(7.47660549231053,-13.0061753066193,
695.824746896223));
#145786=CARTESIAN_POINT('Ctrl Pts',(7.26187257153882,-13.1249840684397,
695.560065518168));
#145787=CARTESIAN_POINT('Ctrl Pts',(7.04680900420729,-13.2439757724389,
695.294976582731));
#145788=CARTESIAN_POINT('Ctrl Pts',(6.82867254414394,-13.3577585382978,
695.029424611831));
#145789=CARTESIAN_POINT('Ctrl Pts',(6.60789087379473,-13.4660973645443,
694.763935985973));
#145790=CARTESIAN_POINT('Ctrl Pts',(6.38751841202005,-13.5742353898067,
694.498939430956));
#145791=CARTESIAN_POINT('Ctrl Pts',(6.16451095707521,-13.6769494552564,
694.234006480313));
#145792=CARTESIAN_POINT('Ctrl Pts',(5.93931613867606,-13.7740525563051,
693.969659695136));
#145793=CARTESIAN_POINT('Ctrl Pts',(5.76696412404157,-13.8483700526488,
693.767342868704));
#145794=CARTESIAN_POINT('Ctrl Pts',(5.5933313572213,-13.9194018353776,693.56536943067));
#145795=CARTESIAN_POINT('Ctrl Pts',(5.41862499293033,-13.9870834413829,
693.363970588235));
#145796=CARTESIAN_POINT('Ctrl Pts',(5.18968353158942,-14.0757758358909,
693.100050349918));
#145797=CARTESIAN_POINT('Ctrl Pts',(4.95837761299169,-14.1589149892218,
692.835315617544));
#145798=CARTESIAN_POINT('Ctrl Pts',(4.72516014117508,-14.2363219141141,
692.57028953527));
#145799=CARTESIAN_POINT('Ctrl Pts',(4.55797722240539,-14.2918113915349,
692.380304481237));
#145800=CARTESIAN_POINT('Ctrl Pts',(4.38981249519733,-14.3443561624571,
692.190169941154));
#145801=CARTESIAN_POINT('Ctrl Pts',(4.22083826280853,-14.3939058062505,
692.000079719204));
#145802=CARTESIAN_POINT('',(-0.139482600723335,-14.9993514727836,692.));
#145803=CARTESIAN_POINT('Origin',(0.,-8.44020893219807E-14,692.));
#145804=CARTESIAN_POINT('Ctrl Pts',(-0.139482600723493,-14.9993514727837,
692.));
#145805=CARTESIAN_POINT('Ctrl Pts',(-0.0929871732231087,-14.9997838450207,
692.050022854097));
#145806=CARTESIAN_POINT('Ctrl Pts',(-0.046497364483948,-15.0000000000001,
692.100018131429));
#145807=CARTESIAN_POINT('Ctrl Pts',(-3.60480930607215E-12,-15.0000000000001,
692.149999999996));
#145808=CARTESIAN_POINT('Origin',(0.,0.,0.));
#145809=CARTESIAN_POINT('',(-1.40148579694423E-15,-11.4440000000002,1504.95));
#145810=CARTESIAN_POINT('Origin',(0.,-1.83556249024732E-13,1504.95));
#145811=CARTESIAN_POINT('',(-1.40148579694423E-15,-11.444,-1.39580565057911E-15));
#145812=CARTESIAN_POINT('',(-1.40148579694423E-15,-11.4440000000001,692.));
#145813=CARTESIAN_POINT('',(-1.40148579694423E-15,-11.444,-1.39580565057911E-15));
#145814=CARTESIAN_POINT('Origin',(0.,-8.44020893219807E-14,692.));
#145815=CARTESIAN_POINT('Ctrl Pts',(0.,-50.8,1501.378125));
#145816=CARTESIAN_POINT('Ctrl Pts',(-4.70731322909511,-50.8,1499.88400735294));
#145817=CARTESIAN_POINT('Ctrl Pts',(-9.33447550508177,-49.9350334639422,
1498.38988970588));
#145818=CARTESIAN_POINT('Ctrl Pts',(-13.9616377810684,-49.0700669278844,
1496.89577205882));
#145819=CARTESIAN_POINT('Ctrl Pts',(-18.3510766423074,-47.3695892537413,
1495.40165441176));
#145820=CARTESIAN_POINT('Ctrl Pts',(-22.7405155035463,-45.6691115795981,
1493.90753676471));
#145821=CARTESIAN_POINT('Ctrl Pts',(-26.7427538741697,-43.1910304950644,
1492.41341911765));
#145822=CARTESIAN_POINT('Ctrl Pts',(-30.744992244793,-40.7129494105307,
1490.91930147059));
#145823=CARTESIAN_POINT('Ctrl Pts',(-34.2237386972451,-37.5416529948095,
1489.42518382353));
#145824=CARTESIAN_POINT('Ctrl Pts',(-37.7024851496972,-34.3703565790883,
1487.93106617647));
#145825=CARTESIAN_POINT('Ctrl Pts',(-40.5392751458362,-30.6138395280662,
1486.43694852941));
#145826=CARTESIAN_POINT('Ctrl Pts',(-43.3760651419751,-26.8573224770441,
1484.94283088235));
#145827=CARTESIAN_POINT('Ctrl Pts',(-45.4742952008371,-22.6435084734481,
1483.44871323529));
#145828=CARTESIAN_POINT('Ctrl Pts',(-47.5725252596992,-18.4296944698521,
1481.95459558824));
#145829=CARTESIAN_POINT('Ctrl Pts',(-48.8607426731792,-13.9020798956618,
1480.46047794118));
#145830=CARTESIAN_POINT('Ctrl Pts',(-50.1489600866593,-9.37446532147148,
1478.96636029412));
#145831=CARTESIAN_POINT('Ctrl Pts',(-50.5832961557877,-4.68723266073574,
1477.47224264706));
#145832=CARTESIAN_POINT('Ctrl Pts',(-51.0176322249162,-3.12392900021603E-15,
1475.978125));
#145833=CARTESIAN_POINT('Ctrl Pts',(-50.5832961557877,4.68723266073573,
1474.48400735294));
#145834=CARTESIAN_POINT('Ctrl Pts',(-50.1489600866593,9.37446532147149,
1472.98988970588));
#145835=CARTESIAN_POINT('Ctrl Pts',(-48.8607426731792,13.9020798956618,
1471.49577205882));
#145836=CARTESIAN_POINT('Ctrl Pts',(-47.5725252596992,18.4296944698521,
1470.00165441177));
#145837=CARTESIAN_POINT('Ctrl Pts',(-45.4742952008371,22.6435084734481,
1468.50753676471));
#145838=CARTESIAN_POINT('Ctrl Pts',(-43.3760651419751,26.8573224770442,
1467.01341911765));
#145839=CARTESIAN_POINT('Ctrl Pts',(-40.5392751458362,30.6138395280662,
1465.51930147059));
#145840=CARTESIAN_POINT('Ctrl Pts',(-37.7024851496972,34.3703565790883,
1464.02518382353));
#145841=CARTESIAN_POINT('Ctrl Pts',(-34.2237386972451,37.5416529948095,
1462.53106617647));
#145842=CARTESIAN_POINT('Ctrl Pts',(-30.744992244793,40.7129494105307,1461.03694852941));
#145843=CARTESIAN_POINT('Ctrl Pts',(-26.7427538741697,43.1910304950644,
1459.54283088235));
#145844=CARTESIAN_POINT('Ctrl Pts',(-22.7405155035463,45.6691115795981,
1458.04871323529));
#145845=CARTESIAN_POINT('Ctrl Pts',(-18.3510766423074,47.3695892537413,
1456.55459558824));
#145846=CARTESIAN_POINT('Ctrl Pts',(-13.9616377810684,49.0700669278844,
1455.06047794118));
#145847=CARTESIAN_POINT('Ctrl Pts',(-9.33447550508177,49.9350334639422,
1453.56636029412));
#145848=CARTESIAN_POINT('Ctrl Pts',(-4.7073132290951,50.8,1452.07224264706));
#145849=CARTESIAN_POINT('Ctrl Pts',(-6.22120573966855E-15,50.8,1450.578125));
#145850=CARTESIAN_POINT('Ctrl Pts',(4.70731322909511,50.8,1449.08400735294));
#145851=CARTESIAN_POINT('Ctrl Pts',(9.33447550508176,49.9350334639422,1447.58988970588));
#145852=CARTESIAN_POINT('Ctrl Pts',(13.9616377810684,49.0700669278844,1446.09577205882));
#145853=CARTESIAN_POINT('Ctrl Pts',(18.3510766423074,47.3695892537413,1444.60165441176));
#145854=CARTESIAN_POINT('Ctrl Pts',(22.7405155035463,45.6691115795981,1443.10753676471));
#145855=CARTESIAN_POINT('Ctrl Pts',(26.7427538741697,43.1910304950644,1441.61341911765));
#145856=CARTESIAN_POINT('Ctrl Pts',(30.744992244793,40.7129494105307,1440.11930147059));
#145857=CARTESIAN_POINT('Ctrl Pts',(34.2237386972451,37.5416529948095,1438.62518382353));
#145858=CARTESIAN_POINT('Ctrl Pts',(37.7024851496972,34.3703565790883,1437.13106617647));
#145859=CARTESIAN_POINT('Ctrl Pts',(40.5392751458362,30.6138395280662,1435.63694852941));
#145860=CARTESIAN_POINT('Ctrl Pts',(43.3760651419751,26.8573224770442,1434.14283088235));
#145861=CARTESIAN_POINT('Ctrl Pts',(45.4742952008372,22.6435084734481,1432.64871323529));
#145862=CARTESIAN_POINT('Ctrl Pts',(47.5725252596992,18.4296944698521,1431.15459558824));
#145863=CARTESIAN_POINT('Ctrl Pts',(48.8607426731792,13.9020798956618,1429.66047794118));
#145864=CARTESIAN_POINT('Ctrl Pts',(50.1489600866593,9.37446532147146,1428.16636029412));
#145865=CARTESIAN_POINT('Ctrl Pts',(50.5832961557877,4.68723266073574,1426.67224264706));
#145866=CARTESIAN_POINT('Ctrl Pts',(51.0176322249162,9.37178700064808E-15,
1425.178125));
#145867=CARTESIAN_POINT('Ctrl Pts',(50.5832961557877,-4.68723266073572,
1423.68400735294));
#145868=CARTESIAN_POINT('Ctrl Pts',(50.1489600866593,-9.37446532147149,
1422.18988970588));
#145869=CARTESIAN_POINT('Ctrl Pts',(48.8607426731792,-13.9020798956618,
1420.69577205882));
#145870=CARTESIAN_POINT('Ctrl Pts',(47.5725252596992,-18.4296944698521,
1419.20165441177));
#145871=CARTESIAN_POINT('Ctrl Pts',(45.4742952008371,-22.6435084734482,
1417.70753676471));
#145872=CARTESIAN_POINT('Ctrl Pts',(43.3760651419751,-26.8573224770441,
1416.21341911765));
#145873=CARTESIAN_POINT('Ctrl Pts',(40.5392751458362,-30.6138395280662,
1414.71930147059));
#145874=CARTESIAN_POINT('Ctrl Pts',(37.7024851496972,-34.3703565790883,
1413.22518382353));
#145875=CARTESIAN_POINT('Ctrl Pts',(34.2237386972451,-37.5416529948095,
1411.73106617647));
#145876=CARTESIAN_POINT('Ctrl Pts',(30.744992244793,-40.7129494105307,1410.23694852941));
#145877=CARTESIAN_POINT('Ctrl Pts',(26.7427538741697,-43.1910304950644,
1408.74283088235));
#145878=CARTESIAN_POINT('Ctrl Pts',(22.7405155035463,-45.6691115795981,
1407.24871323529));
#145879=CARTESIAN_POINT('Ctrl Pts',(18.3510766423074,-47.3695892537413,
1405.75459558824));
#145880=CARTESIAN_POINT('Ctrl Pts',(13.9616377810684,-49.0700669278844,
1404.26047794118));
#145881=CARTESIAN_POINT('Ctrl Pts',(9.33447550508176,-49.9350334639422,
1402.76636029412));
#145882=CARTESIAN_POINT('Ctrl Pts',(4.70731322909511,-50.8,1401.27224264706));
#145883=CARTESIAN_POINT('Ctrl Pts',(0.,-50.8,1399.778125));
#145884=CARTESIAN_POINT('Ctrl Pts',(-4.70731322909511,-50.8,1398.28400735294));
#145885=CARTESIAN_POINT('Ctrl Pts',(-9.33447550508177,-49.9350334639422,
1396.78988970588));
#145886=CARTESIAN_POINT('Ctrl Pts',(-13.9616377810684,-49.0700669278844,
1395.29577205882));
#145887=CARTESIAN_POINT('Ctrl Pts',(-18.3510766423074,-47.3695892537413,
1393.80165441176));
#145888=CARTESIAN_POINT('Ctrl Pts',(-22.7405155035463,-45.6691115795981,
1392.30753676471));
#145889=CARTESIAN_POINT('Ctrl Pts',(-26.7427538741697,-43.1910304950644,
1390.81341911765));
#145890=CARTESIAN_POINT('Ctrl Pts',(-30.744992244793,-40.7129494105307,
1389.31930147059));
#145891=CARTESIAN_POINT('Ctrl Pts',(-34.2237386972451,-37.5416529948095,
1387.82518382353));
#145892=CARTESIAN_POINT('Ctrl Pts',(-37.7024851496972,-34.3703565790883,
1386.33106617647));
#145893=CARTESIAN_POINT('Ctrl Pts',(-40.5392751458362,-30.6138395280662,
1384.83694852941));
#145894=CARTESIAN_POINT('Ctrl Pts',(-43.3760651419751,-26.8573224770441,
1383.34283088235));
#145895=CARTESIAN_POINT('Ctrl Pts',(-45.4742952008371,-22.6435084734481,
1381.84871323529));
#145896=CARTESIAN_POINT('Ctrl Pts',(-47.5725252596992,-18.4296944698521,
1380.35459558824));
#145897=CARTESIAN_POINT('Ctrl Pts',(-48.8607426731792,-13.9020798956618,
1378.86047794118));
#145898=CARTESIAN_POINT('Ctrl Pts',(-50.1489600866593,-9.37446532147148,
1377.36636029412));
#145899=CARTESIAN_POINT('Ctrl Pts',(-50.5832961557877,-4.68723266073574,
1375.87224264706));
#145900=CARTESIAN_POINT('Ctrl Pts',(-51.0176322249162,-3.12392900021603E-15,
1374.378125));
#145901=CARTESIAN_POINT('Ctrl Pts',(-50.5832961557877,4.68723266073573,
1372.88400735294));
#145902=CARTESIAN_POINT('Ctrl Pts',(-50.1489600866593,9.37446532147149,
1371.38988970588));
#145903=CARTESIAN_POINT('Ctrl Pts',(-48.8607426731792,13.9020798956618,
1369.89577205882));
#145904=CARTESIAN_POINT('Ctrl Pts',(-47.5725252596992,18.4296944698521,
1368.40165441177));
#145905=CARTESIAN_POINT('Ctrl Pts',(-45.4742952008371,22.6435084734481,
1366.90753676471));
#145906=CARTESIAN_POINT('Ctrl Pts',(-43.3760651419751,26.8573224770442,
1365.41341911765));
#145907=CARTESIAN_POINT('Ctrl Pts',(-40.5392751458362,30.6138395280662,
1363.91930147059));
#145908=CARTESIAN_POINT('Ctrl Pts',(-37.7024851496972,34.3703565790883,
1362.42518382353));
#145909=CARTESIAN_POINT('Ctrl Pts',(-34.2237386972451,37.5416529948095,
1360.93106617647));
#145910=CARTESIAN_POINT('Ctrl Pts',(-30.744992244793,40.7129494105307,1359.43694852941));
#145911=CARTESIAN_POINT('Ctrl Pts',(-26.7427538741697,43.1910304950644,
1357.94283088235));
#145912=CARTESIAN_POINT('Ctrl Pts',(-22.7405155035463,45.6691115795981,
1356.44871323529));
#145913=CARTESIAN_POINT('Ctrl Pts',(-18.3510766423074,47.3695892537413,
1354.95459558824));
#145914=CARTESIAN_POINT('Ctrl Pts',(-13.9616377810684,49.0700669278844,
1353.46047794118));
#145915=CARTESIAN_POINT('Ctrl Pts',(-9.33447550508177,49.9350334639422,
1351.96636029412));
#145916=CARTESIAN_POINT('Ctrl Pts',(-4.7073132290951,50.8,1350.47224264706));
#145917=CARTESIAN_POINT('Ctrl Pts',(-6.22120573966855E-15,50.8,1348.978125));
#145918=CARTESIAN_POINT('Ctrl Pts',(4.70731322909511,50.8,1347.48400735294));
#145919=CARTESIAN_POINT('Ctrl Pts',(9.33447550508176,49.9350334639422,1345.98988970588));
#145920=CARTESIAN_POINT('Ctrl Pts',(13.9616377810684,49.0700669278844,1344.49577205882));
#145921=CARTESIAN_POINT('Ctrl Pts',(18.3510766423074,47.3695892537413,1343.00165441176));
#145922=CARTESIAN_POINT('Ctrl Pts',(22.7405155035463,45.6691115795981,1341.50753676471));
#145923=CARTESIAN_POINT('Ctrl Pts',(26.7427538741697,43.1910304950644,1340.01341911765));
#145924=CARTESIAN_POINT('Ctrl Pts',(30.744992244793,40.7129494105307,1338.51930147059));
#145925=CARTESIAN_POINT('Ctrl Pts',(34.2237386972451,37.5416529948095,1337.02518382353));
#145926=CARTESIAN_POINT('Ctrl Pts',(37.7024851496972,34.3703565790883,1335.53106617647));
#145927=CARTESIAN_POINT('Ctrl Pts',(40.5392751458362,30.6138395280662,1334.03694852941));
#145928=CARTESIAN_POINT('Ctrl Pts',(43.3760651419751,26.8573224770442,1332.54283088235));
#145929=CARTESIAN_POINT('Ctrl Pts',(45.4742952008372,22.6435084734481,1331.04871323529));
#145930=CARTESIAN_POINT('Ctrl Pts',(47.5725252596992,18.4296944698521,1329.55459558824));
#145931=CARTESIAN_POINT('Ctrl Pts',(48.8607426731792,13.9020798956618,1328.06047794118));
#145932=CARTESIAN_POINT('Ctrl Pts',(50.1489600866593,9.37446532147146,1326.56636029412));
#145933=CARTESIAN_POINT('Ctrl Pts',(50.5832961557877,4.68723266073574,1325.07224264706));
#145934=CARTESIAN_POINT('Ctrl Pts',(51.0176322249162,9.37178700064808E-15,
1323.578125));
#145935=CARTESIAN_POINT('Ctrl Pts',(50.5832961557877,-4.68723266073572,
1322.08400735294));
#145936=CARTESIAN_POINT('Ctrl Pts',(50.1489600866593,-9.37446532147149,
1320.58988970588));
#145937=CARTESIAN_POINT('Ctrl Pts',(48.8607426731792,-13.9020798956618,
1319.09577205882));
#145938=CARTESIAN_POINT('Ctrl Pts',(47.5725252596992,-18.4296944698521,
1317.60165441176));
#145939=CARTESIAN_POINT('Ctrl Pts',(45.4742952008371,-22.6435084734482,
1316.10753676471));
#145940=CARTESIAN_POINT('Ctrl Pts',(43.3760651419751,-26.8573224770441,
1314.61341911765));
#145941=CARTESIAN_POINT('Ctrl Pts',(40.5392751458362,-30.6138395280662,
1313.11930147059));
#145942=CARTESIAN_POINT('Ctrl Pts',(37.7024851496972,-34.3703565790883,
1311.62518382353));
#145943=CARTESIAN_POINT('Ctrl Pts',(34.2237386972451,-37.5416529948095,
1310.13106617647));
#145944=CARTESIAN_POINT('Ctrl Pts',(30.744992244793,-40.7129494105307,1308.63694852941));
#145945=CARTESIAN_POINT('Ctrl Pts',(26.7427538741697,-43.1910304950644,
1307.14283088235));
#145946=CARTESIAN_POINT('Ctrl Pts',(22.7405155035463,-45.6691115795981,
1305.64871323529));
#145947=CARTESIAN_POINT('Ctrl Pts',(18.3510766423074,-47.3695892537413,
1304.15459558824));
#145948=CARTESIAN_POINT('Ctrl Pts',(13.9616377810684,-49.0700669278844,
1302.66047794118));
#145949=CARTESIAN_POINT('Ctrl Pts',(9.33447550508176,-49.9350334639422,
1301.16636029412));
#145950=CARTESIAN_POINT('Ctrl Pts',(4.70731322909511,-50.8,1299.67224264706));
#145951=CARTESIAN_POINT('Ctrl Pts',(0.,-50.8,1298.178125));
#145952=CARTESIAN_POINT('Ctrl Pts',(-4.70731322909511,-50.8,1296.68400735294));
#145953=CARTESIAN_POINT('Ctrl Pts',(-9.33447550508177,-49.9350334639422,
1295.18988970588));
#145954=CARTESIAN_POINT('Ctrl Pts',(-13.9616377810684,-49.0700669278844,
1293.69577205882));
#145955=CARTESIAN_POINT('Ctrl Pts',(-18.3510766423074,-47.3695892537413,
1292.20165441176));
#145956=CARTESIAN_POINT('Ctrl Pts',(-22.7405155035463,-45.6691115795981,
1290.70753676471));
#145957=CARTESIAN_POINT('Ctrl Pts',(-26.7427538741697,-43.1910304950644,
1289.21341911765));
#145958=CARTESIAN_POINT('Ctrl Pts',(-30.744992244793,-40.7129494105307,
1287.71930147059));
#145959=CARTESIAN_POINT('Ctrl Pts',(-34.2237386972451,-37.5416529948095,
1286.22518382353));
#145960=CARTESIAN_POINT('Ctrl Pts',(-37.7024851496972,-34.3703565790883,
1284.73106617647));
#145961=CARTESIAN_POINT('Ctrl Pts',(-40.5392751458362,-30.6138395280662,
1283.23694852941));
#145962=CARTESIAN_POINT('Ctrl Pts',(-43.3760651419751,-26.8573224770441,
1281.74283088235));
#145963=CARTESIAN_POINT('Ctrl Pts',(-45.4742952008371,-22.6435084734481,
1280.24871323529));
#145964=CARTESIAN_POINT('Ctrl Pts',(-47.5725252596992,-18.4296944698521,
1278.75459558824));
#145965=CARTESIAN_POINT('Ctrl Pts',(-48.8607426731792,-13.9020798956618,
1277.26047794118));
#145966=CARTESIAN_POINT('Ctrl Pts',(-50.1489600866593,-9.37446532147148,
1275.76636029412));
#145967=CARTESIAN_POINT('Ctrl Pts',(-50.5832961557877,-4.68723266073574,
1274.27224264706));
#145968=CARTESIAN_POINT('Ctrl Pts',(-51.0176322249162,-3.12392900021603E-15,
1272.778125));
#145969=CARTESIAN_POINT('Ctrl Pts',(-50.5832961557877,4.68723266073573,
1271.28400735294));
#145970=CARTESIAN_POINT('Ctrl Pts',(-50.1489600866593,9.37446532147149,
1269.78988970588));
#145971=CARTESIAN_POINT('Ctrl Pts',(-48.8607426731792,13.9020798956618,
1268.29577205882));
#145972=CARTESIAN_POINT('Ctrl Pts',(-47.5725252596992,18.4296944698521,
1266.80165441176));
#145973=CARTESIAN_POINT('Ctrl Pts',(-45.4742952008371,22.6435084734481,
1265.30753676471));
#145974=CARTESIAN_POINT('Ctrl Pts',(-43.3760651419751,26.8573224770442,
1263.81341911765));
#145975=CARTESIAN_POINT('Ctrl Pts',(-40.5392751458362,30.6138395280662,
1262.31930147059));
#145976=CARTESIAN_POINT('Ctrl Pts',(-37.7024851496972,34.3703565790883,
1260.82518382353));
#145977=CARTESIAN_POINT('Ctrl Pts',(-34.2237386972451,37.5416529948095,
1259.33106617647));
#145978=CARTESIAN_POINT('Ctrl Pts',(-30.744992244793,40.7129494105307,1257.83694852941));
#145979=CARTESIAN_POINT('Ctrl Pts',(-26.7427538741697,43.1910304950644,
1256.34283088235));
#145980=CARTESIAN_POINT('Ctrl Pts',(-22.7405155035463,45.6691115795981,
1254.84871323529));
#145981=CARTESIAN_POINT('Ctrl Pts',(-18.3510766423074,47.3695892537413,
1253.35459558824));
#145982=CARTESIAN_POINT('Ctrl Pts',(-13.9616377810684,49.0700669278844,
1251.86047794118));
#145983=CARTESIAN_POINT('Ctrl Pts',(-9.33447550508177,49.9350334639422,
1250.36636029412));
#145984=CARTESIAN_POINT('Ctrl Pts',(-4.7073132290951,50.8,1248.87224264706));
#145985=CARTESIAN_POINT('Ctrl Pts',(-6.22120573966855E-15,50.8,1247.378125));
#145986=CARTESIAN_POINT('Ctrl Pts',(4.70731322909511,50.8,1245.88400735294));
#145987=CARTESIAN_POINT('Ctrl Pts',(9.33447550508176,49.9350334639422,1244.38988970588));
#145988=CARTESIAN_POINT('Ctrl Pts',(13.9616377810684,49.0700669278844,1242.89577205882));
#145989=CARTESIAN_POINT('Ctrl Pts',(18.3510766423074,47.3695892537413,1241.40165441176));
#145990=CARTESIAN_POINT('Ctrl Pts',(22.7405155035463,45.6691115795981,1239.90753676471));
#145991=CARTESIAN_POINT('Ctrl Pts',(26.7427538741697,43.1910304950644,1238.41341911765));
#145992=CARTESIAN_POINT('Ctrl Pts',(30.744992244793,40.7129494105307,1236.91930147059));
#145993=CARTESIAN_POINT('Ctrl Pts',(34.2237386972451,37.5416529948095,1235.42518382353));
#145994=CARTESIAN_POINT('Ctrl Pts',(37.7024851496972,34.3703565790883,1233.93106617647));
#145995=CARTESIAN_POINT('Ctrl Pts',(40.5392751458362,30.6138395280662,1232.43694852941));
#145996=CARTESIAN_POINT('Ctrl Pts',(43.3760651419751,26.8573224770442,1230.94283088235));
#145997=CARTESIAN_POINT('Ctrl Pts',(45.4742952008372,22.6435084734481,1229.44871323529));
#145998=CARTESIAN_POINT('Ctrl Pts',(47.5725252596992,18.4296944698521,1227.95459558824));
#145999=CARTESIAN_POINT('Ctrl Pts',(48.8607426731792,13.9020798956618,1226.46047794118));
#146000=CARTESIAN_POINT('Ctrl Pts',(50.1489600866593,9.37446532147146,1224.96636029412));
#146001=CARTESIAN_POINT('Ctrl Pts',(50.5832961557877,4.68723266073574,1223.47224264706));
#146002=CARTESIAN_POINT('Ctrl Pts',(51.0176322249162,9.37178700064808E-15,
1221.978125));
#146003=CARTESIAN_POINT('Ctrl Pts',(50.5832961557877,-4.68723266073572,
1220.48400735294));
#146004=CARTESIAN_POINT('Ctrl Pts',(50.1489600866593,-9.37446532147149,
1218.98988970588));
#146005=CARTESIAN_POINT('Ctrl Pts',(48.8607426731792,-13.9020798956618,
1217.49577205882));
#146006=CARTESIAN_POINT('Ctrl Pts',(47.5725252596992,-18.4296944698521,
1216.00165441176));
#146007=CARTESIAN_POINT('Ctrl Pts',(45.4742952008371,-22.6435084734482,
1214.50753676471));
#146008=CARTESIAN_POINT('Ctrl Pts',(43.3760651419751,-26.8573224770441,
1213.01341911765));
#146009=CARTESIAN_POINT('Ctrl Pts',(40.5392751458362,-30.6138395280662,
1211.51930147059));
#146010=CARTESIAN_POINT('Ctrl Pts',(37.7024851496972,-34.3703565790883,
1210.02518382353));
#146011=CARTESIAN_POINT('Ctrl Pts',(34.2237386972451,-37.5416529948095,
1208.53106617647));
#146012=CARTESIAN_POINT('Ctrl Pts',(30.744992244793,-40.7129494105307,1207.03694852941));
#146013=CARTESIAN_POINT('Ctrl Pts',(26.7427538741697,-43.1910304950644,
1205.54283088235));
#146014=CARTESIAN_POINT('Ctrl Pts',(22.7405155035463,-45.6691115795981,
1204.04871323529));
#146015=CARTESIAN_POINT('Ctrl Pts',(18.3510766423074,-47.3695892537413,
1202.55459558824));
#146016=CARTESIAN_POINT('Ctrl Pts',(13.9616377810684,-49.0700669278844,
1201.06047794118));
#146017=CARTESIAN_POINT('Ctrl Pts',(9.33447550508176,-49.9350334639422,
1199.56636029412));
#146018=CARTESIAN_POINT('Ctrl Pts',(4.70731322909511,-50.8,1198.07224264706));
#146019=CARTESIAN_POINT('Ctrl Pts',(0.,-50.8,1196.578125));
#146020=CARTESIAN_POINT('Ctrl Pts',(-4.70731322909511,-50.8,1195.08400735294));
#146021=CARTESIAN_POINT('Ctrl Pts',(-9.33447550508177,-49.9350334639422,
1193.58988970588));
#146022=CARTESIAN_POINT('Ctrl Pts',(-13.9616377810684,-49.0700669278844,
1192.09577205882));
#146023=CARTESIAN_POINT('Ctrl Pts',(-18.3510766423074,-47.3695892537413,
1190.60165441176));
#146024=CARTESIAN_POINT('Ctrl Pts',(-22.7405155035463,-45.6691115795981,
1189.10753676471));
#146025=CARTESIAN_POINT('Ctrl Pts',(-26.7427538741697,-43.1910304950644,
1187.61341911765));
#146026=CARTESIAN_POINT('Ctrl Pts',(-30.744992244793,-40.7129494105307,
1186.11930147059));
#146027=CARTESIAN_POINT('Ctrl Pts',(-34.2237386972451,-37.5416529948095,
1184.62518382353));
#146028=CARTESIAN_POINT('Ctrl Pts',(-37.7024851496972,-34.3703565790883,
1183.13106617647));
#146029=CARTESIAN_POINT('Ctrl Pts',(-40.5392751458362,-30.6138395280662,
1181.63694852941));
#146030=CARTESIAN_POINT('Ctrl Pts',(-43.3760651419751,-26.8573224770441,
1180.14283088235));
#146031=CARTESIAN_POINT('Ctrl Pts',(-45.4742952008371,-22.6435084734481,
1178.64871323529));
#146032=CARTESIAN_POINT('Ctrl Pts',(-47.5725252596992,-18.4296944698521,
1177.15459558824));
#146033=CARTESIAN_POINT('Ctrl Pts',(-48.8607426731792,-13.9020798956618,
1175.66047794118));
#146034=CARTESIAN_POINT('Ctrl Pts',(-50.1489600866593,-9.37446532147148,
1174.16636029412));
#146035=CARTESIAN_POINT('Ctrl Pts',(-50.5832961557877,-4.68723266073574,
1172.67224264706));
#146036=CARTESIAN_POINT('Ctrl Pts',(-51.0176322249162,-3.12392900021603E-15,
1171.178125));
#146037=CARTESIAN_POINT('Ctrl Pts',(-50.5832961557877,4.68723266073573,
1169.68400735294));
#146038=CARTESIAN_POINT('Ctrl Pts',(-50.1489600866593,9.37446532147149,
1168.18988970588));
#146039=CARTESIAN_POINT('Ctrl Pts',(-48.8607426731792,13.9020798956618,
1166.69577205882));
#146040=CARTESIAN_POINT('Ctrl Pts',(-47.5725252596992,18.4296944698521,
1165.20165441177));
#146041=CARTESIAN_POINT('Ctrl Pts',(-45.4742952008371,22.6435084734481,
1163.70753676471));
#146042=CARTESIAN_POINT('Ctrl Pts',(-43.3760651419751,26.8573224770442,
1162.21341911765));
#146043=CARTESIAN_POINT('Ctrl Pts',(-40.5392751458362,30.6138395280662,
1160.71930147059));
#146044=CARTESIAN_POINT('Ctrl Pts',(-37.7024851496972,34.3703565790883,
1159.22518382353));
#146045=CARTESIAN_POINT('Ctrl Pts',(-34.2237386972451,37.5416529948095,
1157.73106617647));
#146046=CARTESIAN_POINT('Ctrl Pts',(-30.744992244793,40.7129494105307,1156.23694852941));
#146047=CARTESIAN_POINT('Ctrl Pts',(-26.7427538741697,43.1910304950644,
1154.74283088235));
#146048=CARTESIAN_POINT('Ctrl Pts',(-22.7405155035463,45.6691115795981,
1153.24871323529));
#146049=CARTESIAN_POINT('Ctrl Pts',(-18.3510766423074,47.3695892537413,
1151.75459558824));
#146050=CARTESIAN_POINT('Ctrl Pts',(-13.9616377810684,49.0700669278844,
1150.26047794118));
#146051=CARTESIAN_POINT('Ctrl Pts',(-9.33447550508177,49.9350334639422,
1148.76636029412));
#146052=CARTESIAN_POINT('Ctrl Pts',(-4.7073132290951,50.8,1147.27224264706));
#146053=CARTESIAN_POINT('Ctrl Pts',(-6.22120573966855E-15,50.8,1145.778125));
#146054=CARTESIAN_POINT('Ctrl Pts',(4.70731322909511,50.8,1144.28400735294));
#146055=CARTESIAN_POINT('Ctrl Pts',(9.33447550508176,49.9350334639422,1142.78988970588));
#146056=CARTESIAN_POINT('Ctrl Pts',(13.9616377810684,49.0700669278844,1141.29577205882));
#146057=CARTESIAN_POINT('Ctrl Pts',(18.3510766423074,47.3695892537413,1139.80165441176));
#146058=CARTESIAN_POINT('Ctrl Pts',(22.7405155035463,45.6691115795981,1138.30753676471));
#146059=CARTESIAN_POINT('Ctrl Pts',(26.7427538741697,43.1910304950644,1136.81341911765));
#146060=CARTESIAN_POINT('Ctrl Pts',(30.744992244793,40.7129494105307,1135.31930147059));
#146061=CARTESIAN_POINT('Ctrl Pts',(34.2237386972451,37.5416529948095,1133.82518382353));
#146062=CARTESIAN_POINT('Ctrl Pts',(37.7024851496972,34.3703565790883,1132.33106617647));
#146063=CARTESIAN_POINT('Ctrl Pts',(40.5392751458362,30.6138395280662,1130.83694852941));
#146064=CARTESIAN_POINT('Ctrl Pts',(43.3760651419751,26.8573224770442,1129.34283088235));
#146065=CARTESIAN_POINT('Ctrl Pts',(45.4742952008372,22.6435084734481,1127.84871323529));
#146066=CARTESIAN_POINT('Ctrl Pts',(47.5725252596992,18.4296944698521,1126.35459558824));
#146067=CARTESIAN_POINT('Ctrl Pts',(48.8607426731792,13.9020798956618,1124.86047794118));
#146068=CARTESIAN_POINT('Ctrl Pts',(50.1489600866593,9.37446532147146,1123.36636029412));
#146069=CARTESIAN_POINT('Ctrl Pts',(50.5832961557877,4.68723266073574,1121.87224264706));
#146070=CARTESIAN_POINT('Ctrl Pts',(51.0176322249162,9.37178700064808E-15,
1120.378125));
#146071=CARTESIAN_POINT('Ctrl Pts',(50.5832961557877,-4.68723266073572,
1118.88400735294));
#146072=CARTESIAN_POINT('Ctrl Pts',(50.1489600866593,-9.37446532147149,
1117.38988970588));
#146073=CARTESIAN_POINT('Ctrl Pts',(48.8607426731792,-13.9020798956618,
1115.89577205882));
#146074=CARTESIAN_POINT('Ctrl Pts',(47.5725252596992,-18.4296944698521,
1114.40165441176));
#146075=CARTESIAN_POINT('Ctrl Pts',(45.4742952008371,-22.6435084734482,
1112.90753676471));
#146076=CARTESIAN_POINT('Ctrl Pts',(43.3760651419751,-26.8573224770441,
1111.41341911765));
#146077=CARTESIAN_POINT('Ctrl Pts',(40.5392751458362,-30.6138395280662,
1109.91930147059));
#146078=CARTESIAN_POINT('Ctrl Pts',(37.7024851496972,-34.3703565790883,
1108.42518382353));
#146079=CARTESIAN_POINT('Ctrl Pts',(34.2237386972451,-37.5416529948095,
1106.93106617647));
#146080=CARTESIAN_POINT('Ctrl Pts',(30.744992244793,-40.7129494105307,1105.43694852941));
#146081=CARTESIAN_POINT('Ctrl Pts',(26.7427538741697,-43.1910304950644,
1103.94283088235));
#146082=CARTESIAN_POINT('Ctrl Pts',(22.7405155035463,-45.6691115795981,
1102.44871323529));
#146083=CARTESIAN_POINT('Ctrl Pts',(18.3510766423074,-47.3695892537413,
1100.95459558824));
#146084=CARTESIAN_POINT('Ctrl Pts',(13.9616377810684,-49.0700669278844,
1099.46047794118));
#146085=CARTESIAN_POINT('Ctrl Pts',(9.33447550508176,-49.9350334639422,
1097.96636029412));
#146086=CARTESIAN_POINT('Ctrl Pts',(4.70731322909511,-50.8,1096.47224264706));
#146087=CARTESIAN_POINT('Ctrl Pts',(0.,-50.8,1094.978125));
#146088=CARTESIAN_POINT('Ctrl Pts',(-4.70731322909511,-50.8,1093.48400735294));
#146089=CARTESIAN_POINT('Ctrl Pts',(-9.33447550508177,-49.9350334639422,
1091.98988970588));
#146090=CARTESIAN_POINT('Ctrl Pts',(-13.9616377810684,-49.0700669278844,
1090.49577205882));
#146091=CARTESIAN_POINT('Ctrl Pts',(-18.3510766423074,-47.3695892537413,
1089.00165441176));
#146092=CARTESIAN_POINT('Ctrl Pts',(-22.7405155035463,-45.6691115795981,
1087.50753676471));
#146093=CARTESIAN_POINT('Ctrl Pts',(-26.7427538741697,-43.1910304950644,
1086.01341911765));
#146094=CARTESIAN_POINT('Ctrl Pts',(-30.744992244793,-40.7129494105307,
1084.51930147059));
#146095=CARTESIAN_POINT('Ctrl Pts',(-34.2237386972451,-37.5416529948095,
1083.02518382353));
#146096=CARTESIAN_POINT('Ctrl Pts',(-37.7024851496972,-34.3703565790883,
1081.53106617647));
#146097=CARTESIAN_POINT('Ctrl Pts',(-40.5392751458362,-30.6138395280662,
1080.03694852941));
#146098=CARTESIAN_POINT('Ctrl Pts',(-43.3760651419751,-26.8573224770441,
1078.54283088235));
#146099=CARTESIAN_POINT('Ctrl Pts',(-45.4742952008371,-22.6435084734481,
1077.04871323529));
#146100=CARTESIAN_POINT('Ctrl Pts',(-47.5725252596992,-18.4296944698521,
1075.55459558824));
#146101=CARTESIAN_POINT('Ctrl Pts',(-48.8607426731792,-13.9020798956618,
1074.06047794118));
#146102=CARTESIAN_POINT('Ctrl Pts',(-50.1489600866593,-9.37446532147148,
1072.56636029412));
#146103=CARTESIAN_POINT('Ctrl Pts',(-50.5832961557877,-4.68723266073574,
1071.07224264706));
#146104=CARTESIAN_POINT('Ctrl Pts',(-51.0176322249162,-3.12392900021603E-15,
1069.578125));
#146105=CARTESIAN_POINT('Ctrl Pts',(-50.5832961557877,4.68723266073573,
1068.08400735294));
#146106=CARTESIAN_POINT('Ctrl Pts',(-50.1489600866593,9.37446532147149,
1066.58988970588));
#146107=CARTESIAN_POINT('Ctrl Pts',(-48.8607426731792,13.9020798956618,
1065.09577205882));
#146108=CARTESIAN_POINT('Ctrl Pts',(-47.5725252596992,18.4296944698521,
1063.60165441176));
#146109=CARTESIAN_POINT('Ctrl Pts',(-45.4742952008371,22.6435084734481,
1062.10753676471));
#146110=CARTESIAN_POINT('Ctrl Pts',(-43.3760651419751,26.8573224770442,
1060.61341911765));
#146111=CARTESIAN_POINT('Ctrl Pts',(-40.5392751458362,30.6138395280662,
1059.11930147059));
#146112=CARTESIAN_POINT('Ctrl Pts',(-37.7024851496972,34.3703565790883,
1057.62518382353));
#146113=CARTESIAN_POINT('Ctrl Pts',(-34.2237386972451,37.5416529948095,
1056.13106617647));
#146114=CARTESIAN_POINT('Ctrl Pts',(-30.744992244793,40.7129494105307,1054.63694852941));
#146115=CARTESIAN_POINT('Ctrl Pts',(-26.7427538741697,43.1910304950644,
1053.14283088235));
#146116=CARTESIAN_POINT('Ctrl Pts',(-22.7405155035463,45.6691115795981,
1051.64871323529));
#146117=CARTESIAN_POINT('Ctrl Pts',(-18.3510766423074,47.3695892537413,
1050.15459558824));
#146118=CARTESIAN_POINT('Ctrl Pts',(-13.9616377810684,49.0700669278844,
1048.66047794118));
#146119=CARTESIAN_POINT('Ctrl Pts',(-9.33447550508177,49.9350334639422,
1047.16636029412));
#146120=CARTESIAN_POINT('Ctrl Pts',(-4.7073132290951,50.8,1045.67224264706));
#146121=CARTESIAN_POINT('Ctrl Pts',(-6.22120573966855E-15,50.8,1044.178125));
#146122=CARTESIAN_POINT('Ctrl Pts',(4.70731322909511,50.8,1042.68400735294));
#146123=CARTESIAN_POINT('Ctrl Pts',(9.33447550508176,49.9350334639422,1041.18988970588));
#146124=CARTESIAN_POINT('Ctrl Pts',(13.9616377810684,49.0700669278844,1039.69577205882));
#146125=CARTESIAN_POINT('Ctrl Pts',(18.3510766423074,47.3695892537413,1038.20165441176));
#146126=CARTESIAN_POINT('Ctrl Pts',(22.7405155035463,45.6691115795981,1036.70753676471));
#146127=CARTESIAN_POINT('Ctrl Pts',(26.7427538741697,43.1910304950644,1035.21341911765));
#146128=CARTESIAN_POINT('Ctrl Pts',(30.744992244793,40.7129494105307,1033.71930147059));
#146129=CARTESIAN_POINT('Ctrl Pts',(34.2237386972451,37.5416529948095,1032.22518382353));
#146130=CARTESIAN_POINT('Ctrl Pts',(37.7024851496972,34.3703565790883,1030.73106617647));
#146131=CARTESIAN_POINT('Ctrl Pts',(40.5392751458362,30.6138395280662,1029.23694852941));
#146132=CARTESIAN_POINT('Ctrl Pts',(43.3760651419751,26.8573224770442,1027.74283088235));
#146133=CARTESIAN_POINT('Ctrl Pts',(45.4742952008372,22.6435084734481,1026.24871323529));
#146134=CARTESIAN_POINT('Ctrl Pts',(47.5725252596992,18.4296944698521,1024.75459558824));
#146135=CARTESIAN_POINT('Ctrl Pts',(48.8607426731792,13.9020798956618,1023.26047794118));
#146136=CARTESIAN_POINT('Ctrl Pts',(50.1489600866593,9.37446532147146,1021.76636029412));
#146137=CARTESIAN_POINT('Ctrl Pts',(50.5832961557877,4.68723266073574,1020.27224264706));
#146138=CARTESIAN_POINT('Ctrl Pts',(51.0176322249162,9.37178700064808E-15,
1018.778125));
#146139=CARTESIAN_POINT('Ctrl Pts',(50.5832961557877,-4.68723266073572,
1017.28400735294));
#146140=CARTESIAN_POINT('Ctrl Pts',(50.1489600866593,-9.37446532147149,
1015.78988970588));
#146141=CARTESIAN_POINT('Ctrl Pts',(48.8607426731792,-13.9020798956618,
1014.29577205882));
#146142=CARTESIAN_POINT('Ctrl Pts',(47.5725252596992,-18.4296944698521,
1012.80165441176));
#146143=CARTESIAN_POINT('Ctrl Pts',(45.4742952008371,-22.6435084734482,
1011.30753676471));
#146144=CARTESIAN_POINT('Ctrl Pts',(43.3760651419751,-26.8573224770441,
1009.81341911765));
#146145=CARTESIAN_POINT('Ctrl Pts',(40.5392751458362,-30.6138395280662,
1008.31930147059));
#146146=CARTESIAN_POINT('Ctrl Pts',(37.7024851496972,-34.3703565790883,
1006.82518382353));
#146147=CARTESIAN_POINT('Ctrl Pts',(34.2237386972451,-37.5416529948095,
1005.33106617647));
#146148=CARTESIAN_POINT('Ctrl Pts',(30.744992244793,-40.7129494105307,1003.83694852941));
#146149=CARTESIAN_POINT('Ctrl Pts',(26.7427538741697,-43.1910304950644,
1002.34283088235));
#146150=CARTESIAN_POINT('Ctrl Pts',(22.7405155035463,-45.6691115795981,
1000.84871323529));
#146151=CARTESIAN_POINT('Ctrl Pts',(18.3510766423074,-47.3695892537413,
999.354595588235));
#146152=CARTESIAN_POINT('Ctrl Pts',(13.9616377810684,-49.0700669278844,
997.860477941177));
#146153=CARTESIAN_POINT('Ctrl Pts',(9.33447550508176,-49.9350334639422,
996.366360294118));
#146154=CARTESIAN_POINT('Ctrl Pts',(4.70731322909511,-50.8,994.872242647059));
#146155=CARTESIAN_POINT('Ctrl Pts',(0.,-50.8,993.378125));
#146156=CARTESIAN_POINT('Ctrl Pts',(-4.70731322909511,-50.8,991.884007352941));
#146157=CARTESIAN_POINT('Ctrl Pts',(-9.33447550508177,-49.9350334639422,
990.389889705883));
#146158=CARTESIAN_POINT('Ctrl Pts',(-13.9616377810684,-49.0700669278844,
988.895772058824));
#146159=CARTESIAN_POINT('Ctrl Pts',(-18.3510766423074,-47.3695892537413,
987.401654411765));
#146160=CARTESIAN_POINT('Ctrl Pts',(-22.7405155035463,-45.6691115795981,
985.907536764706));
#146161=CARTESIAN_POINT('Ctrl Pts',(-26.7427538741697,-43.1910304950644,
984.413419117647));
#146162=CARTESIAN_POINT('Ctrl Pts',(-30.744992244793,-40.7129494105307,
982.919301470588));
#146163=CARTESIAN_POINT('Ctrl Pts',(-34.2237386972451,-37.5416529948095,
981.425183823529));
#146164=CARTESIAN_POINT('Ctrl Pts',(-37.7024851496972,-34.3703565790883,
979.931066176471));
#146165=CARTESIAN_POINT('Ctrl Pts',(-40.5392751458362,-30.6138395280662,
978.436948529412));
#146166=CARTESIAN_POINT('Ctrl Pts',(-43.3760651419751,-26.8573224770441,
976.942830882353));
#146167=CARTESIAN_POINT('Ctrl Pts',(-45.4742952008371,-22.6435084734481,
975.448713235294));
#146168=CARTESIAN_POINT('Ctrl Pts',(-47.5725252596992,-18.4296944698521,
973.954595588235));
#146169=CARTESIAN_POINT('Ctrl Pts',(-48.8607426731792,-13.9020798956618,
972.460477941177));
#146170=CARTESIAN_POINT('Ctrl Pts',(-50.1489600866593,-9.37446532147148,
970.966360294118));
#146171=CARTESIAN_POINT('Ctrl Pts',(-50.5832961557877,-4.68723266073574,
969.472242647059));
#146172=CARTESIAN_POINT('Ctrl Pts',(-51.0176322249162,-3.12392900021603E-15,
967.978125));
#146173=CARTESIAN_POINT('Ctrl Pts',(-50.5832961557877,4.68723266073573,
966.484007352941));
#146174=CARTESIAN_POINT('Ctrl Pts',(-50.1489600866593,9.37446532147149,
964.989889705882));
#146175=CARTESIAN_POINT('Ctrl Pts',(-48.8607426731792,13.9020798956618,
963.495772058824));
#146176=CARTESIAN_POINT('Ctrl Pts',(-47.5725252596992,18.4296944698521,
962.001654411765));
#146177=CARTESIAN_POINT('Ctrl Pts',(-45.4742952008371,22.6435084734481,
960.507536764706));
#146178=CARTESIAN_POINT('Ctrl Pts',(-43.3760651419751,26.8573224770442,
959.013419117647));
#146179=CARTESIAN_POINT('Ctrl Pts',(-40.5392751458362,30.6138395280662,
957.519301470588));
#146180=CARTESIAN_POINT('Ctrl Pts',(-37.7024851496972,34.3703565790883,
956.02518382353));
#146181=CARTESIAN_POINT('Ctrl Pts',(-34.2237386972451,37.5416529948095,
954.531066176471));
#146182=CARTESIAN_POINT('Ctrl Pts',(-30.744992244793,40.7129494105307,953.036948529412));
#146183=CARTESIAN_POINT('Ctrl Pts',(-26.7427538741697,43.1910304950644,
951.542830882353));
#146184=CARTESIAN_POINT('Ctrl Pts',(-22.7405155035463,45.6691115795981,
950.048713235294));
#146185=CARTESIAN_POINT('Ctrl Pts',(-18.3510766423074,47.3695892537413,
948.554595588235));
#146186=CARTESIAN_POINT('Ctrl Pts',(-13.9616377810684,49.0700669278844,
947.060477941177));
#146187=CARTESIAN_POINT('Ctrl Pts',(-9.33447550508177,49.9350334639422,
945.566360294118));
#146188=CARTESIAN_POINT('Ctrl Pts',(-4.7073132290951,50.8,944.072242647059));
#146189=CARTESIAN_POINT('Ctrl Pts',(-6.22120573966855E-15,50.8,942.578125));
#146190=CARTESIAN_POINT('Ctrl Pts',(4.70731322909511,50.8,941.084007352941));
#146191=CARTESIAN_POINT('Ctrl Pts',(9.33447550508176,49.9350334639422,939.589889705883));
#146192=CARTESIAN_POINT('Ctrl Pts',(13.9616377810684,49.0700669278844,938.095772058824));
#146193=CARTESIAN_POINT('Ctrl Pts',(18.3510766423074,47.3695892537413,936.601654411765));
#146194=CARTESIAN_POINT('Ctrl Pts',(22.7405155035463,45.6691115795981,935.107536764706));
#146195=CARTESIAN_POINT('Ctrl Pts',(26.7427538741697,43.1910304950644,933.613419117647));
#146196=CARTESIAN_POINT('Ctrl Pts',(30.744992244793,40.7129494105307,932.119301470589));
#146197=CARTESIAN_POINT('Ctrl Pts',(34.2237386972451,37.5416529948095,930.625183823529));
#146198=CARTESIAN_POINT('Ctrl Pts',(37.7024851496972,34.3703565790883,929.131066176471));
#146199=CARTESIAN_POINT('Ctrl Pts',(40.5392751458362,30.6138395280662,927.636948529412));
#146200=CARTESIAN_POINT('Ctrl Pts',(43.3760651419751,26.8573224770442,926.142830882353));
#146201=CARTESIAN_POINT('Ctrl Pts',(45.4742952008372,22.6435084734481,924.648713235294));
#146202=CARTESIAN_POINT('Ctrl Pts',(47.5725252596992,18.4296944698521,923.154595588235));
#146203=CARTESIAN_POINT('Ctrl Pts',(48.8607426731792,13.9020798956618,921.660477941176));
#146204=CARTESIAN_POINT('Ctrl Pts',(50.1489600866593,9.37446532147146,920.166360294118));
#146205=CARTESIAN_POINT('Ctrl Pts',(50.5832961557877,4.68723266073574,918.672242647059));
#146206=CARTESIAN_POINT('Ctrl Pts',(51.0176322249162,9.37178700064808E-15,
917.178125));
#146207=CARTESIAN_POINT('Ctrl Pts',(50.5832961557877,-4.68723266073572,
915.684007352941));
#146208=CARTESIAN_POINT('Ctrl Pts',(50.1489600866593,-9.37446532147149,
914.189889705882));
#146209=CARTESIAN_POINT('Ctrl Pts',(48.8607426731792,-13.9020798956618,
912.695772058824));
#146210=CARTESIAN_POINT('Ctrl Pts',(47.5725252596992,-18.4296944698521,
911.201654411765));
#146211=CARTESIAN_POINT('Ctrl Pts',(45.4742952008371,-22.6435084734482,
909.707536764706));
#146212=CARTESIAN_POINT('Ctrl Pts',(43.3760651419751,-26.8573224770441,
908.213419117647));
#146213=CARTESIAN_POINT('Ctrl Pts',(40.5392751458362,-30.6138395280662,
906.719301470588));
#146214=CARTESIAN_POINT('Ctrl Pts',(37.7024851496972,-34.3703565790883,
905.22518382353));
#146215=CARTESIAN_POINT('Ctrl Pts',(34.2237386972451,-37.5416529948095,
903.731066176471));
#146216=CARTESIAN_POINT('Ctrl Pts',(30.744992244793,-40.7129494105307,902.236948529412));
#146217=CARTESIAN_POINT('Ctrl Pts',(26.7427538741697,-43.1910304950644,
900.742830882353));
#146218=CARTESIAN_POINT('Ctrl Pts',(22.7405155035463,-45.6691115795981,
899.248713235294));
#146219=CARTESIAN_POINT('Ctrl Pts',(18.3510766423074,-47.3695892537413,
897.754595588235));
#146220=CARTESIAN_POINT('Ctrl Pts',(13.9616377810684,-49.0700669278844,
896.260477941177));
#146221=CARTESIAN_POINT('Ctrl Pts',(9.33447550508176,-49.9350334639422,
894.766360294118));
#146222=CARTESIAN_POINT('Ctrl Pts',(4.70731322909511,-50.8,893.272242647059));
#146223=CARTESIAN_POINT('Ctrl Pts',(0.,-50.8,891.778125));
#146224=CARTESIAN_POINT('Ctrl Pts',(-4.70731322909511,-50.8,890.284007352941));
#146225=CARTESIAN_POINT('Ctrl Pts',(-9.33447550508177,-49.9350334639422,
888.789889705882));
#146226=CARTESIAN_POINT('Ctrl Pts',(-13.9616377810684,-49.0700669278844,
887.295772058824));
#146227=CARTESIAN_POINT('Ctrl Pts',(-18.3510766423074,-47.3695892537413,
885.801654411765));
#146228=CARTESIAN_POINT('Ctrl Pts',(-22.7405155035463,-45.6691115795981,
884.307536764706));
#146229=CARTESIAN_POINT('Ctrl Pts',(-26.7427538741697,-43.1910304950644,
882.813419117647));
#146230=CARTESIAN_POINT('Ctrl Pts',(-30.744992244793,-40.7129494105307,
881.319301470588));
#146231=CARTESIAN_POINT('Ctrl Pts',(-34.2237386972451,-37.5416529948095,
879.82518382353));
#146232=CARTESIAN_POINT('Ctrl Pts',(-37.7024851496972,-34.3703565790883,
878.331066176471));
#146233=CARTESIAN_POINT('Ctrl Pts',(-40.5392751458362,-30.6138395280662,
876.836948529412));
#146234=CARTESIAN_POINT('Ctrl Pts',(-43.3760651419751,-26.8573224770441,
875.342830882353));
#146235=CARTESIAN_POINT('Ctrl Pts',(-45.4742952008371,-22.6435084734481,
873.848713235294));
#146236=CARTESIAN_POINT('Ctrl Pts',(-47.5725252596992,-18.4296944698521,
872.354595588235));
#146237=CARTESIAN_POINT('Ctrl Pts',(-48.8607426731792,-13.9020798956618,
870.860477941176));
#146238=CARTESIAN_POINT('Ctrl Pts',(-50.1489600866593,-9.37446532147148,
869.366360294118));
#146239=CARTESIAN_POINT('Ctrl Pts',(-50.5832961557877,-4.68723266073574,
867.872242647059));
#146240=CARTESIAN_POINT('Ctrl Pts',(-51.0176322249162,-3.12392900021603E-15,
866.378125));
#146241=CARTESIAN_POINT('Ctrl Pts',(-50.5832961557877,4.68723266073573,
864.884007352941));
#146242=CARTESIAN_POINT('Ctrl Pts',(-50.1489600866593,9.37446532147149,
863.389889705882));
#146243=CARTESIAN_POINT('Ctrl Pts',(-48.8607426731792,13.9020798956618,
861.895772058824));
#146244=CARTESIAN_POINT('Ctrl Pts',(-47.5725252596992,18.4296944698521,
860.401654411765));
#146245=CARTESIAN_POINT('Ctrl Pts',(-45.4742952008371,22.6435084734481,
858.907536764706));
#146246=CARTESIAN_POINT('Ctrl Pts',(-43.3760651419751,26.8573224770442,
857.413419117647));
#146247=CARTESIAN_POINT('Ctrl Pts',(-40.5392751458362,30.6138395280662,
855.919301470588));
#146248=CARTESIAN_POINT('Ctrl Pts',(-37.7024851496972,34.3703565790883,
854.425183823529));
#146249=CARTESIAN_POINT('Ctrl Pts',(-34.2237386972451,37.5416529948095,
852.931066176471));
#146250=CARTESIAN_POINT('Ctrl Pts',(-30.744992244793,40.7129494105307,851.436948529412));
#146251=CARTESIAN_POINT('Ctrl Pts',(-26.7427538741697,43.1910304950644,
849.942830882353));
#146252=CARTESIAN_POINT('Ctrl Pts',(-22.7405155035463,45.6691115795981,
848.448713235294));
#146253=CARTESIAN_POINT('Ctrl Pts',(-18.3510766423074,47.3695892537413,
846.954595588235));
#146254=CARTESIAN_POINT('Ctrl Pts',(-13.9616377810684,49.0700669278844,
845.460477941177));
#146255=CARTESIAN_POINT('Ctrl Pts',(-9.33447550508177,49.9350334639422,
843.966360294118));
#146256=CARTESIAN_POINT('Ctrl Pts',(-4.7073132290951,50.8,842.472242647059));
#146257=CARTESIAN_POINT('Ctrl Pts',(-6.22120573966855E-15,50.8,840.978125));
#146258=CARTESIAN_POINT('Ctrl Pts',(4.70731322909511,50.8,839.484007352941));
#146259=CARTESIAN_POINT('Ctrl Pts',(9.33447550508176,49.9350334639422,837.989889705883));
#146260=CARTESIAN_POINT('Ctrl Pts',(13.9616377810684,49.0700669278844,836.495772058824));
#146261=CARTESIAN_POINT('Ctrl Pts',(18.3510766423074,47.3695892537413,835.001654411765));
#146262=CARTESIAN_POINT('Ctrl Pts',(22.7405155035463,45.6691115795981,833.507536764706));
#146263=CARTESIAN_POINT('Ctrl Pts',(26.7427538741697,43.1910304950644,832.013419117647));
#146264=CARTESIAN_POINT('Ctrl Pts',(30.744992244793,40.7129494105307,830.519301470588));
#146265=CARTESIAN_POINT('Ctrl Pts',(34.2237386972451,37.5416529948095,829.025183823529));
#146266=CARTESIAN_POINT('Ctrl Pts',(37.7024851496972,34.3703565790883,827.531066176471));
#146267=CARTESIAN_POINT('Ctrl Pts',(40.5392751458362,30.6138395280662,826.036948529412));
#146268=CARTESIAN_POINT('Ctrl Pts',(43.3760651419751,26.8573224770442,824.542830882353));
#146269=CARTESIAN_POINT('Ctrl Pts',(45.4742952008372,22.6435084734481,823.048713235294));
#146270=CARTESIAN_POINT('Ctrl Pts',(47.5725252596992,18.4296944698521,821.554595588236));
#146271=CARTESIAN_POINT('Ctrl Pts',(48.8607426731792,13.9020798956618,820.060477941176));
#146272=CARTESIAN_POINT('Ctrl Pts',(50.1489600866593,9.37446532147146,818.566360294118));
#146273=CARTESIAN_POINT('Ctrl Pts',(50.5832961557877,4.68723266073574,817.072242647059));
#146274=CARTESIAN_POINT('Ctrl Pts',(51.0176322249162,9.37178700064808E-15,
815.578125));
#146275=CARTESIAN_POINT('Ctrl Pts',(50.5832961557877,-4.68723266073572,
814.084007352941));
#146276=CARTESIAN_POINT('Ctrl Pts',(50.1489600866593,-9.37446532147149,
812.589889705883));
#146277=CARTESIAN_POINT('Ctrl Pts',(48.8607426731792,-13.9020798956618,
811.095772058824));
#146278=CARTESIAN_POINT('Ctrl Pts',(47.5725252596992,-18.4296944698521,
809.601654411765));
#146279=CARTESIAN_POINT('Ctrl Pts',(45.4742952008371,-22.6435084734482,
808.107536764706));
#146280=CARTESIAN_POINT('Ctrl Pts',(43.3760651419751,-26.8573224770441,
806.613419117647));
#146281=CARTESIAN_POINT('Ctrl Pts',(40.5392751458362,-30.6138395280662,
805.119301470588));
#146282=CARTESIAN_POINT('Ctrl Pts',(37.7024851496972,-34.3703565790883,
803.625183823529));
#146283=CARTESIAN_POINT('Ctrl Pts',(34.2237386972451,-37.5416529948095,
802.131066176471));
#146284=CARTESIAN_POINT('Ctrl Pts',(30.744992244793,-40.7129494105307,800.636948529412));
#146285=CARTESIAN_POINT('Ctrl Pts',(26.7427538741697,-43.1910304950644,
799.142830882353));
#146286=CARTESIAN_POINT('Ctrl Pts',(22.7405155035463,-45.6691115795981,
797.648713235294));
#146287=CARTESIAN_POINT('Ctrl Pts',(18.3510766423074,-47.3695892537413,
796.154595588235));
#146288=CARTESIAN_POINT('Ctrl Pts',(13.9616377810684,-49.0700669278844,
794.660477941177));
#146289=CARTESIAN_POINT('Ctrl Pts',(9.33447550508176,-49.9350334639422,
793.166360294118));
#146290=CARTESIAN_POINT('Ctrl Pts',(4.70731322909511,-50.8,791.672242647059));
#146291=CARTESIAN_POINT('Ctrl Pts',(0.,-50.8,790.178125));
#146292=CARTESIAN_POINT('Ctrl Pts',(-4.70731322909511,-50.8,788.684007352941));
#146293=CARTESIAN_POINT('Ctrl Pts',(-9.33447550508177,-49.9350334639422,
787.189889705882));
#146294=CARTESIAN_POINT('Ctrl Pts',(-13.9616377810684,-49.0700669278844,
785.695772058824));
#146295=CARTESIAN_POINT('Ctrl Pts',(-18.3510766423074,-47.3695892537413,
784.201654411765));
#146296=CARTESIAN_POINT('Ctrl Pts',(-22.7405155035463,-45.6691115795981,
782.707536764706));
#146297=CARTESIAN_POINT('Ctrl Pts',(-26.7427538741697,-43.1910304950644,
781.213419117647));
#146298=CARTESIAN_POINT('Ctrl Pts',(-30.744992244793,-40.7129494105307,
779.719301470588));
#146299=CARTESIAN_POINT('Ctrl Pts',(-34.2237386972451,-37.5416529948095,
778.22518382353));
#146300=CARTESIAN_POINT('Ctrl Pts',(-37.7024851496972,-34.3703565790883,
776.731066176471));
#146301=CARTESIAN_POINT('Ctrl Pts',(-40.5392751458362,-30.6138395280662,
775.236948529412));
#146302=CARTESIAN_POINT('Ctrl Pts',(-43.3760651419751,-26.8573224770441,
773.742830882353));
#146303=CARTESIAN_POINT('Ctrl Pts',(-45.4742952008371,-22.6435084734481,
772.248713235294));
#146304=CARTESIAN_POINT('Ctrl Pts',(-47.5725252596992,-18.4296944698521,
770.754595588236));
#146305=CARTESIAN_POINT('Ctrl Pts',(-48.8607426731792,-13.9020798956618,
769.260477941177));
#146306=CARTESIAN_POINT('Ctrl Pts',(-50.1489600866593,-9.37446532147148,
767.766360294118));
#146307=CARTESIAN_POINT('Ctrl Pts',(-50.5832961557877,-4.68723266073574,
766.272242647059));
#146308=CARTESIAN_POINT('Ctrl Pts',(-51.0176322249162,-3.12392900021603E-15,
764.778125));
#146309=CARTESIAN_POINT('Ctrl Pts',(-50.5832961557877,4.68723266073573,
763.284007352941));
#146310=CARTESIAN_POINT('Ctrl Pts',(-50.1489600866593,9.37446532147149,
761.789889705883));
#146311=CARTESIAN_POINT('Ctrl Pts',(-48.8607426731792,13.9020798956618,
760.295772058824));
#146312=CARTESIAN_POINT('Ctrl Pts',(-47.5725252596992,18.4296944698521,
758.801654411765));
#146313=CARTESIAN_POINT('Ctrl Pts',(-45.4742952008371,22.6435084734481,
757.307536764706));
#146314=CARTESIAN_POINT('Ctrl Pts',(-43.3760651419751,26.8573224770442,
755.813419117647));
#146315=CARTESIAN_POINT('Ctrl Pts',(-40.5392751458362,30.6138395280662,
754.319301470588));
#146316=CARTESIAN_POINT('Ctrl Pts',(-37.7024851496972,34.3703565790883,
752.825183823529));
#146317=CARTESIAN_POINT('Ctrl Pts',(-34.2237386972451,37.5416529948095,
751.331066176471));
#146318=CARTESIAN_POINT('Ctrl Pts',(-30.744992244793,40.7129494105307,749.836948529412));
#146319=CARTESIAN_POINT('Ctrl Pts',(-26.7427538741697,43.1910304950644,
748.342830882353));
#146320=CARTESIAN_POINT('Ctrl Pts',(-22.7405155035463,45.6691115795981,
746.848713235294));
#146321=CARTESIAN_POINT('Ctrl Pts',(-18.3510766423074,47.3695892537413,
745.354595588235));
#146322=CARTESIAN_POINT('Ctrl Pts',(-13.9616377810684,49.0700669278844,
743.860477941176));
#146323=CARTESIAN_POINT('Ctrl Pts',(-9.33447550508177,49.9350334639422,
742.366360294118));
#146324=CARTESIAN_POINT('Ctrl Pts',(-4.7073132290951,50.8,740.872242647059));
#146325=CARTESIAN_POINT('Ctrl Pts',(-6.22120573966855E-15,50.8,739.378125));
#146326=CARTESIAN_POINT('Ctrl Pts',(4.70731322909511,50.8,737.884007352941));
#146327=CARTESIAN_POINT('Ctrl Pts',(9.33447550508176,49.9350334639422,736.389889705882));
#146328=CARTESIAN_POINT('Ctrl Pts',(13.9616377810684,49.0700669278844,734.895772058824));
#146329=CARTESIAN_POINT('Ctrl Pts',(18.3510766423074,47.3695892537413,733.401654411765));
#146330=CARTESIAN_POINT('Ctrl Pts',(22.7405155035463,45.6691115795981,731.907536764706));
#146331=CARTESIAN_POINT('Ctrl Pts',(26.7427538741697,43.1910304950644,730.413419117647));
#146332=CARTESIAN_POINT('Ctrl Pts',(30.744992244793,40.7129494105307,728.919301470588));
#146333=CARTESIAN_POINT('Ctrl Pts',(34.2237386972451,37.5416529948095,727.425183823529));
#146334=CARTESIAN_POINT('Ctrl Pts',(37.7024851496972,34.3703565790883,725.931066176471));
#146335=CARTESIAN_POINT('Ctrl Pts',(40.5392751458362,30.6138395280662,724.436948529412));
#146336=CARTESIAN_POINT('Ctrl Pts',(43.3760651419751,26.8573224770442,722.942830882353));
#146337=CARTESIAN_POINT('Ctrl Pts',(45.4742952008372,22.6435084734481,721.448713235294));
#146338=CARTESIAN_POINT('Ctrl Pts',(47.5725252596992,18.4296944698521,719.954595588235));
#146339=CARTESIAN_POINT('Ctrl Pts',(48.8607426731792,13.9020798956618,718.460477941177));
#146340=CARTESIAN_POINT('Ctrl Pts',(50.1489600866593,9.37446532147146,716.966360294118));
#146341=CARTESIAN_POINT('Ctrl Pts',(50.5832961557877,4.68723266073574,715.472242647059));
#146342=CARTESIAN_POINT('Ctrl Pts',(51.0176322249162,9.37178700064808E-15,
713.978125));
#146343=CARTESIAN_POINT('Ctrl Pts',(50.5832961557877,-4.68723266073572,
712.484007352941));
#146344=CARTESIAN_POINT('Ctrl Pts',(50.1489600866593,-9.37446532147149,
710.989889705883));
#146345=CARTESIAN_POINT('Ctrl Pts',(48.8607426731792,-13.9020798956618,
709.495772058823));
#146346=CARTESIAN_POINT('Ctrl Pts',(47.5725252596992,-18.4296944698521,
708.001654411765));
#146347=CARTESIAN_POINT('Ctrl Pts',(45.4742952008371,-22.6435084734482,
706.507536764706));
#146348=CARTESIAN_POINT('Ctrl Pts',(43.3760651419751,-26.8573224770441,
705.013419117647));
#146349=CARTESIAN_POINT('Ctrl Pts',(40.5392751458362,-30.6138395280662,
703.519301470588));
#146350=CARTESIAN_POINT('Ctrl Pts',(37.7024851496972,-34.3703565790883,
702.025183823529));
#146351=CARTESIAN_POINT('Ctrl Pts',(34.2237386972451,-37.5416529948095,
700.531066176471));
#146352=CARTESIAN_POINT('Ctrl Pts',(30.744992244793,-40.7129494105307,699.036948529412));
#146353=CARTESIAN_POINT('Ctrl Pts',(26.7427538741697,-43.1910304950644,
697.542830882353));
#146354=CARTESIAN_POINT('Ctrl Pts',(22.7405155035463,-45.6691115795981,
696.048713235294));
#146355=CARTESIAN_POINT('Ctrl Pts',(18.3510766423074,-47.3695892537413,
694.554595588235));
#146356=CARTESIAN_POINT('Ctrl Pts',(13.9616377810684,-49.0700669278844,
693.060477941176));
#146357=CARTESIAN_POINT('Ctrl Pts',(9.33447550508176,-49.9350334639422,
691.566360294118));
#146358=CARTESIAN_POINT('Ctrl Pts',(4.70731322909511,-50.8,690.072242647059));
#146359=CARTESIAN_POINT('Ctrl Pts',(0.,-50.8,688.578125));
#146360=CARTESIAN_POINT('Ctrl Pts',(-4.70731322909511,-50.8,687.084007352941));
#146361=CARTESIAN_POINT('Ctrl Pts',(-9.33447550508177,-49.9350334639422,
685.589889705882));
#146362=CARTESIAN_POINT('Ctrl Pts',(-13.9616377810684,-49.0700669278844,
684.095772058824));
#146363=CARTESIAN_POINT('Ctrl Pts',(-18.3510766423074,-47.3695892537413,
682.601654411765));
#146364=CARTESIAN_POINT('Ctrl Pts',(-22.7405155035463,-45.6691115795981,
681.107536764706));
#146365=CARTESIAN_POINT('Ctrl Pts',(-26.7427538741697,-43.1910304950644,
679.613419117647));
#146366=CARTESIAN_POINT('Ctrl Pts',(-30.744992244793,-40.7129494105307,
678.119301470588));
#146367=CARTESIAN_POINT('Ctrl Pts',(-34.2237386972451,-37.5416529948095,
676.62518382353));
#146368=CARTESIAN_POINT('Ctrl Pts',(-37.7024851496972,-34.3703565790883,
675.131066176471));
#146369=CARTESIAN_POINT('Ctrl Pts',(-40.5392751458362,-30.6138395280662,
673.636948529412));
#146370=CARTESIAN_POINT('Ctrl Pts',(-43.3760651419751,-26.8573224770441,
672.142830882353));
#146371=CARTESIAN_POINT('Ctrl Pts',(-45.4742952008371,-22.6435084734481,
670.648713235294));
#146372=CARTESIAN_POINT('Ctrl Pts',(-47.5725252596992,-18.4296944698521,
669.154595588235));
#146373=CARTESIAN_POINT('Ctrl Pts',(-48.8607426731792,-13.9020798956618,
667.660477941176));
#146374=CARTESIAN_POINT('Ctrl Pts',(-50.1489600866593,-9.37446532147148,
666.166360294118));
#146375=CARTESIAN_POINT('Ctrl Pts',(-50.5832961557877,-4.68723266073574,
664.672242647059));
#146376=CARTESIAN_POINT('Ctrl Pts',(-51.0176322249162,-3.12392900021603E-15,
663.178125));
#146377=CARTESIAN_POINT('Ctrl Pts',(-50.5832961557877,4.68723266073573,
661.684007352941));
#146378=CARTESIAN_POINT('Ctrl Pts',(-50.1489600866593,9.37446532147149,
660.189889705882));
#146379=CARTESIAN_POINT('Ctrl Pts',(-48.8607426731792,13.9020798956618,
658.695772058824));
#146380=CARTESIAN_POINT('Ctrl Pts',(-47.5725252596992,18.4296944698521,
657.201654411765));
#146381=CARTESIAN_POINT('Ctrl Pts',(-45.4742952008371,22.6435084734481,
655.707536764706));
#146382=CARTESIAN_POINT('Ctrl Pts',(-43.3760651419751,26.8573224770442,
654.213419117647));
#146383=CARTESIAN_POINT('Ctrl Pts',(-40.5392751458362,30.6138395280662,
652.719301470588));
#146384=CARTESIAN_POINT('Ctrl Pts',(-37.7024851496972,34.3703565790883,
651.22518382353));
#146385=CARTESIAN_POINT('Ctrl Pts',(-34.2237386972451,37.5416529948095,
649.731066176471));
#146386=CARTESIAN_POINT('Ctrl Pts',(-30.744992244793,40.7129494105307,648.236948529412));
#146387=CARTESIAN_POINT('Ctrl Pts',(-26.7427538741697,43.1910304950644,
646.742830882353));
#146388=CARTESIAN_POINT('Ctrl Pts',(-22.7405155035463,45.6691115795981,
645.248713235294));
#146389=CARTESIAN_POINT('Ctrl Pts',(-18.3510766423074,47.3695892537413,
643.754595588235));
#146390=CARTESIAN_POINT('Ctrl Pts',(-13.9616377810684,49.0700669278844,
642.260477941177));
#146391=CARTESIAN_POINT('Ctrl Pts',(-9.33447550508177,49.9350334639422,
640.766360294118));
#146392=CARTESIAN_POINT('Ctrl Pts',(-4.7073132290951,50.8,639.272242647059));
#146393=CARTESIAN_POINT('Ctrl Pts',(-6.22120573966855E-15,50.8,637.778125));
#146394=CARTESIAN_POINT('Ctrl Pts',(4.70731322909511,50.8,636.284007352941));
#146395=CARTESIAN_POINT('Ctrl Pts',(9.33447550508176,49.9350334639422,634.789889705882));
#146396=CARTESIAN_POINT('Ctrl Pts',(13.9616377810684,49.0700669278844,633.295772058824));
#146397=CARTESIAN_POINT('Ctrl Pts',(18.3510766423074,47.3695892537413,631.801654411765));
#146398=CARTESIAN_POINT('Ctrl Pts',(22.7405155035463,45.6691115795981,630.307536764706));
#146399=CARTESIAN_POINT('Ctrl Pts',(26.7427538741697,43.1910304950644,628.813419117647));
#146400=CARTESIAN_POINT('Ctrl Pts',(30.744992244793,40.7129494105307,627.319301470588));
#146401=CARTESIAN_POINT('Ctrl Pts',(34.2237386972451,37.5416529948095,625.82518382353));
#146402=CARTESIAN_POINT('Ctrl Pts',(37.7024851496972,34.3703565790883,624.331066176471));
#146403=CARTESIAN_POINT('Ctrl Pts',(40.5392751458362,30.6138395280662,622.836948529412));
#146404=CARTESIAN_POINT('Ctrl Pts',(43.3760651419751,26.8573224770442,621.342830882353));
#146405=CARTESIAN_POINT('Ctrl Pts',(45.4742952008372,22.6435084734481,619.848713235294));
#146406=CARTESIAN_POINT('Ctrl Pts',(47.5725252596992,18.4296944698521,618.354595588235));
#146407=CARTESIAN_POINT('Ctrl Pts',(48.8607426731792,13.9020798956618,616.860477941176));
#146408=CARTESIAN_POINT('Ctrl Pts',(50.1489600866593,9.37446532147146,615.366360294118));
#146409=CARTESIAN_POINT('Ctrl Pts',(50.5832961557877,4.68723266073574,613.872242647059));
#146410=CARTESIAN_POINT('Ctrl Pts',(51.0176322249162,9.37178700064808E-15,
612.378125));
#146411=CARTESIAN_POINT('Ctrl Pts',(50.5832961557877,-4.68723266073572,
610.884007352941));
#146412=CARTESIAN_POINT('Ctrl Pts',(50.1489600866593,-9.37446532147149,
609.389889705882));
#146413=CARTESIAN_POINT('Ctrl Pts',(48.8607426731792,-13.9020798956618,
607.895772058823));
#146414=CARTESIAN_POINT('Ctrl Pts',(47.5725252596992,-18.4296944698521,
606.401654411765));
#146415=CARTESIAN_POINT('Ctrl Pts',(45.4742952008371,-22.6435084734482,
604.907536764706));
#146416=CARTESIAN_POINT('Ctrl Pts',(43.3760651419751,-26.8573224770441,
603.413419117647));
#146417=CARTESIAN_POINT('Ctrl Pts',(40.5392751458362,-30.6138395280662,
601.919301470588));
#146418=CARTESIAN_POINT('Ctrl Pts',(37.7024851496972,-34.3703565790883,
600.42518382353));
#146419=CARTESIAN_POINT('Ctrl Pts',(34.2237386972451,-37.5416529948095,
598.931066176471));
#146420=CARTESIAN_POINT('Ctrl Pts',(30.744992244793,-40.7129494105307,597.436948529412));
#146421=CARTESIAN_POINT('Ctrl Pts',(26.7427538741697,-43.1910304950644,
595.942830882353));
#146422=CARTESIAN_POINT('Ctrl Pts',(22.7405155035463,-45.6691115795981,
594.448713235294));
#146423=CARTESIAN_POINT('Ctrl Pts',(18.3510766423074,-47.3695892537413,
592.954595588235));
#146424=CARTESIAN_POINT('Ctrl Pts',(13.9616377810684,-49.0700669278844,
591.460477941176));
#146425=CARTESIAN_POINT('Ctrl Pts',(9.33447550508176,-49.9350334639422,
589.966360294118));
#146426=CARTESIAN_POINT('Ctrl Pts',(4.70731322909511,-50.8,588.472242647059));
#146427=CARTESIAN_POINT('Ctrl Pts',(0.,-50.8,586.978125));
#146428=CARTESIAN_POINT('Ctrl Pts',(-4.70731322909511,-50.8,585.484007352941));
#146429=CARTESIAN_POINT('Ctrl Pts',(-9.33447550508177,-49.9350334639422,
583.989889705882));
#146430=CARTESIAN_POINT('Ctrl Pts',(-13.9616377810684,-49.0700669278844,
582.495772058823));
#146431=CARTESIAN_POINT('Ctrl Pts',(-18.3510766423074,-47.3695892537413,
581.001654411765));
#146432=CARTESIAN_POINT('Ctrl Pts',(-22.7405155035463,-45.6691115795981,
579.507536764706));
#146433=CARTESIAN_POINT('Ctrl Pts',(-26.7427538741697,-43.1910304950644,
578.013419117647));
#146434=CARTESIAN_POINT('Ctrl Pts',(-30.744992244793,-40.7129494105307,
576.519301470588));
#146435=CARTESIAN_POINT('Ctrl Pts',(-34.2237386972451,-37.5416529948095,
575.025183823529));
#146436=CARTESIAN_POINT('Ctrl Pts',(-37.7024851496972,-34.3703565790883,
573.531066176471));
#146437=CARTESIAN_POINT('Ctrl Pts',(-40.5392751458362,-30.6138395280662,
572.036948529412));
#146438=CARTESIAN_POINT('Ctrl Pts',(-43.3760651419751,-26.8573224770441,
570.542830882353));
#146439=CARTESIAN_POINT('Ctrl Pts',(-45.4742952008371,-22.6435084734481,
569.048713235294));
#146440=CARTESIAN_POINT('Ctrl Pts',(-47.5725252596992,-18.4296944698521,
567.554595588235));
#146441=CARTESIAN_POINT('Ctrl Pts',(-48.8607426731792,-13.9020798956618,
566.060477941176));
#146442=CARTESIAN_POINT('Ctrl Pts',(-50.1489600866593,-9.37446532147148,
564.566360294118));
#146443=CARTESIAN_POINT('Ctrl Pts',(-50.5832961557877,-4.68723266073574,
563.072242647059));
#146444=CARTESIAN_POINT('Ctrl Pts',(-51.0176322249162,-3.12392900021603E-15,
561.578125));
#146445=CARTESIAN_POINT('Ctrl Pts',(-50.5832961557877,4.68723266073573,
560.084007352941));
#146446=CARTESIAN_POINT('Ctrl Pts',(-50.1489600866593,9.37446532147149,
558.589889705882));
#146447=CARTESIAN_POINT('Ctrl Pts',(-48.8607426731792,13.9020798956618,
557.095772058824));
#146448=CARTESIAN_POINT('Ctrl Pts',(-47.5725252596992,18.4296944698521,
555.601654411765));
#146449=CARTESIAN_POINT('Ctrl Pts',(-45.4742952008371,22.6435084734481,
554.107536764706));
#146450=CARTESIAN_POINT('Ctrl Pts',(-43.3760651419751,26.8573224770442,
552.613419117647));
#146451=CARTESIAN_POINT('Ctrl Pts',(-40.5392751458362,30.6138395280662,
551.119301470588));
#146452=CARTESIAN_POINT('Ctrl Pts',(-37.7024851496972,34.3703565790883,
549.62518382353));
#146453=CARTESIAN_POINT('Ctrl Pts',(-34.2237386972451,37.5416529948095,
548.131066176471));
#146454=CARTESIAN_POINT('Ctrl Pts',(-30.744992244793,40.7129494105307,546.636948529412));
#146455=CARTESIAN_POINT('Ctrl Pts',(-26.7427538741697,43.1910304950644,
545.142830882353));
#146456=CARTESIAN_POINT('Ctrl Pts',(-22.7405155035463,45.6691115795981,
543.648713235294));
#146457=CARTESIAN_POINT('Ctrl Pts',(-18.3510766423074,47.3695892537413,
542.154595588235));
#146458=CARTESIAN_POINT('Ctrl Pts',(-13.9616377810684,49.0700669278844,
540.660477941176));
#146459=CARTESIAN_POINT('Ctrl Pts',(-9.33447550508177,49.9350334639422,
539.166360294118));
#146460=CARTESIAN_POINT('Ctrl Pts',(-4.7073132290951,50.8,537.672242647059));
#146461=CARTESIAN_POINT('Ctrl Pts',(-6.22120573966855E-15,50.8,536.178125));
#146462=CARTESIAN_POINT('Ctrl Pts',(4.70731322909511,50.8,534.684007352941));
#146463=CARTESIAN_POINT('Ctrl Pts',(9.33447550508176,49.9350334639422,533.189889705882));
#146464=CARTESIAN_POINT('Ctrl Pts',(13.9616377810684,49.0700669278844,531.695772058824));
#146465=CARTESIAN_POINT('Ctrl Pts',(18.3510766423074,47.3695892537413,530.201654411765));
#146466=CARTESIAN_POINT('Ctrl Pts',(22.7405155035463,45.6691115795981,528.707536764706));
#146467=CARTESIAN_POINT('Ctrl Pts',(26.7427538741697,43.1910304950644,527.213419117647));
#146468=CARTESIAN_POINT('Ctrl Pts',(30.744992244793,40.7129494105307,525.719301470588));
#146469=CARTESIAN_POINT('Ctrl Pts',(34.2237386972451,37.5416529948095,524.22518382353));
#146470=CARTESIAN_POINT('Ctrl Pts',(37.7024851496972,34.3703565790883,522.731066176471));
#146471=CARTESIAN_POINT('Ctrl Pts',(40.5392751458362,30.6138395280662,521.236948529412));
#146472=CARTESIAN_POINT('Ctrl Pts',(43.3760651419751,26.8573224770442,519.742830882353));
#146473=CARTESIAN_POINT('Ctrl Pts',(45.4742952008372,22.6435084734481,518.248713235294));
#146474=CARTESIAN_POINT('Ctrl Pts',(47.5725252596992,18.4296944698521,516.754595588235));
#146475=CARTESIAN_POINT('Ctrl Pts',(48.8607426731792,13.9020798956618,515.260477941176));
#146476=CARTESIAN_POINT('Ctrl Pts',(50.1489600866593,9.37446532147146,513.766360294118));
#146477=CARTESIAN_POINT('Ctrl Pts',(50.5832961557877,4.68723266073574,512.272242647059));
#146478=CARTESIAN_POINT('Ctrl Pts',(51.0176322249162,9.37178700064808E-15,
510.778125));
#146479=CARTESIAN_POINT('Ctrl Pts',(50.5832961557877,-4.68723266073572,
509.284007352941));
#146480=CARTESIAN_POINT('Ctrl Pts',(50.1489600866593,-9.37446532147149,
507.789889705882));
#146481=CARTESIAN_POINT('Ctrl Pts',(48.8607426731792,-13.9020798956618,
506.295772058824));
#146482=CARTESIAN_POINT('Ctrl Pts',(47.5725252596992,-18.4296944698521,
504.801654411765));
#146483=CARTESIAN_POINT('Ctrl Pts',(45.4742952008371,-22.6435084734482,
503.307536764706));
#146484=CARTESIAN_POINT('Ctrl Pts',(43.3760651419751,-26.8573224770441,
501.813419117647));
#146485=CARTESIAN_POINT('Ctrl Pts',(40.5392751458362,-30.6138395280662,
500.319301470588));
#146486=CARTESIAN_POINT('Ctrl Pts',(37.7024851496972,-34.3703565790883,
498.825183823529));
#146487=CARTESIAN_POINT('Ctrl Pts',(34.2237386972451,-37.5416529948095,
497.331066176471));
#146488=CARTESIAN_POINT('Ctrl Pts',(30.744992244793,-40.7129494105307,495.836948529412));
#146489=CARTESIAN_POINT('Ctrl Pts',(26.7427538741697,-43.1910304950644,
494.342830882353));
#146490=CARTESIAN_POINT('Ctrl Pts',(22.7405155035463,-45.6691115795981,
492.848713235294));
#146491=CARTESIAN_POINT('Ctrl Pts',(18.3510766423074,-47.3695892537413,
491.354595588235));
#146492=CARTESIAN_POINT('Ctrl Pts',(13.9616377810684,-49.0700669278844,
489.860477941177));
#146493=CARTESIAN_POINT('Ctrl Pts',(9.33447550508176,-49.9350334639422,
488.366360294118));
#146494=CARTESIAN_POINT('Ctrl Pts',(4.70731322909511,-50.8,486.872242647059));
#146495=CARTESIAN_POINT('Ctrl Pts',(0.,-50.8,485.378125));
#146496=CARTESIAN_POINT('Ctrl Pts',(-4.70731322909511,-50.8,483.884007352941));
#146497=CARTESIAN_POINT('Ctrl Pts',(-9.33447550508177,-49.9350334639422,
482.389889705883));
#146498=CARTESIAN_POINT('Ctrl Pts',(-13.9616377810684,-49.0700669278844,
480.895772058824));
#146499=CARTESIAN_POINT('Ctrl Pts',(-18.3510766423074,-47.3695892537413,
479.401654411765));
#146500=CARTESIAN_POINT('Ctrl Pts',(-22.7405155035463,-45.6691115795981,
477.907536764706));
#146501=CARTESIAN_POINT('Ctrl Pts',(-26.7427538741697,-43.1910304950644,
476.413419117647));
#146502=CARTESIAN_POINT('Ctrl Pts',(-30.744992244793,-40.7129494105307,
474.919301470588));
#146503=CARTESIAN_POINT('Ctrl Pts',(-34.2237386972451,-37.5416529948095,
473.425183823529));
#146504=CARTESIAN_POINT('Ctrl Pts',(-37.7024851496972,-34.3703565790883,
471.931066176471));
#146505=CARTESIAN_POINT('Ctrl Pts',(-40.5392751458362,-30.6138395280662,
470.436948529412));
#146506=CARTESIAN_POINT('Ctrl Pts',(-43.3760651419751,-26.8573224770441,
468.942830882353));
#146507=CARTESIAN_POINT('Ctrl Pts',(-45.4742952008371,-22.6435084734481,
467.448713235294));
#146508=CARTESIAN_POINT('Ctrl Pts',(-47.5725252596992,-18.4296944698521,
465.954595588235));
#146509=CARTESIAN_POINT('Ctrl Pts',(-48.8607426731792,-13.9020798956618,
464.460477941177));
#146510=CARTESIAN_POINT('Ctrl Pts',(-50.1489600866593,-9.37446532147148,
462.966360294118));
#146511=CARTESIAN_POINT('Ctrl Pts',(-50.5832961557877,-4.68723266073574,
461.472242647059));
#146512=CARTESIAN_POINT('Ctrl Pts',(-51.0176322249162,-3.12392900021603E-15,
459.978125));
#146513=CARTESIAN_POINT('Ctrl Pts',(-50.5832961557877,4.68723266073573,
458.484007352941));
#146514=CARTESIAN_POINT('Ctrl Pts',(-50.1489600866593,9.37446532147149,
456.989889705882));
#146515=CARTESIAN_POINT('Ctrl Pts',(-48.8607426731792,13.9020798956618,
455.495772058824));
#146516=CARTESIAN_POINT('Ctrl Pts',(-47.5725252596992,18.4296944698521,
454.001654411765));
#146517=CARTESIAN_POINT('Ctrl Pts',(-45.4742952008371,22.6435084734481,
452.507536764706));
#146518=CARTESIAN_POINT('Ctrl Pts',(-43.3760651419751,26.8573224770442,
451.013419117647));
#146519=CARTESIAN_POINT('Ctrl Pts',(-40.5392751458362,30.6138395280662,
449.519301470588));
#146520=CARTESIAN_POINT('Ctrl Pts',(-37.7024851496972,34.3703565790883,
448.02518382353));
#146521=CARTESIAN_POINT('Ctrl Pts',(-34.2237386972451,37.5416529948095,
446.531066176471));
#146522=CARTESIAN_POINT('Ctrl Pts',(-30.744992244793,40.7129494105307,445.036948529412));
#146523=CARTESIAN_POINT('Ctrl Pts',(-26.7427538741697,43.1910304950644,
443.542830882353));
#146524=CARTESIAN_POINT('Ctrl Pts',(-22.7405155035463,45.6691115795981,
442.048713235294));
#146525=CARTESIAN_POINT('Ctrl Pts',(-18.3510766423074,47.3695892537413,
440.554595588235));
#146526=CARTESIAN_POINT('Ctrl Pts',(-13.9616377810684,49.0700669278844,
439.060477941176));
#146527=CARTESIAN_POINT('Ctrl Pts',(-9.33447550508177,49.9350334639422,
437.566360294118));
#146528=CARTESIAN_POINT('Ctrl Pts',(-4.7073132290951,50.8,436.072242647059));
#146529=CARTESIAN_POINT('Ctrl Pts',(-6.22120573966855E-15,50.8,434.578125));
#146530=CARTESIAN_POINT('Ctrl Pts',(4.70731322909511,50.8,433.084007352941));
#146531=CARTESIAN_POINT('Ctrl Pts',(9.33447550508176,49.9350334639422,431.589889705882));
#146532=CARTESIAN_POINT('Ctrl Pts',(13.9616377810684,49.0700669278844,430.095772058824));
#146533=CARTESIAN_POINT('Ctrl Pts',(18.3510766423074,47.3695892537413,428.601654411765));
#146534=CARTESIAN_POINT('Ctrl Pts',(22.7405155035463,45.6691115795981,427.107536764706));
#146535=CARTESIAN_POINT('Ctrl Pts',(26.7427538741697,43.1910304950644,425.613419117647));
#146536=CARTESIAN_POINT('Ctrl Pts',(30.744992244793,40.7129494105307,424.119301470588));
#146537=CARTESIAN_POINT('Ctrl Pts',(34.2237386972451,37.5416529948095,422.62518382353));
#146538=CARTESIAN_POINT('Ctrl Pts',(37.7024851496972,34.3703565790883,421.131066176471));
#146539=CARTESIAN_POINT('Ctrl Pts',(40.5392751458362,30.6138395280662,419.636948529412));
#146540=CARTESIAN_POINT('Ctrl Pts',(43.3760651419751,26.8573224770442,418.142830882353));
#146541=CARTESIAN_POINT('Ctrl Pts',(45.4742952008372,22.6435084734481,416.648713235294));
#146542=CARTESIAN_POINT('Ctrl Pts',(47.5725252596992,18.4296944698521,415.154595588236));
#146543=CARTESIAN_POINT('Ctrl Pts',(48.8607426731792,13.9020798956618,413.660477941177));
#146544=CARTESIAN_POINT('Ctrl Pts',(50.1489600866593,9.37446532147146,412.166360294118));
#146545=CARTESIAN_POINT('Ctrl Pts',(50.5832961557877,4.68723266073574,410.672242647059));
#146546=CARTESIAN_POINT('Ctrl Pts',(51.0176322249162,9.37178700064808E-15,
409.178125));
#146547=CARTESIAN_POINT('Ctrl Pts',(50.5832961557877,-4.68723266073572,
407.684007352941));
#146548=CARTESIAN_POINT('Ctrl Pts',(50.1489600866593,-9.37446532147149,
406.189889705882));
#146549=CARTESIAN_POINT('Ctrl Pts',(48.8607426731792,-13.9020798956618,
404.695772058824));
#146550=CARTESIAN_POINT('Ctrl Pts',(47.5725252596992,-18.4296944698521,
403.201654411765));
#146551=CARTESIAN_POINT('Ctrl Pts',(45.4742952008371,-22.6435084734482,
401.707536764706));
#146552=CARTESIAN_POINT('Ctrl Pts',(43.3760651419751,-26.8573224770441,
400.213419117647));
#146553=CARTESIAN_POINT('Ctrl Pts',(40.5392751458362,-30.6138395280662,
398.719301470588));
#146554=CARTESIAN_POINT('Ctrl Pts',(37.7024851496972,-34.3703565790883,
397.22518382353));
#146555=CARTESIAN_POINT('Ctrl Pts',(34.2237386972451,-37.5416529948095,
395.731066176471));
#146556=CARTESIAN_POINT('Ctrl Pts',(30.744992244793,-40.7129494105307,394.236948529412));
#146557=CARTESIAN_POINT('Ctrl Pts',(26.7427538741697,-43.1910304950644,
392.742830882353));
#146558=CARTESIAN_POINT('Ctrl Pts',(22.7405155035463,-45.6691115795981,
391.248713235294));
#146559=CARTESIAN_POINT('Ctrl Pts',(18.3510766423074,-47.3695892537413,
389.754595588235));
#146560=CARTESIAN_POINT('Ctrl Pts',(13.9616377810684,-49.0700669278844,
388.260477941176));
#146561=CARTESIAN_POINT('Ctrl Pts',(9.33447550508176,-49.9350334639422,
386.766360294118));
#146562=CARTESIAN_POINT('Ctrl Pts',(4.70731322909511,-50.8,385.272242647059));
#146563=CARTESIAN_POINT('Ctrl Pts',(0.,-50.8,383.778125));
#146564=CARTESIAN_POINT('Ctrl Pts',(-4.70731322909511,-50.8,382.284007352941));
#146565=CARTESIAN_POINT('Ctrl Pts',(-9.33447550508177,-49.9350334639422,
380.789889705882));
#146566=CARTESIAN_POINT('Ctrl Pts',(-13.9616377810684,-49.0700669278844,
379.295772058823));
#146567=CARTESIAN_POINT('Ctrl Pts',(-18.3510766423074,-47.3695892537413,
377.801654411765));
#146568=CARTESIAN_POINT('Ctrl Pts',(-22.7405155035463,-45.6691115795981,
376.307536764706));
#146569=CARTESIAN_POINT('Ctrl Pts',(-26.7427538741697,-43.1910304950644,
374.813419117647));
#146570=CARTESIAN_POINT('Ctrl Pts',(-30.744992244793,-40.7129494105307,
373.319301470588));
#146571=CARTESIAN_POINT('Ctrl Pts',(-34.2237386972451,-37.5416529948095,
371.825183823529));
#146572=CARTESIAN_POINT('Ctrl Pts',(-37.7024851496972,-34.3703565790883,
370.331066176471));
#146573=CARTESIAN_POINT('Ctrl Pts',(-40.5392751458362,-30.6138395280662,
368.836948529412));
#146574=CARTESIAN_POINT('Ctrl Pts',(-43.3760651419751,-26.8573224770441,
367.342830882353));
#146575=CARTESIAN_POINT('Ctrl Pts',(-45.4742952008371,-22.6435084734481,
365.848713235294));
#146576=CARTESIAN_POINT('Ctrl Pts',(-47.5725252596992,-18.4296944698521,
364.354595588235));
#146577=CARTESIAN_POINT('Ctrl Pts',(-48.8607426731792,-13.9020798956618,
362.860477941177));
#146578=CARTESIAN_POINT('Ctrl Pts',(-50.1489600866593,-9.37446532147148,
361.366360294118));
#146579=CARTESIAN_POINT('Ctrl Pts',(-50.5832961557877,-4.68723266073574,
359.872242647059));
#146580=CARTESIAN_POINT('Ctrl Pts',(-51.0176322249162,-3.12392900021603E-15,
358.378125));
#146581=CARTESIAN_POINT('Ctrl Pts',(-50.5832961557877,4.68723266073573,
356.884007352941));
#146582=CARTESIAN_POINT('Ctrl Pts',(-50.1489600866593,9.37446532147149,
355.389889705882));
#146583=CARTESIAN_POINT('Ctrl Pts',(-48.8607426731792,13.9020798956618,
353.895772058824));
#146584=CARTESIAN_POINT('Ctrl Pts',(-47.5725252596992,18.4296944698521,
352.401654411765));
#146585=CARTESIAN_POINT('Ctrl Pts',(-45.4742952008371,22.6435084734481,
350.907536764706));
#146586=CARTESIAN_POINT('Ctrl Pts',(-43.3760651419751,26.8573224770442,
349.413419117647));
#146587=CARTESIAN_POINT('Ctrl Pts',(-40.5392751458362,30.6138395280662,
347.919301470588));
#146588=CARTESIAN_POINT('Ctrl Pts',(-37.7024851496972,34.3703565790883,
346.42518382353));
#146589=CARTESIAN_POINT('Ctrl Pts',(-34.2237386972451,37.5416529948095,
344.931066176471));
#146590=CARTESIAN_POINT('Ctrl Pts',(-30.744992244793,40.7129494105307,343.436948529412));
#146591=CARTESIAN_POINT('Ctrl Pts',(-26.7427538741697,43.1910304950644,
341.942830882353));
#146592=CARTESIAN_POINT('Ctrl Pts',(-22.7405155035463,45.6691115795981,
340.448713235294));
#146593=CARTESIAN_POINT('Ctrl Pts',(-18.3510766423074,47.3695892537413,
338.954595588235));
#146594=CARTESIAN_POINT('Ctrl Pts',(-13.9616377810684,49.0700669278844,
337.460477941177));
#146595=CARTESIAN_POINT('Ctrl Pts',(-9.33447550508177,49.9350334639422,
335.966360294118));
#146596=CARTESIAN_POINT('Ctrl Pts',(-4.7073132290951,50.8,334.472242647059));
#146597=CARTESIAN_POINT('Ctrl Pts',(-6.22120573966855E-15,50.8,332.978125));
#146598=CARTESIAN_POINT('Ctrl Pts',(4.70731322909511,50.8,331.484007352941));
#146599=CARTESIAN_POINT('Ctrl Pts',(9.33447550508176,49.9350334639422,329.989889705882));
#146600=CARTESIAN_POINT('Ctrl Pts',(13.9616377810684,49.0700669278844,328.495772058823));
#146601=CARTESIAN_POINT('Ctrl Pts',(18.3510766423074,47.3695892537413,327.001654411765));
#146602=CARTESIAN_POINT('Ctrl Pts',(22.7405155035463,45.6691115795981,325.507536764706));
#146603=CARTESIAN_POINT('Ctrl Pts',(26.7427538741697,43.1910304950644,324.013419117647));
#146604=CARTESIAN_POINT('Ctrl Pts',(30.744992244793,40.7129494105307,322.519301470588));
#146605=CARTESIAN_POINT('Ctrl Pts',(34.2237386972451,37.5416529948095,321.025183823529));
#146606=CARTESIAN_POINT('Ctrl Pts',(37.7024851496972,34.3703565790883,319.531066176471));
#146607=CARTESIAN_POINT('Ctrl Pts',(40.5392751458362,30.6138395280662,318.036948529412));
#146608=CARTESIAN_POINT('Ctrl Pts',(43.3760651419751,26.8573224770442,316.542830882353));
#146609=CARTESIAN_POINT('Ctrl Pts',(45.4742952008372,22.6435084734481,315.048713235294));
#146610=CARTESIAN_POINT('Ctrl Pts',(47.5725252596992,18.4296944698521,313.554595588235));
#146611=CARTESIAN_POINT('Ctrl Pts',(48.8607426731792,13.9020798956618,312.060477941176));
#146612=CARTESIAN_POINT('Ctrl Pts',(50.1489600866593,9.37446532147146,310.566360294118));
#146613=CARTESIAN_POINT('Ctrl Pts',(50.5832961557877,4.68723266073574,309.072242647059));
#146614=CARTESIAN_POINT('Ctrl Pts',(51.0176322249162,9.37178700064808E-15,
307.578125));
#146615=CARTESIAN_POINT('Ctrl Pts',(50.5832961557877,-4.68723266073572,
306.084007352941));
#146616=CARTESIAN_POINT('Ctrl Pts',(50.1489600866593,-9.37446532147149,
304.589889705882));
#146617=CARTESIAN_POINT('Ctrl Pts',(48.8607426731792,-13.9020798956618,
303.095772058824));
#146618=CARTESIAN_POINT('Ctrl Pts',(47.5725252596992,-18.4296944698521,
301.601654411765));
#146619=CARTESIAN_POINT('Ctrl Pts',(45.4742952008371,-22.6435084734482,
300.107536764706));
#146620=CARTESIAN_POINT('Ctrl Pts',(43.3760651419751,-26.8573224770441,
298.613419117647));
#146621=CARTESIAN_POINT('Ctrl Pts',(40.5392751458362,-30.6138395280662,
297.119301470588));
#146622=CARTESIAN_POINT('Ctrl Pts',(37.7024851496972,-34.3703565790883,
295.625183823529));
#146623=CARTESIAN_POINT('Ctrl Pts',(34.2237386972451,-37.5416529948095,
294.131066176471));
#146624=CARTESIAN_POINT('Ctrl Pts',(30.744992244793,-40.7129494105307,292.636948529412));
#146625=CARTESIAN_POINT('Ctrl Pts',(26.7427538741697,-43.1910304950644,
291.142830882353));
#146626=CARTESIAN_POINT('Ctrl Pts',(22.7405155035463,-45.6691115795981,
289.648713235294));
#146627=CARTESIAN_POINT('Ctrl Pts',(18.3510766423074,-47.3695892537413,
288.154595588235));
#146628=CARTESIAN_POINT('Ctrl Pts',(13.9616377810684,-49.0700669278844,
286.660477941177));
#146629=CARTESIAN_POINT('Ctrl Pts',(9.33447550508176,-49.9350334639422,
285.166360294118));
#146630=CARTESIAN_POINT('Ctrl Pts',(4.70731322909511,-50.8,283.672242647059));
#146631=CARTESIAN_POINT('Ctrl Pts',(0.,-50.8,282.178125));
#146632=CARTESIAN_POINT('Ctrl Pts',(-4.70731322909511,-50.8,280.684007352941));
#146633=CARTESIAN_POINT('Ctrl Pts',(-9.33447550508177,-49.9350334639422,
279.189889705882));
#146634=CARTESIAN_POINT('Ctrl Pts',(-13.9616377810684,-49.0700669278844,
277.695772058824));
#146635=CARTESIAN_POINT('Ctrl Pts',(-18.3510766423074,-47.3695892537413,
276.201654411765));
#146636=CARTESIAN_POINT('Ctrl Pts',(-22.7405155035463,-45.6691115795981,
274.707536764706));
#146637=CARTESIAN_POINT('Ctrl Pts',(-26.7427538741697,-43.1910304950644,
273.213419117647));
#146638=CARTESIAN_POINT('Ctrl Pts',(-30.744992244793,-40.7129494105307,
271.719301470588));
#146639=CARTESIAN_POINT('Ctrl Pts',(-34.2237386972451,-37.5416529948095,
270.225183823529));
#146640=CARTESIAN_POINT('Ctrl Pts',(-37.7024851496972,-34.3703565790883,
268.731066176471));
#146641=CARTESIAN_POINT('Ctrl Pts',(-40.5392751458362,-30.6138395280662,
267.236948529412));
#146642=CARTESIAN_POINT('Ctrl Pts',(-43.3760651419751,-26.8573224770441,
265.742830882353));
#146643=CARTESIAN_POINT('Ctrl Pts',(-45.4742952008371,-22.6435084734481,
264.248713235294));
#146644=CARTESIAN_POINT('Ctrl Pts',(-47.5725252596992,-18.4296944698521,
262.754595588235));
#146645=CARTESIAN_POINT('Ctrl Pts',(-48.8607426731792,-13.9020798956618,
261.260477941176));
#146646=CARTESIAN_POINT('Ctrl Pts',(-50.1489600866593,-9.37446532147148,
259.766360294118));
#146647=CARTESIAN_POINT('Ctrl Pts',(-50.5832961557877,-4.68723266073574,
258.272242647059));
#146648=CARTESIAN_POINT('Ctrl Pts',(-51.0176322249162,-3.12392900021603E-15,
256.778125));
#146649=CARTESIAN_POINT('Ctrl Pts',(-50.5832961557877,4.68723266073573,
255.284007352941));
#146650=CARTESIAN_POINT('Ctrl Pts',(-50.1489600866593,9.37446532147149,
253.789889705882));
#146651=CARTESIAN_POINT('Ctrl Pts',(-48.8607426731792,13.9020798956618,
252.295772058824));
#146652=CARTESIAN_POINT('Ctrl Pts',(-47.5725252596992,18.4296944698521,
250.801654411765));
#146653=CARTESIAN_POINT('Ctrl Pts',(-45.4742952008371,22.6435084734481,
249.307536764706));
#146654=CARTESIAN_POINT('Ctrl Pts',(-43.3760651419751,26.8573224770442,
247.813419117647));
#146655=CARTESIAN_POINT('Ctrl Pts',(-40.5392751458362,30.6138395280662,
246.319301470588));
#146656=CARTESIAN_POINT('Ctrl Pts',(-37.7024851496972,34.3703565790883,
244.825183823529));
#146657=CARTESIAN_POINT('Ctrl Pts',(-34.2237386972451,37.5416529948095,
243.331066176471));
#146658=CARTESIAN_POINT('Ctrl Pts',(-30.744992244793,40.7129494105307,241.836948529412));
#146659=CARTESIAN_POINT('Ctrl Pts',(-26.7427538741697,43.1910304950644,
240.342830882353));
#146660=CARTESIAN_POINT('Ctrl Pts',(-22.7405155035463,45.6691115795981,
238.848713235294));
#146661=CARTESIAN_POINT('Ctrl Pts',(-18.3510766423074,47.3695892537413,
237.354595588235));
#146662=CARTESIAN_POINT('Ctrl Pts',(-13.9616377810684,49.0700669278844,
235.860477941177));
#146663=CARTESIAN_POINT('Ctrl Pts',(-9.33447550508177,49.9350334639422,
234.366360294118));
#146664=CARTESIAN_POINT('Ctrl Pts',(-4.7073132290951,50.8,232.872242647059));
#146665=CARTESIAN_POINT('Ctrl Pts',(-6.22120573966855E-15,50.8,231.378125));
#146666=CARTESIAN_POINT('Ctrl Pts',(4.70731322909511,50.8,229.884007352941));
#146667=CARTESIAN_POINT('Ctrl Pts',(9.33447550508176,49.9350334639422,228.389889705882));
#146668=CARTESIAN_POINT('Ctrl Pts',(13.9616377810684,49.0700669278844,226.895772058824));
#146669=CARTESIAN_POINT('Ctrl Pts',(18.3510766423074,47.3695892537413,225.401654411765));
#146670=CARTESIAN_POINT('Ctrl Pts',(22.7405155035463,45.6691115795981,223.907536764706));
#146671=CARTESIAN_POINT('Ctrl Pts',(26.7427538741697,43.1910304950644,222.413419117647));
#146672=CARTESIAN_POINT('Ctrl Pts',(30.744992244793,40.7129494105307,220.919301470588));
#146673=CARTESIAN_POINT('Ctrl Pts',(34.2237386972451,37.5416529948095,219.425183823529));
#146674=CARTESIAN_POINT('Ctrl Pts',(37.7024851496972,34.3703565790883,217.931066176471));
#146675=CARTESIAN_POINT('Ctrl Pts',(40.5392751458362,30.6138395280662,216.436948529412));
#146676=CARTESIAN_POINT('Ctrl Pts',(43.3760651419751,26.8573224770442,214.942830882353));
#146677=CARTESIAN_POINT('Ctrl Pts',(45.4742952008372,22.6435084734481,213.448713235294));
#146678=CARTESIAN_POINT('Ctrl Pts',(47.5725252596992,18.4296944698521,211.954595588235));
#146679=CARTESIAN_POINT('Ctrl Pts',(48.8607426731792,13.9020798956618,210.460477941177));
#146680=CARTESIAN_POINT('Ctrl Pts',(50.1489600866593,9.37446532147146,208.966360294118));
#146681=CARTESIAN_POINT('Ctrl Pts',(50.5832961557877,4.68723266073574,207.472242647059));
#146682=CARTESIAN_POINT('Ctrl Pts',(51.0176322249162,9.37178700064808E-15,
205.978125));
#146683=CARTESIAN_POINT('Ctrl Pts',(50.5832961557877,-4.68723266073572,
204.484007352941));
#146684=CARTESIAN_POINT('Ctrl Pts',(50.1489600866593,-9.37446532147149,
202.989889705882));
#146685=CARTESIAN_POINT('Ctrl Pts',(48.8607426731792,-13.9020798956618,
201.495772058824));
#146686=CARTESIAN_POINT('Ctrl Pts',(47.5725252596992,-18.4296944698521,
200.001654411765));
#146687=CARTESIAN_POINT('Ctrl Pts',(45.4742952008371,-22.6435084734482,
198.507536764706));
#146688=CARTESIAN_POINT('Ctrl Pts',(43.3760651419751,-26.8573224770441,
197.013419117647));
#146689=CARTESIAN_POINT('Ctrl Pts',(40.5392751458362,-30.6138395280662,
195.519301470588));
#146690=CARTESIAN_POINT('Ctrl Pts',(37.7024851496972,-34.3703565790883,
194.025183823529));
#146691=CARTESIAN_POINT('Ctrl Pts',(34.2237386972451,-37.5416529948095,
192.531066176471));
#146692=CARTESIAN_POINT('Ctrl Pts',(30.744992244793,-40.7129494105307,191.036948529412));
#146693=CARTESIAN_POINT('Ctrl Pts',(26.7427538741697,-43.1910304950644,
189.542830882353));
#146694=CARTESIAN_POINT('Ctrl Pts',(22.7405155035463,-45.6691115795981,
188.048713235294));
#146695=CARTESIAN_POINT('Ctrl Pts',(18.3510766423074,-47.3695892537413,
186.554595588235));
#146696=CARTESIAN_POINT('Ctrl Pts',(13.9616377810684,-49.0700669278844,
185.060477941176));
#146697=CARTESIAN_POINT('Ctrl Pts',(9.33447550508176,-49.9350334639422,
183.566360294118));
#146698=CARTESIAN_POINT('Ctrl Pts',(4.70731322909511,-50.8,182.072242647059));
#146699=CARTESIAN_POINT('Ctrl Pts',(0.,-50.8,180.578125));
#146700=CARTESIAN_POINT('Ctrl Pts',(-4.70731322909511,-50.8,179.084007352941));
#146701=CARTESIAN_POINT('Ctrl Pts',(-9.33447550508177,-49.9350334639422,
177.589889705882));
#146702=CARTESIAN_POINT('Ctrl Pts',(-13.9616377810684,-49.0700669278844,
176.095772058824));
#146703=CARTESIAN_POINT('Ctrl Pts',(-18.3510766423074,-47.3695892537413,
174.601654411765));
#146704=CARTESIAN_POINT('Ctrl Pts',(-22.7405155035463,-45.6691115795981,
173.107536764706));
#146705=CARTESIAN_POINT('Ctrl Pts',(-26.7427538741697,-43.1910304950644,
171.613419117647));
#146706=CARTESIAN_POINT('Ctrl Pts',(-30.744992244793,-40.7129494105307,
170.119301470588));
#146707=CARTESIAN_POINT('Ctrl Pts',(-34.2237386972451,-37.5416529948095,
168.62518382353));
#146708=CARTESIAN_POINT('Ctrl Pts',(-37.7024851496972,-34.3703565790883,
167.131066176471));
#146709=CARTESIAN_POINT('Ctrl Pts',(-40.5392751458362,-30.6138395280662,
165.636948529412));
#146710=CARTESIAN_POINT('Ctrl Pts',(-43.3760651419751,-26.8573224770441,
164.142830882353));
#146711=CARTESIAN_POINT('Ctrl Pts',(-45.4742952008371,-22.6435084734481,
162.648713235294));
#146712=CARTESIAN_POINT('Ctrl Pts',(-47.5725252596992,-18.4296944698521,
161.154595588235));
#146713=CARTESIAN_POINT('Ctrl Pts',(-48.8607426731792,-13.9020798956618,
159.660477941177));
#146714=CARTESIAN_POINT('Ctrl Pts',(-50.1489600866593,-9.37446532147148,
158.166360294118));
#146715=CARTESIAN_POINT('Ctrl Pts',(-50.5832961557877,-4.68723266073574,
156.672242647059));
#146716=CARTESIAN_POINT('Ctrl Pts',(-51.0176322249162,-3.12392900021603E-15,
155.178125));
#146717=CARTESIAN_POINT('Ctrl Pts',(-50.5832961557877,4.68723266073573,
153.684007352941));
#146718=CARTESIAN_POINT('Ctrl Pts',(-50.1489600866593,9.37446532147149,
152.189889705882));
#146719=CARTESIAN_POINT('Ctrl Pts',(-48.8607426731792,13.9020798956618,
150.695772058824));
#146720=CARTESIAN_POINT('Ctrl Pts',(-47.5725252596992,18.4296944698521,
149.201654411765));
#146721=CARTESIAN_POINT('Ctrl Pts',(-45.4742952008371,22.6435084734481,
147.707536764706));
#146722=CARTESIAN_POINT('Ctrl Pts',(-43.3760651419751,26.8573224770442,
146.213419117647));
#146723=CARTESIAN_POINT('Ctrl Pts',(-40.5392751458362,30.6138395280662,
144.719301470588));
#146724=CARTESIAN_POINT('Ctrl Pts',(-37.7024851496972,34.3703565790883,
143.225183823529));
#146725=CARTESIAN_POINT('Ctrl Pts',(-34.2237386972451,37.5416529948095,
141.731066176471));
#146726=CARTESIAN_POINT('Ctrl Pts',(-30.744992244793,40.7129494105307,140.236948529412));
#146727=CARTESIAN_POINT('Ctrl Pts',(-26.7427538741697,43.1910304950644,
138.742830882353));
#146728=CARTESIAN_POINT('Ctrl Pts',(-22.7405155035463,45.6691115795981,
137.248713235294));
#146729=CARTESIAN_POINT('Ctrl Pts',(-18.3510766423074,47.3695892537413,
135.754595588235));
#146730=CARTESIAN_POINT('Ctrl Pts',(-13.9616377810684,49.0700669278844,
134.260477941176));
#146731=CARTESIAN_POINT('Ctrl Pts',(-9.33447550508177,49.9350334639422,
132.766360294118));
#146732=CARTESIAN_POINT('Ctrl Pts',(-4.7073132290951,50.8,131.272242647059));
#146733=CARTESIAN_POINT('Ctrl Pts',(-6.22120573966855E-15,50.8,129.778125));
#146734=CARTESIAN_POINT('Ctrl Pts',(4.70731322909511,50.8,128.284007352941));
#146735=CARTESIAN_POINT('Ctrl Pts',(9.33447550508176,49.9350334639422,126.789889705882));
#146736=CARTESIAN_POINT('Ctrl Pts',(13.9616377810684,49.0700669278844,125.295772058823));
#146737=CARTESIAN_POINT('Ctrl Pts',(18.3510766423074,47.3695892537413,123.801654411765));
#146738=CARTESIAN_POINT('Ctrl Pts',(22.7405155035463,45.6691115795981,122.307536764706));
#146739=CARTESIAN_POINT('Ctrl Pts',(26.7427538741697,43.1910304950644,120.813419117647));
#146740=CARTESIAN_POINT('Ctrl Pts',(30.744992244793,40.7129494105307,119.319301470588));
#146741=CARTESIAN_POINT('Ctrl Pts',(34.2237386972451,37.5416529948095,117.825183823529));
#146742=CARTESIAN_POINT('Ctrl Pts',(37.7024851496972,34.3703565790883,116.331066176471));
#146743=CARTESIAN_POINT('Ctrl Pts',(40.5392751458362,30.6138395280662,114.836948529412));
#146744=CARTESIAN_POINT('Ctrl Pts',(43.3760651419751,26.8573224770442,113.342830882353));
#146745=CARTESIAN_POINT('Ctrl Pts',(45.4742952008372,22.6435084734481,111.848713235294));
#146746=CARTESIAN_POINT('Ctrl Pts',(47.5725252596992,18.4296944698521,110.354595588235));
#146747=CARTESIAN_POINT('Ctrl Pts',(48.8607426731792,13.9020798956618,108.860477941177));
#146748=CARTESIAN_POINT('Ctrl Pts',(50.1489600866593,9.37446532147146,107.366360294118));
#146749=CARTESIAN_POINT('Ctrl Pts',(50.5832961557877,4.68723266073574,105.872242647059));
#146750=CARTESIAN_POINT('Ctrl Pts',(51.0176322249162,9.37178700064808E-15,
104.378125));
#146751=CARTESIAN_POINT('Ctrl Pts',(50.5832961557877,-4.68723266073572,
102.884007352941));
#146752=CARTESIAN_POINT('Ctrl Pts',(50.1489600866593,-9.37446532147149,
101.389889705882));
#146753=CARTESIAN_POINT('Ctrl Pts',(48.8607426731792,-13.9020798956618,
99.8957720588236));
#146754=CARTESIAN_POINT('Ctrl Pts',(47.5725252596992,-18.4296944698521,
98.4016544117648));
#146755=CARTESIAN_POINT('Ctrl Pts',(45.4742952008371,-22.6435084734482,
96.9075367647059));
#146756=CARTESIAN_POINT('Ctrl Pts',(43.3760651419751,-26.8573224770441,
95.413419117647));
#146757=CARTESIAN_POINT('Ctrl Pts',(40.5392751458362,-30.6138395280662,
93.9193014705884));
#146758=CARTESIAN_POINT('Ctrl Pts',(37.7024851496972,-34.3703565790883,
92.4251838235295));
#146759=CARTESIAN_POINT('Ctrl Pts',(34.2237386972451,-37.5416529948095,
90.9310661764706));
#146760=CARTESIAN_POINT('Ctrl Pts',(30.744992244793,-40.7129494105307,89.4369485294118));
#146761=CARTESIAN_POINT('Ctrl Pts',(26.7427538741697,-43.1910304950644,
87.9428308823529));
#146762=CARTESIAN_POINT('Ctrl Pts',(22.7405155035463,-45.6691115795981,
86.4487132352943));
#146763=CARTESIAN_POINT('Ctrl Pts',(18.3510766423074,-47.3695892537413,
84.9545955882354));
#146764=CARTESIAN_POINT('Ctrl Pts',(13.9616377810684,-49.0700669278844,
83.4604779411765));
#146765=CARTESIAN_POINT('Ctrl Pts',(9.33447550508176,-49.9350334639422,
81.9663602941176));
#146766=CARTESIAN_POINT('Ctrl Pts',(4.70731322909511,-50.8,80.4722426470588));
#146767=CARTESIAN_POINT('Ctrl Pts',(0.,-50.8,78.9781250000001));
#146768=CARTESIAN_POINT('Ctrl Pts',(-4.70731322909511,-50.8,77.4840073529412));
#146769=CARTESIAN_POINT('Ctrl Pts',(-9.33447550508177,-49.9350334639422,
75.9898897058824));
#146770=CARTESIAN_POINT('Ctrl Pts',(-13.9616377810684,-49.0700669278844,
74.4957720588235));
#146771=CARTESIAN_POINT('Ctrl Pts',(-18.3510766423074,-47.3695892537413,
73.0016544117646));
#146772=CARTESIAN_POINT('Ctrl Pts',(-22.7405155035463,-45.6691115795981,
71.507536764706));
#146773=CARTESIAN_POINT('Ctrl Pts',(-26.7427538741697,-43.1910304950644,
70.0134191176471));
#146774=CARTESIAN_POINT('Ctrl Pts',(-30.744992244793,-40.7129494105307,
68.5193014705883));
#146775=CARTESIAN_POINT('Ctrl Pts',(-34.2237386972451,-37.5416529948095,
67.0251838235294));
#146776=CARTESIAN_POINT('Ctrl Pts',(-37.7024851496972,-34.3703565790883,
65.5310661764705));
#146777=CARTESIAN_POINT('Ctrl Pts',(-40.5392751458362,-30.6138395280662,
64.0369485294119));
#146778=CARTESIAN_POINT('Ctrl Pts',(-43.3760651419751,-26.8573224770441,
62.542830882353));
#146779=CARTESIAN_POINT('Ctrl Pts',(-45.4742952008371,-22.6435084734481,
61.0487132352942));
#146780=CARTESIAN_POINT('Ctrl Pts',(-47.5725252596992,-18.4296944698521,
59.5545955882353));
#146781=CARTESIAN_POINT('Ctrl Pts',(-48.8607426731792,-13.9020798956618,
58.0604779411764));
#146782=CARTESIAN_POINT('Ctrl Pts',(-50.1489600866593,-9.37446532147148,
56.5663602941178));
#146783=CARTESIAN_POINT('Ctrl Pts',(-50.5832961557877,-4.68723266073574,
55.0722426470589));
#146784=CARTESIAN_POINT('Ctrl Pts',(-51.0176322249162,-3.12392900021603E-15,
53.578125));
#146785=CARTESIAN_POINT('Ctrl Pts',(-50.5832961557877,4.68723266073573,
52.0840073529412));
#146786=CARTESIAN_POINT('Ctrl Pts',(-50.1489600866593,9.37446532147149,
50.5898897058823));
#146787=CARTESIAN_POINT('Ctrl Pts',(-48.8607426731792,13.9020798956618,
49.0957720588236));
#146788=CARTESIAN_POINT('Ctrl Pts',(-47.5725252596992,18.4296944698521,
47.6016544117648));
#146789=CARTESIAN_POINT('Ctrl Pts',(-45.4742952008371,22.6435084734481,
46.1075367647059));
#146790=CARTESIAN_POINT('Ctrl Pts',(-43.3760651419751,26.8573224770442,
44.613419117647));
#146791=CARTESIAN_POINT('Ctrl Pts',(-40.5392751458362,30.6138395280662,
43.1193014705882));
#146792=CARTESIAN_POINT('Ctrl Pts',(-37.7024851496972,34.3703565790883,
41.6251838235295));
#146793=CARTESIAN_POINT('Ctrl Pts',(-34.2237386972451,37.5416529948095,
40.1310661764707));
#146794=CARTESIAN_POINT('Ctrl Pts',(-30.744992244793,40.7129494105307,38.6369485294118));
#146795=CARTESIAN_POINT('Ctrl Pts',(-26.7427538741697,43.1910304950644,
37.1428308823529));
#146796=CARTESIAN_POINT('Ctrl Pts',(-22.7405155035463,45.6691115795981,
35.6487132352941));
#146797=CARTESIAN_POINT('Ctrl Pts',(-18.3510766423074,47.3695892537413,
34.1545955882354));
#146798=CARTESIAN_POINT('Ctrl Pts',(-13.9616377810684,49.0700669278844,
32.6604779411765));
#146799=CARTESIAN_POINT('Ctrl Pts',(-9.33447550508177,49.9350334639422,
31.1663602941177));
#146800=CARTESIAN_POINT('Ctrl Pts',(-4.7073132290951,50.8,29.6722426470588));
#146801=CARTESIAN_POINT('Ctrl Pts',(-6.22120573966855E-15,50.8,28.1781249999999));
#146802=CARTESIAN_POINT('Ctrl Pts',(4.70731322909511,50.8,26.6840073529413));
#146803=CARTESIAN_POINT('Ctrl Pts',(9.33447550508176,49.9350334639422,25.1898897058824));
#146804=CARTESIAN_POINT('Ctrl Pts',(13.9616377810684,49.0700669278844,23.6957720588236));
#146805=CARTESIAN_POINT('Ctrl Pts',(18.3510766423074,47.3695892537413,22.2016544117647));
#146806=CARTESIAN_POINT('Ctrl Pts',(22.7405155035463,45.6691115795981,20.7075367647058));
#146807=CARTESIAN_POINT('Ctrl Pts',(26.7427538741697,43.1910304950644,19.2134191176472));
#146808=CARTESIAN_POINT('Ctrl Pts',(30.744992244793,40.7129494105307,17.7193014705883));
#146809=CARTESIAN_POINT('Ctrl Pts',(34.2237386972451,37.5416529948095,16.2251838235294));
#146810=CARTESIAN_POINT('Ctrl Pts',(37.7024851496972,34.3703565790883,14.7310661764706));
#146811=CARTESIAN_POINT('Ctrl Pts',(40.5392751458362,30.6138395280662,13.2369485294117));
#146812=CARTESIAN_POINT('Ctrl Pts',(43.3760651419751,26.8573224770442,11.7428308823531));
#146813=CARTESIAN_POINT('Ctrl Pts',(45.4742952008372,22.6435084734481,10.2487132352942));
#146814=CARTESIAN_POINT('Ctrl Pts',(47.5725252596992,18.4296944698521,8.75459558823533));
#146815=CARTESIAN_POINT('Ctrl Pts',(48.8607426731792,13.9020798956618,7.26047794117646));
#146816=CARTESIAN_POINT('Ctrl Pts',(50.1489600866593,9.37446532147146,5.76636029411759));
#146817=CARTESIAN_POINT('Ctrl Pts',(50.5832961557877,4.68723266073574,4.27224264705894));
#146818=CARTESIAN_POINT('Ctrl Pts',(51.0176322249162,9.37178700064808E-15,
2.77812500000008));
#146819=CARTESIAN_POINT('Ctrl Pts',(50.5832961557877,-4.68723266073572,
1.28400735294121));
#146820=CARTESIAN_POINT('Ctrl Pts',(50.1489600866593,-9.37446532147149,
-0.21011029411766));
#146821=CARTESIAN_POINT('Ctrl Pts',(48.8607426731792,-13.9020798956618,
-1.70422794117653));
#146822=CARTESIAN_POINT('Ctrl Pts',(47.5725252596992,-18.4296944698521,
-3.19834558823517));
#146823=CARTESIAN_POINT('Ctrl Pts',(45.4742952008371,-22.6435084734482,
-4.69246323529404));
#146824=CARTESIAN_POINT('Ctrl Pts',(43.3760651419751,-26.8573224770441,
-6.18658088235291));
#146825=CARTESIAN_POINT('Ctrl Pts',(40.5392751458362,-30.6138395280662,
-7.68069852941178));
#146826=CARTESIAN_POINT('Ctrl Pts',(37.7024851496972,-34.3703565790883,
-9.17481617647065));
#146827=CARTESIAN_POINT('Ctrl Pts',(34.2237386972451,-37.5416529948095,
-10.6689338235293));
#146828=CARTESIAN_POINT('Ctrl Pts',(30.744992244793,-40.7129494105307,-12.1630514705882));
#146829=CARTESIAN_POINT('Ctrl Pts',(26.7427538741697,-43.1910304950644,
-13.657169117647));
#146830=CARTESIAN_POINT('Ctrl Pts',(22.7405155035463,-45.6691115795981,
-15.1512867647059));
#146831=CARTESIAN_POINT('Ctrl Pts',(18.3510766423074,-47.3695892537413,
-16.6454044117648));
#146832=CARTESIAN_POINT('Ctrl Pts',(13.9616377810684,-49.0700669278844,
-18.1395220588234));
#146833=CARTESIAN_POINT('Ctrl Pts',(9.33447550508176,-49.9350334639422,
-19.6336397058823));
#146834=CARTESIAN_POINT('Ctrl Pts',(4.70731322909511,-50.8,-21.1277573529411));
#146835=CARTESIAN_POINT('Ctrl Pts',(0.,-50.8,-22.621875));
#146836=CARTESIAN_POINT('Ctrl Pts',(-4.70731322909511,-50.8,-24.1159926470589));
#146837=CARTESIAN_POINT('Ctrl Pts',(-9.33447550508177,-49.9350334639422,
-25.6101102941175));
#146838=CARTESIAN_POINT('Ctrl Pts',(-13.9616377810684,-49.0700669278844,
-27.1042279411764));
#146839=CARTESIAN_POINT('Ctrl Pts',(-18.3510766423074,-47.3695892537413,
-28.5983455882353));
#146840=CARTESIAN_POINT('Ctrl Pts',(-22.7405155035463,-45.6691115795981,
-30.0924632352941));
#146841=CARTESIAN_POINT('Ctrl Pts',(-26.7427538741697,-43.1910304950644,
-31.586580882353));
#146842=CARTESIAN_POINT('Ctrl Pts',(-30.744992244793,-40.7129494105307,
-33.0806985294116));
#146843=CARTESIAN_POINT('Ctrl Pts',(-34.2237386972451,-37.5416529948095,
-34.5748161764705));
#146844=CARTESIAN_POINT('Ctrl Pts',(-37.7024851496972,-34.3703565790883,
-36.0689338235294));
#146845=CARTESIAN_POINT('Ctrl Pts',(-40.5392751458362,-30.6138395280662,
-37.5630514705882));
#146846=CARTESIAN_POINT('Ctrl Pts',(-43.3760651419751,-26.8573224770441,
-39.0571691176471));
#146847=CARTESIAN_POINT('Ctrl Pts',(-45.4742952008371,-22.6435084734481,
-40.5512867647058));
#146848=CARTESIAN_POINT('Ctrl Pts',(-47.5725252596992,-18.4296944698521,
-42.0454044117646));
#146849=CARTESIAN_POINT('Ctrl Pts',(-48.8607426731792,-13.9020798956618,
-43.5395220588235));
#146850=CARTESIAN_POINT('Ctrl Pts',(-50.1489600866593,-9.37446532147148,
-45.0336397058824));
#146851=CARTESIAN_POINT('Ctrl Pts',(-50.5832961557877,-4.68723266073574,
-46.5277573529412));
#146852=CARTESIAN_POINT('Ctrl Pts',(-51.0176322249162,-3.12392900021603E-15,
-48.0218749999999));
#146853=CARTESIAN_POINT('Ctrl Pts',(-50.5832961557877,4.68723266073573,
-49.5159926470588));
#146854=CARTESIAN_POINT('Ctrl Pts',(-50.1489600866593,9.37446532147149,
-51.0101102941176));
#146855=CARTESIAN_POINT('Ctrl Pts',(-48.8607426731792,13.9020798956618,
-52.5042279411765));
#146856=CARTESIAN_POINT('Ctrl Pts',(-47.5725252596992,18.4296944698521,
-53.9983455882354));
#146857=CARTESIAN_POINT('Ctrl Pts',(-45.4742952008371,22.6435084734481,
-55.492463235294));
#146858=CARTESIAN_POINT('Ctrl Pts',(-43.3760651419751,26.8573224770442,
-56.9865808823529));
#146859=CARTESIAN_POINT('Ctrl Pts',(-40.5392751458362,30.6138395280662,
-58.4806985294117));
#146860=CARTESIAN_POINT('Ctrl Pts',(-37.7024851496972,34.3703565790883,
-59.9748161764706));
#146861=CARTESIAN_POINT('Ctrl Pts',(-34.2237386972451,37.5416529948095,
-61.4689338235295));
#146862=CARTESIAN_POINT('Ctrl Pts',(-30.744992244793,40.7129494105307,-62.9630514705881));
#146863=CARTESIAN_POINT('Ctrl Pts',(-26.7427538741697,43.1910304950644,
-64.457169117647));
#146864=CARTESIAN_POINT('Ctrl Pts',(-22.7405155035463,45.6691115795981,
-65.9512867647058));
#146865=CARTESIAN_POINT('Ctrl Pts',(-18.3510766423074,47.3695892537413,
-67.4454044117647));
#146866=CARTESIAN_POINT('Ctrl Pts',(-13.9616377810684,49.0700669278844,
-68.9395220588236));
#146867=CARTESIAN_POINT('Ctrl Pts',(-9.33447550508177,49.9350334639422,
-70.4336397058822));
#146868=CARTESIAN_POINT('Ctrl Pts',(-4.7073132290951,50.8,-71.9277573529411));
#146869=CARTESIAN_POINT('Ctrl Pts',(-6.22120573966855E-15,50.8,-73.421875));
#146870=CARTESIAN_POINT('Ctrl Pts',(4.70731322909511,50.8,-74.9159926470588));
#146871=CARTESIAN_POINT('Ctrl Pts',(9.33447550508176,49.9350334639422,-76.4101102941177));
#146872=CARTESIAN_POINT('Ctrl Pts',(13.9616377810684,49.0700669278844,-77.9042279411764));
#146873=CARTESIAN_POINT('Ctrl Pts',(18.3510766423074,47.3695892537413,-79.3983455882352));
#146874=CARTESIAN_POINT('Ctrl Pts',(22.7405155035463,45.6691115795981,-80.8924632352941));
#146875=CARTESIAN_POINT('Ctrl Pts',(26.7427538741697,43.1910304950644,-82.386580882353));
#146876=CARTESIAN_POINT('Ctrl Pts',(30.744992244793,40.7129494105307,-83.8806985294118));
#146877=CARTESIAN_POINT('Ctrl Pts',(34.2237386972451,37.5416529948095,-85.3748161764705));
#146878=CARTESIAN_POINT('Ctrl Pts',(37.7024851496972,34.3703565790883,-86.8689338235293));
#146879=CARTESIAN_POINT('Ctrl Pts',(40.5392751458362,30.6138395280662,-88.3630514705882));
#146880=CARTESIAN_POINT('Ctrl Pts',(43.3760651419751,26.8573224770442,-89.8571691176471));
#146881=CARTESIAN_POINT('Ctrl Pts',(45.4742952008372,22.6435084734481,-91.3512867647059));
#146882=CARTESIAN_POINT('Ctrl Pts',(47.5725252596992,18.4296944698521,-92.8454044117646));
#146883=CARTESIAN_POINT('Ctrl Pts',(48.8607426731792,13.9020798956618,-94.3395220588235));
#146884=CARTESIAN_POINT('Ctrl Pts',(50.1489600866593,9.37446532147146,-95.8336397058823));
#146885=CARTESIAN_POINT('Ctrl Pts',(50.5832961557877,4.68723266073574,-97.3277573529412));
#146886=CARTESIAN_POINT('Ctrl Pts',(51.0176322249162,9.37178700064808E-15,
-98.8218750000001));
#146887=CARTESIAN_POINT('Ctrl Pts',(50.5832961557877,-4.68723266073572,
-100.315992647059));
#146888=CARTESIAN_POINT('Ctrl Pts',(50.1489600866593,-9.37446532147149,
-101.810110294118));
#146889=CARTESIAN_POINT('Ctrl Pts',(48.8607426731792,-13.9020798956618,
-103.304227941176));
#146890=CARTESIAN_POINT('Ctrl Pts',(47.5725252596992,-18.4296944698521,
-104.798345588235));
#146891=CARTESIAN_POINT('Ctrl Pts',(45.4742952008371,-22.6435084734482,
-106.292463235294));
#146892=CARTESIAN_POINT('Ctrl Pts',(43.3760651419751,-26.8573224770441,
-107.786580882353));
#146893=CARTESIAN_POINT('Ctrl Pts',(40.5392751458362,-30.6138395280662,
-109.280698529412));
#146894=CARTESIAN_POINT('Ctrl Pts',(37.7024851496972,-34.3703565790883,
-110.774816176471));
#146895=CARTESIAN_POINT('Ctrl Pts',(34.2237386972451,-37.5416529948095,
-112.268933823529));
#146896=CARTESIAN_POINT('Ctrl Pts',(30.744992244793,-40.7129494105307,-113.763051470588));
#146897=CARTESIAN_POINT('Ctrl Pts',(26.7427538741697,-43.1910304950644,
-115.257169117647));
#146898=CARTESIAN_POINT('Ctrl Pts',(22.7405155035463,-45.6691115795981,
-116.751286764706));
#146899=CARTESIAN_POINT('Ctrl Pts',(18.3510766423074,-47.3695892537413,
-118.245404411765));
#146900=CARTESIAN_POINT('Ctrl Pts',(13.9616377810684,-49.0700669278844,
-119.739522058824));
#146901=CARTESIAN_POINT('Ctrl Pts',(9.33447550508176,-49.9350334639422,
-121.233639705882));
#146902=CARTESIAN_POINT('Ctrl Pts',(4.70731322909511,-50.8,-122.727757352941));
#146903=CARTESIAN_POINT('Ctrl Pts',(0.,-50.8,-124.221875));
#146904=CARTESIAN_POINT('Ctrl Pts',(-4.70731322909511,-50.8,-125.715992647059));
#146905=CARTESIAN_POINT('Ctrl Pts',(-9.33447550508177,-49.9350334639422,
-127.210110294118));
#146906=CARTESIAN_POINT('Ctrl Pts',(-13.9616377810684,-49.0700669278844,
-128.704227941177));
#146907=CARTESIAN_POINT('Ctrl Pts',(-18.3510766423074,-47.3695892537413,
-130.198345588235));
#146908=CARTESIAN_POINT('Ctrl Pts',(-22.7405155035463,-45.6691115795981,
-131.692463235294));
#146909=CARTESIAN_POINT('Ctrl Pts',(-26.7427538741697,-43.1910304950644,
-133.186580882353));
#146910=CARTESIAN_POINT('Ctrl Pts',(-30.744992244793,-40.7129494105307,
-134.680698529412));
#146911=CARTESIAN_POINT('Ctrl Pts',(-34.2237386972451,-37.5416529948095,
-136.174816176471));
#146912=CARTESIAN_POINT('Ctrl Pts',(-37.7024851496972,-34.3703565790883,
-137.668933823529));
#146913=CARTESIAN_POINT('Ctrl Pts',(-40.5392751458362,-30.6138395280662,
-139.163051470588));
#146914=CARTESIAN_POINT('Ctrl Pts',(-43.3760651419751,-26.8573224770441,
-140.657169117647));
#146915=CARTESIAN_POINT('Ctrl Pts',(-45.4742952008371,-22.6435084734481,
-142.151286764706));
#146916=CARTESIAN_POINT('Ctrl Pts',(-47.5725252596992,-18.4296944698521,
-143.645404411765));
#146917=CARTESIAN_POINT('Ctrl Pts',(-48.8607426731792,-13.9020798956618,
-145.139522058823));
#146918=CARTESIAN_POINT('Ctrl Pts',(-50.1489600866593,-9.37446532147148,
-146.633639705882));
#146919=CARTESIAN_POINT('Ctrl Pts',(-50.5832961557877,-4.68723266073574,
-148.127757352941));
#146920=CARTESIAN_POINT('Ctrl Pts',(-51.0176322249162,-3.12392900021603E-15,
-149.621875));
#146921=CARTESIAN_POINT('Ctrl Pts',(-50.5832961557877,4.68723266073573,
-151.115992647059));
#146922=CARTESIAN_POINT('Ctrl Pts',(-50.1489600866593,9.37446532147149,
-152.610110294118));
#146923=CARTESIAN_POINT('Ctrl Pts',(-48.8607426731792,13.9020798956618,
-154.104227941176));
#146924=CARTESIAN_POINT('Ctrl Pts',(-47.5725252596992,18.4296944698521,
-155.598345588235));
#146925=CARTESIAN_POINT('Ctrl Pts',(-45.4742952008371,22.6435084734481,
-157.092463235294));
#146926=CARTESIAN_POINT('Ctrl Pts',(-43.3760651419751,26.8573224770442,
-158.586580882353));
#146927=CARTESIAN_POINT('Ctrl Pts',(-40.5392751458362,30.6138395280662,
-160.080698529412));
#146928=CARTESIAN_POINT('Ctrl Pts',(-37.7024851496972,34.3703565790883,
-161.574816176471));
#146929=CARTESIAN_POINT('Ctrl Pts',(-34.2237386972451,37.5416529948095,
-163.068933823529));
#146930=CARTESIAN_POINT('Ctrl Pts',(-30.744992244793,40.7129494105307,-164.563051470588));
#146931=CARTESIAN_POINT('Ctrl Pts',(-26.7427538741697,43.1910304950644,
-166.057169117647));
#146932=CARTESIAN_POINT('Ctrl Pts',(-22.7405155035463,45.6691115795981,
-167.551286764706));
#146933=CARTESIAN_POINT('Ctrl Pts',(-18.3510766423074,47.3695892537413,
-169.045404411765));
#146934=CARTESIAN_POINT('Ctrl Pts',(-13.9616377810684,49.0700669278844,
-170.539522058824));
#146935=CARTESIAN_POINT('Ctrl Pts',(-9.33447550508177,49.9350334639422,
-172.033639705882));
#146936=CARTESIAN_POINT('Ctrl Pts',(-4.7073132290951,50.8,-173.527757352941));
#146937=CARTESIAN_POINT('Ctrl Pts',(-6.22120573966855E-15,50.8,-175.021875));
#146938=CARTESIAN_POINT('Ctrl Pts',(4.70731322909511,50.8,-176.515992647059));
#146939=CARTESIAN_POINT('Ctrl Pts',(9.33447550508176,49.9350334639422,-178.010110294118));
#146940=CARTESIAN_POINT('Ctrl Pts',(13.9616377810684,49.0700669278844,-179.504227941177));
#146941=CARTESIAN_POINT('Ctrl Pts',(18.3510766423074,47.3695892537413,-180.998345588235));
#146942=CARTESIAN_POINT('Ctrl Pts',(22.7405155035463,45.6691115795981,-182.492463235294));
#146943=CARTESIAN_POINT('Ctrl Pts',(26.7427538741697,43.1910304950644,-183.986580882353));
#146944=CARTESIAN_POINT('Ctrl Pts',(30.744992244793,40.7129494105307,-185.480698529412));
#146945=CARTESIAN_POINT('Ctrl Pts',(34.2237386972451,37.5416529948095,-186.974816176471));
#146946=CARTESIAN_POINT('Ctrl Pts',(37.7024851496972,34.3703565790883,-188.468933823529));
#146947=CARTESIAN_POINT('Ctrl Pts',(40.5392751458362,30.6138395280662,-189.963051470588));
#146948=CARTESIAN_POINT('Ctrl Pts',(43.3760651419751,26.8573224770442,-191.457169117647));
#146949=CARTESIAN_POINT('Ctrl Pts',(45.4742952008372,22.6435084734481,-192.951286764706));
#146950=CARTESIAN_POINT('Ctrl Pts',(47.5725252596992,18.4296944698521,-194.445404411765));
#146951=CARTESIAN_POINT('Ctrl Pts',(48.8607426731792,13.9020798956618,-195.939522058824));
#146952=CARTESIAN_POINT('Ctrl Pts',(50.1489600866593,9.37446532147146,-197.433639705882));
#146953=CARTESIAN_POINT('Ctrl Pts',(50.5832961557877,4.68723266073574,-198.927757352941));
#146954=CARTESIAN_POINT('Ctrl Pts',(51.0176322249162,9.37178700064808E-15,
-200.421875));
#146955=CARTESIAN_POINT('Ctrl Pts',(50.5832961557877,-4.68723266073572,
-201.915992647059));
#146956=CARTESIAN_POINT('Ctrl Pts',(50.1489600866593,-9.37446532147149,
-203.410110294118));
#146957=CARTESIAN_POINT('Ctrl Pts',(48.8607426731792,-13.9020798956618,
-204.904227941176));
#146958=CARTESIAN_POINT('Ctrl Pts',(47.5725252596992,-18.4296944698521,
-206.398345588235));
#146959=CARTESIAN_POINT('Ctrl Pts',(45.4742952008371,-22.6435084734482,
-207.892463235294));
#146960=CARTESIAN_POINT('Ctrl Pts',(43.3760651419751,-26.8573224770441,
-209.386580882353));
#146961=CARTESIAN_POINT('Ctrl Pts',(40.5392751458362,-30.6138395280662,
-210.880698529412));
#146962=CARTESIAN_POINT('Ctrl Pts',(37.7024851496972,-34.3703565790883,
-212.374816176471));
#146963=CARTESIAN_POINT('Ctrl Pts',(34.2237386972451,-37.5416529948095,
-213.868933823529));
#146964=CARTESIAN_POINT('Ctrl Pts',(30.744992244793,-40.7129494105307,-215.363051470588));
#146965=CARTESIAN_POINT('Ctrl Pts',(26.7427538741697,-43.1910304950644,
-216.857169117647));
#146966=CARTESIAN_POINT('Ctrl Pts',(22.7405155035463,-45.6691115795981,
-218.351286764706));
#146967=CARTESIAN_POINT('Ctrl Pts',(18.3510766423074,-47.3695892537413,
-219.845404411765));
#146968=CARTESIAN_POINT('Ctrl Pts',(13.9616377810684,-49.0700669278844,
-221.339522058823));
#146969=CARTESIAN_POINT('Ctrl Pts',(9.33447550508176,-49.9350334639422,
-222.833639705882));
#146970=CARTESIAN_POINT('Ctrl Pts',(4.70731322909511,-50.8,-224.327757352941));
#146971=CARTESIAN_POINT('Ctrl Pts',(0.,-50.8,-225.821875));
#146972=CARTESIAN_POINT('Ctrl Pts',(-4.70731322909511,-50.8,-227.315992647059));
#146973=CARTESIAN_POINT('Ctrl Pts',(-9.33447550508177,-49.9350334639422,
-228.810110294118));
#146974=CARTESIAN_POINT('Ctrl Pts',(-13.9616377810684,-49.0700669278844,
-230.304227941176));
#146975=CARTESIAN_POINT('Ctrl Pts',(-18.3510766423074,-47.3695892537413,
-231.798345588235));
#146976=CARTESIAN_POINT('Ctrl Pts',(-22.7405155035463,-45.6691115795981,
-233.292463235294));
#146977=CARTESIAN_POINT('Ctrl Pts',(-26.7427538741697,-43.1910304950644,
-234.786580882353));
#146978=CARTESIAN_POINT('Ctrl Pts',(-30.744992244793,-40.7129494105307,
-236.280698529412));
#146979=CARTESIAN_POINT('Ctrl Pts',(-34.2237386972451,-37.5416529948095,
-237.774816176471));
#146980=CARTESIAN_POINT('Ctrl Pts',(-37.7024851496972,-34.3703565790883,
-239.268933823529));
#146981=CARTESIAN_POINT('Ctrl Pts',(-40.5392751458362,-30.6138395280662,
-240.763051470588));
#146982=CARTESIAN_POINT('Ctrl Pts',(-43.3760651419751,-26.8573224770441,
-242.257169117647));
#146983=CARTESIAN_POINT('Ctrl Pts',(-45.4742952008371,-22.6435084734481,
-243.751286764706));
#146984=CARTESIAN_POINT('Ctrl Pts',(-47.5725252596992,-18.4296944698521,
-245.245404411765));
#146985=CARTESIAN_POINT('Ctrl Pts',(-48.8607426731792,-13.9020798956618,
-246.739522058824));
#146986=CARTESIAN_POINT('Ctrl Pts',(-50.1489600866593,-9.37446532147148,
-248.233639705882));
#146987=CARTESIAN_POINT('Ctrl Pts',(-50.5832961557877,-4.68723266073574,
-249.727757352941));
#146988=CARTESIAN_POINT('Ctrl Pts',(-51.0176322249162,-3.12392900021603E-15,
-251.221875));
#146989=CARTESIAN_POINT('Ctrl Pts',(-50.5832961557877,4.68723266073573,
-252.715992647059));
#146990=CARTESIAN_POINT('Ctrl Pts',(-50.1489600866593,9.37446532147149,
-254.210110294118));
#146991=CARTESIAN_POINT('Ctrl Pts',(-48.8607426731792,13.9020798956618,
-255.704227941177));
#146992=CARTESIAN_POINT('Ctrl Pts',(-47.5725252596992,18.4296944698521,
-257.198345588235));
#146993=CARTESIAN_POINT('Ctrl Pts',(-45.4742952008371,22.6435084734481,
-258.692463235294));
#146994=CARTESIAN_POINT('Ctrl Pts',(-43.3760651419751,26.8573224770442,
-260.186580882353));
#146995=CARTESIAN_POINT('Ctrl Pts',(-40.5392751458362,30.6138395280662,
-261.680698529412));
#146996=CARTESIAN_POINT('Ctrl Pts',(-37.7024851496972,34.3703565790883,
-263.174816176471));
#146997=CARTESIAN_POINT('Ctrl Pts',(-34.2237386972451,37.5416529948095,
-264.668933823529));
#146998=CARTESIAN_POINT('Ctrl Pts',(-30.744992244793,40.7129494105307,-266.163051470588));
#146999=CARTESIAN_POINT('Ctrl Pts',(-26.7427538741697,43.1910304950644,
-267.657169117647));
#147000=CARTESIAN_POINT('Ctrl Pts',(-22.7405155035463,45.6691115795981,
-269.151286764706));
#147001=CARTESIAN_POINT('Ctrl Pts',(-18.3510766423074,47.3695892537413,
-270.645404411765));
#147002=CARTESIAN_POINT('Ctrl Pts',(-13.9616377810684,49.0700669278844,
-272.139522058824));
#147003=CARTESIAN_POINT('Ctrl Pts',(-9.33447550508177,49.9350334639422,
-273.633639705882));
#147004=CARTESIAN_POINT('Ctrl Pts',(-4.7073132290951,50.8,-275.127757352941));
#147005=CARTESIAN_POINT('Ctrl Pts',(-6.22120573966855E-15,50.8,-276.621875));
#147006=CARTESIAN_POINT('Ctrl Pts',(4.70731322909511,50.8,-278.115992647059));
#147007=CARTESIAN_POINT('Ctrl Pts',(9.33447550508176,49.9350334639422,-279.610110294118));
#147008=CARTESIAN_POINT('Ctrl Pts',(13.9616377810684,49.0700669278844,-281.104227941176));
#147009=CARTESIAN_POINT('Ctrl Pts',(18.3510766423074,47.3695892537413,-282.598345588235));
#147010=CARTESIAN_POINT('Ctrl Pts',(22.7405155035463,45.6691115795981,-284.092463235294));
#147011=CARTESIAN_POINT('Ctrl Pts',(26.7427538741697,43.1910304950644,-285.586580882353));
#147012=CARTESIAN_POINT('Ctrl Pts',(30.744992244793,40.7129494105307,-287.080698529412));
#147013=CARTESIAN_POINT('Ctrl Pts',(34.2237386972451,37.5416529948095,-288.574816176471));
#147014=CARTESIAN_POINT('Ctrl Pts',(37.7024851496972,34.3703565790883,-290.068933823529));
#147015=CARTESIAN_POINT('Ctrl Pts',(40.5392751458362,30.6138395280662,-291.563051470588));
#147016=CARTESIAN_POINT('Ctrl Pts',(43.3760651419751,26.8573224770442,-293.057169117647));
#147017=CARTESIAN_POINT('Ctrl Pts',(45.4742952008372,22.6435084734481,-294.551286764706));
#147018=CARTESIAN_POINT('Ctrl Pts',(47.5725252596992,18.4296944698521,-296.045404411765));
#147019=CARTESIAN_POINT('Ctrl Pts',(48.8607426731792,13.9020798956618,-297.539522058823));
#147020=CARTESIAN_POINT('Ctrl Pts',(50.1489600866593,9.37446532147146,-299.033639705882));
#147021=CARTESIAN_POINT('Ctrl Pts',(50.5832961557877,4.68723266073574,-300.527757352941));
#147022=CARTESIAN_POINT('Ctrl Pts',(51.0176322249162,9.37178700064808E-15,
-302.021875));
#147023=CARTESIAN_POINT('Ctrl Pts',(50.5832961557877,-4.68723266073572,
-303.515992647059));
#147024=CARTESIAN_POINT('Ctrl Pts',(50.1489600866593,-9.37446532147149,
-305.010110294118));
#147025=CARTESIAN_POINT('Ctrl Pts',(48.8607426731792,-13.9020798956618,
-306.504227941177));
#147026=CARTESIAN_POINT('Ctrl Pts',(47.5725252596992,-18.4296944698521,
-307.998345588235));
#147027=CARTESIAN_POINT('Ctrl Pts',(45.4742952008371,-22.6435084734482,
-309.492463235294));
#147028=CARTESIAN_POINT('Ctrl Pts',(43.3760651419751,-26.8573224770441,
-310.986580882353));
#147029=CARTESIAN_POINT('Ctrl Pts',(40.5392751458362,-30.6138395280662,
-312.480698529412));
#147030=CARTESIAN_POINT('Ctrl Pts',(37.7024851496972,-34.3703565790883,
-313.974816176471));
#147031=CARTESIAN_POINT('Ctrl Pts',(34.2237386972451,-37.5416529948095,
-315.468933823529));
#147032=CARTESIAN_POINT('Ctrl Pts',(30.744992244793,-40.7129494105307,-316.963051470588));
#147033=CARTESIAN_POINT('Ctrl Pts',(26.7427538741697,-43.1910304950644,
-318.457169117647));
#147034=CARTESIAN_POINT('Ctrl Pts',(22.7405155035463,-45.6691115795981,
-319.951286764706));
#147035=CARTESIAN_POINT('Ctrl Pts',(18.3510766423074,-47.3695892537413,
-321.445404411765));
#147036=CARTESIAN_POINT('Ctrl Pts',(13.9616377810684,-49.0700669278844,
-322.939522058824));
#147037=CARTESIAN_POINT('Ctrl Pts',(9.33447550508176,-49.9350334639422,
-324.433639705882));
#147038=CARTESIAN_POINT('Ctrl Pts',(4.70731322909511,-50.8,-325.927757352941));
#147039=CARTESIAN_POINT('Ctrl Pts',(0.,-50.8,-327.421875));
#147040=CARTESIAN_POINT('Ctrl Pts',(-4.70731322909511,-50.8,-328.915992647059));
#147041=CARTESIAN_POINT('Ctrl Pts',(-9.33447550508177,-49.9350334639422,
-330.410110294118));
#147042=CARTESIAN_POINT('Ctrl Pts',(-13.9616377810684,-49.0700669278844,
-331.904227941176));
#147043=CARTESIAN_POINT('Ctrl Pts',(-18.3510766423074,-47.3695892537413,
-333.398345588235));
#147044=CARTESIAN_POINT('Ctrl Pts',(-22.7405155035463,-45.6691115795981,
-334.892463235294));
#147045=CARTESIAN_POINT('Ctrl Pts',(-26.7427538741697,-43.1910304950644,
-336.386580882353));
#147046=CARTESIAN_POINT('Ctrl Pts',(-30.744992244793,-40.7129494105307,
-337.880698529412));
#147047=CARTESIAN_POINT('Ctrl Pts',(-34.2237386972451,-37.5416529948095,
-339.37481617647));
#147048=CARTESIAN_POINT('Ctrl Pts',(-37.7024851496972,-34.3703565790883,
-340.868933823529));
#147049=CARTESIAN_POINT('Ctrl Pts',(-40.5392751458362,-30.6138395280662,
-342.363051470588));
#147050=CARTESIAN_POINT('Ctrl Pts',(-43.3760651419751,-26.8573224770441,
-343.857169117647));
#147051=CARTESIAN_POINT('Ctrl Pts',(-45.4742952008371,-22.6435084734481,
-345.351286764706));
#147052=CARTESIAN_POINT('Ctrl Pts',(-47.5725252596992,-18.4296944698521,
-346.845404411765));
#147053=CARTESIAN_POINT('Ctrl Pts',(-48.8607426731792,-13.9020798956618,
-348.339522058823));
#147054=CARTESIAN_POINT('Ctrl Pts',(-50.1489600866593,-9.37446532147148,
-349.833639705882));
#147055=CARTESIAN_POINT('Ctrl Pts',(-50.5832961557877,-4.68723266073574,
-351.327757352941));
#147056=CARTESIAN_POINT('Ctrl Pts',(-51.0176322249162,-3.12392900021603E-15,
-352.821875));
#147057=CARTESIAN_POINT('Ctrl Pts',(-50.5832961557877,4.68723266073573,
-354.315992647059));
#147058=CARTESIAN_POINT('Ctrl Pts',(-50.1489600866593,9.37446532147149,
-355.810110294118));
#147059=CARTESIAN_POINT('Ctrl Pts',(-48.8607426731792,13.9020798956618,
-357.304227941177));
#147060=CARTESIAN_POINT('Ctrl Pts',(-47.5725252596992,18.4296944698521,
-358.798345588235));
#147061=CARTESIAN_POINT('Ctrl Pts',(-45.4742952008371,22.6435084734481,
-360.292463235294));
#147062=CARTESIAN_POINT('Ctrl Pts',(-43.3760651419751,26.8573224770442,
-361.786580882353));
#147063=CARTESIAN_POINT('Ctrl Pts',(-40.5392751458362,30.6138395280662,
-363.280698529412));
#147064=CARTESIAN_POINT('Ctrl Pts',(-37.7024851496972,34.3703565790883,
-364.774816176471));
#147065=CARTESIAN_POINT('Ctrl Pts',(-34.2237386972451,37.5416529948095,
-366.268933823529));
#147066=CARTESIAN_POINT('Ctrl Pts',(-30.744992244793,40.7129494105307,-367.763051470588));
#147067=CARTESIAN_POINT('Ctrl Pts',(-26.7427538741697,43.1910304950644,
-369.257169117647));
#147068=CARTESIAN_POINT('Ctrl Pts',(-22.7405155035463,45.6691115795981,
-370.751286764706));
#147069=CARTESIAN_POINT('Ctrl Pts',(-18.3510766423074,47.3695892537413,
-372.245404411765));
#147070=CARTESIAN_POINT('Ctrl Pts',(-13.9616377810684,49.0700669278844,
-373.739522058824));
#147071=CARTESIAN_POINT('Ctrl Pts',(-9.33447550508177,49.9350334639422,
-375.233639705882));
#147072=CARTESIAN_POINT('Ctrl Pts',(-4.7073132290951,50.8,-376.727757352941));
#147073=CARTESIAN_POINT('Ctrl Pts',(-6.22120573966855E-15,50.8,-378.221875));
#147074=CARTESIAN_POINT('Ctrl Pts',(4.70731322909511,50.8,-379.715992647059));
#147075=CARTESIAN_POINT('Ctrl Pts',(9.33447550508176,49.9350334639422,-381.210110294118));
#147076=CARTESIAN_POINT('Ctrl Pts',(13.9616377810684,49.0700669278844,-382.704227941177));
#147077=CARTESIAN_POINT('Ctrl Pts',(18.3510766423074,47.3695892537413,-384.198345588235));
#147078=CARTESIAN_POINT('Ctrl Pts',(22.7405155035463,45.6691115795981,-385.692463235294));
#147079=CARTESIAN_POINT('Ctrl Pts',(26.7427538741697,43.1910304950644,-387.186580882353));
#147080=CARTESIAN_POINT('Ctrl Pts',(30.744992244793,40.7129494105307,-388.680698529412));
#147081=CARTESIAN_POINT('Ctrl Pts',(34.2237386972451,37.5416529948095,-390.174816176471));
#147082=CARTESIAN_POINT('Ctrl Pts',(37.7024851496972,34.3703565790883,-391.668933823529));
#147083=CARTESIAN_POINT('Ctrl Pts',(40.5392751458362,30.6138395280662,-393.163051470588));
#147084=CARTESIAN_POINT('Ctrl Pts',(43.3760651419751,26.8573224770442,-394.657169117647));
#147085=CARTESIAN_POINT('Ctrl Pts',(45.4742952008372,22.6435084734481,-396.151286764706));
#147086=CARTESIAN_POINT('Ctrl Pts',(47.5725252596992,18.4296944698521,-397.645404411765));
#147087=CARTESIAN_POINT('Ctrl Pts',(48.8607426731792,13.9020798956618,-399.139522058823));
#147088=CARTESIAN_POINT('Ctrl Pts',(50.1489600866593,9.37446532147146,-400.633639705882));
#147089=CARTESIAN_POINT('Ctrl Pts',(50.5832961557877,4.68723266073574,-402.127757352941));
#147090=CARTESIAN_POINT('Ctrl Pts',(51.0176322249162,9.37178700064808E-15,
-403.621875));
#147091=CARTESIAN_POINT('Ctrl Pts',(50.5832961557877,-4.68723266073572,
-405.115992647059));
#147092=CARTESIAN_POINT('Ctrl Pts',(50.1489600866593,-9.37446532147149,
-406.610110294118));
#147093=CARTESIAN_POINT('Ctrl Pts',(48.8607426731792,-13.9020798956618,
-408.104227941176));
#147094=CARTESIAN_POINT('Ctrl Pts',(47.5725252596992,-18.4296944698521,
-409.598345588235));
#147095=CARTESIAN_POINT('Ctrl Pts',(45.4742952008371,-22.6435084734482,
-411.092463235294));
#147096=CARTESIAN_POINT('Ctrl Pts',(43.3760651419751,-26.8573224770441,
-412.586580882353));
#147097=CARTESIAN_POINT('Ctrl Pts',(40.5392751458362,-30.6138395280662,
-414.080698529412));
#147098=CARTESIAN_POINT('Ctrl Pts',(37.7024851496972,-34.3703565790883,
-415.574816176471));
#147099=CARTESIAN_POINT('Ctrl Pts',(34.2237386972451,-37.5416529948095,
-417.068933823529));
#147100=CARTESIAN_POINT('Ctrl Pts',(30.744992244793,-40.7129494105307,-418.563051470588));
#147101=CARTESIAN_POINT('Ctrl Pts',(26.7427538741697,-43.1910304950644,
-420.057169117647));
#147102=CARTESIAN_POINT('Ctrl Pts',(22.7405155035463,-45.6691115795981,
-421.551286764706));
#147103=CARTESIAN_POINT('Ctrl Pts',(18.3510766423074,-47.3695892537413,
-423.045404411765));
#147104=CARTESIAN_POINT('Ctrl Pts',(13.9616377810684,-49.0700669278844,
-424.539522058824));
#147105=CARTESIAN_POINT('Ctrl Pts',(9.33447550508176,-49.9350334639422,
-426.033639705882));
#147106=CARTESIAN_POINT('Ctrl Pts',(4.70731322909511,-50.8,-427.527757352941));
#147107=CARTESIAN_POINT('Ctrl Pts',(0.,-50.8,-429.021875));
#147108=CARTESIAN_POINT('Ctrl Pts',(-4.70731322909511,-50.8,-430.515992647059));
#147109=CARTESIAN_POINT('Ctrl Pts',(-9.33447550508177,-49.9350334639422,
-432.010110294118));
#147110=CARTESIAN_POINT('Ctrl Pts',(-13.9616377810684,-49.0700669278844,
-433.504227941177));
#147111=CARTESIAN_POINT('Ctrl Pts',(-18.3510766423074,-47.3695892537413,
-434.998345588235));
#147112=CARTESIAN_POINT('Ctrl Pts',(-22.7405155035463,-45.6691115795981,
-436.492463235294));
#147113=CARTESIAN_POINT('Ctrl Pts',(-26.7427538741697,-43.1910304950644,
-437.986580882353));
#147114=CARTESIAN_POINT('Ctrl Pts',(-30.744992244793,-40.7129494105307,
-439.480698529412));
#147115=CARTESIAN_POINT('Ctrl Pts',(-34.2237386972451,-37.5416529948095,
-440.974816176471));
#147116=CARTESIAN_POINT('Ctrl Pts',(-37.7024851496972,-34.3703565790883,
-442.46893382353));
#147117=CARTESIAN_POINT('Ctrl Pts',(-40.5392751458362,-30.6138395280662,
-443.963051470588));
#147118=CARTESIAN_POINT('Ctrl Pts',(-43.3760651419751,-26.8573224770441,
-445.457169117647));
#147119=CARTESIAN_POINT('Ctrl Pts',(-45.4742952008371,-22.6435084734481,
-446.951286764706));
#147120=CARTESIAN_POINT('Ctrl Pts',(-47.5725252596992,-18.4296944698521,
-448.445404411765));
#147121=CARTESIAN_POINT('Ctrl Pts',(-48.8607426731792,-13.9020798956618,
-449.939522058824));
#147122=CARTESIAN_POINT('Ctrl Pts',(-50.1489600866593,-9.37446532147148,
-451.433639705882));
#147123=CARTESIAN_POINT('Ctrl Pts',(-50.5832961557877,-4.68723266073574,
-452.927757352941));
#147124=CARTESIAN_POINT('Ctrl Pts',(-51.0176322249162,-3.12392900021603E-15,
-454.421875));
#147125=CARTESIAN_POINT('Ctrl Pts',(-50.5832961557877,4.68723266073573,
-455.915992647059));
#147126=CARTESIAN_POINT('Ctrl Pts',(-50.1489600866593,9.37446532147149,
-457.410110294118));
#147127=CARTESIAN_POINT('Ctrl Pts',(-48.8607426731792,13.9020798956618,
-458.904227941176));
#147128=CARTESIAN_POINT('Ctrl Pts',(-47.5725252596992,18.4296944698521,
-460.398345588235));
#147129=CARTESIAN_POINT('Ctrl Pts',(-45.4742952008371,22.6435084734481,
-461.892463235294));
#147130=CARTESIAN_POINT('Ctrl Pts',(-43.3760651419751,26.8573224770442,
-463.386580882353));
#147131=CARTESIAN_POINT('Ctrl Pts',(-40.5392751458362,30.6138395280662,
-464.880698529412));
#147132=CARTESIAN_POINT('Ctrl Pts',(-37.7024851496972,34.3703565790883,
-466.374816176471));
#147133=CARTESIAN_POINT('Ctrl Pts',(-34.2237386972451,37.5416529948095,
-467.868933823529));
#147134=CARTESIAN_POINT('Ctrl Pts',(-30.744992244793,40.7129494105307,-469.363051470588));
#147135=CARTESIAN_POINT('Ctrl Pts',(-26.7427538741697,43.1910304950644,
-470.857169117647));
#147136=CARTESIAN_POINT('Ctrl Pts',(-22.7405155035463,45.6691115795981,
-472.351286764706));
#147137=CARTESIAN_POINT('Ctrl Pts',(-18.3510766423074,47.3695892537413,
-473.845404411765));
#147138=CARTESIAN_POINT('Ctrl Pts',(-13.9616377810684,49.0700669278844,
-475.339522058823));
#147139=CARTESIAN_POINT('Ctrl Pts',(-9.33447550508177,49.9350334639422,
-476.833639705882));
#147140=CARTESIAN_POINT('Ctrl Pts',(-4.7073132290951,50.8,-478.327757352941));
#147141=CARTESIAN_POINT('Ctrl Pts',(-6.22120573966855E-15,50.8,-479.821875));
#147142=CARTESIAN_POINT('Ctrl Pts',(4.70731322909511,50.8,-481.315992647059));
#147143=CARTESIAN_POINT('Ctrl Pts',(9.33447550508176,49.9350334639422,-482.810110294118));
#147144=CARTESIAN_POINT('Ctrl Pts',(13.9616377810684,49.0700669278844,-484.304227941176));
#147145=CARTESIAN_POINT('Ctrl Pts',(18.3510766423074,47.3695892537413,-485.798345588235));
#147146=CARTESIAN_POINT('Ctrl Pts',(22.7405155035463,45.6691115795981,-487.292463235294));
#147147=CARTESIAN_POINT('Ctrl Pts',(26.7427538741697,43.1910304950644,-488.786580882353));
#147148=CARTESIAN_POINT('Ctrl Pts',(30.744992244793,40.7129494105307,-490.280698529412));
#147149=CARTESIAN_POINT('Ctrl Pts',(34.2237386972451,37.5416529948095,-491.774816176471));
#147150=CARTESIAN_POINT('Ctrl Pts',(37.7024851496972,34.3703565790883,-493.268933823529));
#147151=CARTESIAN_POINT('Ctrl Pts',(40.5392751458362,30.6138395280662,-494.763051470588));
#147152=CARTESIAN_POINT('Ctrl Pts',(43.3760651419751,26.8573224770442,-496.257169117647));
#147153=CARTESIAN_POINT('Ctrl Pts',(45.4742952008372,22.6435084734481,-497.751286764706));
#147154=CARTESIAN_POINT('Ctrl Pts',(47.5725252596992,18.4296944698521,-499.245404411765));
#147155=CARTESIAN_POINT('Ctrl Pts',(48.8607426731792,13.9020798956618,-500.739522058824));
#147156=CARTESIAN_POINT('Ctrl Pts',(50.1489600866593,9.37446532147146,-502.233639705883));
#147157=CARTESIAN_POINT('Ctrl Pts',(50.5832961557877,4.68723266073574,-503.727757352941));
#147158=CARTESIAN_POINT('Ctrl Pts',(51.0176322249162,9.37178700064808E-15,
-505.221875));
#147159=CARTESIAN_POINT('Ctrl Pts',(50.5832961557877,-4.68723266073572,
-506.715992647059));
#147160=CARTESIAN_POINT('Ctrl Pts',(50.1489600866593,-9.37446532147149,
-508.210110294117));
#147161=CARTESIAN_POINT('Ctrl Pts',(48.8607426731792,-13.9020798956618,
-509.704227941176));
#147162=CARTESIAN_POINT('Ctrl Pts',(47.5725252596992,-18.4296944698521,
-511.198345588235));
#147163=CARTESIAN_POINT('Ctrl Pts',(45.4742952008371,-22.6435084734482,
-512.692463235294));
#147164=CARTESIAN_POINT('Ctrl Pts',(43.3760651419751,-26.8573224770441,
-514.186580882353));
#147165=CARTESIAN_POINT('Ctrl Pts',(40.5392751458362,-30.6138395280662,
-515.680698529412));
#147166=CARTESIAN_POINT('Ctrl Pts',(37.7024851496972,-34.3703565790883,
-517.174816176471));
#147167=CARTESIAN_POINT('Ctrl Pts',(34.2237386972451,-37.5416529948095,
-518.66893382353));
#147168=CARTESIAN_POINT('Ctrl Pts',(30.744992244793,-40.7129494105307,-520.163051470588));
#147169=CARTESIAN_POINT('Ctrl Pts',(26.7427538741697,-43.1910304950644,
-521.657169117647));
#147170=CARTESIAN_POINT('Ctrl Pts',(22.7405155035463,-45.6691115795981,
-523.151286764706));
#147171=CARTESIAN_POINT('Ctrl Pts',(18.3510766423074,-47.3695892537413,
-524.645404411765));
#147172=CARTESIAN_POINT('Ctrl Pts',(13.9616377810684,-49.0700669278844,
-526.139522058823));
#147173=CARTESIAN_POINT('Ctrl Pts',(9.33447550508176,-49.9350334639422,
-527.633639705882));
#147174=CARTESIAN_POINT('Ctrl Pts',(4.70731322909511,-50.8,-529.127757352941));
#147175=CARTESIAN_POINT('Ctrl Pts',(0.,-50.8,-530.621875));
#147176=CARTESIAN_POINT('Ctrl Pts',(-4.70731322909511,-50.8,-532.115992647059));
#147177=CARTESIAN_POINT('Ctrl Pts',(-9.33447550508177,-49.9350334639422,
-533.610110294118));
#147178=CARTESIAN_POINT('Ctrl Pts',(-13.9616377810684,-49.0700669278844,
-535.104227941177));
#147179=CARTESIAN_POINT('Ctrl Pts',(-18.3510766423074,-47.3695892537413,
-536.598345588235));
#147180=CARTESIAN_POINT('Ctrl Pts',(-22.7405155035463,-45.6691115795981,
-538.092463235294));
#147181=CARTESIAN_POINT('Ctrl Pts',(-26.7427538741697,-43.1910304950644,
-539.586580882353));
#147182=CARTESIAN_POINT('Ctrl Pts',(-30.744992244793,-40.7129494105307,
-541.080698529412));
#147183=CARTESIAN_POINT('Ctrl Pts',(-34.2237386972451,-37.5416529948095,
-542.574816176471));
#147184=CARTESIAN_POINT('Ctrl Pts',(-37.7024851496972,-34.3703565790883,
-544.068933823529));
#147185=CARTESIAN_POINT('Ctrl Pts',(-40.5392751458362,-30.6138395280662,
-545.563051470588));
#147186=CARTESIAN_POINT('Ctrl Pts',(-43.3760651419751,-26.8573224770441,
-547.057169117647));
#147187=CARTESIAN_POINT('Ctrl Pts',(-45.4742952008371,-22.6435084734481,
-548.551286764706));
#147188=CARTESIAN_POINT('Ctrl Pts',(-47.5725252596992,-18.4296944698521,
-550.045404411765));
#147189=CARTESIAN_POINT('Ctrl Pts',(-48.8607426731792,-13.9020798956618,
-551.539522058823));
#147190=CARTESIAN_POINT('Ctrl Pts',(-50.1489600866593,-9.37446532147148,
-553.033639705882));
#147191=CARTESIAN_POINT('Ctrl Pts',(-50.5832961557877,-4.68723266073574,
-554.527757352941));
#147192=CARTESIAN_POINT('Ctrl Pts',(-51.0176322249162,-3.12392900021603E-15,
-556.021875));
#147193=CARTESIAN_POINT('Ctrl Pts',(-50.5832961557877,4.68723266073573,
-557.515992647059));
#147194=CARTESIAN_POINT('Ctrl Pts',(-50.1489600866593,9.37446532147149,
-559.010110294118));
#147195=CARTESIAN_POINT('Ctrl Pts',(-48.8607426731792,13.9020798956618,
-560.504227941177));
#147196=CARTESIAN_POINT('Ctrl Pts',(-47.5725252596992,18.4296944698521,
-561.998345588236));
#147197=CARTESIAN_POINT('Ctrl Pts',(-45.4742952008371,22.6435084734481,
-563.492463235294));
#147198=CARTESIAN_POINT('Ctrl Pts',(-43.3760651419751,26.8573224770442,
-564.986580882353));
#147199=CARTESIAN_POINT('Ctrl Pts',(-40.5392751458362,30.6138395280662,
-566.480698529411));
#147200=CARTESIAN_POINT('Ctrl Pts',(-37.7024851496972,34.3703565790883,
-567.974816176471));
#147201=CARTESIAN_POINT('Ctrl Pts',(-34.2237386972451,37.5416529948095,
-569.468933823529));
#147202=CARTESIAN_POINT('Ctrl Pts',(-30.744992244793,40.7129494105307,-570.963051470588));
#147203=CARTESIAN_POINT('Ctrl Pts',(-26.7427538741697,43.1910304950644,
-572.457169117647));
#147204=CARTESIAN_POINT('Ctrl Pts',(-22.7405155035463,45.6691115795981,
-573.951286764706));
#147205=CARTESIAN_POINT('Ctrl Pts',(-18.3510766423074,47.3695892537413,
-575.445404411765));
#147206=CARTESIAN_POINT('Ctrl Pts',(-13.9616377810684,49.0700669278844,
-576.939522058824));
#147207=CARTESIAN_POINT('Ctrl Pts',(-9.33447550508177,49.9350334639422,
-578.433639705882));
#147208=CARTESIAN_POINT('Ctrl Pts',(-4.7073132290951,50.8,-579.927757352941));
#147209=CARTESIAN_POINT('Ctrl Pts',(-6.22120573966855E-15,50.8,-581.421875));
#147210=CARTESIAN_POINT('Ctrl Pts',(4.70731322909511,50.8,-582.915992647059));
#147211=CARTESIAN_POINT('Ctrl Pts',(9.33447550508176,49.9350334639422,-584.410110294118));
#147212=CARTESIAN_POINT('Ctrl Pts',(13.9616377810684,49.0700669278844,-585.904227941176));
#147213=CARTESIAN_POINT('Ctrl Pts',(18.3510766423074,47.3695892537413,-587.398345588235));
#147214=CARTESIAN_POINT('Ctrl Pts',(22.7405155035463,45.6691115795981,-588.892463235294));
#147215=CARTESIAN_POINT('Ctrl Pts',(26.7427538741697,43.1910304950644,-590.386580882353));
#147216=CARTESIAN_POINT('Ctrl Pts',(30.744992244793,40.7129494105307,-591.880698529412));
#147217=CARTESIAN_POINT('Ctrl Pts',(34.2237386972451,37.5416529948095,-593.374816176471));
#147218=CARTESIAN_POINT('Ctrl Pts',(37.7024851496972,34.3703565790883,-594.86893382353));
#147219=CARTESIAN_POINT('Ctrl Pts',(40.5392751458362,30.6138395280662,-596.363051470588));
#147220=CARTESIAN_POINT('Ctrl Pts',(43.3760651419751,26.8573224770442,-597.857169117647));
#147221=CARTESIAN_POINT('Ctrl Pts',(45.4742952008372,22.6435084734481,-599.351286764706));
#147222=CARTESIAN_POINT('Ctrl Pts',(47.5725252596992,18.4296944698521,-600.845404411765));
#147223=CARTESIAN_POINT('Ctrl Pts',(48.8607426731792,13.9020798956618,-602.339522058823));
#147224=CARTESIAN_POINT('Ctrl Pts',(50.1489600866593,9.37446532147146,-603.833639705882));
#147225=CARTESIAN_POINT('Ctrl Pts',(50.5832961557877,4.68723266073574,-605.327757352941));
#147226=CARTESIAN_POINT('Ctrl Pts',(51.0176322249162,9.37178700064808E-15,
-606.821875));
#147227=CARTESIAN_POINT('Ctrl Pts',(50.5832961557877,-4.68723266073572,
-608.315992647059));
#147228=CARTESIAN_POINT('Ctrl Pts',(50.1489600866593,-9.37446532147149,
-609.810110294118));
#147229=CARTESIAN_POINT('Ctrl Pts',(48.8607426731792,-13.9020798956618,
-611.304227941176));
#147230=CARTESIAN_POINT('Ctrl Pts',(47.5725252596992,-18.4296944698521,
-612.798345588235));
#147231=CARTESIAN_POINT('Ctrl Pts',(45.4742952008371,-22.6435084734482,
-614.292463235294));
#147232=CARTESIAN_POINT('Ctrl Pts',(43.3760651419751,-26.8573224770441,
-615.786580882353));
#147233=CARTESIAN_POINT('Ctrl Pts',(40.5392751458362,-30.6138395280662,
-617.280698529412));
#147234=CARTESIAN_POINT('Ctrl Pts',(37.7024851496972,-34.3703565790883,
-618.774816176471));
#147235=CARTESIAN_POINT('Ctrl Pts',(34.2237386972451,-37.5416529948095,
-620.268933823529));
#147236=CARTESIAN_POINT('Ctrl Pts',(30.744992244793,-40.7129494105307,-621.763051470588));
#147237=CARTESIAN_POINT('Ctrl Pts',(26.7427538741697,-43.1910304950644,
-623.257169117647));
#147238=CARTESIAN_POINT('Ctrl Pts',(22.7405155035463,-45.6691115795981,
-624.751286764706));
#147239=CARTESIAN_POINT('Ctrl Pts',(18.3510766423074,-47.3695892537413,
-626.245404411764));
#147240=CARTESIAN_POINT('Ctrl Pts',(13.9616377810684,-49.0700669278844,
-627.739522058823));
#147241=CARTESIAN_POINT('Ctrl Pts',(9.33447550508176,-49.9350334639422,
-629.233639705882));
#147242=CARTESIAN_POINT('Ctrl Pts',(4.70731322909511,-50.8,-630.727757352941));
#147243=CARTESIAN_POINT('Ctrl Pts',(0.,-50.8,-632.221875));
#147244=CARTESIAN_POINT('Ctrl Pts',(-4.70731322909511,-50.8,-633.715992647059));
#147245=CARTESIAN_POINT('Ctrl Pts',(-9.33447550508177,-49.9350334639422,
-635.210110294118));
#147246=CARTESIAN_POINT('Ctrl Pts',(-13.9616377810684,-49.0700669278844,
-636.704227941177));
#147247=CARTESIAN_POINT('Ctrl Pts',(-18.3510766423074,-47.3695892537413,
-638.198345588235));
#147248=CARTESIAN_POINT('Ctrl Pts',(-22.7405155035463,-45.6691115795981,
-639.692463235294));
#147249=CARTESIAN_POINT('Ctrl Pts',(-26.7427538741697,-43.1910304950644,
-641.186580882353));
#147250=CARTESIAN_POINT('Ctrl Pts',(-30.744992244793,-40.7129494105307,
-642.680698529412));
#147251=CARTESIAN_POINT('Ctrl Pts',(-34.2237386972451,-37.5416529948095,
-644.174816176471));
#147252=CARTESIAN_POINT('Ctrl Pts',(-37.7024851496972,-34.3703565790883,
-645.668933823529));
#147253=CARTESIAN_POINT('Ctrl Pts',(-40.5392751458362,-30.6138395280662,
-647.163051470588));
#147254=CARTESIAN_POINT('Ctrl Pts',(-43.3760651419751,-26.8573224770441,
-648.657169117647));
#147255=CARTESIAN_POINT('Ctrl Pts',(-45.4742952008371,-22.6435084734481,
-650.151286764706));
#147256=CARTESIAN_POINT('Ctrl Pts',(-47.5725252596992,-18.4296944698521,
-651.645404411765));
#147257=CARTESIAN_POINT('Ctrl Pts',(-48.8607426731792,-13.9020798956618,
-653.139522058824));
#147258=CARTESIAN_POINT('Ctrl Pts',(-50.1489600866593,-9.37446532147148,
-654.633639705883));
#147259=CARTESIAN_POINT('Ctrl Pts',(-50.5832961557877,-4.68723266073574,
-656.127757352941));
#147260=CARTESIAN_POINT('Ctrl Pts',(-51.0176322249162,-3.12392900021603E-15,
-657.621875));
#147261=CARTESIAN_POINT('Ctrl Pts',(-50.5832961557877,4.68723266073573,
-659.115992647059));
#147262=CARTESIAN_POINT('Ctrl Pts',(-50.1489600866593,9.37446532147149,
-660.610110294118));
#147263=CARTESIAN_POINT('Ctrl Pts',(-48.8607426731792,13.9020798956618,
-662.104227941177));
#147264=CARTESIAN_POINT('Ctrl Pts',(-47.5725252596992,18.4296944698521,
-663.598345588235));
#147265=CARTESIAN_POINT('Ctrl Pts',(-45.4742952008371,22.6435084734481,
-665.092463235294));
#147266=CARTESIAN_POINT('Ctrl Pts',(-43.3760651419751,26.8573224770442,
-666.586580882353));
#147267=CARTESIAN_POINT('Ctrl Pts',(-40.5392751458362,30.6138395280662,
-668.080698529412));
#147268=CARTESIAN_POINT('Ctrl Pts',(-37.7024851496972,34.3703565790883,
-669.574816176471));
#147269=CARTESIAN_POINT('Ctrl Pts',(-34.2237386972451,37.5416529948095,
-671.068933823529));
#147270=CARTESIAN_POINT('Ctrl Pts',(-30.744992244793,40.7129494105307,-672.563051470588));
#147271=CARTESIAN_POINT('Ctrl Pts',(-26.7427538741697,43.1910304950644,
-674.057169117647));
#147272=CARTESIAN_POINT('Ctrl Pts',(-22.7405155035463,45.6691115795981,
-675.551286764706));
#147273=CARTESIAN_POINT('Ctrl Pts',(-18.3510766423074,47.3695892537413,
-677.045404411765));
#147274=CARTESIAN_POINT('Ctrl Pts',(-13.9616377810684,49.0700669278844,
-678.539522058824));
#147275=CARTESIAN_POINT('Ctrl Pts',(-9.33447550508177,49.9350334639422,
-680.033639705882));
#147276=CARTESIAN_POINT('Ctrl Pts',(-4.7073132290951,50.8,-681.527757352941));
#147277=CARTESIAN_POINT('Ctrl Pts',(-6.22120573966855E-15,50.8,-683.021875));
#147278=CARTESIAN_POINT('Ctrl Pts',(4.70731322909511,50.8,-684.515992647059));
#147279=CARTESIAN_POINT('Ctrl Pts',(9.33447550508176,49.9350334639422,-686.010110294118));
#147280=CARTESIAN_POINT('Ctrl Pts',(13.9616377810684,49.0700669278844,-687.504227941176));
#147281=CARTESIAN_POINT('Ctrl Pts',(18.3510766423074,47.3695892537413,-688.998345588235));
#147282=CARTESIAN_POINT('Ctrl Pts',(22.7405155035463,45.6691115795981,-690.492463235294));
#147283=CARTESIAN_POINT('Ctrl Pts',(26.7427538741697,43.1910304950644,-691.986580882353));
#147284=CARTESIAN_POINT('Ctrl Pts',(30.744992244793,40.7129494105307,-693.480698529412));
#147285=CARTESIAN_POINT('Ctrl Pts',(34.2237386972451,37.5416529948095,-694.974816176471));
#147286=CARTESIAN_POINT('Ctrl Pts',(37.7024851496972,34.3703565790883,-696.46893382353));
#147287=CARTESIAN_POINT('Ctrl Pts',(40.5392751458362,30.6138395280662,-697.963051470588));
#147288=CARTESIAN_POINT('Ctrl Pts',(43.3760651419751,26.8573224770442,-699.457169117647));
#147289=CARTESIAN_POINT('Ctrl Pts',(45.4742952008372,22.6435084734481,-700.951286764706));
#147290=CARTESIAN_POINT('Ctrl Pts',(47.5725252596992,18.4296944698521,-702.445404411765));
#147291=CARTESIAN_POINT('Ctrl Pts',(48.8607426731792,13.9020798956618,-703.939522058823));
#147292=CARTESIAN_POINT('Ctrl Pts',(50.1489600866593,9.37446532147146,-705.433639705882));
#147293=CARTESIAN_POINT('Ctrl Pts',(50.5832961557877,4.68723266073574,-706.927757352941));
#147294=CARTESIAN_POINT('Ctrl Pts',(51.0176322249162,9.37178700064808E-15,
-708.421875));
#147295=CARTESIAN_POINT('Ctrl Pts',(50.5832961557877,-4.68723266073572,
-709.915992647059));
#147296=CARTESIAN_POINT('Ctrl Pts',(50.1489600866593,-9.37446532147149,
-711.410110294118));
#147297=CARTESIAN_POINT('Ctrl Pts',(48.8607426731792,-13.9020798956618,
-712.904227941177));
#147298=CARTESIAN_POINT('Ctrl Pts',(47.5725252596992,-18.4296944698521,
-714.398345588236));
#147299=CARTESIAN_POINT('Ctrl Pts',(45.4742952008371,-22.6435084734482,
-715.892463235294));
#147300=CARTESIAN_POINT('Ctrl Pts',(43.3760651419751,-26.8573224770441,
-717.386580882353));
#147301=CARTESIAN_POINT('Ctrl Pts',(40.5392751458362,-30.6138395280662,
-718.880698529412));
#147302=CARTESIAN_POINT('Ctrl Pts',(37.7024851496972,-34.3703565790883,
-720.374816176471));
#147303=CARTESIAN_POINT('Ctrl Pts',(34.2237386972451,-37.5416529948095,
-721.868933823529));
#147304=CARTESIAN_POINT('Ctrl Pts',(30.744992244793,-40.7129494105307,-723.363051470588));
#147305=CARTESIAN_POINT('Ctrl Pts',(26.7427538741697,-43.1910304950644,
-724.857169117647));
#147306=CARTESIAN_POINT('Ctrl Pts',(22.7405155035463,-45.6691115795981,
-726.351286764706));
#147307=CARTESIAN_POINT('Ctrl Pts',(18.3510766423074,-47.3695892537413,
-727.845404411765));
#147308=CARTESIAN_POINT('Ctrl Pts',(13.9616377810684,-49.0700669278844,
-729.339522058824));
#147309=CARTESIAN_POINT('Ctrl Pts',(9.33447550508176,-49.9350334639422,
-730.833639705882));
#147310=CARTESIAN_POINT('Ctrl Pts',(4.70731322909511,-50.8,-732.327757352941));
#147311=CARTESIAN_POINT('Ctrl Pts',(0.,-50.8,-733.821875));
#147312=CARTESIAN_POINT('Ctrl Pts',(-4.70731322909511,-50.8,-735.315992647059));
#147313=CARTESIAN_POINT('Ctrl Pts',(-9.33447550508177,-49.9350334639422,
-736.810110294118));
#147314=CARTESIAN_POINT('Ctrl Pts',(-13.9616377810684,-49.0700669278844,
-738.304227941177));
#147315=CARTESIAN_POINT('Ctrl Pts',(-18.3510766423074,-47.3695892537413,
-739.798345588235));
#147316=CARTESIAN_POINT('Ctrl Pts',(-22.7405155035463,-45.6691115795981,
-741.292463235294));
#147317=CARTESIAN_POINT('Ctrl Pts',(-26.7427538741697,-43.1910304950644,
-742.786580882353));
#147318=CARTESIAN_POINT('Ctrl Pts',(-30.744992244793,-40.7129494105307,
-744.280698529412));
#147319=CARTESIAN_POINT('Ctrl Pts',(-34.2237386972451,-37.5416529948095,
-745.77481617647));
#147320=CARTESIAN_POINT('Ctrl Pts',(-37.7024851496972,-34.3703565790883,
-747.268933823529));
#147321=CARTESIAN_POINT('Ctrl Pts',(-40.5392751458362,-30.6138395280662,
-748.763051470588));
#147322=CARTESIAN_POINT('Ctrl Pts',(-43.3760651419751,-26.8573224770441,
-750.257169117647));
#147323=CARTESIAN_POINT('Ctrl Pts',(-45.4742952008371,-22.6435084734481,
-751.751286764706));
#147324=CARTESIAN_POINT('Ctrl Pts',(-47.5725252596992,-18.4296944698521,
-753.245404411765));
#147325=CARTESIAN_POINT('Ctrl Pts',(-48.8607426731792,-13.9020798956618,
-754.739522058824));
#147326=CARTESIAN_POINT('Ctrl Pts',(-50.1489600866593,-9.37446532147148,
-756.233639705882));
#147327=CARTESIAN_POINT('Ctrl Pts',(-50.5832961557877,-4.68723266073574,
-757.727757352941));
#147328=CARTESIAN_POINT('Ctrl Pts',(-51.0176322249162,-3.12392900021603E-15,
-759.221875000001));
#147329=CARTESIAN_POINT('Ctrl Pts',(-50.5832961557877,4.68723266073573,
-760.715992647059));
#147330=CARTESIAN_POINT('Ctrl Pts',(-50.1489600866593,9.37446532147149,
-762.210110294118));
#147331=CARTESIAN_POINT('Ctrl Pts',(-48.8607426731792,13.9020798956618,
-763.704227941176));
#147332=CARTESIAN_POINT('Ctrl Pts',(-47.5725252596992,18.4296944698521,
-765.198345588235));
#147333=CARTESIAN_POINT('Ctrl Pts',(-45.4742952008371,22.6435084734481,
-766.692463235294));
#147334=CARTESIAN_POINT('Ctrl Pts',(-43.3760651419751,26.8573224770442,
-768.186580882353));
#147335=CARTESIAN_POINT('Ctrl Pts',(-40.5392751458362,30.6138395280662,
-769.680698529412));
#147336=CARTESIAN_POINT('Ctrl Pts',(-37.7024851496972,34.3703565790883,
-771.174816176471));
#147337=CARTESIAN_POINT('Ctrl Pts',(-34.2237386972451,37.5416529948095,
-772.66893382353));
#147338=CARTESIAN_POINT('Ctrl Pts',(-30.744992244793,40.7129494105307,-774.163051470589));
#147339=CARTESIAN_POINT('Ctrl Pts',(-26.7427538741697,43.1910304950644,
-775.657169117647));
#147340=CARTESIAN_POINT('Ctrl Pts',(-22.7405155035463,45.6691115795981,
-777.151286764706));
#147341=CARTESIAN_POINT('Ctrl Pts',(-18.3510766423074,47.3695892537413,
-778.645404411765));
#147342=CARTESIAN_POINT('Ctrl Pts',(-13.9616377810684,49.0700669278844,
-780.139522058824));
#147343=CARTESIAN_POINT('Ctrl Pts',(-9.33447550508177,49.9350334639422,
-781.633639705882));
#147344=CARTESIAN_POINT('Ctrl Pts',(-4.7073132290951,50.8,-783.127757352941));
#147345=CARTESIAN_POINT('Ctrl Pts',(-6.22120573966855E-15,50.8,-784.621875));
#147346=CARTESIAN_POINT('Ctrl Pts',(4.70731322909511,50.8,-786.115992647059));
#147347=CARTESIAN_POINT('Ctrl Pts',(9.33447550508176,49.9350334639422,-787.610110294118));
#147348=CARTESIAN_POINT('Ctrl Pts',(13.9616377810684,49.0700669278844,-789.104227941177));
#147349=CARTESIAN_POINT('Ctrl Pts',(18.3510766423074,47.3695892537413,-790.598345588235));
#147350=CARTESIAN_POINT('Ctrl Pts',(22.7405155035463,45.6691115795981,-792.092463235294));
#147351=CARTESIAN_POINT('Ctrl Pts',(26.7427538741697,43.1910304950644,-793.586580882353));
#147352=CARTESIAN_POINT('Ctrl Pts',(30.744992244793,40.7129494105307,-795.080698529412));
#147353=CARTESIAN_POINT('Ctrl Pts',(34.2237386972451,37.5416529948095,-796.574816176471));
#147354=CARTESIAN_POINT('Ctrl Pts',(37.7024851496972,34.3703565790883,-798.068933823529));
#147355=CARTESIAN_POINT('Ctrl Pts',(40.5392751458362,30.6138395280662,-799.563051470588));
#147356=CARTESIAN_POINT('Ctrl Pts',(43.3760651419751,26.8573224770442,-801.057169117647));
#147357=CARTESIAN_POINT('Ctrl Pts',(45.4742952008372,22.6435084734481,-802.551286764706));
#147358=CARTESIAN_POINT('Ctrl Pts',(47.5725252596992,18.4296944698521,-804.045404411765));
#147359=CARTESIAN_POINT('Ctrl Pts',(48.8607426731792,13.9020798956618,-805.539522058823));
#147360=CARTESIAN_POINT('Ctrl Pts',(50.1489600866593,9.37446532147146,-807.033639705882));
#147361=CARTESIAN_POINT('Ctrl Pts',(50.5832961557877,4.68723266073574,-808.527757352941));
#147362=CARTESIAN_POINT('Ctrl Pts',(51.0176322249162,9.37178700064808E-15,
-810.021875));
#147363=CARTESIAN_POINT('Ctrl Pts',(50.5832961557877,-4.68723266073572,
-811.515992647059));
#147364=CARTESIAN_POINT('Ctrl Pts',(50.1489600866593,-9.37446532147149,
-813.010110294118));
#147365=CARTESIAN_POINT('Ctrl Pts',(48.8607426731792,-13.9020798956618,
-814.504227941177));
#147366=CARTESIAN_POINT('Ctrl Pts',(47.5725252596992,-18.4296944698521,
-815.998345588235));
#147367=CARTESIAN_POINT('Ctrl Pts',(45.4742952008371,-22.6435084734482,
-817.492463235294));
#147368=CARTESIAN_POINT('Ctrl Pts',(43.3760651419751,-26.8573224770441,
-818.986580882353));
#147369=CARTESIAN_POINT('Ctrl Pts',(40.5392751458362,-30.6138395280662,
-820.480698529411));
#147370=CARTESIAN_POINT('Ctrl Pts',(37.7024851496972,-34.3703565790883,
-821.97481617647));
#147371=CARTESIAN_POINT('Ctrl Pts',(34.2237386972451,-37.5416529948095,
-823.468933823529));
#147372=CARTESIAN_POINT('Ctrl Pts',(30.744992244793,-40.7129494105307,-824.963051470588));
#147373=CARTESIAN_POINT('Ctrl Pts',(26.7427538741697,-43.1910304950644,
-826.457169117647));
#147374=CARTESIAN_POINT('Ctrl Pts',(22.7405155035463,-45.6691115795981,
-827.951286764706));
#147375=CARTESIAN_POINT('Ctrl Pts',(18.3510766423074,-47.3695892537413,
-829.445404411765));
#147376=CARTESIAN_POINT('Ctrl Pts',(13.9616377810684,-49.0700669278844,
-830.939522058824));
#147377=CARTESIAN_POINT('Ctrl Pts',(9.33447550508176,-49.9350334639422,
-832.433639705882));
#147378=CARTESIAN_POINT('Ctrl Pts',(4.70731322909511,-50.8,-833.927757352942));
#147379=CARTESIAN_POINT('Ctrl Pts',(0.,-50.8,-835.421875));
#147380=CARTESIAN_POINT('Ctrl Pts',(-4.70731322909511,-50.8,-836.915992647059));
#147381=CARTESIAN_POINT('Ctrl Pts',(-9.33447550508177,-49.9350334639422,
-838.410110294118));
#147382=CARTESIAN_POINT('Ctrl Pts',(-13.9616377810684,-49.0700669278844,
-839.904227941177));
#147383=CARTESIAN_POINT('Ctrl Pts',(-18.3510766423074,-47.3695892537413,
-841.398345588235));
#147384=CARTESIAN_POINT('Ctrl Pts',(-22.7405155035463,-45.6691115795981,
-842.892463235294));
#147385=CARTESIAN_POINT('Ctrl Pts',(-26.7427538741697,-43.1910304950644,
-844.386580882353));
#147386=CARTESIAN_POINT('Ctrl Pts',(-30.744992244793,-40.7129494105307,
-845.880698529412));
#147387=CARTESIAN_POINT('Ctrl Pts',(-34.2237386972451,-37.5416529948095,
-847.374816176471));
#147388=CARTESIAN_POINT('Ctrl Pts',(-37.7024851496972,-34.3703565790883,
-848.86893382353));
#147389=CARTESIAN_POINT('Ctrl Pts',(-40.5392751458362,-30.6138395280662,
-850.363051470588));
#147390=CARTESIAN_POINT('Ctrl Pts',(-43.3760651419751,-26.8573224770441,
-851.857169117647));
#147391=CARTESIAN_POINT('Ctrl Pts',(-45.4742952008371,-22.6435084734481,
-853.351286764706));
#147392=CARTESIAN_POINT('Ctrl Pts',(-47.5725252596992,-18.4296944698521,
-854.845404411765));
#147393=CARTESIAN_POINT('Ctrl Pts',(-48.8607426731792,-13.9020798956618,
-856.339522058823));
#147394=CARTESIAN_POINT('Ctrl Pts',(-50.1489600866593,-9.37446532147148,
-857.833639705882));
#147395=CARTESIAN_POINT('Ctrl Pts',(-50.5832961557877,-4.68723266073574,
-859.327757352941));
#147396=CARTESIAN_POINT('Ctrl Pts',(-51.0176322249162,-3.12392900021603E-15,
-860.821875));
#147397=CARTESIAN_POINT('Ctrl Pts',(-50.5832961557877,4.68723266073573,
-862.315992647059));
#147398=CARTESIAN_POINT('Ctrl Pts',(-50.1489600866593,9.37446532147149,
-863.810110294118));
#147399=CARTESIAN_POINT('Ctrl Pts',(-48.8607426731792,13.9020798956618,
-865.304227941176));
#147400=CARTESIAN_POINT('Ctrl Pts',(-47.5725252596992,18.4296944698521,
-866.798345588235));
#147401=CARTESIAN_POINT('Ctrl Pts',(-45.4742952008371,22.6435084734481,
-868.292463235294));
#147402=CARTESIAN_POINT('Ctrl Pts',(-43.3760651419751,26.8573224770442,
-869.786580882353));
#147403=CARTESIAN_POINT('Ctrl Pts',(-40.5392751458362,30.6138395280662,
-871.280698529412));
#147404=CARTESIAN_POINT('Ctrl Pts',(-37.7024851496972,34.3703565790883,
-872.774816176471));
#147405=CARTESIAN_POINT('Ctrl Pts',(-34.2237386972451,37.5416529948095,
-874.268933823529));
#147406=CARTESIAN_POINT('Ctrl Pts',(-30.744992244793,40.7129494105307,-875.763051470589));
#147407=CARTESIAN_POINT('Ctrl Pts',(-26.7427538741697,43.1910304950644,
-877.257169117647));
#147408=CARTESIAN_POINT('Ctrl Pts',(-22.7405155035463,45.6691115795981,
-878.751286764706));
#147409=CARTESIAN_POINT('Ctrl Pts',(-18.3510766423074,47.3695892537413,
-880.245404411764));
#147410=CARTESIAN_POINT('Ctrl Pts',(-13.9616377810684,49.0700669278844,
-881.739522058823));
#147411=CARTESIAN_POINT('Ctrl Pts',(-9.33447550508177,49.9350334639422,
-883.233639705882));
#147412=CARTESIAN_POINT('Ctrl Pts',(-4.7073132290951,50.8,-884.727757352941));
#147413=CARTESIAN_POINT('Ctrl Pts',(-6.22120573966855E-15,50.8,-886.221875));
#147414=CARTESIAN_POINT('Ctrl Pts',(4.70731322909511,50.8,-887.715992647059));
#147415=CARTESIAN_POINT('Ctrl Pts',(9.33447550508176,49.9350334639422,-889.210110294118));
#147416=CARTESIAN_POINT('Ctrl Pts',(13.9616377810684,49.0700669278844,-890.704227941177));
#147417=CARTESIAN_POINT('Ctrl Pts',(18.3510766423074,47.3695892537413,-892.198345588235));
#147418=CARTESIAN_POINT('Ctrl Pts',(22.7405155035463,45.6691115795981,-893.692463235295));
#147419=CARTESIAN_POINT('Ctrl Pts',(26.7427538741697,43.1910304950644,-895.186580882353));
#147420=CARTESIAN_POINT('Ctrl Pts',(30.744992244793,40.7129494105307,-896.680698529412));
#147421=CARTESIAN_POINT('Ctrl Pts',(34.2237386972451,37.5416529948095,-898.17481617647));
#147422=CARTESIAN_POINT('Ctrl Pts',(37.7024851496972,34.3703565790883,-899.66893382353));
#147423=CARTESIAN_POINT('Ctrl Pts',(40.5392751458362,30.6138395280662,-901.163051470588));
#147424=CARTESIAN_POINT('Ctrl Pts',(43.3760651419751,26.8573224770442,-902.657169117647));
#147425=CARTESIAN_POINT('Ctrl Pts',(45.4742952008372,22.6435084734481,-904.151286764706));
#147426=CARTESIAN_POINT('Ctrl Pts',(47.5725252596992,18.4296944698521,-905.645404411765));
#147427=CARTESIAN_POINT('Ctrl Pts',(48.8607426731792,13.9020798956618,-907.139522058824));
#147428=CARTESIAN_POINT('Ctrl Pts',(50.1489600866593,9.37446532147146,-908.633639705883));
#147429=CARTESIAN_POINT('Ctrl Pts',(50.5832961557877,4.68723266073574,-910.127757352941));
#147430=CARTESIAN_POINT('Ctrl Pts',(51.0176322249162,9.37178700064808E-15,
-911.621875));
#147431=CARTESIAN_POINT('Ctrl Pts',(50.5832961557877,-4.68723266073572,
-913.115992647059));
#147432=CARTESIAN_POINT('Ctrl Pts',(50.1489600866593,-9.37446532147149,
-914.610110294118));
#147433=CARTESIAN_POINT('Ctrl Pts',(48.8607426731792,-13.9020798956618,
-916.104227941177));
#147434=CARTESIAN_POINT('Ctrl Pts',(47.5725252596992,-18.4296944698521,
-917.598345588235));
#147435=CARTESIAN_POINT('Ctrl Pts',(45.4742952008371,-22.6435084734482,
-919.092463235294));
#147436=CARTESIAN_POINT('Ctrl Pts',(43.3760651419751,-26.8573224770441,
-920.586580882353));
#147437=CARTESIAN_POINT('Ctrl Pts',(40.5392751458362,-30.6138395280662,
-922.080698529412));
#147438=CARTESIAN_POINT('Ctrl Pts',(37.7024851496972,-34.3703565790883,
-923.574816176471));
#147439=CARTESIAN_POINT('Ctrl Pts',(34.2237386972451,-37.5416529948095,
-925.068933823529));
#147440=CARTESIAN_POINT('Ctrl Pts',(30.744992244793,-40.7129494105307,-926.563051470588));
#147441=CARTESIAN_POINT('Ctrl Pts',(26.7427538741697,-43.1910304950644,
-928.057169117647));
#147442=CARTESIAN_POINT('Ctrl Pts',(22.7405155035463,-45.6691115795981,
-929.551286764706));
#147443=CARTESIAN_POINT('Ctrl Pts',(18.3510766423074,-47.3695892537413,
-931.045404411765));
#147444=CARTESIAN_POINT('Ctrl Pts',(13.9616377810684,-49.0700669278844,
-932.539522058824));
#147445=CARTESIAN_POINT('Ctrl Pts',(9.33447550508176,-49.9350334639422,
-934.033639705882));
#147446=CARTESIAN_POINT('Ctrl Pts',(4.70731322909511,-50.8,-935.527757352942));
#147447=CARTESIAN_POINT('Ctrl Pts',(0.,-50.8,-937.021875));
#147448=CARTESIAN_POINT('Ctrl Pts',(-4.70731322909511,-50.8,-938.515992647059));
#147449=CARTESIAN_POINT('Ctrl Pts',(-9.33447550508177,-49.9350334639422,
-940.010110294118));
#147450=CARTESIAN_POINT('Ctrl Pts',(-13.9616377810684,-49.0700669278844,
-941.504227941176));
#147451=CARTESIAN_POINT('Ctrl Pts',(-18.3510766423074,-47.3695892537413,
-942.998345588235));
#147452=CARTESIAN_POINT('Ctrl Pts',(-22.7405155035463,-45.6691115795981,
-944.492463235294));
#147453=CARTESIAN_POINT('Ctrl Pts',(-26.7427538741697,-43.1910304950644,
-945.986580882353));
#147454=CARTESIAN_POINT('Ctrl Pts',(-30.744992244793,-40.7129494105307,
-947.480698529412));
#147455=CARTESIAN_POINT('Ctrl Pts',(-34.2237386972451,-37.5416529948095,
-948.974816176471));
#147456=CARTESIAN_POINT('Ctrl Pts',(-37.7024851496972,-34.3703565790883,
-950.46893382353));
#147457=CARTESIAN_POINT('Ctrl Pts',(-40.5392751458362,-30.6138395280662,
-951.963051470588));
#147458=CARTESIAN_POINT('Ctrl Pts',(-43.3760651419751,-26.8573224770441,
-953.457169117647));
#147459=CARTESIAN_POINT('Ctrl Pts',(-45.4742952008371,-22.6435084734481,
-954.951286764706));
#147460=CARTESIAN_POINT('Ctrl Pts',(-47.5725252596992,-18.4296944698521,
-956.445404411765));
#147461=CARTESIAN_POINT('Ctrl Pts',(-48.8607426731792,-13.9020798956618,
-957.939522058824));
#147462=CARTESIAN_POINT('Ctrl Pts',(-50.1489600866593,-9.37446532147148,
-959.433639705883));
#147463=CARTESIAN_POINT('Ctrl Pts',(-50.5832961557877,-4.68723266073574,
-960.927757352941));
#147464=CARTESIAN_POINT('Ctrl Pts',(-51.0176322249162,-3.12392900021603E-15,
-962.421875));
#147465=CARTESIAN_POINT('Ctrl Pts',(-50.5832961557877,4.68723266073573,
-963.915992647059));
#147466=CARTESIAN_POINT('Ctrl Pts',(-50.1489600866593,9.37446532147149,
-965.410110294118));
#147467=CARTESIAN_POINT('Ctrl Pts',(-48.8607426731792,13.9020798956618,
-966.904227941177));
#147468=CARTESIAN_POINT('Ctrl Pts',(-47.5725252596992,18.4296944698521,
-968.398345588236));
#147469=CARTESIAN_POINT('Ctrl Pts',(-45.4742952008371,22.6435084734481,
-969.892463235294));
#147470=CARTESIAN_POINT('Ctrl Pts',(-43.3760651419751,26.8573224770442,
-971.386580882353));
#147471=CARTESIAN_POINT('Ctrl Pts',(-40.5392751458362,30.6138395280662,
-972.880698529412));
#147472=CARTESIAN_POINT('Ctrl Pts',(-37.7024851496972,34.3703565790883,
-974.374816176471));
#147473=CARTESIAN_POINT('Ctrl Pts',(-34.2237386972451,37.5416529948095,
-975.868933823529));
#147474=CARTESIAN_POINT('Ctrl Pts',(-30.744992244793,40.7129494105307,-977.363051470588));
#147475=CARTESIAN_POINT('Ctrl Pts',(-26.7427538741697,43.1910304950644,
-978.857169117647));
#147476=CARTESIAN_POINT('Ctrl Pts',(-22.7405155035463,45.6691115795981,
-980.351286764706));
#147477=CARTESIAN_POINT('Ctrl Pts',(-18.3510766423074,47.3695892537413,
-981.845404411765));
#147478=CARTESIAN_POINT('Ctrl Pts',(-13.9616377810684,49.0700669278844,
-983.339522058824));
#147479=CARTESIAN_POINT('Ctrl Pts',(-9.33447550508177,49.9350334639422,
-984.833639705882));
#147480=CARTESIAN_POINT('Ctrl Pts',(-4.7073132290951,50.8,-986.327757352941));
#147481=CARTESIAN_POINT('Ctrl Pts',(-6.22120573966855E-15,50.8,-987.821875));
#147482=CARTESIAN_POINT('Ctrl Pts',(4.70731322909511,50.8,-989.315992647059));
#147483=CARTESIAN_POINT('Ctrl Pts',(9.33447550508176,49.9350334639422,-990.810110294118));
#147484=CARTESIAN_POINT('Ctrl Pts',(13.9616377810684,49.0700669278844,-992.304227941177));
#147485=CARTESIAN_POINT('Ctrl Pts',(18.3510766423074,47.3695892537413,-993.798345588235));
#147486=CARTESIAN_POINT('Ctrl Pts',(22.7405155035463,45.6691115795981,-995.292463235294));
#147487=CARTESIAN_POINT('Ctrl Pts',(26.7427538741697,43.1910304950644,-996.786580882353));
#147488=CARTESIAN_POINT('Ctrl Pts',(30.744992244793,40.7129494105307,-998.280698529412));
#147489=CARTESIAN_POINT('Ctrl Pts',(34.2237386972451,37.5416529948095,-999.77481617647));
#147490=CARTESIAN_POINT('Ctrl Pts',(37.7024851496972,34.3703565790883,-1001.26893382353));
#147491=CARTESIAN_POINT('Ctrl Pts',(40.5392751458362,30.6138395280662,-1002.76305147059));
#147492=CARTESIAN_POINT('Ctrl Pts',(43.3760651419751,26.8573224770442,-1004.25716911765));
#147493=CARTESIAN_POINT('Ctrl Pts',(45.4742952008372,22.6435084734481,-1005.75128676471));
#147494=CARTESIAN_POINT('Ctrl Pts',(47.5725252596992,18.4296944698521,-1007.24540441176));
#147495=CARTESIAN_POINT('Ctrl Pts',(48.8607426731792,13.9020798956618,-1008.73952205882));
#147496=CARTESIAN_POINT('Ctrl Pts',(50.1489600866593,9.37446532147146,-1010.23363970588));
#147497=CARTESIAN_POINT('Ctrl Pts',(50.5832961557877,4.68723266073574,-1011.72775735294));
#147498=CARTESIAN_POINT('Ctrl Pts',(51.0176322249162,9.37178700064808E-15,
-1013.221875));
#147499=CARTESIAN_POINT('Ctrl Pts',(50.5832961557877,-4.68723266073572,
-1014.71599264706));
#147500=CARTESIAN_POINT('Ctrl Pts',(50.1489600866593,-9.37446532147149,
-1016.21011029412));
#147501=CARTESIAN_POINT('Ctrl Pts',(48.8607426731792,-13.9020798956618,
-1017.70422794118));
#147502=CARTESIAN_POINT('Ctrl Pts',(47.5725252596992,-18.4296944698521,
-1019.19834558824));
#147503=CARTESIAN_POINT('Ctrl Pts',(45.4742952008371,-22.6435084734482,
-1020.69246323529));
#147504=CARTESIAN_POINT('Ctrl Pts',(43.3760651419751,-26.8573224770441,
-1022.18658088235));
#147505=CARTESIAN_POINT('Ctrl Pts',(40.5392751458362,-30.6138395280662,
-1023.68069852941));
#147506=CARTESIAN_POINT('Ctrl Pts',(37.7024851496972,-34.3703565790883,
-1025.17481617647));
#147507=CARTESIAN_POINT('Ctrl Pts',(34.2237386972451,-37.5416529948095,
-1026.66893382353));
#147508=CARTESIAN_POINT('Ctrl Pts',(30.744992244793,-40.7129494105307,-1028.16305147059));
#147509=CARTESIAN_POINT('Ctrl Pts',(26.7427538741697,-43.1910304950644,
-1029.65716911765));
#147510=CARTESIAN_POINT('Ctrl Pts',(22.7405155035463,-45.6691115795981,
-1031.15128676471));
#147511=CARTESIAN_POINT('Ctrl Pts',(18.3510766423074,-47.3695892537413,
-1032.64540441176));
#147512=CARTESIAN_POINT('Ctrl Pts',(13.9616377810684,-49.0700669278844,
-1034.13952205882));
#147513=CARTESIAN_POINT('Ctrl Pts',(9.33447550508176,-49.9350334639422,
-1035.63363970588));
#147514=CARTESIAN_POINT('Ctrl Pts',(4.70731322909511,-50.8,-1037.12775735294));
#147515=CARTESIAN_POINT('Ctrl Pts',(0.,-50.8,-1038.621875));
#147516=CARTESIAN_POINT('Ctrl Pts',(-4.70731322909511,-50.8,-1040.11599264706));
#147517=CARTESIAN_POINT('Ctrl Pts',(-9.33447550508177,-49.9350334639422,
-1041.61011029412));
#147518=CARTESIAN_POINT('Ctrl Pts',(-13.9616377810684,-49.0700669278844,
-1043.10422794118));
#147519=CARTESIAN_POINT('Ctrl Pts',(-18.3510766423074,-47.3695892537413,
-1044.59834558824));
#147520=CARTESIAN_POINT('Ctrl Pts',(-22.7405155035463,-45.6691115795981,
-1046.09246323529));
#147521=CARTESIAN_POINT('Ctrl Pts',(-26.7427538741697,-43.1910304950644,
-1047.58658088235));
#147522=CARTESIAN_POINT('Ctrl Pts',(-30.744992244793,-40.7129494105307,
-1049.08069852941));
#147523=CARTESIAN_POINT('Ctrl Pts',(-34.2237386972451,-37.5416529948095,
-1050.57481617647));
#147524=CARTESIAN_POINT('Ctrl Pts',(-37.7024851496972,-34.3703565790883,
-1052.06893382353));
#147525=CARTESIAN_POINT('Ctrl Pts',(-40.5392751458362,-30.6138395280662,
-1053.56305147059));
#147526=CARTESIAN_POINT('Ctrl Pts',(-43.3760651419751,-26.8573224770441,
-1055.05716911765));
#147527=CARTESIAN_POINT('Ctrl Pts',(-45.4742952008371,-22.6435084734481,
-1056.55128676471));
#147528=CARTESIAN_POINT('Ctrl Pts',(-47.5725252596992,-18.4296944698521,
-1058.04540441177));
#147529=CARTESIAN_POINT('Ctrl Pts',(-48.8607426731792,-13.9020798956618,
-1059.53952205882));
#147530=CARTESIAN_POINT('Ctrl Pts',(-50.1489600866593,-9.37446532147148,
-1061.03363970588));
#147531=CARTESIAN_POINT('Ctrl Pts',(-50.5832961557877,-4.68723266073574,
-1062.52775735294));
#147532=CARTESIAN_POINT('Ctrl Pts',(-51.0176322249162,-3.12392900021603E-15,
-1064.021875));
#147533=CARTESIAN_POINT('Ctrl Pts',(-50.5832961557877,4.68723266073573,
-1065.51599264706));
#147534=CARTESIAN_POINT('Ctrl Pts',(-50.1489600866593,9.37446532147149,
-1067.01011029412));
#147535=CARTESIAN_POINT('Ctrl Pts',(-48.8607426731792,13.9020798956618,
-1068.50422794118));
#147536=CARTESIAN_POINT('Ctrl Pts',(-47.5725252596992,18.4296944698521,
-1069.99834558824));
#147537=CARTESIAN_POINT('Ctrl Pts',(-45.4742952008371,22.6435084734481,
-1071.49246323529));
#147538=CARTESIAN_POINT('Ctrl Pts',(-43.3760651419751,26.8573224770442,
-1072.98658088235));
#147539=CARTESIAN_POINT('Ctrl Pts',(-40.5392751458362,30.6138395280662,
-1074.48069852941));
#147540=CARTESIAN_POINT('Ctrl Pts',(-37.7024851496972,34.3703565790883,
-1075.97481617647));
#147541=CARTESIAN_POINT('Ctrl Pts',(-34.2237386972451,37.5416529948095,
-1077.46893382353));
#147542=CARTESIAN_POINT('Ctrl Pts',(-30.744992244793,40.7129494105307,-1078.96305147059));
#147543=CARTESIAN_POINT('Ctrl Pts',(-26.7427538741697,43.1910304950644,
-1080.45716911765));
#147544=CARTESIAN_POINT('Ctrl Pts',(-22.7405155035463,45.6691115795981,
-1081.95128676471));
#147545=CARTESIAN_POINT('Ctrl Pts',(-18.3510766423074,47.3695892537413,
-1083.44540441176));
#147546=CARTESIAN_POINT('Ctrl Pts',(-13.9616377810684,49.0700669278844,
-1084.93952205882));
#147547=CARTESIAN_POINT('Ctrl Pts',(-9.33447550508177,49.9350334639422,
-1086.43363970588));
#147548=CARTESIAN_POINT('Ctrl Pts',(-4.7073132290951,50.8,-1087.92775735294));
#147549=CARTESIAN_POINT('Ctrl Pts',(-6.22120573966855E-15,50.8,-1089.421875));
#147550=CARTESIAN_POINT('Ctrl Pts',(4.70731322909511,50.8,-1090.91599264706));
#147551=CARTESIAN_POINT('Ctrl Pts',(9.33447550508176,49.9350334639422,-1092.41011029412));
#147552=CARTESIAN_POINT('Ctrl Pts',(13.9616377810684,49.0700669278844,-1093.90422794118));
#147553=CARTESIAN_POINT('Ctrl Pts',(18.3510766423074,47.3695892537413,-1095.39834558824));
#147554=CARTESIAN_POINT('Ctrl Pts',(22.7405155035463,45.6691115795981,-1096.89246323529));
#147555=CARTESIAN_POINT('Ctrl Pts',(26.7427538741697,43.1910304950644,-1098.38658088235));
#147556=CARTESIAN_POINT('Ctrl Pts',(30.744992244793,40.7129494105307,-1099.88069852941));
#147557=CARTESIAN_POINT('Ctrl Pts',(34.2237386972451,37.5416529948095,-1101.37481617647));
#147558=CARTESIAN_POINT('Ctrl Pts',(37.7024851496972,34.3703565790883,-1102.86893382353));
#147559=CARTESIAN_POINT('Ctrl Pts',(40.5392751458362,30.6138395280662,-1104.36305147059));
#147560=CARTESIAN_POINT('Ctrl Pts',(43.3760651419751,26.8573224770442,-1105.85716911765));
#147561=CARTESIAN_POINT('Ctrl Pts',(45.4742952008372,22.6435084734481,-1107.35128676471));
#147562=CARTESIAN_POINT('Ctrl Pts',(47.5725252596992,18.4296944698521,-1108.84540441177));
#147563=CARTESIAN_POINT('Ctrl Pts',(48.8607426731792,13.9020798956618,-1110.33952205882));
#147564=CARTESIAN_POINT('Ctrl Pts',(50.1489600866593,9.37446532147146,-1111.83363970588));
#147565=CARTESIAN_POINT('Ctrl Pts',(50.5832961557877,4.68723266073574,-1113.32775735294));
#147566=CARTESIAN_POINT('Ctrl Pts',(51.0176322249162,9.37178700064808E-15,
-1114.821875));
#147567=CARTESIAN_POINT('Ctrl Pts',(50.5832961557877,-4.68723266073572,
-1116.31599264706));
#147568=CARTESIAN_POINT('Ctrl Pts',(50.1489600866593,-9.37446532147149,
-1117.81011029412));
#147569=CARTESIAN_POINT('Ctrl Pts',(48.8607426731792,-13.9020798956618,
-1119.30422794118));
#147570=CARTESIAN_POINT('Ctrl Pts',(47.5725252596992,-18.4296944698521,
-1120.79834558823));
#147571=CARTESIAN_POINT('Ctrl Pts',(45.4742952008371,-22.6435084734482,
-1122.29246323529));
#147572=CARTESIAN_POINT('Ctrl Pts',(43.3760651419751,-26.8573224770441,
-1123.78658088235));
#147573=CARTESIAN_POINT('Ctrl Pts',(40.5392751458362,-30.6138395280662,
-1125.28069852941));
#147574=CARTESIAN_POINT('Ctrl Pts',(37.7024851496972,-34.3703565790883,
-1126.77481617647));
#147575=CARTESIAN_POINT('Ctrl Pts',(34.2237386972451,-37.5416529948095,
-1128.26893382353));
#147576=CARTESIAN_POINT('Ctrl Pts',(30.744992244793,-40.7129494105307,-1129.76305147059));
#147577=CARTESIAN_POINT('Ctrl Pts',(26.7427538741697,-43.1910304950644,
-1131.25716911765));
#147578=CARTESIAN_POINT('Ctrl Pts',(22.7405155035463,-45.6691115795981,
-1132.75128676471));
#147579=CARTESIAN_POINT('Ctrl Pts',(18.3510766423074,-47.3695892537413,
-1134.24540441176));
#147580=CARTESIAN_POINT('Ctrl Pts',(13.9616377810684,-49.0700669278844,
-1135.73952205882));
#147581=CARTESIAN_POINT('Ctrl Pts',(9.33447550508176,-49.9350334639422,
-1137.23363970588));
#147582=CARTESIAN_POINT('Ctrl Pts',(4.70731322909511,-50.8,-1138.72775735294));
#147583=CARTESIAN_POINT('Ctrl Pts',(0.,-50.8,-1140.221875));
#147584=CARTESIAN_POINT('Ctrl Pts',(-4.70731322909511,-50.8,-1141.71599264706));
#147585=CARTESIAN_POINT('Ctrl Pts',(-9.33447550508177,-49.9350334639422,
-1143.21011029412));
#147586=CARTESIAN_POINT('Ctrl Pts',(-13.9616377810684,-49.0700669278844,
-1144.70422794118));
#147587=CARTESIAN_POINT('Ctrl Pts',(-18.3510766423074,-47.3695892537413,
-1146.19834558824));
#147588=CARTESIAN_POINT('Ctrl Pts',(-22.7405155035463,-45.6691115795981,
-1147.69246323529));
#147589=CARTESIAN_POINT('Ctrl Pts',(-26.7427538741697,-43.1910304950644,
-1149.18658088235));
#147590=CARTESIAN_POINT('Ctrl Pts',(-30.744992244793,-40.7129494105307,
-1150.68069852941));
#147591=CARTESIAN_POINT('Ctrl Pts',(-34.2237386972451,-37.5416529948095,
-1152.17481617647));
#147592=CARTESIAN_POINT('Ctrl Pts',(-37.7024851496972,-34.3703565790883,
-1153.66893382353));
#147593=CARTESIAN_POINT('Ctrl Pts',(-40.5392751458362,-30.6138395280662,
-1155.16305147059));
#147594=CARTESIAN_POINT('Ctrl Pts',(-43.3760651419751,-26.8573224770441,
-1156.65716911765));
#147595=CARTESIAN_POINT('Ctrl Pts',(-45.4742952008371,-22.6435084734481,
-1158.15128676471));
#147596=CARTESIAN_POINT('Ctrl Pts',(-47.5725252596992,-18.4296944698521,
-1159.64540441176));
#147597=CARTESIAN_POINT('Ctrl Pts',(-48.8607426731792,-13.9020798956618,
-1161.13952205882));
#147598=CARTESIAN_POINT('Ctrl Pts',(-50.1489600866593,-9.37446532147148,
-1162.63363970588));
#147599=CARTESIAN_POINT('Ctrl Pts',(-50.5832961557877,-4.68723266073574,
-1164.12775735294));
#147600=CARTESIAN_POINT('Ctrl Pts',(-51.0176322249162,-3.12392900021603E-15,
-1165.621875));
#147601=CARTESIAN_POINT('Ctrl Pts',(-50.5832961557877,4.68723266073573,
-1167.11599264706));
#147602=CARTESIAN_POINT('Ctrl Pts',(-50.1489600866593,9.37446532147149,
-1168.61011029412));
#147603=CARTESIAN_POINT('Ctrl Pts',(-48.8607426731792,13.9020798956618,
-1170.10422794118));
#147604=CARTESIAN_POINT('Ctrl Pts',(-47.5725252596992,18.4296944698521,
-1171.59834558824));
#147605=CARTESIAN_POINT('Ctrl Pts',(-45.4742952008371,22.6435084734481,
-1173.09246323529));
#147606=CARTESIAN_POINT('Ctrl Pts',(-43.3760651419751,26.8573224770442,
-1174.58658088235));
#147607=CARTESIAN_POINT('Ctrl Pts',(-40.5392751458362,30.6138395280662,
-1176.08069852941));
#147608=CARTESIAN_POINT('Ctrl Pts',(-37.7024851496972,34.3703565790883,
-1177.57481617647));
#147609=CARTESIAN_POINT('Ctrl Pts',(-34.2237386972451,37.5416529948095,
-1179.06893382353));
#147610=CARTESIAN_POINT('Ctrl Pts',(-30.744992244793,40.7129494105307,-1180.56305147059));
#147611=CARTESIAN_POINT('Ctrl Pts',(-26.7427538741697,43.1910304950644,
-1182.05716911765));
#147612=CARTESIAN_POINT('Ctrl Pts',(-22.7405155035463,45.6691115795981,
-1183.55128676471));
#147613=CARTESIAN_POINT('Ctrl Pts',(-18.3510766423074,47.3695892537413,
-1185.04540441176));
#147614=CARTESIAN_POINT('Ctrl Pts',(-13.9616377810684,49.0700669278844,
-1186.53952205882));
#147615=CARTESIAN_POINT('Ctrl Pts',(-9.33447550508177,49.9350334639422,
-1188.03363970588));
#147616=CARTESIAN_POINT('Ctrl Pts',(-4.7073132290951,50.8,-1189.52775735294));
#147617=CARTESIAN_POINT('Ctrl Pts',(-6.22120573966855E-15,50.8,-1191.021875));
#147618=CARTESIAN_POINT('Ctrl Pts',(4.70731322909511,50.8,-1192.51599264706));
#147619=CARTESIAN_POINT('Ctrl Pts',(9.33447550508176,49.9350334639422,-1194.01011029412));
#147620=CARTESIAN_POINT('Ctrl Pts',(13.9616377810684,49.0700669278844,-1195.50422794118));
#147621=CARTESIAN_POINT('Ctrl Pts',(18.3510766423074,47.3695892537413,-1196.99834558824));
#147622=CARTESIAN_POINT('Ctrl Pts',(22.7405155035463,45.6691115795981,-1198.49246323529));
#147623=CARTESIAN_POINT('Ctrl Pts',(26.7427538741697,43.1910304950644,-1199.98658088235));
#147624=CARTESIAN_POINT('Ctrl Pts',(30.744992244793,40.7129494105307,-1201.48069852941));
#147625=CARTESIAN_POINT('Ctrl Pts',(34.2237386972451,37.5416529948095,-1202.97481617647));
#147626=CARTESIAN_POINT('Ctrl Pts',(37.7024851496972,34.3703565790883,-1204.46893382353));
#147627=CARTESIAN_POINT('Ctrl Pts',(40.5392751458362,30.6138395280662,-1205.96305147059));
#147628=CARTESIAN_POINT('Ctrl Pts',(43.3760651419751,26.8573224770442,-1207.45716911765));
#147629=CARTESIAN_POINT('Ctrl Pts',(45.4742952008372,22.6435084734481,-1208.95128676471));
#147630=CARTESIAN_POINT('Ctrl Pts',(47.5725252596992,18.4296944698521,-1210.44540441176));
#147631=CARTESIAN_POINT('Ctrl Pts',(48.8607426731792,13.9020798956618,-1211.93952205882));
#147632=CARTESIAN_POINT('Ctrl Pts',(50.1489600866593,9.37446532147146,-1213.43363970588));
#147633=CARTESIAN_POINT('Ctrl Pts',(50.5832961557877,4.68723266073574,-1214.92775735294));
#147634=CARTESIAN_POINT('Ctrl Pts',(51.0176322249162,9.37178700064808E-15,
-1216.421875));
#147635=CARTESIAN_POINT('Ctrl Pts',(50.5832961557877,-4.68723266073572,
-1217.91599264706));
#147636=CARTESIAN_POINT('Ctrl Pts',(50.1489600866593,-9.37446532147149,
-1219.41011029412));
#147637=CARTESIAN_POINT('Ctrl Pts',(48.8607426731792,-13.9020798956618,
-1220.90422794118));
#147638=CARTESIAN_POINT('Ctrl Pts',(47.5725252596992,-18.4296944698521,
-1222.39834558824));
#147639=CARTESIAN_POINT('Ctrl Pts',(45.4742952008371,-22.6435084734482,
-1223.89246323529));
#147640=CARTESIAN_POINT('Ctrl Pts',(43.3760651419751,-26.8573224770441,
-1225.38658088235));
#147641=CARTESIAN_POINT('Ctrl Pts',(40.5392751458362,-30.6138395280662,
-1226.88069852941));
#147642=CARTESIAN_POINT('Ctrl Pts',(37.7024851496972,-34.3703565790883,
-1228.37481617647));
#147643=CARTESIAN_POINT('Ctrl Pts',(34.2237386972451,-37.5416529948095,
-1229.86893382353));
#147644=CARTESIAN_POINT('Ctrl Pts',(30.744992244793,-40.7129494105307,-1231.36305147059));
#147645=CARTESIAN_POINT('Ctrl Pts',(26.7427538741697,-43.1910304950644,
-1232.85716911765));
#147646=CARTESIAN_POINT('Ctrl Pts',(22.7405155035463,-45.6691115795981,
-1234.35128676471));
#147647=CARTESIAN_POINT('Ctrl Pts',(18.3510766423074,-47.3695892537413,
-1235.84540441176));
#147648=CARTESIAN_POINT('Ctrl Pts',(13.9616377810684,-49.0700669278844,
-1237.33952205882));
#147649=CARTESIAN_POINT('Ctrl Pts',(9.33447550508176,-49.9350334639422,
-1238.83363970588));
#147650=CARTESIAN_POINT('Ctrl Pts',(4.70731322909511,-50.8,-1240.32775735294));
#147651=CARTESIAN_POINT('Ctrl Pts',(0.,-50.8,-1241.821875));
#147652=CARTESIAN_POINT('Ctrl Pts',(-4.70731322909511,-50.8,-1243.31599264706));
#147653=CARTESIAN_POINT('Ctrl Pts',(-9.33447550508177,-49.9350334639422,
-1244.81011029412));
#147654=CARTESIAN_POINT('Ctrl Pts',(-13.9616377810684,-49.0700669278844,
-1246.30422794118));
#147655=CARTESIAN_POINT('Ctrl Pts',(-18.3510766423074,-47.3695892537413,
-1247.79834558824));
#147656=CARTESIAN_POINT('Ctrl Pts',(-22.7405155035463,-45.6691115795981,
-1249.29246323529));
#147657=CARTESIAN_POINT('Ctrl Pts',(-26.7427538741697,-43.1910304950644,
-1250.78658088235));
#147658=CARTESIAN_POINT('Ctrl Pts',(-30.744992244793,-40.7129494105307,
-1252.28069852941));
#147659=CARTESIAN_POINT('Ctrl Pts',(-34.2237386972451,-37.5416529948095,
-1253.77481617647));
#147660=CARTESIAN_POINT('Ctrl Pts',(-37.7024851496972,-34.3703565790883,
-1255.26893382353));
#147661=CARTESIAN_POINT('Ctrl Pts',(-40.5392751458362,-30.6138395280662,
-1256.76305147059));
#147662=CARTESIAN_POINT('Ctrl Pts',(-43.3760651419751,-26.8573224770441,
-1258.25716911765));
#147663=CARTESIAN_POINT('Ctrl Pts',(-45.4742952008371,-22.6435084734481,
-1259.75128676471));
#147664=CARTESIAN_POINT('Ctrl Pts',(-47.5725252596992,-18.4296944698521,
-1261.24540441176));
#147665=CARTESIAN_POINT('Ctrl Pts',(-48.8607426731792,-13.9020798956618,
-1262.73952205882));
#147666=CARTESIAN_POINT('Ctrl Pts',(-50.1489600866593,-9.37446532147148,
-1264.23363970588));
#147667=CARTESIAN_POINT('Ctrl Pts',(-50.5832961557877,-4.68723266073574,
-1265.72775735294));
#147668=CARTESIAN_POINT('Ctrl Pts',(-51.0176322249162,-3.12392900021603E-15,
-1267.221875));
#147669=CARTESIAN_POINT('Ctrl Pts',(-50.5832961557877,4.68723266073573,
-1268.71599264706));
#147670=CARTESIAN_POINT('Ctrl Pts',(-50.1489600866593,9.37446532147149,
-1270.21011029412));
#147671=CARTESIAN_POINT('Ctrl Pts',(-48.8607426731792,13.9020798956618,
-1271.70422794118));
#147672=CARTESIAN_POINT('Ctrl Pts',(-47.5725252596992,18.4296944698521,
-1273.19834558824));
#147673=CARTESIAN_POINT('Ctrl Pts',(-45.4742952008371,22.6435084734481,
-1274.69246323529));
#147674=CARTESIAN_POINT('Ctrl Pts',(-43.3760651419751,26.8573224770442,
-1276.18658088235));
#147675=CARTESIAN_POINT('Ctrl Pts',(-40.5392751458362,30.6138395280662,
-1277.68069852941));
#147676=CARTESIAN_POINT('Ctrl Pts',(-37.7024851496972,34.3703565790883,
-1279.17481617647));
#147677=CARTESIAN_POINT('Ctrl Pts',(-34.2237386972451,37.5416529948095,
-1280.66893382353));
#147678=CARTESIAN_POINT('Ctrl Pts',(-30.744992244793,40.7129494105307,-1282.16305147059));
#147679=CARTESIAN_POINT('Ctrl Pts',(-26.7427538741697,43.1910304950644,
-1283.65716911765));
#147680=CARTESIAN_POINT('Ctrl Pts',(-22.7405155035463,45.6691115795981,
-1285.15128676471));
#147681=CARTESIAN_POINT('Ctrl Pts',(-18.3510766423074,47.3695892537413,
-1286.64540441176));
#147682=CARTESIAN_POINT('Ctrl Pts',(-13.9616377810684,49.0700669278844,
-1288.13952205882));
#147683=CARTESIAN_POINT('Ctrl Pts',(-9.33447550508177,49.9350334639422,
-1289.63363970588));
#147684=CARTESIAN_POINT('Ctrl Pts',(-4.7073132290951,50.8,-1291.12775735294));
#147685=CARTESIAN_POINT('Ctrl Pts',(-6.22120573966855E-15,50.8,-1292.621875));
#147686=CARTESIAN_POINT('Ctrl Pts',(4.70731322909511,50.8,-1294.11599264706));
#147687=CARTESIAN_POINT('Ctrl Pts',(9.33447550508176,49.9350334639422,-1295.61011029412));
#147688=CARTESIAN_POINT('Ctrl Pts',(13.9616377810684,49.0700669278844,-1297.10422794118));
#147689=CARTESIAN_POINT('Ctrl Pts',(18.3510766423074,47.3695892537413,-1298.59834558824));
#147690=CARTESIAN_POINT('Ctrl Pts',(22.7405155035463,45.6691115795981,-1300.09246323529));
#147691=CARTESIAN_POINT('Ctrl Pts',(26.7427538741697,43.1910304950644,-1301.58658088235));
#147692=CARTESIAN_POINT('Ctrl Pts',(30.744992244793,40.7129494105307,-1303.08069852941));
#147693=CARTESIAN_POINT('Ctrl Pts',(34.2237386972451,37.5416529948095,-1304.57481617647));
#147694=CARTESIAN_POINT('Ctrl Pts',(37.7024851496972,34.3703565790883,-1306.06893382353));
#147695=CARTESIAN_POINT('Ctrl Pts',(40.5392751458362,30.6138395280662,-1307.56305147059));
#147696=CARTESIAN_POINT('Ctrl Pts',(43.3760651419751,26.8573224770442,-1309.05716911765));
#147697=CARTESIAN_POINT('Ctrl Pts',(45.4742952008372,22.6435084734481,-1310.55128676471));
#147698=CARTESIAN_POINT('Ctrl Pts',(47.5725252596992,18.4296944698521,-1312.04540441176));
#147699=CARTESIAN_POINT('Ctrl Pts',(48.8607426731792,13.9020798956618,-1313.53952205882));
#147700=CARTESIAN_POINT('Ctrl Pts',(50.1489600866593,9.37446532147146,-1315.03363970588));
#147701=CARTESIAN_POINT('Ctrl Pts',(50.5832961557877,4.68723266073574,-1316.52775735294));
#147702=CARTESIAN_POINT('Ctrl Pts',(51.0176322249162,9.37178700064808E-15,
-1318.021875));
#147703=CARTESIAN_POINT('Ctrl Pts',(50.5832961557877,-4.68723266073572,
-1319.51599264706));
#147704=CARTESIAN_POINT('Ctrl Pts',(50.1489600866593,-9.37446532147149,
-1321.01011029412));
#147705=CARTESIAN_POINT('Ctrl Pts',(48.8607426731792,-13.9020798956618,
-1322.50422794118));
#147706=CARTESIAN_POINT('Ctrl Pts',(47.5725252596992,-18.4296944698521,
-1323.99834558824));
#147707=CARTESIAN_POINT('Ctrl Pts',(45.4742952008371,-22.6435084734482,
-1325.49246323529));
#147708=CARTESIAN_POINT('Ctrl Pts',(43.3760651419751,-26.8573224770441,
-1326.98658088235));
#147709=CARTESIAN_POINT('Ctrl Pts',(40.5392751458362,-30.6138395280662,
-1328.48069852941));
#147710=CARTESIAN_POINT('Ctrl Pts',(37.7024851496972,-34.3703565790883,
-1329.97481617647));
#147711=CARTESIAN_POINT('Ctrl Pts',(34.2237386972451,-37.5416529948095,
-1331.46893382353));
#147712=CARTESIAN_POINT('Ctrl Pts',(30.744992244793,-40.7129494105307,-1332.96305147059));
#147713=CARTESIAN_POINT('Ctrl Pts',(26.7427538741697,-43.1910304950644,
-1334.45716911765));
#147714=CARTESIAN_POINT('Ctrl Pts',(22.7405155035463,-45.6691115795981,
-1335.95128676471));
#147715=CARTESIAN_POINT('Ctrl Pts',(18.3510766423074,-47.3695892537413,
-1337.44540441176));
#147716=CARTESIAN_POINT('Ctrl Pts',(13.9616377810684,-49.0700669278844,
-1338.93952205882));
#147717=CARTESIAN_POINT('Ctrl Pts',(9.33447550508176,-49.9350334639422,
-1340.43363970588));
#147718=CARTESIAN_POINT('Ctrl Pts',(4.70731322909511,-50.8,-1341.92775735294));
#147719=CARTESIAN_POINT('Ctrl Pts',(0.,-50.8,-1343.421875));
#147720=CARTESIAN_POINT('Ctrl Pts',(-4.70731322909511,-50.8,-1344.91599264706));
#147721=CARTESIAN_POINT('Ctrl Pts',(-9.33447550508177,-49.9350334639422,
-1346.41011029412));
#147722=CARTESIAN_POINT('Ctrl Pts',(-13.9616377810684,-49.0700669278844,
-1347.90422794118));
#147723=CARTESIAN_POINT('Ctrl Pts',(-18.3510766423074,-47.3695892537413,
-1349.39834558824));
#147724=CARTESIAN_POINT('Ctrl Pts',(-22.7405155035463,-45.6691115795981,
-1350.89246323529));
#147725=CARTESIAN_POINT('Ctrl Pts',(-26.7427538741697,-43.1910304950644,
-1352.38658088235));
#147726=CARTESIAN_POINT('Ctrl Pts',(-30.744992244793,-40.7129494105307,
-1353.88069852941));
#147727=CARTESIAN_POINT('Ctrl Pts',(-34.2237386972451,-37.5416529948095,
-1355.37481617647));
#147728=CARTESIAN_POINT('Ctrl Pts',(-37.7024851496972,-34.3703565790883,
-1356.86893382353));
#147729=CARTESIAN_POINT('Ctrl Pts',(-40.5392751458362,-30.6138395280662,
-1358.36305147059));
#147730=CARTESIAN_POINT('Ctrl Pts',(-43.3760651419751,-26.8573224770441,
-1359.85716911765));
#147731=CARTESIAN_POINT('Ctrl Pts',(-45.4742952008371,-22.6435084734481,
-1361.35128676471));
#147732=CARTESIAN_POINT('Ctrl Pts',(-47.5725252596992,-18.4296944698521,
-1362.84540441176));
#147733=CARTESIAN_POINT('Ctrl Pts',(-48.8607426731792,-13.9020798956618,
-1364.33952205882));
#147734=CARTESIAN_POINT('Ctrl Pts',(-50.1489600866593,-9.37446532147148,
-1365.83363970588));
#147735=CARTESIAN_POINT('Ctrl Pts',(-50.5832961557877,-4.68723266073574,
-1367.32775735294));
#147736=CARTESIAN_POINT('Ctrl Pts',(-51.0176322249162,-3.12392900021603E-15,
-1368.821875));
#147737=CARTESIAN_POINT('Ctrl Pts',(-50.5832961557877,4.68723266073573,
-1370.31599264706));
#147738=CARTESIAN_POINT('Ctrl Pts',(-50.1489600866593,9.37446532147149,
-1371.81011029412));
#147739=CARTESIAN_POINT('Ctrl Pts',(-48.8607426731792,13.9020798956618,
-1373.30422794118));
#147740=CARTESIAN_POINT('Ctrl Pts',(-47.5725252596992,18.4296944698521,
-1374.79834558824));
#147741=CARTESIAN_POINT('Ctrl Pts',(-45.4742952008371,22.6435084734481,
-1376.29246323529));
#147742=CARTESIAN_POINT('Ctrl Pts',(-43.3760651419751,26.8573224770442,
-1377.78658088235));
#147743=CARTESIAN_POINT('Ctrl Pts',(-40.5392751458362,30.6138395280662,
-1379.28069852941));
#147744=CARTESIAN_POINT('Ctrl Pts',(-37.7024851496972,34.3703565790883,
-1380.77481617647));
#147745=CARTESIAN_POINT('Ctrl Pts',(-34.2237386972451,37.5416529948095,
-1382.26893382353));
#147746=CARTESIAN_POINT('Ctrl Pts',(-30.744992244793,40.7129494105307,-1383.76305147059));
#147747=CARTESIAN_POINT('Ctrl Pts',(-26.7427538741697,43.1910304950644,
-1385.25716911765));
#147748=CARTESIAN_POINT('Ctrl Pts',(-22.7405155035463,45.6691115795981,
-1386.75128676471));
#147749=CARTESIAN_POINT('Ctrl Pts',(-18.3510766423074,47.3695892537413,
-1388.24540441176));
#147750=CARTESIAN_POINT('Ctrl Pts',(-13.9616377810684,49.0700669278844,
-1389.73952205882));
#147751=CARTESIAN_POINT('Ctrl Pts',(-9.33447550508177,49.9350334639422,
-1391.23363970588));
#147752=CARTESIAN_POINT('Ctrl Pts',(-4.7073132290951,50.8,-1392.72775735294));
#147753=CARTESIAN_POINT('Ctrl Pts',(-6.22120573966855E-15,50.8,-1394.221875));
#147754=CARTESIAN_POINT('Ctrl Pts',(4.70731322909511,50.8,-1395.71599264706));
#147755=CARTESIAN_POINT('Ctrl Pts',(9.33447550508176,49.9350334639422,-1397.21011029412));
#147756=CARTESIAN_POINT('Ctrl Pts',(13.9616377810684,49.0700669278844,-1398.70422794118));
#147757=CARTESIAN_POINT('Ctrl Pts',(18.3510766423074,47.3695892537413,-1400.19834558824));
#147758=CARTESIAN_POINT('Ctrl Pts',(22.7405155035463,45.6691115795981,-1401.69246323529));
#147759=CARTESIAN_POINT('Ctrl Pts',(26.7427538741697,43.1910304950644,-1403.18658088235));
#147760=CARTESIAN_POINT('Ctrl Pts',(30.744992244793,40.7129494105307,-1404.68069852941));
#147761=CARTESIAN_POINT('Ctrl Pts',(34.2237386972451,37.5416529948095,-1406.17481617647));
#147762=CARTESIAN_POINT('Ctrl Pts',(37.7024851496972,34.3703565790883,-1407.66893382353));
#147763=CARTESIAN_POINT('Ctrl Pts',(40.5392751458362,30.6138395280662,-1409.16305147059));
#147764=CARTESIAN_POINT('Ctrl Pts',(43.3760651419751,26.8573224770442,-1410.65716911765));
#147765=CARTESIAN_POINT('Ctrl Pts',(45.4742952008372,22.6435084734481,-1412.15128676471));
#147766=CARTESIAN_POINT('Ctrl Pts',(47.5725252596992,18.4296944698521,-1413.64540441176));
#147767=CARTESIAN_POINT('Ctrl Pts',(48.8607426731792,13.9020798956618,-1415.13952205882));
#147768=CARTESIAN_POINT('Ctrl Pts',(50.1489600866593,9.37446532147146,-1416.63363970588));
#147769=CARTESIAN_POINT('Ctrl Pts',(50.5832961557877,4.68723266073574,-1418.12775735294));
#147770=CARTESIAN_POINT('Ctrl Pts',(51.0176322249162,9.37178700064808E-15,
-1419.621875));
#147771=CARTESIAN_POINT('Ctrl Pts',(50.5832961557877,-4.68723266073572,
-1421.11599264706));
#147772=CARTESIAN_POINT('Ctrl Pts',(50.1489600866593,-9.37446532147149,
-1422.61011029412));
#147773=CARTESIAN_POINT('Ctrl Pts',(48.8607426731792,-13.9020798956618,
-1424.10422794118));
#147774=CARTESIAN_POINT('Ctrl Pts',(47.5725252596992,-18.4296944698521,
-1425.59834558824));
#147775=CARTESIAN_POINT('Ctrl Pts',(45.4742952008371,-22.6435084734482,
-1427.09246323529));
#147776=CARTESIAN_POINT('Ctrl Pts',(43.3760651419751,-26.8573224770441,
-1428.58658088235));
#147777=CARTESIAN_POINT('Ctrl Pts',(40.5392751458362,-30.6138395280662,
-1430.08069852941));
#147778=CARTESIAN_POINT('Ctrl Pts',(37.7024851496972,-34.3703565790883,
-1431.57481617647));
#147779=CARTESIAN_POINT('Ctrl Pts',(34.2237386972451,-37.5416529948095,
-1433.06893382353));
#147780=CARTESIAN_POINT('Ctrl Pts',(30.744992244793,-40.7129494105307,-1434.56305147059));
#147781=CARTESIAN_POINT('Ctrl Pts',(26.7427538741697,-43.1910304950644,
-1436.05716911765));
#147782=CARTESIAN_POINT('Ctrl Pts',(22.7405155035463,-45.6691115795981,
-1437.55128676471));
#147783=CARTESIAN_POINT('Ctrl Pts',(18.3510766423074,-47.3695892537413,
-1439.04540441176));
#147784=CARTESIAN_POINT('Ctrl Pts',(13.9616377810684,-49.0700669278844,
-1440.53952205882));
#147785=CARTESIAN_POINT('Ctrl Pts',(9.33447550508176,-49.9350334639422,
-1442.03363970588));
#147786=CARTESIAN_POINT('Ctrl Pts',(4.70731322909511,-50.8,-1443.52775735294));
#147787=CARTESIAN_POINT('Ctrl Pts',(0.,-50.8,-1445.021875));
#147788=CARTESIAN_POINT('Ctrl Pts',(-4.70731322909511,-50.8,-1446.51599264706));
#147789=CARTESIAN_POINT('Ctrl Pts',(-9.33447550508177,-49.9350334639422,
-1448.01011029412));
#147790=CARTESIAN_POINT('Ctrl Pts',(-13.9616377810684,-49.0700669278844,
-1449.50422794118));
#147791=CARTESIAN_POINT('Ctrl Pts',(-18.3510766423074,-47.3695892537413,
-1450.99834558824));
#147792=CARTESIAN_POINT('Ctrl Pts',(-22.7405155035463,-45.6691115795981,
-1452.49246323529));
#147793=CARTESIAN_POINT('Ctrl Pts',(-26.7427538741697,-43.1910304950644,
-1453.98658088235));
#147794=CARTESIAN_POINT('Ctrl Pts',(-30.744992244793,-40.7129494105307,
-1455.48069852941));
#147795=CARTESIAN_POINT('Ctrl Pts',(-34.2237386972451,-37.5416529948095,
-1456.97481617647));
#147796=CARTESIAN_POINT('Ctrl Pts',(-37.7024851496972,-34.3703565790883,
-1458.46893382353));
#147797=CARTESIAN_POINT('Ctrl Pts',(-40.5392751458362,-30.6138395280662,
-1459.96305147059));
#147798=CARTESIAN_POINT('Ctrl Pts',(-43.3760651419751,-26.8573224770441,
-1461.45716911765));
#147799=CARTESIAN_POINT('Ctrl Pts',(-45.4742952008371,-22.6435084734481,
-1462.95128676471));
#147800=CARTESIAN_POINT('Ctrl Pts',(-47.5725252596992,-18.4296944698521,
-1464.44540441176));
#147801=CARTESIAN_POINT('Ctrl Pts',(-48.8607426731792,-13.9020798956618,
-1465.93952205882));
#147802=CARTESIAN_POINT('Ctrl Pts',(-50.1489600866593,-9.37446532147148,
-1467.43363970588));
#147803=CARTESIAN_POINT('Ctrl Pts',(-50.5832961557877,-4.68723266073574,
-1468.92775735294));
#147804=CARTESIAN_POINT('Ctrl Pts',(-51.0176322249162,-3.12392900021603E-15,
-1470.421875));
#147805=CARTESIAN_POINT('Ctrl Pts',(-50.5832961557877,4.68723266073573,
-1471.91599264706));
#147806=CARTESIAN_POINT('Ctrl Pts',(-50.1489600866593,9.37446532147149,
-1473.41011029412));
#147807=CARTESIAN_POINT('Ctrl Pts',(-48.8607426731792,13.9020798956618,
-1474.90422794118));
#147808=CARTESIAN_POINT('Ctrl Pts',(-47.5725252596992,18.4296944698521,
-1476.39834558824));
#147809=CARTESIAN_POINT('Ctrl Pts',(-45.4742952008371,22.6435084734481,
-1477.89246323529));
#147810=CARTESIAN_POINT('Ctrl Pts',(-43.3760651419751,26.8573224770442,
-1479.38658088235));
#147811=CARTESIAN_POINT('Ctrl Pts',(-40.5392751458362,30.6138395280662,
-1480.88069852941));
#147812=CARTESIAN_POINT('Ctrl Pts',(-37.7024851496972,34.3703565790883,
-1482.37481617647));
#147813=CARTESIAN_POINT('Ctrl Pts',(-34.2237386972451,37.5416529948095,
-1483.86893382353));
#147814=CARTESIAN_POINT('Ctrl Pts',(-30.744992244793,40.7129494105307,-1485.36305147059));
#147815=CARTESIAN_POINT('Ctrl Pts',(-26.7427538741697,43.1910304950644,
-1486.85716911765));
#147816=CARTESIAN_POINT('Ctrl Pts',(-22.7405155035463,45.6691115795981,
-1488.35128676471));
#147817=CARTESIAN_POINT('Ctrl Pts',(-18.3510766423074,47.3695892537413,
-1489.84540441176));
#147818=CARTESIAN_POINT('Ctrl Pts',(-13.9616377810684,49.0700669278844,
-1491.33952205882));
#147819=CARTESIAN_POINT('Ctrl Pts',(-9.33447550508177,49.9350334639422,
-1492.83363970588));
#147820=CARTESIAN_POINT('Ctrl Pts',(-4.7073132290951,50.8,-1494.32775735294));
#147821=CARTESIAN_POINT('Ctrl Pts',(-6.22120573966855E-15,50.8,-1495.821875));
#147822=CARTESIAN_POINT('Ctrl Pts',(4.70731322909511,50.8,-1497.31599264706));
#147823=CARTESIAN_POINT('Ctrl Pts',(9.33447550508176,49.9350334639422,-1498.81011029412));
#147824=CARTESIAN_POINT('Ctrl Pts',(13.9616377810684,49.0700669278844,-1500.30422794118));
#147825=CARTESIAN_POINT('Ctrl Pts',(18.3510766423074,47.3695892537413,-1501.79834558824));
#147826=CARTESIAN_POINT('Ctrl Pts',(21.2268878088737,46.2554940724685,-1502.77724069292));
#147827=CARTESIAN_POINT('Ctrl Pts',(23.9468011449081,44.8016820546531,-1503.75991977561));
#147828=CARTESIAN_POINT('Ctrl Pts',(0.,-18.048,1500.28886941341));
#147829=CARTESIAN_POINT('Ctrl Pts',(-1.67239348737615,-18.048,1498.79475176635));
#147830=CARTESIAN_POINT('Ctrl Pts',(-3.31631129755346,-17.7406985030951,
1497.30063411929));
#147831=CARTESIAN_POINT('Ctrl Pts',(-4.96022910773077,-17.4333970061901,
1495.80651647223));
#147832=CARTESIAN_POINT('Ctrl Pts',(-6.51968959134574,-16.8292587962898,
1494.31239882517));
#147833=CARTESIAN_POINT('Ctrl Pts',(-8.07915007496071,-16.2251205863895,
1492.81828117811));
#147834=CARTESIAN_POINT('Ctrl Pts',(-9.50104767561052,-15.3447188656481,
1491.32416353106));
#147835=CARTESIAN_POINT('Ctrl Pts',(-10.9229452762603,-14.4643171449067,
1489.830045884));
#147836=CARTESIAN_POINT('Ctrl Pts',(-12.1588589765331,-13.3376329379985,
1488.33592823694));
#147837=CARTESIAN_POINT('Ctrl Pts',(-13.3947726768058,-12.2109487310903,
1486.84181058988));
#147838=CARTESIAN_POINT('Ctrl Pts',(-14.4026149179538,-10.8763499173728,
1485.34769294282));
#147839=CARTESIAN_POINT('Ctrl Pts',(-15.4104571591017,-9.54175110365538,
1483.85357529576));
#147840=CARTESIAN_POINT('Ctrl Pts',(-16.1559070823762,-8.04468584505497,
1482.3594576487));
#147841=CARTESIAN_POINT('Ctrl Pts',(-16.9013570056506,-6.54762058645456,
1480.86534000164));
#147842=CARTESIAN_POINT('Ctrl Pts',(-17.3590292079831,-4.93906964482095,
1479.37122235458));
#147843=CARTESIAN_POINT('Ctrl Pts',(-17.8167014103155,-3.33051870318735,
1477.87710470753));
#147844=CARTESIAN_POINT('Ctrl Pts',(-17.9710104137728,-1.66525935159368,
1476.38298706047));
#147845=CARTESIAN_POINT('Ctrl Pts',(-18.1253194172301,-1.10985572039171E-15,
1474.88886941341));
#147846=CARTESIAN_POINT('Ctrl Pts',(-17.9710104137728,1.66525935159367,
1473.39475176635));
#147847=CARTESIAN_POINT('Ctrl Pts',(-17.8167014103155,3.33051870318735,
1471.90063411929));
#147848=CARTESIAN_POINT('Ctrl Pts',(-17.3590292079831,4.93906964482096,
1470.40651647223));
#147849=CARTESIAN_POINT('Ctrl Pts',(-16.9013570056506,6.54762058645456,
1468.91239882517));
#147850=CARTESIAN_POINT('Ctrl Pts',(-16.1559070823762,8.04468584505497,
1467.41828117811));
#147851=CARTESIAN_POINT('Ctrl Pts',(-15.4104571591017,9.54175110365538,
1465.92416353106));
#147852=CARTESIAN_POINT('Ctrl Pts',(-14.4026149179538,10.8763499173728,
1464.430045884));
#147853=CARTESIAN_POINT('Ctrl Pts',(-13.3947726768058,12.2109487310903,
1462.93592823694));
#147854=CARTESIAN_POINT('Ctrl Pts',(-12.1588589765331,13.3376329379985,
1461.44181058988));
#147855=CARTESIAN_POINT('Ctrl Pts',(-10.9229452762603,14.4643171449067,
1459.94769294282));
#147856=CARTESIAN_POINT('Ctrl Pts',(-9.50104767561052,15.3447188656481,
1458.45357529576));
#147857=CARTESIAN_POINT('Ctrl Pts',(-8.07915007496071,16.2251205863895,
1456.9594576487));
#147858=CARTESIAN_POINT('Ctrl Pts',(-6.51968959134574,16.8292587962898,
1455.46534000164));
#147859=CARTESIAN_POINT('Ctrl Pts',(-4.96022910773078,17.4333970061901,
1453.97122235458));
#147860=CARTESIAN_POINT('Ctrl Pts',(-3.31631129755346,17.7406985030951,
1452.47710470753));
#147861=CARTESIAN_POINT('Ctrl Pts',(-1.67239348737615,18.048,1450.98298706047));
#147862=CARTESIAN_POINT('Ctrl Pts',(-2.21024254310115E-15,18.048,1449.48886941341));
#147863=CARTESIAN_POINT('Ctrl Pts',(1.67239348737616,18.048,1447.99475176635));
#147864=CARTESIAN_POINT('Ctrl Pts',(3.31631129755346,17.7406985030951,1446.50063411929));
#147865=CARTESIAN_POINT('Ctrl Pts',(4.96022910773077,17.4333970061901,1445.00651647223));
#147866=CARTESIAN_POINT('Ctrl Pts',(6.51968959134575,16.8292587962898,1443.51239882517));
#147867=CARTESIAN_POINT('Ctrl Pts',(8.07915007496071,16.2251205863895,1442.01828117811));
#147868=CARTESIAN_POINT('Ctrl Pts',(9.50104767561053,15.3447188656481,1440.52416353105));
#147869=CARTESIAN_POINT('Ctrl Pts',(10.9229452762603,14.4643171449067,1439.030045884));
#147870=CARTESIAN_POINT('Ctrl Pts',(12.1588589765331,13.3376329379985,1437.53592823694));
#147871=CARTESIAN_POINT('Ctrl Pts',(13.3947726768058,12.2109487310903,1436.04181058988));
#147872=CARTESIAN_POINT('Ctrl Pts',(14.4026149179538,10.8763499173728,1434.54769294282));
#147873=CARTESIAN_POINT('Ctrl Pts',(15.4104571591017,9.54175110365538,1433.05357529576));
#147874=CARTESIAN_POINT('Ctrl Pts',(16.1559070823762,8.04468584505496,1431.5594576487));
#147875=CARTESIAN_POINT('Ctrl Pts',(16.9013570056506,6.54762058645456,1430.06534000164));
#147876=CARTESIAN_POINT('Ctrl Pts',(17.3590292079831,4.93906964482096,1428.57122235458));
#147877=CARTESIAN_POINT('Ctrl Pts',(17.8167014103155,3.33051870318735,1427.07710470753));
#147878=CARTESIAN_POINT('Ctrl Pts',(17.9710104137728,1.66525935159367,1425.58298706047));
#147879=CARTESIAN_POINT('Ctrl Pts',(18.1253194172301,3.32956716117513E-15,
1424.08886941341));
#147880=CARTESIAN_POINT('Ctrl Pts',(17.9710104137728,-1.66525935159367,
1422.59475176635));
#147881=CARTESIAN_POINT('Ctrl Pts',(17.8167014103155,-3.33051870318736,
1421.10063411929));
#147882=CARTESIAN_POINT('Ctrl Pts',(17.3590292079831,-4.93906964482095,
1419.60651647223));
#147883=CARTESIAN_POINT('Ctrl Pts',(16.9013570056506,-6.54762058645456,
1418.11239882517));
#147884=CARTESIAN_POINT('Ctrl Pts',(16.1559070823762,-8.04468584505497,
1416.61828117811));
#147885=CARTESIAN_POINT('Ctrl Pts',(15.4104571591017,-9.54175110365538,
1415.12416353105));
#147886=CARTESIAN_POINT('Ctrl Pts',(14.4026149179538,-10.8763499173728,
1413.630045884));
#147887=CARTESIAN_POINT('Ctrl Pts',(13.3947726768058,-12.2109487310903,
1412.13592823694));
#147888=CARTESIAN_POINT('Ctrl Pts',(12.1588589765331,-13.3376329379985,
1410.64181058988));
#147889=CARTESIAN_POINT('Ctrl Pts',(10.9229452762603,-14.4643171449067,
1409.14769294282));
#147890=CARTESIAN_POINT('Ctrl Pts',(9.50104767561053,-15.3447188656481,
1407.65357529576));
#147891=CARTESIAN_POINT('Ctrl Pts',(8.07915007496071,-16.2251205863895,
1406.1594576487));
#147892=CARTESIAN_POINT('Ctrl Pts',(6.51968959134574,-16.8292587962898,
1404.66534000164));
#147893=CARTESIAN_POINT('Ctrl Pts',(4.96022910773078,-17.4333970061901,
1403.17122235458));
#147894=CARTESIAN_POINT('Ctrl Pts',(3.31631129755346,-17.7406985030951,
1401.67710470753));
#147895=CARTESIAN_POINT('Ctrl Pts',(1.67239348737615,-18.048,1400.18298706047));
#147896=CARTESIAN_POINT('Ctrl Pts',(0.,-18.048,1398.68886941341));
#147897=CARTESIAN_POINT('Ctrl Pts',(-1.67239348737615,-18.048,1397.19475176635));
#147898=CARTESIAN_POINT('Ctrl Pts',(-3.31631129755346,-17.7406985030951,
1395.70063411929));
#147899=CARTESIAN_POINT('Ctrl Pts',(-4.96022910773077,-17.4333970061901,
1394.20651647223));
#147900=CARTESIAN_POINT('Ctrl Pts',(-6.51968959134574,-16.8292587962898,
1392.71239882517));
#147901=CARTESIAN_POINT('Ctrl Pts',(-8.07915007496071,-16.2251205863895,
1391.21828117811));
#147902=CARTESIAN_POINT('Ctrl Pts',(-9.50104767561052,-15.3447188656481,
1389.72416353105));
#147903=CARTESIAN_POINT('Ctrl Pts',(-10.9229452762603,-14.4643171449067,
1388.230045884));
#147904=CARTESIAN_POINT('Ctrl Pts',(-12.1588589765331,-13.3376329379985,
1386.73592823694));
#147905=CARTESIAN_POINT('Ctrl Pts',(-13.3947726768058,-12.2109487310903,
1385.24181058988));
#147906=CARTESIAN_POINT('Ctrl Pts',(-14.4026149179538,-10.8763499173728,
1383.74769294282));
#147907=CARTESIAN_POINT('Ctrl Pts',(-15.4104571591017,-9.54175110365538,
1382.25357529576));
#147908=CARTESIAN_POINT('Ctrl Pts',(-16.1559070823762,-8.04468584505497,
1380.7594576487));
#147909=CARTESIAN_POINT('Ctrl Pts',(-16.9013570056506,-6.54762058645456,
1379.26534000164));
#147910=CARTESIAN_POINT('Ctrl Pts',(-17.3590292079831,-4.93906964482095,
1377.77122235458));
#147911=CARTESIAN_POINT('Ctrl Pts',(-17.8167014103155,-3.33051870318735,
1376.27710470753));
#147912=CARTESIAN_POINT('Ctrl Pts',(-17.9710104137728,-1.66525935159368,
1374.78298706047));
#147913=CARTESIAN_POINT('Ctrl Pts',(-18.1253194172301,-1.10985572039171E-15,
1373.28886941341));
#147914=CARTESIAN_POINT('Ctrl Pts',(-17.9710104137728,1.66525935159367,
1371.79475176635));
#147915=CARTESIAN_POINT('Ctrl Pts',(-17.8167014103155,3.33051870318735,
1370.30063411929));
#147916=CARTESIAN_POINT('Ctrl Pts',(-17.3590292079831,4.93906964482096,
1368.80651647223));
#147917=CARTESIAN_POINT('Ctrl Pts',(-16.9013570056506,6.54762058645456,
1367.31239882517));
#147918=CARTESIAN_POINT('Ctrl Pts',(-16.1559070823762,8.04468584505497,
1365.81828117811));
#147919=CARTESIAN_POINT('Ctrl Pts',(-15.4104571591017,9.54175110365538,
1364.32416353105));
#147920=CARTESIAN_POINT('Ctrl Pts',(-14.4026149179538,10.8763499173728,
1362.830045884));
#147921=CARTESIAN_POINT('Ctrl Pts',(-13.3947726768058,12.2109487310903,
1361.33592823694));
#147922=CARTESIAN_POINT('Ctrl Pts',(-12.1588589765331,13.3376329379985,
1359.84181058988));
#147923=CARTESIAN_POINT('Ctrl Pts',(-10.9229452762603,14.4643171449067,
1358.34769294282));
#147924=CARTESIAN_POINT('Ctrl Pts',(-9.50104767561052,15.3447188656481,
1356.85357529576));
#147925=CARTESIAN_POINT('Ctrl Pts',(-8.07915007496071,16.2251205863895,
1355.3594576487));
#147926=CARTESIAN_POINT('Ctrl Pts',(-6.51968959134574,16.8292587962898,
1353.86534000164));
#147927=CARTESIAN_POINT('Ctrl Pts',(-4.96022910773078,17.4333970061901,
1352.37122235458));
#147928=CARTESIAN_POINT('Ctrl Pts',(-3.31631129755346,17.7406985030951,
1350.87710470753));
#147929=CARTESIAN_POINT('Ctrl Pts',(-1.67239348737615,18.048,1349.38298706047));
#147930=CARTESIAN_POINT('Ctrl Pts',(-2.21024254310115E-15,18.048,1347.88886941341));
#147931=CARTESIAN_POINT('Ctrl Pts',(1.67239348737616,18.048,1346.39475176635));
#147932=CARTESIAN_POINT('Ctrl Pts',(3.31631129755346,17.7406985030951,1344.90063411929));
#147933=CARTESIAN_POINT('Ctrl Pts',(4.96022910773077,17.4333970061901,1343.40651647223));
#147934=CARTESIAN_POINT('Ctrl Pts',(6.51968959134575,16.8292587962898,1341.91239882517));
#147935=CARTESIAN_POINT('Ctrl Pts',(8.07915007496071,16.2251205863895,1340.41828117811));
#147936=CARTESIAN_POINT('Ctrl Pts',(9.50104767561053,15.3447188656481,1338.92416353106));
#147937=CARTESIAN_POINT('Ctrl Pts',(10.9229452762603,14.4643171449067,1337.430045884));
#147938=CARTESIAN_POINT('Ctrl Pts',(12.1588589765331,13.3376329379985,1335.93592823694));
#147939=CARTESIAN_POINT('Ctrl Pts',(13.3947726768058,12.2109487310903,1334.44181058988));
#147940=CARTESIAN_POINT('Ctrl Pts',(14.4026149179538,10.8763499173728,1332.94769294282));
#147941=CARTESIAN_POINT('Ctrl Pts',(15.4104571591017,9.54175110365538,1331.45357529576));
#147942=CARTESIAN_POINT('Ctrl Pts',(16.1559070823762,8.04468584505496,1329.9594576487));
#147943=CARTESIAN_POINT('Ctrl Pts',(16.9013570056506,6.54762058645456,1328.46534000164));
#147944=CARTESIAN_POINT('Ctrl Pts',(17.3590292079831,4.93906964482096,1326.97122235458));
#147945=CARTESIAN_POINT('Ctrl Pts',(17.8167014103155,3.33051870318735,1325.47710470753));
#147946=CARTESIAN_POINT('Ctrl Pts',(17.9710104137728,1.66525935159367,1323.98298706047));
#147947=CARTESIAN_POINT('Ctrl Pts',(18.1253194172301,3.32956716117513E-15,
1322.48886941341));
#147948=CARTESIAN_POINT('Ctrl Pts',(17.9710104137728,-1.66525935159367,
1320.99475176635));
#147949=CARTESIAN_POINT('Ctrl Pts',(17.8167014103155,-3.33051870318736,
1319.50063411929));
#147950=CARTESIAN_POINT('Ctrl Pts',(17.3590292079831,-4.93906964482095,
1318.00651647223));
#147951=CARTESIAN_POINT('Ctrl Pts',(16.9013570056506,-6.54762058645456,
1316.51239882517));
#147952=CARTESIAN_POINT('Ctrl Pts',(16.1559070823762,-8.04468584505497,
1315.01828117811));
#147953=CARTESIAN_POINT('Ctrl Pts',(15.4104571591017,-9.54175110365538,
1313.52416353105));
#147954=CARTESIAN_POINT('Ctrl Pts',(14.4026149179538,-10.8763499173728,
1312.030045884));
#147955=CARTESIAN_POINT('Ctrl Pts',(13.3947726768058,-12.2109487310903,
1310.53592823694));
#147956=CARTESIAN_POINT('Ctrl Pts',(12.1588589765331,-13.3376329379985,
1309.04181058988));
#147957=CARTESIAN_POINT('Ctrl Pts',(10.9229452762603,-14.4643171449067,
1307.54769294282));
#147958=CARTESIAN_POINT('Ctrl Pts',(9.50104767561053,-15.3447188656481,
1306.05357529576));
#147959=CARTESIAN_POINT('Ctrl Pts',(8.07915007496071,-16.2251205863895,
1304.5594576487));
#147960=CARTESIAN_POINT('Ctrl Pts',(6.51968959134574,-16.8292587962898,
1303.06534000164));
#147961=CARTESIAN_POINT('Ctrl Pts',(4.96022910773078,-17.4333970061901,
1301.57122235458));
#147962=CARTESIAN_POINT('Ctrl Pts',(3.31631129755346,-17.7406985030951,
1300.07710470753));
#147963=CARTESIAN_POINT('Ctrl Pts',(1.67239348737615,-18.048,1298.58298706047));
#147964=CARTESIAN_POINT('Ctrl Pts',(0.,-18.048,1297.08886941341));
#147965=CARTESIAN_POINT('Ctrl Pts',(-1.67239348737615,-18.048,1295.59475176635));
#147966=CARTESIAN_POINT('Ctrl Pts',(-3.31631129755346,-17.7406985030951,
1294.10063411929));
#147967=CARTESIAN_POINT('Ctrl Pts',(-4.96022910773077,-17.4333970061901,
1292.60651647223));
#147968=CARTESIAN_POINT('Ctrl Pts',(-6.51968959134574,-16.8292587962898,
1291.11239882517));
#147969=CARTESIAN_POINT('Ctrl Pts',(-8.07915007496071,-16.2251205863895,
1289.61828117811));
#147970=CARTESIAN_POINT('Ctrl Pts',(-9.50104767561052,-15.3447188656481,
1288.12416353105));
#147971=CARTESIAN_POINT('Ctrl Pts',(-10.9229452762603,-14.4643171449067,
1286.630045884));
#147972=CARTESIAN_POINT('Ctrl Pts',(-12.1588589765331,-13.3376329379985,
1285.13592823694));
#147973=CARTESIAN_POINT('Ctrl Pts',(-13.3947726768058,-12.2109487310903,
1283.64181058988));
#147974=CARTESIAN_POINT('Ctrl Pts',(-14.4026149179538,-10.8763499173728,
1282.14769294282));
#147975=CARTESIAN_POINT('Ctrl Pts',(-15.4104571591017,-9.54175110365538,
1280.65357529576));
#147976=CARTESIAN_POINT('Ctrl Pts',(-16.1559070823762,-8.04468584505497,
1279.1594576487));
#147977=CARTESIAN_POINT('Ctrl Pts',(-16.9013570056506,-6.54762058645456,
1277.66534000164));
#147978=CARTESIAN_POINT('Ctrl Pts',(-17.3590292079831,-4.93906964482095,
1276.17122235458));
#147979=CARTESIAN_POINT('Ctrl Pts',(-17.8167014103155,-3.33051870318735,
1274.67710470753));
#147980=CARTESIAN_POINT('Ctrl Pts',(-17.9710104137728,-1.66525935159368,
1273.18298706047));
#147981=CARTESIAN_POINT('Ctrl Pts',(-18.1253194172301,-1.10985572039171E-15,
1271.68886941341));
#147982=CARTESIAN_POINT('Ctrl Pts',(-17.9710104137728,1.66525935159367,
1270.19475176635));
#147983=CARTESIAN_POINT('Ctrl Pts',(-17.8167014103155,3.33051870318735,
1268.70063411929));
#147984=CARTESIAN_POINT('Ctrl Pts',(-17.3590292079831,4.93906964482096,
1267.20651647223));
#147985=CARTESIAN_POINT('Ctrl Pts',(-16.9013570056506,6.54762058645456,
1265.71239882517));
#147986=CARTESIAN_POINT('Ctrl Pts',(-16.1559070823762,8.04468584505497,
1264.21828117811));
#147987=CARTESIAN_POINT('Ctrl Pts',(-15.4104571591017,9.54175110365538,
1262.72416353105));
#147988=CARTESIAN_POINT('Ctrl Pts',(-14.4026149179538,10.8763499173728,
1261.230045884));
#147989=CARTESIAN_POINT('Ctrl Pts',(-13.3947726768058,12.2109487310903,
1259.73592823694));
#147990=CARTESIAN_POINT('Ctrl Pts',(-12.1588589765331,13.3376329379985,
1258.24181058988));
#147991=CARTESIAN_POINT('Ctrl Pts',(-10.9229452762603,14.4643171449067,
1256.74769294282));
#147992=CARTESIAN_POINT('Ctrl Pts',(-9.50104767561052,15.3447188656481,
1255.25357529576));
#147993=CARTESIAN_POINT('Ctrl Pts',(-8.07915007496071,16.2251205863895,
1253.7594576487));
#147994=CARTESIAN_POINT('Ctrl Pts',(-6.51968959134574,16.8292587962898,
1252.26534000164));
#147995=CARTESIAN_POINT('Ctrl Pts',(-4.96022910773078,17.4333970061901,
1250.77122235458));
#147996=CARTESIAN_POINT('Ctrl Pts',(-3.31631129755346,17.7406985030951,
1249.27710470753));
#147997=CARTESIAN_POINT('Ctrl Pts',(-1.67239348737615,18.048,1247.78298706047));
#147998=CARTESIAN_POINT('Ctrl Pts',(-2.21024254310115E-15,18.048,1246.28886941341));
#147999=CARTESIAN_POINT('Ctrl Pts',(1.67239348737616,18.048,1244.79475176635));
#148000=CARTESIAN_POINT('Ctrl Pts',(3.31631129755346,17.7406985030951,1243.30063411929));
#148001=CARTESIAN_POINT('Ctrl Pts',(4.96022910773077,17.4333970061901,1241.80651647223));
#148002=CARTESIAN_POINT('Ctrl Pts',(6.51968959134575,16.8292587962898,1240.31239882517));
#148003=CARTESIAN_POINT('Ctrl Pts',(8.07915007496071,16.2251205863895,1238.81828117811));
#148004=CARTESIAN_POINT('Ctrl Pts',(9.50104767561053,15.3447188656481,1237.32416353105));
#148005=CARTESIAN_POINT('Ctrl Pts',(10.9229452762603,14.4643171449067,1235.830045884));
#148006=CARTESIAN_POINT('Ctrl Pts',(12.1588589765331,13.3376329379985,1234.33592823694));
#148007=CARTESIAN_POINT('Ctrl Pts',(13.3947726768058,12.2109487310903,1232.84181058988));
#148008=CARTESIAN_POINT('Ctrl Pts',(14.4026149179538,10.8763499173728,1231.34769294282));
#148009=CARTESIAN_POINT('Ctrl Pts',(15.4104571591017,9.54175110365538,1229.85357529576));
#148010=CARTESIAN_POINT('Ctrl Pts',(16.1559070823762,8.04468584505496,1228.3594576487));
#148011=CARTESIAN_POINT('Ctrl Pts',(16.9013570056506,6.54762058645456,1226.86534000164));
#148012=CARTESIAN_POINT('Ctrl Pts',(17.3590292079831,4.93906964482096,1225.37122235458));
#148013=CARTESIAN_POINT('Ctrl Pts',(17.8167014103155,3.33051870318735,1223.87710470753));
#148014=CARTESIAN_POINT('Ctrl Pts',(17.9710104137728,1.66525935159367,1222.38298706047));
#148015=CARTESIAN_POINT('Ctrl Pts',(18.1253194172301,3.32956716117513E-15,
1220.88886941341));
#148016=CARTESIAN_POINT('Ctrl Pts',(17.9710104137728,-1.66525935159367,
1219.39475176635));
#148017=CARTESIAN_POINT('Ctrl Pts',(17.8167014103155,-3.33051870318736,
1217.90063411929));
#148018=CARTESIAN_POINT('Ctrl Pts',(17.3590292079831,-4.93906964482095,
1216.40651647223));
#148019=CARTESIAN_POINT('Ctrl Pts',(16.9013570056506,-6.54762058645456,
1214.91239882517));
#148020=CARTESIAN_POINT('Ctrl Pts',(16.1559070823762,-8.04468584505497,
1213.41828117811));
#148021=CARTESIAN_POINT('Ctrl Pts',(15.4104571591017,-9.54175110365538,
1211.92416353105));
#148022=CARTESIAN_POINT('Ctrl Pts',(14.4026149179538,-10.8763499173728,
1210.430045884));
#148023=CARTESIAN_POINT('Ctrl Pts',(13.3947726768058,-12.2109487310903,
1208.93592823694));
#148024=CARTESIAN_POINT('Ctrl Pts',(12.1588589765331,-13.3376329379985,
1207.44181058988));
#148025=CARTESIAN_POINT('Ctrl Pts',(10.9229452762603,-14.4643171449067,
1205.94769294282));
#148026=CARTESIAN_POINT('Ctrl Pts',(9.50104767561053,-15.3447188656481,
1204.45357529576));
#148027=CARTESIAN_POINT('Ctrl Pts',(8.07915007496071,-16.2251205863895,
1202.9594576487));
#148028=CARTESIAN_POINT('Ctrl Pts',(6.51968959134574,-16.8292587962898,
1201.46534000164));
#148029=CARTESIAN_POINT('Ctrl Pts',(4.96022910773078,-17.4333970061901,
1199.97122235458));
#148030=CARTESIAN_POINT('Ctrl Pts',(3.31631129755346,-17.7406985030951,
1198.47710470753));
#148031=CARTESIAN_POINT('Ctrl Pts',(1.67239348737615,-18.048,1196.98298706047));
#148032=CARTESIAN_POINT('Ctrl Pts',(0.,-18.048,1195.48886941341));
#148033=CARTESIAN_POINT('Ctrl Pts',(-1.67239348737615,-18.048,1193.99475176635));
#148034=CARTESIAN_POINT('Ctrl Pts',(-3.31631129755346,-17.7406985030951,
1192.50063411929));
#148035=CARTESIAN_POINT('Ctrl Pts',(-4.96022910773077,-17.4333970061901,
1191.00651647223));
#148036=CARTESIAN_POINT('Ctrl Pts',(-6.51968959134574,-16.8292587962898,
1189.51239882517));
#148037=CARTESIAN_POINT('Ctrl Pts',(-8.07915007496071,-16.2251205863895,
1188.01828117811));
#148038=CARTESIAN_POINT('Ctrl Pts',(-9.50104767561052,-15.3447188656481,
1186.52416353105));
#148039=CARTESIAN_POINT('Ctrl Pts',(-10.9229452762603,-14.4643171449067,
1185.030045884));
#148040=CARTESIAN_POINT('Ctrl Pts',(-12.1588589765331,-13.3376329379985,
1183.53592823694));
#148041=CARTESIAN_POINT('Ctrl Pts',(-13.3947726768058,-12.2109487310903,
1182.04181058988));
#148042=CARTESIAN_POINT('Ctrl Pts',(-14.4026149179538,-10.8763499173728,
1180.54769294282));
#148043=CARTESIAN_POINT('Ctrl Pts',(-15.4104571591017,-9.54175110365538,
1179.05357529576));
#148044=CARTESIAN_POINT('Ctrl Pts',(-16.1559070823762,-8.04468584505497,
1177.5594576487));
#148045=CARTESIAN_POINT('Ctrl Pts',(-16.9013570056506,-6.54762058645456,
1176.06534000164));
#148046=CARTESIAN_POINT('Ctrl Pts',(-17.3590292079831,-4.93906964482095,
1174.57122235458));
#148047=CARTESIAN_POINT('Ctrl Pts',(-17.8167014103155,-3.33051870318735,
1173.07710470753));
#148048=CARTESIAN_POINT('Ctrl Pts',(-17.9710104137728,-1.66525935159368,
1171.58298706047));
#148049=CARTESIAN_POINT('Ctrl Pts',(-18.1253194172301,-1.10985572039171E-15,
1170.08886941341));
#148050=CARTESIAN_POINT('Ctrl Pts',(-17.9710104137728,1.66525935159367,
1168.59475176635));
#148051=CARTESIAN_POINT('Ctrl Pts',(-17.8167014103155,3.33051870318735,
1167.10063411929));
#148052=CARTESIAN_POINT('Ctrl Pts',(-17.3590292079831,4.93906964482096,
1165.60651647223));
#148053=CARTESIAN_POINT('Ctrl Pts',(-16.9013570056506,6.54762058645456,
1164.11239882517));
#148054=CARTESIAN_POINT('Ctrl Pts',(-16.1559070823762,8.04468584505497,
1162.61828117811));
#148055=CARTESIAN_POINT('Ctrl Pts',(-15.4104571591017,9.54175110365538,
1161.12416353106));
#148056=CARTESIAN_POINT('Ctrl Pts',(-14.4026149179538,10.8763499173728,
1159.630045884));
#148057=CARTESIAN_POINT('Ctrl Pts',(-13.3947726768058,12.2109487310903,
1158.13592823694));
#148058=CARTESIAN_POINT('Ctrl Pts',(-12.1588589765331,13.3376329379985,
1156.64181058988));
#148059=CARTESIAN_POINT('Ctrl Pts',(-10.9229452762603,14.4643171449067,
1155.14769294282));
#148060=CARTESIAN_POINT('Ctrl Pts',(-9.50104767561052,15.3447188656481,
1153.65357529576));
#148061=CARTESIAN_POINT('Ctrl Pts',(-8.07915007496071,16.2251205863895,
1152.1594576487));
#148062=CARTESIAN_POINT('Ctrl Pts',(-6.51968959134574,16.8292587962898,
1150.66534000164));
#148063=CARTESIAN_POINT('Ctrl Pts',(-4.96022910773078,17.4333970061901,
1149.17122235458));
#148064=CARTESIAN_POINT('Ctrl Pts',(-3.31631129755346,17.7406985030951,
1147.67710470753));
#148065=CARTESIAN_POINT('Ctrl Pts',(-1.67239348737615,18.048,1146.18298706047));
#148066=CARTESIAN_POINT('Ctrl Pts',(-2.21024254310115E-15,18.048,1144.68886941341));
#148067=CARTESIAN_POINT('Ctrl Pts',(1.67239348737616,18.048,1143.19475176635));
#148068=CARTESIAN_POINT('Ctrl Pts',(3.31631129755346,17.7406985030951,1141.70063411929));
#148069=CARTESIAN_POINT('Ctrl Pts',(4.96022910773077,17.4333970061901,1140.20651647223));
#148070=CARTESIAN_POINT('Ctrl Pts',(6.51968959134575,16.8292587962898,1138.71239882517));
#148071=CARTESIAN_POINT('Ctrl Pts',(8.07915007496071,16.2251205863895,1137.21828117811));
#148072=CARTESIAN_POINT('Ctrl Pts',(9.50104767561053,15.3447188656481,1135.72416353105));
#148073=CARTESIAN_POINT('Ctrl Pts',(10.9229452762603,14.4643171449067,1134.230045884));
#148074=CARTESIAN_POINT('Ctrl Pts',(12.1588589765331,13.3376329379985,1132.73592823694));
#148075=CARTESIAN_POINT('Ctrl Pts',(13.3947726768058,12.2109487310903,1131.24181058988));
#148076=CARTESIAN_POINT('Ctrl Pts',(14.4026149179538,10.8763499173728,1129.74769294282));
#148077=CARTESIAN_POINT('Ctrl Pts',(15.4104571591017,9.54175110365538,1128.25357529576));
#148078=CARTESIAN_POINT('Ctrl Pts',(16.1559070823762,8.04468584505496,1126.7594576487));
#148079=CARTESIAN_POINT('Ctrl Pts',(16.9013570056506,6.54762058645456,1125.26534000164));
#148080=CARTESIAN_POINT('Ctrl Pts',(17.3590292079831,4.93906964482096,1123.77122235458));
#148081=CARTESIAN_POINT('Ctrl Pts',(17.8167014103155,3.33051870318735,1122.27710470753));
#148082=CARTESIAN_POINT('Ctrl Pts',(17.9710104137728,1.66525935159367,1120.78298706047));
#148083=CARTESIAN_POINT('Ctrl Pts',(18.1253194172301,3.32956716117513E-15,
1119.28886941341));
#148084=CARTESIAN_POINT('Ctrl Pts',(17.9710104137728,-1.66525935159367,
1117.79475176635));
#148085=CARTESIAN_POINT('Ctrl Pts',(17.8167014103155,-3.33051870318736,
1116.30063411929));
#148086=CARTESIAN_POINT('Ctrl Pts',(17.3590292079831,-4.93906964482095,
1114.80651647223));
#148087=CARTESIAN_POINT('Ctrl Pts',(16.9013570056506,-6.54762058645456,
1113.31239882517));
#148088=CARTESIAN_POINT('Ctrl Pts',(16.1559070823762,-8.04468584505497,
1111.81828117811));
#148089=CARTESIAN_POINT('Ctrl Pts',(15.4104571591017,-9.54175110365538,
1110.32416353105));
#148090=CARTESIAN_POINT('Ctrl Pts',(14.4026149179538,-10.8763499173728,
1108.830045884));
#148091=CARTESIAN_POINT('Ctrl Pts',(13.3947726768058,-12.2109487310903,
1107.33592823694));
#148092=CARTESIAN_POINT('Ctrl Pts',(12.1588589765331,-13.3376329379985,
1105.84181058988));
#148093=CARTESIAN_POINT('Ctrl Pts',(10.9229452762603,-14.4643171449067,
1104.34769294282));
#148094=CARTESIAN_POINT('Ctrl Pts',(9.50104767561053,-15.3447188656481,
1102.85357529576));
#148095=CARTESIAN_POINT('Ctrl Pts',(8.07915007496071,-16.2251205863895,
1101.3594576487));
#148096=CARTESIAN_POINT('Ctrl Pts',(6.51968959134574,-16.8292587962898,
1099.86534000164));
#148097=CARTESIAN_POINT('Ctrl Pts',(4.96022910773078,-17.4333970061901,
1098.37122235458));
#148098=CARTESIAN_POINT('Ctrl Pts',(3.31631129755346,-17.7406985030951,
1096.87710470753));
#148099=CARTESIAN_POINT('Ctrl Pts',(1.67239348737615,-18.048,1095.38298706047));
#148100=CARTESIAN_POINT('Ctrl Pts',(0.,-18.048,1093.88886941341));
#148101=CARTESIAN_POINT('Ctrl Pts',(-1.67239348737615,-18.048,1092.39475176635));
#148102=CARTESIAN_POINT('Ctrl Pts',(-3.31631129755346,-17.7406985030951,
1090.90063411929));
#148103=CARTESIAN_POINT('Ctrl Pts',(-4.96022910773077,-17.4333970061901,
1089.40651647223));
#148104=CARTESIAN_POINT('Ctrl Pts',(-6.51968959134574,-16.8292587962898,
1087.91239882517));
#148105=CARTESIAN_POINT('Ctrl Pts',(-8.07915007496071,-16.2251205863895,
1086.41828117811));
#148106=CARTESIAN_POINT('Ctrl Pts',(-9.50104767561052,-15.3447188656481,
1084.92416353106));
#148107=CARTESIAN_POINT('Ctrl Pts',(-10.9229452762603,-14.4643171449067,
1083.430045884));
#148108=CARTESIAN_POINT('Ctrl Pts',(-12.1588589765331,-13.3376329379985,
1081.93592823694));
#148109=CARTESIAN_POINT('Ctrl Pts',(-13.3947726768058,-12.2109487310903,
1080.44181058988));
#148110=CARTESIAN_POINT('Ctrl Pts',(-14.4026149179538,-10.8763499173728,
1078.94769294282));
#148111=CARTESIAN_POINT('Ctrl Pts',(-15.4104571591017,-9.54175110365538,
1077.45357529576));
#148112=CARTESIAN_POINT('Ctrl Pts',(-16.1559070823762,-8.04468584505497,
1075.9594576487));
#148113=CARTESIAN_POINT('Ctrl Pts',(-16.9013570056506,-6.54762058645456,
1074.46534000164));
#148114=CARTESIAN_POINT('Ctrl Pts',(-17.3590292079831,-4.93906964482095,
1072.97122235458));
#148115=CARTESIAN_POINT('Ctrl Pts',(-17.8167014103155,-3.33051870318735,
1071.47710470753));
#148116=CARTESIAN_POINT('Ctrl Pts',(-17.9710104137728,-1.66525935159368,
1069.98298706047));
#148117=CARTESIAN_POINT('Ctrl Pts',(-18.1253194172301,-1.10985572039171E-15,
1068.48886941341));
#148118=CARTESIAN_POINT('Ctrl Pts',(-17.9710104137728,1.66525935159367,
1066.99475176635));
#148119=CARTESIAN_POINT('Ctrl Pts',(-17.8167014103155,3.33051870318735,
1065.50063411929));
#148120=CARTESIAN_POINT('Ctrl Pts',(-17.3590292079831,4.93906964482096,
1064.00651647223));
#148121=CARTESIAN_POINT('Ctrl Pts',(-16.9013570056506,6.54762058645456,
1062.51239882517));
#148122=CARTESIAN_POINT('Ctrl Pts',(-16.1559070823762,8.04468584505497,
1061.01828117811));
#148123=CARTESIAN_POINT('Ctrl Pts',(-15.4104571591017,9.54175110365538,
1059.52416353105));
#148124=CARTESIAN_POINT('Ctrl Pts',(-14.4026149179538,10.8763499173728,
1058.030045884));
#148125=CARTESIAN_POINT('Ctrl Pts',(-13.3947726768058,12.2109487310903,
1056.53592823694));
#148126=CARTESIAN_POINT('Ctrl Pts',(-12.1588589765331,13.3376329379985,
1055.04181058988));
#148127=CARTESIAN_POINT('Ctrl Pts',(-10.9229452762603,14.4643171449067,
1053.54769294282));
#148128=CARTESIAN_POINT('Ctrl Pts',(-9.50104767561052,15.3447188656481,
1052.05357529576));
#148129=CARTESIAN_POINT('Ctrl Pts',(-8.07915007496071,16.2251205863895,
1050.5594576487));
#148130=CARTESIAN_POINT('Ctrl Pts',(-6.51968959134574,16.8292587962898,
1049.06534000164));
#148131=CARTESIAN_POINT('Ctrl Pts',(-4.96022910773078,17.4333970061901,
1047.57122235458));
#148132=CARTESIAN_POINT('Ctrl Pts',(-3.31631129755346,17.7406985030951,
1046.07710470753));
#148133=CARTESIAN_POINT('Ctrl Pts',(-1.67239348737615,18.048,1044.58298706047));
#148134=CARTESIAN_POINT('Ctrl Pts',(-2.21024254310115E-15,18.048,1043.08886941341));
#148135=CARTESIAN_POINT('Ctrl Pts',(1.67239348737616,18.048,1041.59475176635));
#148136=CARTESIAN_POINT('Ctrl Pts',(3.31631129755346,17.7406985030951,1040.10063411929));
#148137=CARTESIAN_POINT('Ctrl Pts',(4.96022910773077,17.4333970061901,1038.60651647223));
#148138=CARTESIAN_POINT('Ctrl Pts',(6.51968959134575,16.8292587962898,1037.11239882517));
#148139=CARTESIAN_POINT('Ctrl Pts',(8.07915007496071,16.2251205863895,1035.61828117811));
#148140=CARTESIAN_POINT('Ctrl Pts',(9.50104767561053,15.3447188656481,1034.12416353105));
#148141=CARTESIAN_POINT('Ctrl Pts',(10.9229452762603,14.4643171449067,1032.630045884));
#148142=CARTESIAN_POINT('Ctrl Pts',(12.1588589765331,13.3376329379985,1031.13592823694));
#148143=CARTESIAN_POINT('Ctrl Pts',(13.3947726768058,12.2109487310903,1029.64181058988));
#148144=CARTESIAN_POINT('Ctrl Pts',(14.4026149179538,10.8763499173728,1028.14769294282));
#148145=CARTESIAN_POINT('Ctrl Pts',(15.4104571591017,9.54175110365538,1026.65357529576));
#148146=CARTESIAN_POINT('Ctrl Pts',(16.1559070823762,8.04468584505496,1025.1594576487));
#148147=CARTESIAN_POINT('Ctrl Pts',(16.9013570056506,6.54762058645456,1023.66534000164));
#148148=CARTESIAN_POINT('Ctrl Pts',(17.3590292079831,4.93906964482096,1022.17122235458));
#148149=CARTESIAN_POINT('Ctrl Pts',(17.8167014103155,3.33051870318735,1020.67710470753));
#148150=CARTESIAN_POINT('Ctrl Pts',(17.9710104137728,1.66525935159367,1019.18298706047));
#148151=CARTESIAN_POINT('Ctrl Pts',(18.1253194172301,3.32956716117513E-15,
1017.68886941341));
#148152=CARTESIAN_POINT('Ctrl Pts',(17.9710104137728,-1.66525935159367,
1016.19475176635));
#148153=CARTESIAN_POINT('Ctrl Pts',(17.8167014103155,-3.33051870318736,
1014.70063411929));
#148154=CARTESIAN_POINT('Ctrl Pts',(17.3590292079831,-4.93906964482095,
1013.20651647223));
#148155=CARTESIAN_POINT('Ctrl Pts',(16.9013570056506,-6.54762058645456,
1011.71239882517));
#148156=CARTESIAN_POINT('Ctrl Pts',(16.1559070823762,-8.04468584505497,
1010.21828117811));
#148157=CARTESIAN_POINT('Ctrl Pts',(15.4104571591017,-9.54175110365538,
1008.72416353105));
#148158=CARTESIAN_POINT('Ctrl Pts',(14.4026149179538,-10.8763499173728,
1007.230045884));
#148159=CARTESIAN_POINT('Ctrl Pts',(13.3947726768058,-12.2109487310903,
1005.73592823694));
#148160=CARTESIAN_POINT('Ctrl Pts',(12.1588589765331,-13.3376329379985,
1004.24181058988));
#148161=CARTESIAN_POINT('Ctrl Pts',(10.9229452762603,-14.4643171449067,
1002.74769294282));
#148162=CARTESIAN_POINT('Ctrl Pts',(9.50104767561053,-15.3447188656481,
1001.25357529576));
#148163=CARTESIAN_POINT('Ctrl Pts',(8.07915007496071,-16.2251205863895,
999.759457648702));
#148164=CARTESIAN_POINT('Ctrl Pts',(6.51968959134574,-16.8292587962898,
998.265340001643));
#148165=CARTESIAN_POINT('Ctrl Pts',(4.96022910773078,-17.4333970061901,
996.771222354585));
#148166=CARTESIAN_POINT('Ctrl Pts',(3.31631129755346,-17.7406985030951,
995.277104707525));
#148167=CARTESIAN_POINT('Ctrl Pts',(1.67239348737615,-18.048,993.782987060467));
#148168=CARTESIAN_POINT('Ctrl Pts',(0.,-18.048,992.288869413408));
#148169=CARTESIAN_POINT('Ctrl Pts',(-1.67239348737615,-18.048,990.794751766349));
#148170=CARTESIAN_POINT('Ctrl Pts',(-3.31631129755346,-17.7406985030951,
989.30063411929));
#148171=CARTESIAN_POINT('Ctrl Pts',(-4.96022910773077,-17.4333970061901,
987.806516472232));
#148172=CARTESIAN_POINT('Ctrl Pts',(-6.51968959134574,-16.8292587962898,
986.312398825173));
#148173=CARTESIAN_POINT('Ctrl Pts',(-8.07915007496071,-16.2251205863895,
984.818281178114));
#148174=CARTESIAN_POINT('Ctrl Pts',(-9.50104767561052,-15.3447188656481,
983.324163531055));
#148175=CARTESIAN_POINT('Ctrl Pts',(-10.9229452762603,-14.4643171449067,
981.830045883996));
#148176=CARTESIAN_POINT('Ctrl Pts',(-12.1588589765331,-13.3376329379985,
980.335928236937));
#148177=CARTESIAN_POINT('Ctrl Pts',(-13.3947726768058,-12.2109487310903,
978.841810589878));
#148178=CARTESIAN_POINT('Ctrl Pts',(-14.4026149179538,-10.8763499173728,
977.34769294282));
#148179=CARTESIAN_POINT('Ctrl Pts',(-15.4104571591017,-9.54175110365538,
975.853575295761));
#148180=CARTESIAN_POINT('Ctrl Pts',(-16.1559070823762,-8.04468584505497,
974.359457648702));
#148181=CARTESIAN_POINT('Ctrl Pts',(-16.9013570056506,-6.54762058645456,
972.865340001643));
#148182=CARTESIAN_POINT('Ctrl Pts',(-17.3590292079831,-4.93906964482095,
971.371222354584));
#148183=CARTESIAN_POINT('Ctrl Pts',(-17.8167014103155,-3.33051870318735,
969.877104707525));
#148184=CARTESIAN_POINT('Ctrl Pts',(-17.9710104137728,-1.66525935159368,
968.382987060467));
#148185=CARTESIAN_POINT('Ctrl Pts',(-18.1253194172301,-1.10985572039171E-15,
966.888869413408));
#148186=CARTESIAN_POINT('Ctrl Pts',(-17.9710104137728,1.66525935159367,
965.394751766349));
#148187=CARTESIAN_POINT('Ctrl Pts',(-17.8167014103155,3.33051870318735,
963.90063411929));
#148188=CARTESIAN_POINT('Ctrl Pts',(-17.3590292079831,4.93906964482096,
962.406516472231));
#148189=CARTESIAN_POINT('Ctrl Pts',(-16.9013570056506,6.54762058645456,
960.912398825173));
#148190=CARTESIAN_POINT('Ctrl Pts',(-16.1559070823762,8.04468584505497,
959.418281178114));
#148191=CARTESIAN_POINT('Ctrl Pts',(-15.4104571591017,9.54175110365538,
957.924163531055));
#148192=CARTESIAN_POINT('Ctrl Pts',(-14.4026149179538,10.8763499173728,
956.430045883996));
#148193=CARTESIAN_POINT('Ctrl Pts',(-13.3947726768058,12.2109487310903,
954.935928236937));
#148194=CARTESIAN_POINT('Ctrl Pts',(-12.1588589765331,13.3376329379985,
953.441810589878));
#148195=CARTESIAN_POINT('Ctrl Pts',(-10.9229452762603,14.4643171449067,
951.94769294282));
#148196=CARTESIAN_POINT('Ctrl Pts',(-9.50104767561052,15.3447188656481,
950.453575295761));
#148197=CARTESIAN_POINT('Ctrl Pts',(-8.07915007496071,16.2251205863895,
948.959457648702));
#148198=CARTESIAN_POINT('Ctrl Pts',(-6.51968959134574,16.8292587962898,
947.465340001643));
#148199=CARTESIAN_POINT('Ctrl Pts',(-4.96022910773078,17.4333970061901,
945.971222354585));
#148200=CARTESIAN_POINT('Ctrl Pts',(-3.31631129755346,17.7406985030951,
944.477104707526));
#148201=CARTESIAN_POINT('Ctrl Pts',(-1.67239348737615,18.048,942.982987060467));
#148202=CARTESIAN_POINT('Ctrl Pts',(-2.21024254310115E-15,18.048,941.488869413408));
#148203=CARTESIAN_POINT('Ctrl Pts',(1.67239348737616,18.048,939.994751766349));
#148204=CARTESIAN_POINT('Ctrl Pts',(3.31631129755346,17.7406985030951,938.50063411929));
#148205=CARTESIAN_POINT('Ctrl Pts',(4.96022910773077,17.4333970061901,937.006516472232));
#148206=CARTESIAN_POINT('Ctrl Pts',(6.51968959134575,16.8292587962898,935.512398825173));
#148207=CARTESIAN_POINT('Ctrl Pts',(8.07915007496071,16.2251205863895,934.018281178114));
#148208=CARTESIAN_POINT('Ctrl Pts',(9.50104767561053,15.3447188656481,932.524163531055));
#148209=CARTESIAN_POINT('Ctrl Pts',(10.9229452762603,14.4643171449067,931.030045883996));
#148210=CARTESIAN_POINT('Ctrl Pts',(12.1588589765331,13.3376329379985,929.535928236937));
#148211=CARTESIAN_POINT('Ctrl Pts',(13.3947726768058,12.2109487310903,928.041810589879));
#148212=CARTESIAN_POINT('Ctrl Pts',(14.4026149179538,10.8763499173728,926.54769294282));
#148213=CARTESIAN_POINT('Ctrl Pts',(15.4104571591017,9.54175110365538,925.053575295761));
#148214=CARTESIAN_POINT('Ctrl Pts',(16.1559070823762,8.04468584505496,923.559457648702));
#148215=CARTESIAN_POINT('Ctrl Pts',(16.9013570056506,6.54762058645456,922.065340001643));
#148216=CARTESIAN_POINT('Ctrl Pts',(17.3590292079831,4.93906964482096,920.571222354584));
#148217=CARTESIAN_POINT('Ctrl Pts',(17.8167014103155,3.33051870318735,919.077104707525));
#148218=CARTESIAN_POINT('Ctrl Pts',(17.9710104137728,1.66525935159367,917.582987060467));
#148219=CARTESIAN_POINT('Ctrl Pts',(18.1253194172301,3.32956716117513E-15,
916.088869413408));
#148220=CARTESIAN_POINT('Ctrl Pts',(17.9710104137728,-1.66525935159367,
914.594751766349));
#148221=CARTESIAN_POINT('Ctrl Pts',(17.8167014103155,-3.33051870318736,
913.10063411929));
#148222=CARTESIAN_POINT('Ctrl Pts',(17.3590292079831,-4.93906964482095,
911.606516472231));
#148223=CARTESIAN_POINT('Ctrl Pts',(16.9013570056506,-6.54762058645456,
910.112398825173));
#148224=CARTESIAN_POINT('Ctrl Pts',(16.1559070823762,-8.04468584505497,
908.618281178114));
#148225=CARTESIAN_POINT('Ctrl Pts',(15.4104571591017,-9.54175110365538,
907.124163531055));
#148226=CARTESIAN_POINT('Ctrl Pts',(14.4026149179538,-10.8763499173728,
905.630045883996));
#148227=CARTESIAN_POINT('Ctrl Pts',(13.3947726768058,-12.2109487310903,
904.135928236937));
#148228=CARTESIAN_POINT('Ctrl Pts',(12.1588589765331,-13.3376329379985,
902.641810589878));
#148229=CARTESIAN_POINT('Ctrl Pts',(10.9229452762603,-14.4643171449067,
901.14769294282));
#148230=CARTESIAN_POINT('Ctrl Pts',(9.50104767561053,-15.3447188656481,
899.653575295761));
#148231=CARTESIAN_POINT('Ctrl Pts',(8.07915007496071,-16.2251205863895,
898.159457648702));
#148232=CARTESIAN_POINT('Ctrl Pts',(6.51968959134574,-16.8292587962898,
896.665340001643));
#148233=CARTESIAN_POINT('Ctrl Pts',(4.96022910773078,-17.4333970061901,
895.171222354584));
#148234=CARTESIAN_POINT('Ctrl Pts',(3.31631129755346,-17.7406985030951,
893.677104707526));
#148235=CARTESIAN_POINT('Ctrl Pts',(1.67239348737615,-18.048,892.182987060467));
#148236=CARTESIAN_POINT('Ctrl Pts',(0.,-18.048,890.688869413408));
#148237=CARTESIAN_POINT('Ctrl Pts',(-1.67239348737615,-18.048,889.194751766349));
#148238=CARTESIAN_POINT('Ctrl Pts',(-3.31631129755346,-17.7406985030951,
887.70063411929));
#148239=CARTESIAN_POINT('Ctrl Pts',(-4.96022910773077,-17.4333970061901,
886.206516472232));
#148240=CARTESIAN_POINT('Ctrl Pts',(-6.51968959134574,-16.8292587962898,
884.712398825172));
#148241=CARTESIAN_POINT('Ctrl Pts',(-8.07915007496071,-16.2251205863895,
883.218281178114));
#148242=CARTESIAN_POINT('Ctrl Pts',(-9.50104767561052,-15.3447188656481,
881.724163531055));
#148243=CARTESIAN_POINT('Ctrl Pts',(-10.9229452762603,-14.4643171449067,
880.230045883996));
#148244=CARTESIAN_POINT('Ctrl Pts',(-12.1588589765331,-13.3376329379985,
878.735928236937));
#148245=CARTESIAN_POINT('Ctrl Pts',(-13.3947726768058,-12.2109487310903,
877.241810589879));
#148246=CARTESIAN_POINT('Ctrl Pts',(-14.4026149179538,-10.8763499173728,
875.74769294282));
#148247=CARTESIAN_POINT('Ctrl Pts',(-15.4104571591017,-9.54175110365538,
874.253575295761));
#148248=CARTESIAN_POINT('Ctrl Pts',(-16.1559070823762,-8.04468584505497,
872.759457648702));
#148249=CARTESIAN_POINT('Ctrl Pts',(-16.9013570056506,-6.54762058645456,
871.265340001643));
#148250=CARTESIAN_POINT('Ctrl Pts',(-17.3590292079831,-4.93906964482095,
869.771222354584));
#148251=CARTESIAN_POINT('Ctrl Pts',(-17.8167014103155,-3.33051870318735,
868.277104707525));
#148252=CARTESIAN_POINT('Ctrl Pts',(-17.9710104137728,-1.66525935159368,
866.782987060467));
#148253=CARTESIAN_POINT('Ctrl Pts',(-18.1253194172301,-1.10985572039171E-15,
865.288869413408));
#148254=CARTESIAN_POINT('Ctrl Pts',(-17.9710104137728,1.66525935159367,
863.794751766349));
#148255=CARTESIAN_POINT('Ctrl Pts',(-17.8167014103155,3.33051870318735,
862.30063411929));
#148256=CARTESIAN_POINT('Ctrl Pts',(-17.3590292079831,4.93906964482096,
860.806516472231));
#148257=CARTESIAN_POINT('Ctrl Pts',(-16.9013570056506,6.54762058645456,
859.312398825173));
#148258=CARTESIAN_POINT('Ctrl Pts',(-16.1559070823762,8.04468584505497,
857.818281178114));
#148259=CARTESIAN_POINT('Ctrl Pts',(-15.4104571591017,9.54175110365538,
856.324163531055));
#148260=CARTESIAN_POINT('Ctrl Pts',(-14.4026149179538,10.8763499173728,
854.830045883996));
#148261=CARTESIAN_POINT('Ctrl Pts',(-13.3947726768058,12.2109487310903,
853.335928236937));
#148262=CARTESIAN_POINT('Ctrl Pts',(-12.1588589765331,13.3376329379985,
851.841810589878));
#148263=CARTESIAN_POINT('Ctrl Pts',(-10.9229452762603,14.4643171449067,
850.34769294282));
#148264=CARTESIAN_POINT('Ctrl Pts',(-9.50104767561052,15.3447188656481,
848.853575295761));
#148265=CARTESIAN_POINT('Ctrl Pts',(-8.07915007496071,16.2251205863895,
847.359457648702));
#148266=CARTESIAN_POINT('Ctrl Pts',(-6.51968959134574,16.8292587962898,
845.865340001643));
#148267=CARTESIAN_POINT('Ctrl Pts',(-4.96022910773078,17.4333970061901,
844.371222354584));
#148268=CARTESIAN_POINT('Ctrl Pts',(-3.31631129755346,17.7406985030951,
842.877104707525));
#148269=CARTESIAN_POINT('Ctrl Pts',(-1.67239348737615,18.048,841.382987060467));
#148270=CARTESIAN_POINT('Ctrl Pts',(-2.21024254310115E-15,18.048,839.888869413408));
#148271=CARTESIAN_POINT('Ctrl Pts',(1.67239348737616,18.048,838.394751766349));
#148272=CARTESIAN_POINT('Ctrl Pts',(3.31631129755346,17.7406985030951,836.90063411929));
#148273=CARTESIAN_POINT('Ctrl Pts',(4.96022910773077,17.4333970061901,835.406516472232));
#148274=CARTESIAN_POINT('Ctrl Pts',(6.51968959134575,16.8292587962898,833.912398825173));
#148275=CARTESIAN_POINT('Ctrl Pts',(8.07915007496071,16.2251205863895,832.418281178114));
#148276=CARTESIAN_POINT('Ctrl Pts',(9.50104767561053,15.3447188656481,830.924163531055));
#148277=CARTESIAN_POINT('Ctrl Pts',(10.9229452762603,14.4643171449067,829.430045883996));
#148278=CARTESIAN_POINT('Ctrl Pts',(12.1588589765331,13.3376329379985,827.935928236937));
#148279=CARTESIAN_POINT('Ctrl Pts',(13.3947726768058,12.2109487310903,826.441810589879));
#148280=CARTESIAN_POINT('Ctrl Pts',(14.4026149179538,10.8763499173728,824.94769294282));
#148281=CARTESIAN_POINT('Ctrl Pts',(15.4104571591017,9.54175110365538,823.453575295761));
#148282=CARTESIAN_POINT('Ctrl Pts',(16.1559070823762,8.04468584505496,821.959457648702));
#148283=CARTESIAN_POINT('Ctrl Pts',(16.9013570056506,6.54762058645456,820.465340001643));
#148284=CARTESIAN_POINT('Ctrl Pts',(17.3590292079831,4.93906964482096,818.971222354584));
#148285=CARTESIAN_POINT('Ctrl Pts',(17.8167014103155,3.33051870318735,817.477104707526));
#148286=CARTESIAN_POINT('Ctrl Pts',(17.9710104137728,1.66525935159367,815.982987060467));
#148287=CARTESIAN_POINT('Ctrl Pts',(18.1253194172301,3.32956716117513E-15,
814.488869413408));
#148288=CARTESIAN_POINT('Ctrl Pts',(17.9710104137728,-1.66525935159367,
812.994751766349));
#148289=CARTESIAN_POINT('Ctrl Pts',(17.8167014103155,-3.33051870318736,
811.50063411929));
#148290=CARTESIAN_POINT('Ctrl Pts',(17.3590292079831,-4.93906964482095,
810.006516472231));
#148291=CARTESIAN_POINT('Ctrl Pts',(16.9013570056506,-6.54762058645456,
808.512398825172));
#148292=CARTESIAN_POINT('Ctrl Pts',(16.1559070823762,-8.04468584505497,
807.018281178114));
#148293=CARTESIAN_POINT('Ctrl Pts',(15.4104571591017,-9.54175110365538,
805.524163531055));
#148294=CARTESIAN_POINT('Ctrl Pts',(14.4026149179538,-10.8763499173728,
804.030045883996));
#148295=CARTESIAN_POINT('Ctrl Pts',(13.3947726768058,-12.2109487310903,
802.535928236937));
#148296=CARTESIAN_POINT('Ctrl Pts',(12.1588589765331,-13.3376329379985,
801.041810589878));
#148297=CARTESIAN_POINT('Ctrl Pts',(10.9229452762603,-14.4643171449067,
799.54769294282));
#148298=CARTESIAN_POINT('Ctrl Pts',(9.50104767561053,-15.3447188656481,
798.053575295761));
#148299=CARTESIAN_POINT('Ctrl Pts',(8.07915007496071,-16.2251205863895,
796.559457648702));
#148300=CARTESIAN_POINT('Ctrl Pts',(6.51968959134574,-16.8292587962898,
795.065340001643));
#148301=CARTESIAN_POINT('Ctrl Pts',(4.96022910773078,-17.4333970061901,
793.571222354584));
#148302=CARTESIAN_POINT('Ctrl Pts',(3.31631129755346,-17.7406985030951,
792.077104707525));
#148303=CARTESIAN_POINT('Ctrl Pts',(1.67239348737615,-18.048,790.582987060467));
#148304=CARTESIAN_POINT('Ctrl Pts',(0.,-18.048,789.088869413408));
#148305=CARTESIAN_POINT('Ctrl Pts',(-1.67239348737615,-18.048,787.594751766349));
#148306=CARTESIAN_POINT('Ctrl Pts',(-3.31631129755346,-17.7406985030951,
786.10063411929));
#148307=CARTESIAN_POINT('Ctrl Pts',(-4.96022910773077,-17.4333970061901,
784.606516472231));
#148308=CARTESIAN_POINT('Ctrl Pts',(-6.51968959134574,-16.8292587962898,
783.112398825173));
#148309=CARTESIAN_POINT('Ctrl Pts',(-8.07915007496071,-16.2251205863895,
781.618281178114));
#148310=CARTESIAN_POINT('Ctrl Pts',(-9.50104767561052,-15.3447188656481,
780.124163531055));
#148311=CARTESIAN_POINT('Ctrl Pts',(-10.9229452762603,-14.4643171449067,
778.630045883996));
#148312=CARTESIAN_POINT('Ctrl Pts',(-12.1588589765331,-13.3376329379985,
777.135928236937));
#148313=CARTESIAN_POINT('Ctrl Pts',(-13.3947726768058,-12.2109487310903,
775.641810589879));
#148314=CARTESIAN_POINT('Ctrl Pts',(-14.4026149179538,-10.8763499173728,
774.14769294282));
#148315=CARTESIAN_POINT('Ctrl Pts',(-15.4104571591017,-9.54175110365538,
772.653575295761));
#148316=CARTESIAN_POINT('Ctrl Pts',(-16.1559070823762,-8.04468584505497,
771.159457648702));
#148317=CARTESIAN_POINT('Ctrl Pts',(-16.9013570056506,-6.54762058645456,
769.665340001643));
#148318=CARTESIAN_POINT('Ctrl Pts',(-17.3590292079831,-4.93906964482095,
768.171222354584));
#148319=CARTESIAN_POINT('Ctrl Pts',(-17.8167014103155,-3.33051870318735,
766.677104707526));
#148320=CARTESIAN_POINT('Ctrl Pts',(-17.9710104137728,-1.66525935159368,
765.182987060467));
#148321=CARTESIAN_POINT('Ctrl Pts',(-18.1253194172301,-1.10985572039171E-15,
763.688869413408));
#148322=CARTESIAN_POINT('Ctrl Pts',(-17.9710104137728,1.66525935159367,
762.194751766349));
#148323=CARTESIAN_POINT('Ctrl Pts',(-17.8167014103155,3.33051870318735,
760.70063411929));
#148324=CARTESIAN_POINT('Ctrl Pts',(-17.3590292079831,4.93906964482096,
759.206516472231));
#148325=CARTESIAN_POINT('Ctrl Pts',(-16.9013570056506,6.54762058645456,
757.712398825172));
#148326=CARTESIAN_POINT('Ctrl Pts',(-16.1559070823762,8.04468584505497,
756.218281178114));
#148327=CARTESIAN_POINT('Ctrl Pts',(-15.4104571591017,9.54175110365538,
754.724163531055));
#148328=CARTESIAN_POINT('Ctrl Pts',(-14.4026149179538,10.8763499173728,
753.230045883996));
#148329=CARTESIAN_POINT('Ctrl Pts',(-13.3947726768058,12.2109487310903,
751.735928236937));
#148330=CARTESIAN_POINT('Ctrl Pts',(-12.1588589765331,13.3376329379985,
750.241810589878));
#148331=CARTESIAN_POINT('Ctrl Pts',(-10.9229452762603,14.4643171449067,
748.74769294282));
#148332=CARTESIAN_POINT('Ctrl Pts',(-9.50104767561052,15.3447188656481,
747.253575295761));
#148333=CARTESIAN_POINT('Ctrl Pts',(-8.07915007496071,16.2251205863895,
745.759457648702));
#148334=CARTESIAN_POINT('Ctrl Pts',(-6.51968959134574,16.8292587962898,
744.265340001643));
#148335=CARTESIAN_POINT('Ctrl Pts',(-4.96022910773078,17.4333970061901,
742.771222354584));
#148336=CARTESIAN_POINT('Ctrl Pts',(-3.31631129755346,17.7406985030951,
741.277104707525));
#148337=CARTESIAN_POINT('Ctrl Pts',(-1.67239348737615,18.048,739.782987060467));
#148338=CARTESIAN_POINT('Ctrl Pts',(-2.21024254310115E-15,18.048,738.288869413408));
#148339=CARTESIAN_POINT('Ctrl Pts',(1.67239348737616,18.048,736.794751766349));
#148340=CARTESIAN_POINT('Ctrl Pts',(3.31631129755346,17.7406985030951,735.30063411929));
#148341=CARTESIAN_POINT('Ctrl Pts',(4.96022910773077,17.4333970061901,733.806516472231));
#148342=CARTESIAN_POINT('Ctrl Pts',(6.51968959134575,16.8292587962898,732.312398825173));
#148343=CARTESIAN_POINT('Ctrl Pts',(8.07915007496071,16.2251205863895,730.818281178114));
#148344=CARTESIAN_POINT('Ctrl Pts',(9.50104767561053,15.3447188656481,729.324163531055));
#148345=CARTESIAN_POINT('Ctrl Pts',(10.9229452762603,14.4643171449067,727.830045883996));
#148346=CARTESIAN_POINT('Ctrl Pts',(12.1588589765331,13.3376329379985,726.335928236937));
#148347=CARTESIAN_POINT('Ctrl Pts',(13.3947726768058,12.2109487310903,724.841810589879));
#148348=CARTESIAN_POINT('Ctrl Pts',(14.4026149179538,10.8763499173728,723.34769294282));
#148349=CARTESIAN_POINT('Ctrl Pts',(15.4104571591017,9.54175110365538,721.853575295761));
#148350=CARTESIAN_POINT('Ctrl Pts',(16.1559070823762,8.04468584505496,720.359457648702));
#148351=CARTESIAN_POINT('Ctrl Pts',(16.9013570056506,6.54762058645456,718.865340001643));
#148352=CARTESIAN_POINT('Ctrl Pts',(17.3590292079831,4.93906964482096,717.371222354584));
#148353=CARTESIAN_POINT('Ctrl Pts',(17.8167014103155,3.33051870318735,715.877104707526));
#148354=CARTESIAN_POINT('Ctrl Pts',(17.9710104137728,1.66525935159367,714.382987060467));
#148355=CARTESIAN_POINT('Ctrl Pts',(18.1253194172301,3.32956716117513E-15,
712.888869413408));
#148356=CARTESIAN_POINT('Ctrl Pts',(17.9710104137728,-1.66525935159367,
711.394751766349));
#148357=CARTESIAN_POINT('Ctrl Pts',(17.8167014103155,-3.33051870318736,
709.90063411929));
#148358=CARTESIAN_POINT('Ctrl Pts',(17.3590292079831,-4.93906964482095,
708.406516472231));
#148359=CARTESIAN_POINT('Ctrl Pts',(16.9013570056506,-6.54762058645456,
706.912398825173));
#148360=CARTESIAN_POINT('Ctrl Pts',(16.1559070823762,-8.04468584505497,
705.418281178114));
#148361=CARTESIAN_POINT('Ctrl Pts',(15.4104571591017,-9.54175110365538,
703.924163531055));
#148362=CARTESIAN_POINT('Ctrl Pts',(14.4026149179538,-10.8763499173728,
702.430045883996));
#148363=CARTESIAN_POINT('Ctrl Pts',(13.3947726768058,-12.2109487310903,
700.935928236937));
#148364=CARTESIAN_POINT('Ctrl Pts',(12.1588589765331,-13.3376329379985,
699.441810589878));
#148365=CARTESIAN_POINT('Ctrl Pts',(10.9229452762603,-14.4643171449067,
697.94769294282));
#148366=CARTESIAN_POINT('Ctrl Pts',(9.50104767561053,-15.3447188656481,
696.453575295761));
#148367=CARTESIAN_POINT('Ctrl Pts',(8.07915007496071,-16.2251205863895,
694.959457648702));
#148368=CARTESIAN_POINT('Ctrl Pts',(6.51968959134574,-16.8292587962898,
693.465340001643));
#148369=CARTESIAN_POINT('Ctrl Pts',(4.96022910773078,-17.4333970061901,
691.971222354584));
#148370=CARTESIAN_POINT('Ctrl Pts',(3.31631129755346,-17.7406985030951,
690.477104707526));
#148371=CARTESIAN_POINT('Ctrl Pts',(1.67239348737615,-18.048,688.982987060467));
#148372=CARTESIAN_POINT('Ctrl Pts',(0.,-18.048,687.488869413408));
#148373=CARTESIAN_POINT('Ctrl Pts',(-1.67239348737615,-18.048,685.994751766349));
#148374=CARTESIAN_POINT('Ctrl Pts',(-3.31631129755346,-17.7406985030951,
684.50063411929));
#148375=CARTESIAN_POINT('Ctrl Pts',(-4.96022910773077,-17.4333970061901,
683.006516472232));
#148376=CARTESIAN_POINT('Ctrl Pts',(-6.51968959134574,-16.8292587962898,
681.512398825172));
#148377=CARTESIAN_POINT('Ctrl Pts',(-8.07915007496071,-16.2251205863895,
680.018281178114));
#148378=CARTESIAN_POINT('Ctrl Pts',(-9.50104767561052,-15.3447188656481,
678.524163531055));
#148379=CARTESIAN_POINT('Ctrl Pts',(-10.9229452762603,-14.4643171449067,
677.030045883996));
#148380=CARTESIAN_POINT('Ctrl Pts',(-12.1588589765331,-13.3376329379985,
675.535928236937));
#148381=CARTESIAN_POINT('Ctrl Pts',(-13.3947726768058,-12.2109487310903,
674.041810589878));
#148382=CARTESIAN_POINT('Ctrl Pts',(-14.4026149179538,-10.8763499173728,
672.54769294282));
#148383=CARTESIAN_POINT('Ctrl Pts',(-15.4104571591017,-9.54175110365538,
671.053575295761));
#148384=CARTESIAN_POINT('Ctrl Pts',(-16.1559070823762,-8.04468584505497,
669.559457648702));
#148385=CARTESIAN_POINT('Ctrl Pts',(-16.9013570056506,-6.54762058645456,
668.065340001643));
#148386=CARTESIAN_POINT('Ctrl Pts',(-17.3590292079831,-4.93906964482095,
666.571222354584));
#148387=CARTESIAN_POINT('Ctrl Pts',(-17.8167014103155,-3.33051870318735,
665.077104707526));
#148388=CARTESIAN_POINT('Ctrl Pts',(-17.9710104137728,-1.66525935159368,
663.582987060467));
#148389=CARTESIAN_POINT('Ctrl Pts',(-18.1253194172301,-1.10985572039171E-15,
662.088869413408));
#148390=CARTESIAN_POINT('Ctrl Pts',(-17.9710104137728,1.66525935159367,
660.594751766349));
#148391=CARTESIAN_POINT('Ctrl Pts',(-17.8167014103155,3.33051870318735,
659.10063411929));
#148392=CARTESIAN_POINT('Ctrl Pts',(-17.3590292079831,4.93906964482096,
657.606516472231));
#148393=CARTESIAN_POINT('Ctrl Pts',(-16.9013570056506,6.54762058645456,
656.112398825172));
#148394=CARTESIAN_POINT('Ctrl Pts',(-16.1559070823762,8.04468584505497,
654.618281178114));
#148395=CARTESIAN_POINT('Ctrl Pts',(-15.4104571591017,9.54175110365538,
653.124163531055));
#148396=CARTESIAN_POINT('Ctrl Pts',(-14.4026149179538,10.8763499173728,
651.630045883996));
#148397=CARTESIAN_POINT('Ctrl Pts',(-13.3947726768058,12.2109487310903,
650.135928236937));
#148398=CARTESIAN_POINT('Ctrl Pts',(-12.1588589765331,13.3376329379985,
648.641810589878));
#148399=CARTESIAN_POINT('Ctrl Pts',(-10.9229452762603,14.4643171449067,
647.14769294282));
#148400=CARTESIAN_POINT('Ctrl Pts',(-9.50104767561052,15.3447188656481,
645.653575295761));
#148401=CARTESIAN_POINT('Ctrl Pts',(-8.07915007496071,16.2251205863895,
644.159457648702));
#148402=CARTESIAN_POINT('Ctrl Pts',(-6.51968959134574,16.8292587962898,
642.665340001643));
#148403=CARTESIAN_POINT('Ctrl Pts',(-4.96022910773078,17.4333970061901,
641.171222354584));
#148404=CARTESIAN_POINT('Ctrl Pts',(-3.31631129755346,17.7406985030951,
639.677104707525));
#148405=CARTESIAN_POINT('Ctrl Pts',(-1.67239348737615,18.048,638.182987060467));
#148406=CARTESIAN_POINT('Ctrl Pts',(-2.21024254310115E-15,18.048,636.688869413408));
#148407=CARTESIAN_POINT('Ctrl Pts',(1.67239348737616,18.048,635.194751766349));
#148408=CARTESIAN_POINT('Ctrl Pts',(3.31631129755346,17.7406985030951,633.70063411929));
#148409=CARTESIAN_POINT('Ctrl Pts',(4.96022910773077,17.4333970061901,632.206516472231));
#148410=CARTESIAN_POINT('Ctrl Pts',(6.51968959134575,16.8292587962898,630.712398825172));
#148411=CARTESIAN_POINT('Ctrl Pts',(8.07915007496071,16.2251205863895,629.218281178114));
#148412=CARTESIAN_POINT('Ctrl Pts',(9.50104767561053,15.3447188656481,627.724163531055));
#148413=CARTESIAN_POINT('Ctrl Pts',(10.9229452762603,14.4643171449067,626.230045883996));
#148414=CARTESIAN_POINT('Ctrl Pts',(12.1588589765331,13.3376329379985,624.735928236937));
#148415=CARTESIAN_POINT('Ctrl Pts',(13.3947726768058,12.2109487310903,623.241810589878));
#148416=CARTESIAN_POINT('Ctrl Pts',(14.4026149179538,10.8763499173728,621.74769294282));
#148417=CARTESIAN_POINT('Ctrl Pts',(15.4104571591017,9.54175110365538,620.253575295761));
#148418=CARTESIAN_POINT('Ctrl Pts',(16.1559070823762,8.04468584505496,618.759457648702));
#148419=CARTESIAN_POINT('Ctrl Pts',(16.9013570056506,6.54762058645456,617.265340001643));
#148420=CARTESIAN_POINT('Ctrl Pts',(17.3590292079831,4.93906964482096,615.771222354584));
#148421=CARTESIAN_POINT('Ctrl Pts',(17.8167014103155,3.33051870318735,614.277104707526));
#148422=CARTESIAN_POINT('Ctrl Pts',(17.9710104137728,1.66525935159367,612.782987060467));
#148423=CARTESIAN_POINT('Ctrl Pts',(18.1253194172301,3.32956716117513E-15,
611.288869413408));
#148424=CARTESIAN_POINT('Ctrl Pts',(17.9710104137728,-1.66525935159367,
609.794751766349));
#148425=CARTESIAN_POINT('Ctrl Pts',(17.8167014103155,-3.33051870318736,
608.30063411929));
#148426=CARTESIAN_POINT('Ctrl Pts',(17.3590292079831,-4.93906964482095,
606.806516472231));
#148427=CARTESIAN_POINT('Ctrl Pts',(16.9013570056506,-6.54762058645456,
605.312398825173));
#148428=CARTESIAN_POINT('Ctrl Pts',(16.1559070823762,-8.04468584505497,
603.818281178114));
#148429=CARTESIAN_POINT('Ctrl Pts',(15.4104571591017,-9.54175110365538,
602.324163531055));
#148430=CARTESIAN_POINT('Ctrl Pts',(14.4026149179538,-10.8763499173728,
600.830045883996));
#148431=CARTESIAN_POINT('Ctrl Pts',(13.3947726768058,-12.2109487310903,
599.335928236937));
#148432=CARTESIAN_POINT('Ctrl Pts',(12.1588589765331,-13.3376329379985,
597.841810589878));
#148433=CARTESIAN_POINT('Ctrl Pts',(10.9229452762603,-14.4643171449067,
596.34769294282));
#148434=CARTESIAN_POINT('Ctrl Pts',(9.50104767561053,-15.3447188656481,
594.853575295761));
#148435=CARTESIAN_POINT('Ctrl Pts',(8.07915007496071,-16.2251205863895,
593.359457648702));
#148436=CARTESIAN_POINT('Ctrl Pts',(6.51968959134574,-16.8292587962898,
591.865340001643));
#148437=CARTESIAN_POINT('Ctrl Pts',(4.96022910773078,-17.4333970061901,
590.371222354584));
#148438=CARTESIAN_POINT('Ctrl Pts',(3.31631129755346,-17.7406985030951,
588.877104707525));
#148439=CARTESIAN_POINT('Ctrl Pts',(1.67239348737615,-18.048,587.382987060467));
#148440=CARTESIAN_POINT('Ctrl Pts',(0.,-18.048,585.888869413408));
#148441=CARTESIAN_POINT('Ctrl Pts',(-1.67239348737615,-18.048,584.394751766349));
#148442=CARTESIAN_POINT('Ctrl Pts',(-3.31631129755346,-17.7406985030951,
582.90063411929));
#148443=CARTESIAN_POINT('Ctrl Pts',(-4.96022910773077,-17.4333970061901,
581.406516472231));
#148444=CARTESIAN_POINT('Ctrl Pts',(-6.51968959134574,-16.8292587962898,
579.912398825173));
#148445=CARTESIAN_POINT('Ctrl Pts',(-8.07915007496071,-16.2251205863895,
578.418281178114));
#148446=CARTESIAN_POINT('Ctrl Pts',(-9.50104767561052,-15.3447188656481,
576.924163531055));
#148447=CARTESIAN_POINT('Ctrl Pts',(-10.9229452762603,-14.4643171449067,
575.430045883996));
#148448=CARTESIAN_POINT('Ctrl Pts',(-12.1588589765331,-13.3376329379985,
573.935928236937));
#148449=CARTESIAN_POINT('Ctrl Pts',(-13.3947726768058,-12.2109487310903,
572.441810589879));
#148450=CARTESIAN_POINT('Ctrl Pts',(-14.4026149179538,-10.8763499173728,
570.94769294282));
#148451=CARTESIAN_POINT('Ctrl Pts',(-15.4104571591017,-9.54175110365538,
569.453575295761));
#148452=CARTESIAN_POINT('Ctrl Pts',(-16.1559070823762,-8.04468584505497,
567.959457648702));
#148453=CARTESIAN_POINT('Ctrl Pts',(-16.9013570056506,-6.54762058645456,
566.465340001643));
#148454=CARTESIAN_POINT('Ctrl Pts',(-17.3590292079831,-4.93906964482095,
564.971222354584));
#148455=CARTESIAN_POINT('Ctrl Pts',(-17.8167014103155,-3.33051870318735,
563.477104707526));
#148456=CARTESIAN_POINT('Ctrl Pts',(-17.9710104137728,-1.66525935159368,
561.982987060467));
#148457=CARTESIAN_POINT('Ctrl Pts',(-18.1253194172301,-1.10985572039171E-15,
560.488869413408));
#148458=CARTESIAN_POINT('Ctrl Pts',(-17.9710104137728,1.66525935159367,
558.994751766349));
#148459=CARTESIAN_POINT('Ctrl Pts',(-17.8167014103155,3.33051870318735,
557.50063411929));
#148460=CARTESIAN_POINT('Ctrl Pts',(-17.3590292079831,4.93906964482096,
556.006516472231));
#148461=CARTESIAN_POINT('Ctrl Pts',(-16.9013570056506,6.54762058645456,
554.512398825173));
#148462=CARTESIAN_POINT('Ctrl Pts',(-16.1559070823762,8.04468584505497,
553.018281178114));
#148463=CARTESIAN_POINT('Ctrl Pts',(-15.4104571591017,9.54175110365538,
551.524163531055));
#148464=CARTESIAN_POINT('Ctrl Pts',(-14.4026149179538,10.8763499173728,
550.030045883996));
#148465=CARTESIAN_POINT('Ctrl Pts',(-13.3947726768058,12.2109487310903,
548.535928236937));
#148466=CARTESIAN_POINT('Ctrl Pts',(-12.1588589765331,13.3376329379985,
547.041810589878));
#148467=CARTESIAN_POINT('Ctrl Pts',(-10.9229452762603,14.4643171449067,
545.54769294282));
#148468=CARTESIAN_POINT('Ctrl Pts',(-9.50104767561052,15.3447188656481,
544.053575295761));
#148469=CARTESIAN_POINT('Ctrl Pts',(-8.07915007496071,16.2251205863895,
542.559457648702));
#148470=CARTESIAN_POINT('Ctrl Pts',(-6.51968959134574,16.8292587962898,
541.065340001643));
#148471=CARTESIAN_POINT('Ctrl Pts',(-4.96022910773078,17.4333970061901,
539.571222354584));
#148472=CARTESIAN_POINT('Ctrl Pts',(-3.31631129755346,17.7406985030951,
538.077104707525));
#148473=CARTESIAN_POINT('Ctrl Pts',(-1.67239348737615,18.048,536.582987060467));
#148474=CARTESIAN_POINT('Ctrl Pts',(-2.21024254310115E-15,18.048,535.088869413408));
#148475=CARTESIAN_POINT('Ctrl Pts',(1.67239348737616,18.048,533.594751766349));
#148476=CARTESIAN_POINT('Ctrl Pts',(3.31631129755346,17.7406985030951,532.10063411929));
#148477=CARTESIAN_POINT('Ctrl Pts',(4.96022910773077,17.4333970061901,530.606516472231));
#148478=CARTESIAN_POINT('Ctrl Pts',(6.51968959134575,16.8292587962898,529.112398825172));
#148479=CARTESIAN_POINT('Ctrl Pts',(8.07915007496071,16.2251205863895,527.618281178114));
#148480=CARTESIAN_POINT('Ctrl Pts',(9.50104767561053,15.3447188656481,526.124163531055));
#148481=CARTESIAN_POINT('Ctrl Pts',(10.9229452762603,14.4643171449067,524.630045883996));
#148482=CARTESIAN_POINT('Ctrl Pts',(12.1588589765331,13.3376329379985,523.135928236937));
#148483=CARTESIAN_POINT('Ctrl Pts',(13.3947726768058,12.2109487310903,521.641810589878));
#148484=CARTESIAN_POINT('Ctrl Pts',(14.4026149179538,10.8763499173728,520.14769294282));
#148485=CARTESIAN_POINT('Ctrl Pts',(15.4104571591017,9.54175110365538,518.653575295761));
#148486=CARTESIAN_POINT('Ctrl Pts',(16.1559070823762,8.04468584505496,517.159457648702));
#148487=CARTESIAN_POINT('Ctrl Pts',(16.9013570056506,6.54762058645456,515.665340001643));
#148488=CARTESIAN_POINT('Ctrl Pts',(17.3590292079831,4.93906964482096,514.171222354584));
#148489=CARTESIAN_POINT('Ctrl Pts',(17.8167014103155,3.33051870318735,512.677104707525));
#148490=CARTESIAN_POINT('Ctrl Pts',(17.9710104137728,1.66525935159367,511.182987060467));
#148491=CARTESIAN_POINT('Ctrl Pts',(18.1253194172301,3.32956716117513E-15,
509.688869413408));
#148492=CARTESIAN_POINT('Ctrl Pts',(17.9710104137728,-1.66525935159367,
508.194751766349));
#148493=CARTESIAN_POINT('Ctrl Pts',(17.8167014103155,-3.33051870318736,
506.70063411929));
#148494=CARTESIAN_POINT('Ctrl Pts',(17.3590292079831,-4.93906964482095,
505.206516472231));
#148495=CARTESIAN_POINT('Ctrl Pts',(16.9013570056506,-6.54762058645456,
503.712398825173));
#148496=CARTESIAN_POINT('Ctrl Pts',(16.1559070823762,-8.04468584505497,
502.218281178114));
#148497=CARTESIAN_POINT('Ctrl Pts',(15.4104571591017,-9.54175110365538,
500.724163531055));
#148498=CARTESIAN_POINT('Ctrl Pts',(14.4026149179538,-10.8763499173728,
499.230045883996));
#148499=CARTESIAN_POINT('Ctrl Pts',(13.3947726768058,-12.2109487310903,
497.735928236937));
#148500=CARTESIAN_POINT('Ctrl Pts',(12.1588589765331,-13.3376329379985,
496.241810589879));
#148501=CARTESIAN_POINT('Ctrl Pts',(10.9229452762603,-14.4643171449067,
494.74769294282));
#148502=CARTESIAN_POINT('Ctrl Pts',(9.50104767561053,-15.3447188656481,
493.253575295761));
#148503=CARTESIAN_POINT('Ctrl Pts',(8.07915007496071,-16.2251205863895,
491.759457648702));
#148504=CARTESIAN_POINT('Ctrl Pts',(6.51968959134574,-16.8292587962898,
490.265340001643));
#148505=CARTESIAN_POINT('Ctrl Pts',(4.96022910773078,-17.4333970061901,
488.771222354584));
#148506=CARTESIAN_POINT('Ctrl Pts',(3.31631129755346,-17.7406985030951,
487.277104707526));
#148507=CARTESIAN_POINT('Ctrl Pts',(1.67239348737615,-18.048,485.782987060467));
#148508=CARTESIAN_POINT('Ctrl Pts',(0.,-18.048,484.288869413408));
#148509=CARTESIAN_POINT('Ctrl Pts',(-1.67239348737615,-18.048,482.794751766349));
#148510=CARTESIAN_POINT('Ctrl Pts',(-3.31631129755346,-17.7406985030951,
481.30063411929));
#148511=CARTESIAN_POINT('Ctrl Pts',(-4.96022910773077,-17.4333970061901,
479.806516472231));
#148512=CARTESIAN_POINT('Ctrl Pts',(-6.51968959134574,-16.8292587962898,
478.312398825173));
#148513=CARTESIAN_POINT('Ctrl Pts',(-8.07915007496071,-16.2251205863895,
476.818281178114));
#148514=CARTESIAN_POINT('Ctrl Pts',(-9.50104767561052,-15.3447188656481,
475.324163531055));
#148515=CARTESIAN_POINT('Ctrl Pts',(-10.9229452762603,-14.4643171449067,
473.830045883996));
#148516=CARTESIAN_POINT('Ctrl Pts',(-12.1588589765331,-13.3376329379985,
472.335928236937));
#148517=CARTESIAN_POINT('Ctrl Pts',(-13.3947726768058,-12.2109487310903,
470.841810589878));
#148518=CARTESIAN_POINT('Ctrl Pts',(-14.4026149179538,-10.8763499173728,
469.34769294282));
#148519=CARTESIAN_POINT('Ctrl Pts',(-15.4104571591017,-9.54175110365538,
467.853575295761));
#148520=CARTESIAN_POINT('Ctrl Pts',(-16.1559070823762,-8.04468584505497,
466.359457648702));
#148521=CARTESIAN_POINT('Ctrl Pts',(-16.9013570056506,-6.54762058645456,
464.865340001643));
#148522=CARTESIAN_POINT('Ctrl Pts',(-17.3590292079831,-4.93906964482095,
463.371222354584));
#148523=CARTESIAN_POINT('Ctrl Pts',(-17.8167014103155,-3.33051870318735,
461.877104707525));
#148524=CARTESIAN_POINT('Ctrl Pts',(-17.9710104137728,-1.66525935159368,
460.382987060467));
#148525=CARTESIAN_POINT('Ctrl Pts',(-18.1253194172301,-1.10985572039171E-15,
458.888869413408));
#148526=CARTESIAN_POINT('Ctrl Pts',(-17.9710104137728,1.66525935159367,
457.394751766349));
#148527=CARTESIAN_POINT('Ctrl Pts',(-17.8167014103155,3.33051870318735,
455.90063411929));
#148528=CARTESIAN_POINT('Ctrl Pts',(-17.3590292079831,4.93906964482096,
454.406516472231));
#148529=CARTESIAN_POINT('Ctrl Pts',(-16.9013570056506,6.54762058645456,
452.912398825173));
#148530=CARTESIAN_POINT('Ctrl Pts',(-16.1559070823762,8.04468584505497,
451.418281178114));
#148531=CARTESIAN_POINT('Ctrl Pts',(-15.4104571591017,9.54175110365538,
449.924163531055));
#148532=CARTESIAN_POINT('Ctrl Pts',(-14.4026149179538,10.8763499173728,
448.430045883996));
#148533=CARTESIAN_POINT('Ctrl Pts',(-13.3947726768058,12.2109487310903,
446.935928236937));
#148534=CARTESIAN_POINT('Ctrl Pts',(-12.1588589765331,13.3376329379985,
445.441810589878));
#148535=CARTESIAN_POINT('Ctrl Pts',(-10.9229452762603,14.4643171449067,
443.94769294282));
#148536=CARTESIAN_POINT('Ctrl Pts',(-9.50104767561052,15.3447188656481,
442.453575295761));
#148537=CARTESIAN_POINT('Ctrl Pts',(-8.07915007496071,16.2251205863895,
440.959457648702));
#148538=CARTESIAN_POINT('Ctrl Pts',(-6.51968959134574,16.8292587962898,
439.465340001643));
#148539=CARTESIAN_POINT('Ctrl Pts',(-4.96022910773078,17.4333970061901,
437.971222354584));
#148540=CARTESIAN_POINT('Ctrl Pts',(-3.31631129755346,17.7406985030951,
436.477104707526));
#148541=CARTESIAN_POINT('Ctrl Pts',(-1.67239348737615,18.048,434.982987060467));
#148542=CARTESIAN_POINT('Ctrl Pts',(-2.21024254310115E-15,18.048,433.488869413408));
#148543=CARTESIAN_POINT('Ctrl Pts',(1.67239348737616,18.048,431.994751766349));
#148544=CARTESIAN_POINT('Ctrl Pts',(3.31631129755346,17.7406985030951,430.50063411929));
#148545=CARTESIAN_POINT('Ctrl Pts',(4.96022910773077,17.4333970061901,429.006516472231));
#148546=CARTESIAN_POINT('Ctrl Pts',(6.51968959134575,16.8292587962898,427.512398825173));
#148547=CARTESIAN_POINT('Ctrl Pts',(8.07915007496071,16.2251205863895,426.018281178114));
#148548=CARTESIAN_POINT('Ctrl Pts',(9.50104767561053,15.3447188656481,424.524163531055));
#148549=CARTESIAN_POINT('Ctrl Pts',(10.9229452762603,14.4643171449067,423.030045883996));
#148550=CARTESIAN_POINT('Ctrl Pts',(12.1588589765331,13.3376329379985,421.535928236937));
#148551=CARTESIAN_POINT('Ctrl Pts',(13.3947726768058,12.2109487310903,420.041810589879));
#148552=CARTESIAN_POINT('Ctrl Pts',(14.4026149179538,10.8763499173728,418.54769294282));
#148553=CARTESIAN_POINT('Ctrl Pts',(15.4104571591017,9.54175110365538,417.053575295761));
#148554=CARTESIAN_POINT('Ctrl Pts',(16.1559070823762,8.04468584505496,415.559457648702));
#148555=CARTESIAN_POINT('Ctrl Pts',(16.9013570056506,6.54762058645456,414.065340001643));
#148556=CARTESIAN_POINT('Ctrl Pts',(17.3590292079831,4.93906964482096,412.571222354584));
#148557=CARTESIAN_POINT('Ctrl Pts',(17.8167014103155,3.33051870318735,411.077104707526));
#148558=CARTESIAN_POINT('Ctrl Pts',(17.9710104137728,1.66525935159367,409.582987060467));
#148559=CARTESIAN_POINT('Ctrl Pts',(18.1253194172301,3.32956716117513E-15,
408.088869413408));
#148560=CARTESIAN_POINT('Ctrl Pts',(17.9710104137728,-1.66525935159367,
406.594751766349));
#148561=CARTESIAN_POINT('Ctrl Pts',(17.8167014103155,-3.33051870318736,
405.10063411929));
#148562=CARTESIAN_POINT('Ctrl Pts',(17.3590292079831,-4.93906964482095,
403.606516472231));
#148563=CARTESIAN_POINT('Ctrl Pts',(16.9013570056506,-6.54762058645456,
402.112398825173));
#148564=CARTESIAN_POINT('Ctrl Pts',(16.1559070823762,-8.04468584505497,
400.618281178114));
#148565=CARTESIAN_POINT('Ctrl Pts',(15.4104571591017,-9.54175110365538,
399.124163531055));
#148566=CARTESIAN_POINT('Ctrl Pts',(14.4026149179538,-10.8763499173728,
397.630045883996));
#148567=CARTESIAN_POINT('Ctrl Pts',(13.3947726768058,-12.2109487310903,
396.135928236937));
#148568=CARTESIAN_POINT('Ctrl Pts',(12.1588589765331,-13.3376329379985,
394.641810589878));
#148569=CARTESIAN_POINT('Ctrl Pts',(10.9229452762603,-14.4643171449067,
393.147692942819));
#148570=CARTESIAN_POINT('Ctrl Pts',(9.50104767561053,-15.3447188656481,
391.653575295761));
#148571=CARTESIAN_POINT('Ctrl Pts',(8.07915007496071,-16.2251205863895,
390.159457648702));
#148572=CARTESIAN_POINT('Ctrl Pts',(6.51968959134574,-16.8292587962898,
388.665340001643));
#148573=CARTESIAN_POINT('Ctrl Pts',(4.96022910773078,-17.4333970061901,
387.171222354584));
#148574=CARTESIAN_POINT('Ctrl Pts',(3.31631129755346,-17.7406985030951,
385.677104707525));
#148575=CARTESIAN_POINT('Ctrl Pts',(1.67239348737615,-18.048,384.182987060467));
#148576=CARTESIAN_POINT('Ctrl Pts',(0.,-18.048,382.688869413408));
#148577=CARTESIAN_POINT('Ctrl Pts',(-1.67239348737615,-18.048,381.194751766349));
#148578=CARTESIAN_POINT('Ctrl Pts',(-3.31631129755346,-17.7406985030951,
379.70063411929));
#148579=CARTESIAN_POINT('Ctrl Pts',(-4.96022910773077,-17.4333970061901,
378.206516472231));
#148580=CARTESIAN_POINT('Ctrl Pts',(-6.51968959134574,-16.8292587962898,
376.712398825173));
#148581=CARTESIAN_POINT('Ctrl Pts',(-8.07915007496071,-16.2251205863895,
375.218281178114));
#148582=CARTESIAN_POINT('Ctrl Pts',(-9.50104767561052,-15.3447188656481,
373.724163531055));
#148583=CARTESIAN_POINT('Ctrl Pts',(-10.9229452762603,-14.4643171449067,
372.230045883996));
#148584=CARTESIAN_POINT('Ctrl Pts',(-12.1588589765331,-13.3376329379985,
370.735928236937));
#148585=CARTESIAN_POINT('Ctrl Pts',(-13.3947726768058,-12.2109487310903,
369.241810589879));
#148586=CARTESIAN_POINT('Ctrl Pts',(-14.4026149179538,-10.8763499173728,
367.74769294282));
#148587=CARTESIAN_POINT('Ctrl Pts',(-15.4104571591017,-9.54175110365538,
366.253575295761));
#148588=CARTESIAN_POINT('Ctrl Pts',(-16.1559070823762,-8.04468584505497,
364.759457648702));
#148589=CARTESIAN_POINT('Ctrl Pts',(-16.9013570056506,-6.54762058645456,
363.265340001643));
#148590=CARTESIAN_POINT('Ctrl Pts',(-17.3590292079831,-4.93906964482095,
361.771222354584));
#148591=CARTESIAN_POINT('Ctrl Pts',(-17.8167014103155,-3.33051870318735,
360.277104707525));
#148592=CARTESIAN_POINT('Ctrl Pts',(-17.9710104137728,-1.66525935159368,
358.782987060467));
#148593=CARTESIAN_POINT('Ctrl Pts',(-18.1253194172301,-1.10985572039171E-15,
357.288869413408));
#148594=CARTESIAN_POINT('Ctrl Pts',(-17.9710104137728,1.66525935159367,
355.794751766349));
#148595=CARTESIAN_POINT('Ctrl Pts',(-17.8167014103155,3.33051870318735,
354.30063411929));
#148596=CARTESIAN_POINT('Ctrl Pts',(-17.3590292079831,4.93906964482096,
352.806516472231));
#148597=CARTESIAN_POINT('Ctrl Pts',(-16.9013570056506,6.54762058645456,
351.312398825173));
#148598=CARTESIAN_POINT('Ctrl Pts',(-16.1559070823762,8.04468584505497,
349.818281178114));
#148599=CARTESIAN_POINT('Ctrl Pts',(-15.4104571591017,9.54175110365538,
348.324163531055));
#148600=CARTESIAN_POINT('Ctrl Pts',(-14.4026149179538,10.8763499173728,
346.830045883996));
#148601=CARTESIAN_POINT('Ctrl Pts',(-13.3947726768058,12.2109487310903,
345.335928236937));
#148602=CARTESIAN_POINT('Ctrl Pts',(-12.1588589765331,13.3376329379985,
343.841810589878));
#148603=CARTESIAN_POINT('Ctrl Pts',(-10.9229452762603,14.4643171449067,
342.34769294282));
#148604=CARTESIAN_POINT('Ctrl Pts',(-9.50104767561052,15.3447188656481,
340.853575295761));
#148605=CARTESIAN_POINT('Ctrl Pts',(-8.07915007496071,16.2251205863895,
339.359457648702));
#148606=CARTESIAN_POINT('Ctrl Pts',(-6.51968959134574,16.8292587962898,
337.865340001643));
#148607=CARTESIAN_POINT('Ctrl Pts',(-4.96022910773078,17.4333970061901,
336.371222354584));
#148608=CARTESIAN_POINT('Ctrl Pts',(-3.31631129755346,17.7406985030951,
334.877104707525));
#148609=CARTESIAN_POINT('Ctrl Pts',(-1.67239348737615,18.048,333.382987060467));
#148610=CARTESIAN_POINT('Ctrl Pts',(-2.21024254310115E-15,18.048,331.888869413408));
#148611=CARTESIAN_POINT('Ctrl Pts',(1.67239348737616,18.048,330.394751766349));
#148612=CARTESIAN_POINT('Ctrl Pts',(3.31631129755346,17.7406985030951,328.90063411929));
#148613=CARTESIAN_POINT('Ctrl Pts',(4.96022910773077,17.4333970061901,327.406516472231));
#148614=CARTESIAN_POINT('Ctrl Pts',(6.51968959134575,16.8292587962898,325.912398825172));
#148615=CARTESIAN_POINT('Ctrl Pts',(8.07915007496071,16.2251205863895,324.418281178114));
#148616=CARTESIAN_POINT('Ctrl Pts',(9.50104767561053,15.3447188656481,322.924163531055));
#148617=CARTESIAN_POINT('Ctrl Pts',(10.9229452762603,14.4643171449067,321.430045883996));
#148618=CARTESIAN_POINT('Ctrl Pts',(12.1588589765331,13.3376329379985,319.935928236937));
#148619=CARTESIAN_POINT('Ctrl Pts',(13.3947726768058,12.2109487310903,318.441810589878));
#148620=CARTESIAN_POINT('Ctrl Pts',(14.4026149179538,10.8763499173728,316.94769294282));
#148621=CARTESIAN_POINT('Ctrl Pts',(15.4104571591017,9.54175110365538,315.453575295761));
#148622=CARTESIAN_POINT('Ctrl Pts',(16.1559070823762,8.04468584505496,313.959457648702));
#148623=CARTESIAN_POINT('Ctrl Pts',(16.9013570056506,6.54762058645456,312.465340001643));
#148624=CARTESIAN_POINT('Ctrl Pts',(17.3590292079831,4.93906964482096,310.971222354584));
#148625=CARTESIAN_POINT('Ctrl Pts',(17.8167014103155,3.33051870318735,309.477104707526));
#148626=CARTESIAN_POINT('Ctrl Pts',(17.9710104137728,1.66525935159367,307.982987060467));
#148627=CARTESIAN_POINT('Ctrl Pts',(18.1253194172301,3.32956716117513E-15,
306.488869413408));
#148628=CARTESIAN_POINT('Ctrl Pts',(17.9710104137728,-1.66525935159367,
304.994751766349));
#148629=CARTESIAN_POINT('Ctrl Pts',(17.8167014103155,-3.33051870318736,
303.50063411929));
#148630=CARTESIAN_POINT('Ctrl Pts',(17.3590292079831,-4.93906964482095,
302.006516472231));
#148631=CARTESIAN_POINT('Ctrl Pts',(16.9013570056506,-6.54762058645456,
300.512398825173));
#148632=CARTESIAN_POINT('Ctrl Pts',(16.1559070823762,-8.04468584505497,
299.018281178114));
#148633=CARTESIAN_POINT('Ctrl Pts',(15.4104571591017,-9.54175110365538,
297.524163531055));
#148634=CARTESIAN_POINT('Ctrl Pts',(14.4026149179538,-10.8763499173728,
296.030045883996));
#148635=CARTESIAN_POINT('Ctrl Pts',(13.3947726768058,-12.2109487310903,
294.535928236937));
#148636=CARTESIAN_POINT('Ctrl Pts',(12.1588589765331,-13.3376329379985,
293.041810589878));
#148637=CARTESIAN_POINT('Ctrl Pts',(10.9229452762603,-14.4643171449067,
291.54769294282));
#148638=CARTESIAN_POINT('Ctrl Pts',(9.50104767561053,-15.3447188656481,
290.053575295761));
#148639=CARTESIAN_POINT('Ctrl Pts',(8.07915007496071,-16.2251205863895,
288.559457648702));
#148640=CARTESIAN_POINT('Ctrl Pts',(6.51968959134574,-16.8292587962898,
287.065340001643));
#148641=CARTESIAN_POINT('Ctrl Pts',(4.96022910773078,-17.4333970061901,
285.571222354584));
#148642=CARTESIAN_POINT('Ctrl Pts',(3.31631129755346,-17.7406985030951,
284.077104707525));
#148643=CARTESIAN_POINT('Ctrl Pts',(1.67239348737615,-18.048,282.582987060467));
#148644=CARTESIAN_POINT('Ctrl Pts',(0.,-18.048,281.088869413408));
#148645=CARTESIAN_POINT('Ctrl Pts',(-1.67239348737615,-18.048,279.594751766349));
#148646=CARTESIAN_POINT('Ctrl Pts',(-3.31631129755346,-17.7406985030951,
278.10063411929));
#148647=CARTESIAN_POINT('Ctrl Pts',(-4.96022910773077,-17.4333970061901,
276.606516472231));
#148648=CARTESIAN_POINT('Ctrl Pts',(-6.51968959134574,-16.8292587962898,
275.112398825172));
#148649=CARTESIAN_POINT('Ctrl Pts',(-8.07915007496071,-16.2251205863895,
273.618281178114));
#148650=CARTESIAN_POINT('Ctrl Pts',(-9.50104767561052,-15.3447188656481,
272.124163531055));
#148651=CARTESIAN_POINT('Ctrl Pts',(-10.9229452762603,-14.4643171449067,
270.630045883996));
#148652=CARTESIAN_POINT('Ctrl Pts',(-12.1588589765331,-13.3376329379985,
269.135928236937));
#148653=CARTESIAN_POINT('Ctrl Pts',(-13.3947726768058,-12.2109487310903,
267.641810589878));
#148654=CARTESIAN_POINT('Ctrl Pts',(-14.4026149179538,-10.8763499173728,
266.14769294282));
#148655=CARTESIAN_POINT('Ctrl Pts',(-15.4104571591017,-9.54175110365538,
264.653575295761));
#148656=CARTESIAN_POINT('Ctrl Pts',(-16.1559070823762,-8.04468584505497,
263.159457648702));
#148657=CARTESIAN_POINT('Ctrl Pts',(-16.9013570056506,-6.54762058645456,
261.665340001643));
#148658=CARTESIAN_POINT('Ctrl Pts',(-17.3590292079831,-4.93906964482095,
260.171222354584));
#148659=CARTESIAN_POINT('Ctrl Pts',(-17.8167014103155,-3.33051870318735,
258.677104707525));
#148660=CARTESIAN_POINT('Ctrl Pts',(-17.9710104137728,-1.66525935159368,
257.182987060467));
#148661=CARTESIAN_POINT('Ctrl Pts',(-18.1253194172301,-1.10985572039171E-15,
255.688869413408));
#148662=CARTESIAN_POINT('Ctrl Pts',(-17.9710104137728,1.66525935159367,
254.194751766349));
#148663=CARTESIAN_POINT('Ctrl Pts',(-17.8167014103155,3.33051870318735,
252.70063411929));
#148664=CARTESIAN_POINT('Ctrl Pts',(-17.3590292079831,4.93906964482096,
251.206516472231));
#148665=CARTESIAN_POINT('Ctrl Pts',(-16.9013570056506,6.54762058645456,
249.712398825173));
#148666=CARTESIAN_POINT('Ctrl Pts',(-16.1559070823762,8.04468584505497,
248.218281178114));
#148667=CARTESIAN_POINT('Ctrl Pts',(-15.4104571591017,9.54175110365538,
246.724163531055));
#148668=CARTESIAN_POINT('Ctrl Pts',(-14.4026149179538,10.8763499173728,
245.230045883996));
#148669=CARTESIAN_POINT('Ctrl Pts',(-13.3947726768058,12.2109487310903,
243.735928236937));
#148670=CARTESIAN_POINT('Ctrl Pts',(-12.1588589765331,13.3376329379985,
242.241810589878));
#148671=CARTESIAN_POINT('Ctrl Pts',(-10.9229452762603,14.4643171449067,
240.74769294282));
#148672=CARTESIAN_POINT('Ctrl Pts',(-9.50104767561052,15.3447188656481,
239.253575295761));
#148673=CARTESIAN_POINT('Ctrl Pts',(-8.07915007496071,16.2251205863895,
237.759457648702));
#148674=CARTESIAN_POINT('Ctrl Pts',(-6.51968959134574,16.8292587962898,
236.265340001643));
#148675=CARTESIAN_POINT('Ctrl Pts',(-4.96022910773078,17.4333970061901,
234.771222354584));
#148676=CARTESIAN_POINT('Ctrl Pts',(-3.31631129755346,17.7406985030951,
233.277104707525));
#148677=CARTESIAN_POINT('Ctrl Pts',(-1.67239348737615,18.048,231.782987060467));
#148678=CARTESIAN_POINT('Ctrl Pts',(-2.21024254310115E-15,18.048,230.288869413408));
#148679=CARTESIAN_POINT('Ctrl Pts',(1.67239348737616,18.048,228.794751766349));
#148680=CARTESIAN_POINT('Ctrl Pts',(3.31631129755346,17.7406985030951,227.30063411929));
#148681=CARTESIAN_POINT('Ctrl Pts',(4.96022910773077,17.4333970061901,225.806516472231));
#148682=CARTESIAN_POINT('Ctrl Pts',(6.51968959134575,16.8292587962898,224.312398825173));
#148683=CARTESIAN_POINT('Ctrl Pts',(8.07915007496071,16.2251205863895,222.818281178114));
#148684=CARTESIAN_POINT('Ctrl Pts',(9.50104767561053,15.3447188656481,221.324163531055));
#148685=CARTESIAN_POINT('Ctrl Pts',(10.9229452762603,14.4643171449067,219.830045883996));
#148686=CARTESIAN_POINT('Ctrl Pts',(12.1588589765331,13.3376329379985,218.335928236937));
#148687=CARTESIAN_POINT('Ctrl Pts',(13.3947726768058,12.2109487310903,216.841810589878));
#148688=CARTESIAN_POINT('Ctrl Pts',(14.4026149179538,10.8763499173728,215.34769294282));
#148689=CARTESIAN_POINT('Ctrl Pts',(15.4104571591017,9.54175110365538,213.853575295761));
#148690=CARTESIAN_POINT('Ctrl Pts',(16.1559070823762,8.04468584505496,212.359457648702));
#148691=CARTESIAN_POINT('Ctrl Pts',(16.9013570056506,6.54762058645456,210.865340001643));
#148692=CARTESIAN_POINT('Ctrl Pts',(17.3590292079831,4.93906964482096,209.371222354584));
#148693=CARTESIAN_POINT('Ctrl Pts',(17.8167014103155,3.33051870318735,207.877104707525));
#148694=CARTESIAN_POINT('Ctrl Pts',(17.9710104137728,1.66525935159367,206.382987060467));
#148695=CARTESIAN_POINT('Ctrl Pts',(18.1253194172301,3.32956716117513E-15,
204.888869413408));
#148696=CARTESIAN_POINT('Ctrl Pts',(17.9710104137728,-1.66525935159367,
203.394751766349));
#148697=CARTESIAN_POINT('Ctrl Pts',(17.8167014103155,-3.33051870318736,
201.90063411929));
#148698=CARTESIAN_POINT('Ctrl Pts',(17.3590292079831,-4.93906964482095,
200.406516472231));
#148699=CARTESIAN_POINT('Ctrl Pts',(16.9013570056506,-6.54762058645456,
198.912398825172));
#148700=CARTESIAN_POINT('Ctrl Pts',(16.1559070823762,-8.04468584505497,
197.418281178114));
#148701=CARTESIAN_POINT('Ctrl Pts',(15.4104571591017,-9.54175110365538,
195.924163531055));
#148702=CARTESIAN_POINT('Ctrl Pts',(14.4026149179538,-10.8763499173728,
194.430045883996));
#148703=CARTESIAN_POINT('Ctrl Pts',(13.3947726768058,-12.2109487310903,
192.935928236937));
#148704=CARTESIAN_POINT('Ctrl Pts',(12.1588589765331,-13.3376329379985,
191.441810589878));
#148705=CARTESIAN_POINT('Ctrl Pts',(10.9229452762603,-14.4643171449067,
189.94769294282));
#148706=CARTESIAN_POINT('Ctrl Pts',(9.50104767561053,-15.3447188656481,
188.453575295761));
#148707=CARTESIAN_POINT('Ctrl Pts',(8.07915007496071,-16.2251205863895,
186.959457648702));
#148708=CARTESIAN_POINT('Ctrl Pts',(6.51968959134574,-16.8292587962898,
185.465340001643));
#148709=CARTESIAN_POINT('Ctrl Pts',(4.96022910773078,-17.4333970061901,
183.971222354584));
#148710=CARTESIAN_POINT('Ctrl Pts',(3.31631129755346,-17.7406985030951,
182.477104707526));
#148711=CARTESIAN_POINT('Ctrl Pts',(1.67239348737615,-18.048,180.982987060467));
#148712=CARTESIAN_POINT('Ctrl Pts',(0.,-18.048,179.488869413408));
#148713=CARTESIAN_POINT('Ctrl Pts',(-1.67239348737615,-18.048,177.994751766349));
#148714=CARTESIAN_POINT('Ctrl Pts',(-3.31631129755346,-17.7406985030951,
176.50063411929));
#148715=CARTESIAN_POINT('Ctrl Pts',(-4.96022910773077,-17.4333970061901,
175.006516472231));
#148716=CARTESIAN_POINT('Ctrl Pts',(-6.51968959134574,-16.8292587962898,
173.512398825173));
#148717=CARTESIAN_POINT('Ctrl Pts',(-8.07915007496071,-16.2251205863895,
172.018281178114));
#148718=CARTESIAN_POINT('Ctrl Pts',(-9.50104767561052,-15.3447188656481,
170.524163531055));
#148719=CARTESIAN_POINT('Ctrl Pts',(-10.9229452762603,-14.4643171449067,
169.030045883996));
#148720=CARTESIAN_POINT('Ctrl Pts',(-12.1588589765331,-13.3376329379985,
167.535928236937));
#148721=CARTESIAN_POINT('Ctrl Pts',(-13.3947726768058,-12.2109487310903,
166.041810589878));
#148722=CARTESIAN_POINT('Ctrl Pts',(-14.4026149179538,-10.8763499173728,
164.54769294282));
#148723=CARTESIAN_POINT('Ctrl Pts',(-15.4104571591017,-9.54175110365538,
163.053575295761));
#148724=CARTESIAN_POINT('Ctrl Pts',(-16.1559070823762,-8.04468584505497,
161.559457648702));
#148725=CARTESIAN_POINT('Ctrl Pts',(-16.9013570056506,-6.54762058645456,
160.065340001643));
#148726=CARTESIAN_POINT('Ctrl Pts',(-17.3590292079831,-4.93906964482095,
158.571222354584));
#148727=CARTESIAN_POINT('Ctrl Pts',(-17.8167014103155,-3.33051870318735,
157.077104707525));
#148728=CARTESIAN_POINT('Ctrl Pts',(-17.9710104137728,-1.66525935159368,
155.582987060467));
#148729=CARTESIAN_POINT('Ctrl Pts',(-18.1253194172301,-1.10985572039171E-15,
154.088869413408));
#148730=CARTESIAN_POINT('Ctrl Pts',(-17.9710104137728,1.66525935159367,
152.594751766349));
#148731=CARTESIAN_POINT('Ctrl Pts',(-17.8167014103155,3.33051870318735,
151.10063411929));
#148732=CARTESIAN_POINT('Ctrl Pts',(-17.3590292079831,4.93906964482096,
149.606516472231));
#148733=CARTESIAN_POINT('Ctrl Pts',(-16.9013570056506,6.54762058645456,
148.112398825172));
#148734=CARTESIAN_POINT('Ctrl Pts',(-16.1559070823762,8.04468584505497,
146.618281178114));
#148735=CARTESIAN_POINT('Ctrl Pts',(-15.4104571591017,9.54175110365538,
145.124163531055));
#148736=CARTESIAN_POINT('Ctrl Pts',(-14.4026149179538,10.8763499173728,
143.630045883996));
#148737=CARTESIAN_POINT('Ctrl Pts',(-13.3947726768058,12.2109487310903,
142.135928236937));
#148738=CARTESIAN_POINT('Ctrl Pts',(-12.1588589765331,13.3376329379985,
140.641810589878));
#148739=CARTESIAN_POINT('Ctrl Pts',(-10.9229452762603,14.4643171449067,
139.147692942819));
#148740=CARTESIAN_POINT('Ctrl Pts',(-9.50104767561052,15.3447188656481,
137.653575295761));
#148741=CARTESIAN_POINT('Ctrl Pts',(-8.07915007496071,16.2251205863895,
136.159457648702));
#148742=CARTESIAN_POINT('Ctrl Pts',(-6.51968959134574,16.8292587962898,
134.665340001643));
#148743=CARTESIAN_POINT('Ctrl Pts',(-4.96022910773078,17.4333970061901,
133.171222354584));
#148744=CARTESIAN_POINT('Ctrl Pts',(-3.31631129755346,17.7406985030951,
131.677104707525));
#148745=CARTESIAN_POINT('Ctrl Pts',(-1.67239348737615,18.048,130.182987060467));
#148746=CARTESIAN_POINT('Ctrl Pts',(-2.21024254310115E-15,18.048,128.688869413408));
#148747=CARTESIAN_POINT('Ctrl Pts',(1.67239348737616,18.048,127.194751766349));
#148748=CARTESIAN_POINT('Ctrl Pts',(3.31631129755346,17.7406985030951,125.70063411929));
#148749=CARTESIAN_POINT('Ctrl Pts',(4.96022910773077,17.4333970061901,124.206516472231));
#148750=CARTESIAN_POINT('Ctrl Pts',(6.51968959134575,16.8292587962898,122.712398825173));
#148751=CARTESIAN_POINT('Ctrl Pts',(8.07915007496071,16.2251205863895,121.218281178114));
#148752=CARTESIAN_POINT('Ctrl Pts',(9.50104767561053,15.3447188656481,119.724163531055));
#148753=CARTESIAN_POINT('Ctrl Pts',(10.9229452762603,14.4643171449067,118.230045883996));
#148754=CARTESIAN_POINT('Ctrl Pts',(12.1588589765331,13.3376329379985,116.735928236937));
#148755=CARTESIAN_POINT('Ctrl Pts',(13.3947726768058,12.2109487310903,115.241810589878));
#148756=CARTESIAN_POINT('Ctrl Pts',(14.4026149179538,10.8763499173728,113.74769294282));
#148757=CARTESIAN_POINT('Ctrl Pts',(15.4104571591017,9.54175110365538,112.253575295761));
#148758=CARTESIAN_POINT('Ctrl Pts',(16.1559070823762,8.04468584505496,110.759457648702));
#148759=CARTESIAN_POINT('Ctrl Pts',(16.9013570056506,6.54762058645456,109.265340001643));
#148760=CARTESIAN_POINT('Ctrl Pts',(17.3590292079831,4.93906964482096,107.771222354584));
#148761=CARTESIAN_POINT('Ctrl Pts',(17.8167014103155,3.33051870318735,106.277104707526));
#148762=CARTESIAN_POINT('Ctrl Pts',(17.9710104137728,1.66525935159367,104.782987060467));
#148763=CARTESIAN_POINT('Ctrl Pts',(18.1253194172301,3.32956716117513E-15,
103.288869413408));
#148764=CARTESIAN_POINT('Ctrl Pts',(17.9710104137728,-1.66525935159367,
101.794751766349));
#148765=CARTESIAN_POINT('Ctrl Pts',(17.8167014103155,-3.33051870318736,
100.30063411929));
#148766=CARTESIAN_POINT('Ctrl Pts',(17.3590292079831,-4.93906964482095,
98.8065164722314));
#148767=CARTESIAN_POINT('Ctrl Pts',(16.9013570056506,-6.54762058645456,
97.3123988251725));
#148768=CARTESIAN_POINT('Ctrl Pts',(16.1559070823762,-8.04468584505497,
95.8182811781136));
#148769=CARTESIAN_POINT('Ctrl Pts',(15.4104571591017,-9.54175110365538,
94.3241635310548));
#148770=CARTESIAN_POINT('Ctrl Pts',(14.4026149179538,-10.8763499173728,
92.8300458839961));
#148771=CARTESIAN_POINT('Ctrl Pts',(13.3947726768058,-12.2109487310903,
91.3359282369372));
#148772=CARTESIAN_POINT('Ctrl Pts',(12.1588589765331,-13.3376329379985,
89.8418105898784));
#148773=CARTESIAN_POINT('Ctrl Pts',(10.9229452762603,-14.4643171449067,
88.3476929428195));
#148774=CARTESIAN_POINT('Ctrl Pts',(9.50104767561053,-15.3447188656481,
86.8535752957606));
#148775=CARTESIAN_POINT('Ctrl Pts',(8.07915007496071,-16.2251205863895,
85.359457648702));
#148776=CARTESIAN_POINT('Ctrl Pts',(6.51968959134574,-16.8292587962898,
83.8653400016432));
#148777=CARTESIAN_POINT('Ctrl Pts',(4.96022910773078,-17.4333970061901,
82.3712223545843));
#148778=CARTESIAN_POINT('Ctrl Pts',(3.31631129755346,-17.7406985030951,
80.8771047075254));
#148779=CARTESIAN_POINT('Ctrl Pts',(1.67239348737615,-18.048,79.3829870604665));
#148780=CARTESIAN_POINT('Ctrl Pts',(0.,-18.048,77.8888694134079));
#148781=CARTESIAN_POINT('Ctrl Pts',(-1.67239348737615,-18.048,76.394751766349));
#148782=CARTESIAN_POINT('Ctrl Pts',(-3.31631129755346,-17.7406985030951,
74.9006341192902));
#148783=CARTESIAN_POINT('Ctrl Pts',(-4.96022910773077,-17.4333970061901,
73.4065164722313));
#148784=CARTESIAN_POINT('Ctrl Pts',(-6.51968959134574,-16.8292587962898,
71.9123988251724));
#148785=CARTESIAN_POINT('Ctrl Pts',(-8.07915007496071,-16.2251205863895,
70.4182811781138));
#148786=CARTESIAN_POINT('Ctrl Pts',(-9.50104767561052,-15.3447188656481,
68.9241635310549));
#148787=CARTESIAN_POINT('Ctrl Pts',(-10.9229452762603,-14.4643171449067,
67.430045883996));
#148788=CARTESIAN_POINT('Ctrl Pts',(-12.1588589765331,-13.3376329379985,
65.9359282369372));
#148789=CARTESIAN_POINT('Ctrl Pts',(-13.3947726768058,-12.2109487310903,
64.4418105898783));
#148790=CARTESIAN_POINT('Ctrl Pts',(-14.4026149179538,-10.8763499173728,
62.9476929428197));
#148791=CARTESIAN_POINT('Ctrl Pts',(-15.4104571591017,-9.54175110365538,
61.4535752957608));
#148792=CARTESIAN_POINT('Ctrl Pts',(-16.1559070823762,-8.04468584505497,
59.9594576487019));
#148793=CARTESIAN_POINT('Ctrl Pts',(-16.9013570056506,-6.54762058645456,
58.4653400016431));
#148794=CARTESIAN_POINT('Ctrl Pts',(-17.3590292079831,-4.93906964482095,
56.9712223545842));
#148795=CARTESIAN_POINT('Ctrl Pts',(-17.8167014103155,-3.33051870318735,
55.4771047075255));
#148796=CARTESIAN_POINT('Ctrl Pts',(-17.9710104137728,-1.66525935159368,
53.9829870604667));
#148797=CARTESIAN_POINT('Ctrl Pts',(-18.1253194172301,-1.10985572039171E-15,
52.4888694134078));
#148798=CARTESIAN_POINT('Ctrl Pts',(-17.9710104137728,1.66525935159367,
50.9947517663489));
#148799=CARTESIAN_POINT('Ctrl Pts',(-17.8167014103155,3.33051870318735,
49.5006341192901));
#148800=CARTESIAN_POINT('Ctrl Pts',(-17.3590292079831,4.93906964482096,
48.0065164722314));
#148801=CARTESIAN_POINT('Ctrl Pts',(-16.9013570056506,6.54762058645456,
46.5123988251726));
#148802=CARTESIAN_POINT('Ctrl Pts',(-16.1559070823762,8.04468584505497,
45.0182811781137));
#148803=CARTESIAN_POINT('Ctrl Pts',(-15.4104571591017,9.54175110365538,
43.5241635310548));
#148804=CARTESIAN_POINT('Ctrl Pts',(-14.4026149179538,10.8763499173728,
42.0300458839959));
#148805=CARTESIAN_POINT('Ctrl Pts',(-13.3947726768058,12.2109487310903,
40.5359282369373));
#148806=CARTESIAN_POINT('Ctrl Pts',(-12.1588589765331,13.3376329379985,
39.0418105898784));
#148807=CARTESIAN_POINT('Ctrl Pts',(-10.9229452762603,14.4643171449067,
37.5476929428196));
#148808=CARTESIAN_POINT('Ctrl Pts',(-9.50104767561052,15.3447188656481,
36.0535752957607));
#148809=CARTESIAN_POINT('Ctrl Pts',(-8.07915007496071,16.2251205863895,
34.5594576487018));
#148810=CARTESIAN_POINT('Ctrl Pts',(-6.51968959134574,16.8292587962898,
33.0653400016432));
#148811=CARTESIAN_POINT('Ctrl Pts',(-4.96022910773078,17.4333970061901,
31.5712223545843));
#148812=CARTESIAN_POINT('Ctrl Pts',(-3.31631129755346,17.7406985030951,
30.0771047075255));
#148813=CARTESIAN_POINT('Ctrl Pts',(-1.67239348737615,18.048,28.5829870604666));
#148814=CARTESIAN_POINT('Ctrl Pts',(-2.21024254310115E-15,18.048,27.0888694134077));
#148815=CARTESIAN_POINT('Ctrl Pts',(1.67239348737616,18.048,25.5947517663491));
#148816=CARTESIAN_POINT('Ctrl Pts',(3.31631129755346,17.7406985030951,24.1006341192902));
#148817=CARTESIAN_POINT('Ctrl Pts',(4.96022910773077,17.4333970061901,22.6065164722313));
#148818=CARTESIAN_POINT('Ctrl Pts',(6.51968959134575,16.8292587962898,21.1123988251725));
#148819=CARTESIAN_POINT('Ctrl Pts',(8.07915007496071,16.2251205863895,19.6182811781136));
#148820=CARTESIAN_POINT('Ctrl Pts',(9.50104767561053,15.3447188656481,18.1241635310549));
#148821=CARTESIAN_POINT('Ctrl Pts',(10.9229452762603,14.4643171449067,16.6300458839961));
#148822=CARTESIAN_POINT('Ctrl Pts',(12.1588589765331,13.3376329379985,15.1359282369372));
#148823=CARTESIAN_POINT('Ctrl Pts',(13.3947726768058,12.2109487310903,13.6418105898783));
#148824=CARTESIAN_POINT('Ctrl Pts',(14.4026149179538,10.8763499173728,12.1476929428195));
#148825=CARTESIAN_POINT('Ctrl Pts',(15.4104571591017,9.54175110365538,10.6535752957608));
#148826=CARTESIAN_POINT('Ctrl Pts',(16.1559070823762,8.04468584505496,9.15945764870196));
#148827=CARTESIAN_POINT('Ctrl Pts',(16.9013570056506,6.54762058645456,7.6653400016431));
#148828=CARTESIAN_POINT('Ctrl Pts',(17.3590292079831,4.93906964482096,6.17122235458423));
#148829=CARTESIAN_POINT('Ctrl Pts',(17.8167014103155,3.33051870318735,4.67710470752536));
#148830=CARTESIAN_POINT('Ctrl Pts',(17.9710104137728,1.66525935159367,3.18298706046671));
#148831=CARTESIAN_POINT('Ctrl Pts',(18.1253194172301,3.32956716117513E-15,
1.68886941340785));
#148832=CARTESIAN_POINT('Ctrl Pts',(17.9710104137728,-1.66525935159367,
0.194751766348977));
#148833=CARTESIAN_POINT('Ctrl Pts',(17.8167014103155,-3.33051870318736,
-1.29936588070989));
#148834=CARTESIAN_POINT('Ctrl Pts',(17.3590292079831,-4.93906964482095,
-2.79348352776876));
#148835=CARTESIAN_POINT('Ctrl Pts',(16.9013570056506,-6.54762058645456,
-4.2876011748274));
#148836=CARTESIAN_POINT('Ctrl Pts',(16.1559070823762,-8.04468584505497,
-5.78171882188627));
#148837=CARTESIAN_POINT('Ctrl Pts',(15.4104571591017,-9.54175110365538,
-7.27583646894514));
#148838=CARTESIAN_POINT('Ctrl Pts',(14.4026149179538,-10.8763499173728,
-8.76995411600401));
#148839=CARTESIAN_POINT('Ctrl Pts',(13.3947726768058,-12.2109487310903,
-10.2640717630629));
#148840=CARTESIAN_POINT('Ctrl Pts',(12.1588589765331,-13.3376329379985,
-11.7581894101215));
#148841=CARTESIAN_POINT('Ctrl Pts',(10.9229452762603,-14.4643171449067,
-13.2523070571804));
#148842=CARTESIAN_POINT('Ctrl Pts',(9.50104767561053,-15.3447188656481,
-14.7464247042393));
#148843=CARTESIAN_POINT('Ctrl Pts',(8.07915007496071,-16.2251205863895,
-16.2405423512981));
#148844=CARTESIAN_POINT('Ctrl Pts',(6.51968959134574,-16.8292587962898,
-17.734659998357));
#148845=CARTESIAN_POINT('Ctrl Pts',(4.96022910773078,-17.4333970061901,
-19.2287776454156));
#148846=CARTESIAN_POINT('Ctrl Pts',(3.31631129755346,-17.7406985030951,
-20.7228952924745));
#148847=CARTESIAN_POINT('Ctrl Pts',(1.67239348737615,-18.048,-22.2170129395334));
#148848=CARTESIAN_POINT('Ctrl Pts',(0.,-18.048,-23.7111305865922));
#148849=CARTESIAN_POINT('Ctrl Pts',(-1.67239348737615,-18.048,-25.2052482336511));
#148850=CARTESIAN_POINT('Ctrl Pts',(-3.31631129755346,-17.7406985030951,
-26.6993658807098));
#148851=CARTESIAN_POINT('Ctrl Pts',(-4.96022910773077,-17.4333970061901,
-28.1934835277686));
#148852=CARTESIAN_POINT('Ctrl Pts',(-6.51968959134574,-16.8292587962898,
-29.6876011748275));
#148853=CARTESIAN_POINT('Ctrl Pts',(-8.07915007496071,-16.2251205863895,
-31.1817188218864));
#148854=CARTESIAN_POINT('Ctrl Pts',(-9.50104767561052,-15.3447188656481,
-32.6758364689452));
#148855=CARTESIAN_POINT('Ctrl Pts',(-10.9229452762603,-14.4643171449067,
-34.1699541160039));
#148856=CARTESIAN_POINT('Ctrl Pts',(-12.1588589765331,-13.3376329379985,
-35.6640717630627));
#148857=CARTESIAN_POINT('Ctrl Pts',(-13.3947726768058,-12.2109487310903,
-37.1581894101216));
#148858=CARTESIAN_POINT('Ctrl Pts',(-14.4026149179538,-10.8763499173728,
-38.6523070571805));
#148859=CARTESIAN_POINT('Ctrl Pts',(-15.4104571591017,-9.54175110365538,
-40.1464247042394));
#148860=CARTESIAN_POINT('Ctrl Pts',(-16.1559070823762,-8.04468584505497,
-41.640542351298));
#148861=CARTESIAN_POINT('Ctrl Pts',(-16.9013570056506,-6.54762058645456,
-43.1346599983569));
#148862=CARTESIAN_POINT('Ctrl Pts',(-17.3590292079831,-4.93906964482095,
-44.6287776454157));
#148863=CARTESIAN_POINT('Ctrl Pts',(-17.8167014103155,-3.33051870318735,
-46.1228952924746));
#148864=CARTESIAN_POINT('Ctrl Pts',(-17.9710104137728,-1.66525935159368,
-47.6170129395335));
#148865=CARTESIAN_POINT('Ctrl Pts',(-18.1253194172301,-1.10985572039171E-15,
-49.1111305865921));
#148866=CARTESIAN_POINT('Ctrl Pts',(-17.9710104137728,1.66525935159367,
-50.605248233651));
#148867=CARTESIAN_POINT('Ctrl Pts',(-17.8167014103155,3.33051870318735,
-52.0993658807098));
#148868=CARTESIAN_POINT('Ctrl Pts',(-17.3590292079831,4.93906964482096,
-53.5934835277687));
#148869=CARTESIAN_POINT('Ctrl Pts',(-16.9013570056506,6.54762058645456,
-55.0876011748276));
#148870=CARTESIAN_POINT('Ctrl Pts',(-16.1559070823762,8.04468584505497,
-56.5817188218862));
#148871=CARTESIAN_POINT('Ctrl Pts',(-15.4104571591017,9.54175110365538,
-58.0758364689451));
#148872=CARTESIAN_POINT('Ctrl Pts',(-14.4026149179538,10.8763499173728,
-59.569954116004));
#148873=CARTESIAN_POINT('Ctrl Pts',(-13.3947726768058,12.2109487310903,
-61.0640717630628));
#148874=CARTESIAN_POINT('Ctrl Pts',(-12.1588589765331,13.3376329379985,
-62.5581894101217));
#148875=CARTESIAN_POINT('Ctrl Pts',(-10.9229452762603,14.4643171449067,
-64.0523070571803));
#148876=CARTESIAN_POINT('Ctrl Pts',(-9.50104767561052,15.3447188656481,
-65.5464247042392));
#148877=CARTESIAN_POINT('Ctrl Pts',(-8.07915007496071,16.2251205863895,
-67.0405423512981));
#148878=CARTESIAN_POINT('Ctrl Pts',(-6.51968959134574,16.8292587962898,
-68.5346599983569));
#148879=CARTESIAN_POINT('Ctrl Pts',(-4.96022910773078,17.4333970061901,
-70.0287776454158));
#148880=CARTESIAN_POINT('Ctrl Pts',(-3.31631129755346,17.7406985030951,
-71.5228952924745));
#148881=CARTESIAN_POINT('Ctrl Pts',(-1.67239348737615,18.048,-73.0170129395333));
#148882=CARTESIAN_POINT('Ctrl Pts',(-2.21024254310115E-15,18.048,-74.5111305865922));
#148883=CARTESIAN_POINT('Ctrl Pts',(1.67239348737616,18.048,-76.0052482336511));
#148884=CARTESIAN_POINT('Ctrl Pts',(3.31631129755346,17.7406985030951,-77.4993658807099));
#148885=CARTESIAN_POINT('Ctrl Pts',(4.96022910773077,17.4333970061901,-78.9934835277686));
#148886=CARTESIAN_POINT('Ctrl Pts',(6.51968959134575,16.8292587962898,-80.4876011748274));
#148887=CARTESIAN_POINT('Ctrl Pts',(8.07915007496071,16.2251205863895,-81.9817188218863));
#148888=CARTESIAN_POINT('Ctrl Pts',(9.50104767561053,15.3447188656481,-83.4758364689452));
#148889=CARTESIAN_POINT('Ctrl Pts',(10.9229452762603,14.4643171449067,-84.9699541160041));
#148890=CARTESIAN_POINT('Ctrl Pts',(12.1588589765331,13.3376329379985,-86.4640717630627));
#148891=CARTESIAN_POINT('Ctrl Pts',(13.3947726768058,12.2109487310903,-87.9581894101216));
#148892=CARTESIAN_POINT('Ctrl Pts',(14.4026149179538,10.8763499173728,-89.4523070571804));
#148893=CARTESIAN_POINT('Ctrl Pts',(15.4104571591017,9.54175110365538,-90.9464247042393));
#148894=CARTESIAN_POINT('Ctrl Pts',(16.1559070823762,8.04468584505496,-92.4405423512982));
#148895=CARTESIAN_POINT('Ctrl Pts',(16.9013570056506,6.54762058645456,-93.9346599983568));
#148896=CARTESIAN_POINT('Ctrl Pts',(17.3590292079831,4.93906964482096,-95.4287776454157));
#148897=CARTESIAN_POINT('Ctrl Pts',(17.8167014103155,3.33051870318735,-96.9228952924745));
#148898=CARTESIAN_POINT('Ctrl Pts',(17.9710104137728,1.66525935159367,-98.4170129395334));
#148899=CARTESIAN_POINT('Ctrl Pts',(18.1253194172301,3.32956716117513E-15,
-99.9111305865923));
#148900=CARTESIAN_POINT('Ctrl Pts',(17.9710104137728,-1.66525935159367,
-101.405248233651));
#148901=CARTESIAN_POINT('Ctrl Pts',(17.8167014103155,-3.33051870318736,
-102.89936588071));
#148902=CARTESIAN_POINT('Ctrl Pts',(17.3590292079831,-4.93906964482095,
-104.393483527769));
#148903=CARTESIAN_POINT('Ctrl Pts',(16.9013570056506,-6.54762058645456,
-105.887601174828));
#148904=CARTESIAN_POINT('Ctrl Pts',(16.1559070823762,-8.04468584505497,
-107.381718821886));
#148905=CARTESIAN_POINT('Ctrl Pts',(15.4104571591017,-9.54175110365538,
-108.875836468945));
#148906=CARTESIAN_POINT('Ctrl Pts',(14.4026149179538,-10.8763499173728,
-110.369954116004));
#148907=CARTESIAN_POINT('Ctrl Pts',(13.3947726768058,-12.2109487310903,
-111.864071763063));
#148908=CARTESIAN_POINT('Ctrl Pts',(12.1588589765331,-13.3376329379985,
-113.358189410122));
#148909=CARTESIAN_POINT('Ctrl Pts',(10.9229452762603,-14.4643171449067,
-114.852307057181));
#148910=CARTESIAN_POINT('Ctrl Pts',(9.50104767561053,-15.3447188656481,
-116.346424704239));
#148911=CARTESIAN_POINT('Ctrl Pts',(8.07915007496071,-16.2251205863895,
-117.840542351298));
#148912=CARTESIAN_POINT('Ctrl Pts',(6.51968959134574,-16.8292587962898,
-119.334659998357));
#148913=CARTESIAN_POINT('Ctrl Pts',(4.96022910773078,-17.4333970061901,
-120.828777645416));
#148914=CARTESIAN_POINT('Ctrl Pts',(3.31631129755346,-17.7406985030951,
-122.322895292475));
#148915=CARTESIAN_POINT('Ctrl Pts',(1.67239348737615,-18.048,-123.817012939533));
#148916=CARTESIAN_POINT('Ctrl Pts',(0.,-18.048,-125.311130586592));
#148917=CARTESIAN_POINT('Ctrl Pts',(-1.67239348737615,-18.048,-126.805248233651));
#148918=CARTESIAN_POINT('Ctrl Pts',(-3.31631129755346,-17.7406985030951,
-128.29936588071));
#148919=CARTESIAN_POINT('Ctrl Pts',(-4.96022910773077,-17.4333970061901,
-129.793483527769));
#148920=CARTESIAN_POINT('Ctrl Pts',(-6.51968959134574,-16.8292587962898,
-131.287601174827));
#148921=CARTESIAN_POINT('Ctrl Pts',(-8.07915007496071,-16.2251205863895,
-132.781718821886));
#148922=CARTESIAN_POINT('Ctrl Pts',(-9.50104767561052,-15.3447188656481,
-134.275836468945));
#148923=CARTESIAN_POINT('Ctrl Pts',(-10.9229452762603,-14.4643171449067,
-135.769954116004));
#148924=CARTESIAN_POINT('Ctrl Pts',(-12.1588589765331,-13.3376329379985,
-137.264071763063));
#148925=CARTESIAN_POINT('Ctrl Pts',(-13.3947726768058,-12.2109487310903,
-138.758189410122));
#148926=CARTESIAN_POINT('Ctrl Pts',(-14.4026149179538,-10.8763499173728,
-140.25230705718));
#148927=CARTESIAN_POINT('Ctrl Pts',(-15.4104571591017,-9.54175110365538,
-141.746424704239));
#148928=CARTESIAN_POINT('Ctrl Pts',(-16.1559070823762,-8.04468584505497,
-143.240542351298));
#148929=CARTESIAN_POINT('Ctrl Pts',(-16.9013570056506,-6.54762058645456,
-144.734659998357));
#148930=CARTESIAN_POINT('Ctrl Pts',(-17.3590292079831,-4.93906964482095,
-146.228777645416));
#148931=CARTESIAN_POINT('Ctrl Pts',(-17.8167014103155,-3.33051870318735,
-147.722895292475));
#148932=CARTESIAN_POINT('Ctrl Pts',(-17.9710104137728,-1.66525935159368,
-149.217012939533));
#148933=CARTESIAN_POINT('Ctrl Pts',(-18.1253194172301,-1.10985572039171E-15,
-150.711130586592));
#148934=CARTESIAN_POINT('Ctrl Pts',(-17.9710104137728,1.66525935159367,
-152.205248233651));
#148935=CARTESIAN_POINT('Ctrl Pts',(-17.8167014103155,3.33051870318735,
-153.69936588071));
#148936=CARTESIAN_POINT('Ctrl Pts',(-17.3590292079831,4.93906964482096,
-155.193483527769));
#148937=CARTESIAN_POINT('Ctrl Pts',(-16.9013570056506,6.54762058645456,
-156.687601174828));
#148938=CARTESIAN_POINT('Ctrl Pts',(-16.1559070823762,8.04468584505497,
-158.181718821886));
#148939=CARTESIAN_POINT('Ctrl Pts',(-15.4104571591017,9.54175110365538,
-159.675836468945));
#148940=CARTESIAN_POINT('Ctrl Pts',(-14.4026149179538,10.8763499173728,
-161.169954116004));
#148941=CARTESIAN_POINT('Ctrl Pts',(-13.3947726768058,12.2109487310903,
-162.664071763063));
#148942=CARTESIAN_POINT('Ctrl Pts',(-12.1588589765331,13.3376329379985,
-164.158189410122));
#148943=CARTESIAN_POINT('Ctrl Pts',(-10.9229452762603,14.4643171449067,
-165.65230705718));
#148944=CARTESIAN_POINT('Ctrl Pts',(-9.50104767561052,15.3447188656481,
-167.146424704239));
#148945=CARTESIAN_POINT('Ctrl Pts',(-8.07915007496071,16.2251205863895,
-168.640542351298));
#148946=CARTESIAN_POINT('Ctrl Pts',(-6.51968959134574,16.8292587962898,
-170.134659998357));
#148947=CARTESIAN_POINT('Ctrl Pts',(-4.96022910773078,17.4333970061901,
-171.628777645416));
#148948=CARTESIAN_POINT('Ctrl Pts',(-3.31631129755346,17.7406985030951,
-173.122895292475));
#148949=CARTESIAN_POINT('Ctrl Pts',(-1.67239348737615,18.048,-174.617012939534));
#148950=CARTESIAN_POINT('Ctrl Pts',(-2.21024254310115E-15,18.048,-176.111130586592));
#148951=CARTESIAN_POINT('Ctrl Pts',(1.67239348737616,18.048,-177.605248233651));
#148952=CARTESIAN_POINT('Ctrl Pts',(3.31631129755346,17.7406985030951,-179.09936588071));
#148953=CARTESIAN_POINT('Ctrl Pts',(4.96022910773077,17.4333970061901,-180.593483527769));
#148954=CARTESIAN_POINT('Ctrl Pts',(6.51968959134575,16.8292587962898,-182.087601174828));
#148955=CARTESIAN_POINT('Ctrl Pts',(8.07915007496071,16.2251205863895,-183.581718821886));
#148956=CARTESIAN_POINT('Ctrl Pts',(9.50104767561053,15.3447188656481,-185.075836468945));
#148957=CARTESIAN_POINT('Ctrl Pts',(10.9229452762603,14.4643171449067,-186.569954116004));
#148958=CARTESIAN_POINT('Ctrl Pts',(12.1588589765331,13.3376329379985,-188.064071763063));
#148959=CARTESIAN_POINT('Ctrl Pts',(13.3947726768058,12.2109487310903,-189.558189410122));
#148960=CARTESIAN_POINT('Ctrl Pts',(14.4026149179538,10.8763499173728,-191.05230705718));
#148961=CARTESIAN_POINT('Ctrl Pts',(15.4104571591017,9.54175110365538,-192.546424704239));
#148962=CARTESIAN_POINT('Ctrl Pts',(16.1559070823762,8.04468584505496,-194.040542351298));
#148963=CARTESIAN_POINT('Ctrl Pts',(16.9013570056506,6.54762058645456,-195.534659998357));
#148964=CARTESIAN_POINT('Ctrl Pts',(17.3590292079831,4.93906964482096,-197.028777645416));
#148965=CARTESIAN_POINT('Ctrl Pts',(17.8167014103155,3.33051870318735,-198.522895292475));
#148966=CARTESIAN_POINT('Ctrl Pts',(17.9710104137728,1.66525935159367,-200.017012939533));
#148967=CARTESIAN_POINT('Ctrl Pts',(18.1253194172301,3.32956716117513E-15,
-201.511130586592));
#148968=CARTESIAN_POINT('Ctrl Pts',(17.9710104137728,-1.66525935159367,
-203.005248233651));
#148969=CARTESIAN_POINT('Ctrl Pts',(17.8167014103155,-3.33051870318736,
-204.49936588071));
#148970=CARTESIAN_POINT('Ctrl Pts',(17.3590292079831,-4.93906964482095,
-205.993483527769));
#148971=CARTESIAN_POINT('Ctrl Pts',(16.9013570056506,-6.54762058645456,
-207.487601174827));
#148972=CARTESIAN_POINT('Ctrl Pts',(16.1559070823762,-8.04468584505497,
-208.981718821886));
#148973=CARTESIAN_POINT('Ctrl Pts',(15.4104571591017,-9.54175110365538,
-210.475836468945));
#148974=CARTESIAN_POINT('Ctrl Pts',(14.4026149179538,-10.8763499173728,
-211.969954116004));
#148975=CARTESIAN_POINT('Ctrl Pts',(13.3947726768058,-12.2109487310903,
-213.464071763063));
#148976=CARTESIAN_POINT('Ctrl Pts',(12.1588589765331,-13.3376329379985,
-214.958189410122));
#148977=CARTESIAN_POINT('Ctrl Pts',(10.9229452762603,-14.4643171449067,
-216.45230705718));
#148978=CARTESIAN_POINT('Ctrl Pts',(9.50104767561053,-15.3447188656481,
-217.946424704239));
#148979=CARTESIAN_POINT('Ctrl Pts',(8.07915007496071,-16.2251205863895,
-219.440542351298));
#148980=CARTESIAN_POINT('Ctrl Pts',(6.51968959134574,-16.8292587962898,
-220.934659998357));
#148981=CARTESIAN_POINT('Ctrl Pts',(4.96022910773078,-17.4333970061901,
-222.428777645416));
#148982=CARTESIAN_POINT('Ctrl Pts',(3.31631129755346,-17.7406985030951,
-223.922895292475));
#148983=CARTESIAN_POINT('Ctrl Pts',(1.67239348737615,-18.048,-225.417012939533));
#148984=CARTESIAN_POINT('Ctrl Pts',(0.,-18.048,-226.911130586592));
#148985=CARTESIAN_POINT('Ctrl Pts',(-1.67239348737615,-18.048,-228.405248233651));
#148986=CARTESIAN_POINT('Ctrl Pts',(-3.31631129755346,-17.7406985030951,
-229.89936588071));
#148987=CARTESIAN_POINT('Ctrl Pts',(-4.96022910773077,-17.4333970061901,
-231.393483527769));
#148988=CARTESIAN_POINT('Ctrl Pts',(-6.51968959134574,-16.8292587962898,
-232.887601174828));
#148989=CARTESIAN_POINT('Ctrl Pts',(-8.07915007496071,-16.2251205863895,
-234.381718821886));
#148990=CARTESIAN_POINT('Ctrl Pts',(-9.50104767561052,-15.3447188656481,
-235.875836468945));
#148991=CARTESIAN_POINT('Ctrl Pts',(-10.9229452762603,-14.4643171449067,
-237.369954116004));
#148992=CARTESIAN_POINT('Ctrl Pts',(-12.1588589765331,-13.3376329379985,
-238.864071763063));
#148993=CARTESIAN_POINT('Ctrl Pts',(-13.3947726768058,-12.2109487310903,
-240.358189410122));
#148994=CARTESIAN_POINT('Ctrl Pts',(-14.4026149179538,-10.8763499173728,
-241.852307057181));
#148995=CARTESIAN_POINT('Ctrl Pts',(-15.4104571591017,-9.54175110365538,
-243.346424704239));
#148996=CARTESIAN_POINT('Ctrl Pts',(-16.1559070823762,-8.04468584505497,
-244.840542351298));
#148997=CARTESIAN_POINT('Ctrl Pts',(-16.9013570056506,-6.54762058645456,
-246.334659998357));
#148998=CARTESIAN_POINT('Ctrl Pts',(-17.3590292079831,-4.93906964482095,
-247.828777645416));
#148999=CARTESIAN_POINT('Ctrl Pts',(-17.8167014103155,-3.33051870318735,
-249.322895292475));
#149000=CARTESIAN_POINT('Ctrl Pts',(-17.9710104137728,-1.66525935159368,
-250.817012939533));
#149001=CARTESIAN_POINT('Ctrl Pts',(-18.1253194172301,-1.10985572039171E-15,
-252.311130586592));
#149002=CARTESIAN_POINT('Ctrl Pts',(-17.9710104137728,1.66525935159367,
-253.805248233651));
#149003=CARTESIAN_POINT('Ctrl Pts',(-17.8167014103155,3.33051870318735,
-255.29936588071));
#149004=CARTESIAN_POINT('Ctrl Pts',(-17.3590292079831,4.93906964482096,
-256.793483527769));
#149005=CARTESIAN_POINT('Ctrl Pts',(-16.9013570056506,6.54762058645456,
-258.287601174827));
#149006=CARTESIAN_POINT('Ctrl Pts',(-16.1559070823762,8.04468584505497,
-259.781718821886));
#149007=CARTESIAN_POINT('Ctrl Pts',(-15.4104571591017,9.54175110365538,
-261.275836468945));
#149008=CARTESIAN_POINT('Ctrl Pts',(-14.4026149179538,10.8763499173728,
-262.769954116004));
#149009=CARTESIAN_POINT('Ctrl Pts',(-13.3947726768058,12.2109487310903,
-264.264071763063));
#149010=CARTESIAN_POINT('Ctrl Pts',(-12.1588589765331,13.3376329379985,
-265.758189410122));
#149011=CARTESIAN_POINT('Ctrl Pts',(-10.9229452762603,14.4643171449067,
-267.25230705718));
#149012=CARTESIAN_POINT('Ctrl Pts',(-9.50104767561052,15.3447188656481,
-268.746424704239));
#149013=CARTESIAN_POINT('Ctrl Pts',(-8.07915007496071,16.2251205863895,
-270.240542351298));
#149014=CARTESIAN_POINT('Ctrl Pts',(-6.51968959134574,16.8292587962898,
-271.734659998357));
#149015=CARTESIAN_POINT('Ctrl Pts',(-4.96022910773078,17.4333970061901,
-273.228777645416));
#149016=CARTESIAN_POINT('Ctrl Pts',(-3.31631129755346,17.7406985030951,
-274.722895292475));
#149017=CARTESIAN_POINT('Ctrl Pts',(-1.67239348737615,18.048,-276.217012939533));
#149018=CARTESIAN_POINT('Ctrl Pts',(-2.21024254310115E-15,18.048,-277.711130586592));
#149019=CARTESIAN_POINT('Ctrl Pts',(1.67239348737616,18.048,-279.205248233651));
#149020=CARTESIAN_POINT('Ctrl Pts',(3.31631129755346,17.7406985030951,-280.69936588071));
#149021=CARTESIAN_POINT('Ctrl Pts',(4.96022910773077,17.4333970061901,-282.193483527769));
#149022=CARTESIAN_POINT('Ctrl Pts',(6.51968959134575,16.8292587962898,-283.687601174827));
#149023=CARTESIAN_POINT('Ctrl Pts',(8.07915007496071,16.2251205863895,-285.181718821886));
#149024=CARTESIAN_POINT('Ctrl Pts',(9.50104767561053,15.3447188656481,-286.675836468945));
#149025=CARTESIAN_POINT('Ctrl Pts',(10.9229452762603,14.4643171449067,-288.169954116004));
#149026=CARTESIAN_POINT('Ctrl Pts',(12.1588589765331,13.3376329379985,-289.664071763063));
#149027=CARTESIAN_POINT('Ctrl Pts',(13.3947726768058,12.2109487310903,-291.158189410122));
#149028=CARTESIAN_POINT('Ctrl Pts',(14.4026149179538,10.8763499173728,-292.652307057181));
#149029=CARTESIAN_POINT('Ctrl Pts',(15.4104571591017,9.54175110365538,-294.146424704239));
#149030=CARTESIAN_POINT('Ctrl Pts',(16.1559070823762,8.04468584505496,-295.640542351298));
#149031=CARTESIAN_POINT('Ctrl Pts',(16.9013570056506,6.54762058645456,-297.134659998357));
#149032=CARTESIAN_POINT('Ctrl Pts',(17.3590292079831,4.93906964482096,-298.628777645416));
#149033=CARTESIAN_POINT('Ctrl Pts',(17.8167014103155,3.33051870318735,-300.122895292475));
#149034=CARTESIAN_POINT('Ctrl Pts',(17.9710104137728,1.66525935159367,-301.617012939533));
#149035=CARTESIAN_POINT('Ctrl Pts',(18.1253194172301,3.32956716117513E-15,
-303.111130586592));
#149036=CARTESIAN_POINT('Ctrl Pts',(17.9710104137728,-1.66525935159367,
-304.605248233651));
#149037=CARTESIAN_POINT('Ctrl Pts',(17.8167014103155,-3.33051870318736,
-306.09936588071));
#149038=CARTESIAN_POINT('Ctrl Pts',(17.3590292079831,-4.93906964482095,
-307.593483527769));
#149039=CARTESIAN_POINT('Ctrl Pts',(16.9013570056506,-6.54762058645456,
-309.087601174828));
#149040=CARTESIAN_POINT('Ctrl Pts',(16.1559070823762,-8.04468584505497,
-310.581718821886));
#149041=CARTESIAN_POINT('Ctrl Pts',(15.4104571591017,-9.54175110365538,
-312.075836468945));
#149042=CARTESIAN_POINT('Ctrl Pts',(14.4026149179538,-10.8763499173728,
-313.569954116004));
#149043=CARTESIAN_POINT('Ctrl Pts',(13.3947726768058,-12.2109487310903,
-315.064071763063));
#149044=CARTESIAN_POINT('Ctrl Pts',(12.1588589765331,-13.3376329379985,
-316.558189410122));
#149045=CARTESIAN_POINT('Ctrl Pts',(10.9229452762603,-14.4643171449067,
-318.05230705718));
#149046=CARTESIAN_POINT('Ctrl Pts',(9.50104767561053,-15.3447188656481,
-319.546424704239));
#149047=CARTESIAN_POINT('Ctrl Pts',(8.07915007496071,-16.2251205863895,
-321.040542351298));
#149048=CARTESIAN_POINT('Ctrl Pts',(6.51968959134574,-16.8292587962898,
-322.534659998357));
#149049=CARTESIAN_POINT('Ctrl Pts',(4.96022910773078,-17.4333970061901,
-324.028777645416));
#149050=CARTESIAN_POINT('Ctrl Pts',(3.31631129755346,-17.7406985030951,
-325.522895292474));
#149051=CARTESIAN_POINT('Ctrl Pts',(1.67239348737615,-18.048,-327.017012939533));
#149052=CARTESIAN_POINT('Ctrl Pts',(0.,-18.048,-328.511130586592));
#149053=CARTESIAN_POINT('Ctrl Pts',(-1.67239348737615,-18.048,-330.005248233651));
#149054=CARTESIAN_POINT('Ctrl Pts',(-3.31631129755346,-17.7406985030951,
-331.49936588071));
#149055=CARTESIAN_POINT('Ctrl Pts',(-4.96022910773077,-17.4333970061901,
-332.993483527769));
#149056=CARTESIAN_POINT('Ctrl Pts',(-6.51968959134574,-16.8292587962898,
-334.487601174827));
#149057=CARTESIAN_POINT('Ctrl Pts',(-8.07915007496071,-16.2251205863895,
-335.981718821886));
#149058=CARTESIAN_POINT('Ctrl Pts',(-9.50104767561052,-15.3447188656481,
-337.475836468945));
#149059=CARTESIAN_POINT('Ctrl Pts',(-10.9229452762603,-14.4643171449067,
-338.969954116004));
#149060=CARTESIAN_POINT('Ctrl Pts',(-12.1588589765331,-13.3376329379985,
-340.464071763063));
#149061=CARTESIAN_POINT('Ctrl Pts',(-13.3947726768058,-12.2109487310903,
-341.958189410122));
#149062=CARTESIAN_POINT('Ctrl Pts',(-14.4026149179538,-10.8763499173728,
-343.45230705718));
#149063=CARTESIAN_POINT('Ctrl Pts',(-15.4104571591017,-9.54175110365538,
-344.946424704239));
#149064=CARTESIAN_POINT('Ctrl Pts',(-16.1559070823762,-8.04468584505497,
-346.440542351298));
#149065=CARTESIAN_POINT('Ctrl Pts',(-16.9013570056506,-6.54762058645456,
-347.934659998357));
#149066=CARTESIAN_POINT('Ctrl Pts',(-17.3590292079831,-4.93906964482095,
-349.428777645416));
#149067=CARTESIAN_POINT('Ctrl Pts',(-17.8167014103155,-3.33051870318735,
-350.922895292475));
#149068=CARTESIAN_POINT('Ctrl Pts',(-17.9710104137728,-1.66525935159368,
-352.417012939533));
#149069=CARTESIAN_POINT('Ctrl Pts',(-18.1253194172301,-1.10985572039171E-15,
-353.911130586592));
#149070=CARTESIAN_POINT('Ctrl Pts',(-17.9710104137728,1.66525935159367,
-355.405248233651));
#149071=CARTESIAN_POINT('Ctrl Pts',(-17.8167014103155,3.33051870318735,
-356.89936588071));
#149072=CARTESIAN_POINT('Ctrl Pts',(-17.3590292079831,4.93906964482096,
-358.393483527769));
#149073=CARTESIAN_POINT('Ctrl Pts',(-16.9013570056506,6.54762058645456,
-359.887601174828));
#149074=CARTESIAN_POINT('Ctrl Pts',(-16.1559070823762,8.04468584505497,
-361.381718821886));
#149075=CARTESIAN_POINT('Ctrl Pts',(-15.4104571591017,9.54175110365538,
-362.875836468945));
#149076=CARTESIAN_POINT('Ctrl Pts',(-14.4026149179538,10.8763499173728,
-364.369954116004));
#149077=CARTESIAN_POINT('Ctrl Pts',(-13.3947726768058,12.2109487310903,
-365.864071763063));
#149078=CARTESIAN_POINT('Ctrl Pts',(-12.1588589765331,13.3376329379985,
-367.358189410122));
#149079=CARTESIAN_POINT('Ctrl Pts',(-10.9229452762603,14.4643171449067,
-368.85230705718));
#149080=CARTESIAN_POINT('Ctrl Pts',(-9.50104767561052,15.3447188656481,
-370.346424704239));
#149081=CARTESIAN_POINT('Ctrl Pts',(-8.07915007496071,16.2251205863895,
-371.840542351298));
#149082=CARTESIAN_POINT('Ctrl Pts',(-6.51968959134574,16.8292587962898,
-373.334659998357));
#149083=CARTESIAN_POINT('Ctrl Pts',(-4.96022910773078,17.4333970061901,
-374.828777645416));
#149084=CARTESIAN_POINT('Ctrl Pts',(-3.31631129755346,17.7406985030951,
-376.322895292475));
#149085=CARTESIAN_POINT('Ctrl Pts',(-1.67239348737615,18.048,-377.817012939533));
#149086=CARTESIAN_POINT('Ctrl Pts',(-2.21024254310115E-15,18.048,-379.311130586592));
#149087=CARTESIAN_POINT('Ctrl Pts',(1.67239348737616,18.048,-380.805248233651));
#149088=CARTESIAN_POINT('Ctrl Pts',(3.31631129755346,17.7406985030951,-382.29936588071));
#149089=CARTESIAN_POINT('Ctrl Pts',(4.96022910773077,17.4333970061901,-383.793483527769));
#149090=CARTESIAN_POINT('Ctrl Pts',(6.51968959134575,16.8292587962898,-385.287601174827));
#149091=CARTESIAN_POINT('Ctrl Pts',(8.07915007496071,16.2251205863895,-386.781718821886));
#149092=CARTESIAN_POINT('Ctrl Pts',(9.50104767561053,15.3447188656481,-388.275836468945));
#149093=CARTESIAN_POINT('Ctrl Pts',(10.9229452762603,14.4643171449067,-389.769954116004));
#149094=CARTESIAN_POINT('Ctrl Pts',(12.1588589765331,13.3376329379985,-391.264071763063));
#149095=CARTESIAN_POINT('Ctrl Pts',(13.3947726768058,12.2109487310903,-392.758189410122));
#149096=CARTESIAN_POINT('Ctrl Pts',(14.4026149179538,10.8763499173728,-394.25230705718));
#149097=CARTESIAN_POINT('Ctrl Pts',(15.4104571591017,9.54175110365538,-395.746424704239));
#149098=CARTESIAN_POINT('Ctrl Pts',(16.1559070823762,8.04468584505496,-397.240542351298));
#149099=CARTESIAN_POINT('Ctrl Pts',(16.9013570056506,6.54762058645456,-398.734659998357));
#149100=CARTESIAN_POINT('Ctrl Pts',(17.3590292079831,4.93906964482096,-400.228777645416));
#149101=CARTESIAN_POINT('Ctrl Pts',(17.8167014103155,3.33051870318735,-401.722895292475));
#149102=CARTESIAN_POINT('Ctrl Pts',(17.9710104137728,1.66525935159367,-403.217012939533));
#149103=CARTESIAN_POINT('Ctrl Pts',(18.1253194172301,3.32956716117513E-15,
-404.711130586592));
#149104=CARTESIAN_POINT('Ctrl Pts',(17.9710104137728,-1.66525935159367,
-406.205248233651));
#149105=CARTESIAN_POINT('Ctrl Pts',(17.8167014103155,-3.33051870318736,
-407.69936588071));
#149106=CARTESIAN_POINT('Ctrl Pts',(17.3590292079831,-4.93906964482095,
-409.193483527769));
#149107=CARTESIAN_POINT('Ctrl Pts',(16.9013570056506,-6.54762058645456,
-410.687601174828));
#149108=CARTESIAN_POINT('Ctrl Pts',(16.1559070823762,-8.04468584505497,
-412.181718821886));
#149109=CARTESIAN_POINT('Ctrl Pts',(15.4104571591017,-9.54175110365538,
-413.675836468945));
#149110=CARTESIAN_POINT('Ctrl Pts',(14.4026149179538,-10.8763499173728,
-415.169954116004));
#149111=CARTESIAN_POINT('Ctrl Pts',(13.3947726768058,-12.2109487310903,
-416.664071763063));
#149112=CARTESIAN_POINT('Ctrl Pts',(12.1588589765331,-13.3376329379985,
-418.158189410122));
#149113=CARTESIAN_POINT('Ctrl Pts',(10.9229452762603,-14.4643171449067,
-419.652307057181));
#149114=CARTESIAN_POINT('Ctrl Pts',(9.50104767561053,-15.3447188656481,
-421.146424704239));
#149115=CARTESIAN_POINT('Ctrl Pts',(8.07915007496071,-16.2251205863895,
-422.640542351298));
#149116=CARTESIAN_POINT('Ctrl Pts',(6.51968959134574,-16.8292587962898,
-424.134659998357));
#149117=CARTESIAN_POINT('Ctrl Pts',(4.96022910773078,-17.4333970061901,
-425.628777645416));
#149118=CARTESIAN_POINT('Ctrl Pts',(3.31631129755346,-17.7406985030951,
-427.122895292475));
#149119=CARTESIAN_POINT('Ctrl Pts',(1.67239348737615,-18.048,-428.617012939534));
#149120=CARTESIAN_POINT('Ctrl Pts',(0.,-18.048,-430.111130586592));
#149121=CARTESIAN_POINT('Ctrl Pts',(-1.67239348737615,-18.048,-431.605248233651));
#149122=CARTESIAN_POINT('Ctrl Pts',(-3.31631129755346,-17.7406985030951,
-433.09936588071));
#149123=CARTESIAN_POINT('Ctrl Pts',(-4.96022910773077,-17.4333970061901,
-434.593483527769));
#149124=CARTESIAN_POINT('Ctrl Pts',(-6.51968959134574,-16.8292587962898,
-436.087601174828));
#149125=CARTESIAN_POINT('Ctrl Pts',(-8.07915007496071,-16.2251205863895,
-437.581718821886));
#149126=CARTESIAN_POINT('Ctrl Pts',(-9.50104767561052,-15.3447188656481,
-439.075836468945));
#149127=CARTESIAN_POINT('Ctrl Pts',(-10.9229452762603,-14.4643171449067,
-440.569954116004));
#149128=CARTESIAN_POINT('Ctrl Pts',(-12.1588589765331,-13.3376329379985,
-442.064071763063));
#149129=CARTESIAN_POINT('Ctrl Pts',(-13.3947726768058,-12.2109487310903,
-443.558189410122));
#149130=CARTESIAN_POINT('Ctrl Pts',(-14.4026149179538,-10.8763499173728,
-445.05230705718));
#149131=CARTESIAN_POINT('Ctrl Pts',(-15.4104571591017,-9.54175110365538,
-446.546424704239));
#149132=CARTESIAN_POINT('Ctrl Pts',(-16.1559070823762,-8.04468584505497,
-448.040542351298));
#149133=CARTESIAN_POINT('Ctrl Pts',(-16.9013570056506,-6.54762058645456,
-449.534659998357));
#149134=CARTESIAN_POINT('Ctrl Pts',(-17.3590292079831,-4.93906964482095,
-451.028777645416));
#149135=CARTESIAN_POINT('Ctrl Pts',(-17.8167014103155,-3.33051870318735,
-452.522895292475));
#149136=CARTESIAN_POINT('Ctrl Pts',(-17.9710104137728,-1.66525935159368,
-454.017012939533));
#149137=CARTESIAN_POINT('Ctrl Pts',(-18.1253194172301,-1.10985572039171E-15,
-455.511130586592));
#149138=CARTESIAN_POINT('Ctrl Pts',(-17.9710104137728,1.66525935159367,
-457.005248233651));
#149139=CARTESIAN_POINT('Ctrl Pts',(-17.8167014103155,3.33051870318735,
-458.49936588071));
#149140=CARTESIAN_POINT('Ctrl Pts',(-17.3590292079831,4.93906964482096,
-459.993483527769));
#149141=CARTESIAN_POINT('Ctrl Pts',(-16.9013570056506,6.54762058645456,
-461.487601174828));
#149142=CARTESIAN_POINT('Ctrl Pts',(-16.1559070823762,8.04468584505497,
-462.981718821886));
#149143=CARTESIAN_POINT('Ctrl Pts',(-15.4104571591017,9.54175110365538,
-464.475836468945));
#149144=CARTESIAN_POINT('Ctrl Pts',(-14.4026149179538,10.8763499173728,
-465.969954116004));
#149145=CARTESIAN_POINT('Ctrl Pts',(-13.3947726768058,12.2109487310903,
-467.464071763063));
#149146=CARTESIAN_POINT('Ctrl Pts',(-12.1588589765331,13.3376329379985,
-468.958189410122));
#149147=CARTESIAN_POINT('Ctrl Pts',(-10.9229452762603,14.4643171449067,
-470.45230705718));
#149148=CARTESIAN_POINT('Ctrl Pts',(-9.50104767561052,15.3447188656481,
-471.946424704239));
#149149=CARTESIAN_POINT('Ctrl Pts',(-8.07915007496071,16.2251205863895,
-473.440542351298));
#149150=CARTESIAN_POINT('Ctrl Pts',(-6.51968959134574,16.8292587962898,
-474.934659998357));
#149151=CARTESIAN_POINT('Ctrl Pts',(-4.96022910773078,17.4333970061901,
-476.428777645416));
#149152=CARTESIAN_POINT('Ctrl Pts',(-3.31631129755346,17.7406985030951,
-477.922895292475));
#149153=CARTESIAN_POINT('Ctrl Pts',(-1.67239348737615,18.048,-479.417012939533));
#149154=CARTESIAN_POINT('Ctrl Pts',(-2.21024254310115E-15,18.048,-480.911130586592));
#149155=CARTESIAN_POINT('Ctrl Pts',(1.67239348737616,18.048,-482.405248233651));
#149156=CARTESIAN_POINT('Ctrl Pts',(3.31631129755346,17.7406985030951,-483.89936588071));
#149157=CARTESIAN_POINT('Ctrl Pts',(4.96022910773077,17.4333970061901,-485.393483527769));
#149158=CARTESIAN_POINT('Ctrl Pts',(6.51968959134575,16.8292587962898,-486.887601174828));
#149159=CARTESIAN_POINT('Ctrl Pts',(8.07915007496071,16.2251205863895,-488.381718821887));
#149160=CARTESIAN_POINT('Ctrl Pts',(9.50104767561053,15.3447188656481,-489.875836468945));
#149161=CARTESIAN_POINT('Ctrl Pts',(10.9229452762603,14.4643171449067,-491.369954116004));
#149162=CARTESIAN_POINT('Ctrl Pts',(12.1588589765331,13.3376329379985,-492.864071763063));
#149163=CARTESIAN_POINT('Ctrl Pts',(13.3947726768058,12.2109487310903,-494.358189410122));
#149164=CARTESIAN_POINT('Ctrl Pts',(14.4026149179538,10.8763499173728,-495.852307057181));
#149165=CARTESIAN_POINT('Ctrl Pts',(15.4104571591017,9.54175110365538,-497.346424704239));
#149166=CARTESIAN_POINT('Ctrl Pts',(16.1559070823762,8.04468584505496,-498.840542351298));
#149167=CARTESIAN_POINT('Ctrl Pts',(16.9013570056506,6.54762058645456,-500.334659998357));
#149168=CARTESIAN_POINT('Ctrl Pts',(17.3590292079831,4.93906964482096,-501.828777645416));
#149169=CARTESIAN_POINT('Ctrl Pts',(17.8167014103155,3.33051870318735,-503.322895292475));
#149170=CARTESIAN_POINT('Ctrl Pts',(17.9710104137728,1.66525935159367,-504.817012939534));
#149171=CARTESIAN_POINT('Ctrl Pts',(18.1253194172301,3.32956716117513E-15,
-506.311130586592));
#149172=CARTESIAN_POINT('Ctrl Pts',(17.9710104137728,-1.66525935159367,
-507.805248233651));
#149173=CARTESIAN_POINT('Ctrl Pts',(17.8167014103155,-3.33051870318736,
-509.29936588071));
#149174=CARTESIAN_POINT('Ctrl Pts',(17.3590292079831,-4.93906964482095,
-510.793483527769));
#149175=CARTESIAN_POINT('Ctrl Pts',(16.9013570056506,-6.54762058645456,
-512.287601174828));
#149176=CARTESIAN_POINT('Ctrl Pts',(16.1559070823762,-8.04468584505497,
-513.781718821886));
#149177=CARTESIAN_POINT('Ctrl Pts',(15.4104571591017,-9.54175110365538,
-515.275836468945));
#149178=CARTESIAN_POINT('Ctrl Pts',(14.4026149179538,-10.8763499173728,
-516.769954116004));
#149179=CARTESIAN_POINT('Ctrl Pts',(13.3947726768058,-12.2109487310903,
-518.264071763063));
#149180=CARTESIAN_POINT('Ctrl Pts',(12.1588589765331,-13.3376329379985,
-519.758189410122));
#149181=CARTESIAN_POINT('Ctrl Pts',(10.9229452762603,-14.4643171449067,
-521.252307057181));
#149182=CARTESIAN_POINT('Ctrl Pts',(9.50104767561053,-15.3447188656481,
-522.746424704239));
#149183=CARTESIAN_POINT('Ctrl Pts',(8.07915007496071,-16.2251205863895,
-524.240542351298));
#149184=CARTESIAN_POINT('Ctrl Pts',(6.51968959134574,-16.8292587962898,
-525.734659998357));
#149185=CARTESIAN_POINT('Ctrl Pts',(4.96022910773078,-17.4333970061901,
-527.228777645416));
#149186=CARTESIAN_POINT('Ctrl Pts',(3.31631129755346,-17.7406985030951,
-528.722895292475));
#149187=CARTESIAN_POINT('Ctrl Pts',(1.67239348737615,-18.048,-530.217012939533));
#149188=CARTESIAN_POINT('Ctrl Pts',(0.,-18.048,-531.711130586592));
#149189=CARTESIAN_POINT('Ctrl Pts',(-1.67239348737615,-18.048,-533.205248233651));
#149190=CARTESIAN_POINT('Ctrl Pts',(-3.31631129755346,-17.7406985030951,
-534.69936588071));
#149191=CARTESIAN_POINT('Ctrl Pts',(-4.96022910773077,-17.4333970061901,
-536.193483527769));
#149192=CARTESIAN_POINT('Ctrl Pts',(-6.51968959134574,-16.8292587962898,
-537.687601174827));
#149193=CARTESIAN_POINT('Ctrl Pts',(-8.07915007496071,-16.2251205863895,
-539.181718821886));
#149194=CARTESIAN_POINT('Ctrl Pts',(-9.50104767561052,-15.3447188656481,
-540.675836468945));
#149195=CARTESIAN_POINT('Ctrl Pts',(-10.9229452762603,-14.4643171449067,
-542.169954116004));
#149196=CARTESIAN_POINT('Ctrl Pts',(-12.1588589765331,-13.3376329379985,
-543.664071763063));
#149197=CARTESIAN_POINT('Ctrl Pts',(-13.3947726768058,-12.2109487310903,
-545.158189410122));
#149198=CARTESIAN_POINT('Ctrl Pts',(-14.4026149179538,-10.8763499173728,
-546.65230705718));
#149199=CARTESIAN_POINT('Ctrl Pts',(-15.4104571591017,-9.54175110365538,
-548.14642470424));
#149200=CARTESIAN_POINT('Ctrl Pts',(-16.1559070823762,-8.04468584505497,
-549.640542351298));
#149201=CARTESIAN_POINT('Ctrl Pts',(-16.9013570056506,-6.54762058645456,
-551.134659998357));
#149202=CARTESIAN_POINT('Ctrl Pts',(-17.3590292079831,-4.93906964482095,
-552.628777645416));
#149203=CARTESIAN_POINT('Ctrl Pts',(-17.8167014103155,-3.33051870318735,
-554.122895292474));
#149204=CARTESIAN_POINT('Ctrl Pts',(-17.9710104137728,-1.66525935159368,
-555.617012939533));
#149205=CARTESIAN_POINT('Ctrl Pts',(-18.1253194172301,-1.10985572039171E-15,
-557.111130586592));
#149206=CARTESIAN_POINT('Ctrl Pts',(-17.9710104137728,1.66525935159367,
-558.605248233651));
#149207=CARTESIAN_POINT('Ctrl Pts',(-17.8167014103155,3.33051870318735,
-560.09936588071));
#149208=CARTESIAN_POINT('Ctrl Pts',(-17.3590292079831,4.93906964482096,
-561.593483527769));
#149209=CARTESIAN_POINT('Ctrl Pts',(-16.9013570056506,6.54762058645456,
-563.087601174828));
#149210=CARTESIAN_POINT('Ctrl Pts',(-16.1559070823762,8.04468584505497,
-564.581718821887));
#149211=CARTESIAN_POINT('Ctrl Pts',(-15.4104571591017,9.54175110365538,
-566.075836468945));
#149212=CARTESIAN_POINT('Ctrl Pts',(-14.4026149179538,10.8763499173728,
-567.569954116004));
#149213=CARTESIAN_POINT('Ctrl Pts',(-13.3947726768058,12.2109487310903,
-569.064071763063));
#149214=CARTESIAN_POINT('Ctrl Pts',(-12.1588589765331,13.3376329379985,
-570.558189410121));
#149215=CARTESIAN_POINT('Ctrl Pts',(-10.9229452762603,14.4643171449067,
-572.05230705718));
#149216=CARTESIAN_POINT('Ctrl Pts',(-9.50104767561052,15.3447188656481,
-573.546424704239));
#149217=CARTESIAN_POINT('Ctrl Pts',(-8.07915007496071,16.2251205863895,
-575.040542351298));
#149218=CARTESIAN_POINT('Ctrl Pts',(-6.51968959134574,16.8292587962898,
-576.534659998357));
#149219=CARTESIAN_POINT('Ctrl Pts',(-4.96022910773078,17.4333970061901,
-578.028777645416));
#149220=CARTESIAN_POINT('Ctrl Pts',(-3.31631129755346,17.7406985030951,
-579.522895292475));
#149221=CARTESIAN_POINT('Ctrl Pts',(-1.67239348737615,18.048,-581.017012939534));
#149222=CARTESIAN_POINT('Ctrl Pts',(-2.21024254310115E-15,18.048,-582.511130586592));
#149223=CARTESIAN_POINT('Ctrl Pts',(1.67239348737616,18.048,-584.005248233651));
#149224=CARTESIAN_POINT('Ctrl Pts',(3.31631129755346,17.7406985030951,-585.49936588071));
#149225=CARTESIAN_POINT('Ctrl Pts',(4.96022910773077,17.4333970061901,-586.993483527769));
#149226=CARTESIAN_POINT('Ctrl Pts',(6.51968959134575,16.8292587962898,-588.487601174827));
#149227=CARTESIAN_POINT('Ctrl Pts',(8.07915007496071,16.2251205863895,-589.981718821886));
#149228=CARTESIAN_POINT('Ctrl Pts',(9.50104767561053,15.3447188656481,-591.475836468945));
#149229=CARTESIAN_POINT('Ctrl Pts',(10.9229452762603,14.4643171449067,-592.969954116004));
#149230=CARTESIAN_POINT('Ctrl Pts',(12.1588589765331,13.3376329379985,-594.464071763063));
#149231=CARTESIAN_POINT('Ctrl Pts',(13.3947726768058,12.2109487310903,-595.958189410122));
#149232=CARTESIAN_POINT('Ctrl Pts',(14.4026149179538,10.8763499173728,-597.45230705718));
#149233=CARTESIAN_POINT('Ctrl Pts',(15.4104571591017,9.54175110365538,-598.946424704239));
#149234=CARTESIAN_POINT('Ctrl Pts',(16.1559070823762,8.04468584505496,-600.440542351298));
#149235=CARTESIAN_POINT('Ctrl Pts',(16.9013570056506,6.54762058645456,-601.934659998357));
#149236=CARTESIAN_POINT('Ctrl Pts',(17.3590292079831,4.93906964482096,-603.428777645416));
#149237=CARTESIAN_POINT('Ctrl Pts',(17.8167014103155,3.33051870318735,-604.922895292475));
#149238=CARTESIAN_POINT('Ctrl Pts',(17.9710104137728,1.66525935159367,-606.417012939533));
#149239=CARTESIAN_POINT('Ctrl Pts',(18.1253194172301,3.32956716117513E-15,
-607.911130586592));
#149240=CARTESIAN_POINT('Ctrl Pts',(17.9710104137728,-1.66525935159367,
-609.405248233651));
#149241=CARTESIAN_POINT('Ctrl Pts',(17.8167014103155,-3.33051870318736,
-610.89936588071));
#149242=CARTESIAN_POINT('Ctrl Pts',(17.3590292079831,-4.93906964482095,
-612.393483527768));
#149243=CARTESIAN_POINT('Ctrl Pts',(16.9013570056506,-6.54762058645456,
-613.887601174828));
#149244=CARTESIAN_POINT('Ctrl Pts',(16.1559070823762,-8.04468584505497,
-615.381718821886));
#149245=CARTESIAN_POINT('Ctrl Pts',(15.4104571591017,-9.54175110365538,
-616.875836468945));
#149246=CARTESIAN_POINT('Ctrl Pts',(14.4026149179538,-10.8763499173728,
-618.369954116004));
#149247=CARTESIAN_POINT('Ctrl Pts',(13.3947726768058,-12.2109487310903,
-619.864071763063));
#149248=CARTESIAN_POINT('Ctrl Pts',(12.1588589765331,-13.3376329379985,
-621.358189410122));
#149249=CARTESIAN_POINT('Ctrl Pts',(10.9229452762603,-14.4643171449067,
-622.852307057181));
#149250=CARTESIAN_POINT('Ctrl Pts',(9.50104767561053,-15.3447188656481,
-624.346424704239));
#149251=CARTESIAN_POINT('Ctrl Pts',(8.07915007496071,-16.2251205863895,
-625.840542351298));
#149252=CARTESIAN_POINT('Ctrl Pts',(6.51968959134574,-16.8292587962898,
-627.334659998357));
#149253=CARTESIAN_POINT('Ctrl Pts',(4.96022910773078,-17.4333970061901,
-628.828777645416));
#149254=CARTESIAN_POINT('Ctrl Pts',(3.31631129755346,-17.7406985030951,
-630.322895292474));
#149255=CARTESIAN_POINT('Ctrl Pts',(1.67239348737615,-18.048,-631.817012939533));
#149256=CARTESIAN_POINT('Ctrl Pts',(0.,-18.048,-633.311130586592));
#149257=CARTESIAN_POINT('Ctrl Pts',(-1.67239348737615,-18.048,-634.805248233651));
#149258=CARTESIAN_POINT('Ctrl Pts',(-3.31631129755346,-17.7406985030951,
-636.29936588071));
#149259=CARTESIAN_POINT('Ctrl Pts',(-4.96022910773077,-17.4333970061901,
-637.793483527769));
#149260=CARTESIAN_POINT('Ctrl Pts',(-6.51968959134574,-16.8292587962898,
-639.287601174828));
#149261=CARTESIAN_POINT('Ctrl Pts',(-8.07915007496071,-16.2251205863895,
-640.781718821886));
#149262=CARTESIAN_POINT('Ctrl Pts',(-9.50104767561052,-15.3447188656481,
-642.275836468945));
#149263=CARTESIAN_POINT('Ctrl Pts',(-10.9229452762603,-14.4643171449067,
-643.769954116004));
#149264=CARTESIAN_POINT('Ctrl Pts',(-12.1588589765331,-13.3376329379985,
-645.264071763063));
#149265=CARTESIAN_POINT('Ctrl Pts',(-13.3947726768058,-12.2109487310903,
-646.758189410122));
#149266=CARTESIAN_POINT('Ctrl Pts',(-14.4026149179538,-10.8763499173728,
-648.25230705718));
#149267=CARTESIAN_POINT('Ctrl Pts',(-15.4104571591017,-9.54175110365538,
-649.746424704239));
#149268=CARTESIAN_POINT('Ctrl Pts',(-16.1559070823762,-8.04468584505497,
-651.240542351298));
#149269=CARTESIAN_POINT('Ctrl Pts',(-16.9013570056506,-6.54762058645456,
-652.734659998357));
#149270=CARTESIAN_POINT('Ctrl Pts',(-17.3590292079831,-4.93906964482095,
-654.228777645416));
#149271=CARTESIAN_POINT('Ctrl Pts',(-17.8167014103155,-3.33051870318735,
-655.722895292475));
#149272=CARTESIAN_POINT('Ctrl Pts',(-17.9710104137728,-1.66525935159368,
-657.217012939533));
#149273=CARTESIAN_POINT('Ctrl Pts',(-18.1253194172301,-1.10985572039171E-15,
-658.711130586592));
#149274=CARTESIAN_POINT('Ctrl Pts',(-17.9710104137728,1.66525935159367,
-660.205248233651));
#149275=CARTESIAN_POINT('Ctrl Pts',(-17.8167014103155,3.33051870318735,
-661.69936588071));
#149276=CARTESIAN_POINT('Ctrl Pts',(-17.3590292079831,4.93906964482096,
-663.193483527769));
#149277=CARTESIAN_POINT('Ctrl Pts',(-16.9013570056506,6.54762058645456,
-664.687601174827));
#149278=CARTESIAN_POINT('Ctrl Pts',(-16.1559070823762,8.04468584505497,
-666.181718821887));
#149279=CARTESIAN_POINT('Ctrl Pts',(-15.4104571591017,9.54175110365538,
-667.675836468945));
#149280=CARTESIAN_POINT('Ctrl Pts',(-14.4026149179538,10.8763499173728,
-669.169954116004));
#149281=CARTESIAN_POINT('Ctrl Pts',(-13.3947726768058,12.2109487310903,
-670.664071763063));
#149282=CARTESIAN_POINT('Ctrl Pts',(-12.1588589765331,13.3376329379985,
-672.158189410121));
#149283=CARTESIAN_POINT('Ctrl Pts',(-10.9229452762603,14.4643171449067,
-673.65230705718));
#149284=CARTESIAN_POINT('Ctrl Pts',(-9.50104767561052,15.3447188656481,
-675.146424704239));
#149285=CARTESIAN_POINT('Ctrl Pts',(-8.07915007496071,16.2251205863895,
-676.640542351298));
#149286=CARTESIAN_POINT('Ctrl Pts',(-6.51968959134574,16.8292587962898,
-678.134659998357));
#149287=CARTESIAN_POINT('Ctrl Pts',(-4.96022910773078,17.4333970061901,
-679.628777645416));
#149288=CARTESIAN_POINT('Ctrl Pts',(-3.31631129755346,17.7406985030951,
-681.122895292475));
#149289=CARTESIAN_POINT('Ctrl Pts',(-1.67239348737615,18.048,-682.617012939534));
#149290=CARTESIAN_POINT('Ctrl Pts',(-2.21024254310115E-15,18.048,-684.111130586592));
#149291=CARTESIAN_POINT('Ctrl Pts',(1.67239348737616,18.048,-685.605248233651));
#149292=CARTESIAN_POINT('Ctrl Pts',(3.31631129755346,17.7406985030951,-687.09936588071));
#149293=CARTESIAN_POINT('Ctrl Pts',(4.96022910773077,17.4333970061901,-688.593483527769));
#149294=CARTESIAN_POINT('Ctrl Pts',(6.51968959134575,16.8292587962898,-690.087601174827));
#149295=CARTESIAN_POINT('Ctrl Pts',(8.07915007496071,16.2251205863895,-691.581718821886));
#149296=CARTESIAN_POINT('Ctrl Pts',(9.50104767561053,15.3447188656481,-693.075836468945));
#149297=CARTESIAN_POINT('Ctrl Pts',(10.9229452762603,14.4643171449067,-694.569954116004));
#149298=CARTESIAN_POINT('Ctrl Pts',(12.1588589765331,13.3376329379985,-696.064071763063));
#149299=CARTESIAN_POINT('Ctrl Pts',(13.3947726768058,12.2109487310903,-697.558189410122));
#149300=CARTESIAN_POINT('Ctrl Pts',(14.4026149179538,10.8763499173728,-699.052307057181));
#149301=CARTESIAN_POINT('Ctrl Pts',(15.4104571591017,9.54175110365538,-700.546424704239));
#149302=CARTESIAN_POINT('Ctrl Pts',(16.1559070823762,8.04468584505496,-702.040542351298));
#149303=CARTESIAN_POINT('Ctrl Pts',(16.9013570056506,6.54762058645456,-703.534659998357));
#149304=CARTESIAN_POINT('Ctrl Pts',(17.3590292079831,4.93906964482096,-705.028777645416));
#149305=CARTESIAN_POINT('Ctrl Pts',(17.8167014103155,3.33051870318735,-706.522895292475));
#149306=CARTESIAN_POINT('Ctrl Pts',(17.9710104137728,1.66525935159367,-708.017012939533));
#149307=CARTESIAN_POINT('Ctrl Pts',(18.1253194172301,3.32956716117513E-15,
-709.511130586592));
#149308=CARTESIAN_POINT('Ctrl Pts',(17.9710104137728,-1.66525935159367,
-711.005248233651));
#149309=CARTESIAN_POINT('Ctrl Pts',(17.8167014103155,-3.33051870318736,
-712.49936588071));
#149310=CARTESIAN_POINT('Ctrl Pts',(17.3590292079831,-4.93906964482095,
-713.993483527769));
#149311=CARTESIAN_POINT('Ctrl Pts',(16.9013570056506,-6.54762058645456,
-715.487601174828));
#149312=CARTESIAN_POINT('Ctrl Pts',(16.1559070823762,-8.04468584505497,
-716.981718821886));
#149313=CARTESIAN_POINT('Ctrl Pts',(15.4104571591017,-9.54175110365538,
-718.475836468945));
#149314=CARTESIAN_POINT('Ctrl Pts',(14.4026149179538,-10.8763499173728,
-719.969954116004));
#149315=CARTESIAN_POINT('Ctrl Pts',(13.3947726768058,-12.2109487310903,
-721.464071763063));
#149316=CARTESIAN_POINT('Ctrl Pts',(12.1588589765331,-13.3376329379985,
-722.958189410122));
#149317=CARTESIAN_POINT('Ctrl Pts',(10.9229452762603,-14.4643171449067,
-724.452307057181));
#149318=CARTESIAN_POINT('Ctrl Pts',(9.50104767561053,-15.3447188656481,
-725.946424704239));
#149319=CARTESIAN_POINT('Ctrl Pts',(8.07915007496071,-16.2251205863895,
-727.440542351298));
#149320=CARTESIAN_POINT('Ctrl Pts',(6.51968959134574,-16.8292587962898,
-728.934659998357));
#149321=CARTESIAN_POINT('Ctrl Pts',(4.96022910773078,-17.4333970061901,
-730.428777645416));
#149322=CARTESIAN_POINT('Ctrl Pts',(3.31631129755346,-17.7406985030951,
-731.922895292474));
#149323=CARTESIAN_POINT('Ctrl Pts',(1.67239348737615,-18.048,-733.417012939533));
#149324=CARTESIAN_POINT('Ctrl Pts',(0.,-18.048,-734.911130586592));
#149325=CARTESIAN_POINT('Ctrl Pts',(-1.67239348737615,-18.048,-736.405248233651));
#149326=CARTESIAN_POINT('Ctrl Pts',(-3.31631129755346,-17.7406985030951,
-737.89936588071));
#149327=CARTESIAN_POINT('Ctrl Pts',(-4.96022910773077,-17.4333970061901,
-739.393483527769));
#149328=CARTESIAN_POINT('Ctrl Pts',(-6.51968959134574,-16.8292587962898,
-740.887601174828));
#149329=CARTESIAN_POINT('Ctrl Pts',(-8.07915007496071,-16.2251205863895,
-742.381718821887));
#149330=CARTESIAN_POINT('Ctrl Pts',(-9.50104767561052,-15.3447188656481,
-743.875836468945));
#149331=CARTESIAN_POINT('Ctrl Pts',(-10.9229452762603,-14.4643171449067,
-745.369954116004));
#149332=CARTESIAN_POINT('Ctrl Pts',(-12.1588589765331,-13.3376329379985,
-746.864071763063));
#149333=CARTESIAN_POINT('Ctrl Pts',(-13.3947726768058,-12.2109487310903,
-748.358189410122));
#149334=CARTESIAN_POINT('Ctrl Pts',(-14.4026149179538,-10.8763499173728,
-749.85230705718));
#149335=CARTESIAN_POINT('Ctrl Pts',(-15.4104571591017,-9.54175110365538,
-751.346424704239));
#149336=CARTESIAN_POINT('Ctrl Pts',(-16.1559070823762,-8.04468584505497,
-752.840542351298));
#149337=CARTESIAN_POINT('Ctrl Pts',(-16.9013570056506,-6.54762058645456,
-754.334659998357));
#149338=CARTESIAN_POINT('Ctrl Pts',(-17.3590292079831,-4.93906964482095,
-755.828777645416));
#149339=CARTESIAN_POINT('Ctrl Pts',(-17.8167014103155,-3.33051870318735,
-757.322895292475));
#149340=CARTESIAN_POINT('Ctrl Pts',(-17.9710104137728,-1.66525935159368,
-758.817012939534));
#149341=CARTESIAN_POINT('Ctrl Pts',(-18.1253194172301,-1.10985572039171E-15,
-760.311130586593));
#149342=CARTESIAN_POINT('Ctrl Pts',(-17.9710104137728,1.66525935159367,
-761.805248233651));
#149343=CARTESIAN_POINT('Ctrl Pts',(-17.8167014103155,3.33051870318735,
-763.29936588071));
#149344=CARTESIAN_POINT('Ctrl Pts',(-17.3590292079831,4.93906964482096,
-764.793483527769));
#149345=CARTESIAN_POINT('Ctrl Pts',(-16.9013570056506,6.54762058645456,
-766.287601174827));
#149346=CARTESIAN_POINT('Ctrl Pts',(-16.1559070823762,8.04468584505497,
-767.781718821886));
#149347=CARTESIAN_POINT('Ctrl Pts',(-15.4104571591017,9.54175110365538,
-769.275836468945));
#149348=CARTESIAN_POINT('Ctrl Pts',(-14.4026149179538,10.8763499173728,
-770.769954116004));
#149349=CARTESIAN_POINT('Ctrl Pts',(-13.3947726768058,12.2109487310903,
-772.264071763063));
#149350=CARTESIAN_POINT('Ctrl Pts',(-12.1588589765331,13.3376329379985,
-773.758189410122));
#149351=CARTESIAN_POINT('Ctrl Pts',(-10.9229452762603,14.4643171449067,
-775.252307057181));
#149352=CARTESIAN_POINT('Ctrl Pts',(-9.50104767561052,15.3447188656481,
-776.746424704239));
#149353=CARTESIAN_POINT('Ctrl Pts',(-8.07915007496071,16.2251205863895,
-778.240542351298));
#149354=CARTESIAN_POINT('Ctrl Pts',(-6.51968959134574,16.8292587962898,
-779.734659998357));
#149355=CARTESIAN_POINT('Ctrl Pts',(-4.96022910773078,17.4333970061901,
-781.228777645416));
#149356=CARTESIAN_POINT('Ctrl Pts',(-3.31631129755346,17.7406985030951,
-782.722895292475));
#149357=CARTESIAN_POINT('Ctrl Pts',(-1.67239348737615,18.048,-784.217012939534));
#149358=CARTESIAN_POINT('Ctrl Pts',(-2.21024254310115E-15,18.048,-785.711130586592));
#149359=CARTESIAN_POINT('Ctrl Pts',(1.67239348737616,18.048,-787.205248233651));
#149360=CARTESIAN_POINT('Ctrl Pts',(3.31631129755346,17.7406985030951,-788.69936588071));
#149361=CARTESIAN_POINT('Ctrl Pts',(4.96022910773077,17.4333970061901,-790.193483527769));
#149362=CARTESIAN_POINT('Ctrl Pts',(6.51968959134575,16.8292587962898,-791.687601174827));
#149363=CARTESIAN_POINT('Ctrl Pts',(8.07915007496071,16.2251205863895,-793.181718821886));
#149364=CARTESIAN_POINT('Ctrl Pts',(9.50104767561053,15.3447188656481,-794.675836468945));
#149365=CARTESIAN_POINT('Ctrl Pts',(10.9229452762603,14.4643171449067,-796.169954116004));
#149366=CARTESIAN_POINT('Ctrl Pts',(12.1588589765331,13.3376329379985,-797.664071763063));
#149367=CARTESIAN_POINT('Ctrl Pts',(13.3947726768058,12.2109487310903,-799.158189410122));
#149368=CARTESIAN_POINT('Ctrl Pts',(14.4026149179538,10.8763499173728,-800.65230705718));
#149369=CARTESIAN_POINT('Ctrl Pts',(15.4104571591017,9.54175110365538,-802.146424704239));
#149370=CARTESIAN_POINT('Ctrl Pts',(16.1559070823762,8.04468584505496,-803.640542351298));
#149371=CARTESIAN_POINT('Ctrl Pts',(16.9013570056506,6.54762058645456,-805.134659998357));
#149372=CARTESIAN_POINT('Ctrl Pts',(17.3590292079831,4.93906964482096,-806.628777645416));
#149373=CARTESIAN_POINT('Ctrl Pts',(17.8167014103155,3.33051870318735,-808.122895292474));
#149374=CARTESIAN_POINT('Ctrl Pts',(17.9710104137728,1.66525935159367,-809.617012939533));
#149375=CARTESIAN_POINT('Ctrl Pts',(18.1253194172301,3.32956716117513E-15,
-811.111130586592));
#149376=CARTESIAN_POINT('Ctrl Pts',(17.9710104137728,-1.66525935159367,
-812.605248233651));
#149377=CARTESIAN_POINT('Ctrl Pts',(17.8167014103155,-3.33051870318736,
-814.09936588071));
#149378=CARTESIAN_POINT('Ctrl Pts',(17.3590292079831,-4.93906964482095,
-815.593483527769));
#149379=CARTESIAN_POINT('Ctrl Pts',(16.9013570056506,-6.54762058645456,
-817.087601174828));
#149380=CARTESIAN_POINT('Ctrl Pts',(16.1559070823762,-8.04468584505497,
-818.581718821887));
#149381=CARTESIAN_POINT('Ctrl Pts',(15.4104571591017,-9.54175110365538,
-820.075836468945));
#149382=CARTESIAN_POINT('Ctrl Pts',(14.4026149179538,-10.8763499173728,
-821.569954116004));
#149383=CARTESIAN_POINT('Ctrl Pts',(13.3947726768058,-12.2109487310903,
-823.064071763063));
#149384=CARTESIAN_POINT('Ctrl Pts',(12.1588589765331,-13.3376329379985,
-824.558189410121));
#149385=CARTESIAN_POINT('Ctrl Pts',(10.9229452762603,-14.4643171449067,
-826.05230705718));
#149386=CARTESIAN_POINT('Ctrl Pts',(9.50104767561053,-15.3447188656481,
-827.546424704239));
#149387=CARTESIAN_POINT('Ctrl Pts',(8.07915007496071,-16.2251205863895,
-829.040542351298));
#149388=CARTESIAN_POINT('Ctrl Pts',(6.51968959134574,-16.8292587962898,
-830.534659998357));
#149389=CARTESIAN_POINT('Ctrl Pts',(4.96022910773078,-17.4333970061901,
-832.028777645416));
#149390=CARTESIAN_POINT('Ctrl Pts',(3.31631129755346,-17.7406985030951,
-833.522895292475));
#149391=CARTESIAN_POINT('Ctrl Pts',(1.67239348737615,-18.048,-835.017012939534));
#149392=CARTESIAN_POINT('Ctrl Pts',(0.,-18.048,-836.511130586592));
#149393=CARTESIAN_POINT('Ctrl Pts',(-1.67239348737615,-18.048,-838.005248233651));
#149394=CARTESIAN_POINT('Ctrl Pts',(-3.31631129755346,-17.7406985030951,
-839.49936588071));
#149395=CARTESIAN_POINT('Ctrl Pts',(-4.96022910773077,-17.4333970061901,
-840.993483527769));
#149396=CARTESIAN_POINT('Ctrl Pts',(-6.51968959134574,-16.8292587962898,
-842.487601174827));
#149397=CARTESIAN_POINT('Ctrl Pts',(-8.07915007496071,-16.2251205863895,
-843.981718821886));
#149398=CARTESIAN_POINT('Ctrl Pts',(-9.50104767561052,-15.3447188656481,
-845.475836468945));
#149399=CARTESIAN_POINT('Ctrl Pts',(-10.9229452762603,-14.4643171449067,
-846.969954116004));
#149400=CARTESIAN_POINT('Ctrl Pts',(-12.1588589765331,-13.3376329379985,
-848.464071763063));
#149401=CARTESIAN_POINT('Ctrl Pts',(-13.3947726768058,-12.2109487310903,
-849.958189410122));
#149402=CARTESIAN_POINT('Ctrl Pts',(-14.4026149179538,-10.8763499173728,
-851.45230705718));
#149403=CARTESIAN_POINT('Ctrl Pts',(-15.4104571591017,-9.54175110365538,
-852.946424704239));
#149404=CARTESIAN_POINT('Ctrl Pts',(-16.1559070823762,-8.04468584505497,
-854.440542351298));
#149405=CARTESIAN_POINT('Ctrl Pts',(-16.9013570056506,-6.54762058645456,
-855.934659998357));
#149406=CARTESIAN_POINT('Ctrl Pts',(-17.3590292079831,-4.93906964482095,
-857.428777645416));
#149407=CARTESIAN_POINT('Ctrl Pts',(-17.8167014103155,-3.33051870318735,
-858.922895292475));
#149408=CARTESIAN_POINT('Ctrl Pts',(-17.9710104137728,-1.66525935159368,
-860.417012939533));
#149409=CARTESIAN_POINT('Ctrl Pts',(-18.1253194172301,-1.10985572039171E-15,
-861.911130586592));
#149410=CARTESIAN_POINT('Ctrl Pts',(-17.9710104137728,1.66525935159367,
-863.405248233651));
#149411=CARTESIAN_POINT('Ctrl Pts',(-17.8167014103155,3.33051870318735,
-864.89936588071));
#149412=CARTESIAN_POINT('Ctrl Pts',(-17.3590292079831,4.93906964482096,
-866.393483527768));
#149413=CARTESIAN_POINT('Ctrl Pts',(-16.9013570056506,6.54762058645456,
-867.887601174827));
#149414=CARTESIAN_POINT('Ctrl Pts',(-16.1559070823762,8.04468584505497,
-869.381718821886));
#149415=CARTESIAN_POINT('Ctrl Pts',(-15.4104571591017,9.54175110365538,
-870.875836468945));
#149416=CARTESIAN_POINT('Ctrl Pts',(-14.4026149179538,10.8763499173728,
-872.369954116004));
#149417=CARTESIAN_POINT('Ctrl Pts',(-13.3947726768058,12.2109487310903,
-873.864071763063));
#149418=CARTESIAN_POINT('Ctrl Pts',(-12.1588589765331,13.3376329379985,
-875.358189410122));
#149419=CARTESIAN_POINT('Ctrl Pts',(-10.9229452762603,14.4643171449067,
-876.85230705718));
#149420=CARTESIAN_POINT('Ctrl Pts',(-9.50104767561052,15.3447188656481,
-878.346424704239));
#149421=CARTESIAN_POINT('Ctrl Pts',(-8.07915007496071,16.2251205863895,
-879.840542351298));
#149422=CARTESIAN_POINT('Ctrl Pts',(-6.51968959134574,16.8292587962898,
-881.334659998357));
#149423=CARTESIAN_POINT('Ctrl Pts',(-4.96022910773078,17.4333970061901,
-882.828777645416));
#149424=CARTESIAN_POINT('Ctrl Pts',(-3.31631129755346,17.7406985030951,
-884.322895292474));
#149425=CARTESIAN_POINT('Ctrl Pts',(-1.67239348737615,18.048,-885.817012939534));
#149426=CARTESIAN_POINT('Ctrl Pts',(-2.21024254310115E-15,18.048,-887.311130586592));
#149427=CARTESIAN_POINT('Ctrl Pts',(1.67239348737616,18.048,-888.805248233651));
#149428=CARTESIAN_POINT('Ctrl Pts',(3.31631129755346,17.7406985030951,-890.29936588071));
#149429=CARTESIAN_POINT('Ctrl Pts',(4.96022910773077,17.4333970061901,-891.793483527769));
#149430=CARTESIAN_POINT('Ctrl Pts',(6.51968959134575,16.8292587962898,-893.287601174828));
#149431=CARTESIAN_POINT('Ctrl Pts',(8.07915007496071,16.2251205863895,-894.781718821887));
#149432=CARTESIAN_POINT('Ctrl Pts',(9.50104767561053,15.3447188656481,-896.275836468945));
#149433=CARTESIAN_POINT('Ctrl Pts',(10.9229452762603,14.4643171449067,-897.769954116004));
#149434=CARTESIAN_POINT('Ctrl Pts',(12.1588589765331,13.3376329379985,-899.264071763063));
#149435=CARTESIAN_POINT('Ctrl Pts',(13.3947726768058,12.2109487310903,-900.758189410122));
#149436=CARTESIAN_POINT('Ctrl Pts',(14.4026149179538,10.8763499173728,-902.25230705718));
#149437=CARTESIAN_POINT('Ctrl Pts',(15.4104571591017,9.54175110365538,-903.746424704239));
#149438=CARTESIAN_POINT('Ctrl Pts',(16.1559070823762,8.04468584505496,-905.240542351298));
#149439=CARTESIAN_POINT('Ctrl Pts',(16.9013570056506,6.54762058645456,-906.734659998357));
#149440=CARTESIAN_POINT('Ctrl Pts',(17.3590292079831,4.93906964482096,-908.228777645416));
#149441=CARTESIAN_POINT('Ctrl Pts',(17.8167014103155,3.33051870318735,-909.722895292475));
#149442=CARTESIAN_POINT('Ctrl Pts',(17.9710104137728,1.66525935159367,-911.217012939533));
#149443=CARTESIAN_POINT('Ctrl Pts',(18.1253194172301,3.32956716117513E-15,
-912.711130586592));
#149444=CARTESIAN_POINT('Ctrl Pts',(17.9710104137728,-1.66525935159367,
-914.205248233651));
#149445=CARTESIAN_POINT('Ctrl Pts',(17.8167014103155,-3.33051870318736,
-915.69936588071));
#149446=CARTESIAN_POINT('Ctrl Pts',(17.3590292079831,-4.93906964482095,
-917.193483527769));
#149447=CARTESIAN_POINT('Ctrl Pts',(16.9013570056506,-6.54762058645456,
-918.687601174827));
#149448=CARTESIAN_POINT('Ctrl Pts',(16.1559070823762,-8.04468584505497,
-920.181718821887));
#149449=CARTESIAN_POINT('Ctrl Pts',(15.4104571591017,-9.54175110365538,
-921.675836468945));
#149450=CARTESIAN_POINT('Ctrl Pts',(14.4026149179538,-10.8763499173728,
-923.169954116004));
#149451=CARTESIAN_POINT('Ctrl Pts',(13.3947726768058,-12.2109487310903,
-924.664071763063));
#149452=CARTESIAN_POINT('Ctrl Pts',(12.1588589765331,-13.3376329379985,
-926.158189410122));
#149453=CARTESIAN_POINT('Ctrl Pts',(10.9229452762603,-14.4643171449067,
-927.65230705718));
#149454=CARTESIAN_POINT('Ctrl Pts',(9.50104767561053,-15.3447188656481,
-929.146424704239));
#149455=CARTESIAN_POINT('Ctrl Pts',(8.07915007496071,-16.2251205863895,
-930.640542351298));
#149456=CARTESIAN_POINT('Ctrl Pts',(6.51968959134574,-16.8292587962898,
-932.134659998357));
#149457=CARTESIAN_POINT('Ctrl Pts',(4.96022910773078,-17.4333970061901,
-933.628777645416));
#149458=CARTESIAN_POINT('Ctrl Pts',(3.31631129755346,-17.7406985030951,
-935.122895292475));
#149459=CARTESIAN_POINT('Ctrl Pts',(1.67239348737615,-18.048,-936.617012939534));
#149460=CARTESIAN_POINT('Ctrl Pts',(0.,-18.048,-938.111130586592));
#149461=CARTESIAN_POINT('Ctrl Pts',(-1.67239348737615,-18.048,-939.605248233651));
#149462=CARTESIAN_POINT('Ctrl Pts',(-3.31631129755346,-17.7406985030951,
-941.09936588071));
#149463=CARTESIAN_POINT('Ctrl Pts',(-4.96022910773077,-17.4333970061901,
-942.593483527769));
#149464=CARTESIAN_POINT('Ctrl Pts',(-6.51968959134574,-16.8292587962898,
-944.087601174827));
#149465=CARTESIAN_POINT('Ctrl Pts',(-8.07915007496071,-16.2251205863895,
-945.581718821886));
#149466=CARTESIAN_POINT('Ctrl Pts',(-9.50104767561052,-15.3447188656481,
-947.075836468945));
#149467=CARTESIAN_POINT('Ctrl Pts',(-10.9229452762603,-14.4643171449067,
-948.569954116004));
#149468=CARTESIAN_POINT('Ctrl Pts',(-12.1588589765331,-13.3376329379985,
-950.064071763063));
#149469=CARTESIAN_POINT('Ctrl Pts',(-13.3947726768058,-12.2109487310903,
-951.558189410122));
#149470=CARTESIAN_POINT('Ctrl Pts',(-14.4026149179538,-10.8763499173728,
-953.052307057181));
#149471=CARTESIAN_POINT('Ctrl Pts',(-15.4104571591017,-9.54175110365538,
-954.54642470424));
#149472=CARTESIAN_POINT('Ctrl Pts',(-16.1559070823762,-8.04468584505497,
-956.040542351298));
#149473=CARTESIAN_POINT('Ctrl Pts',(-16.9013570056506,-6.54762058645456,
-957.534659998357));
#149474=CARTESIAN_POINT('Ctrl Pts',(-17.3590292079831,-4.93906964482095,
-959.028777645416));
#149475=CARTESIAN_POINT('Ctrl Pts',(-17.8167014103155,-3.33051870318735,
-960.522895292475));
#149476=CARTESIAN_POINT('Ctrl Pts',(-17.9710104137728,-1.66525935159368,
-962.017012939533));
#149477=CARTESIAN_POINT('Ctrl Pts',(-18.1253194172301,-1.10985572039171E-15,
-963.511130586592));
#149478=CARTESIAN_POINT('Ctrl Pts',(-17.9710104137728,1.66525935159367,
-965.005248233651));
#149479=CARTESIAN_POINT('Ctrl Pts',(-17.8167014103155,3.33051870318735,
-966.49936588071));
#149480=CARTESIAN_POINT('Ctrl Pts',(-17.3590292079831,4.93906964482096,
-967.993483527769));
#149481=CARTESIAN_POINT('Ctrl Pts',(-16.9013570056506,6.54762058645456,
-969.487601174828));
#149482=CARTESIAN_POINT('Ctrl Pts',(-16.1559070823762,8.04468584505497,
-970.981718821886));
#149483=CARTESIAN_POINT('Ctrl Pts',(-15.4104571591017,9.54175110365538,
-972.475836468945));
#149484=CARTESIAN_POINT('Ctrl Pts',(-14.4026149179538,10.8763499173728,
-973.969954116004));
#149485=CARTESIAN_POINT('Ctrl Pts',(-13.3947726768058,12.2109487310903,
-975.464071763063));
#149486=CARTESIAN_POINT('Ctrl Pts',(-12.1588589765331,13.3376329379985,
-976.958189410122));
#149487=CARTESIAN_POINT('Ctrl Pts',(-10.9229452762603,14.4643171449067,
-978.452307057181));
#149488=CARTESIAN_POINT('Ctrl Pts',(-9.50104767561052,15.3447188656481,
-979.946424704239));
#149489=CARTESIAN_POINT('Ctrl Pts',(-8.07915007496071,16.2251205863895,
-981.440542351298));
#149490=CARTESIAN_POINT('Ctrl Pts',(-6.51968959134574,16.8292587962898,
-982.934659998357));
#149491=CARTESIAN_POINT('Ctrl Pts',(-4.96022910773078,17.4333970061901,
-984.428777645416));
#149492=CARTESIAN_POINT('Ctrl Pts',(-3.31631129755346,17.7406985030951,
-985.922895292474));
#149493=CARTESIAN_POINT('Ctrl Pts',(-1.67239348737615,18.048,-987.417012939533));
#149494=CARTESIAN_POINT('Ctrl Pts',(-2.21024254310115E-15,18.048,-988.911130586592));
#149495=CARTESIAN_POINT('Ctrl Pts',(1.67239348737616,18.048,-990.405248233651));
#149496=CARTESIAN_POINT('Ctrl Pts',(3.31631129755346,17.7406985030951,-991.89936588071));
#149497=CARTESIAN_POINT('Ctrl Pts',(4.96022910773077,17.4333970061901,-993.393483527769));
#149498=CARTESIAN_POINT('Ctrl Pts',(6.51968959134575,16.8292587962898,-994.887601174828));
#149499=CARTESIAN_POINT('Ctrl Pts',(8.07915007496071,16.2251205863895,-996.381718821887));
#149500=CARTESIAN_POINT('Ctrl Pts',(9.50104767561053,15.3447188656481,-997.875836468945));
#149501=CARTESIAN_POINT('Ctrl Pts',(10.9229452762603,14.4643171449067,-999.369954116004));
#149502=CARTESIAN_POINT('Ctrl Pts',(12.1588589765331,13.3376329379985,-1000.86407176306));
#149503=CARTESIAN_POINT('Ctrl Pts',(13.3947726768058,12.2109487310903,-1002.35818941012));
#149504=CARTESIAN_POINT('Ctrl Pts',(14.4026149179538,10.8763499173728,-1003.85230705718));
#149505=CARTESIAN_POINT('Ctrl Pts',(15.4104571591017,9.54175110365538,-1005.34642470424));
#149506=CARTESIAN_POINT('Ctrl Pts',(16.1559070823762,8.04468584505496,-1006.8405423513));
#149507=CARTESIAN_POINT('Ctrl Pts',(16.9013570056506,6.54762058645456,-1008.33465999836));
#149508=CARTESIAN_POINT('Ctrl Pts',(17.3590292079831,4.93906964482096,-1009.82877764542));
#149509=CARTESIAN_POINT('Ctrl Pts',(17.8167014103155,3.33051870318735,-1011.32289529247));
#149510=CARTESIAN_POINT('Ctrl Pts',(17.9710104137728,1.66525935159367,-1012.81701293953));
#149511=CARTESIAN_POINT('Ctrl Pts',(18.1253194172301,3.32956716117513E-15,
-1014.31113058659));
#149512=CARTESIAN_POINT('Ctrl Pts',(17.9710104137728,-1.66525935159367,
-1015.80524823365));
#149513=CARTESIAN_POINT('Ctrl Pts',(17.8167014103155,-3.33051870318736,
-1017.29936588071));
#149514=CARTESIAN_POINT('Ctrl Pts',(17.3590292079831,-4.93906964482095,
-1018.79348352777));
#149515=CARTESIAN_POINT('Ctrl Pts',(16.9013570056506,-6.54762058645456,
-1020.28760117483));
#149516=CARTESIAN_POINT('Ctrl Pts',(16.1559070823762,-8.04468584505497,
-1021.78171882189));
#149517=CARTESIAN_POINT('Ctrl Pts',(15.4104571591017,-9.54175110365538,
-1023.27583646895));
#149518=CARTESIAN_POINT('Ctrl Pts',(14.4026149179538,-10.8763499173728,
-1024.769954116));
#149519=CARTESIAN_POINT('Ctrl Pts',(13.3947726768058,-12.2109487310903,
-1026.26407176306));
#149520=CARTESIAN_POINT('Ctrl Pts',(12.1588589765331,-13.3376329379985,
-1027.75818941012));
#149521=CARTESIAN_POINT('Ctrl Pts',(10.9229452762603,-14.4643171449067,
-1029.25230705718));
#149522=CARTESIAN_POINT('Ctrl Pts',(9.50104767561053,-15.3447188656481,
-1030.74642470424));
#149523=CARTESIAN_POINT('Ctrl Pts',(8.07915007496071,-16.2251205863895,
-1032.2405423513));
#149524=CARTESIAN_POINT('Ctrl Pts',(6.51968959134574,-16.8292587962898,
-1033.73465999836));
#149525=CARTESIAN_POINT('Ctrl Pts',(4.96022910773078,-17.4333970061901,
-1035.22877764542));
#149526=CARTESIAN_POINT('Ctrl Pts',(3.31631129755346,-17.7406985030951,
-1036.72289529247));
#149527=CARTESIAN_POINT('Ctrl Pts',(1.67239348737615,-18.048,-1038.21701293953));
#149528=CARTESIAN_POINT('Ctrl Pts',(0.,-18.048,-1039.71113058659));
#149529=CARTESIAN_POINT('Ctrl Pts',(-1.67239348737615,-18.048,-1041.20524823365));
#149530=CARTESIAN_POINT('Ctrl Pts',(-3.31631129755346,-17.7406985030951,
-1042.69936588071));
#149531=CARTESIAN_POINT('Ctrl Pts',(-4.96022910773077,-17.4333970061901,
-1044.19348352777));
#149532=CARTESIAN_POINT('Ctrl Pts',(-6.51968959134574,-16.8292587962898,
-1045.68760117483));
#149533=CARTESIAN_POINT('Ctrl Pts',(-8.07915007496071,-16.2251205863895,
-1047.18171882189));
#149534=CARTESIAN_POINT('Ctrl Pts',(-9.50104767561052,-15.3447188656481,
-1048.67583646894));
#149535=CARTESIAN_POINT('Ctrl Pts',(-10.9229452762603,-14.4643171449067,
-1050.169954116));
#149536=CARTESIAN_POINT('Ctrl Pts',(-12.1588589765331,-13.3376329379985,
-1051.66407176306));
#149537=CARTESIAN_POINT('Ctrl Pts',(-13.3947726768058,-12.2109487310903,
-1053.15818941012));
#149538=CARTESIAN_POINT('Ctrl Pts',(-14.4026149179538,-10.8763499173728,
-1054.65230705718));
#149539=CARTESIAN_POINT('Ctrl Pts',(-15.4104571591017,-9.54175110365538,
-1056.14642470424));
#149540=CARTESIAN_POINT('Ctrl Pts',(-16.1559070823762,-8.04468584505497,
-1057.6405423513));
#149541=CARTESIAN_POINT('Ctrl Pts',(-16.9013570056506,-6.54762058645456,
-1059.13465999836));
#149542=CARTESIAN_POINT('Ctrl Pts',(-17.3590292079831,-4.93906964482095,
-1060.62877764542));
#149543=CARTESIAN_POINT('Ctrl Pts',(-17.8167014103155,-3.33051870318735,
-1062.12289529247));
#149544=CARTESIAN_POINT('Ctrl Pts',(-17.9710104137728,-1.66525935159368,
-1063.61701293953));
#149545=CARTESIAN_POINT('Ctrl Pts',(-18.1253194172301,-1.10985572039171E-15,
-1065.11113058659));
#149546=CARTESIAN_POINT('Ctrl Pts',(-17.9710104137728,1.66525935159367,
-1066.60524823365));
#149547=CARTESIAN_POINT('Ctrl Pts',(-17.8167014103155,3.33051870318735,
-1068.09936588071));
#149548=CARTESIAN_POINT('Ctrl Pts',(-17.3590292079831,4.93906964482096,
-1069.59348352777));
#149549=CARTESIAN_POINT('Ctrl Pts',(-16.9013570056506,6.54762058645456,
-1071.08760117483));
#149550=CARTESIAN_POINT('Ctrl Pts',(-16.1559070823762,8.04468584505497,
-1072.58171882189));
#149551=CARTESIAN_POINT('Ctrl Pts',(-15.4104571591017,9.54175110365538,
-1074.07583646895));
#149552=CARTESIAN_POINT('Ctrl Pts',(-14.4026149179538,10.8763499173728,
-1075.569954116));
#149553=CARTESIAN_POINT('Ctrl Pts',(-13.3947726768058,12.2109487310903,
-1077.06407176306));
#149554=CARTESIAN_POINT('Ctrl Pts',(-12.1588589765331,13.3376329379985,
-1078.55818941012));
#149555=CARTESIAN_POINT('Ctrl Pts',(-10.9229452762603,14.4643171449067,
-1080.05230705718));
#149556=CARTESIAN_POINT('Ctrl Pts',(-9.50104767561052,15.3447188656481,
-1081.54642470424));
#149557=CARTESIAN_POINT('Ctrl Pts',(-8.07915007496071,16.2251205863895,
-1083.0405423513));
#149558=CARTESIAN_POINT('Ctrl Pts',(-6.51968959134574,16.8292587962898,
-1084.53465999836));
#149559=CARTESIAN_POINT('Ctrl Pts',(-4.96022910773078,17.4333970061901,
-1086.02877764542));
#149560=CARTESIAN_POINT('Ctrl Pts',(-3.31631129755346,17.7406985030951,
-1087.52289529247));
#149561=CARTESIAN_POINT('Ctrl Pts',(-1.67239348737615,18.048,-1089.01701293953));
#149562=CARTESIAN_POINT('Ctrl Pts',(-2.21024254310115E-15,18.048,-1090.51113058659));
#149563=CARTESIAN_POINT('Ctrl Pts',(1.67239348737616,18.048,-1092.00524823365));
#149564=CARTESIAN_POINT('Ctrl Pts',(3.31631129755346,17.7406985030951,-1093.49936588071));
#149565=CARTESIAN_POINT('Ctrl Pts',(4.96022910773077,17.4333970061901,-1094.99348352777));
#149566=CARTESIAN_POINT('Ctrl Pts',(6.51968959134575,16.8292587962898,-1096.48760117483));
#149567=CARTESIAN_POINT('Ctrl Pts',(8.07915007496071,16.2251205863895,-1097.98171882189));
#149568=CARTESIAN_POINT('Ctrl Pts',(9.50104767561053,15.3447188656481,-1099.47583646895));
#149569=CARTESIAN_POINT('Ctrl Pts',(10.9229452762603,14.4643171449067,-1100.969954116));
#149570=CARTESIAN_POINT('Ctrl Pts',(12.1588589765331,13.3376329379985,-1102.46407176306));
#149571=CARTESIAN_POINT('Ctrl Pts',(13.3947726768058,12.2109487310903,-1103.95818941012));
#149572=CARTESIAN_POINT('Ctrl Pts',(14.4026149179538,10.8763499173728,-1105.45230705718));
#149573=CARTESIAN_POINT('Ctrl Pts',(15.4104571591017,9.54175110365538,-1106.94642470424));
#149574=CARTESIAN_POINT('Ctrl Pts',(16.1559070823762,8.04468584505496,-1108.4405423513));
#149575=CARTESIAN_POINT('Ctrl Pts',(16.9013570056506,6.54762058645456,-1109.93465999836));
#149576=CARTESIAN_POINT('Ctrl Pts',(17.3590292079831,4.93906964482096,-1111.42877764542));
#149577=CARTESIAN_POINT('Ctrl Pts',(17.8167014103155,3.33051870318735,-1112.92289529247));
#149578=CARTESIAN_POINT('Ctrl Pts',(17.9710104137728,1.66525935159367,-1114.41701293953));
#149579=CARTESIAN_POINT('Ctrl Pts',(18.1253194172301,3.32956716117513E-15,
-1115.91113058659));
#149580=CARTESIAN_POINT('Ctrl Pts',(17.9710104137728,-1.66525935159367,
-1117.40524823365));
#149581=CARTESIAN_POINT('Ctrl Pts',(17.8167014103155,-3.33051870318736,
-1118.89936588071));
#149582=CARTESIAN_POINT('Ctrl Pts',(17.3590292079831,-4.93906964482095,
-1120.39348352777));
#149583=CARTESIAN_POINT('Ctrl Pts',(16.9013570056506,-6.54762058645456,
-1121.88760117483));
#149584=CARTESIAN_POINT('Ctrl Pts',(16.1559070823762,-8.04468584505497,
-1123.38171882189));
#149585=CARTESIAN_POINT('Ctrl Pts',(15.4104571591017,-9.54175110365538,
-1124.87583646895));
#149586=CARTESIAN_POINT('Ctrl Pts',(14.4026149179538,-10.8763499173728,
-1126.369954116));
#149587=CARTESIAN_POINT('Ctrl Pts',(13.3947726768058,-12.2109487310903,
-1127.86407176306));
#149588=CARTESIAN_POINT('Ctrl Pts',(12.1588589765331,-13.3376329379985,
-1129.35818941012));
#149589=CARTESIAN_POINT('Ctrl Pts',(10.9229452762603,-14.4643171449067,
-1130.85230705718));
#149590=CARTESIAN_POINT('Ctrl Pts',(9.50104767561053,-15.3447188656481,
-1132.34642470424));
#149591=CARTESIAN_POINT('Ctrl Pts',(8.07915007496071,-16.2251205863895,
-1133.8405423513));
#149592=CARTESIAN_POINT('Ctrl Pts',(6.51968959134574,-16.8292587962898,
-1135.33465999836));
#149593=CARTESIAN_POINT('Ctrl Pts',(4.96022910773078,-17.4333970061901,
-1136.82877764542));
#149594=CARTESIAN_POINT('Ctrl Pts',(3.31631129755346,-17.7406985030951,
-1138.32289529247));
#149595=CARTESIAN_POINT('Ctrl Pts',(1.67239348737615,-18.048,-1139.81701293953));
#149596=CARTESIAN_POINT('Ctrl Pts',(0.,-18.048,-1141.31113058659));
#149597=CARTESIAN_POINT('Ctrl Pts',(-1.67239348737615,-18.048,-1142.80524823365));
#149598=CARTESIAN_POINT('Ctrl Pts',(-3.31631129755346,-17.7406985030951,
-1144.29936588071));
#149599=CARTESIAN_POINT('Ctrl Pts',(-4.96022910773077,-17.4333970061901,
-1145.79348352777));
#149600=CARTESIAN_POINT('Ctrl Pts',(-6.51968959134574,-16.8292587962898,
-1147.28760117483));
#149601=CARTESIAN_POINT('Ctrl Pts',(-8.07915007496071,-16.2251205863895,
-1148.78171882189));
#149602=CARTESIAN_POINT('Ctrl Pts',(-9.50104767561052,-15.3447188656481,
-1150.27583646895));
#149603=CARTESIAN_POINT('Ctrl Pts',(-10.9229452762603,-14.4643171449067,
-1151.769954116));
#149604=CARTESIAN_POINT('Ctrl Pts',(-12.1588589765331,-13.3376329379985,
-1153.26407176306));
#149605=CARTESIAN_POINT('Ctrl Pts',(-13.3947726768058,-12.2109487310903,
-1154.75818941012));
#149606=CARTESIAN_POINT('Ctrl Pts',(-14.4026149179538,-10.8763499173728,
-1156.25230705718));
#149607=CARTESIAN_POINT('Ctrl Pts',(-15.4104571591017,-9.54175110365538,
-1157.74642470424));
#149608=CARTESIAN_POINT('Ctrl Pts',(-16.1559070823762,-8.04468584505497,
-1159.2405423513));
#149609=CARTESIAN_POINT('Ctrl Pts',(-16.9013570056506,-6.54762058645456,
-1160.73465999836));
#149610=CARTESIAN_POINT('Ctrl Pts',(-17.3590292079831,-4.93906964482095,
-1162.22877764542));
#149611=CARTESIAN_POINT('Ctrl Pts',(-17.8167014103155,-3.33051870318735,
-1163.72289529247));
#149612=CARTESIAN_POINT('Ctrl Pts',(-17.9710104137728,-1.66525935159368,
-1165.21701293953));
#149613=CARTESIAN_POINT('Ctrl Pts',(-18.1253194172301,-1.10985572039171E-15,
-1166.71113058659));
#149614=CARTESIAN_POINT('Ctrl Pts',(-17.9710104137728,1.66525935159367,
-1168.20524823365));
#149615=CARTESIAN_POINT('Ctrl Pts',(-17.8167014103155,3.33051870318735,
-1169.69936588071));
#149616=CARTESIAN_POINT('Ctrl Pts',(-17.3590292079831,4.93906964482096,
-1171.19348352777));
#149617=CARTESIAN_POINT('Ctrl Pts',(-16.9013570056506,6.54762058645456,
-1172.68760117483));
#149618=CARTESIAN_POINT('Ctrl Pts',(-16.1559070823762,8.04468584505497,
-1174.18171882189));
#149619=CARTESIAN_POINT('Ctrl Pts',(-15.4104571591017,9.54175110365538,
-1175.67583646895));
#149620=CARTESIAN_POINT('Ctrl Pts',(-14.4026149179538,10.8763499173728,
-1177.169954116));
#149621=CARTESIAN_POINT('Ctrl Pts',(-13.3947726768058,12.2109487310903,
-1178.66407176306));
#149622=CARTESIAN_POINT('Ctrl Pts',(-12.1588589765331,13.3376329379985,
-1180.15818941012));
#149623=CARTESIAN_POINT('Ctrl Pts',(-10.9229452762603,14.4643171449067,
-1181.65230705718));
#149624=CARTESIAN_POINT('Ctrl Pts',(-9.50104767561052,15.3447188656481,
-1183.14642470424));
#149625=CARTESIAN_POINT('Ctrl Pts',(-8.07915007496071,16.2251205863895,
-1184.6405423513));
#149626=CARTESIAN_POINT('Ctrl Pts',(-6.51968959134574,16.8292587962898,
-1186.13465999836));
#149627=CARTESIAN_POINT('Ctrl Pts',(-4.96022910773078,17.4333970061901,
-1187.62877764542));
#149628=CARTESIAN_POINT('Ctrl Pts',(-3.31631129755346,17.7406985030951,
-1189.12289529247));
#149629=CARTESIAN_POINT('Ctrl Pts',(-1.67239348737615,18.048,-1190.61701293953));
#149630=CARTESIAN_POINT('Ctrl Pts',(-2.21024254310115E-15,18.048,-1192.11113058659));
#149631=CARTESIAN_POINT('Ctrl Pts',(1.67239348737616,18.048,-1193.60524823365));
#149632=CARTESIAN_POINT('Ctrl Pts',(3.31631129755346,17.7406985030951,-1195.09936588071));
#149633=CARTESIAN_POINT('Ctrl Pts',(4.96022910773077,17.4333970061901,-1196.59348352777));
#149634=CARTESIAN_POINT('Ctrl Pts',(6.51968959134575,16.8292587962898,-1198.08760117483));
#149635=CARTESIAN_POINT('Ctrl Pts',(8.07915007496071,16.2251205863895,-1199.58171882189));
#149636=CARTESIAN_POINT('Ctrl Pts',(9.50104767561053,15.3447188656481,-1201.07583646894));
#149637=CARTESIAN_POINT('Ctrl Pts',(10.9229452762603,14.4643171449067,-1202.569954116));
#149638=CARTESIAN_POINT('Ctrl Pts',(12.1588589765331,13.3376329379985,-1204.06407176306));
#149639=CARTESIAN_POINT('Ctrl Pts',(13.3947726768058,12.2109487310903,-1205.55818941012));
#149640=CARTESIAN_POINT('Ctrl Pts',(14.4026149179538,10.8763499173728,-1207.05230705718));
#149641=CARTESIAN_POINT('Ctrl Pts',(15.4104571591017,9.54175110365538,-1208.54642470424));
#149642=CARTESIAN_POINT('Ctrl Pts',(16.1559070823762,8.04468584505496,-1210.0405423513));
#149643=CARTESIAN_POINT('Ctrl Pts',(16.9013570056506,6.54762058645456,-1211.53465999836));
#149644=CARTESIAN_POINT('Ctrl Pts',(17.3590292079831,4.93906964482096,-1213.02877764542));
#149645=CARTESIAN_POINT('Ctrl Pts',(17.8167014103155,3.33051870318735,-1214.52289529247));
#149646=CARTESIAN_POINT('Ctrl Pts',(17.9710104137728,1.66525935159367,-1216.01701293953));
#149647=CARTESIAN_POINT('Ctrl Pts',(18.1253194172301,3.32956716117513E-15,
-1217.51113058659));
#149648=CARTESIAN_POINT('Ctrl Pts',(17.9710104137728,-1.66525935159367,
-1219.00524823365));
#149649=CARTESIAN_POINT('Ctrl Pts',(17.8167014103155,-3.33051870318736,
-1220.49936588071));
#149650=CARTESIAN_POINT('Ctrl Pts',(17.3590292079831,-4.93906964482095,
-1221.99348352777));
#149651=CARTESIAN_POINT('Ctrl Pts',(16.9013570056506,-6.54762058645456,
-1223.48760117483));
#149652=CARTESIAN_POINT('Ctrl Pts',(16.1559070823762,-8.04468584505497,
-1224.98171882189));
#149653=CARTESIAN_POINT('Ctrl Pts',(15.4104571591017,-9.54175110365538,
-1226.47583646895));
#149654=CARTESIAN_POINT('Ctrl Pts',(14.4026149179538,-10.8763499173728,
-1227.969954116));
#149655=CARTESIAN_POINT('Ctrl Pts',(13.3947726768058,-12.2109487310903,
-1229.46407176306));
#149656=CARTESIAN_POINT('Ctrl Pts',(12.1588589765331,-13.3376329379985,
-1230.95818941012));
#149657=CARTESIAN_POINT('Ctrl Pts',(10.9229452762603,-14.4643171449067,
-1232.45230705718));
#149658=CARTESIAN_POINT('Ctrl Pts',(9.50104767561053,-15.3447188656481,
-1233.94642470424));
#149659=CARTESIAN_POINT('Ctrl Pts',(8.07915007496071,-16.2251205863895,
-1235.4405423513));
#149660=CARTESIAN_POINT('Ctrl Pts',(6.51968959134574,-16.8292587962898,
-1236.93465999836));
#149661=CARTESIAN_POINT('Ctrl Pts',(4.96022910773078,-17.4333970061901,
-1238.42877764542));
#149662=CARTESIAN_POINT('Ctrl Pts',(3.31631129755346,-17.7406985030951,
-1239.92289529247));
#149663=CARTESIAN_POINT('Ctrl Pts',(1.67239348737615,-18.048,-1241.41701293953));
#149664=CARTESIAN_POINT('Ctrl Pts',(0.,-18.048,-1242.91113058659));
#149665=CARTESIAN_POINT('Ctrl Pts',(-1.67239348737615,-18.048,-1244.40524823365));
#149666=CARTESIAN_POINT('Ctrl Pts',(-3.31631129755346,-17.7406985030951,
-1245.89936588071));
#149667=CARTESIAN_POINT('Ctrl Pts',(-4.96022910773077,-17.4333970061901,
-1247.39348352777));
#149668=CARTESIAN_POINT('Ctrl Pts',(-6.51968959134574,-16.8292587962898,
-1248.88760117483));
#149669=CARTESIAN_POINT('Ctrl Pts',(-8.07915007496071,-16.2251205863895,
-1250.38171882189));
#149670=CARTESIAN_POINT('Ctrl Pts',(-9.50104767561052,-15.3447188656481,
-1251.87583646895));
#149671=CARTESIAN_POINT('Ctrl Pts',(-10.9229452762603,-14.4643171449067,
-1253.369954116));
#149672=CARTESIAN_POINT('Ctrl Pts',(-12.1588589765331,-13.3376329379985,
-1254.86407176306));
#149673=CARTESIAN_POINT('Ctrl Pts',(-13.3947726768058,-12.2109487310903,
-1256.35818941012));
#149674=CARTESIAN_POINT('Ctrl Pts',(-14.4026149179538,-10.8763499173728,
-1257.85230705718));
#149675=CARTESIAN_POINT('Ctrl Pts',(-15.4104571591017,-9.54175110365538,
-1259.34642470424));
#149676=CARTESIAN_POINT('Ctrl Pts',(-16.1559070823762,-8.04468584505497,
-1260.8405423513));
#149677=CARTESIAN_POINT('Ctrl Pts',(-16.9013570056506,-6.54762058645456,
-1262.33465999836));
#149678=CARTESIAN_POINT('Ctrl Pts',(-17.3590292079831,-4.93906964482095,
-1263.82877764542));
#149679=CARTESIAN_POINT('Ctrl Pts',(-17.8167014103155,-3.33051870318735,
-1265.32289529247));
#149680=CARTESIAN_POINT('Ctrl Pts',(-17.9710104137728,-1.66525935159368,
-1266.81701293953));
#149681=CARTESIAN_POINT('Ctrl Pts',(-18.1253194172301,-1.10985572039171E-15,
-1268.31113058659));
#149682=CARTESIAN_POINT('Ctrl Pts',(-17.9710104137728,1.66525935159367,
-1269.80524823365));
#149683=CARTESIAN_POINT('Ctrl Pts',(-17.8167014103155,3.33051870318735,
-1271.29936588071));
#149684=CARTESIAN_POINT('Ctrl Pts',(-17.3590292079831,4.93906964482096,
-1272.79348352777));
#149685=CARTESIAN_POINT('Ctrl Pts',(-16.9013570056506,6.54762058645456,
-1274.28760117483));
#149686=CARTESIAN_POINT('Ctrl Pts',(-16.1559070823762,8.04468584505497,
-1275.78171882189));
#149687=CARTESIAN_POINT('Ctrl Pts',(-15.4104571591017,9.54175110365538,
-1277.27583646895));
#149688=CARTESIAN_POINT('Ctrl Pts',(-14.4026149179538,10.8763499173728,
-1278.769954116));
#149689=CARTESIAN_POINT('Ctrl Pts',(-13.3947726768058,12.2109487310903,
-1280.26407176306));
#149690=CARTESIAN_POINT('Ctrl Pts',(-12.1588589765331,13.3376329379985,
-1281.75818941012));
#149691=CARTESIAN_POINT('Ctrl Pts',(-10.9229452762603,14.4643171449067,
-1283.25230705718));
#149692=CARTESIAN_POINT('Ctrl Pts',(-9.50104767561052,15.3447188656481,
-1284.74642470424));
#149693=CARTESIAN_POINT('Ctrl Pts',(-8.07915007496071,16.2251205863895,
-1286.2405423513));
#149694=CARTESIAN_POINT('Ctrl Pts',(-6.51968959134574,16.8292587962898,
-1287.73465999836));
#149695=CARTESIAN_POINT('Ctrl Pts',(-4.96022910773078,17.4333970061901,
-1289.22877764542));
#149696=CARTESIAN_POINT('Ctrl Pts',(-3.31631129755346,17.7406985030951,
-1290.72289529247));
#149697=CARTESIAN_POINT('Ctrl Pts',(-1.67239348737615,18.048,-1292.21701293953));
#149698=CARTESIAN_POINT('Ctrl Pts',(-2.21024254310115E-15,18.048,-1293.71113058659));
#149699=CARTESIAN_POINT('Ctrl Pts',(1.67239348737616,18.048,-1295.20524823365));
#149700=CARTESIAN_POINT('Ctrl Pts',(3.31631129755346,17.7406985030951,-1296.69936588071));
#149701=CARTESIAN_POINT('Ctrl Pts',(4.96022910773077,17.4333970061901,-1298.19348352777));
#149702=CARTESIAN_POINT('Ctrl Pts',(6.51968959134575,16.8292587962898,-1299.68760117483));
#149703=CARTESIAN_POINT('Ctrl Pts',(8.07915007496071,16.2251205863895,-1301.18171882189));
#149704=CARTESIAN_POINT('Ctrl Pts',(9.50104767561053,15.3447188656481,-1302.67583646895));
#149705=CARTESIAN_POINT('Ctrl Pts',(10.9229452762603,14.4643171449067,-1304.169954116));
#149706=CARTESIAN_POINT('Ctrl Pts',(12.1588589765331,13.3376329379985,-1305.66407176306));
#149707=CARTESIAN_POINT('Ctrl Pts',(13.3947726768058,12.2109487310903,-1307.15818941012));
#149708=CARTESIAN_POINT('Ctrl Pts',(14.4026149179538,10.8763499173728,-1308.65230705718));
#149709=CARTESIAN_POINT('Ctrl Pts',(15.4104571591017,9.54175110365538,-1310.14642470424));
#149710=CARTESIAN_POINT('Ctrl Pts',(16.1559070823762,8.04468584505496,-1311.6405423513));
#149711=CARTESIAN_POINT('Ctrl Pts',(16.9013570056506,6.54762058645456,-1313.13465999836));
#149712=CARTESIAN_POINT('Ctrl Pts',(17.3590292079831,4.93906964482096,-1314.62877764542));
#149713=CARTESIAN_POINT('Ctrl Pts',(17.8167014103155,3.33051870318735,-1316.12289529247));
#149714=CARTESIAN_POINT('Ctrl Pts',(17.9710104137728,1.66525935159367,-1317.61701293953));
#149715=CARTESIAN_POINT('Ctrl Pts',(18.1253194172301,3.32956716117513E-15,
-1319.11113058659));
#149716=CARTESIAN_POINT('Ctrl Pts',(17.9710104137728,-1.66525935159367,
-1320.60524823365));
#149717=CARTESIAN_POINT('Ctrl Pts',(17.8167014103155,-3.33051870318736,
-1322.09936588071));
#149718=CARTESIAN_POINT('Ctrl Pts',(17.3590292079831,-4.93906964482095,
-1323.59348352777));
#149719=CARTESIAN_POINT('Ctrl Pts',(16.9013570056506,-6.54762058645456,
-1325.08760117483));
#149720=CARTESIAN_POINT('Ctrl Pts',(16.1559070823762,-8.04468584505497,
-1326.58171882189));
#149721=CARTESIAN_POINT('Ctrl Pts',(15.4104571591017,-9.54175110365538,
-1328.07583646895));
#149722=CARTESIAN_POINT('Ctrl Pts',(14.4026149179538,-10.8763499173728,
-1329.569954116));
#149723=CARTESIAN_POINT('Ctrl Pts',(13.3947726768058,-12.2109487310903,
-1331.06407176306));
#149724=CARTESIAN_POINT('Ctrl Pts',(12.1588589765331,-13.3376329379985,
-1332.55818941012));
#149725=CARTESIAN_POINT('Ctrl Pts',(10.9229452762603,-14.4643171449067,
-1334.05230705718));
#149726=CARTESIAN_POINT('Ctrl Pts',(9.50104767561053,-15.3447188656481,
-1335.54642470424));
#149727=CARTESIAN_POINT('Ctrl Pts',(8.07915007496071,-16.2251205863895,
-1337.0405423513));
#149728=CARTESIAN_POINT('Ctrl Pts',(6.51968959134574,-16.8292587962898,
-1338.53465999836));
#149729=CARTESIAN_POINT('Ctrl Pts',(4.96022910773078,-17.4333970061901,
-1340.02877764542));
#149730=CARTESIAN_POINT('Ctrl Pts',(3.31631129755346,-17.7406985030951,
-1341.52289529247));
#149731=CARTESIAN_POINT('Ctrl Pts',(1.67239348737615,-18.048,-1343.01701293953));
#149732=CARTESIAN_POINT('Ctrl Pts',(0.,-18.048,-1344.51113058659));
#149733=CARTESIAN_POINT('Ctrl Pts',(-1.67239348737615,-18.048,-1346.00524823365));
#149734=CARTESIAN_POINT('Ctrl Pts',(-3.31631129755346,-17.7406985030951,
-1347.49936588071));
#149735=CARTESIAN_POINT('Ctrl Pts',(-4.96022910773077,-17.4333970061901,
-1348.99348352777));
#149736=CARTESIAN_POINT('Ctrl Pts',(-6.51968959134574,-16.8292587962898,
-1350.48760117483));
#149737=CARTESIAN_POINT('Ctrl Pts',(-8.07915007496071,-16.2251205863895,
-1351.98171882189));
#149738=CARTESIAN_POINT('Ctrl Pts',(-9.50104767561052,-15.3447188656481,
-1353.47583646895));
#149739=CARTESIAN_POINT('Ctrl Pts',(-10.9229452762603,-14.4643171449067,
-1354.969954116));
#149740=CARTESIAN_POINT('Ctrl Pts',(-12.1588589765331,-13.3376329379985,
-1356.46407176306));
#149741=CARTESIAN_POINT('Ctrl Pts',(-13.3947726768058,-12.2109487310903,
-1357.95818941012));
#149742=CARTESIAN_POINT('Ctrl Pts',(-14.4026149179538,-10.8763499173728,
-1359.45230705718));
#149743=CARTESIAN_POINT('Ctrl Pts',(-15.4104571591017,-9.54175110365538,
-1360.94642470424));
#149744=CARTESIAN_POINT('Ctrl Pts',(-16.1559070823762,-8.04468584505497,
-1362.4405423513));
#149745=CARTESIAN_POINT('Ctrl Pts',(-16.9013570056506,-6.54762058645456,
-1363.93465999836));
#149746=CARTESIAN_POINT('Ctrl Pts',(-17.3590292079831,-4.93906964482095,
-1365.42877764542));
#149747=CARTESIAN_POINT('Ctrl Pts',(-17.8167014103155,-3.33051870318735,
-1366.92289529248));
#149748=CARTESIAN_POINT('Ctrl Pts',(-17.9710104137728,-1.66525935159368,
-1368.41701293953));
#149749=CARTESIAN_POINT('Ctrl Pts',(-18.1253194172301,-1.10985572039171E-15,
-1369.91113058659));
#149750=CARTESIAN_POINT('Ctrl Pts',(-17.9710104137728,1.66525935159367,
-1371.40524823365));
#149751=CARTESIAN_POINT('Ctrl Pts',(-17.8167014103155,3.33051870318735,
-1372.89936588071));
#149752=CARTESIAN_POINT('Ctrl Pts',(-17.3590292079831,4.93906964482096,
-1374.39348352777));
#149753=CARTESIAN_POINT('Ctrl Pts',(-16.9013570056506,6.54762058645456,
-1375.88760117483));
#149754=CARTESIAN_POINT('Ctrl Pts',(-16.1559070823762,8.04468584505497,
-1377.38171882189));
#149755=CARTESIAN_POINT('Ctrl Pts',(-15.4104571591017,9.54175110365538,
-1378.87583646895));
#149756=CARTESIAN_POINT('Ctrl Pts',(-14.4026149179538,10.8763499173728,
-1380.369954116));
#149757=CARTESIAN_POINT('Ctrl Pts',(-13.3947726768058,12.2109487310903,
-1381.86407176306));
#149758=CARTESIAN_POINT('Ctrl Pts',(-12.1588589765331,13.3376329379985,
-1383.35818941012));
#149759=CARTESIAN_POINT('Ctrl Pts',(-10.9229452762603,14.4643171449067,
-1384.85230705718));
#149760=CARTESIAN_POINT('Ctrl Pts',(-9.50104767561052,15.3447188656481,
-1386.34642470424));
#149761=CARTESIAN_POINT('Ctrl Pts',(-8.07915007496071,16.2251205863895,
-1387.8405423513));
#149762=CARTESIAN_POINT('Ctrl Pts',(-6.51968959134574,16.8292587962898,
-1389.33465999836));
#149763=CARTESIAN_POINT('Ctrl Pts',(-4.96022910773078,17.4333970061901,
-1390.82877764542));
#149764=CARTESIAN_POINT('Ctrl Pts',(-3.31631129755346,17.7406985030951,
-1392.32289529247));
#149765=CARTESIAN_POINT('Ctrl Pts',(-1.67239348737615,18.048,-1393.81701293953));
#149766=CARTESIAN_POINT('Ctrl Pts',(-2.21024254310115E-15,18.048,-1395.31113058659));
#149767=CARTESIAN_POINT('Ctrl Pts',(1.67239348737616,18.048,-1396.80524823365));
#149768=CARTESIAN_POINT('Ctrl Pts',(3.31631129755346,17.7406985030951,-1398.29936588071));
#149769=CARTESIAN_POINT('Ctrl Pts',(4.96022910773077,17.4333970061901,-1399.79348352777));
#149770=CARTESIAN_POINT('Ctrl Pts',(6.51968959134575,16.8292587962898,-1401.28760117483));
#149771=CARTESIAN_POINT('Ctrl Pts',(8.07915007496071,16.2251205863895,-1402.78171882189));
#149772=CARTESIAN_POINT('Ctrl Pts',(9.50104767561053,15.3447188656481,-1404.27583646895));
#149773=CARTESIAN_POINT('Ctrl Pts',(10.9229452762603,14.4643171449067,-1405.769954116));
#149774=CARTESIAN_POINT('Ctrl Pts',(12.1588589765331,13.3376329379985,-1407.26407176306));
#149775=CARTESIAN_POINT('Ctrl Pts',(13.3947726768058,12.2109487310903,-1408.75818941012));
#149776=CARTESIAN_POINT('Ctrl Pts',(14.4026149179538,10.8763499173728,-1410.25230705718));
#149777=CARTESIAN_POINT('Ctrl Pts',(15.4104571591017,9.54175110365538,-1411.74642470424));
#149778=CARTESIAN_POINT('Ctrl Pts',(16.1559070823762,8.04468584505496,-1413.2405423513));
#149779=CARTESIAN_POINT('Ctrl Pts',(16.9013570056506,6.54762058645456,-1414.73465999836));
#149780=CARTESIAN_POINT('Ctrl Pts',(17.3590292079831,4.93906964482096,-1416.22877764542));
#149781=CARTESIAN_POINT('Ctrl Pts',(17.8167014103155,3.33051870318735,-1417.72289529247));
#149782=CARTESIAN_POINT('Ctrl Pts',(17.9710104137728,1.66525935159367,-1419.21701293953));
#149783=CARTESIAN_POINT('Ctrl Pts',(18.1253194172301,3.32956716117513E-15,
-1420.71113058659));
#149784=CARTESIAN_POINT('Ctrl Pts',(17.9710104137728,-1.66525935159367,
-1422.20524823365));
#149785=CARTESIAN_POINT('Ctrl Pts',(17.8167014103155,-3.33051870318736,
-1423.69936588071));
#149786=CARTESIAN_POINT('Ctrl Pts',(17.3590292079831,-4.93906964482095,
-1425.19348352777));
#149787=CARTESIAN_POINT('Ctrl Pts',(16.9013570056506,-6.54762058645456,
-1426.68760117483));
#149788=CARTESIAN_POINT('Ctrl Pts',(16.1559070823762,-8.04468584505497,
-1428.18171882189));
#149789=CARTESIAN_POINT('Ctrl Pts',(15.4104571591017,-9.54175110365538,
-1429.67583646895));
#149790=CARTESIAN_POINT('Ctrl Pts',(14.4026149179538,-10.8763499173728,
-1431.169954116));
#149791=CARTESIAN_POINT('Ctrl Pts',(13.3947726768058,-12.2109487310903,
-1432.66407176306));
#149792=CARTESIAN_POINT('Ctrl Pts',(12.1588589765331,-13.3376329379985,
-1434.15818941012));
#149793=CARTESIAN_POINT('Ctrl Pts',(10.9229452762603,-14.4643171449067,
-1435.65230705718));
#149794=CARTESIAN_POINT('Ctrl Pts',(9.50104767561053,-15.3447188656481,
-1437.14642470424));
#149795=CARTESIAN_POINT('Ctrl Pts',(8.07915007496071,-16.2251205863895,
-1438.6405423513));
#149796=CARTESIAN_POINT('Ctrl Pts',(6.51968959134574,-16.8292587962898,
-1440.13465999836));
#149797=CARTESIAN_POINT('Ctrl Pts',(4.96022910773078,-17.4333970061901,
-1441.62877764542));
#149798=CARTESIAN_POINT('Ctrl Pts',(3.31631129755346,-17.7406985030951,
-1443.12289529247));
#149799=CARTESIAN_POINT('Ctrl Pts',(1.67239348737615,-18.048,-1444.61701293953));
#149800=CARTESIAN_POINT('Ctrl Pts',(0.,-18.048,-1446.11113058659));
#149801=CARTESIAN_POINT('Ctrl Pts',(-1.67239348737615,-18.048,-1447.60524823365));
#149802=CARTESIAN_POINT('Ctrl Pts',(-3.31631129755346,-17.7406985030951,
-1449.09936588071));
#149803=CARTESIAN_POINT('Ctrl Pts',(-4.96022910773077,-17.4333970061901,
-1450.59348352777));
#149804=CARTESIAN_POINT('Ctrl Pts',(-6.51968959134574,-16.8292587962898,
-1452.08760117483));
#149805=CARTESIAN_POINT('Ctrl Pts',(-8.07915007496071,-16.2251205863895,
-1453.58171882189));
#149806=CARTESIAN_POINT('Ctrl Pts',(-9.50104767561052,-15.3447188656481,
-1455.07583646895));
#149807=CARTESIAN_POINT('Ctrl Pts',(-10.9229452762603,-14.4643171449067,
-1456.569954116));
#149808=CARTESIAN_POINT('Ctrl Pts',(-12.1588589765331,-13.3376329379985,
-1458.06407176306));
#149809=CARTESIAN_POINT('Ctrl Pts',(-13.3947726768058,-12.2109487310903,
-1459.55818941012));
#149810=CARTESIAN_POINT('Ctrl Pts',(-14.4026149179538,-10.8763499173728,
-1461.05230705718));
#149811=CARTESIAN_POINT('Ctrl Pts',(-15.4104571591017,-9.54175110365538,
-1462.54642470424));
#149812=CARTESIAN_POINT('Ctrl Pts',(-16.1559070823762,-8.04468584505497,
-1464.0405423513));
#149813=CARTESIAN_POINT('Ctrl Pts',(-16.9013570056506,-6.54762058645456,
-1465.53465999836));
#149814=CARTESIAN_POINT('Ctrl Pts',(-17.3590292079831,-4.93906964482095,
-1467.02877764542));
#149815=CARTESIAN_POINT('Ctrl Pts',(-17.8167014103155,-3.33051870318735,
-1468.52289529247));
#149816=CARTESIAN_POINT('Ctrl Pts',(-17.9710104137728,-1.66525935159368,
-1470.01701293953));
#149817=CARTESIAN_POINT('Ctrl Pts',(-18.1253194172301,-1.10985572039171E-15,
-1471.51113058659));
#149818=CARTESIAN_POINT('Ctrl Pts',(-17.9710104137728,1.66525935159367,
-1473.00524823365));
#149819=CARTESIAN_POINT('Ctrl Pts',(-17.8167014103155,3.33051870318735,
-1474.49936588071));
#149820=CARTESIAN_POINT('Ctrl Pts',(-17.3590292079831,4.93906964482096,
-1475.99348352777));
#149821=CARTESIAN_POINT('Ctrl Pts',(-16.9013570056506,6.54762058645456,
-1477.48760117483));
#149822=CARTESIAN_POINT('Ctrl Pts',(-16.1559070823762,8.04468584505497,
-1478.98171882189));
#149823=CARTESIAN_POINT('Ctrl Pts',(-15.4104571591017,9.54175110365538,
-1480.47583646895));
#149824=CARTESIAN_POINT('Ctrl Pts',(-14.4026149179538,10.8763499173728,
-1481.969954116));
#149825=CARTESIAN_POINT('Ctrl Pts',(-13.3947726768058,12.2109487310903,
-1483.46407176306));
#149826=CARTESIAN_POINT('Ctrl Pts',(-12.1588589765331,13.3376329379985,
-1484.95818941012));
#149827=CARTESIAN_POINT('Ctrl Pts',(-10.9229452762603,14.4643171449067,
-1486.45230705718));
#149828=CARTESIAN_POINT('Ctrl Pts',(-9.50104767561052,15.3447188656481,
-1487.94642470424));
#149829=CARTESIAN_POINT('Ctrl Pts',(-8.07915007496071,16.2251205863895,
-1489.4405423513));
#149830=CARTESIAN_POINT('Ctrl Pts',(-6.51968959134574,16.8292587962898,
-1490.93465999836));
#149831=CARTESIAN_POINT('Ctrl Pts',(-4.96022910773078,17.4333970061901,
-1492.42877764542));
#149832=CARTESIAN_POINT('Ctrl Pts',(-3.31631129755346,17.7406985030951,
-1493.92289529247));
#149833=CARTESIAN_POINT('Ctrl Pts',(-1.67239348737615,18.048,-1495.41701293953));
#149834=CARTESIAN_POINT('Ctrl Pts',(-2.21024254310115E-15,18.048,-1496.91113058659));
#149835=CARTESIAN_POINT('Ctrl Pts',(1.67239348737616,18.048,-1498.40524823365));
#149836=CARTESIAN_POINT('Ctrl Pts',(3.31631129755346,17.7406985030951,-1499.89936588071));
#149837=CARTESIAN_POINT('Ctrl Pts',(4.96022910773077,17.4333970061901,-1501.39348352777));
#149838=CARTESIAN_POINT('Ctrl Pts',(6.51968959134575,16.8292587962898,-1502.88760117483));
#149839=CARTESIAN_POINT('Ctrl Pts',(7.54139510186126,16.4334479728329,-1503.86649627951));
#149840=CARTESIAN_POINT('Ctrl Pts',(8.50771391856893,15.9169440496532,-1504.8491753622));
#149841=CARTESIAN_POINT('',(4.96991138555256,-17.3502243449402,692.));
#149842=CARTESIAN_POINT('Origin',(-231.282509043856,-78.0829325244463,692.000033290347));
#149843=CARTESIAN_POINT('',(0.,-18.048,1500.28886941341));
#149844=CARTESIAN_POINT('Ctrl Pts',(0.,-18.048,1500.28886941341));
#149845=CARTESIAN_POINT('Ctrl Pts',(-1.67239348737611,-18.048,1498.79475176635));
#149846=CARTESIAN_POINT('Ctrl Pts',(-3.31631129755346,-17.7406985030951,
1497.30063411929));
#149847=CARTESIAN_POINT('Ctrl Pts',(-4.96022910773077,-17.4333970061901,
1495.80651647223));
#149848=CARTESIAN_POINT('Ctrl Pts',(-6.51968959134574,-16.8292587962898,
1494.31239882517));
#149849=CARTESIAN_POINT('Ctrl Pts',(-8.07915007496071,-16.2251205863895,
1492.81828117811));
#149850=CARTESIAN_POINT('Ctrl Pts',(-9.50104767561052,-15.3447188656481,
1491.32416353106));
#149851=CARTESIAN_POINT('Ctrl Pts',(-10.9229452762603,-14.4643171449067,
1489.830045884));
#149852=CARTESIAN_POINT('Ctrl Pts',(-12.1588589765331,-13.3376329379985,
1488.33592823694));
#149853=CARTESIAN_POINT('Ctrl Pts',(-13.3947726768058,-12.2109487310903,
1486.84181058988));
#149854=CARTESIAN_POINT('Ctrl Pts',(-14.4026149179538,-10.8763499173728,
1485.34769294282));
#149855=CARTESIAN_POINT('Ctrl Pts',(-15.4104571591017,-9.54175110365538,
1483.85357529576));
#149856=CARTESIAN_POINT('Ctrl Pts',(-16.1559070823762,-8.04468584505497,
1482.3594576487));
#149857=CARTESIAN_POINT('Ctrl Pts',(-16.9013570056506,-6.54762058645456,
1480.86534000164));
#149858=CARTESIAN_POINT('Ctrl Pts',(-17.3590292079831,-4.93906964482095,
1479.37122235458));
#149859=CARTESIAN_POINT('Ctrl Pts',(-17.8167014103155,-3.33051870318735,
1477.87710470753));
#149860=CARTESIAN_POINT('Ctrl Pts',(-17.9710104137728,-1.66525935159368,
1476.38298706047));
#149861=CARTESIAN_POINT('Ctrl Pts',(-18.1253194172301,-1.10985572039171E-15,
1474.88886941341));
#149862=CARTESIAN_POINT('Ctrl Pts',(-17.9710104137728,1.66525935159367,
1473.39475176635));
#149863=CARTESIAN_POINT('Ctrl Pts',(-17.8167014103155,3.33051870318735,
1471.90063411929));
#149864=CARTESIAN_POINT('Ctrl Pts',(-17.3590292079831,4.93906964482096,
1470.40651647223));
#149865=CARTESIAN_POINT('Ctrl Pts',(-16.9013570056506,6.54762058645456,
1468.91239882517));
#149866=CARTESIAN_POINT('Ctrl Pts',(-16.1559070823762,8.04468584505497,
1467.41828117811));
#149867=CARTESIAN_POINT('Ctrl Pts',(-15.4104571591017,9.54175110365538,
1465.92416353106));
#149868=CARTESIAN_POINT('Ctrl Pts',(-14.4026149179538,10.8763499173728,
1464.430045884));
#149869=CARTESIAN_POINT('Ctrl Pts',(-13.3947726768058,12.2109487310903,
1462.93592823694));
#149870=CARTESIAN_POINT('Ctrl Pts',(-12.1588589765331,13.3376329379985,
1461.44181058988));
#149871=CARTESIAN_POINT('Ctrl Pts',(-10.9229452762603,14.4643171449067,
1459.94769294282));
#149872=CARTESIAN_POINT('Ctrl Pts',(-9.50104767561052,15.3447188656481,
1458.45357529576));
#149873=CARTESIAN_POINT('Ctrl Pts',(-8.07915007496071,16.2251205863895,
1456.9594576487));
#149874=CARTESIAN_POINT('Ctrl Pts',(-6.51968959134574,16.8292587962898,
1455.46534000164));
#149875=CARTESIAN_POINT('Ctrl Pts',(-4.96022910773078,17.4333970061901,
1453.97122235458));
#149876=CARTESIAN_POINT('Ctrl Pts',(-3.31631129755346,17.7406985030951,
1452.47710470753));
#149877=CARTESIAN_POINT('Ctrl Pts',(-1.67239348737615,18.048,1450.98298706047));
#149878=CARTESIAN_POINT('Ctrl Pts',(-2.21024254310115E-15,18.048,1449.48886941341));
#149879=CARTESIAN_POINT('Ctrl Pts',(1.67239348737616,18.048,1447.99475176635));
#149880=CARTESIAN_POINT('Ctrl Pts',(3.31631129755346,17.7406985030951,1446.50063411929));
#149881=CARTESIAN_POINT('Ctrl Pts',(4.96022910773077,17.4333970061901,1445.00651647223));
#149882=CARTESIAN_POINT('Ctrl Pts',(6.51968959134575,16.8292587962898,1443.51239882517));
#149883=CARTESIAN_POINT('Ctrl Pts',(8.07915007496071,16.2251205863895,1442.01828117811));
#149884=CARTESIAN_POINT('Ctrl Pts',(9.50104767561053,15.3447188656481,1440.52416353105));
#149885=CARTESIAN_POINT('Ctrl Pts',(10.9229452762603,14.4643171449067,1439.030045884));
#149886=CARTESIAN_POINT('Ctrl Pts',(12.1588589765331,13.3376329379985,1437.53592823694));
#149887=CARTESIAN_POINT('Ctrl Pts',(13.3947726768058,12.2109487310903,1436.04181058988));
#149888=CARTESIAN_POINT('Ctrl Pts',(14.4026149179538,10.8763499173728,1434.54769294282));
#149889=CARTESIAN_POINT('Ctrl Pts',(15.4104571591017,9.54175110365539,1433.05357529576));
#149890=CARTESIAN_POINT('Ctrl Pts',(16.1559070823762,8.04468584505496,1431.5594576487));
#149891=CARTESIAN_POINT('Ctrl Pts',(16.9013570056506,6.54762058645456,1430.06534000164));
#149892=CARTESIAN_POINT('Ctrl Pts',(17.3590292079831,4.93906964482096,1428.57122235458));
#149893=CARTESIAN_POINT('Ctrl Pts',(17.8167014103155,3.33051870318735,1427.07710470753));
#149894=CARTESIAN_POINT('Ctrl Pts',(17.9710104137728,1.66525935159367,1425.58298706047));
#149895=CARTESIAN_POINT('Ctrl Pts',(18.1253194172301,3.32956716117513E-15,
1424.08886941341));
#149896=CARTESIAN_POINT('Ctrl Pts',(17.9710104137728,-1.66525935159367,
1422.59475176635));
#149897=CARTESIAN_POINT('Ctrl Pts',(17.8167014103155,-3.33051870318736,
1421.10063411929));
#149898=CARTESIAN_POINT('Ctrl Pts',(17.3590292079831,-4.93906964482095,
1419.60651647223));
#149899=CARTESIAN_POINT('Ctrl Pts',(16.9013570056506,-6.54762058645456,
1418.11239882517));
#149900=CARTESIAN_POINT('Ctrl Pts',(16.1559070823762,-8.04468584505497,
1416.61828117811));
#149901=CARTESIAN_POINT('Ctrl Pts',(15.4104571591017,-9.54175110365538,
1415.12416353105));
#149902=CARTESIAN_POINT('Ctrl Pts',(14.4026149179538,-10.8763499173728,
1413.630045884));
#149903=CARTESIAN_POINT('Ctrl Pts',(13.3947726768058,-12.2109487310903,
1412.13592823694));
#149904=CARTESIAN_POINT('Ctrl Pts',(12.1588589765331,-13.3376329379985,
1410.64181058988));
#149905=CARTESIAN_POINT('Ctrl Pts',(10.9229452762603,-14.4643171449067,
1409.14769294282));
#149906=CARTESIAN_POINT('Ctrl Pts',(9.50104767561053,-15.3447188656481,
1407.65357529576));
#149907=CARTESIAN_POINT('Ctrl Pts',(8.07915007496071,-16.2251205863895,
1406.1594576487));
#149908=CARTESIAN_POINT('Ctrl Pts',(6.51968959134574,-16.8292587962898,
1404.66534000164));
#149909=CARTESIAN_POINT('Ctrl Pts',(4.96022910773078,-17.4333970061901,
1403.17122235458));
#149910=CARTESIAN_POINT('Ctrl Pts',(3.31631129755346,-17.7406985030951,
1401.67710470753));
#149911=CARTESIAN_POINT('Ctrl Pts',(1.67239348737615,-18.048,1400.18298706047));
#149912=CARTESIAN_POINT('Ctrl Pts',(0.,-18.048,1398.68886941341));
#149913=CARTESIAN_POINT('Ctrl Pts',(-1.67239348737615,-18.048,1397.19475176635));
#149914=CARTESIAN_POINT('Ctrl Pts',(-3.31631129755346,-17.7406985030951,
1395.70063411929));
#149915=CARTESIAN_POINT('Ctrl Pts',(-4.96022910773077,-17.4333970061901,
1394.20651647223));
#149916=CARTESIAN_POINT('Ctrl Pts',(-6.51968959134574,-16.8292587962898,
1392.71239882517));
#149917=CARTESIAN_POINT('Ctrl Pts',(-8.07915007496071,-16.2251205863895,
1391.21828117811));
#149918=CARTESIAN_POINT('Ctrl Pts',(-9.50104767561052,-15.3447188656481,
1389.72416353105));
#149919=CARTESIAN_POINT('Ctrl Pts',(-10.9229452762603,-14.4643171449067,
1388.230045884));
#149920=CARTESIAN_POINT('Ctrl Pts',(-12.1588589765331,-13.3376329379985,
1386.73592823694));
#149921=CARTESIAN_POINT('Ctrl Pts',(-13.3947726768058,-12.2109487310903,
1385.24181058988));
#149922=CARTESIAN_POINT('Ctrl Pts',(-14.4026149179538,-10.8763499173728,
1383.74769294282));
#149923=CARTESIAN_POINT('Ctrl Pts',(-15.4104571591017,-9.54175110365538,
1382.25357529576));
#149924=CARTESIAN_POINT('Ctrl Pts',(-16.1559070823762,-8.04468584505497,
1380.7594576487));
#149925=CARTESIAN_POINT('Ctrl Pts',(-16.9013570056506,-6.54762058645456,
1379.26534000164));
#149926=CARTESIAN_POINT('Ctrl Pts',(-17.3590292079831,-4.93906964482095,
1377.77122235458));
#149927=CARTESIAN_POINT('Ctrl Pts',(-17.8167014103155,-3.33051870318735,
1376.27710470753));
#149928=CARTESIAN_POINT('Ctrl Pts',(-17.9710104137728,-1.66525935159368,
1374.78298706047));
#149929=CARTESIAN_POINT('Ctrl Pts',(-18.1253194172301,-1.10985572039171E-15,
1373.28886941341));
#149930=CARTESIAN_POINT('Ctrl Pts',(-17.9710104137728,1.66525935159367,
1371.79475176635));
#149931=CARTESIAN_POINT('Ctrl Pts',(-17.8167014103155,3.33051870318735,
1370.30063411929));
#149932=CARTESIAN_POINT('Ctrl Pts',(-17.3590292079831,4.93906964482096,
1368.80651647223));
#149933=CARTESIAN_POINT('Ctrl Pts',(-16.9013570056506,6.54762058645456,
1367.31239882517));
#149934=CARTESIAN_POINT('Ctrl Pts',(-16.1559070823762,8.04468584505497,
1365.81828117811));
#149935=CARTESIAN_POINT('Ctrl Pts',(-15.4104571591017,9.54175110365538,
1364.32416353105));
#149936=CARTESIAN_POINT('Ctrl Pts',(-14.4026149179538,10.8763499173728,
1362.830045884));
#149937=CARTESIAN_POINT('Ctrl Pts',(-13.3947726768058,12.2109487310903,
1361.33592823694));
#149938=CARTESIAN_POINT('Ctrl Pts',(-12.1588589765331,13.3376329379985,
1359.84181058988));
#149939=CARTESIAN_POINT('Ctrl Pts',(-10.9229452762603,14.4643171449067,
1358.34769294282));
#149940=CARTESIAN_POINT('Ctrl Pts',(-9.50104767561052,15.3447188656481,
1356.85357529576));
#149941=CARTESIAN_POINT('Ctrl Pts',(-8.07915007496071,16.2251205863895,
1355.3594576487));
#149942=CARTESIAN_POINT('Ctrl Pts',(-6.51968959134574,16.8292587962898,
1353.86534000164));
#149943=CARTESIAN_POINT('Ctrl Pts',(-4.96022910773078,17.4333970061901,
1352.37122235458));
#149944=CARTESIAN_POINT('Ctrl Pts',(-3.31631129755346,17.7406985030951,
1350.87710470753));
#149945=CARTESIAN_POINT('Ctrl Pts',(-1.67239348737615,18.048,1349.38298706047));
#149946=CARTESIAN_POINT('Ctrl Pts',(-2.21024254310115E-15,18.048,1347.88886941341));
#149947=CARTESIAN_POINT('Ctrl Pts',(1.67239348737616,18.048,1346.39475176635));
#149948=CARTESIAN_POINT('Ctrl Pts',(3.31631129755346,17.7406985030951,1344.90063411929));
#149949=CARTESIAN_POINT('Ctrl Pts',(4.96022910773077,17.4333970061901,1343.40651647223));
#149950=CARTESIAN_POINT('Ctrl Pts',(6.51968959134575,16.8292587962898,1341.91239882517));
#149951=CARTESIAN_POINT('Ctrl Pts',(8.07915007496071,16.2251205863895,1340.41828117811));
#149952=CARTESIAN_POINT('Ctrl Pts',(9.50104767561053,15.3447188656481,1338.92416353106));
#149953=CARTESIAN_POINT('Ctrl Pts',(10.9229452762603,14.4643171449067,1337.430045884));
#149954=CARTESIAN_POINT('Ctrl Pts',(12.1588589765331,13.3376329379985,1335.93592823694));
#149955=CARTESIAN_POINT('Ctrl Pts',(13.3947726768058,12.2109487310903,1334.44181058988));
#149956=CARTESIAN_POINT('Ctrl Pts',(14.4026149179538,10.8763499173728,1332.94769294282));
#149957=CARTESIAN_POINT('Ctrl Pts',(15.4104571591017,9.54175110365539,1331.45357529576));
#149958=CARTESIAN_POINT('Ctrl Pts',(16.1559070823762,8.04468584505496,1329.9594576487));
#149959=CARTESIAN_POINT('Ctrl Pts',(16.9013570056506,6.54762058645456,1328.46534000164));
#149960=CARTESIAN_POINT('Ctrl Pts',(17.3590292079831,4.93906964482096,1326.97122235458));
#149961=CARTESIAN_POINT('Ctrl Pts',(17.8167014103155,3.33051870318735,1325.47710470753));
#149962=CARTESIAN_POINT('Ctrl Pts',(17.9710104137728,1.66525935159367,1323.98298706047));
#149963=CARTESIAN_POINT('Ctrl Pts',(18.1253194172301,3.32956716117513E-15,
1322.48886941341));
#149964=CARTESIAN_POINT('Ctrl Pts',(17.9710104137728,-1.66525935159367,
1320.99475176635));
#149965=CARTESIAN_POINT('Ctrl Pts',(17.8167014103155,-3.33051870318736,
1319.50063411929));
#149966=CARTESIAN_POINT('Ctrl Pts',(17.3590292079831,-4.93906964482095,
1318.00651647223));
#149967=CARTESIAN_POINT('Ctrl Pts',(16.9013570056506,-6.54762058645456,
1316.51239882517));
#149968=CARTESIAN_POINT('Ctrl Pts',(16.1559070823762,-8.04468584505497,
1315.01828117811));
#149969=CARTESIAN_POINT('Ctrl Pts',(15.4104571591017,-9.54175110365538,
1313.52416353105));
#149970=CARTESIAN_POINT('Ctrl Pts',(14.4026149179538,-10.8763499173728,
1312.030045884));
#149971=CARTESIAN_POINT('Ctrl Pts',(13.3947726768058,-12.2109487310903,
1310.53592823694));
#149972=CARTESIAN_POINT('Ctrl Pts',(12.1588589765331,-13.3376329379985,
1309.04181058988));
#149973=CARTESIAN_POINT('Ctrl Pts',(10.9229452762603,-14.4643171449067,
1307.54769294282));
#149974=CARTESIAN_POINT('Ctrl Pts',(9.50104767561053,-15.3447188656481,
1306.05357529576));
#149975=CARTESIAN_POINT('Ctrl Pts',(8.07915007496071,-16.2251205863895,
1304.5594576487));
#149976=CARTESIAN_POINT('Ctrl Pts',(6.51968959134574,-16.8292587962898,
1303.06534000164));
#149977=CARTESIAN_POINT('Ctrl Pts',(4.96022910773078,-17.4333970061901,
1301.57122235458));
#149978=CARTESIAN_POINT('Ctrl Pts',(3.31631129755346,-17.7406985030951,
1300.07710470753));
#149979=CARTESIAN_POINT('Ctrl Pts',(1.67239348737615,-18.048,1298.58298706047));
#149980=CARTESIAN_POINT('Ctrl Pts',(0.,-18.048,1297.08886941341));
#149981=CARTESIAN_POINT('Ctrl Pts',(-1.67239348737615,-18.048,1295.59475176635));
#149982=CARTESIAN_POINT('Ctrl Pts',(-3.31631129755346,-17.7406985030951,
1294.10063411929));
#149983=CARTESIAN_POINT('Ctrl Pts',(-4.96022910773077,-17.4333970061901,
1292.60651647223));
#149984=CARTESIAN_POINT('Ctrl Pts',(-6.51968959134574,-16.8292587962898,
1291.11239882517));
#149985=CARTESIAN_POINT('Ctrl Pts',(-8.07915007496071,-16.2251205863895,
1289.61828117811));
#149986=CARTESIAN_POINT('Ctrl Pts',(-9.50104767561052,-15.3447188656481,
1288.12416353105));
#149987=CARTESIAN_POINT('Ctrl Pts',(-10.9229452762603,-14.4643171449067,
1286.630045884));
#149988=CARTESIAN_POINT('Ctrl Pts',(-12.1588589765331,-13.3376329379985,
1285.13592823694));
#149989=CARTESIAN_POINT('Ctrl Pts',(-13.3947726768058,-12.2109487310903,
1283.64181058988));
#149990=CARTESIAN_POINT('Ctrl Pts',(-14.4026149179538,-10.8763499173728,
1282.14769294282));
#149991=CARTESIAN_POINT('Ctrl Pts',(-15.4104571591017,-9.54175110365538,
1280.65357529576));
#149992=CARTESIAN_POINT('Ctrl Pts',(-16.1559070823762,-8.04468584505497,
1279.1594576487));
#149993=CARTESIAN_POINT('Ctrl Pts',(-16.9013570056506,-6.54762058645456,
1277.66534000164));
#149994=CARTESIAN_POINT('Ctrl Pts',(-17.3590292079831,-4.93906964482095,
1276.17122235458));
#149995=CARTESIAN_POINT('Ctrl Pts',(-17.8167014103155,-3.33051870318735,
1274.67710470753));
#149996=CARTESIAN_POINT('Ctrl Pts',(-17.9710104137728,-1.66525935159368,
1273.18298706047));
#149997=CARTESIAN_POINT('Ctrl Pts',(-18.1253194172301,-1.10985572039171E-15,
1271.68886941341));
#149998=CARTESIAN_POINT('Ctrl Pts',(-17.9710104137728,1.66525935159367,
1270.19475176635));
#149999=CARTESIAN_POINT('Ctrl Pts',(-17.8167014103155,3.33051870318735,
1268.70063411929));
#150000=CARTESIAN_POINT('Ctrl Pts',(-17.3590292079831,4.93906964482096,
1267.20651647223));
#150001=CARTESIAN_POINT('Ctrl Pts',(-16.9013570056506,6.54762058645456,
1265.71239882517));
#150002=CARTESIAN_POINT('Ctrl Pts',(-16.1559070823762,8.04468584505497,
1264.21828117811));
#150003=CARTESIAN_POINT('Ctrl Pts',(-15.4104571591017,9.54175110365538,
1262.72416353105));
#150004=CARTESIAN_POINT('Ctrl Pts',(-14.4026149179538,10.8763499173728,
1261.230045884));
#150005=CARTESIAN_POINT('Ctrl Pts',(-13.3947726768058,12.2109487310903,
1259.73592823694));
#150006=CARTESIAN_POINT('Ctrl Pts',(-12.1588589765331,13.3376329379985,
1258.24181058988));
#150007=CARTESIAN_POINT('Ctrl Pts',(-10.9229452762603,14.4643171449067,
1256.74769294282));
#150008=CARTESIAN_POINT('Ctrl Pts',(-9.50104767561052,15.3447188656481,
1255.25357529576));
#150009=CARTESIAN_POINT('Ctrl Pts',(-8.07915007496071,16.2251205863895,
1253.7594576487));
#150010=CARTESIAN_POINT('Ctrl Pts',(-6.51968959134574,16.8292587962898,
1252.26534000164));
#150011=CARTESIAN_POINT('Ctrl Pts',(-4.96022910773078,17.4333970061901,
1250.77122235458));
#150012=CARTESIAN_POINT('Ctrl Pts',(-3.31631129755346,17.7406985030951,
1249.27710470753));
#150013=CARTESIAN_POINT('Ctrl Pts',(-1.67239348737615,18.048,1247.78298706047));
#150014=CARTESIAN_POINT('Ctrl Pts',(-2.21024254310115E-15,18.048,1246.28886941341));
#150015=CARTESIAN_POINT('Ctrl Pts',(1.67239348737616,18.048,1244.79475176635));
#150016=CARTESIAN_POINT('Ctrl Pts',(3.31631129755346,17.7406985030951,1243.30063411929));
#150017=CARTESIAN_POINT('Ctrl Pts',(4.96022910773077,17.4333970061901,1241.80651647223));
#150018=CARTESIAN_POINT('Ctrl Pts',(6.51968959134575,16.8292587962898,1240.31239882517));
#150019=CARTESIAN_POINT('Ctrl Pts',(8.07915007496071,16.2251205863895,1238.81828117811));
#150020=CARTESIAN_POINT('Ctrl Pts',(9.50104767561053,15.3447188656481,1237.32416353105));
#150021=CARTESIAN_POINT('Ctrl Pts',(10.9229452762603,14.4643171449067,1235.830045884));
#150022=CARTESIAN_POINT('Ctrl Pts',(12.1588589765331,13.3376329379985,1234.33592823694));
#150023=CARTESIAN_POINT('Ctrl Pts',(13.3947726768058,12.2109487310903,1232.84181058988));
#150024=CARTESIAN_POINT('Ctrl Pts',(14.4026149179538,10.8763499173728,1231.34769294282));
#150025=CARTESIAN_POINT('Ctrl Pts',(15.4104571591017,9.54175110365539,1229.85357529576));
#150026=CARTESIAN_POINT('Ctrl Pts',(16.1559070823762,8.04468584505496,1228.3594576487));
#150027=CARTESIAN_POINT('Ctrl Pts',(16.9013570056506,6.54762058645456,1226.86534000164));
#150028=CARTESIAN_POINT('Ctrl Pts',(17.3590292079831,4.93906964482096,1225.37122235458));
#150029=CARTESIAN_POINT('Ctrl Pts',(17.8167014103155,3.33051870318735,1223.87710470753));
#150030=CARTESIAN_POINT('Ctrl Pts',(17.9710104137728,1.66525935159367,1222.38298706047));
#150031=CARTESIAN_POINT('Ctrl Pts',(18.1253194172301,3.32956716117513E-15,
1220.88886941341));
#150032=CARTESIAN_POINT('Ctrl Pts',(17.9710104137728,-1.66525935159367,
1219.39475176635));
#150033=CARTESIAN_POINT('Ctrl Pts',(17.8167014103155,-3.33051870318736,
1217.90063411929));
#150034=CARTESIAN_POINT('Ctrl Pts',(17.3590292079831,-4.93906964482095,
1216.40651647223));
#150035=CARTESIAN_POINT('Ctrl Pts',(16.9013570056506,-6.54762058645456,
1214.91239882517));
#150036=CARTESIAN_POINT('Ctrl Pts',(16.1559070823762,-8.04468584505497,
1213.41828117811));
#150037=CARTESIAN_POINT('Ctrl Pts',(15.4104571591017,-9.54175110365538,
1211.92416353106));
#150038=CARTESIAN_POINT('Ctrl Pts',(14.4026149179538,-10.8763499173728,
1210.430045884));
#150039=CARTESIAN_POINT('Ctrl Pts',(13.3947726768058,-12.2109487310903,
1208.93592823694));
#150040=CARTESIAN_POINT('Ctrl Pts',(12.1588589765331,-13.3376329379985,
1207.44181058988));
#150041=CARTESIAN_POINT('Ctrl Pts',(10.9229452762603,-14.4643171449067,
1205.94769294282));
#150042=CARTESIAN_POINT('Ctrl Pts',(9.50104767561053,-15.3447188656481,
1204.45357529576));
#150043=CARTESIAN_POINT('Ctrl Pts',(8.07915007496071,-16.2251205863895,
1202.9594576487));
#150044=CARTESIAN_POINT('Ctrl Pts',(6.51968959134574,-16.8292587962898,
1201.46534000164));
#150045=CARTESIAN_POINT('Ctrl Pts',(4.96022910773078,-17.4333970061901,
1199.97122235458));
#150046=CARTESIAN_POINT('Ctrl Pts',(3.31631129755346,-17.7406985030951,
1198.47710470753));
#150047=CARTESIAN_POINT('Ctrl Pts',(1.67239348737615,-18.048,1196.98298706047));
#150048=CARTESIAN_POINT('Ctrl Pts',(0.,-18.048,1195.48886941341));
#150049=CARTESIAN_POINT('Ctrl Pts',(-1.67239348737615,-18.048,1193.99475176635));
#150050=CARTESIAN_POINT('Ctrl Pts',(-3.31631129755346,-17.7406985030951,
1192.50063411929));
#150051=CARTESIAN_POINT('Ctrl Pts',(-4.96022910773077,-17.4333970061901,
1191.00651647223));
#150052=CARTESIAN_POINT('Ctrl Pts',(-6.51968959134574,-16.8292587962898,
1189.51239882517));
#150053=CARTESIAN_POINT('Ctrl Pts',(-8.07915007496071,-16.2251205863895,
1188.01828117811));
#150054=CARTESIAN_POINT('Ctrl Pts',(-9.50104767561052,-15.3447188656481,
1186.52416353105));
#150055=CARTESIAN_POINT('Ctrl Pts',(-10.9229452762603,-14.4643171449067,
1185.030045884));
#150056=CARTESIAN_POINT('Ctrl Pts',(-12.1588589765331,-13.3376329379985,
1183.53592823694));
#150057=CARTESIAN_POINT('Ctrl Pts',(-13.3947726768058,-12.2109487310903,
1182.04181058988));
#150058=CARTESIAN_POINT('Ctrl Pts',(-14.4026149179538,-10.8763499173728,
1180.54769294282));
#150059=CARTESIAN_POINT('Ctrl Pts',(-15.4104571591017,-9.54175110365538,
1179.05357529576));
#150060=CARTESIAN_POINT('Ctrl Pts',(-16.1559070823762,-8.04468584505497,
1177.5594576487));
#150061=CARTESIAN_POINT('Ctrl Pts',(-16.9013570056506,-6.54762058645456,
1176.06534000164));
#150062=CARTESIAN_POINT('Ctrl Pts',(-17.3590292079831,-4.93906964482095,
1174.57122235458));
#150063=CARTESIAN_POINT('Ctrl Pts',(-17.8167014103155,-3.33051870318735,
1173.07710470753));
#150064=CARTESIAN_POINT('Ctrl Pts',(-17.9710104137728,-1.66525935159368,
1171.58298706047));
#150065=CARTESIAN_POINT('Ctrl Pts',(-18.1253194172301,-1.10985572039171E-15,
1170.08886941341));
#150066=CARTESIAN_POINT('Ctrl Pts',(-17.9710104137728,1.66525935159367,
1168.59475176635));
#150067=CARTESIAN_POINT('Ctrl Pts',(-17.8167014103155,3.33051870318735,
1167.10063411929));
#150068=CARTESIAN_POINT('Ctrl Pts',(-17.3590292079831,4.93906964482096,
1165.60651647223));
#150069=CARTESIAN_POINT('Ctrl Pts',(-16.9013570056506,6.54762058645456,
1164.11239882517));
#150070=CARTESIAN_POINT('Ctrl Pts',(-16.1559070823762,8.04468584505497,
1162.61828117811));
#150071=CARTESIAN_POINT('Ctrl Pts',(-15.4104571591017,9.54175110365538,
1161.12416353106));
#150072=CARTESIAN_POINT('Ctrl Pts',(-14.4026149179538,10.8763499173728,
1159.630045884));
#150073=CARTESIAN_POINT('Ctrl Pts',(-13.3947726768058,12.2109487310903,
1158.13592823694));
#150074=CARTESIAN_POINT('Ctrl Pts',(-12.1588589765331,13.3376329379985,
1156.64181058988));
#150075=CARTESIAN_POINT('Ctrl Pts',(-10.9229452762603,14.4643171449067,
1155.14769294282));
#150076=CARTESIAN_POINT('Ctrl Pts',(-9.50104767561052,15.3447188656481,
1153.65357529576));
#150077=CARTESIAN_POINT('Ctrl Pts',(-8.07915007496071,16.2251205863895,
1152.1594576487));
#150078=CARTESIAN_POINT('Ctrl Pts',(-6.51968959134574,16.8292587962898,
1150.66534000164));
#150079=CARTESIAN_POINT('Ctrl Pts',(-4.96022910773078,17.4333970061901,
1149.17122235458));
#150080=CARTESIAN_POINT('Ctrl Pts',(-3.31631129755346,17.7406985030951,
1147.67710470753));
#150081=CARTESIAN_POINT('Ctrl Pts',(-1.67239348737615,18.048,1146.18298706047));
#150082=CARTESIAN_POINT('Ctrl Pts',(-2.21024254310115E-15,18.048,1144.68886941341));
#150083=CARTESIAN_POINT('Ctrl Pts',(1.67239348737616,18.048,1143.19475176635));
#150084=CARTESIAN_POINT('Ctrl Pts',(3.31631129755346,17.7406985030951,1141.70063411929));
#150085=CARTESIAN_POINT('Ctrl Pts',(4.96022910773077,17.4333970061901,1140.20651647223));
#150086=CARTESIAN_POINT('Ctrl Pts',(6.51968959134575,16.8292587962898,1138.71239882517));
#150087=CARTESIAN_POINT('Ctrl Pts',(8.07915007496071,16.2251205863895,1137.21828117811));
#150088=CARTESIAN_POINT('Ctrl Pts',(9.50104767561053,15.3447188656481,1135.72416353105));
#150089=CARTESIAN_POINT('Ctrl Pts',(10.9229452762603,14.4643171449067,1134.230045884));
#150090=CARTESIAN_POINT('Ctrl Pts',(12.1588589765331,13.3376329379985,1132.73592823694));
#150091=CARTESIAN_POINT('Ctrl Pts',(13.3947726768058,12.2109487310903,1131.24181058988));
#150092=CARTESIAN_POINT('Ctrl Pts',(14.4026149179538,10.8763499173728,1129.74769294282));
#150093=CARTESIAN_POINT('Ctrl Pts',(15.4104571591017,9.54175110365539,1128.25357529576));
#150094=CARTESIAN_POINT('Ctrl Pts',(16.1559070823762,8.04468584505496,1126.7594576487));
#150095=CARTESIAN_POINT('Ctrl Pts',(16.9013570056506,6.54762058645456,1125.26534000164));
#150096=CARTESIAN_POINT('Ctrl Pts',(17.3590292079831,4.93906964482096,1123.77122235458));
#150097=CARTESIAN_POINT('Ctrl Pts',(17.8167014103155,3.33051870318735,1122.27710470753));
#150098=CARTESIAN_POINT('Ctrl Pts',(17.9710104137728,1.66525935159367,1120.78298706047));
#150099=CARTESIAN_POINT('Ctrl Pts',(18.1253194172301,3.32956716117513E-15,
1119.28886941341));
#150100=CARTESIAN_POINT('Ctrl Pts',(17.9710104137728,-1.66525935159367,
1117.79475176635));
#150101=CARTESIAN_POINT('Ctrl Pts',(17.8167014103155,-3.33051870318736,
1116.30063411929));
#150102=CARTESIAN_POINT('Ctrl Pts',(17.3590292079831,-4.93906964482095,
1114.80651647223));
#150103=CARTESIAN_POINT('Ctrl Pts',(16.9013570056506,-6.54762058645456,
1113.31239882517));
#150104=CARTESIAN_POINT('Ctrl Pts',(16.1559070823762,-8.04468584505497,
1111.81828117811));
#150105=CARTESIAN_POINT('Ctrl Pts',(15.4104571591017,-9.54175110365538,
1110.32416353105));
#150106=CARTESIAN_POINT('Ctrl Pts',(14.4026149179538,-10.8763499173728,
1108.830045884));
#150107=CARTESIAN_POINT('Ctrl Pts',(13.3947726768058,-12.2109487310903,
1107.33592823694));
#150108=CARTESIAN_POINT('Ctrl Pts',(12.1588589765331,-13.3376329379985,
1105.84181058988));
#150109=CARTESIAN_POINT('Ctrl Pts',(10.9229452762603,-14.4643171449067,
1104.34769294282));
#150110=CARTESIAN_POINT('Ctrl Pts',(9.50104767561053,-15.3447188656481,
1102.85357529576));
#150111=CARTESIAN_POINT('Ctrl Pts',(8.07915007496071,-16.2251205863895,
1101.3594576487));
#150112=CARTESIAN_POINT('Ctrl Pts',(6.51968959134574,-16.8292587962898,
1099.86534000164));
#150113=CARTESIAN_POINT('Ctrl Pts',(4.96022910773078,-17.4333970061901,
1098.37122235458));
#150114=CARTESIAN_POINT('Ctrl Pts',(3.31631129755346,-17.7406985030951,
1096.87710470753));
#150115=CARTESIAN_POINT('Ctrl Pts',(1.67239348737615,-18.048,1095.38298706047));
#150116=CARTESIAN_POINT('Ctrl Pts',(0.,-18.048,1093.88886941341));
#150117=CARTESIAN_POINT('Ctrl Pts',(-1.67239348737615,-18.048,1092.39475176635));
#150118=CARTESIAN_POINT('Ctrl Pts',(-3.31631129755346,-17.7406985030951,
1090.90063411929));
#150119=CARTESIAN_POINT('Ctrl Pts',(-4.96022910773077,-17.4333970061901,
1089.40651647223));
#150120=CARTESIAN_POINT('Ctrl Pts',(-6.51968959134574,-16.8292587962898,
1087.91239882517));
#150121=CARTESIAN_POINT('Ctrl Pts',(-8.07915007496071,-16.2251205863895,
1086.41828117811));
#150122=CARTESIAN_POINT('Ctrl Pts',(-9.50104767561052,-15.3447188656481,
1084.92416353106));
#150123=CARTESIAN_POINT('Ctrl Pts',(-10.9229452762603,-14.4643171449067,
1083.430045884));
#150124=CARTESIAN_POINT('Ctrl Pts',(-12.1588589765331,-13.3376329379985,
1081.93592823694));
#150125=CARTESIAN_POINT('Ctrl Pts',(-13.3947726768058,-12.2109487310903,
1080.44181058988));
#150126=CARTESIAN_POINT('Ctrl Pts',(-14.4026149179538,-10.8763499173728,
1078.94769294282));
#150127=CARTESIAN_POINT('Ctrl Pts',(-15.4104571591017,-9.54175110365538,
1077.45357529576));
#150128=CARTESIAN_POINT('Ctrl Pts',(-16.1559070823762,-8.04468584505497,
1075.9594576487));
#150129=CARTESIAN_POINT('Ctrl Pts',(-16.9013570056506,-6.54762058645456,
1074.46534000164));
#150130=CARTESIAN_POINT('Ctrl Pts',(-17.3590292079831,-4.93906964482095,
1072.97122235458));
#150131=CARTESIAN_POINT('Ctrl Pts',(-17.8167014103155,-3.33051870318735,
1071.47710470753));
#150132=CARTESIAN_POINT('Ctrl Pts',(-17.9710104137728,-1.66525935159368,
1069.98298706047));
#150133=CARTESIAN_POINT('Ctrl Pts',(-18.1253194172301,-1.10985572039171E-15,
1068.48886941341));
#150134=CARTESIAN_POINT('Ctrl Pts',(-17.9710104137728,1.66525935159367,
1066.99475176635));
#150135=CARTESIAN_POINT('Ctrl Pts',(-17.8167014103155,3.33051870318735,
1065.50063411929));
#150136=CARTESIAN_POINT('Ctrl Pts',(-17.3590292079831,4.93906964482096,
1064.00651647223));
#150137=CARTESIAN_POINT('Ctrl Pts',(-16.9013570056506,6.54762058645456,
1062.51239882517));
#150138=CARTESIAN_POINT('Ctrl Pts',(-16.1559070823762,8.04468584505497,
1061.01828117811));
#150139=CARTESIAN_POINT('Ctrl Pts',(-15.4104571591017,9.54175110365538,
1059.52416353105));
#150140=CARTESIAN_POINT('Ctrl Pts',(-14.4026149179538,10.8763499173728,
1058.030045884));
#150141=CARTESIAN_POINT('Ctrl Pts',(-13.3947726768058,12.2109487310903,
1056.53592823694));
#150142=CARTESIAN_POINT('Ctrl Pts',(-12.1588589765331,13.3376329379985,
1055.04181058988));
#150143=CARTESIAN_POINT('Ctrl Pts',(-10.9229452762603,14.4643171449067,
1053.54769294282));
#150144=CARTESIAN_POINT('Ctrl Pts',(-9.50104767561052,15.3447188656481,
1052.05357529576));
#150145=CARTESIAN_POINT('Ctrl Pts',(-8.07915007496071,16.2251205863895,
1050.5594576487));
#150146=CARTESIAN_POINT('Ctrl Pts',(-6.51968959134574,16.8292587962898,
1049.06534000164));
#150147=CARTESIAN_POINT('Ctrl Pts',(-4.96022910773078,17.4333970061901,
1047.57122235458));
#150148=CARTESIAN_POINT('Ctrl Pts',(-3.31631129755346,17.7406985030951,
1046.07710470753));
#150149=CARTESIAN_POINT('Ctrl Pts',(-1.67239348737615,18.048,1044.58298706047));
#150150=CARTESIAN_POINT('Ctrl Pts',(-2.21024254310115E-15,18.048,1043.08886941341));
#150151=CARTESIAN_POINT('Ctrl Pts',(1.67239348737616,18.048,1041.59475176635));
#150152=CARTESIAN_POINT('Ctrl Pts',(3.31631129755346,17.7406985030951,1040.10063411929));
#150153=CARTESIAN_POINT('Ctrl Pts',(4.96022910773077,17.4333970061901,1038.60651647223));
#150154=CARTESIAN_POINT('Ctrl Pts',(6.51968959134575,16.8292587962898,1037.11239882517));
#150155=CARTESIAN_POINT('Ctrl Pts',(8.07915007496071,16.2251205863895,1035.61828117811));
#150156=CARTESIAN_POINT('Ctrl Pts',(9.50104767561053,15.3447188656481,1034.12416353105));
#150157=CARTESIAN_POINT('Ctrl Pts',(10.9229452762603,14.4643171449067,1032.630045884));
#150158=CARTESIAN_POINT('Ctrl Pts',(12.1588589765331,13.3376329379985,1031.13592823694));
#150159=CARTESIAN_POINT('Ctrl Pts',(13.3947726768058,12.2109487310903,1029.64181058988));
#150160=CARTESIAN_POINT('Ctrl Pts',(14.4026149179538,10.8763499173728,1028.14769294282));
#150161=CARTESIAN_POINT('Ctrl Pts',(15.4104571591017,9.54175110365539,1026.65357529576));
#150162=CARTESIAN_POINT('Ctrl Pts',(16.1559070823762,8.04468584505496,1025.1594576487));
#150163=CARTESIAN_POINT('Ctrl Pts',(16.9013570056506,6.54762058645456,1023.66534000164));
#150164=CARTESIAN_POINT('Ctrl Pts',(17.3590292079831,4.93906964482096,1022.17122235458));
#150165=CARTESIAN_POINT('Ctrl Pts',(17.8167014103155,3.33051870318735,1020.67710470753));
#150166=CARTESIAN_POINT('Ctrl Pts',(17.9710104137728,1.66525935159367,1019.18298706047));
#150167=CARTESIAN_POINT('Ctrl Pts',(18.1253194172301,3.32956716117513E-15,
1017.68886941341));
#150168=CARTESIAN_POINT('Ctrl Pts',(17.9710104137728,-1.66525935159367,
1016.19475176635));
#150169=CARTESIAN_POINT('Ctrl Pts',(17.8167014103155,-3.33051870318736,
1014.70063411929));
#150170=CARTESIAN_POINT('Ctrl Pts',(17.3590292079831,-4.93906964482095,
1013.20651647223));
#150171=CARTESIAN_POINT('Ctrl Pts',(16.9013570056506,-6.54762058645456,
1011.71239882517));
#150172=CARTESIAN_POINT('Ctrl Pts',(16.1559070823762,-8.04468584505497,
1010.21828117811));
#150173=CARTESIAN_POINT('Ctrl Pts',(15.4104571591017,-9.54175110365538,
1008.72416353105));
#150174=CARTESIAN_POINT('Ctrl Pts',(14.4026149179538,-10.8763499173728,
1007.230045884));
#150175=CARTESIAN_POINT('Ctrl Pts',(13.3947726768058,-12.2109487310903,
1005.73592823694));
#150176=CARTESIAN_POINT('Ctrl Pts',(12.1588589765331,-13.3376329379985,
1004.24181058988));
#150177=CARTESIAN_POINT('Ctrl Pts',(10.9229452762603,-14.4643171449067,
1002.74769294282));
#150178=CARTESIAN_POINT('Ctrl Pts',(9.50104767561053,-15.3447188656481,
1001.25357529576));
#150179=CARTESIAN_POINT('Ctrl Pts',(8.07915007496071,-16.2251205863895,
999.759457648702));
#150180=CARTESIAN_POINT('Ctrl Pts',(6.51968959134574,-16.8292587962898,
998.265340001643));
#150181=CARTESIAN_POINT('Ctrl Pts',(4.96022910773078,-17.4333970061901,
996.771222354584));
#150182=CARTESIAN_POINT('Ctrl Pts',(3.31631129755346,-17.7406985030951,
995.277104707525));
#150183=CARTESIAN_POINT('Ctrl Pts',(1.67239348737615,-18.048,993.782987060467));
#150184=CARTESIAN_POINT('Ctrl Pts',(0.,-18.048,992.288869413408));
#150185=CARTESIAN_POINT('Ctrl Pts',(-1.67239348737615,-18.048,990.794751766349));
#150186=CARTESIAN_POINT('Ctrl Pts',(-3.31631129755346,-17.7406985030951,
989.30063411929));
#150187=CARTESIAN_POINT('Ctrl Pts',(-4.96022910773077,-17.4333970061901,
987.806516472231));
#150188=CARTESIAN_POINT('Ctrl Pts',(-6.51968959134574,-16.8292587962898,
986.312398825173));
#150189=CARTESIAN_POINT('Ctrl Pts',(-8.07915007496071,-16.2251205863895,
984.818281178114));
#150190=CARTESIAN_POINT('Ctrl Pts',(-9.50104767561052,-15.3447188656481,
983.324163531055));
#150191=CARTESIAN_POINT('Ctrl Pts',(-10.9229452762603,-14.4643171449067,
981.830045883996));
#150192=CARTESIAN_POINT('Ctrl Pts',(-12.1588589765331,-13.3376329379985,
980.335928236937));
#150193=CARTESIAN_POINT('Ctrl Pts',(-13.3947726768058,-12.2109487310903,
978.841810589878));
#150194=CARTESIAN_POINT('Ctrl Pts',(-14.4026149179538,-10.8763499173728,
977.34769294282));
#150195=CARTESIAN_POINT('Ctrl Pts',(-15.4104571591017,-9.54175110365538,
975.853575295761));
#150196=CARTESIAN_POINT('Ctrl Pts',(-16.1559070823762,-8.04468584505497,
974.359457648702));
#150197=CARTESIAN_POINT('Ctrl Pts',(-16.9013570056506,-6.54762058645456,
972.865340001643));
#150198=CARTESIAN_POINT('Ctrl Pts',(-17.3590292079831,-4.93906964482095,
971.371222354584));
#150199=CARTESIAN_POINT('Ctrl Pts',(-17.8167014103155,-3.33051870318735,
969.877104707525));
#150200=CARTESIAN_POINT('Ctrl Pts',(-17.9710104137728,-1.66525935159368,
968.382987060467));
#150201=CARTESIAN_POINT('Ctrl Pts',(-18.1253194172301,-1.10985572039171E-15,
966.888869413408));
#150202=CARTESIAN_POINT('Ctrl Pts',(-17.9710104137728,1.66525935159367,
965.394751766349));
#150203=CARTESIAN_POINT('Ctrl Pts',(-17.8167014103155,3.33051870318735,
963.90063411929));
#150204=CARTESIAN_POINT('Ctrl Pts',(-17.3590292079831,4.93906964482096,
962.406516472231));
#150205=CARTESIAN_POINT('Ctrl Pts',(-16.9013570056506,6.54762058645456,
960.912398825173));
#150206=CARTESIAN_POINT('Ctrl Pts',(-16.1559070823762,8.04468584505497,
959.418281178114));
#150207=CARTESIAN_POINT('Ctrl Pts',(-15.4104571591017,9.54175110365538,
957.924163531055));
#150208=CARTESIAN_POINT('Ctrl Pts',(-14.4026149179538,10.8763499173728,
956.430045883996));
#150209=CARTESIAN_POINT('Ctrl Pts',(-13.3947726768058,12.2109487310903,
954.935928236937));
#150210=CARTESIAN_POINT('Ctrl Pts',(-12.1588589765331,13.3376329379985,
953.441810589878));
#150211=CARTESIAN_POINT('Ctrl Pts',(-10.9229452762603,14.4643171449067,
951.94769294282));
#150212=CARTESIAN_POINT('Ctrl Pts',(-9.50104767561052,15.3447188656481,
950.453575295761));
#150213=CARTESIAN_POINT('Ctrl Pts',(-8.07915007496071,16.2251205863895,
948.959457648702));
#150214=CARTESIAN_POINT('Ctrl Pts',(-6.51968959134574,16.8292587962898,
947.465340001643));
#150215=CARTESIAN_POINT('Ctrl Pts',(-4.96022910773078,17.4333970061901,
945.971222354584));
#150216=CARTESIAN_POINT('Ctrl Pts',(-3.31631129755346,17.7406985030951,
944.477104707526));
#150217=CARTESIAN_POINT('Ctrl Pts',(-1.67239348737615,18.048,942.982987060467));
#150218=CARTESIAN_POINT('Ctrl Pts',(-2.21024254310115E-15,18.048,941.488869413408));
#150219=CARTESIAN_POINT('Ctrl Pts',(1.67239348737616,18.048,939.994751766349));
#150220=CARTESIAN_POINT('Ctrl Pts',(3.31631129755346,17.7406985030951,938.50063411929));
#150221=CARTESIAN_POINT('Ctrl Pts',(4.96022910773077,17.4333970061901,937.006516472231));
#150222=CARTESIAN_POINT('Ctrl Pts',(6.51968959134575,16.8292587962898,935.512398825173));
#150223=CARTESIAN_POINT('Ctrl Pts',(8.07915007496071,16.2251205863895,934.018281178114));
#150224=CARTESIAN_POINT('Ctrl Pts',(9.50104767561053,15.3447188656481,932.524163531055));
#150225=CARTESIAN_POINT('Ctrl Pts',(10.9229452762603,14.4643171449067,931.030045883996));
#150226=CARTESIAN_POINT('Ctrl Pts',(12.1588589765331,13.3376329379985,929.535928236937));
#150227=CARTESIAN_POINT('Ctrl Pts',(13.3947726768058,12.2109487310903,928.041810589879));
#150228=CARTESIAN_POINT('Ctrl Pts',(14.4026149179538,10.8763499173728,926.54769294282));
#150229=CARTESIAN_POINT('Ctrl Pts',(15.4104571591017,9.54175110365539,925.053575295761));
#150230=CARTESIAN_POINT('Ctrl Pts',(16.1559070823762,8.04468584505496,923.559457648702));
#150231=CARTESIAN_POINT('Ctrl Pts',(16.9013570056506,6.54762058645456,922.065340001643));
#150232=CARTESIAN_POINT('Ctrl Pts',(17.3590292079831,4.93906964482096,920.571222354584));
#150233=CARTESIAN_POINT('Ctrl Pts',(17.8167014103155,3.33051870318735,919.077104707525));
#150234=CARTESIAN_POINT('Ctrl Pts',(17.9710104137728,1.66525935159367,917.582987060467));
#150235=CARTESIAN_POINT('Ctrl Pts',(18.1253194172301,3.32956716117513E-15,
916.088869413408));
#150236=CARTESIAN_POINT('Ctrl Pts',(17.9710104137728,-1.66525935159367,
914.594751766349));
#150237=CARTESIAN_POINT('Ctrl Pts',(17.8167014103155,-3.33051870318736,
913.10063411929));
#150238=CARTESIAN_POINT('Ctrl Pts',(17.3590292079831,-4.93906964482095,
911.606516472231));
#150239=CARTESIAN_POINT('Ctrl Pts',(16.9013570056506,-6.54762058645456,
910.112398825173));
#150240=CARTESIAN_POINT('Ctrl Pts',(16.1559070823762,-8.04468584505497,
908.618281178114));
#150241=CARTESIAN_POINT('Ctrl Pts',(15.4104571591017,-9.54175110365538,
907.124163531055));
#150242=CARTESIAN_POINT('Ctrl Pts',(14.4026149179538,-10.8763499173728,
905.630045883996));
#150243=CARTESIAN_POINT('Ctrl Pts',(13.3947726768058,-12.2109487310903,
904.135928236937));
#150244=CARTESIAN_POINT('Ctrl Pts',(12.1588589765331,-13.3376329379985,
902.641810589878));
#150245=CARTESIAN_POINT('Ctrl Pts',(10.9229452762603,-14.4643171449067,
901.14769294282));
#150246=CARTESIAN_POINT('Ctrl Pts',(9.50104767561053,-15.3447188656481,
899.653575295761));
#150247=CARTESIAN_POINT('Ctrl Pts',(8.07915007496071,-16.2251205863895,
898.159457648702));
#150248=CARTESIAN_POINT('Ctrl Pts',(6.51968959134574,-16.8292587962898,
896.665340001643));
#150249=CARTESIAN_POINT('Ctrl Pts',(4.96022910773078,-17.4333970061901,
895.171222354584));
#150250=CARTESIAN_POINT('Ctrl Pts',(3.31631129755346,-17.7406985030951,
893.677104707526));
#150251=CARTESIAN_POINT('Ctrl Pts',(1.67239348737615,-18.048,892.182987060467));
#150252=CARTESIAN_POINT('Ctrl Pts',(0.,-18.048,890.688869413408));
#150253=CARTESIAN_POINT('Ctrl Pts',(-1.67239348737615,-18.048,889.194751766349));
#150254=CARTESIAN_POINT('Ctrl Pts',(-3.31631129755346,-17.7406985030951,
887.70063411929));
#150255=CARTESIAN_POINT('Ctrl Pts',(-4.96022910773077,-17.4333970061901,
886.206516472232));
#150256=CARTESIAN_POINT('Ctrl Pts',(-6.51968959134574,-16.8292587962898,
884.712398825172));
#150257=CARTESIAN_POINT('Ctrl Pts',(-8.07915007496071,-16.2251205863895,
883.218281178114));
#150258=CARTESIAN_POINT('Ctrl Pts',(-9.50104767561052,-15.3447188656481,
881.724163531055));
#150259=CARTESIAN_POINT('Ctrl Pts',(-10.9229452762603,-14.4643171449067,
880.230045883996));
#150260=CARTESIAN_POINT('Ctrl Pts',(-12.1588589765331,-13.3376329379985,
878.735928236937));
#150261=CARTESIAN_POINT('Ctrl Pts',(-13.3947726768058,-12.2109487310903,
877.241810589878));
#150262=CARTESIAN_POINT('Ctrl Pts',(-14.4026149179538,-10.8763499173728,
875.74769294282));
#150263=CARTESIAN_POINT('Ctrl Pts',(-15.4104571591017,-9.54175110365538,
874.253575295761));
#150264=CARTESIAN_POINT('Ctrl Pts',(-16.1559070823762,-8.04468584505497,
872.759457648702));
#150265=CARTESIAN_POINT('Ctrl Pts',(-16.9013570056506,-6.54762058645456,
871.265340001643));
#150266=CARTESIAN_POINT('Ctrl Pts',(-17.3590292079831,-4.93906964482095,
869.771222354584));
#150267=CARTESIAN_POINT('Ctrl Pts',(-17.8167014103155,-3.33051870318735,
868.277104707525));
#150268=CARTESIAN_POINT('Ctrl Pts',(-17.9710104137728,-1.66525935159368,
866.782987060467));
#150269=CARTESIAN_POINT('Ctrl Pts',(-18.1253194172301,-1.10985572039171E-15,
865.288869413408));
#150270=CARTESIAN_POINT('Ctrl Pts',(-17.9710104137728,1.66525935159367,
863.794751766349));
#150271=CARTESIAN_POINT('Ctrl Pts',(-17.8167014103155,3.33051870318735,
862.30063411929));
#150272=CARTESIAN_POINT('Ctrl Pts',(-17.3590292079831,4.93906964482096,
860.806516472231));
#150273=CARTESIAN_POINT('Ctrl Pts',(-16.9013570056506,6.54762058645456,
859.312398825173));
#150274=CARTESIAN_POINT('Ctrl Pts',(-16.1559070823762,8.04468584505497,
857.818281178114));
#150275=CARTESIAN_POINT('Ctrl Pts',(-15.4104571591017,9.54175110365538,
856.324163531055));
#150276=CARTESIAN_POINT('Ctrl Pts',(-14.4026149179538,10.8763499173728,
854.830045883996));
#150277=CARTESIAN_POINT('Ctrl Pts',(-13.3947726768058,12.2109487310903,
853.335928236937));
#150278=CARTESIAN_POINT('Ctrl Pts',(-12.1588589765331,13.3376329379985,
851.841810589878));
#150279=CARTESIAN_POINT('Ctrl Pts',(-10.9229452762603,14.4643171449067,
850.34769294282));
#150280=CARTESIAN_POINT('Ctrl Pts',(-9.50104767561052,15.3447188656481,
848.853575295761));
#150281=CARTESIAN_POINT('Ctrl Pts',(-8.07915007496071,16.2251205863895,
847.359457648702));
#150282=CARTESIAN_POINT('Ctrl Pts',(-6.51968959134574,16.8292587962898,
845.865340001643));
#150283=CARTESIAN_POINT('Ctrl Pts',(-4.96022910773078,17.4333970061901,
844.371222354584));
#150284=CARTESIAN_POINT('Ctrl Pts',(-3.31631129755346,17.7406985030951,
842.877104707525));
#150285=CARTESIAN_POINT('Ctrl Pts',(-1.67239348737615,18.048,841.382987060467));
#150286=CARTESIAN_POINT('Ctrl Pts',(-2.21024254310115E-15,18.048,839.888869413408));
#150287=CARTESIAN_POINT('Ctrl Pts',(1.67239348737616,18.048,838.394751766349));
#150288=CARTESIAN_POINT('Ctrl Pts',(3.31631129755346,17.7406985030951,836.90063411929));
#150289=CARTESIAN_POINT('Ctrl Pts',(4.96022910773077,17.4333970061901,835.406516472231));
#150290=CARTESIAN_POINT('Ctrl Pts',(6.51968959134575,16.8292587962898,833.912398825173));
#150291=CARTESIAN_POINT('Ctrl Pts',(8.07915007496071,16.2251205863895,832.418281178114));
#150292=CARTESIAN_POINT('Ctrl Pts',(9.50104767561053,15.3447188656481,830.924163531055));
#150293=CARTESIAN_POINT('Ctrl Pts',(10.9229452762603,14.4643171449067,829.430045883996));
#150294=CARTESIAN_POINT('Ctrl Pts',(12.1588589765331,13.3376329379985,827.935928236937));
#150295=CARTESIAN_POINT('Ctrl Pts',(13.3947726768058,12.2109487310903,826.441810589879));
#150296=CARTESIAN_POINT('Ctrl Pts',(14.4026149179538,10.8763499173728,824.94769294282));
#150297=CARTESIAN_POINT('Ctrl Pts',(15.4104571591017,9.54175110365539,823.453575295761));
#150298=CARTESIAN_POINT('Ctrl Pts',(16.1559070823762,8.04468584505496,821.959457648702));
#150299=CARTESIAN_POINT('Ctrl Pts',(16.9013570056506,6.54762058645456,820.465340001643));
#150300=CARTESIAN_POINT('Ctrl Pts',(17.3590292079831,4.93906964482096,818.971222354584));
#150301=CARTESIAN_POINT('Ctrl Pts',(17.8167014103155,3.33051870318735,817.477104707526));
#150302=CARTESIAN_POINT('Ctrl Pts',(17.9710104137728,1.66525935159367,815.982987060467));
#150303=CARTESIAN_POINT('Ctrl Pts',(18.1253194172301,3.32956716117513E-15,
814.488869413408));
#150304=CARTESIAN_POINT('Ctrl Pts',(17.9710104137728,-1.66525935159367,
812.994751766349));
#150305=CARTESIAN_POINT('Ctrl Pts',(17.8167014103155,-3.33051870318736,
811.50063411929));
#150306=CARTESIAN_POINT('Ctrl Pts',(17.3590292079831,-4.93906964482095,
810.006516472231));
#150307=CARTESIAN_POINT('Ctrl Pts',(16.9013570056506,-6.54762058645456,
808.512398825172));
#150308=CARTESIAN_POINT('Ctrl Pts',(16.1559070823762,-8.04468584505497,
807.018281178114));
#150309=CARTESIAN_POINT('Ctrl Pts',(15.4104571591017,-9.54175110365538,
805.524163531055));
#150310=CARTESIAN_POINT('Ctrl Pts',(14.4026149179538,-10.8763499173728,
804.030045883996));
#150311=CARTESIAN_POINT('Ctrl Pts',(13.3947726768058,-12.2109487310903,
802.535928236937));
#150312=CARTESIAN_POINT('Ctrl Pts',(12.1588589765331,-13.3376329379985,
801.041810589878));
#150313=CARTESIAN_POINT('Ctrl Pts',(10.9229452762603,-14.4643171449067,
799.54769294282));
#150314=CARTESIAN_POINT('Ctrl Pts',(9.50104767561053,-15.3447188656481,
798.053575295761));
#150315=CARTESIAN_POINT('Ctrl Pts',(8.07915007496071,-16.2251205863895,
796.559457648702));
#150316=CARTESIAN_POINT('Ctrl Pts',(6.51968959134574,-16.8292587962898,
795.065340001643));
#150317=CARTESIAN_POINT('Ctrl Pts',(4.96022910773078,-17.4333970061901,
793.571222354584));
#150318=CARTESIAN_POINT('Ctrl Pts',(3.31631129755346,-17.7406985030951,
792.077104707525));
#150319=CARTESIAN_POINT('Ctrl Pts',(1.67239348737615,-18.048,790.582987060467));
#150320=CARTESIAN_POINT('Ctrl Pts',(0.,-18.048,789.088869413408));
#150321=CARTESIAN_POINT('Ctrl Pts',(-1.67239348737615,-18.048,787.594751766349));
#150322=CARTESIAN_POINT('Ctrl Pts',(-3.31631129755346,-17.7406985030951,
786.10063411929));
#150323=CARTESIAN_POINT('Ctrl Pts',(-4.96022910773077,-17.4333970061901,
784.606516472231));
#150324=CARTESIAN_POINT('Ctrl Pts',(-6.51968959134574,-16.8292587962898,
783.112398825173));
#150325=CARTESIAN_POINT('Ctrl Pts',(-8.07915007496071,-16.2251205863895,
781.618281178114));
#150326=CARTESIAN_POINT('Ctrl Pts',(-9.50104767561052,-15.3447188656481,
780.124163531055));
#150327=CARTESIAN_POINT('Ctrl Pts',(-10.9229452762603,-14.4643171449067,
778.630045883996));
#150328=CARTESIAN_POINT('Ctrl Pts',(-12.1588589765331,-13.3376329379985,
777.135928236937));
#150329=CARTESIAN_POINT('Ctrl Pts',(-13.3947726768058,-12.2109487310903,
775.641810589879));
#150330=CARTESIAN_POINT('Ctrl Pts',(-14.4026149179538,-10.8763499173728,
774.14769294282));
#150331=CARTESIAN_POINT('Ctrl Pts',(-15.4104571591017,-9.54175110365538,
772.653575295761));
#150332=CARTESIAN_POINT('Ctrl Pts',(-16.1559070823762,-8.04468584505497,
771.159457648702));
#150333=CARTESIAN_POINT('Ctrl Pts',(-16.9013570056506,-6.54762058645456,
769.665340001643));
#150334=CARTESIAN_POINT('Ctrl Pts',(-17.3590292079831,-4.93906964482095,
768.171222354584));
#150335=CARTESIAN_POINT('Ctrl Pts',(-17.8167014103155,-3.33051870318735,
766.677104707526));
#150336=CARTESIAN_POINT('Ctrl Pts',(-17.9710104137728,-1.66525935159368,
765.182987060467));
#150337=CARTESIAN_POINT('Ctrl Pts',(-18.1253194172301,-1.10985572039171E-15,
763.688869413408));
#150338=CARTESIAN_POINT('Ctrl Pts',(-17.9710104137728,1.66525935159367,
762.194751766349));
#150339=CARTESIAN_POINT('Ctrl Pts',(-17.8167014103155,3.33051870318735,
760.70063411929));
#150340=CARTESIAN_POINT('Ctrl Pts',(-17.3590292079831,4.93906964482096,
759.206516472231));
#150341=CARTESIAN_POINT('Ctrl Pts',(-16.9013570056506,6.54762058645456,
757.712398825172));
#150342=CARTESIAN_POINT('Ctrl Pts',(-16.1559070823762,8.04468584505497,
756.218281178114));
#150343=CARTESIAN_POINT('Ctrl Pts',(-15.4104571591017,9.54175110365538,
754.724163531055));
#150344=CARTESIAN_POINT('Ctrl Pts',(-14.4026149179538,10.8763499173728,
753.230045883996));
#150345=CARTESIAN_POINT('Ctrl Pts',(-13.3947726768058,12.2109487310903,
751.735928236937));
#150346=CARTESIAN_POINT('Ctrl Pts',(-12.1588589765331,13.3376329379985,
750.241810589878));
#150347=CARTESIAN_POINT('Ctrl Pts',(-10.9229452762603,14.4643171449067,
748.74769294282));
#150348=CARTESIAN_POINT('Ctrl Pts',(-9.50104767561052,15.3447188656481,
747.253575295761));
#150349=CARTESIAN_POINT('Ctrl Pts',(-8.07915007496071,16.2251205863895,
745.759457648702));
#150350=CARTESIAN_POINT('Ctrl Pts',(-6.51968959134574,16.8292587962898,
744.265340001643));
#150351=CARTESIAN_POINT('Ctrl Pts',(-4.96022910773078,17.4333970061901,
742.771222354584));
#150352=CARTESIAN_POINT('Ctrl Pts',(-3.31631129755346,17.7406985030951,
741.277104707525));
#150353=CARTESIAN_POINT('Ctrl Pts',(-1.67239348737615,18.048,739.782987060467));
#150354=CARTESIAN_POINT('Ctrl Pts',(-2.21024254310115E-15,18.048,738.288869413408));
#150355=CARTESIAN_POINT('Ctrl Pts',(1.67239348737616,18.048,736.794751766349));
#150356=CARTESIAN_POINT('Ctrl Pts',(3.31631129755346,17.7406985030951,735.30063411929));
#150357=CARTESIAN_POINT('Ctrl Pts',(4.96022910773077,17.4333970061901,733.806516472231));
#150358=CARTESIAN_POINT('Ctrl Pts',(6.51968959134575,16.8292587962898,732.312398825173));
#150359=CARTESIAN_POINT('Ctrl Pts',(8.07915007496071,16.2251205863895,730.818281178114));
#150360=CARTESIAN_POINT('Ctrl Pts',(9.50104767561053,15.3447188656481,729.324163531055));
#150361=CARTESIAN_POINT('Ctrl Pts',(10.9229452762603,14.4643171449067,727.830045883996));
#150362=CARTESIAN_POINT('Ctrl Pts',(12.1588589765331,13.3376329379985,726.335928236937));
#150363=CARTESIAN_POINT('Ctrl Pts',(13.3947726768058,12.2109487310903,724.841810589879));
#150364=CARTESIAN_POINT('Ctrl Pts',(14.4026149179538,10.8763499173728,723.34769294282));
#150365=CARTESIAN_POINT('Ctrl Pts',(15.4104571591017,9.54175110365539,721.853575295761));
#150366=CARTESIAN_POINT('Ctrl Pts',(16.1559070823762,8.04468584505496,720.359457648702));
#150367=CARTESIAN_POINT('Ctrl Pts',(16.9013570056506,6.54762058645456,718.865340001643));
#150368=CARTESIAN_POINT('Ctrl Pts',(17.3590292079831,4.93906964482096,717.371222354584));
#150369=CARTESIAN_POINT('Ctrl Pts',(17.8167014103155,3.33051870318735,715.877104707526));
#150370=CARTESIAN_POINT('Ctrl Pts',(17.9710104137728,1.66525935159367,714.382987060467));
#150371=CARTESIAN_POINT('Ctrl Pts',(18.1253194172301,3.32956716117513E-15,
712.888869413408));
#150372=CARTESIAN_POINT('Ctrl Pts',(17.9710104137728,-1.66525935159367,
711.394751766349));
#150373=CARTESIAN_POINT('Ctrl Pts',(17.8167014103155,-3.33051870318736,
709.90063411929));
#150374=CARTESIAN_POINT('Ctrl Pts',(17.3590292079831,-4.93906964482095,
708.406516472231));
#150375=CARTESIAN_POINT('Ctrl Pts',(16.9013570056506,-6.54762058645456,
706.912398825173));
#150376=CARTESIAN_POINT('Ctrl Pts',(16.1559070823762,-8.04468584505497,
705.418281178114));
#150377=CARTESIAN_POINT('Ctrl Pts',(15.4104571591017,-9.54175110365538,
703.924163531055));
#150378=CARTESIAN_POINT('Ctrl Pts',(14.4026149179538,-10.8763499173728,
702.430045883996));
#150379=CARTESIAN_POINT('Ctrl Pts',(13.3947726768058,-12.2109487310903,
700.935928236937));
#150380=CARTESIAN_POINT('Ctrl Pts',(12.1588589765331,-13.3376329379985,
699.441810589878));
#150381=CARTESIAN_POINT('Ctrl Pts',(10.9229452762603,-14.4643171449067,
697.94769294282));
#150382=CARTESIAN_POINT('Ctrl Pts',(9.50104767561053,-15.3447188656481,
696.453575295761));
#150383=CARTESIAN_POINT('Ctrl Pts',(8.07915007496071,-16.2251205863895,
694.959457648702));
#150384=CARTESIAN_POINT('Ctrl Pts',(6.51968959134574,-16.8292587962898,
693.465340001643));
#150385=CARTESIAN_POINT('Ctrl Pts',(5.75661139047343,-17.1248768662138,
692.734235483133));
#150386=CARTESIAN_POINT('Ctrl Pts',(4.96991138555256,-17.3502243449402,
692.));
#150387=CARTESIAN_POINT('',(0.,-39.,1500.98568435754));
#150388=CARTESIAN_POINT('Ctrl Pts',(0.,-18.048,1504.84863058659));
#150389=CARTESIAN_POINT('Ctrl Pts',(-1.67239348737615,-18.048,1503.35451293953));
#150390=CARTESIAN_POINT('Ctrl Pts',(-3.31631129755346,-17.7406985030951,
1501.86039529247));
#150391=CARTESIAN_POINT('Ctrl Pts',(-4.96022910773077,-17.4333970061901,
1500.36627764542));
#150392=CARTESIAN_POINT('Ctrl Pts',(-6.51968959134574,-16.8292587962898,
1498.87215999836));
#150393=CARTESIAN_POINT('Ctrl Pts',(-8.07915007496071,-16.2251205863895,
1497.3780423513));
#150394=CARTESIAN_POINT('Ctrl Pts',(-9.50104767561052,-15.3447188656481,
1495.88392470424));
#150395=CARTESIAN_POINT('Ctrl Pts',(-10.9229452762603,-14.4643171449067,
1494.38980705718));
#150396=CARTESIAN_POINT('Ctrl Pts',(-12.1588589765331,-13.3376329379985,
1492.89568941012));
#150397=CARTESIAN_POINT('Ctrl Pts',(-13.3947726768058,-12.2109487310903,
1491.40157176306));
#150398=CARTESIAN_POINT('Ctrl Pts',(-14.4026149179538,-10.8763499173728,
1489.907454116));
#150399=CARTESIAN_POINT('Ctrl Pts',(-15.4104571591017,-9.54175110365538,
1488.41333646895));
#150400=CARTESIAN_POINT('Ctrl Pts',(-16.1559070823762,-8.04468584505497,
1486.91921882189));
#150401=CARTESIAN_POINT('Ctrl Pts',(-16.9013570056506,-6.54762058645456,
1485.42510117483));
#150402=CARTESIAN_POINT('Ctrl Pts',(-17.3590292079831,-4.93906964482095,
1483.93098352777));
#150403=CARTESIAN_POINT('Ctrl Pts',(-17.8167014103155,-3.33051870318735,
1482.43686588071));
#150404=CARTESIAN_POINT('Ctrl Pts',(-17.9710104137728,-1.66525935159368,
1480.94274823365));
#150405=CARTESIAN_POINT('Ctrl Pts',(-18.1253194172301,-1.10985572039171E-15,
1479.44863058659));
#150406=CARTESIAN_POINT('Ctrl Pts',(-17.9710104137728,1.66525935159367,
1477.95451293953));
#150407=CARTESIAN_POINT('Ctrl Pts',(-17.8167014103155,3.33051870318735,
1476.46039529247));
#150408=CARTESIAN_POINT('Ctrl Pts',(-17.3590292079831,4.93906964482096,
1474.96627764542));
#150409=CARTESIAN_POINT('Ctrl Pts',(-16.9013570056506,6.54762058645456,
1473.47215999836));
#150410=CARTESIAN_POINT('Ctrl Pts',(-16.1559070823762,8.04468584505497,
1471.9780423513));
#150411=CARTESIAN_POINT('Ctrl Pts',(-15.4104571591017,9.54175110365538,
1470.48392470424));
#150412=CARTESIAN_POINT('Ctrl Pts',(-14.4026149179538,10.8763499173728,
1468.98980705718));
#150413=CARTESIAN_POINT('Ctrl Pts',(-13.3947726768058,12.2109487310903,
1467.49568941012));
#150414=CARTESIAN_POINT('Ctrl Pts',(-12.1588589765331,13.3376329379985,
1466.00157176306));
#150415=CARTESIAN_POINT('Ctrl Pts',(-10.9229452762603,14.4643171449067,
1464.507454116));
#150416=CARTESIAN_POINT('Ctrl Pts',(-9.50104767561052,15.3447188656481,
1463.01333646895));
#150417=CARTESIAN_POINT('Ctrl Pts',(-8.07915007496071,16.2251205863895,
1461.51921882189));
#150418=CARTESIAN_POINT('Ctrl Pts',(-6.51968959134574,16.8292587962898,
1460.02510117483));
#150419=CARTESIAN_POINT('Ctrl Pts',(-4.96022910773078,17.4333970061901,
1458.53098352777));
#150420=CARTESIAN_POINT('Ctrl Pts',(-3.31631129755346,17.7406985030951,
1457.03686588071));
#150421=CARTESIAN_POINT('Ctrl Pts',(-1.67239348737615,18.048,1455.54274823365));
#150422=CARTESIAN_POINT('Ctrl Pts',(-2.21024254310115E-15,18.048,1454.04863058659));
#150423=CARTESIAN_POINT('Ctrl Pts',(1.67239348737616,18.048,1452.55451293953));
#150424=CARTESIAN_POINT('Ctrl Pts',(3.31631129755346,17.7406985030951,1451.06039529247));
#150425=CARTESIAN_POINT('Ctrl Pts',(4.96022910773077,17.4333970061901,1449.56627764542));
#150426=CARTESIAN_POINT('Ctrl Pts',(6.51968959134575,16.8292587962898,1448.07215999836));
#150427=CARTESIAN_POINT('Ctrl Pts',(8.07915007496071,16.2251205863895,1446.5780423513));
#150428=CARTESIAN_POINT('Ctrl Pts',(9.50104767561053,15.3447188656481,1445.08392470424));
#150429=CARTESIAN_POINT('Ctrl Pts',(10.9229452762603,14.4643171449067,1443.58980705718));
#150430=CARTESIAN_POINT('Ctrl Pts',(12.1588589765331,13.3376329379985,1442.09568941012));
#150431=CARTESIAN_POINT('Ctrl Pts',(13.3947726768058,12.2109487310903,1440.60157176306));
#150432=CARTESIAN_POINT('Ctrl Pts',(14.4026149179538,10.8763499173728,1439.107454116));
#150433=CARTESIAN_POINT('Ctrl Pts',(15.4104571591017,9.54175110365538,1437.61333646895));
#150434=CARTESIAN_POINT('Ctrl Pts',(16.1559070823762,8.04468584505496,1436.11921882189));
#150435=CARTESIAN_POINT('Ctrl Pts',(16.9013570056506,6.54762058645456,1434.62510117483));
#150436=CARTESIAN_POINT('Ctrl Pts',(17.3590292079831,4.93906964482096,1433.13098352777));
#150437=CARTESIAN_POINT('Ctrl Pts',(17.8167014103155,3.33051870318735,1431.63686588071));
#150438=CARTESIAN_POINT('Ctrl Pts',(17.9710104137728,1.66525935159367,1430.14274823365));
#150439=CARTESIAN_POINT('Ctrl Pts',(18.1253194172301,3.32956716117513E-15,
1428.64863058659));
#150440=CARTESIAN_POINT('Ctrl Pts',(17.9710104137728,-1.66525935159367,
1427.15451293953));
#150441=CARTESIAN_POINT('Ctrl Pts',(17.8167014103155,-3.33051870318736,
1425.66039529247));
#150442=CARTESIAN_POINT('Ctrl Pts',(17.3590292079831,-4.93906964482095,
1424.16627764542));
#150443=CARTESIAN_POINT('Ctrl Pts',(16.9013570056506,-6.54762058645456,
1422.67215999836));
#150444=CARTESIAN_POINT('Ctrl Pts',(16.1559070823762,-8.04468584505497,
1421.1780423513));
#150445=CARTESIAN_POINT('Ctrl Pts',(15.4104571591017,-9.54175110365538,
1419.68392470424));
#150446=CARTESIAN_POINT('Ctrl Pts',(14.4026149179538,-10.8763499173728,
1418.18980705718));
#150447=CARTESIAN_POINT('Ctrl Pts',(13.3947726768058,-12.2109487310903,
1416.69568941012));
#150448=CARTESIAN_POINT('Ctrl Pts',(12.1588589765331,-13.3376329379985,
1415.20157176306));
#150449=CARTESIAN_POINT('Ctrl Pts',(10.9229452762603,-14.4643171449067,
1413.707454116));
#150450=CARTESIAN_POINT('Ctrl Pts',(9.50104767561053,-15.3447188656481,
1412.21333646895));
#150451=CARTESIAN_POINT('Ctrl Pts',(8.07915007496071,-16.2251205863895,
1410.71921882189));
#150452=CARTESIAN_POINT('Ctrl Pts',(6.51968959134574,-16.8292587962898,
1409.22510117483));
#150453=CARTESIAN_POINT('Ctrl Pts',(4.96022910773078,-17.4333970061901,
1407.73098352777));
#150454=CARTESIAN_POINT('Ctrl Pts',(3.31631129755346,-17.7406985030951,
1406.23686588071));
#150455=CARTESIAN_POINT('Ctrl Pts',(1.67239348737615,-18.048,1404.74274823365));
#150456=CARTESIAN_POINT('Ctrl Pts',(0.,-18.048,1403.24863058659));
#150457=CARTESIAN_POINT('Ctrl Pts',(-1.67239348737615,-18.048,1401.75451293953));
#150458=CARTESIAN_POINT('Ctrl Pts',(-3.31631129755346,-17.7406985030951,
1400.26039529247));
#150459=CARTESIAN_POINT('Ctrl Pts',(-4.96022910773077,-17.4333970061901,
1398.76627764542));
#150460=CARTESIAN_POINT('Ctrl Pts',(-6.51968959134574,-16.8292587962898,
1397.27215999836));
#150461=CARTESIAN_POINT('Ctrl Pts',(-8.07915007496071,-16.2251205863895,
1395.7780423513));
#150462=CARTESIAN_POINT('Ctrl Pts',(-9.50104767561052,-15.3447188656481,
1394.28392470424));
#150463=CARTESIAN_POINT('Ctrl Pts',(-10.9229452762603,-14.4643171449067,
1392.78980705718));
#150464=CARTESIAN_POINT('Ctrl Pts',(-12.1588589765331,-13.3376329379985,
1391.29568941012));
#150465=CARTESIAN_POINT('Ctrl Pts',(-13.3947726768058,-12.2109487310903,
1389.80157176306));
#150466=CARTESIAN_POINT('Ctrl Pts',(-14.4026149179538,-10.8763499173728,
1388.307454116));
#150467=CARTESIAN_POINT('Ctrl Pts',(-15.4104571591017,-9.54175110365538,
1386.81333646895));
#150468=CARTESIAN_POINT('Ctrl Pts',(-16.1559070823762,-8.04468584505497,
1385.31921882189));
#150469=CARTESIAN_POINT('Ctrl Pts',(-16.9013570056506,-6.54762058645456,
1383.82510117483));
#150470=CARTESIAN_POINT('Ctrl Pts',(-17.3590292079831,-4.93906964482095,
1382.33098352777));
#150471=CARTESIAN_POINT('Ctrl Pts',(-17.8167014103155,-3.33051870318735,
1380.83686588071));
#150472=CARTESIAN_POINT('Ctrl Pts',(-17.9710104137728,-1.66525935159368,
1379.34274823365));
#150473=CARTESIAN_POINT('Ctrl Pts',(-18.1253194172301,-1.10985572039171E-15,
1377.84863058659));
#150474=CARTESIAN_POINT('Ctrl Pts',(-17.9710104137728,1.66525935159367,
1376.35451293953));
#150475=CARTESIAN_POINT('Ctrl Pts',(-17.8167014103155,3.33051870318735,
1374.86039529247));
#150476=CARTESIAN_POINT('Ctrl Pts',(-17.3590292079831,4.93906964482096,
1373.36627764542));
#150477=CARTESIAN_POINT('Ctrl Pts',(-16.9013570056506,6.54762058645456,
1371.87215999836));
#150478=CARTESIAN_POINT('Ctrl Pts',(-16.1559070823762,8.04468584505497,
1370.3780423513));
#150479=CARTESIAN_POINT('Ctrl Pts',(-15.4104571591017,9.54175110365538,
1368.88392470424));
#150480=CARTESIAN_POINT('Ctrl Pts',(-14.4026149179538,10.8763499173728,
1367.38980705718));
#150481=CARTESIAN_POINT('Ctrl Pts',(-13.3947726768058,12.2109487310903,
1365.89568941012));
#150482=CARTESIAN_POINT('Ctrl Pts',(-12.1588589765331,13.3376329379985,
1364.40157176306));
#150483=CARTESIAN_POINT('Ctrl Pts',(-10.9229452762603,14.4643171449067,
1362.907454116));
#150484=CARTESIAN_POINT('Ctrl Pts',(-9.50104767561052,15.3447188656481,
1361.41333646895));
#150485=CARTESIAN_POINT('Ctrl Pts',(-8.07915007496071,16.2251205863895,
1359.91921882189));
#150486=CARTESIAN_POINT('Ctrl Pts',(-6.51968959134574,16.8292587962898,
1358.42510117483));
#150487=CARTESIAN_POINT('Ctrl Pts',(-4.96022910773078,17.4333970061901,
1356.93098352777));
#150488=CARTESIAN_POINT('Ctrl Pts',(-3.31631129755346,17.7406985030951,
1355.43686588071));
#150489=CARTESIAN_POINT('Ctrl Pts',(-1.67239348737615,18.048,1353.94274823365));
#150490=CARTESIAN_POINT('Ctrl Pts',(-2.21024254310115E-15,18.048,1352.44863058659));
#150491=CARTESIAN_POINT('Ctrl Pts',(1.67239348737616,18.048,1350.95451293953));
#150492=CARTESIAN_POINT('Ctrl Pts',(3.31631129755346,17.7406985030951,1349.46039529247));
#150493=CARTESIAN_POINT('Ctrl Pts',(4.96022910773077,17.4333970061901,1347.96627764542));
#150494=CARTESIAN_POINT('Ctrl Pts',(6.51968959134575,16.8292587962898,1346.47215999836));
#150495=CARTESIAN_POINT('Ctrl Pts',(8.07915007496071,16.2251205863895,1344.9780423513));
#150496=CARTESIAN_POINT('Ctrl Pts',(9.50104767561053,15.3447188656481,1343.48392470424));
#150497=CARTESIAN_POINT('Ctrl Pts',(10.9229452762603,14.4643171449067,1341.98980705718));
#150498=CARTESIAN_POINT('Ctrl Pts',(12.1588589765331,13.3376329379985,1340.49568941012));
#150499=CARTESIAN_POINT('Ctrl Pts',(13.3947726768058,12.2109487310903,1339.00157176306));
#150500=CARTESIAN_POINT('Ctrl Pts',(14.4026149179538,10.8763499173728,1337.507454116));
#150501=CARTESIAN_POINT('Ctrl Pts',(15.4104571591017,9.54175110365538,1336.01333646895));
#150502=CARTESIAN_POINT('Ctrl Pts',(16.1559070823762,8.04468584505496,1334.51921882189));
#150503=CARTESIAN_POINT('Ctrl Pts',(16.9013570056506,6.54762058645456,1333.02510117483));
#150504=CARTESIAN_POINT('Ctrl Pts',(17.3590292079831,4.93906964482096,1331.53098352777));
#150505=CARTESIAN_POINT('Ctrl Pts',(17.8167014103155,3.33051870318735,1330.03686588071));
#150506=CARTESIAN_POINT('Ctrl Pts',(17.9710104137728,1.66525935159367,1328.54274823365));
#150507=CARTESIAN_POINT('Ctrl Pts',(18.1253194172301,3.32956716117513E-15,
1327.04863058659));
#150508=CARTESIAN_POINT('Ctrl Pts',(17.9710104137728,-1.66525935159367,
1325.55451293953));
#150509=CARTESIAN_POINT('Ctrl Pts',(17.8167014103155,-3.33051870318736,
1324.06039529247));
#150510=CARTESIAN_POINT('Ctrl Pts',(17.3590292079831,-4.93906964482095,
1322.56627764542));
#150511=CARTESIAN_POINT('Ctrl Pts',(16.9013570056506,-6.54762058645456,
1321.07215999836));
#150512=CARTESIAN_POINT('Ctrl Pts',(16.1559070823762,-8.04468584505497,
1319.5780423513));
#150513=CARTESIAN_POINT('Ctrl Pts',(15.4104571591017,-9.54175110365538,
1318.08392470424));
#150514=CARTESIAN_POINT('Ctrl Pts',(14.4026149179538,-10.8763499173728,
1316.58980705718));
#150515=CARTESIAN_POINT('Ctrl Pts',(13.3947726768058,-12.2109487310903,
1315.09568941012));
#150516=CARTESIAN_POINT('Ctrl Pts',(12.1588589765331,-13.3376329379985,
1313.60157176306));
#150517=CARTESIAN_POINT('Ctrl Pts',(10.9229452762603,-14.4643171449067,
1312.107454116));
#150518=CARTESIAN_POINT('Ctrl Pts',(9.50104767561053,-15.3447188656481,
1310.61333646895));
#150519=CARTESIAN_POINT('Ctrl Pts',(8.07915007496071,-16.2251205863895,
1309.11921882189));
#150520=CARTESIAN_POINT('Ctrl Pts',(6.51968959134574,-16.8292587962898,
1307.62510117483));
#150521=CARTESIAN_POINT('Ctrl Pts',(4.96022910773078,-17.4333970061901,
1306.13098352777));
#150522=CARTESIAN_POINT('Ctrl Pts',(3.31631129755346,-17.7406985030951,
1304.63686588071));
#150523=CARTESIAN_POINT('Ctrl Pts',(1.67239348737615,-18.048,1303.14274823365));
#150524=CARTESIAN_POINT('Ctrl Pts',(0.,-18.048,1301.64863058659));
#150525=CARTESIAN_POINT('Ctrl Pts',(-1.67239348737615,-18.048,1300.15451293953));
#150526=CARTESIAN_POINT('Ctrl Pts',(-3.31631129755346,-17.7406985030951,
1298.66039529247));
#150527=CARTESIAN_POINT('Ctrl Pts',(-4.96022910773077,-17.4333970061901,
1297.16627764542));
#150528=CARTESIAN_POINT('Ctrl Pts',(-6.51968959134574,-16.8292587962898,
1295.67215999836));
#150529=CARTESIAN_POINT('Ctrl Pts',(-8.07915007496071,-16.2251205863895,
1294.1780423513));
#150530=CARTESIAN_POINT('Ctrl Pts',(-9.50104767561052,-15.3447188656481,
1292.68392470424));
#150531=CARTESIAN_POINT('Ctrl Pts',(-10.9229452762603,-14.4643171449067,
1291.18980705718));
#150532=CARTESIAN_POINT('Ctrl Pts',(-12.1588589765331,-13.3376329379985,
1289.69568941012));
#150533=CARTESIAN_POINT('Ctrl Pts',(-13.3947726768058,-12.2109487310903,
1288.20157176306));
#150534=CARTESIAN_POINT('Ctrl Pts',(-14.4026149179538,-10.8763499173728,
1286.707454116));
#150535=CARTESIAN_POINT('Ctrl Pts',(-15.4104571591017,-9.54175110365538,
1285.21333646895));
#150536=CARTESIAN_POINT('Ctrl Pts',(-16.1559070823762,-8.04468584505497,
1283.71921882189));
#150537=CARTESIAN_POINT('Ctrl Pts',(-16.9013570056506,-6.54762058645456,
1282.22510117483));
#150538=CARTESIAN_POINT('Ctrl Pts',(-17.3590292079831,-4.93906964482095,
1280.73098352777));
#150539=CARTESIAN_POINT('Ctrl Pts',(-17.8167014103155,-3.33051870318735,
1279.23686588071));
#150540=CARTESIAN_POINT('Ctrl Pts',(-17.9710104137728,-1.66525935159368,
1277.74274823365));
#150541=CARTESIAN_POINT('Ctrl Pts',(-18.1253194172301,-1.10985572039171E-15,
1276.24863058659));
#150542=CARTESIAN_POINT('Ctrl Pts',(-17.9710104137728,1.66525935159367,
1274.75451293953));
#150543=CARTESIAN_POINT('Ctrl Pts',(-17.8167014103155,3.33051870318735,
1273.26039529247));
#150544=CARTESIAN_POINT('Ctrl Pts',(-17.3590292079831,4.93906964482096,
1271.76627764542));
#150545=CARTESIAN_POINT('Ctrl Pts',(-16.9013570056506,6.54762058645456,
1270.27215999836));
#150546=CARTESIAN_POINT('Ctrl Pts',(-16.1559070823762,8.04468584505497,
1268.7780423513));
#150547=CARTESIAN_POINT('Ctrl Pts',(-15.4104571591017,9.54175110365538,
1267.28392470424));
#150548=CARTESIAN_POINT('Ctrl Pts',(-14.4026149179538,10.8763499173728,
1265.78980705718));
#150549=CARTESIAN_POINT('Ctrl Pts',(-13.3947726768058,12.2109487310903,
1264.29568941012));
#150550=CARTESIAN_POINT('Ctrl Pts',(-12.1588589765331,13.3376329379985,
1262.80157176306));
#150551=CARTESIAN_POINT('Ctrl Pts',(-10.9229452762603,14.4643171449067,
1261.307454116));
#150552=CARTESIAN_POINT('Ctrl Pts',(-9.50104767561052,15.3447188656481,
1259.81333646895));
#150553=CARTESIAN_POINT('Ctrl Pts',(-8.07915007496071,16.2251205863895,
1258.31921882189));
#150554=CARTESIAN_POINT('Ctrl Pts',(-6.51968959134574,16.8292587962898,
1256.82510117483));
#150555=CARTESIAN_POINT('Ctrl Pts',(-4.96022910773078,17.4333970061901,
1255.33098352777));
#150556=CARTESIAN_POINT('Ctrl Pts',(-3.31631129755346,17.7406985030951,
1253.83686588071));
#150557=CARTESIAN_POINT('Ctrl Pts',(-1.67239348737615,18.048,1252.34274823365));
#150558=CARTESIAN_POINT('Ctrl Pts',(-2.21024254310115E-15,18.048,1250.84863058659));
#150559=CARTESIAN_POINT('Ctrl Pts',(1.67239348737616,18.048,1249.35451293953));
#150560=CARTESIAN_POINT('Ctrl Pts',(3.31631129755346,17.7406985030951,1247.86039529247));
#150561=CARTESIAN_POINT('Ctrl Pts',(4.96022910773077,17.4333970061901,1246.36627764542));
#150562=CARTESIAN_POINT('Ctrl Pts',(6.51968959134575,16.8292587962898,1244.87215999836));
#150563=CARTESIAN_POINT('Ctrl Pts',(8.07915007496071,16.2251205863895,1243.3780423513));
#150564=CARTESIAN_POINT('Ctrl Pts',(9.50104767561053,15.3447188656481,1241.88392470424));
#150565=CARTESIAN_POINT('Ctrl Pts',(10.9229452762603,14.4643171449067,1240.38980705718));
#150566=CARTESIAN_POINT('Ctrl Pts',(12.1588589765331,13.3376329379985,1238.89568941012));
#150567=CARTESIAN_POINT('Ctrl Pts',(13.3947726768058,12.2109487310903,1237.40157176306));
#150568=CARTESIAN_POINT('Ctrl Pts',(14.4026149179538,10.8763499173728,1235.907454116));
#150569=CARTESIAN_POINT('Ctrl Pts',(15.4104571591017,9.54175110365538,1234.41333646895));
#150570=CARTESIAN_POINT('Ctrl Pts',(16.1559070823762,8.04468584505496,1232.91921882189));
#150571=CARTESIAN_POINT('Ctrl Pts',(16.9013570056506,6.54762058645456,1231.42510117483));
#150572=CARTESIAN_POINT('Ctrl Pts',(17.3590292079831,4.93906964482096,1229.93098352777));
#150573=CARTESIAN_POINT('Ctrl Pts',(17.8167014103155,3.33051870318735,1228.43686588071));
#150574=CARTESIAN_POINT('Ctrl Pts',(17.9710104137728,1.66525935159367,1226.94274823365));
#150575=CARTESIAN_POINT('Ctrl Pts',(18.1253194172301,3.32956716117513E-15,
1225.44863058659));
#150576=CARTESIAN_POINT('Ctrl Pts',(17.9710104137728,-1.66525935159367,
1223.95451293953));
#150577=CARTESIAN_POINT('Ctrl Pts',(17.8167014103155,-3.33051870318736,
1222.46039529247));
#150578=CARTESIAN_POINT('Ctrl Pts',(17.3590292079831,-4.93906964482095,
1220.96627764542));
#150579=CARTESIAN_POINT('Ctrl Pts',(16.9013570056506,-6.54762058645456,
1219.47215999836));
#150580=CARTESIAN_POINT('Ctrl Pts',(16.1559070823762,-8.04468584505497,
1217.9780423513));
#150581=CARTESIAN_POINT('Ctrl Pts',(15.4104571591017,-9.54175110365538,
1216.48392470424));
#150582=CARTESIAN_POINT('Ctrl Pts',(14.4026149179538,-10.8763499173728,
1214.98980705718));
#150583=CARTESIAN_POINT('Ctrl Pts',(13.3947726768058,-12.2109487310903,
1213.49568941012));
#150584=CARTESIAN_POINT('Ctrl Pts',(12.1588589765331,-13.3376329379985,
1212.00157176306));
#150585=CARTESIAN_POINT('Ctrl Pts',(10.9229452762603,-14.4643171449067,
1210.507454116));
#150586=CARTESIAN_POINT('Ctrl Pts',(9.50104767561053,-15.3447188656481,
1209.01333646895));
#150587=CARTESIAN_POINT('Ctrl Pts',(8.07915007496071,-16.2251205863895,
1207.51921882189));
#150588=CARTESIAN_POINT('Ctrl Pts',(6.51968959134574,-16.8292587962898,
1206.02510117483));
#150589=CARTESIAN_POINT('Ctrl Pts',(4.96022910773078,-17.4333970061901,
1204.53098352777));
#150590=CARTESIAN_POINT('Ctrl Pts',(3.31631129755346,-17.7406985030951,
1203.03686588071));
#150591=CARTESIAN_POINT('Ctrl Pts',(1.67239348737615,-18.048,1201.54274823365));
#150592=CARTESIAN_POINT('Ctrl Pts',(0.,-18.048,1200.04863058659));
#150593=CARTESIAN_POINT('Ctrl Pts',(-1.67239348737615,-18.048,1198.55451293953));
#150594=CARTESIAN_POINT('Ctrl Pts',(-3.31631129755346,-17.7406985030951,
1197.06039529247));
#150595=CARTESIAN_POINT('Ctrl Pts',(-4.96022910773077,-17.4333970061901,
1195.56627764542));
#150596=CARTESIAN_POINT('Ctrl Pts',(-6.51968959134574,-16.8292587962898,
1194.07215999836));
#150597=CARTESIAN_POINT('Ctrl Pts',(-8.07915007496071,-16.2251205863895,
1192.5780423513));
#150598=CARTESIAN_POINT('Ctrl Pts',(-9.50104767561052,-15.3447188656481,
1191.08392470424));
#150599=CARTESIAN_POINT('Ctrl Pts',(-10.9229452762603,-14.4643171449067,
1189.58980705718));
#150600=CARTESIAN_POINT('Ctrl Pts',(-12.1588589765331,-13.3376329379985,
1188.09568941012));
#150601=CARTESIAN_POINT('Ctrl Pts',(-13.3947726768058,-12.2109487310903,
1186.60157176306));
#150602=CARTESIAN_POINT('Ctrl Pts',(-14.4026149179538,-10.8763499173728,
1185.107454116));
#150603=CARTESIAN_POINT('Ctrl Pts',(-15.4104571591017,-9.54175110365538,
1183.61333646895));
#150604=CARTESIAN_POINT('Ctrl Pts',(-16.1559070823762,-8.04468584505497,
1182.11921882189));
#150605=CARTESIAN_POINT('Ctrl Pts',(-16.9013570056506,-6.54762058645456,
1180.62510117483));
#150606=CARTESIAN_POINT('Ctrl Pts',(-17.3590292079831,-4.93906964482095,
1179.13098352777));
#150607=CARTESIAN_POINT('Ctrl Pts',(-17.8167014103155,-3.33051870318735,
1177.63686588071));
#150608=CARTESIAN_POINT('Ctrl Pts',(-17.9710104137728,-1.66525935159368,
1176.14274823365));
#150609=CARTESIAN_POINT('Ctrl Pts',(-18.1253194172301,-1.10985572039171E-15,
1174.64863058659));
#150610=CARTESIAN_POINT('Ctrl Pts',(-17.9710104137728,1.66525935159367,
1173.15451293953));
#150611=CARTESIAN_POINT('Ctrl Pts',(-17.8167014103155,3.33051870318735,
1171.66039529247));
#150612=CARTESIAN_POINT('Ctrl Pts',(-17.3590292079831,4.93906964482096,
1170.16627764542));
#150613=CARTESIAN_POINT('Ctrl Pts',(-16.9013570056506,6.54762058645456,
1168.67215999836));
#150614=CARTESIAN_POINT('Ctrl Pts',(-16.1559070823762,8.04468584505497,
1167.1780423513));
#150615=CARTESIAN_POINT('Ctrl Pts',(-15.4104571591017,9.54175110365538,
1165.68392470424));
#150616=CARTESIAN_POINT('Ctrl Pts',(-14.4026149179538,10.8763499173728,
1164.18980705718));
#150617=CARTESIAN_POINT('Ctrl Pts',(-13.3947726768058,12.2109487310903,
1162.69568941012));
#150618=CARTESIAN_POINT('Ctrl Pts',(-12.1588589765331,13.3376329379985,
1161.20157176306));
#150619=CARTESIAN_POINT('Ctrl Pts',(-10.9229452762603,14.4643171449067,
1159.707454116));
#150620=CARTESIAN_POINT('Ctrl Pts',(-9.50104767561052,15.3447188656481,
1158.21333646895));
#150621=CARTESIAN_POINT('Ctrl Pts',(-8.07915007496071,16.2251205863895,
1156.71921882189));
#150622=CARTESIAN_POINT('Ctrl Pts',(-6.51968959134574,16.8292587962898,
1155.22510117483));
#150623=CARTESIAN_POINT('Ctrl Pts',(-4.96022910773078,17.4333970061901,
1153.73098352777));
#150624=CARTESIAN_POINT('Ctrl Pts',(-3.31631129755346,17.7406985030951,
1152.23686588071));
#150625=CARTESIAN_POINT('Ctrl Pts',(-1.67239348737615,18.048,1150.74274823365));
#150626=CARTESIAN_POINT('Ctrl Pts',(-2.21024254310115E-15,18.048,1149.24863058659));
#150627=CARTESIAN_POINT('Ctrl Pts',(1.67239348737616,18.048,1147.75451293953));
#150628=CARTESIAN_POINT('Ctrl Pts',(3.31631129755346,17.7406985030951,1146.26039529247));
#150629=CARTESIAN_POINT('Ctrl Pts',(4.96022910773077,17.4333970061901,1144.76627764542));
#150630=CARTESIAN_POINT('Ctrl Pts',(6.51968959134575,16.8292587962898,1143.27215999836));
#150631=CARTESIAN_POINT('Ctrl Pts',(8.07915007496071,16.2251205863895,1141.7780423513));
#150632=CARTESIAN_POINT('Ctrl Pts',(9.50104767561053,15.3447188656481,1140.28392470424));
#150633=CARTESIAN_POINT('Ctrl Pts',(10.9229452762603,14.4643171449067,1138.78980705718));
#150634=CARTESIAN_POINT('Ctrl Pts',(12.1588589765331,13.3376329379985,1137.29568941012));
#150635=CARTESIAN_POINT('Ctrl Pts',(13.3947726768058,12.2109487310903,1135.80157176306));
#150636=CARTESIAN_POINT('Ctrl Pts',(14.4026149179538,10.8763499173728,1134.307454116));
#150637=CARTESIAN_POINT('Ctrl Pts',(15.4104571591017,9.54175110365538,1132.81333646895));
#150638=CARTESIAN_POINT('Ctrl Pts',(16.1559070823762,8.04468584505496,1131.31921882189));
#150639=CARTESIAN_POINT('Ctrl Pts',(16.9013570056506,6.54762058645456,1129.82510117483));
#150640=CARTESIAN_POINT('Ctrl Pts',(17.3590292079831,4.93906964482096,1128.33098352777));
#150641=CARTESIAN_POINT('Ctrl Pts',(17.8167014103155,3.33051870318735,1126.83686588071));
#150642=CARTESIAN_POINT('Ctrl Pts',(17.9710104137728,1.66525935159367,1125.34274823365));
#150643=CARTESIAN_POINT('Ctrl Pts',(18.1253194172301,3.32956716117513E-15,
1123.84863058659));
#150644=CARTESIAN_POINT('Ctrl Pts',(17.9710104137728,-1.66525935159367,
1122.35451293953));
#150645=CARTESIAN_POINT('Ctrl Pts',(17.8167014103155,-3.33051870318736,
1120.86039529247));
#150646=CARTESIAN_POINT('Ctrl Pts',(17.3590292079831,-4.93906964482095,
1119.36627764542));
#150647=CARTESIAN_POINT('Ctrl Pts',(16.9013570056506,-6.54762058645456,
1117.87215999836));
#150648=CARTESIAN_POINT('Ctrl Pts',(16.1559070823762,-8.04468584505497,
1116.3780423513));
#150649=CARTESIAN_POINT('Ctrl Pts',(15.4104571591017,-9.54175110365538,
1114.88392470424));
#150650=CARTESIAN_POINT('Ctrl Pts',(14.4026149179538,-10.8763499173728,
1113.38980705718));
#150651=CARTESIAN_POINT('Ctrl Pts',(13.3947726768058,-12.2109487310903,
1111.89568941012));
#150652=CARTESIAN_POINT('Ctrl Pts',(12.1588589765331,-13.3376329379985,
1110.40157176306));
#150653=CARTESIAN_POINT('Ctrl Pts',(10.9229452762603,-14.4643171449067,
1108.907454116));
#150654=CARTESIAN_POINT('Ctrl Pts',(9.50104767561053,-15.3447188656481,
1107.41333646895));
#150655=CARTESIAN_POINT('Ctrl Pts',(8.07915007496071,-16.2251205863895,
1105.91921882189));
#150656=CARTESIAN_POINT('Ctrl Pts',(6.51968959134574,-16.8292587962898,
1104.42510117483));
#150657=CARTESIAN_POINT('Ctrl Pts',(4.96022910773078,-17.4333970061901,
1102.93098352777));
#150658=CARTESIAN_POINT('Ctrl Pts',(3.31631129755346,-17.7406985030951,
1101.43686588071));
#150659=CARTESIAN_POINT('Ctrl Pts',(1.67239348737615,-18.048,1099.94274823365));
#150660=CARTESIAN_POINT('Ctrl Pts',(0.,-18.048,1098.44863058659));
#150661=CARTESIAN_POINT('Ctrl Pts',(-1.67239348737615,-18.048,1096.95451293953));
#150662=CARTESIAN_POINT('Ctrl Pts',(-3.31631129755346,-17.7406985030951,
1095.46039529247));
#150663=CARTESIAN_POINT('Ctrl Pts',(-4.96022910773077,-17.4333970061901,
1093.96627764542));
#150664=CARTESIAN_POINT('Ctrl Pts',(-6.51968959134574,-16.8292587962898,
1092.47215999836));
#150665=CARTESIAN_POINT('Ctrl Pts',(-8.07915007496071,-16.2251205863895,
1090.9780423513));
#150666=CARTESIAN_POINT('Ctrl Pts',(-9.50104767561052,-15.3447188656481,
1089.48392470424));
#150667=CARTESIAN_POINT('Ctrl Pts',(-10.9229452762603,-14.4643171449067,
1087.98980705718));
#150668=CARTESIAN_POINT('Ctrl Pts',(-12.1588589765331,-13.3376329379985,
1086.49568941012));
#150669=CARTESIAN_POINT('Ctrl Pts',(-13.3947726768058,-12.2109487310903,
1085.00157176306));
#150670=CARTESIAN_POINT('Ctrl Pts',(-14.4026149179538,-10.8763499173728,
1083.507454116));
#150671=CARTESIAN_POINT('Ctrl Pts',(-15.4104571591017,-9.54175110365538,
1082.01333646895));
#150672=CARTESIAN_POINT('Ctrl Pts',(-16.1559070823762,-8.04468584505497,
1080.51921882189));
#150673=CARTESIAN_POINT('Ctrl Pts',(-16.9013570056506,-6.54762058645456,
1079.02510117483));
#150674=CARTESIAN_POINT('Ctrl Pts',(-17.3590292079831,-4.93906964482095,
1077.53098352777));
#150675=CARTESIAN_POINT('Ctrl Pts',(-17.8167014103155,-3.33051870318735,
1076.03686588071));
#150676=CARTESIAN_POINT('Ctrl Pts',(-17.9710104137728,-1.66525935159368,
1074.54274823365));
#150677=CARTESIAN_POINT('Ctrl Pts',(-18.1253194172301,-1.10985572039171E-15,
1073.04863058659));
#150678=CARTESIAN_POINT('Ctrl Pts',(-17.9710104137728,1.66525935159367,
1071.55451293953));
#150679=CARTESIAN_POINT('Ctrl Pts',(-17.8167014103155,3.33051870318735,
1070.06039529247));
#150680=CARTESIAN_POINT('Ctrl Pts',(-17.3590292079831,4.93906964482096,
1068.56627764542));
#150681=CARTESIAN_POINT('Ctrl Pts',(-16.9013570056506,6.54762058645456,
1067.07215999836));
#150682=CARTESIAN_POINT('Ctrl Pts',(-16.1559070823762,8.04468584505497,
1065.5780423513));
#150683=CARTESIAN_POINT('Ctrl Pts',(-15.4104571591017,9.54175110365538,
1064.08392470424));
#150684=CARTESIAN_POINT('Ctrl Pts',(-14.4026149179538,10.8763499173728,
1062.58980705718));
#150685=CARTESIAN_POINT('Ctrl Pts',(-13.3947726768058,12.2109487310903,
1061.09568941012));
#150686=CARTESIAN_POINT('Ctrl Pts',(-12.1588589765331,13.3376329379985,
1059.60157176306));
#150687=CARTESIAN_POINT('Ctrl Pts',(-10.9229452762603,14.4643171449067,
1058.107454116));
#150688=CARTESIAN_POINT('Ctrl Pts',(-9.50104767561052,15.3447188656481,
1056.61333646895));
#150689=CARTESIAN_POINT('Ctrl Pts',(-8.07915007496071,16.2251205863895,
1055.11921882189));
#150690=CARTESIAN_POINT('Ctrl Pts',(-6.51968959134574,16.8292587962898,
1053.62510117483));
#150691=CARTESIAN_POINT('Ctrl Pts',(-4.96022910773078,17.4333970061901,
1052.13098352777));
#150692=CARTESIAN_POINT('Ctrl Pts',(-3.31631129755346,17.7406985030951,
1050.63686588071));
#150693=CARTESIAN_POINT('Ctrl Pts',(-1.67239348737615,18.048,1049.14274823365));
#150694=CARTESIAN_POINT('Ctrl Pts',(-2.21024254310115E-15,18.048,1047.64863058659));
#150695=CARTESIAN_POINT('Ctrl Pts',(1.67239348737616,18.048,1046.15451293953));
#150696=CARTESIAN_POINT('Ctrl Pts',(3.31631129755346,17.7406985030951,1044.66039529247));
#150697=CARTESIAN_POINT('Ctrl Pts',(4.96022910773077,17.4333970061901,1043.16627764542));
#150698=CARTESIAN_POINT('Ctrl Pts',(6.51968959134575,16.8292587962898,1041.67215999836));
#150699=CARTESIAN_POINT('Ctrl Pts',(8.07915007496071,16.2251205863895,1040.1780423513));
#150700=CARTESIAN_POINT('Ctrl Pts',(9.50104767561053,15.3447188656481,1038.68392470424));
#150701=CARTESIAN_POINT('Ctrl Pts',(10.9229452762603,14.4643171449067,1037.18980705718));
#150702=CARTESIAN_POINT('Ctrl Pts',(12.1588589765331,13.3376329379985,1035.69568941012));
#150703=CARTESIAN_POINT('Ctrl Pts',(13.3947726768058,12.2109487310903,1034.20157176306));
#150704=CARTESIAN_POINT('Ctrl Pts',(14.4026149179538,10.8763499173728,1032.707454116));
#150705=CARTESIAN_POINT('Ctrl Pts',(15.4104571591017,9.54175110365538,1031.21333646895));
#150706=CARTESIAN_POINT('Ctrl Pts',(16.1559070823762,8.04468584505496,1029.71921882189));
#150707=CARTESIAN_POINT('Ctrl Pts',(16.9013570056506,6.54762058645456,1028.22510117483));
#150708=CARTESIAN_POINT('Ctrl Pts',(17.3590292079831,4.93906964482096,1026.73098352777));
#150709=CARTESIAN_POINT('Ctrl Pts',(17.8167014103155,3.33051870318735,1025.23686588071));
#150710=CARTESIAN_POINT('Ctrl Pts',(17.9710104137728,1.66525935159367,1023.74274823365));
#150711=CARTESIAN_POINT('Ctrl Pts',(18.1253194172301,3.32956716117513E-15,
1022.24863058659));
#150712=CARTESIAN_POINT('Ctrl Pts',(17.9710104137728,-1.66525935159367,
1020.75451293953));
#150713=CARTESIAN_POINT('Ctrl Pts',(17.8167014103155,-3.33051870318736,
1019.26039529247));
#150714=CARTESIAN_POINT('Ctrl Pts',(17.3590292079831,-4.93906964482095,
1017.76627764542));
#150715=CARTESIAN_POINT('Ctrl Pts',(16.9013570056506,-6.54762058645456,
1016.27215999836));
#150716=CARTESIAN_POINT('Ctrl Pts',(16.1559070823762,-8.04468584505497,
1014.7780423513));
#150717=CARTESIAN_POINT('Ctrl Pts',(15.4104571591017,-9.54175110365538,
1013.28392470424));
#150718=CARTESIAN_POINT('Ctrl Pts',(14.4026149179538,-10.8763499173728,
1011.78980705718));
#150719=CARTESIAN_POINT('Ctrl Pts',(13.3947726768058,-12.2109487310903,
1010.29568941012));
#150720=CARTESIAN_POINT('Ctrl Pts',(12.1588589765331,-13.3376329379985,
1008.80157176306));
#150721=CARTESIAN_POINT('Ctrl Pts',(10.9229452762603,-14.4643171449067,
1007.307454116));
#150722=CARTESIAN_POINT('Ctrl Pts',(9.50104767561053,-15.3447188656481,
1005.81333646895));
#150723=CARTESIAN_POINT('Ctrl Pts',(8.07915007496071,-16.2251205863895,
1004.31921882189));
#150724=CARTESIAN_POINT('Ctrl Pts',(6.51968959134574,-16.8292587962898,
1002.82510117483));
#150725=CARTESIAN_POINT('Ctrl Pts',(4.96022910773078,-17.4333970061901,
1001.33098352777));
#150726=CARTESIAN_POINT('Ctrl Pts',(3.31631129755346,-17.7406985030951,
999.83686588071));
#150727=CARTESIAN_POINT('Ctrl Pts',(1.67239348737615,-18.048,998.342748233651));
#150728=CARTESIAN_POINT('Ctrl Pts',(0.,-18.048,996.848630586592));
#150729=CARTESIAN_POINT('Ctrl Pts',(-1.67239348737615,-18.048,995.354512939534));
#150730=CARTESIAN_POINT('Ctrl Pts',(-3.31631129755346,-17.7406985030951,
993.860395292475));
#150731=CARTESIAN_POINT('Ctrl Pts',(-4.96022910773077,-17.4333970061901,
992.366277645416));
#150732=CARTESIAN_POINT('Ctrl Pts',(-6.51968959134574,-16.8292587962898,
990.872159998357));
#150733=CARTESIAN_POINT('Ctrl Pts',(-8.07915007496071,-16.2251205863895,
989.378042351298));
#150734=CARTESIAN_POINT('Ctrl Pts',(-9.50104767561052,-15.3447188656481,
987.883924704239));
#150735=CARTESIAN_POINT('Ctrl Pts',(-10.9229452762603,-14.4643171449067,
986.38980705718));
#150736=CARTESIAN_POINT('Ctrl Pts',(-12.1588589765331,-13.3376329379985,
984.895689410122));
#150737=CARTESIAN_POINT('Ctrl Pts',(-13.3947726768058,-12.2109487310903,
983.401571763063));
#150738=CARTESIAN_POINT('Ctrl Pts',(-14.4026149179538,-10.8763499173728,
981.907454116004));
#150739=CARTESIAN_POINT('Ctrl Pts',(-15.4104571591017,-9.54175110365538,
980.413336468945));
#150740=CARTESIAN_POINT('Ctrl Pts',(-16.1559070823762,-8.04468584505497,
978.919218821886));
#150741=CARTESIAN_POINT('Ctrl Pts',(-16.9013570056506,-6.54762058645456,
977.425101174828));
#150742=CARTESIAN_POINT('Ctrl Pts',(-17.3590292079831,-4.93906964482095,
975.930983527769));
#150743=CARTESIAN_POINT('Ctrl Pts',(-17.8167014103155,-3.33051870318735,
974.43686588071));
#150744=CARTESIAN_POINT('Ctrl Pts',(-17.9710104137728,-1.66525935159368,
972.942748233651));
#150745=CARTESIAN_POINT('Ctrl Pts',(-18.1253194172301,-1.10985572039171E-15,
971.448630586592));
#150746=CARTESIAN_POINT('Ctrl Pts',(-17.9710104137728,1.66525935159367,
969.954512939534));
#150747=CARTESIAN_POINT('Ctrl Pts',(-17.8167014103155,3.33051870318735,
968.460395292475));
#150748=CARTESIAN_POINT('Ctrl Pts',(-17.3590292079831,4.93906964482096,
966.966277645416));
#150749=CARTESIAN_POINT('Ctrl Pts',(-16.9013570056506,6.54762058645456,
965.472159998357));
#150750=CARTESIAN_POINT('Ctrl Pts',(-16.1559070823762,8.04468584505497,
963.978042351298));
#150751=CARTESIAN_POINT('Ctrl Pts',(-15.4104571591017,9.54175110365538,
962.483924704239));
#150752=CARTESIAN_POINT('Ctrl Pts',(-14.4026149179538,10.8763499173728,
960.989807057181));
#150753=CARTESIAN_POINT('Ctrl Pts',(-13.3947726768058,12.2109487310903,
959.495689410122));
#150754=CARTESIAN_POINT('Ctrl Pts',(-12.1588589765331,13.3376329379985,
958.001571763063));
#150755=CARTESIAN_POINT('Ctrl Pts',(-10.9229452762603,14.4643171449067,
956.507454116004));
#150756=CARTESIAN_POINT('Ctrl Pts',(-9.50104767561052,15.3447188656481,
955.013336468945));
#150757=CARTESIAN_POINT('Ctrl Pts',(-8.07915007496071,16.2251205863895,
953.519218821887));
#150758=CARTESIAN_POINT('Ctrl Pts',(-6.51968959134574,16.8292587962898,
952.025101174828));
#150759=CARTESIAN_POINT('Ctrl Pts',(-4.96022910773078,17.4333970061901,
950.530983527769));
#150760=CARTESIAN_POINT('Ctrl Pts',(-3.31631129755346,17.7406985030951,
949.03686588071));
#150761=CARTESIAN_POINT('Ctrl Pts',(-1.67239348737615,18.048,947.542748233651));
#150762=CARTESIAN_POINT('Ctrl Pts',(-2.21024254310115E-15,18.048,946.048630586592));
#150763=CARTESIAN_POINT('Ctrl Pts',(1.67239348737616,18.048,944.554512939534));
#150764=CARTESIAN_POINT('Ctrl Pts',(3.31631129755346,17.7406985030951,943.060395292475));
#150765=CARTESIAN_POINT('Ctrl Pts',(4.96022910773077,17.4333970061901,941.566277645416));
#150766=CARTESIAN_POINT('Ctrl Pts',(6.51968959134575,16.8292587962898,940.072159998357));
#150767=CARTESIAN_POINT('Ctrl Pts',(8.07915007496071,16.2251205863895,938.578042351298));
#150768=CARTESIAN_POINT('Ctrl Pts',(9.50104767561053,15.3447188656481,937.083924704239));
#150769=CARTESIAN_POINT('Ctrl Pts',(10.9229452762603,14.4643171449067,935.589807057181));
#150770=CARTESIAN_POINT('Ctrl Pts',(12.1588589765331,13.3376329379985,934.095689410122));
#150771=CARTESIAN_POINT('Ctrl Pts',(13.3947726768058,12.2109487310903,932.601571763063));
#150772=CARTESIAN_POINT('Ctrl Pts',(14.4026149179538,10.8763499173728,931.107454116004));
#150773=CARTESIAN_POINT('Ctrl Pts',(15.4104571591017,9.54175110365538,929.613336468945));
#150774=CARTESIAN_POINT('Ctrl Pts',(16.1559070823762,8.04468584505496,928.119218821886));
#150775=CARTESIAN_POINT('Ctrl Pts',(16.9013570056506,6.54762058645456,926.625101174827));
#150776=CARTESIAN_POINT('Ctrl Pts',(17.3590292079831,4.93906964482096,925.130983527769));
#150777=CARTESIAN_POINT('Ctrl Pts',(17.8167014103155,3.33051870318735,923.63686588071));
#150778=CARTESIAN_POINT('Ctrl Pts',(17.9710104137728,1.66525935159367,922.142748233651));
#150779=CARTESIAN_POINT('Ctrl Pts',(18.1253194172301,3.32956716117513E-15,
920.648630586593));
#150780=CARTESIAN_POINT('Ctrl Pts',(17.9710104137728,-1.66525935159367,
919.154512939534));
#150781=CARTESIAN_POINT('Ctrl Pts',(17.8167014103155,-3.33051870318736,
917.660395292475));
#150782=CARTESIAN_POINT('Ctrl Pts',(17.3590292079831,-4.93906964482095,
916.166277645416));
#150783=CARTESIAN_POINT('Ctrl Pts',(16.9013570056506,-6.54762058645456,
914.672159998357));
#150784=CARTESIAN_POINT('Ctrl Pts',(16.1559070823762,-8.04468584505497,
913.178042351298));
#150785=CARTESIAN_POINT('Ctrl Pts',(15.4104571591017,-9.54175110365538,
911.683924704239));
#150786=CARTESIAN_POINT('Ctrl Pts',(14.4026149179538,-10.8763499173728,
910.18980705718));
#150787=CARTESIAN_POINT('Ctrl Pts',(13.3947726768058,-12.2109487310903,
908.695689410122));
#150788=CARTESIAN_POINT('Ctrl Pts',(12.1588589765331,-13.3376329379985,
907.201571763063));
#150789=CARTESIAN_POINT('Ctrl Pts',(10.9229452762603,-14.4643171449067,
905.707454116004));
#150790=CARTESIAN_POINT('Ctrl Pts',(9.50104767561053,-15.3447188656481,
904.213336468945));
#150791=CARTESIAN_POINT('Ctrl Pts',(8.07915007496071,-16.2251205863895,
902.719218821886));
#150792=CARTESIAN_POINT('Ctrl Pts',(6.51968959134574,-16.8292587962898,
901.225101174828));
#150793=CARTESIAN_POINT('Ctrl Pts',(4.96022910773078,-17.4333970061901,
899.730983527769));
#150794=CARTESIAN_POINT('Ctrl Pts',(3.31631129755346,-17.7406985030951,
898.23686588071));
#150795=CARTESIAN_POINT('Ctrl Pts',(1.67239348737615,-18.048,896.742748233651));
#150796=CARTESIAN_POINT('Ctrl Pts',(0.,-18.048,895.248630586592));
#150797=CARTESIAN_POINT('Ctrl Pts',(-1.67239348737615,-18.048,893.754512939534));
#150798=CARTESIAN_POINT('Ctrl Pts',(-3.31631129755346,-17.7406985030951,
892.260395292475));
#150799=CARTESIAN_POINT('Ctrl Pts',(-4.96022910773077,-17.4333970061901,
890.766277645416));
#150800=CARTESIAN_POINT('Ctrl Pts',(-6.51968959134574,-16.8292587962898,
889.272159998357));
#150801=CARTESIAN_POINT('Ctrl Pts',(-8.07915007496071,-16.2251205863895,
887.778042351298));
#150802=CARTESIAN_POINT('Ctrl Pts',(-9.50104767561052,-15.3447188656481,
886.283924704239));
#150803=CARTESIAN_POINT('Ctrl Pts',(-10.9229452762603,-14.4643171449067,
884.789807057181));
#150804=CARTESIAN_POINT('Ctrl Pts',(-12.1588589765331,-13.3376329379985,
883.295689410122));
#150805=CARTESIAN_POINT('Ctrl Pts',(-13.3947726768058,-12.2109487310903,
881.801571763063));
#150806=CARTESIAN_POINT('Ctrl Pts',(-14.4026149179538,-10.8763499173728,
880.307454116004));
#150807=CARTESIAN_POINT('Ctrl Pts',(-15.4104571591017,-9.54175110365538,
878.813336468945));
#150808=CARTESIAN_POINT('Ctrl Pts',(-16.1559070823762,-8.04468584505497,
877.319218821886));
#150809=CARTESIAN_POINT('Ctrl Pts',(-16.9013570056506,-6.54762058645456,
875.825101174828));
#150810=CARTESIAN_POINT('Ctrl Pts',(-17.3590292079831,-4.93906964482095,
874.330983527769));
#150811=CARTESIAN_POINT('Ctrl Pts',(-17.8167014103155,-3.33051870318735,
872.83686588071));
#150812=CARTESIAN_POINT('Ctrl Pts',(-17.9710104137728,-1.66525935159368,
871.342748233651));
#150813=CARTESIAN_POINT('Ctrl Pts',(-18.1253194172301,-1.10985572039171E-15,
869.848630586592));
#150814=CARTESIAN_POINT('Ctrl Pts',(-17.9710104137728,1.66525935159367,
868.354512939534));
#150815=CARTESIAN_POINT('Ctrl Pts',(-17.8167014103155,3.33051870318735,
866.860395292475));
#150816=CARTESIAN_POINT('Ctrl Pts',(-17.3590292079831,4.93906964482096,
865.366277645416));
#150817=CARTESIAN_POINT('Ctrl Pts',(-16.9013570056506,6.54762058645456,
863.872159998357));
#150818=CARTESIAN_POINT('Ctrl Pts',(-16.1559070823762,8.04468584505497,
862.378042351298));
#150819=CARTESIAN_POINT('Ctrl Pts',(-15.4104571591017,9.54175110365538,
860.883924704239));
#150820=CARTESIAN_POINT('Ctrl Pts',(-14.4026149179538,10.8763499173728,
859.389807057181));
#150821=CARTESIAN_POINT('Ctrl Pts',(-13.3947726768058,12.2109487310903,
857.895689410122));
#150822=CARTESIAN_POINT('Ctrl Pts',(-12.1588589765331,13.3376329379985,
856.401571763063));
#150823=CARTESIAN_POINT('Ctrl Pts',(-10.9229452762603,14.4643171449067,
854.907454116004));
#150824=CARTESIAN_POINT('Ctrl Pts',(-9.50104767561052,15.3447188656481,
853.413336468945));
#150825=CARTESIAN_POINT('Ctrl Pts',(-8.07915007496071,16.2251205863895,
851.919218821886));
#150826=CARTESIAN_POINT('Ctrl Pts',(-6.51968959134574,16.8292587962898,
850.425101174828));
#150827=CARTESIAN_POINT('Ctrl Pts',(-4.96022910773078,17.4333970061901,
848.930983527769));
#150828=CARTESIAN_POINT('Ctrl Pts',(-3.31631129755346,17.7406985030951,
847.43686588071));
#150829=CARTESIAN_POINT('Ctrl Pts',(-1.67239348737615,18.048,845.942748233651));
#150830=CARTESIAN_POINT('Ctrl Pts',(-2.21024254310115E-15,18.048,844.448630586592));
#150831=CARTESIAN_POINT('Ctrl Pts',(1.67239348737616,18.048,842.954512939534));
#150832=CARTESIAN_POINT('Ctrl Pts',(3.31631129755346,17.7406985030951,841.460395292475));
#150833=CARTESIAN_POINT('Ctrl Pts',(4.96022910773077,17.4333970061901,839.966277645416));
#150834=CARTESIAN_POINT('Ctrl Pts',(6.51968959134575,16.8292587962898,838.472159998357));
#150835=CARTESIAN_POINT('Ctrl Pts',(8.07915007496071,16.2251205863895,836.978042351298));
#150836=CARTESIAN_POINT('Ctrl Pts',(9.50104767561053,15.3447188656481,835.483924704239));
#150837=CARTESIAN_POINT('Ctrl Pts',(10.9229452762603,14.4643171449067,833.989807057181));
#150838=CARTESIAN_POINT('Ctrl Pts',(12.1588589765331,13.3376329379985,832.495689410122));
#150839=CARTESIAN_POINT('Ctrl Pts',(13.3947726768058,12.2109487310903,831.001571763063));
#150840=CARTESIAN_POINT('Ctrl Pts',(14.4026149179538,10.8763499173728,829.507454116004));
#150841=CARTESIAN_POINT('Ctrl Pts',(15.4104571591017,9.54175110365538,828.013336468945));
#150842=CARTESIAN_POINT('Ctrl Pts',(16.1559070823762,8.04468584505496,826.519218821886));
#150843=CARTESIAN_POINT('Ctrl Pts',(16.9013570056506,6.54762058645456,825.025101174828));
#150844=CARTESIAN_POINT('Ctrl Pts',(17.3590292079831,4.93906964482096,823.530983527769));
#150845=CARTESIAN_POINT('Ctrl Pts',(17.8167014103155,3.33051870318735,822.03686588071));
#150846=CARTESIAN_POINT('Ctrl Pts',(17.9710104137728,1.66525935159367,820.542748233651));
#150847=CARTESIAN_POINT('Ctrl Pts',(18.1253194172301,3.32956716117513E-15,
819.048630586593));
#150848=CARTESIAN_POINT('Ctrl Pts',(17.9710104137728,-1.66525935159367,
817.554512939533));
#150849=CARTESIAN_POINT('Ctrl Pts',(17.8167014103155,-3.33051870318736,
816.060395292475));
#150850=CARTESIAN_POINT('Ctrl Pts',(17.3590292079831,-4.93906964482095,
814.566277645416));
#150851=CARTESIAN_POINT('Ctrl Pts',(16.9013570056506,-6.54762058645456,
813.072159998357));
#150852=CARTESIAN_POINT('Ctrl Pts',(16.1559070823762,-8.04468584505497,
811.578042351298));
#150853=CARTESIAN_POINT('Ctrl Pts',(15.4104571591017,-9.54175110365538,
810.083924704239));
#150854=CARTESIAN_POINT('Ctrl Pts',(14.4026149179538,-10.8763499173728,
808.589807057181));
#150855=CARTESIAN_POINT('Ctrl Pts',(13.3947726768058,-12.2109487310903,
807.095689410122));
#150856=CARTESIAN_POINT('Ctrl Pts',(12.1588589765331,-13.3376329379985,
805.601571763063));
#150857=CARTESIAN_POINT('Ctrl Pts',(10.9229452762603,-14.4643171449067,
804.107454116004));
#150858=CARTESIAN_POINT('Ctrl Pts',(9.50104767561053,-15.3447188656481,
802.613336468945));
#150859=CARTESIAN_POINT('Ctrl Pts',(8.07915007496071,-16.2251205863895,
801.119218821887));
#150860=CARTESIAN_POINT('Ctrl Pts',(6.51968959134574,-16.8292587962898,
799.625101174828));
#150861=CARTESIAN_POINT('Ctrl Pts',(4.96022910773078,-17.4333970061901,
798.130983527769));
#150862=CARTESIAN_POINT('Ctrl Pts',(3.31631129755346,-17.7406985030951,
796.63686588071));
#150863=CARTESIAN_POINT('Ctrl Pts',(1.67239348737615,-18.048,795.142748233651));
#150864=CARTESIAN_POINT('Ctrl Pts',(0.,-18.048,793.648630586592));
#150865=CARTESIAN_POINT('Ctrl Pts',(-1.67239348737615,-18.048,792.154512939534));
#150866=CARTESIAN_POINT('Ctrl Pts',(-3.31631129755346,-17.7406985030951,
790.660395292475));
#150867=CARTESIAN_POINT('Ctrl Pts',(-4.96022910773077,-17.4333970061901,
789.166277645416));
#150868=CARTESIAN_POINT('Ctrl Pts',(-6.51968959134574,-16.8292587962898,
787.672159998357));
#150869=CARTESIAN_POINT('Ctrl Pts',(-8.07915007496071,-16.2251205863895,
786.178042351298));
#150870=CARTESIAN_POINT('Ctrl Pts',(-9.50104767561052,-15.3447188656481,
784.683924704239));
#150871=CARTESIAN_POINT('Ctrl Pts',(-10.9229452762603,-14.4643171449067,
783.189807057181));
#150872=CARTESIAN_POINT('Ctrl Pts',(-12.1588589765331,-13.3376329379985,
781.695689410122));
#150873=CARTESIAN_POINT('Ctrl Pts',(-13.3947726768058,-12.2109487310903,
780.201571763063));
#150874=CARTESIAN_POINT('Ctrl Pts',(-14.4026149179538,-10.8763499173728,
778.707454116004));
#150875=CARTESIAN_POINT('Ctrl Pts',(-15.4104571591017,-9.54175110365538,
777.213336468945));
#150876=CARTESIAN_POINT('Ctrl Pts',(-16.1559070823762,-8.04468584505497,
775.719218821886));
#150877=CARTESIAN_POINT('Ctrl Pts',(-16.9013570056506,-6.54762058645456,
774.225101174828));
#150878=CARTESIAN_POINT('Ctrl Pts',(-17.3590292079831,-4.93906964482095,
772.730983527769));
#150879=CARTESIAN_POINT('Ctrl Pts',(-17.8167014103155,-3.33051870318735,
771.23686588071));
#150880=CARTESIAN_POINT('Ctrl Pts',(-17.9710104137728,-1.66525935159368,
769.742748233651));
#150881=CARTESIAN_POINT('Ctrl Pts',(-18.1253194172301,-1.10985572039171E-15,
768.248630586593));
#150882=CARTESIAN_POINT('Ctrl Pts',(-17.9710104137728,1.66525935159367,
766.754512939533));
#150883=CARTESIAN_POINT('Ctrl Pts',(-17.8167014103155,3.33051870318735,
765.260395292475));
#150884=CARTESIAN_POINT('Ctrl Pts',(-17.3590292079831,4.93906964482096,
763.766277645416));
#150885=CARTESIAN_POINT('Ctrl Pts',(-16.9013570056506,6.54762058645456,
762.272159998357));
#150886=CARTESIAN_POINT('Ctrl Pts',(-16.1559070823762,8.04468584505497,
760.778042351298));
#150887=CARTESIAN_POINT('Ctrl Pts',(-15.4104571591017,9.54175110365538,
759.28392470424));
#150888=CARTESIAN_POINT('Ctrl Pts',(-14.4026149179538,10.8763499173728,
757.78980705718));
#150889=CARTESIAN_POINT('Ctrl Pts',(-13.3947726768058,12.2109487310903,
756.295689410122));
#150890=CARTESIAN_POINT('Ctrl Pts',(-12.1588589765331,13.3376329379985,
754.801571763063));
#150891=CARTESIAN_POINT('Ctrl Pts',(-10.9229452762603,14.4643171449067,
753.307454116004));
#150892=CARTESIAN_POINT('Ctrl Pts',(-9.50104767561052,15.3447188656481,
751.813336468945));
#150893=CARTESIAN_POINT('Ctrl Pts',(-8.07915007496071,16.2251205863895,
750.319218821886));
#150894=CARTESIAN_POINT('Ctrl Pts',(-6.51968959134574,16.8292587962898,
748.825101174828));
#150895=CARTESIAN_POINT('Ctrl Pts',(-4.96022910773078,17.4333970061901,
747.330983527769));
#150896=CARTESIAN_POINT('Ctrl Pts',(-3.31631129755346,17.7406985030951,
745.83686588071));
#150897=CARTESIAN_POINT('Ctrl Pts',(-1.67239348737615,18.048,744.342748233651));
#150898=CARTESIAN_POINT('Ctrl Pts',(-2.21024254310115E-15,18.048,742.848630586592));
#150899=CARTESIAN_POINT('Ctrl Pts',(1.67239348737616,18.048,741.354512939533));
#150900=CARTESIAN_POINT('Ctrl Pts',(3.31631129755346,17.7406985030951,739.860395292475));
#150901=CARTESIAN_POINT('Ctrl Pts',(4.96022910773077,17.4333970061901,738.366277645416));
#150902=CARTESIAN_POINT('Ctrl Pts',(6.51968959134575,16.8292587962898,736.872159998357));
#150903=CARTESIAN_POINT('Ctrl Pts',(8.07915007496071,16.2251205863895,735.378042351298));
#150904=CARTESIAN_POINT('Ctrl Pts',(9.50104767561053,15.3447188656481,733.883924704239));
#150905=CARTESIAN_POINT('Ctrl Pts',(10.9229452762603,14.4643171449067,732.389807057181));
#150906=CARTESIAN_POINT('Ctrl Pts',(12.1588589765331,13.3376329379985,730.895689410122));
#150907=CARTESIAN_POINT('Ctrl Pts',(13.3947726768058,12.2109487310903,729.401571763063));
#150908=CARTESIAN_POINT('Ctrl Pts',(14.4026149179538,10.8763499173728,727.907454116004));
#150909=CARTESIAN_POINT('Ctrl Pts',(15.4104571591017,9.54175110365538,726.413336468945));
#150910=CARTESIAN_POINT('Ctrl Pts',(16.1559070823762,8.04468584505496,724.919218821886));
#150911=CARTESIAN_POINT('Ctrl Pts',(16.9013570056506,6.54762058645456,723.425101174828));
#150912=CARTESIAN_POINT('Ctrl Pts',(17.3590292079831,4.93906964482096,721.930983527769));
#150913=CARTESIAN_POINT('Ctrl Pts',(17.8167014103155,3.33051870318735,720.43686588071));
#150914=CARTESIAN_POINT('Ctrl Pts',(17.9710104137728,1.66525935159367,718.942748233651));
#150915=CARTESIAN_POINT('Ctrl Pts',(18.1253194172301,3.32956716117513E-15,
717.448630586592));
#150916=CARTESIAN_POINT('Ctrl Pts',(17.9710104137728,-1.66525935159367,
715.954512939534));
#150917=CARTESIAN_POINT('Ctrl Pts',(17.8167014103155,-3.33051870318736,
714.460395292475));
#150918=CARTESIAN_POINT('Ctrl Pts',(17.3590292079831,-4.93906964482095,
712.966277645416));
#150919=CARTESIAN_POINT('Ctrl Pts',(16.9013570056506,-6.54762058645456,
711.472159998357));
#150920=CARTESIAN_POINT('Ctrl Pts',(16.1559070823762,-8.04468584505497,
709.978042351298));
#150921=CARTESIAN_POINT('Ctrl Pts',(15.4104571591017,-9.54175110365538,
708.483924704239));
#150922=CARTESIAN_POINT('Ctrl Pts',(14.4026149179538,-10.8763499173728,
706.989807057181));
#150923=CARTESIAN_POINT('Ctrl Pts',(13.3947726768058,-12.2109487310903,
705.495689410122));
#150924=CARTESIAN_POINT('Ctrl Pts',(12.1588589765331,-13.3376329379985,
704.001571763063));
#150925=CARTESIAN_POINT('Ctrl Pts',(10.9229452762603,-14.4643171449067,
702.507454116004));
#150926=CARTESIAN_POINT('Ctrl Pts',(9.50104767561053,-15.3447188656481,
701.013336468945));
#150927=CARTESIAN_POINT('Ctrl Pts',(8.07915007496071,-16.2251205863895,
699.519218821886));
#150928=CARTESIAN_POINT('Ctrl Pts',(6.51968959134574,-16.8292587962898,
698.025101174828));
#150929=CARTESIAN_POINT('Ctrl Pts',(4.96022910773078,-17.4333970061901,
696.530983527769));
#150930=CARTESIAN_POINT('Ctrl Pts',(3.31631129755346,-17.7406985030951,
695.03686588071));
#150931=CARTESIAN_POINT('Ctrl Pts',(1.67239348737615,-18.048,693.542748233651));
#150932=CARTESIAN_POINT('Ctrl Pts',(0.,-18.048,692.048630586592));
#150933=CARTESIAN_POINT('Ctrl Pts',(-1.67239348737615,-18.048,690.554512939533));
#150934=CARTESIAN_POINT('Ctrl Pts',(-3.31631129755346,-17.7406985030951,
689.060395292475));
#150935=CARTESIAN_POINT('Ctrl Pts',(-4.96022910773077,-17.4333970061901,
687.566277645416));
#150936=CARTESIAN_POINT('Ctrl Pts',(-6.51968959134574,-16.8292587962898,
686.072159998357));
#150937=CARTESIAN_POINT('Ctrl Pts',(-8.07915007496071,-16.2251205863895,
684.578042351298));
#150938=CARTESIAN_POINT('Ctrl Pts',(-9.50104767561052,-15.3447188656481,
683.083924704239));
#150939=CARTESIAN_POINT('Ctrl Pts',(-10.9229452762603,-14.4643171449067,
681.589807057181));
#150940=CARTESIAN_POINT('Ctrl Pts',(-12.1588589765331,-13.3376329379985,
680.095689410122));
#150941=CARTESIAN_POINT('Ctrl Pts',(-13.3947726768058,-12.2109487310903,
678.601571763063));
#150942=CARTESIAN_POINT('Ctrl Pts',(-14.4026149179538,-10.8763499173728,
677.107454116004));
#150943=CARTESIAN_POINT('Ctrl Pts',(-15.4104571591017,-9.54175110365538,
675.613336468945));
#150944=CARTESIAN_POINT('Ctrl Pts',(-16.1559070823762,-8.04468584505497,
674.119218821887));
#150945=CARTESIAN_POINT('Ctrl Pts',(-16.9013570056506,-6.54762058645456,
672.625101174828));
#150946=CARTESIAN_POINT('Ctrl Pts',(-17.3590292079831,-4.93906964482095,
671.130983527769));
#150947=CARTESIAN_POINT('Ctrl Pts',(-17.8167014103155,-3.33051870318735,
669.63686588071));
#150948=CARTESIAN_POINT('Ctrl Pts',(-17.9710104137728,-1.66525935159368,
668.142748233651));
#150949=CARTESIAN_POINT('Ctrl Pts',(-18.1253194172301,-1.10985572039171E-15,
666.648630586592));
#150950=CARTESIAN_POINT('Ctrl Pts',(-17.9710104137728,1.66525935159367,
665.154512939533));
#150951=CARTESIAN_POINT('Ctrl Pts',(-17.8167014103155,3.33051870318735,
663.660395292475));
#150952=CARTESIAN_POINT('Ctrl Pts',(-17.3590292079831,4.93906964482096,
662.166277645416));
#150953=CARTESIAN_POINT('Ctrl Pts',(-16.9013570056506,6.54762058645456,
660.672159998357));
#150954=CARTESIAN_POINT('Ctrl Pts',(-16.1559070823762,8.04468584505497,
659.178042351298));
#150955=CARTESIAN_POINT('Ctrl Pts',(-15.4104571591017,9.54175110365538,
657.68392470424));
#150956=CARTESIAN_POINT('Ctrl Pts',(-14.4026149179538,10.8763499173728,
656.18980705718));
#150957=CARTESIAN_POINT('Ctrl Pts',(-13.3947726768058,12.2109487310903,
654.695689410122));
#150958=CARTESIAN_POINT('Ctrl Pts',(-12.1588589765331,13.3376329379985,
653.201571763063));
#150959=CARTESIAN_POINT('Ctrl Pts',(-10.9229452762603,14.4643171449067,
651.707454116004));
#150960=CARTESIAN_POINT('Ctrl Pts',(-9.50104767561052,15.3447188656481,
650.213336468945));
#150961=CARTESIAN_POINT('Ctrl Pts',(-8.07915007496071,16.2251205863895,
648.719218821886));
#150962=CARTESIAN_POINT('Ctrl Pts',(-6.51968959134574,16.8292587962898,
647.225101174828));
#150963=CARTESIAN_POINT('Ctrl Pts',(-4.96022910773078,17.4333970061901,
645.730983527769));
#150964=CARTESIAN_POINT('Ctrl Pts',(-3.31631129755346,17.7406985030951,
644.23686588071));
#150965=CARTESIAN_POINT('Ctrl Pts',(-1.67239348737615,18.048,642.742748233651));
#150966=CARTESIAN_POINT('Ctrl Pts',(-2.21024254310115E-15,18.048,641.248630586592));
#150967=CARTESIAN_POINT('Ctrl Pts',(1.67239348737616,18.048,639.754512939533));
#150968=CARTESIAN_POINT('Ctrl Pts',(3.31631129755346,17.7406985030951,638.260395292475));
#150969=CARTESIAN_POINT('Ctrl Pts',(4.96022910773077,17.4333970061901,636.766277645416));
#150970=CARTESIAN_POINT('Ctrl Pts',(6.51968959134575,16.8292587962898,635.272159998357));
#150971=CARTESIAN_POINT('Ctrl Pts',(8.07915007496071,16.2251205863895,633.778042351298));
#150972=CARTESIAN_POINT('Ctrl Pts',(9.50104767561053,15.3447188656481,632.283924704239));
#150973=CARTESIAN_POINT('Ctrl Pts',(10.9229452762603,14.4643171449067,630.78980705718));
#150974=CARTESIAN_POINT('Ctrl Pts',(12.1588589765331,13.3376329379985,629.295689410122));
#150975=CARTESIAN_POINT('Ctrl Pts',(13.3947726768058,12.2109487310903,627.801571763063));
#150976=CARTESIAN_POINT('Ctrl Pts',(14.4026149179538,10.8763499173728,626.307454116004));
#150977=CARTESIAN_POINT('Ctrl Pts',(15.4104571591017,9.54175110365538,624.813336468945));
#150978=CARTESIAN_POINT('Ctrl Pts',(16.1559070823762,8.04468584505496,623.319218821886));
#150979=CARTESIAN_POINT('Ctrl Pts',(16.9013570056506,6.54762058645456,621.825101174828));
#150980=CARTESIAN_POINT('Ctrl Pts',(17.3590292079831,4.93906964482096,620.330983527769));
#150981=CARTESIAN_POINT('Ctrl Pts',(17.8167014103155,3.33051870318735,618.83686588071));
#150982=CARTESIAN_POINT('Ctrl Pts',(17.9710104137728,1.66525935159367,617.342748233651));
#150983=CARTESIAN_POINT('Ctrl Pts',(18.1253194172301,3.32956716117513E-15,
615.848630586592));
#150984=CARTESIAN_POINT('Ctrl Pts',(17.9710104137728,-1.66525935159367,
614.354512939533));
#150985=CARTESIAN_POINT('Ctrl Pts',(17.8167014103155,-3.33051870318736,
612.860395292475));
#150986=CARTESIAN_POINT('Ctrl Pts',(17.3590292079831,-4.93906964482095,
611.366277645416));
#150987=CARTESIAN_POINT('Ctrl Pts',(16.9013570056506,-6.54762058645456,
609.872159998357));
#150988=CARTESIAN_POINT('Ctrl Pts',(16.1559070823762,-8.04468584505497,
608.378042351298));
#150989=CARTESIAN_POINT('Ctrl Pts',(15.4104571591017,-9.54175110365538,
606.88392470424));
#150990=CARTESIAN_POINT('Ctrl Pts',(14.4026149179538,-10.8763499173728,
605.389807057181));
#150991=CARTESIAN_POINT('Ctrl Pts',(13.3947726768058,-12.2109487310903,
603.895689410122));
#150992=CARTESIAN_POINT('Ctrl Pts',(12.1588589765331,-13.3376329379985,
602.401571763063));
#150993=CARTESIAN_POINT('Ctrl Pts',(10.9229452762603,-14.4643171449067,
600.907454116004));
#150994=CARTESIAN_POINT('Ctrl Pts',(9.50104767561053,-15.3447188656481,
599.413336468945));
#150995=CARTESIAN_POINT('Ctrl Pts',(8.07915007496071,-16.2251205863895,
597.919218821887));
#150996=CARTESIAN_POINT('Ctrl Pts',(6.51968959134574,-16.8292587962898,
596.425101174828));
#150997=CARTESIAN_POINT('Ctrl Pts',(4.96022910773078,-17.4333970061901,
594.930983527769));
#150998=CARTESIAN_POINT('Ctrl Pts',(3.31631129755346,-17.7406985030951,
593.43686588071));
#150999=CARTESIAN_POINT('Ctrl Pts',(1.67239348737615,-18.048,591.942748233651));
#151000=CARTESIAN_POINT('Ctrl Pts',(0.,-18.048,590.448630586592));
#151001=CARTESIAN_POINT('Ctrl Pts',(-1.67239348737615,-18.048,588.954512939533));
#151002=CARTESIAN_POINT('Ctrl Pts',(-3.31631129755346,-17.7406985030951,
587.460395292475));
#151003=CARTESIAN_POINT('Ctrl Pts',(-4.96022910773077,-17.4333970061901,
585.966277645416));
#151004=CARTESIAN_POINT('Ctrl Pts',(-6.51968959134574,-16.8292587962898,
584.472159998357));
#151005=CARTESIAN_POINT('Ctrl Pts',(-8.07915007496071,-16.2251205863895,
582.978042351298));
#151006=CARTESIAN_POINT('Ctrl Pts',(-9.50104767561052,-15.3447188656481,
581.483924704239));
#151007=CARTESIAN_POINT('Ctrl Pts',(-10.9229452762603,-14.4643171449067,
579.989807057181));
#151008=CARTESIAN_POINT('Ctrl Pts',(-12.1588589765331,-13.3376329379985,
578.495689410122));
#151009=CARTESIAN_POINT('Ctrl Pts',(-13.3947726768058,-12.2109487310903,
577.001571763063));
#151010=CARTESIAN_POINT('Ctrl Pts',(-14.4026149179538,-10.8763499173728,
575.507454116004));
#151011=CARTESIAN_POINT('Ctrl Pts',(-15.4104571591017,-9.54175110365538,
574.013336468945));
#151012=CARTESIAN_POINT('Ctrl Pts',(-16.1559070823762,-8.04468584505497,
572.519218821886));
#151013=CARTESIAN_POINT('Ctrl Pts',(-16.9013570056506,-6.54762058645456,
571.025101174828));
#151014=CARTESIAN_POINT('Ctrl Pts',(-17.3590292079831,-4.93906964482095,
569.530983527769));
#151015=CARTESIAN_POINT('Ctrl Pts',(-17.8167014103155,-3.33051870318735,
568.03686588071));
#151016=CARTESIAN_POINT('Ctrl Pts',(-17.9710104137728,-1.66525935159368,
566.542748233651));
#151017=CARTESIAN_POINT('Ctrl Pts',(-18.1253194172301,-1.10985572039171E-15,
565.048630586592));
#151018=CARTESIAN_POINT('Ctrl Pts',(-17.9710104137728,1.66525935159367,
563.554512939533));
#151019=CARTESIAN_POINT('Ctrl Pts',(-17.8167014103155,3.33051870318735,
562.060395292475));
#151020=CARTESIAN_POINT('Ctrl Pts',(-17.3590292079831,4.93906964482096,
560.566277645416));
#151021=CARTESIAN_POINT('Ctrl Pts',(-16.9013570056506,6.54762058645456,
559.072159998357));
#151022=CARTESIAN_POINT('Ctrl Pts',(-16.1559070823762,8.04468584505497,
557.578042351298));
#151023=CARTESIAN_POINT('Ctrl Pts',(-15.4104571591017,9.54175110365538,
556.083924704239));
#151024=CARTESIAN_POINT('Ctrl Pts',(-14.4026149179538,10.8763499173728,
554.589807057181));
#151025=CARTESIAN_POINT('Ctrl Pts',(-13.3947726768058,12.2109487310903,
553.095689410122));
#151026=CARTESIAN_POINT('Ctrl Pts',(-12.1588589765331,13.3376329379985,
551.601571763063));
#151027=CARTESIAN_POINT('Ctrl Pts',(-10.9229452762603,14.4643171449067,
550.107454116004));
#151028=CARTESIAN_POINT('Ctrl Pts',(-9.50104767561052,15.3447188656481,
548.613336468945));
#151029=CARTESIAN_POINT('Ctrl Pts',(-8.07915007496071,16.2251205863895,
547.119218821887));
#151030=CARTESIAN_POINT('Ctrl Pts',(-6.51968959134574,16.8292587962898,
545.625101174828));
#151031=CARTESIAN_POINT('Ctrl Pts',(-4.96022910773078,17.4333970061901,
544.130983527769));
#151032=CARTESIAN_POINT('Ctrl Pts',(-3.31631129755346,17.7406985030951,
542.63686588071));
#151033=CARTESIAN_POINT('Ctrl Pts',(-1.67239348737615,18.048,541.142748233651));
#151034=CARTESIAN_POINT('Ctrl Pts',(-2.21024254310115E-15,18.048,539.648630586592));
#151035=CARTESIAN_POINT('Ctrl Pts',(1.67239348737616,18.048,538.154512939533));
#151036=CARTESIAN_POINT('Ctrl Pts',(3.31631129755346,17.7406985030951,536.660395292475));
#151037=CARTESIAN_POINT('Ctrl Pts',(4.96022910773077,17.4333970061901,535.166277645416));
#151038=CARTESIAN_POINT('Ctrl Pts',(6.51968959134575,16.8292587962898,533.672159998357));
#151039=CARTESIAN_POINT('Ctrl Pts',(8.07915007496071,16.2251205863895,532.178042351298));
#151040=CARTESIAN_POINT('Ctrl Pts',(9.50104767561053,15.3447188656481,530.683924704239));
#151041=CARTESIAN_POINT('Ctrl Pts',(10.9229452762603,14.4643171449067,529.18980705718));
#151042=CARTESIAN_POINT('Ctrl Pts',(12.1588589765331,13.3376329379985,527.695689410122));
#151043=CARTESIAN_POINT('Ctrl Pts',(13.3947726768058,12.2109487310903,526.201571763063));
#151044=CARTESIAN_POINT('Ctrl Pts',(14.4026149179538,10.8763499173728,524.707454116004));
#151045=CARTESIAN_POINT('Ctrl Pts',(15.4104571591017,9.54175110365538,523.213336468945));
#151046=CARTESIAN_POINT('Ctrl Pts',(16.1559070823762,8.04468584505496,521.719218821886));
#151047=CARTESIAN_POINT('Ctrl Pts',(16.9013570056506,6.54762058645456,520.225101174828));
#151048=CARTESIAN_POINT('Ctrl Pts',(17.3590292079831,4.93906964482096,518.730983527769));
#151049=CARTESIAN_POINT('Ctrl Pts',(17.8167014103155,3.33051870318735,517.23686588071));
#151050=CARTESIAN_POINT('Ctrl Pts',(17.9710104137728,1.66525935159367,515.742748233651));
#151051=CARTESIAN_POINT('Ctrl Pts',(18.1253194172301,3.32956716117513E-15,
514.248630586592));
#151052=CARTESIAN_POINT('Ctrl Pts',(17.9710104137728,-1.66525935159367,
512.754512939533));
#151053=CARTESIAN_POINT('Ctrl Pts',(17.8167014103155,-3.33051870318736,
511.260395292475));
#151054=CARTESIAN_POINT('Ctrl Pts',(17.3590292079831,-4.93906964482095,
509.766277645416));
#151055=CARTESIAN_POINT('Ctrl Pts',(16.9013570056506,-6.54762058645456,
508.272159998357));
#151056=CARTESIAN_POINT('Ctrl Pts',(16.1559070823762,-8.04468584505497,
506.778042351298));
#151057=CARTESIAN_POINT('Ctrl Pts',(15.4104571591017,-9.54175110365538,
505.283924704239));
#151058=CARTESIAN_POINT('Ctrl Pts',(14.4026149179538,-10.8763499173728,
503.78980705718));
#151059=CARTESIAN_POINT('Ctrl Pts',(13.3947726768058,-12.2109487310903,
502.295689410122));
#151060=CARTESIAN_POINT('Ctrl Pts',(12.1588589765331,-13.3376329379985,
500.801571763063));
#151061=CARTESIAN_POINT('Ctrl Pts',(10.9229452762603,-14.4643171449067,
499.307454116004));
#151062=CARTESIAN_POINT('Ctrl Pts',(9.50104767561053,-15.3447188656481,
497.813336468945));
#151063=CARTESIAN_POINT('Ctrl Pts',(8.07915007496071,-16.2251205863895,
496.319218821886));
#151064=CARTESIAN_POINT('Ctrl Pts',(6.51968959134574,-16.8292587962898,
494.825101174827));
#151065=CARTESIAN_POINT('Ctrl Pts',(4.96022910773078,-17.4333970061901,
493.330983527769));
#151066=CARTESIAN_POINT('Ctrl Pts',(3.31631129755346,-17.7406985030951,
491.83686588071));
#151067=CARTESIAN_POINT('Ctrl Pts',(1.67239348737615,-18.048,490.342748233651));
#151068=CARTESIAN_POINT('Ctrl Pts',(0.,-18.048,488.848630586592));
#151069=CARTESIAN_POINT('Ctrl Pts',(-1.67239348737615,-18.048,487.354512939533));
#151070=CARTESIAN_POINT('Ctrl Pts',(-3.31631129755346,-17.7406985030951,
485.860395292475));
#151071=CARTESIAN_POINT('Ctrl Pts',(-4.96022910773077,-17.4333970061901,
484.366277645416));
#151072=CARTESIAN_POINT('Ctrl Pts',(-6.51968959134574,-16.8292587962898,
482.872159998357));
#151073=CARTESIAN_POINT('Ctrl Pts',(-8.07915007496071,-16.2251205863895,
481.378042351298));
#151074=CARTESIAN_POINT('Ctrl Pts',(-9.50104767561052,-15.3447188656481,
479.883924704239));
#151075=CARTESIAN_POINT('Ctrl Pts',(-10.9229452762603,-14.4643171449067,
478.389807057181));
#151076=CARTESIAN_POINT('Ctrl Pts',(-12.1588589765331,-13.3376329379985,
476.895689410122));
#151077=CARTESIAN_POINT('Ctrl Pts',(-13.3947726768058,-12.2109487310903,
475.401571763063));
#151078=CARTESIAN_POINT('Ctrl Pts',(-14.4026149179538,-10.8763499173728,
473.907454116004));
#151079=CARTESIAN_POINT('Ctrl Pts',(-15.4104571591017,-9.54175110365538,
472.413336468945));
#151080=CARTESIAN_POINT('Ctrl Pts',(-16.1559070823762,-8.04468584505497,
470.919218821886));
#151081=CARTESIAN_POINT('Ctrl Pts',(-16.9013570056506,-6.54762058645456,
469.425101174828));
#151082=CARTESIAN_POINT('Ctrl Pts',(-17.3590292079831,-4.93906964482095,
467.930983527769));
#151083=CARTESIAN_POINT('Ctrl Pts',(-17.8167014103155,-3.33051870318735,
466.43686588071));
#151084=CARTESIAN_POINT('Ctrl Pts',(-17.9710104137728,-1.66525935159368,
464.942748233651));
#151085=CARTESIAN_POINT('Ctrl Pts',(-18.1253194172301,-1.10985572039171E-15,
463.448630586592));
#151086=CARTESIAN_POINT('Ctrl Pts',(-17.9710104137728,1.66525935159367,
461.954512939534));
#151087=CARTESIAN_POINT('Ctrl Pts',(-17.8167014103155,3.33051870318735,
460.460395292475));
#151088=CARTESIAN_POINT('Ctrl Pts',(-17.3590292079831,4.93906964482096,
458.966277645416));
#151089=CARTESIAN_POINT('Ctrl Pts',(-16.9013570056506,6.54762058645456,
457.472159998357));
#151090=CARTESIAN_POINT('Ctrl Pts',(-16.1559070823762,8.04468584505497,
455.978042351298));
#151091=CARTESIAN_POINT('Ctrl Pts',(-15.4104571591017,9.54175110365538,
454.483924704239));
#151092=CARTESIAN_POINT('Ctrl Pts',(-14.4026149179538,10.8763499173728,
452.989807057181));
#151093=CARTESIAN_POINT('Ctrl Pts',(-13.3947726768058,12.2109487310903,
451.495689410122));
#151094=CARTESIAN_POINT('Ctrl Pts',(-12.1588589765331,13.3376329379985,
450.001571763063));
#151095=CARTESIAN_POINT('Ctrl Pts',(-10.9229452762603,14.4643171449067,
448.507454116004));
#151096=CARTESIAN_POINT('Ctrl Pts',(-9.50104767561052,15.3447188656481,
447.013336468945));
#151097=CARTESIAN_POINT('Ctrl Pts',(-8.07915007496071,16.2251205863895,
445.519218821887));
#151098=CARTESIAN_POINT('Ctrl Pts',(-6.51968959134574,16.8292587962898,
444.025101174828));
#151099=CARTESIAN_POINT('Ctrl Pts',(-4.96022910773078,17.4333970061901,
442.530983527769));
#151100=CARTESIAN_POINT('Ctrl Pts',(-3.31631129755346,17.7406985030951,
441.03686588071));
#151101=CARTESIAN_POINT('Ctrl Pts',(-1.67239348737615,18.048,439.542748233651));
#151102=CARTESIAN_POINT('Ctrl Pts',(-2.21024254310115E-15,18.048,438.048630586592));
#151103=CARTESIAN_POINT('Ctrl Pts',(1.67239348737616,18.048,436.554512939533));
#151104=CARTESIAN_POINT('Ctrl Pts',(3.31631129755346,17.7406985030951,435.060395292475));
#151105=CARTESIAN_POINT('Ctrl Pts',(4.96022910773077,17.4333970061901,433.566277645416));
#151106=CARTESIAN_POINT('Ctrl Pts',(6.51968959134575,16.8292587962898,432.072159998357));
#151107=CARTESIAN_POINT('Ctrl Pts',(8.07915007496071,16.2251205863895,430.578042351298));
#151108=CARTESIAN_POINT('Ctrl Pts',(9.50104767561053,15.3447188656481,429.083924704239));
#151109=CARTESIAN_POINT('Ctrl Pts',(10.9229452762603,14.4643171449067,427.58980705718));
#151110=CARTESIAN_POINT('Ctrl Pts',(12.1588589765331,13.3376329379985,426.095689410122));
#151111=CARTESIAN_POINT('Ctrl Pts',(13.3947726768058,12.2109487310903,424.601571763063));
#151112=CARTESIAN_POINT('Ctrl Pts',(14.4026149179538,10.8763499173728,423.107454116004));
#151113=CARTESIAN_POINT('Ctrl Pts',(15.4104571591017,9.54175110365538,421.613336468945));
#151114=CARTESIAN_POINT('Ctrl Pts',(16.1559070823762,8.04468584505496,420.119218821886));
#151115=CARTESIAN_POINT('Ctrl Pts',(16.9013570056506,6.54762058645456,418.625101174828));
#151116=CARTESIAN_POINT('Ctrl Pts',(17.3590292079831,4.93906964482096,417.130983527769));
#151117=CARTESIAN_POINT('Ctrl Pts',(17.8167014103155,3.33051870318735,415.63686588071));
#151118=CARTESIAN_POINT('Ctrl Pts',(17.9710104137728,1.66525935159367,414.142748233651));
#151119=CARTESIAN_POINT('Ctrl Pts',(18.1253194172301,3.32956716117513E-15,
412.648630586592));
#151120=CARTESIAN_POINT('Ctrl Pts',(17.9710104137728,-1.66525935159367,
411.154512939534));
#151121=CARTESIAN_POINT('Ctrl Pts',(17.8167014103155,-3.33051870318736,
409.660395292475));
#151122=CARTESIAN_POINT('Ctrl Pts',(17.3590292079831,-4.93906964482095,
408.166277645416));
#151123=CARTESIAN_POINT('Ctrl Pts',(16.9013570056506,-6.54762058645456,
406.672159998357));
#151124=CARTESIAN_POINT('Ctrl Pts',(16.1559070823762,-8.04468584505497,
405.178042351298));
#151125=CARTESIAN_POINT('Ctrl Pts',(15.4104571591017,-9.54175110365538,
403.683924704239));
#151126=CARTESIAN_POINT('Ctrl Pts',(14.4026149179538,-10.8763499173728,
402.189807057181));
#151127=CARTESIAN_POINT('Ctrl Pts',(13.3947726768058,-12.2109487310903,
400.695689410122));
#151128=CARTESIAN_POINT('Ctrl Pts',(12.1588589765331,-13.3376329379985,
399.201571763063));
#151129=CARTESIAN_POINT('Ctrl Pts',(10.9229452762603,-14.4643171449067,
397.707454116004));
#151130=CARTESIAN_POINT('Ctrl Pts',(9.50104767561053,-15.3447188656481,
396.213336468945));
#151131=CARTESIAN_POINT('Ctrl Pts',(8.07915007496071,-16.2251205863895,
394.719218821887));
#151132=CARTESIAN_POINT('Ctrl Pts',(6.51968959134574,-16.8292587962898,
393.225101174828));
#151133=CARTESIAN_POINT('Ctrl Pts',(4.96022910773078,-17.4333970061901,
391.730983527769));
#151134=CARTESIAN_POINT('Ctrl Pts',(3.31631129755346,-17.7406985030951,
390.23686588071));
#151135=CARTESIAN_POINT('Ctrl Pts',(1.67239348737615,-18.048,388.742748233651));
#151136=CARTESIAN_POINT('Ctrl Pts',(0.,-18.048,387.248630586592));
#151137=CARTESIAN_POINT('Ctrl Pts',(-1.67239348737615,-18.048,385.754512939533));
#151138=CARTESIAN_POINT('Ctrl Pts',(-3.31631129755346,-17.7406985030951,
384.260395292475));
#151139=CARTESIAN_POINT('Ctrl Pts',(-4.96022910773077,-17.4333970061901,
382.766277645416));
#151140=CARTESIAN_POINT('Ctrl Pts',(-6.51968959134574,-16.8292587962898,
381.272159998357));
#151141=CARTESIAN_POINT('Ctrl Pts',(-8.07915007496071,-16.2251205863895,
379.778042351298));
#151142=CARTESIAN_POINT('Ctrl Pts',(-9.50104767561052,-15.3447188656481,
378.283924704239));
#151143=CARTESIAN_POINT('Ctrl Pts',(-10.9229452762603,-14.4643171449067,
376.789807057181));
#151144=CARTESIAN_POINT('Ctrl Pts',(-12.1588589765331,-13.3376329379985,
375.295689410122));
#151145=CARTESIAN_POINT('Ctrl Pts',(-13.3947726768058,-12.2109487310903,
373.801571763063));
#151146=CARTESIAN_POINT('Ctrl Pts',(-14.4026149179538,-10.8763499173728,
372.307454116004));
#151147=CARTESIAN_POINT('Ctrl Pts',(-15.4104571591017,-9.54175110365538,
370.813336468945));
#151148=CARTESIAN_POINT('Ctrl Pts',(-16.1559070823762,-8.04468584505497,
369.319218821886));
#151149=CARTESIAN_POINT('Ctrl Pts',(-16.9013570056506,-6.54762058645456,
367.825101174827));
#151150=CARTESIAN_POINT('Ctrl Pts',(-17.3590292079831,-4.93906964482095,
366.330983527769));
#151151=CARTESIAN_POINT('Ctrl Pts',(-17.8167014103155,-3.33051870318735,
364.83686588071));
#151152=CARTESIAN_POINT('Ctrl Pts',(-17.9710104137728,-1.66525935159368,
363.342748233651));
#151153=CARTESIAN_POINT('Ctrl Pts',(-18.1253194172301,-1.10985572039171E-15,
361.848630586592));
#151154=CARTESIAN_POINT('Ctrl Pts',(-17.9710104137728,1.66525935159367,
360.354512939533));
#151155=CARTESIAN_POINT('Ctrl Pts',(-17.8167014103155,3.33051870318735,
358.860395292475));
#151156=CARTESIAN_POINT('Ctrl Pts',(-17.3590292079831,4.93906964482096,
357.366277645416));
#151157=CARTESIAN_POINT('Ctrl Pts',(-16.9013570056506,6.54762058645456,
355.872159998357));
#151158=CARTESIAN_POINT('Ctrl Pts',(-16.1559070823762,8.04468584505497,
354.378042351298));
#151159=CARTESIAN_POINT('Ctrl Pts',(-15.4104571591017,9.54175110365538,
352.883924704239));
#151160=CARTESIAN_POINT('Ctrl Pts',(-14.4026149179538,10.8763499173728,
351.389807057181));
#151161=CARTESIAN_POINT('Ctrl Pts',(-13.3947726768058,12.2109487310903,
349.895689410122));
#151162=CARTESIAN_POINT('Ctrl Pts',(-12.1588589765331,13.3376329379985,
348.401571763063));
#151163=CARTESIAN_POINT('Ctrl Pts',(-10.9229452762603,14.4643171449067,
346.907454116004));
#151164=CARTESIAN_POINT('Ctrl Pts',(-9.50104767561052,15.3447188656481,
345.413336468945));
#151165=CARTESIAN_POINT('Ctrl Pts',(-8.07915007496071,16.2251205863895,
343.919218821887));
#151166=CARTESIAN_POINT('Ctrl Pts',(-6.51968959134574,16.8292587962898,
342.425101174828));
#151167=CARTESIAN_POINT('Ctrl Pts',(-4.96022910773078,17.4333970061901,
340.930983527769));
#151168=CARTESIAN_POINT('Ctrl Pts',(-3.31631129755346,17.7406985030951,
339.43686588071));
#151169=CARTESIAN_POINT('Ctrl Pts',(-1.67239348737615,18.048,337.942748233651));
#151170=CARTESIAN_POINT('Ctrl Pts',(-2.21024254310115E-15,18.048,336.448630586592));
#151171=CARTESIAN_POINT('Ctrl Pts',(1.67239348737616,18.048,334.954512939533));
#151172=CARTESIAN_POINT('Ctrl Pts',(3.31631129755346,17.7406985030951,333.460395292475));
#151173=CARTESIAN_POINT('Ctrl Pts',(4.96022910773077,17.4333970061901,331.966277645416));
#151174=CARTESIAN_POINT('Ctrl Pts',(6.51968959134575,16.8292587962898,330.472159998357));
#151175=CARTESIAN_POINT('Ctrl Pts',(8.07915007496071,16.2251205863895,328.978042351298));
#151176=CARTESIAN_POINT('Ctrl Pts',(9.50104767561053,15.3447188656481,327.483924704239));
#151177=CARTESIAN_POINT('Ctrl Pts',(10.9229452762603,14.4643171449067,325.98980705718));
#151178=CARTESIAN_POINT('Ctrl Pts',(12.1588589765331,13.3376329379985,324.495689410122));
#151179=CARTESIAN_POINT('Ctrl Pts',(13.3947726768058,12.2109487310903,323.001571763063));
#151180=CARTESIAN_POINT('Ctrl Pts',(14.4026149179538,10.8763499173728,321.507454116004));
#151181=CARTESIAN_POINT('Ctrl Pts',(15.4104571591017,9.54175110365538,320.013336468945));
#151182=CARTESIAN_POINT('Ctrl Pts',(16.1559070823762,8.04468584505496,318.519218821886));
#151183=CARTESIAN_POINT('Ctrl Pts',(16.9013570056506,6.54762058645456,317.025101174828));
#151184=CARTESIAN_POINT('Ctrl Pts',(17.3590292079831,4.93906964482096,315.530983527769));
#151185=CARTESIAN_POINT('Ctrl Pts',(17.8167014103155,3.33051870318735,314.03686588071));
#151186=CARTESIAN_POINT('Ctrl Pts',(17.9710104137728,1.66525935159367,312.542748233651));
#151187=CARTESIAN_POINT('Ctrl Pts',(18.1253194172301,3.32956716117513E-15,
311.048630586592));
#151188=CARTESIAN_POINT('Ctrl Pts',(17.9710104137728,-1.66525935159367,
309.554512939533));
#151189=CARTESIAN_POINT('Ctrl Pts',(17.8167014103155,-3.33051870318736,
308.060395292475));
#151190=CARTESIAN_POINT('Ctrl Pts',(17.3590292079831,-4.93906964482095,
306.566277645416));
#151191=CARTESIAN_POINT('Ctrl Pts',(16.9013570056506,-6.54762058645456,
305.072159998357));
#151192=CARTESIAN_POINT('Ctrl Pts',(16.1559070823762,-8.04468584505497,
303.578042351298));
#151193=CARTESIAN_POINT('Ctrl Pts',(15.4104571591017,-9.54175110365538,
302.083924704239));
#151194=CARTESIAN_POINT('Ctrl Pts',(14.4026149179538,-10.8763499173728,
300.58980705718));
#151195=CARTESIAN_POINT('Ctrl Pts',(13.3947726768058,-12.2109487310903,
299.095689410122));
#151196=CARTESIAN_POINT('Ctrl Pts',(12.1588589765331,-13.3376329379985,
297.601571763063));
#151197=CARTESIAN_POINT('Ctrl Pts',(10.9229452762603,-14.4643171449067,
296.107454116004));
#151198=CARTESIAN_POINT('Ctrl Pts',(9.50104767561053,-15.3447188656481,
294.613336468945));
#151199=CARTESIAN_POINT('Ctrl Pts',(8.07915007496071,-16.2251205863895,
293.119218821886));
#151200=CARTESIAN_POINT('Ctrl Pts',(6.51968959134574,-16.8292587962898,
291.625101174828));
#151201=CARTESIAN_POINT('Ctrl Pts',(4.96022910773078,-17.4333970061901,
290.130983527769));
#151202=CARTESIAN_POINT('Ctrl Pts',(3.31631129755346,-17.7406985030951,
288.63686588071));
#151203=CARTESIAN_POINT('Ctrl Pts',(1.67239348737615,-18.048,287.142748233651));
#151204=CARTESIAN_POINT('Ctrl Pts',(0.,-18.048,285.648630586592));
#151205=CARTESIAN_POINT('Ctrl Pts',(-1.67239348737615,-18.048,284.154512939534));
#151206=CARTESIAN_POINT('Ctrl Pts',(-3.31631129755346,-17.7406985030951,
282.660395292475));
#151207=CARTESIAN_POINT('Ctrl Pts',(-4.96022910773077,-17.4333970061901,
281.166277645416));
#151208=CARTESIAN_POINT('Ctrl Pts',(-6.51968959134574,-16.8292587962898,
279.672159998357));
#151209=CARTESIAN_POINT('Ctrl Pts',(-8.07915007496071,-16.2251205863895,
278.178042351298));
#151210=CARTESIAN_POINT('Ctrl Pts',(-9.50104767561052,-15.3447188656481,
276.683924704239));
#151211=CARTESIAN_POINT('Ctrl Pts',(-10.9229452762603,-14.4643171449067,
275.189807057181));
#151212=CARTESIAN_POINT('Ctrl Pts',(-12.1588589765331,-13.3376329379985,
273.695689410122));
#151213=CARTESIAN_POINT('Ctrl Pts',(-13.3947726768058,-12.2109487310903,
272.201571763063));
#151214=CARTESIAN_POINT('Ctrl Pts',(-14.4026149179538,-10.8763499173728,
270.707454116004));
#151215=CARTESIAN_POINT('Ctrl Pts',(-15.4104571591017,-9.54175110365538,
269.213336468945));
#151216=CARTESIAN_POINT('Ctrl Pts',(-16.1559070823762,-8.04468584505497,
267.719218821886));
#151217=CARTESIAN_POINT('Ctrl Pts',(-16.9013570056506,-6.54762058645456,
266.225101174828));
#151218=CARTESIAN_POINT('Ctrl Pts',(-17.3590292079831,-4.93906964482095,
264.730983527769));
#151219=CARTESIAN_POINT('Ctrl Pts',(-17.8167014103155,-3.33051870318735,
263.23686588071));
#151220=CARTESIAN_POINT('Ctrl Pts',(-17.9710104137728,-1.66525935159368,
261.742748233651));
#151221=CARTESIAN_POINT('Ctrl Pts',(-18.1253194172301,-1.10985572039171E-15,
260.248630586592));
#151222=CARTESIAN_POINT('Ctrl Pts',(-17.9710104137728,1.66525935159367,
258.754512939533));
#151223=CARTESIAN_POINT('Ctrl Pts',(-17.8167014103155,3.33051870318735,
257.260395292475));
#151224=CARTESIAN_POINT('Ctrl Pts',(-17.3590292079831,4.93906964482096,
255.766277645416));
#151225=CARTESIAN_POINT('Ctrl Pts',(-16.9013570056506,6.54762058645456,
254.272159998357));
#151226=CARTESIAN_POINT('Ctrl Pts',(-16.1559070823762,8.04468584505497,
252.778042351298));
#151227=CARTESIAN_POINT('Ctrl Pts',(-15.4104571591017,9.54175110365538,
251.283924704239));
#151228=CARTESIAN_POINT('Ctrl Pts',(-14.4026149179538,10.8763499173728,
249.78980705718));
#151229=CARTESIAN_POINT('Ctrl Pts',(-13.3947726768058,12.2109487310903,
248.295689410122));
#151230=CARTESIAN_POINT('Ctrl Pts',(-12.1588589765331,13.3376329379985,
246.801571763063));
#151231=CARTESIAN_POINT('Ctrl Pts',(-10.9229452762603,14.4643171449067,
245.307454116004));
#151232=CARTESIAN_POINT('Ctrl Pts',(-9.50104767561052,15.3447188656481,
243.813336468945));
#151233=CARTESIAN_POINT('Ctrl Pts',(-8.07915007496071,16.2251205863895,
242.319218821886));
#151234=CARTESIAN_POINT('Ctrl Pts',(-6.51968959134574,16.8292587962898,
240.825101174827));
#151235=CARTESIAN_POINT('Ctrl Pts',(-4.96022910773078,17.4333970061901,
239.330983527769));
#151236=CARTESIAN_POINT('Ctrl Pts',(-3.31631129755346,17.7406985030951,
237.83686588071));
#151237=CARTESIAN_POINT('Ctrl Pts',(-1.67239348737615,18.048,236.342748233651));
#151238=CARTESIAN_POINT('Ctrl Pts',(-2.21024254310115E-15,18.048,234.848630586592));
#151239=CARTESIAN_POINT('Ctrl Pts',(1.67239348737616,18.048,233.354512939533));
#151240=CARTESIAN_POINT('Ctrl Pts',(3.31631129755346,17.7406985030951,231.860395292475));
#151241=CARTESIAN_POINT('Ctrl Pts',(4.96022910773077,17.4333970061901,230.366277645416));
#151242=CARTESIAN_POINT('Ctrl Pts',(6.51968959134575,16.8292587962898,228.872159998357));
#151243=CARTESIAN_POINT('Ctrl Pts',(8.07915007496071,16.2251205863895,227.378042351298));
#151244=CARTESIAN_POINT('Ctrl Pts',(9.50104767561053,15.3447188656481,225.883924704239));
#151245=CARTESIAN_POINT('Ctrl Pts',(10.9229452762603,14.4643171449067,224.389807057181));
#151246=CARTESIAN_POINT('Ctrl Pts',(12.1588589765331,13.3376329379985,222.895689410122));
#151247=CARTESIAN_POINT('Ctrl Pts',(13.3947726768058,12.2109487310903,221.401571763063));
#151248=CARTESIAN_POINT('Ctrl Pts',(14.4026149179538,10.8763499173728,219.907454116004));
#151249=CARTESIAN_POINT('Ctrl Pts',(15.4104571591017,9.54175110365538,218.413336468945));
#151250=CARTESIAN_POINT('Ctrl Pts',(16.1559070823762,8.04468584505496,216.919218821886));
#151251=CARTESIAN_POINT('Ctrl Pts',(16.9013570056506,6.54762058645456,215.425101174828));
#151252=CARTESIAN_POINT('Ctrl Pts',(17.3590292079831,4.93906964482096,213.930983527769));
#151253=CARTESIAN_POINT('Ctrl Pts',(17.8167014103155,3.33051870318735,212.43686588071));
#151254=CARTESIAN_POINT('Ctrl Pts',(17.9710104137728,1.66525935159367,210.942748233651));
#151255=CARTESIAN_POINT('Ctrl Pts',(18.1253194172301,3.32956716117513E-15,
209.448630586592));
#151256=CARTESIAN_POINT('Ctrl Pts',(17.9710104137728,-1.66525935159367,
207.954512939533));
#151257=CARTESIAN_POINT('Ctrl Pts',(17.8167014103155,-3.33051870318736,
206.460395292475));
#151258=CARTESIAN_POINT('Ctrl Pts',(17.3590292079831,-4.93906964482095,
204.966277645416));
#151259=CARTESIAN_POINT('Ctrl Pts',(16.9013570056506,-6.54762058645456,
203.472159998357));
#151260=CARTESIAN_POINT('Ctrl Pts',(16.1559070823762,-8.04468584505497,
201.978042351298));
#151261=CARTESIAN_POINT('Ctrl Pts',(15.4104571591017,-9.54175110365538,
200.483924704239));
#151262=CARTESIAN_POINT('Ctrl Pts',(14.4026149179538,-10.8763499173728,
198.989807057181));
#151263=CARTESIAN_POINT('Ctrl Pts',(13.3947726768058,-12.2109487310903,
197.495689410122));
#151264=CARTESIAN_POINT('Ctrl Pts',(12.1588589765331,-13.3376329379985,
196.001571763063));
#151265=CARTESIAN_POINT('Ctrl Pts',(10.9229452762603,-14.4643171449067,
194.507454116004));
#151266=CARTESIAN_POINT('Ctrl Pts',(9.50104767561053,-15.3447188656481,
193.013336468945));
#151267=CARTESIAN_POINT('Ctrl Pts',(8.07915007496071,-16.2251205863895,
191.519218821886));
#151268=CARTESIAN_POINT('Ctrl Pts',(6.51968959134574,-16.8292587962898,
190.025101174828));
#151269=CARTESIAN_POINT('Ctrl Pts',(4.96022910773078,-17.4333970061901,
188.530983527769));
#151270=CARTESIAN_POINT('Ctrl Pts',(3.31631129755346,-17.7406985030951,
187.03686588071));
#151271=CARTESIAN_POINT('Ctrl Pts',(1.67239348737615,-18.048,185.542748233651));
#151272=CARTESIAN_POINT('Ctrl Pts',(0.,-18.048,184.048630586592));
#151273=CARTESIAN_POINT('Ctrl Pts',(-1.67239348737615,-18.048,182.554512939533));
#151274=CARTESIAN_POINT('Ctrl Pts',(-3.31631129755346,-17.7406985030951,
181.060395292475));
#151275=CARTESIAN_POINT('Ctrl Pts',(-4.96022910773077,-17.4333970061901,
179.566277645416));
#151276=CARTESIAN_POINT('Ctrl Pts',(-6.51968959134574,-16.8292587962898,
178.072159998357));
#151277=CARTESIAN_POINT('Ctrl Pts',(-8.07915007496071,-16.2251205863895,
176.578042351298));
#151278=CARTESIAN_POINT('Ctrl Pts',(-9.50104767561052,-15.3447188656481,
175.083924704239));
#151279=CARTESIAN_POINT('Ctrl Pts',(-10.9229452762603,-14.4643171449067,
173.58980705718));
#151280=CARTESIAN_POINT('Ctrl Pts',(-12.1588589765331,-13.3376329379985,
172.095689410122));
#151281=CARTESIAN_POINT('Ctrl Pts',(-13.3947726768058,-12.2109487310903,
170.601571763063));
#151282=CARTESIAN_POINT('Ctrl Pts',(-14.4026149179538,-10.8763499173728,
169.107454116004));
#151283=CARTESIAN_POINT('Ctrl Pts',(-15.4104571591017,-9.54175110365538,
167.613336468945));
#151284=CARTESIAN_POINT('Ctrl Pts',(-16.1559070823762,-8.04468584505497,
166.119218821886));
#151285=CARTESIAN_POINT('Ctrl Pts',(-16.9013570056506,-6.54762058645456,
164.625101174828));
#151286=CARTESIAN_POINT('Ctrl Pts',(-17.3590292079831,-4.93906964482095,
163.130983527769));
#151287=CARTESIAN_POINT('Ctrl Pts',(-17.8167014103155,-3.33051870318735,
161.63686588071));
#151288=CARTESIAN_POINT('Ctrl Pts',(-17.9710104137728,-1.66525935159368,
160.142748233651));
#151289=CARTESIAN_POINT('Ctrl Pts',(-18.1253194172301,-1.10985572039171E-15,
158.648630586592));
#151290=CARTESIAN_POINT('Ctrl Pts',(-17.9710104137728,1.66525935159367,
157.154512939534));
#151291=CARTESIAN_POINT('Ctrl Pts',(-17.8167014103155,3.33051870318735,
155.660395292475));
#151292=CARTESIAN_POINT('Ctrl Pts',(-17.3590292079831,4.93906964482096,
154.166277645416));
#151293=CARTESIAN_POINT('Ctrl Pts',(-16.9013570056506,6.54762058645456,
152.672159998357));
#151294=CARTESIAN_POINT('Ctrl Pts',(-16.1559070823762,8.04468584505497,
151.178042351298));
#151295=CARTESIAN_POINT('Ctrl Pts',(-15.4104571591017,9.54175110365538,
149.683924704239));
#151296=CARTESIAN_POINT('Ctrl Pts',(-14.4026149179538,10.8763499173728,
148.189807057181));
#151297=CARTESIAN_POINT('Ctrl Pts',(-13.3947726768058,12.2109487310903,
146.695689410122));
#151298=CARTESIAN_POINT('Ctrl Pts',(-12.1588589765331,13.3376329379985,
145.201571763063));
#151299=CARTESIAN_POINT('Ctrl Pts',(-10.9229452762603,14.4643171449067,
143.707454116004));
#151300=CARTESIAN_POINT('Ctrl Pts',(-9.50104767561052,15.3447188656481,
142.213336468945));
#151301=CARTESIAN_POINT('Ctrl Pts',(-8.07915007496071,16.2251205863895,
140.719218821886));
#151302=CARTESIAN_POINT('Ctrl Pts',(-6.51968959134574,16.8292587962898,
139.225101174828));
#151303=CARTESIAN_POINT('Ctrl Pts',(-4.96022910773078,17.4333970061901,
137.730983527769));
#151304=CARTESIAN_POINT('Ctrl Pts',(-3.31631129755346,17.7406985030951,
136.23686588071));
#151305=CARTESIAN_POINT('Ctrl Pts',(-1.67239348737615,18.048,134.742748233651));
#151306=CARTESIAN_POINT('Ctrl Pts',(-2.21024254310115E-15,18.048,133.248630586592));
#151307=CARTESIAN_POINT('Ctrl Pts',(1.67239348737616,18.048,131.754512939533));
#151308=CARTESIAN_POINT('Ctrl Pts',(3.31631129755346,17.7406985030951,130.260395292475));
#151309=CARTESIAN_POINT('Ctrl Pts',(4.96022910773077,17.4333970061901,128.766277645416));
#151310=CARTESIAN_POINT('Ctrl Pts',(6.51968959134575,16.8292587962898,127.272159998357));
#151311=CARTESIAN_POINT('Ctrl Pts',(8.07915007496071,16.2251205863895,125.778042351298));
#151312=CARTESIAN_POINT('Ctrl Pts',(9.50104767561053,15.3447188656481,124.283924704239));
#151313=CARTESIAN_POINT('Ctrl Pts',(10.9229452762603,14.4643171449067,122.78980705718));
#151314=CARTESIAN_POINT('Ctrl Pts',(12.1588589765331,13.3376329379985,121.295689410122));
#151315=CARTESIAN_POINT('Ctrl Pts',(13.3947726768058,12.2109487310903,119.801571763063));
#151316=CARTESIAN_POINT('Ctrl Pts',(14.4026149179538,10.8763499173728,118.307454116004));
#151317=CARTESIAN_POINT('Ctrl Pts',(15.4104571591017,9.54175110365538,116.813336468945));
#151318=CARTESIAN_POINT('Ctrl Pts',(16.1559070823762,8.04468584505496,115.319218821886));
#151319=CARTESIAN_POINT('Ctrl Pts',(16.9013570056506,6.54762058645456,113.825101174828));
#151320=CARTESIAN_POINT('Ctrl Pts',(17.3590292079831,4.93906964482096,112.330983527769));
#151321=CARTESIAN_POINT('Ctrl Pts',(17.8167014103155,3.33051870318735,110.83686588071));
#151322=CARTESIAN_POINT('Ctrl Pts',(17.9710104137728,1.66525935159367,109.342748233651));
#151323=CARTESIAN_POINT('Ctrl Pts',(18.1253194172301,3.32956716117513E-15,
107.848630586592));
#151324=CARTESIAN_POINT('Ctrl Pts',(17.9710104137728,-1.66525935159367,
106.354512939533));
#151325=CARTESIAN_POINT('Ctrl Pts',(17.8167014103155,-3.33051870318736,
104.860395292475));
#151326=CARTESIAN_POINT('Ctrl Pts',(17.3590292079831,-4.93906964482095,
103.366277645416));
#151327=CARTESIAN_POINT('Ctrl Pts',(16.9013570056506,-6.54762058645456,
101.872159998357));
#151328=CARTESIAN_POINT('Ctrl Pts',(16.1559070823762,-8.04468584505497,
100.378042351298));
#151329=CARTESIAN_POINT('Ctrl Pts',(15.4104571591017,-9.54175110365538,
98.8839247042392));
#151330=CARTESIAN_POINT('Ctrl Pts',(14.4026149179538,-10.8763499173728,
97.3898070571806));
#151331=CARTESIAN_POINT('Ctrl Pts',(13.3947726768058,-12.2109487310903,
95.8956894101217));
#151332=CARTESIAN_POINT('Ctrl Pts',(12.1588589765331,-13.3376329379985,
94.4015717630628));
#151333=CARTESIAN_POINT('Ctrl Pts',(10.9229452762603,-14.4643171449067,
92.907454116004));
#151334=CARTESIAN_POINT('Ctrl Pts',(9.50104767561053,-15.3447188656481,
91.4133364689451));
#151335=CARTESIAN_POINT('Ctrl Pts',(8.07915007496071,-16.2251205863895,
89.9192188218865));
#151336=CARTESIAN_POINT('Ctrl Pts',(6.51968959134574,-16.8292587962898,
88.4251011748276));
#151337=CARTESIAN_POINT('Ctrl Pts',(4.96022910773078,-17.4333970061901,
86.9309835277687));
#151338=CARTESIAN_POINT('Ctrl Pts',(3.31631129755346,-17.7406985030951,
85.4368658807099));
#151339=CARTESIAN_POINT('Ctrl Pts',(1.67239348737615,-18.048,83.942748233651));
#151340=CARTESIAN_POINT('Ctrl Pts',(0.,-18.048,82.4486305865924));
#151341=CARTESIAN_POINT('Ctrl Pts',(-1.67239348737615,-18.048,80.9545129395335));
#151342=CARTESIAN_POINT('Ctrl Pts',(-3.31631129755346,-17.7406985030951,
79.4603952924746));
#151343=CARTESIAN_POINT('Ctrl Pts',(-4.96022910773077,-17.4333970061901,
77.9662776454158));
#151344=CARTESIAN_POINT('Ctrl Pts',(-6.51968959134574,-16.8292587962898,
76.4721599983569));
#151345=CARTESIAN_POINT('Ctrl Pts',(-8.07915007496071,-16.2251205863895,
74.9780423512982));
#151346=CARTESIAN_POINT('Ctrl Pts',(-9.50104767561052,-15.3447188656481,
73.4839247042394));
#151347=CARTESIAN_POINT('Ctrl Pts',(-10.9229452762603,-14.4643171449067,
71.9898070571805));
#151348=CARTESIAN_POINT('Ctrl Pts',(-12.1588589765331,-13.3376329379985,
70.4956894101216));
#151349=CARTESIAN_POINT('Ctrl Pts',(-13.3947726768058,-12.2109487310903,
69.0015717630628));
#151350=CARTESIAN_POINT('Ctrl Pts',(-14.4026149179538,-10.8763499173728,
67.5074541160041));
#151351=CARTESIAN_POINT('Ctrl Pts',(-15.4104571591017,-9.54175110365538,
66.0133364689453));
#151352=CARTESIAN_POINT('Ctrl Pts',(-16.1559070823762,-8.04468584505497,
64.5192188218864));
#151353=CARTESIAN_POINT('Ctrl Pts',(-16.9013570056506,-6.54762058645456,
63.0251011748275));
#151354=CARTESIAN_POINT('Ctrl Pts',(-17.3590292079831,-4.93906964482095,
61.5309835277687));
#151355=CARTESIAN_POINT('Ctrl Pts',(-17.8167014103155,-3.33051870318735,
60.03686588071));
#151356=CARTESIAN_POINT('Ctrl Pts',(-17.9710104137728,-1.66525935159368,
58.5427482336511));
#151357=CARTESIAN_POINT('Ctrl Pts',(-18.1253194172301,-1.10985572039171E-15,
57.0486305865923));
#151358=CARTESIAN_POINT('Ctrl Pts',(-17.9710104137728,1.66525935159367,
55.5545129395334));
#151359=CARTESIAN_POINT('Ctrl Pts',(-17.8167014103155,3.33051870318735,
54.0603952924745));
#151360=CARTESIAN_POINT('Ctrl Pts',(-17.3590292079831,4.93906964482096,
52.5662776454159));
#151361=CARTESIAN_POINT('Ctrl Pts',(-16.9013570056506,6.54762058645456,
51.072159998357));
#151362=CARTESIAN_POINT('Ctrl Pts',(-16.1559070823762,8.04468584505497,
49.5780423512981));
#151363=CARTESIAN_POINT('Ctrl Pts',(-15.4104571591017,9.54175110365538,
48.0839247042393));
#151364=CARTESIAN_POINT('Ctrl Pts',(-14.4026149179538,10.8763499173728,
46.5898070571804));
#151365=CARTESIAN_POINT('Ctrl Pts',(-13.3947726768058,12.2109487310903,
45.0956894101218));
#151366=CARTESIAN_POINT('Ctrl Pts',(-12.1588589765331,13.3376329379985,
43.6015717630629));
#151367=CARTESIAN_POINT('Ctrl Pts',(-10.9229452762603,14.4643171449067,
42.107454116004));
#151368=CARTESIAN_POINT('Ctrl Pts',(-9.50104767561052,15.3447188656481,
40.6133364689452));
#151369=CARTESIAN_POINT('Ctrl Pts',(-8.07915007496071,16.2251205863895,
39.1192188218863));
#151370=CARTESIAN_POINT('Ctrl Pts',(-6.51968959134574,16.8292587962898,
37.6251011748276));
#151371=CARTESIAN_POINT('Ctrl Pts',(-4.96022910773078,17.4333970061901,
36.1309835277688));
#151372=CARTESIAN_POINT('Ctrl Pts',(-3.31631129755346,17.7406985030951,
34.6368658807099));
#151373=CARTESIAN_POINT('Ctrl Pts',(-1.67239348737615,18.048,33.142748233651));
#151374=CARTESIAN_POINT('Ctrl Pts',(-2.21024254310115E-15,18.048,31.6486305865922));
#151375=CARTESIAN_POINT('Ctrl Pts',(1.67239348737616,18.048,30.1545129395335));
#151376=CARTESIAN_POINT('Ctrl Pts',(3.31631129755346,17.7406985030951,28.6603952924747));
#151377=CARTESIAN_POINT('Ctrl Pts',(4.96022910773077,17.4333970061901,27.1662776454158));
#151378=CARTESIAN_POINT('Ctrl Pts',(6.51968959134575,16.8292587962898,25.6721599983569));
#151379=CARTESIAN_POINT('Ctrl Pts',(8.07915007496071,16.2251205863895,24.1780423512981));
#151380=CARTESIAN_POINT('Ctrl Pts',(9.50104767561053,15.3447188656481,22.6839247042394));
#151381=CARTESIAN_POINT('Ctrl Pts',(10.9229452762603,14.4643171449067,21.1898070571805));
#151382=CARTESIAN_POINT('Ctrl Pts',(12.1588589765331,13.3376329379985,19.6956894101217));
#151383=CARTESIAN_POINT('Ctrl Pts',(13.3947726768058,12.2109487310903,18.2015717630628));
#151384=CARTESIAN_POINT('Ctrl Pts',(14.4026149179538,10.8763499173728,16.7074541160039));
#151385=CARTESIAN_POINT('Ctrl Pts',(15.4104571591017,9.54175110365538,15.2133364689453));
#151386=CARTESIAN_POINT('Ctrl Pts',(16.1559070823762,8.04468584505496,13.7192188218864));
#151387=CARTESIAN_POINT('Ctrl Pts',(16.9013570056506,6.54762058645456,12.2251011748276));
#151388=CARTESIAN_POINT('Ctrl Pts',(17.3590292079831,4.93906964482096,10.7309835277687));
#151389=CARTESIAN_POINT('Ctrl Pts',(17.8167014103155,3.33051870318735,9.23686588070982));
#151390=CARTESIAN_POINT('Ctrl Pts',(17.9710104137728,1.66525935159367,7.74274823365118));
#151391=CARTESIAN_POINT('Ctrl Pts',(18.1253194172301,3.32956716117513E-15,
6.24863058659231));
#151392=CARTESIAN_POINT('Ctrl Pts',(17.9710104137728,-1.66525935159367,
4.75451293953344));
#151393=CARTESIAN_POINT('Ctrl Pts',(17.8167014103155,-3.33051870318736,
3.26039529247457));
#151394=CARTESIAN_POINT('Ctrl Pts',(17.3590292079831,-4.93906964482095,
1.7662776454157));
#151395=CARTESIAN_POINT('Ctrl Pts',(16.9013570056506,-6.54762058645456,
0.272159998357058));
#151396=CARTESIAN_POINT('Ctrl Pts',(16.1559070823762,-8.04468584505497,
-1.22195764870181));
#151397=CARTESIAN_POINT('Ctrl Pts',(15.4104571591017,-9.54175110365538,
-2.71607529576068));
#151398=CARTESIAN_POINT('Ctrl Pts',(14.4026149179538,-10.8763499173728,
-4.21019294281955));
#151399=CARTESIAN_POINT('Ctrl Pts',(13.3947726768058,-12.2109487310903,
-5.70431058987841));
#151400=CARTESIAN_POINT('Ctrl Pts',(12.1588589765331,-13.3376329379985,
-7.19842823693706));
#151401=CARTESIAN_POINT('Ctrl Pts',(10.9229452762603,-14.4643171449067,
-8.69254588399593));
#151402=CARTESIAN_POINT('Ctrl Pts',(9.50104767561053,-15.3447188656481,
-10.1866635310548));
#151403=CARTESIAN_POINT('Ctrl Pts',(8.07915007496071,-16.2251205863895,
-11.6807811781137));
#151404=CARTESIAN_POINT('Ctrl Pts',(6.51968959134574,-16.8292587962898,
-13.1748988251725));
#151405=CARTESIAN_POINT('Ctrl Pts',(4.96022910773078,-17.4333970061901,
-14.6690164722312));
#151406=CARTESIAN_POINT('Ctrl Pts',(3.31631129755346,-17.7406985030951,
-16.16313411929));
#151407=CARTESIAN_POINT('Ctrl Pts',(1.67239348737615,-18.048,-17.6572517663489));
#151408=CARTESIAN_POINT('Ctrl Pts',(0.,-18.048,-19.1513694134078));
#151409=CARTESIAN_POINT('Ctrl Pts',(-1.67239348737615,-18.048,-20.6454870604667));
#151410=CARTESIAN_POINT('Ctrl Pts',(-3.31631129755346,-17.7406985030951,
-22.1396047075253));
#151411=CARTESIAN_POINT('Ctrl Pts',(-4.96022910773077,-17.4333970061901,
-23.6337223545842));
#151412=CARTESIAN_POINT('Ctrl Pts',(-6.51968959134574,-16.8292587962898,
-25.127840001643));
#151413=CARTESIAN_POINT('Ctrl Pts',(-8.07915007496071,-16.2251205863895,
-26.6219576487019));
#151414=CARTESIAN_POINT('Ctrl Pts',(-9.50104767561052,-15.3447188656481,
-28.1160752957608));
#151415=CARTESIAN_POINT('Ctrl Pts',(-10.9229452762603,-14.4643171449067,
-29.6101929428194));
#151416=CARTESIAN_POINT('Ctrl Pts',(-12.1588589765331,-13.3376329379985,
-31.1043105898783));
#151417=CARTESIAN_POINT('Ctrl Pts',(-13.3947726768058,-12.2109487310903,
-32.5984282369372));
#151418=CARTESIAN_POINT('Ctrl Pts',(-14.4026149179538,-10.8763499173728,
-34.092545883996));
#151419=CARTESIAN_POINT('Ctrl Pts',(-15.4104571591017,-9.54175110365538,
-35.5866635310549));
#151420=CARTESIAN_POINT('Ctrl Pts',(-16.1559070823762,-8.04468584505497,
-37.0807811781135));
#151421=CARTESIAN_POINT('Ctrl Pts',(-16.9013570056506,-6.54762058645456,
-38.5748988251724));
#151422=CARTESIAN_POINT('Ctrl Pts',(-17.3590292079831,-4.93906964482095,
-40.0690164722313));
#151423=CARTESIAN_POINT('Ctrl Pts',(-17.8167014103155,-3.33051870318735,
-41.5631341192901));
#151424=CARTESIAN_POINT('Ctrl Pts',(-17.9710104137728,-1.66525935159368,
-43.057251766349));
#151425=CARTESIAN_POINT('Ctrl Pts',(-18.1253194172301,-1.10985572039171E-15,
-44.5513694134076));
#151426=CARTESIAN_POINT('Ctrl Pts',(-17.9710104137728,1.66525935159367,
-46.0454870604665));
#151427=CARTESIAN_POINT('Ctrl Pts',(-17.8167014103155,3.33051870318735,
-47.5396047075254));
#151428=CARTESIAN_POINT('Ctrl Pts',(-17.3590292079831,4.93906964482096,
-49.0337223545843));
#151429=CARTESIAN_POINT('Ctrl Pts',(-16.9013570056506,6.54762058645456,
-50.5278400016431));
#151430=CARTESIAN_POINT('Ctrl Pts',(-16.1559070823762,8.04468584505497,
-52.0219576487018));
#151431=CARTESIAN_POINT('Ctrl Pts',(-15.4104571591017,9.54175110365538,
-53.5160752957606));
#151432=CARTESIAN_POINT('Ctrl Pts',(-14.4026149179538,10.8763499173728,
-55.0101929428195));
#151433=CARTESIAN_POINT('Ctrl Pts',(-13.3947726768058,12.2109487310903,
-56.5043105898784));
#151434=CARTESIAN_POINT('Ctrl Pts',(-12.1588589765331,13.3376329379985,
-57.9984282369372));
#151435=CARTESIAN_POINT('Ctrl Pts',(-10.9229452762603,14.4643171449067,
-59.4925458839959));
#151436=CARTESIAN_POINT('Ctrl Pts',(-9.50104767561052,15.3447188656481,
-60.9866635310548));
#151437=CARTESIAN_POINT('Ctrl Pts',(-8.07915007496071,16.2251205863895,
-62.4807811781136));
#151438=CARTESIAN_POINT('Ctrl Pts',(-6.51968959134574,16.8292587962898,
-63.9748988251725));
#151439=CARTESIAN_POINT('Ctrl Pts',(-4.96022910773078,17.4333970061901,
-65.4690164722314));
#151440=CARTESIAN_POINT('Ctrl Pts',(-3.31631129755346,17.7406985030951,
-66.96313411929));
#151441=CARTESIAN_POINT('Ctrl Pts',(-1.67239348737615,18.048,-68.4572517663489));
#151442=CARTESIAN_POINT('Ctrl Pts',(-2.21024254310115E-15,18.048,-69.9513694134077));
#151443=CARTESIAN_POINT('Ctrl Pts',(1.67239348737616,18.048,-71.4454870604666));
#151444=CARTESIAN_POINT('Ctrl Pts',(3.31631129755346,17.7406985030951,-72.9396047075255));
#151445=CARTESIAN_POINT('Ctrl Pts',(4.96022910773077,17.4333970061901,-74.4337223545841));
#151446=CARTESIAN_POINT('Ctrl Pts',(6.51968959134575,16.8292587962898,-75.927840001643));
#151447=CARTESIAN_POINT('Ctrl Pts',(8.07915007496071,16.2251205863895,-77.4219576487019));
#151448=CARTESIAN_POINT('Ctrl Pts',(9.50104767561053,15.3447188656481,-78.9160752957607));
#151449=CARTESIAN_POINT('Ctrl Pts',(10.9229452762603,14.4643171449067,-80.4101929428196));
#151450=CARTESIAN_POINT('Ctrl Pts',(12.1588589765331,13.3376329379985,-81.9043105898782));
#151451=CARTESIAN_POINT('Ctrl Pts',(13.3947726768058,12.2109487310903,-83.3984282369371));
#151452=CARTESIAN_POINT('Ctrl Pts',(14.4026149179538,10.8763499173728,-84.892545883996));
#151453=CARTESIAN_POINT('Ctrl Pts',(15.4104571591017,9.54175110365538,-86.3866635310549));
#151454=CARTESIAN_POINT('Ctrl Pts',(16.1559070823762,8.04468584505496,-87.8807811781137));
#151455=CARTESIAN_POINT('Ctrl Pts',(16.9013570056506,6.54762058645456,-89.3748988251724));
#151456=CARTESIAN_POINT('Ctrl Pts',(17.3590292079831,4.93906964482096,-90.8690164722312));
#151457=CARTESIAN_POINT('Ctrl Pts',(17.8167014103155,3.33051870318735,-92.3631341192901));
#151458=CARTESIAN_POINT('Ctrl Pts',(17.9710104137728,1.66525935159367,-93.857251766349));
#151459=CARTESIAN_POINT('Ctrl Pts',(18.1253194172301,3.32956716117513E-15,
-95.3513694134078));
#151460=CARTESIAN_POINT('Ctrl Pts',(17.9710104137728,-1.66525935159367,
-96.8454870604665));
#151461=CARTESIAN_POINT('Ctrl Pts',(17.8167014103155,-3.33051870318736,
-98.3396047075254));
#151462=CARTESIAN_POINT('Ctrl Pts',(17.3590292079831,-4.93906964482095,
-99.8337223545842));
#151463=CARTESIAN_POINT('Ctrl Pts',(16.9013570056506,-6.54762058645456,
-101.327840001643));
#151464=CARTESIAN_POINT('Ctrl Pts',(16.1559070823762,-8.04468584505497,
-102.821957648702));
#151465=CARTESIAN_POINT('Ctrl Pts',(15.4104571591017,-9.54175110365538,
-104.316075295761));
#151466=CARTESIAN_POINT('Ctrl Pts',(14.4026149179538,-10.8763499173728,
-105.810192942819));
#151467=CARTESIAN_POINT('Ctrl Pts',(13.3947726768058,-12.2109487310903,
-107.304310589878));
#151468=CARTESIAN_POINT('Ctrl Pts',(12.1588589765331,-13.3376329379985,
-108.798428236937));
#151469=CARTESIAN_POINT('Ctrl Pts',(10.9229452762603,-14.4643171449067,
-110.292545883996));
#151470=CARTESIAN_POINT('Ctrl Pts',(9.50104767561053,-15.3447188656481,
-111.786663531055));
#151471=CARTESIAN_POINT('Ctrl Pts',(8.07915007496071,-16.2251205863895,
-113.280781178114));
#151472=CARTESIAN_POINT('Ctrl Pts',(6.51968959134574,-16.8292587962898,
-114.774898825172));
#151473=CARTESIAN_POINT('Ctrl Pts',(4.96022910773078,-17.4333970061901,
-116.269016472231));
#151474=CARTESIAN_POINT('Ctrl Pts',(3.31631129755346,-17.7406985030951,
-117.76313411929));
#151475=CARTESIAN_POINT('Ctrl Pts',(1.67239348737615,-18.048,-119.257251766349));
#151476=CARTESIAN_POINT('Ctrl Pts',(0.,-18.048,-120.751369413408));
#151477=CARTESIAN_POINT('Ctrl Pts',(-1.67239348737615,-18.048,-122.245487060467));
#151478=CARTESIAN_POINT('Ctrl Pts',(-3.31631129755346,-17.7406985030951,
-123.739604707525));
#151479=CARTESIAN_POINT('Ctrl Pts',(-4.96022910773077,-17.4333970061901,
-125.233722354584));
#151480=CARTESIAN_POINT('Ctrl Pts',(-6.51968959134574,-16.8292587962898,
-126.727840001643));
#151481=CARTESIAN_POINT('Ctrl Pts',(-8.07915007496071,-16.2251205863895,
-128.221957648702));
#151482=CARTESIAN_POINT('Ctrl Pts',(-9.50104767561052,-15.3447188656481,
-129.716075295761));
#151483=CARTESIAN_POINT('Ctrl Pts',(-10.9229452762603,-14.4643171449067,
-131.21019294282));
#151484=CARTESIAN_POINT('Ctrl Pts',(-12.1588589765331,-13.3376329379985,
-132.704310589878));
#151485=CARTESIAN_POINT('Ctrl Pts',(-13.3947726768058,-12.2109487310903,
-134.198428236937));
#151486=CARTESIAN_POINT('Ctrl Pts',(-14.4026149179538,-10.8763499173728,
-135.692545883996));
#151487=CARTESIAN_POINT('Ctrl Pts',(-15.4104571591017,-9.54175110365538,
-137.186663531055));
#151488=CARTESIAN_POINT('Ctrl Pts',(-16.1559070823762,-8.04468584505497,
-138.680781178114));
#151489=CARTESIAN_POINT('Ctrl Pts',(-16.9013570056506,-6.54762058645456,
-140.174898825173));
#151490=CARTESIAN_POINT('Ctrl Pts',(-17.3590292079831,-4.93906964482095,
-141.669016472231));
#151491=CARTESIAN_POINT('Ctrl Pts',(-17.8167014103155,-3.33051870318735,
-143.16313411929));
#151492=CARTESIAN_POINT('Ctrl Pts',(-17.9710104137728,-1.66525935159368,
-144.657251766349));
#151493=CARTESIAN_POINT('Ctrl Pts',(-18.1253194172301,-1.10985572039171E-15,
-146.151369413408));
#151494=CARTESIAN_POINT('Ctrl Pts',(-17.9710104137728,1.66525935159367,
-147.645487060467));
#151495=CARTESIAN_POINT('Ctrl Pts',(-17.8167014103155,3.33051870318735,
-149.139604707525));
#151496=CARTESIAN_POINT('Ctrl Pts',(-17.3590292079831,4.93906964482096,
-150.633722354584));
#151497=CARTESIAN_POINT('Ctrl Pts',(-16.9013570056506,6.54762058645456,
-152.127840001643));
#151498=CARTESIAN_POINT('Ctrl Pts',(-16.1559070823762,8.04468584505497,
-153.621957648702));
#151499=CARTESIAN_POINT('Ctrl Pts',(-15.4104571591017,9.54175110365538,
-155.116075295761));
#151500=CARTESIAN_POINT('Ctrl Pts',(-14.4026149179538,10.8763499173728,
-156.610192942819));
#151501=CARTESIAN_POINT('Ctrl Pts',(-13.3947726768058,12.2109487310903,
-158.104310589878));
#151502=CARTESIAN_POINT('Ctrl Pts',(-12.1588589765331,13.3376329379985,
-159.598428236937));
#151503=CARTESIAN_POINT('Ctrl Pts',(-10.9229452762603,14.4643171449067,
-161.092545883996));
#151504=CARTESIAN_POINT('Ctrl Pts',(-9.50104767561052,15.3447188656481,
-162.586663531055));
#151505=CARTESIAN_POINT('Ctrl Pts',(-8.07915007496071,16.2251205863895,
-164.080781178114));
#151506=CARTESIAN_POINT('Ctrl Pts',(-6.51968959134574,16.8292587962898,
-165.574898825172));
#151507=CARTESIAN_POINT('Ctrl Pts',(-4.96022910773078,17.4333970061901,
-167.069016472231));
#151508=CARTESIAN_POINT('Ctrl Pts',(-3.31631129755346,17.7406985030951,
-168.56313411929));
#151509=CARTESIAN_POINT('Ctrl Pts',(-1.67239348737615,18.048,-170.057251766349));
#151510=CARTESIAN_POINT('Ctrl Pts',(-2.21024254310115E-15,18.048,-171.551369413408));
#151511=CARTESIAN_POINT('Ctrl Pts',(1.67239348737616,18.048,-173.045487060467));
#151512=CARTESIAN_POINT('Ctrl Pts',(3.31631129755346,17.7406985030951,-174.539604707525));
#151513=CARTESIAN_POINT('Ctrl Pts',(4.96022910773077,17.4333970061901,-176.033722354584));
#151514=CARTESIAN_POINT('Ctrl Pts',(6.51968959134575,16.8292587962898,-177.527840001643));
#151515=CARTESIAN_POINT('Ctrl Pts',(8.07915007496071,16.2251205863895,-179.021957648702));
#151516=CARTESIAN_POINT('Ctrl Pts',(9.50104767561053,15.3447188656481,-180.516075295761));
#151517=CARTESIAN_POINT('Ctrl Pts',(10.9229452762603,14.4643171449067,-182.01019294282));
#151518=CARTESIAN_POINT('Ctrl Pts',(12.1588589765331,13.3376329379985,-183.504310589878));
#151519=CARTESIAN_POINT('Ctrl Pts',(13.3947726768058,12.2109487310903,-184.998428236937));
#151520=CARTESIAN_POINT('Ctrl Pts',(14.4026149179538,10.8763499173728,-186.492545883996));
#151521=CARTESIAN_POINT('Ctrl Pts',(15.4104571591017,9.54175110365538,-187.986663531055));
#151522=CARTESIAN_POINT('Ctrl Pts',(16.1559070823762,8.04468584505496,-189.480781178114));
#151523=CARTESIAN_POINT('Ctrl Pts',(16.9013570056506,6.54762058645456,-190.974898825173));
#151524=CARTESIAN_POINT('Ctrl Pts',(17.3590292079831,4.93906964482096,-192.469016472231));
#151525=CARTESIAN_POINT('Ctrl Pts',(17.8167014103155,3.33051870318735,-193.96313411929));
#151526=CARTESIAN_POINT('Ctrl Pts',(17.9710104137728,1.66525935159367,-195.457251766349));
#151527=CARTESIAN_POINT('Ctrl Pts',(18.1253194172301,3.32956716117513E-15,
-196.951369413408));
#151528=CARTESIAN_POINT('Ctrl Pts',(17.9710104137728,-1.66525935159367,
-198.445487060467));
#151529=CARTESIAN_POINT('Ctrl Pts',(17.8167014103155,-3.33051870318736,
-199.939604707526));
#151530=CARTESIAN_POINT('Ctrl Pts',(17.3590292079831,-4.93906964482095,
-201.433722354584));
#151531=CARTESIAN_POINT('Ctrl Pts',(16.9013570056506,-6.54762058645456,
-202.927840001643));
#151532=CARTESIAN_POINT('Ctrl Pts',(16.1559070823762,-8.04468584505497,
-204.421957648702));
#151533=CARTESIAN_POINT('Ctrl Pts',(15.4104571591017,-9.54175110365538,
-205.916075295761));
#151534=CARTESIAN_POINT('Ctrl Pts',(14.4026149179538,-10.8763499173728,
-207.41019294282));
#151535=CARTESIAN_POINT('Ctrl Pts',(13.3947726768058,-12.2109487310903,
-208.904310589878));
#151536=CARTESIAN_POINT('Ctrl Pts',(12.1588589765331,-13.3376329379985,
-210.398428236937));
#151537=CARTESIAN_POINT('Ctrl Pts',(10.9229452762603,-14.4643171449067,
-211.892545883996));
#151538=CARTESIAN_POINT('Ctrl Pts',(9.50104767561053,-15.3447188656481,
-213.386663531055));
#151539=CARTESIAN_POINT('Ctrl Pts',(8.07915007496071,-16.2251205863895,
-214.880781178114));
#151540=CARTESIAN_POINT('Ctrl Pts',(6.51968959134574,-16.8292587962898,
-216.374898825172));
#151541=CARTESIAN_POINT('Ctrl Pts',(4.96022910773078,-17.4333970061901,
-217.869016472231));
#151542=CARTESIAN_POINT('Ctrl Pts',(3.31631129755346,-17.7406985030951,
-219.36313411929));
#151543=CARTESIAN_POINT('Ctrl Pts',(1.67239348737615,-18.048,-220.857251766349));
#151544=CARTESIAN_POINT('Ctrl Pts',(0.,-18.048,-222.351369413408));
#151545=CARTESIAN_POINT('Ctrl Pts',(-1.67239348737615,-18.048,-223.845487060466));
#151546=CARTESIAN_POINT('Ctrl Pts',(-3.31631129755346,-17.7406985030951,
-225.339604707525));
#151547=CARTESIAN_POINT('Ctrl Pts',(-4.96022910773077,-17.4333970061901,
-226.833722354584));
#151548=CARTESIAN_POINT('Ctrl Pts',(-6.51968959134574,-16.8292587962898,
-228.327840001643));
#151549=CARTESIAN_POINT('Ctrl Pts',(-8.07915007496071,-16.2251205863895,
-229.821957648702));
#151550=CARTESIAN_POINT('Ctrl Pts',(-9.50104767561052,-15.3447188656481,
-231.316075295761));
#151551=CARTESIAN_POINT('Ctrl Pts',(-10.9229452762603,-14.4643171449067,
-232.810192942819));
#151552=CARTESIAN_POINT('Ctrl Pts',(-12.1588589765331,-13.3376329379985,
-234.304310589878));
#151553=CARTESIAN_POINT('Ctrl Pts',(-13.3947726768058,-12.2109487310903,
-235.798428236937));
#151554=CARTESIAN_POINT('Ctrl Pts',(-14.4026149179538,-10.8763499173728,
-237.292545883996));
#151555=CARTESIAN_POINT('Ctrl Pts',(-15.4104571591017,-9.54175110365538,
-238.786663531055));
#151556=CARTESIAN_POINT('Ctrl Pts',(-16.1559070823762,-8.04468584505497,
-240.280781178114));
#151557=CARTESIAN_POINT('Ctrl Pts',(-16.9013570056506,-6.54762058645456,
-241.774898825172));
#151558=CARTESIAN_POINT('Ctrl Pts',(-17.3590292079831,-4.93906964482095,
-243.269016472231));
#151559=CARTESIAN_POINT('Ctrl Pts',(-17.8167014103155,-3.33051870318735,
-244.76313411929));
#151560=CARTESIAN_POINT('Ctrl Pts',(-17.9710104137728,-1.66525935159368,
-246.257251766349));
#151561=CARTESIAN_POINT('Ctrl Pts',(-18.1253194172301,-1.10985572039171E-15,
-247.751369413408));
#151562=CARTESIAN_POINT('Ctrl Pts',(-17.9710104137728,1.66525935159367,
-249.245487060467));
#151563=CARTESIAN_POINT('Ctrl Pts',(-17.8167014103155,3.33051870318735,
-250.739604707525));
#151564=CARTESIAN_POINT('Ctrl Pts',(-17.3590292079831,4.93906964482096,
-252.233722354584));
#151565=CARTESIAN_POINT('Ctrl Pts',(-16.9013570056506,6.54762058645456,
-253.727840001643));
#151566=CARTESIAN_POINT('Ctrl Pts',(-16.1559070823762,8.04468584505497,
-255.221957648702));
#151567=CARTESIAN_POINT('Ctrl Pts',(-15.4104571591017,9.54175110365538,
-256.716075295761));
#151568=CARTESIAN_POINT('Ctrl Pts',(-14.4026149179538,10.8763499173728,
-258.21019294282));
#151569=CARTESIAN_POINT('Ctrl Pts',(-13.3947726768058,12.2109487310903,
-259.704310589879));
#151570=CARTESIAN_POINT('Ctrl Pts',(-12.1588589765331,13.3376329379985,
-261.198428236937));
#151571=CARTESIAN_POINT('Ctrl Pts',(-10.9229452762603,14.4643171449067,
-262.692545883996));
#151572=CARTESIAN_POINT('Ctrl Pts',(-9.50104767561052,15.3447188656481,
-264.186663531055));
#151573=CARTESIAN_POINT('Ctrl Pts',(-8.07915007496071,16.2251205863895,
-265.680781178114));
#151574=CARTESIAN_POINT('Ctrl Pts',(-6.51968959134574,16.8292587962898,
-267.174898825173));
#151575=CARTESIAN_POINT('Ctrl Pts',(-4.96022910773078,17.4333970061901,
-268.669016472231));
#151576=CARTESIAN_POINT('Ctrl Pts',(-3.31631129755346,17.7406985030951,
-270.16313411929));
#151577=CARTESIAN_POINT('Ctrl Pts',(-1.67239348737615,18.048,-271.657251766349));
#151578=CARTESIAN_POINT('Ctrl Pts',(-2.21024254310115E-15,18.048,-273.151369413408));
#151579=CARTESIAN_POINT('Ctrl Pts',(1.67239348737616,18.048,-274.645487060467));
#151580=CARTESIAN_POINT('Ctrl Pts',(3.31631129755346,17.7406985030951,-276.139604707525));
#151581=CARTESIAN_POINT('Ctrl Pts',(4.96022910773077,17.4333970061901,-277.633722354584));
#151582=CARTESIAN_POINT('Ctrl Pts',(6.51968959134575,16.8292587962898,-279.127840001643));
#151583=CARTESIAN_POINT('Ctrl Pts',(8.07915007496071,16.2251205863895,-280.621957648702));
#151584=CARTESIAN_POINT('Ctrl Pts',(9.50104767561053,15.3447188656481,-282.116075295761));
#151585=CARTESIAN_POINT('Ctrl Pts',(10.9229452762603,14.4643171449067,-283.610192942819));
#151586=CARTESIAN_POINT('Ctrl Pts',(12.1588589765331,13.3376329379985,-285.104310589878));
#151587=CARTESIAN_POINT('Ctrl Pts',(13.3947726768058,12.2109487310903,-286.598428236937));
#151588=CARTESIAN_POINT('Ctrl Pts',(14.4026149179538,10.8763499173728,-288.092545883996));
#151589=CARTESIAN_POINT('Ctrl Pts',(15.4104571591017,9.54175110365538,-289.586663531055));
#151590=CARTESIAN_POINT('Ctrl Pts',(16.1559070823762,8.04468584505496,-291.080781178114));
#151591=CARTESIAN_POINT('Ctrl Pts',(16.9013570056506,6.54762058645456,-292.574898825172));
#151592=CARTESIAN_POINT('Ctrl Pts',(17.3590292079831,4.93906964482096,-294.069016472231));
#151593=CARTESIAN_POINT('Ctrl Pts',(17.8167014103155,3.33051870318735,-295.56313411929));
#151594=CARTESIAN_POINT('Ctrl Pts',(17.9710104137728,1.66525935159367,-297.057251766349));
#151595=CARTESIAN_POINT('Ctrl Pts',(18.1253194172301,3.32956716117513E-15,
-298.551369413408));
#151596=CARTESIAN_POINT('Ctrl Pts',(17.9710104137728,-1.66525935159367,
-300.045487060467));
#151597=CARTESIAN_POINT('Ctrl Pts',(17.8167014103155,-3.33051870318736,
-301.539604707525));
#151598=CARTESIAN_POINT('Ctrl Pts',(17.3590292079831,-4.93906964482095,
-303.033722354584));
#151599=CARTESIAN_POINT('Ctrl Pts',(16.9013570056506,-6.54762058645456,
-304.527840001643));
#151600=CARTESIAN_POINT('Ctrl Pts',(16.1559070823762,-8.04468584505497,
-306.021957648702));
#151601=CARTESIAN_POINT('Ctrl Pts',(15.4104571591017,-9.54175110365538,
-307.516075295761));
#151602=CARTESIAN_POINT('Ctrl Pts',(14.4026149179538,-10.8763499173728,
-309.01019294282));
#151603=CARTESIAN_POINT('Ctrl Pts',(13.3947726768058,-12.2109487310903,
-310.504310589878));
#151604=CARTESIAN_POINT('Ctrl Pts',(12.1588589765331,-13.3376329379985,
-311.998428236937));
#151605=CARTESIAN_POINT('Ctrl Pts',(10.9229452762603,-14.4643171449067,
-313.492545883996));
#151606=CARTESIAN_POINT('Ctrl Pts',(9.50104767561053,-15.3447188656481,
-314.986663531055));
#151607=CARTESIAN_POINT('Ctrl Pts',(8.07915007496071,-16.2251205863895,
-316.480781178114));
#151608=CARTESIAN_POINT('Ctrl Pts',(6.51968959134574,-16.8292587962898,
-317.974898825172));
#151609=CARTESIAN_POINT('Ctrl Pts',(4.96022910773078,-17.4333970061901,
-319.469016472231));
#151610=CARTESIAN_POINT('Ctrl Pts',(3.31631129755346,-17.7406985030951,
-320.96313411929));
#151611=CARTESIAN_POINT('Ctrl Pts',(1.67239348737615,-18.048,-322.457251766349));
#151612=CARTESIAN_POINT('Ctrl Pts',(0.,-18.048,-323.951369413408));
#151613=CARTESIAN_POINT('Ctrl Pts',(-1.67239348737615,-18.048,-325.445487060467));
#151614=CARTESIAN_POINT('Ctrl Pts',(-3.31631129755346,-17.7406985030951,
-326.939604707526));
#151615=CARTESIAN_POINT('Ctrl Pts',(-4.96022910773077,-17.4333970061901,
-328.433722354584));
#151616=CARTESIAN_POINT('Ctrl Pts',(-6.51968959134574,-16.8292587962898,
-329.927840001643));
#151617=CARTESIAN_POINT('Ctrl Pts',(-8.07915007496071,-16.2251205863895,
-331.421957648702));
#151618=CARTESIAN_POINT('Ctrl Pts',(-9.50104767561052,-15.3447188656481,
-332.916075295761));
#151619=CARTESIAN_POINT('Ctrl Pts',(-10.9229452762603,-14.4643171449067,
-334.41019294282));
#151620=CARTESIAN_POINT('Ctrl Pts',(-12.1588589765331,-13.3376329379985,
-335.904310589878));
#151621=CARTESIAN_POINT('Ctrl Pts',(-13.3947726768058,-12.2109487310903,
-337.398428236937));
#151622=CARTESIAN_POINT('Ctrl Pts',(-14.4026149179538,-10.8763499173728,
-338.892545883996));
#151623=CARTESIAN_POINT('Ctrl Pts',(-15.4104571591017,-9.54175110365538,
-340.386663531055));
#151624=CARTESIAN_POINT('Ctrl Pts',(-16.1559070823762,-8.04468584505497,
-341.880781178114));
#151625=CARTESIAN_POINT('Ctrl Pts',(-16.9013570056506,-6.54762058645456,
-343.374898825172));
#151626=CARTESIAN_POINT('Ctrl Pts',(-17.3590292079831,-4.93906964482095,
-344.869016472231));
#151627=CARTESIAN_POINT('Ctrl Pts',(-17.8167014103155,-3.33051870318735,
-346.36313411929));
#151628=CARTESIAN_POINT('Ctrl Pts',(-17.9710104137728,-1.66525935159368,
-347.857251766349));
#151629=CARTESIAN_POINT('Ctrl Pts',(-18.1253194172301,-1.10985572039171E-15,
-349.351369413408));
#151630=CARTESIAN_POINT('Ctrl Pts',(-17.9710104137728,1.66525935159367,
-350.845487060467));
#151631=CARTESIAN_POINT('Ctrl Pts',(-17.8167014103155,3.33051870318735,
-352.339604707525));
#151632=CARTESIAN_POINT('Ctrl Pts',(-17.3590292079831,4.93906964482096,
-353.833722354584));
#151633=CARTESIAN_POINT('Ctrl Pts',(-16.9013570056506,6.54762058645456,
-355.327840001643));
#151634=CARTESIAN_POINT('Ctrl Pts',(-16.1559070823762,8.04468584505497,
-356.821957648702));
#151635=CARTESIAN_POINT('Ctrl Pts',(-15.4104571591017,9.54175110365538,
-358.316075295761));
#151636=CARTESIAN_POINT('Ctrl Pts',(-14.4026149179538,10.8763499173728,
-359.81019294282));
#151637=CARTESIAN_POINT('Ctrl Pts',(-13.3947726768058,12.2109487310903,
-361.304310589878));
#151638=CARTESIAN_POINT('Ctrl Pts',(-12.1588589765331,13.3376329379985,
-362.798428236937));
#151639=CARTESIAN_POINT('Ctrl Pts',(-10.9229452762603,14.4643171449067,
-364.292545883996));
#151640=CARTESIAN_POINT('Ctrl Pts',(-9.50104767561052,15.3447188656481,
-365.786663531055));
#151641=CARTESIAN_POINT('Ctrl Pts',(-8.07915007496071,16.2251205863895,
-367.280781178114));
#151642=CARTESIAN_POINT('Ctrl Pts',(-6.51968959134574,16.8292587962898,
-368.774898825172));
#151643=CARTESIAN_POINT('Ctrl Pts',(-4.96022910773078,17.4333970061901,
-370.269016472231));
#151644=CARTESIAN_POINT('Ctrl Pts',(-3.31631129755346,17.7406985030951,
-371.76313411929));
#151645=CARTESIAN_POINT('Ctrl Pts',(-1.67239348737615,18.048,-373.257251766349));
#151646=CARTESIAN_POINT('Ctrl Pts',(-2.21024254310115E-15,18.048,-374.751369413408));
#151647=CARTESIAN_POINT('Ctrl Pts',(1.67239348737616,18.048,-376.245487060467));
#151648=CARTESIAN_POINT('Ctrl Pts',(3.31631129755346,17.7406985030951,-377.739604707525));
#151649=CARTESIAN_POINT('Ctrl Pts',(4.96022910773077,17.4333970061901,-379.233722354584));
#151650=CARTESIAN_POINT('Ctrl Pts',(6.51968959134575,16.8292587962898,-380.727840001643));
#151651=CARTESIAN_POINT('Ctrl Pts',(8.07915007496071,16.2251205863895,-382.221957648702));
#151652=CARTESIAN_POINT('Ctrl Pts',(9.50104767561053,15.3447188656481,-383.716075295761));
#151653=CARTESIAN_POINT('Ctrl Pts',(10.9229452762603,14.4643171449067,-385.21019294282));
#151654=CARTESIAN_POINT('Ctrl Pts',(12.1588589765331,13.3376329379985,-386.704310589878));
#151655=CARTESIAN_POINT('Ctrl Pts',(13.3947726768058,12.2109487310903,-388.198428236937));
#151656=CARTESIAN_POINT('Ctrl Pts',(14.4026149179538,10.8763499173728,-389.692545883996));
#151657=CARTESIAN_POINT('Ctrl Pts',(15.4104571591017,9.54175110365538,-391.186663531055));
#151658=CARTESIAN_POINT('Ctrl Pts',(16.1559070823762,8.04468584505496,-392.680781178114));
#151659=CARTESIAN_POINT('Ctrl Pts',(16.9013570056506,6.54762058645456,-394.174898825173));
#151660=CARTESIAN_POINT('Ctrl Pts',(17.3590292079831,4.93906964482096,-395.669016472231));
#151661=CARTESIAN_POINT('Ctrl Pts',(17.8167014103155,3.33051870318735,-397.16313411929));
#151662=CARTESIAN_POINT('Ctrl Pts',(17.9710104137728,1.66525935159367,-398.657251766349));
#151663=CARTESIAN_POINT('Ctrl Pts',(18.1253194172301,3.32956716117513E-15,
-400.151369413408));
#151664=CARTESIAN_POINT('Ctrl Pts',(17.9710104137728,-1.66525935159367,
-401.645487060467));
#151665=CARTESIAN_POINT('Ctrl Pts',(17.8167014103155,-3.33051870318736,
-403.139604707525));
#151666=CARTESIAN_POINT('Ctrl Pts',(17.3590292079831,-4.93906964482095,
-404.633722354584));
#151667=CARTESIAN_POINT('Ctrl Pts',(16.9013570056506,-6.54762058645456,
-406.127840001643));
#151668=CARTESIAN_POINT('Ctrl Pts',(16.1559070823762,-8.04468584505497,
-407.621957648702));
#151669=CARTESIAN_POINT('Ctrl Pts',(15.4104571591017,-9.54175110365538,
-409.116075295761));
#151670=CARTESIAN_POINT('Ctrl Pts',(14.4026149179538,-10.8763499173728,
-410.610192942819));
#151671=CARTESIAN_POINT('Ctrl Pts',(13.3947726768058,-12.2109487310903,
-412.104310589878));
#151672=CARTESIAN_POINT('Ctrl Pts',(12.1588589765331,-13.3376329379985,
-413.598428236937));
#151673=CARTESIAN_POINT('Ctrl Pts',(10.9229452762603,-14.4643171449067,
-415.092545883996));
#151674=CARTESIAN_POINT('Ctrl Pts',(9.50104767561053,-15.3447188656481,
-416.586663531055));
#151675=CARTESIAN_POINT('Ctrl Pts',(8.07915007496071,-16.2251205863895,
-418.080781178114));
#151676=CARTESIAN_POINT('Ctrl Pts',(6.51968959134574,-16.8292587962898,
-419.574898825172));
#151677=CARTESIAN_POINT('Ctrl Pts',(4.96022910773078,-17.4333970061901,
-421.069016472231));
#151678=CARTESIAN_POINT('Ctrl Pts',(3.31631129755346,-17.7406985030951,
-422.56313411929));
#151679=CARTESIAN_POINT('Ctrl Pts',(1.67239348737615,-18.048,-424.057251766349));
#151680=CARTESIAN_POINT('Ctrl Pts',(0.,-18.048,-425.551369413408));
#151681=CARTESIAN_POINT('Ctrl Pts',(-1.67239348737615,-18.048,-427.045487060466));
#151682=CARTESIAN_POINT('Ctrl Pts',(-3.31631129755346,-17.7406985030951,
-428.539604707525));
#151683=CARTESIAN_POINT('Ctrl Pts',(-4.96022910773077,-17.4333970061901,
-430.033722354584));
#151684=CARTESIAN_POINT('Ctrl Pts',(-6.51968959134574,-16.8292587962898,
-431.527840001643));
#151685=CARTESIAN_POINT('Ctrl Pts',(-8.07915007496071,-16.2251205863895,
-433.021957648702));
#151686=CARTESIAN_POINT('Ctrl Pts',(-9.50104767561052,-15.3447188656481,
-434.516075295761));
#151687=CARTESIAN_POINT('Ctrl Pts',(-10.9229452762603,-14.4643171449067,
-436.01019294282));
#151688=CARTESIAN_POINT('Ctrl Pts',(-12.1588589765331,-13.3376329379985,
-437.504310589878));
#151689=CARTESIAN_POINT('Ctrl Pts',(-13.3947726768058,-12.2109487310903,
-438.998428236937));
#151690=CARTESIAN_POINT('Ctrl Pts',(-14.4026149179538,-10.8763499173728,
-440.492545883996));
#151691=CARTESIAN_POINT('Ctrl Pts',(-15.4104571591017,-9.54175110365538,
-441.986663531055));
#151692=CARTESIAN_POINT('Ctrl Pts',(-16.1559070823762,-8.04468584505497,
-443.480781178114));
#151693=CARTESIAN_POINT('Ctrl Pts',(-16.9013570056506,-6.54762058645456,
-444.974898825172));
#151694=CARTESIAN_POINT('Ctrl Pts',(-17.3590292079831,-4.93906964482095,
-446.469016472231));
#151695=CARTESIAN_POINT('Ctrl Pts',(-17.8167014103155,-3.33051870318735,
-447.96313411929));
#151696=CARTESIAN_POINT('Ctrl Pts',(-17.9710104137728,-1.66525935159368,
-449.457251766349));
#151697=CARTESIAN_POINT('Ctrl Pts',(-18.1253194172301,-1.10985572039171E-15,
-450.951369413408));
#151698=CARTESIAN_POINT('Ctrl Pts',(-17.9710104137728,1.66525935159367,
-452.445487060467));
#151699=CARTESIAN_POINT('Ctrl Pts',(-17.8167014103155,3.33051870318735,
-453.939604707526));
#151700=CARTESIAN_POINT('Ctrl Pts',(-17.3590292079831,4.93906964482096,
-455.433722354584));
#151701=CARTESIAN_POINT('Ctrl Pts',(-16.9013570056506,6.54762058645456,
-456.927840001643));
#151702=CARTESIAN_POINT('Ctrl Pts',(-16.1559070823762,8.04468584505497,
-458.421957648702));
#151703=CARTESIAN_POINT('Ctrl Pts',(-15.4104571591017,9.54175110365538,
-459.916075295761));
#151704=CARTESIAN_POINT('Ctrl Pts',(-14.4026149179538,10.8763499173728,
-461.41019294282));
#151705=CARTESIAN_POINT('Ctrl Pts',(-13.3947726768058,12.2109487310903,
-462.904310589878));
#151706=CARTESIAN_POINT('Ctrl Pts',(-12.1588589765331,13.3376329379985,
-464.398428236937));
#151707=CARTESIAN_POINT('Ctrl Pts',(-10.9229452762603,14.4643171449067,
-465.892545883996));
#151708=CARTESIAN_POINT('Ctrl Pts',(-9.50104767561052,15.3447188656481,
-467.386663531055));
#151709=CARTESIAN_POINT('Ctrl Pts',(-8.07915007496071,16.2251205863895,
-468.880781178114));
#151710=CARTESIAN_POINT('Ctrl Pts',(-6.51968959134574,16.8292587962898,
-470.374898825172));
#151711=CARTESIAN_POINT('Ctrl Pts',(-4.96022910773078,17.4333970061901,
-471.869016472231));
#151712=CARTESIAN_POINT('Ctrl Pts',(-3.31631129755346,17.7406985030951,
-473.36313411929));
#151713=CARTESIAN_POINT('Ctrl Pts',(-1.67239348737615,18.048,-474.857251766349));
#151714=CARTESIAN_POINT('Ctrl Pts',(-2.21024254310115E-15,18.048,-476.351369413408));
#151715=CARTESIAN_POINT('Ctrl Pts',(1.67239348737616,18.048,-477.845487060466));
#151716=CARTESIAN_POINT('Ctrl Pts',(3.31631129755346,17.7406985030951,-479.339604707525));
#151717=CARTESIAN_POINT('Ctrl Pts',(4.96022910773077,17.4333970061901,-480.833722354584));
#151718=CARTESIAN_POINT('Ctrl Pts',(6.51968959134575,16.8292587962898,-482.327840001643));
#151719=CARTESIAN_POINT('Ctrl Pts',(8.07915007496071,16.2251205863895,-483.821957648702));
#151720=CARTESIAN_POINT('Ctrl Pts',(9.50104767561053,15.3447188656481,-485.316075295761));
#151721=CARTESIAN_POINT('Ctrl Pts',(10.9229452762603,14.4643171449067,-486.81019294282));
#151722=CARTESIAN_POINT('Ctrl Pts',(12.1588589765331,13.3376329379985,-488.304310589878));
#151723=CARTESIAN_POINT('Ctrl Pts',(13.3947726768058,12.2109487310903,-489.798428236937));
#151724=CARTESIAN_POINT('Ctrl Pts',(14.4026149179538,10.8763499173728,-491.292545883996));
#151725=CARTESIAN_POINT('Ctrl Pts',(15.4104571591017,9.54175110365538,-492.786663531055));
#151726=CARTESIAN_POINT('Ctrl Pts',(16.1559070823762,8.04468584505496,-494.280781178114));
#151727=CARTESIAN_POINT('Ctrl Pts',(16.9013570056506,6.54762058645456,-495.774898825173));
#151728=CARTESIAN_POINT('Ctrl Pts',(17.3590292079831,4.93906964482096,-497.269016472231));
#151729=CARTESIAN_POINT('Ctrl Pts',(17.8167014103155,3.33051870318735,-498.76313411929));
#151730=CARTESIAN_POINT('Ctrl Pts',(17.9710104137728,1.66525935159367,-500.257251766349));
#151731=CARTESIAN_POINT('Ctrl Pts',(18.1253194172301,3.32956716117513E-15,
-501.751369413408));
#151732=CARTESIAN_POINT('Ctrl Pts',(17.9710104137728,-1.66525935159367,
-503.245487060466));
#151733=CARTESIAN_POINT('Ctrl Pts',(17.8167014103155,-3.33051870318736,
-504.739604707525));
#151734=CARTESIAN_POINT('Ctrl Pts',(17.3590292079831,-4.93906964482095,
-506.233722354584));
#151735=CARTESIAN_POINT('Ctrl Pts',(16.9013570056506,-6.54762058645456,
-507.727840001643));
#151736=CARTESIAN_POINT('Ctrl Pts',(16.1559070823762,-8.04468584505497,
-509.221957648702));
#151737=CARTESIAN_POINT('Ctrl Pts',(15.4104571591017,-9.54175110365538,
-510.716075295761));
#151738=CARTESIAN_POINT('Ctrl Pts',(14.4026149179538,-10.8763499173728,
-512.21019294282));
#151739=CARTESIAN_POINT('Ctrl Pts',(13.3947726768058,-12.2109487310903,
-513.704310589878));
#151740=CARTESIAN_POINT('Ctrl Pts',(12.1588589765331,-13.3376329379985,
-515.198428236937));
#151741=CARTESIAN_POINT('Ctrl Pts',(10.9229452762603,-14.4643171449067,
-516.692545883996));
#151742=CARTESIAN_POINT('Ctrl Pts',(9.50104767561053,-15.3447188656481,
-518.186663531055));
#151743=CARTESIAN_POINT('Ctrl Pts',(8.07915007496071,-16.2251205863895,
-519.680781178114));
#151744=CARTESIAN_POINT('Ctrl Pts',(6.51968959134574,-16.8292587962898,
-521.174898825172));
#151745=CARTESIAN_POINT('Ctrl Pts',(4.96022910773078,-17.4333970061901,
-522.669016472231));
#151746=CARTESIAN_POINT('Ctrl Pts',(3.31631129755346,-17.7406985030951,
-524.16313411929));
#151747=CARTESIAN_POINT('Ctrl Pts',(1.67239348737615,-18.048,-525.657251766349));
#151748=CARTESIAN_POINT('Ctrl Pts',(0.,-18.048,-527.151369413408));
#151749=CARTESIAN_POINT('Ctrl Pts',(-1.67239348737615,-18.048,-528.645487060467));
#151750=CARTESIAN_POINT('Ctrl Pts',(-3.31631129755346,-17.7406985030951,
-530.139604707526));
#151751=CARTESIAN_POINT('Ctrl Pts',(-4.96022910773077,-17.4333970061901,
-531.633722354584));
#151752=CARTESIAN_POINT('Ctrl Pts',(-6.51968959134574,-16.8292587962898,
-533.127840001643));
#151753=CARTESIAN_POINT('Ctrl Pts',(-8.07915007496071,-16.2251205863895,
-534.621957648702));
#151754=CARTESIAN_POINT('Ctrl Pts',(-9.50104767561052,-15.3447188656481,
-536.116075295761));
#151755=CARTESIAN_POINT('Ctrl Pts',(-10.9229452762603,-14.4643171449067,
-537.610192942819));
#151756=CARTESIAN_POINT('Ctrl Pts',(-12.1588589765331,-13.3376329379985,
-539.104310589878));
#151757=CARTESIAN_POINT('Ctrl Pts',(-13.3947726768058,-12.2109487310903,
-540.598428236937));
#151758=CARTESIAN_POINT('Ctrl Pts',(-14.4026149179538,-10.8763499173728,
-542.092545883996));
#151759=CARTESIAN_POINT('Ctrl Pts',(-15.4104571591017,-9.54175110365538,
-543.586663531055));
#151760=CARTESIAN_POINT('Ctrl Pts',(-16.1559070823762,-8.04468584505497,
-545.080781178114));
#151761=CARTESIAN_POINT('Ctrl Pts',(-16.9013570056506,-6.54762058645456,
-546.574898825173));
#151762=CARTESIAN_POINT('Ctrl Pts',(-17.3590292079831,-4.93906964482095,
-548.069016472231));
#151763=CARTESIAN_POINT('Ctrl Pts',(-17.8167014103155,-3.33051870318735,
-549.56313411929));
#151764=CARTESIAN_POINT('Ctrl Pts',(-17.9710104137728,-1.66525935159368,
-551.057251766349));
#151765=CARTESIAN_POINT('Ctrl Pts',(-18.1253194172301,-1.10985572039171E-15,
-552.551369413408));
#151766=CARTESIAN_POINT('Ctrl Pts',(-17.9710104137728,1.66525935159367,
-554.045487060466));
#151767=CARTESIAN_POINT('Ctrl Pts',(-17.8167014103155,3.33051870318735,
-555.539604707526));
#151768=CARTESIAN_POINT('Ctrl Pts',(-17.3590292079831,4.93906964482096,
-557.033722354584));
#151769=CARTESIAN_POINT('Ctrl Pts',(-16.9013570056506,6.54762058645456,
-558.527840001643));
#151770=CARTESIAN_POINT('Ctrl Pts',(-16.1559070823762,8.04468584505497,
-560.021957648702));
#151771=CARTESIAN_POINT('Ctrl Pts',(-15.4104571591017,9.54175110365538,
-561.516075295761));
#151772=CARTESIAN_POINT('Ctrl Pts',(-14.4026149179538,10.8763499173728,
-563.010192942819));
#151773=CARTESIAN_POINT('Ctrl Pts',(-13.3947726768058,12.2109487310903,
-564.504310589878));
#151774=CARTESIAN_POINT('Ctrl Pts',(-12.1588589765331,13.3376329379985,
-565.998428236937));
#151775=CARTESIAN_POINT('Ctrl Pts',(-10.9229452762603,14.4643171449067,
-567.492545883996));
#151776=CARTESIAN_POINT('Ctrl Pts',(-9.50104767561052,15.3447188656481,
-568.986663531055));
#151777=CARTESIAN_POINT('Ctrl Pts',(-8.07915007496071,16.2251205863895,
-570.480781178114));
#151778=CARTESIAN_POINT('Ctrl Pts',(-6.51968959134574,16.8292587962898,
-571.974898825173));
#151779=CARTESIAN_POINT('Ctrl Pts',(-4.96022910773078,17.4333970061901,
-573.469016472231));
#151780=CARTESIAN_POINT('Ctrl Pts',(-3.31631129755346,17.7406985030951,
-574.96313411929));
#151781=CARTESIAN_POINT('Ctrl Pts',(-1.67239348737615,18.048,-576.457251766349));
#151782=CARTESIAN_POINT('Ctrl Pts',(-2.21024254310115E-15,18.048,-577.951369413408));
#151783=CARTESIAN_POINT('Ctrl Pts',(1.67239348737616,18.048,-579.445487060466));
#151784=CARTESIAN_POINT('Ctrl Pts',(3.31631129755346,17.7406985030951,-580.939604707525));
#151785=CARTESIAN_POINT('Ctrl Pts',(4.96022910773077,17.4333970061901,-582.433722354584));
#151786=CARTESIAN_POINT('Ctrl Pts',(6.51968959134575,16.8292587962898,-583.927840001643));
#151787=CARTESIAN_POINT('Ctrl Pts',(8.07915007496071,16.2251205863895,-585.421957648702));
#151788=CARTESIAN_POINT('Ctrl Pts',(9.50104767561053,15.3447188656481,-586.916075295761));
#151789=CARTESIAN_POINT('Ctrl Pts',(10.9229452762603,14.4643171449067,-588.41019294282));
#151790=CARTESIAN_POINT('Ctrl Pts',(12.1588589765331,13.3376329379985,-589.904310589878));
#151791=CARTESIAN_POINT('Ctrl Pts',(13.3947726768058,12.2109487310903,-591.398428236938));
#151792=CARTESIAN_POINT('Ctrl Pts',(14.4026149179538,10.8763499173728,-592.892545883996));
#151793=CARTESIAN_POINT('Ctrl Pts',(15.4104571591017,9.54175110365538,-594.386663531055));
#151794=CARTESIAN_POINT('Ctrl Pts',(16.1559070823762,8.04468584505496,-595.880781178113));
#151795=CARTESIAN_POINT('Ctrl Pts',(16.9013570056506,6.54762058645456,-597.374898825172));
#151796=CARTESIAN_POINT('Ctrl Pts',(17.3590292079831,4.93906964482096,-598.869016472231));
#151797=CARTESIAN_POINT('Ctrl Pts',(17.8167014103155,3.33051870318735,-600.36313411929));
#151798=CARTESIAN_POINT('Ctrl Pts',(17.9710104137728,1.66525935159367,-601.857251766349));
#151799=CARTESIAN_POINT('Ctrl Pts',(18.1253194172301,3.32956716117513E-15,
-603.351369413408));
#151800=CARTESIAN_POINT('Ctrl Pts',(17.9710104137728,-1.66525935159367,
-604.845487060467));
#151801=CARTESIAN_POINT('Ctrl Pts',(17.8167014103155,-3.33051870318736,
-606.339604707526));
#151802=CARTESIAN_POINT('Ctrl Pts',(17.3590292079831,-4.93906964482095,
-607.833722354584));
#151803=CARTESIAN_POINT('Ctrl Pts',(16.9013570056506,-6.54762058645456,
-609.327840001643));
#151804=CARTESIAN_POINT('Ctrl Pts',(16.1559070823762,-8.04468584505497,
-610.821957648702));
#151805=CARTESIAN_POINT('Ctrl Pts',(15.4104571591017,-9.54175110365538,
-612.316075295761));
#151806=CARTESIAN_POINT('Ctrl Pts',(14.4026149179538,-10.8763499173728,
-613.810192942819));
#151807=CARTESIAN_POINT('Ctrl Pts',(13.3947726768058,-12.2109487310903,
-615.304310589878));
#151808=CARTESIAN_POINT('Ctrl Pts',(12.1588589765331,-13.3376329379985,
-616.798428236937));
#151809=CARTESIAN_POINT('Ctrl Pts',(10.9229452762603,-14.4643171449067,
-618.292545883996));
#151810=CARTESIAN_POINT('Ctrl Pts',(9.50104767561053,-15.3447188656481,
-619.786663531055));
#151811=CARTESIAN_POINT('Ctrl Pts',(8.07915007496071,-16.2251205863895,
-621.280781178114));
#151812=CARTESIAN_POINT('Ctrl Pts',(6.51968959134574,-16.8292587962898,
-622.774898825172));
#151813=CARTESIAN_POINT('Ctrl Pts',(4.96022910773078,-17.4333970061901,
-624.269016472231));
#151814=CARTESIAN_POINT('Ctrl Pts',(3.31631129755346,-17.7406985030951,
-625.76313411929));
#151815=CARTESIAN_POINT('Ctrl Pts',(1.67239348737615,-18.048,-627.257251766349));
#151816=CARTESIAN_POINT('Ctrl Pts',(0.,-18.048,-628.751369413408));
#151817=CARTESIAN_POINT('Ctrl Pts',(-1.67239348737615,-18.048,-630.245487060467));
#151818=CARTESIAN_POINT('Ctrl Pts',(-3.31631129755346,-17.7406985030951,
-631.739604707525));
#151819=CARTESIAN_POINT('Ctrl Pts',(-4.96022910773077,-17.4333970061901,
-633.233722354584));
#151820=CARTESIAN_POINT('Ctrl Pts',(-6.51968959134574,-16.8292587962898,
-634.727840001643));
#151821=CARTESIAN_POINT('Ctrl Pts',(-8.07915007496071,-16.2251205863895,
-636.221957648702));
#151822=CARTESIAN_POINT('Ctrl Pts',(-9.50104767561052,-15.3447188656481,
-637.71607529576));
#151823=CARTESIAN_POINT('Ctrl Pts',(-10.9229452762603,-14.4643171449067,
-639.210192942819));
#151824=CARTESIAN_POINT('Ctrl Pts',(-12.1588589765331,-13.3376329379985,
-640.704310589878));
#151825=CARTESIAN_POINT('Ctrl Pts',(-13.3947726768058,-12.2109487310903,
-642.198428236937));
#151826=CARTESIAN_POINT('Ctrl Pts',(-14.4026149179538,-10.8763499173728,
-643.692545883996));
#151827=CARTESIAN_POINT('Ctrl Pts',(-15.4104571591017,-9.54175110365538,
-645.186663531055));
#151828=CARTESIAN_POINT('Ctrl Pts',(-16.1559070823762,-8.04468584505497,
-646.680781178114));
#151829=CARTESIAN_POINT('Ctrl Pts',(-16.9013570056506,-6.54762058645456,
-648.174898825173));
#151830=CARTESIAN_POINT('Ctrl Pts',(-17.3590292079831,-4.93906964482095,
-649.669016472231));
#151831=CARTESIAN_POINT('Ctrl Pts',(-17.8167014103155,-3.33051870318735,
-651.163134119291));
#151832=CARTESIAN_POINT('Ctrl Pts',(-17.9710104137728,-1.66525935159368,
-652.657251766349));
#151833=CARTESIAN_POINT('Ctrl Pts',(-18.1253194172301,-1.10985572039171E-15,
-654.151369413408));
#151834=CARTESIAN_POINT('Ctrl Pts',(-17.9710104137728,1.66525935159367,
-655.645487060466));
#151835=CARTESIAN_POINT('Ctrl Pts',(-17.8167014103155,3.33051870318735,
-657.139604707525));
#151836=CARTESIAN_POINT('Ctrl Pts',(-17.3590292079831,4.93906964482096,
-658.633722354584));
#151837=CARTESIAN_POINT('Ctrl Pts',(-16.9013570056506,6.54762058645456,
-660.127840001643));
#151838=CARTESIAN_POINT('Ctrl Pts',(-16.1559070823762,8.04468584505497,
-661.621957648702));
#151839=CARTESIAN_POINT('Ctrl Pts',(-15.4104571591017,9.54175110365538,
-663.116075295761));
#151840=CARTESIAN_POINT('Ctrl Pts',(-14.4026149179538,10.8763499173728,
-664.61019294282));
#151841=CARTESIAN_POINT('Ctrl Pts',(-13.3947726768058,12.2109487310903,
-666.104310589879));
#151842=CARTESIAN_POINT('Ctrl Pts',(-12.1588589765331,13.3376329379985,
-667.598428236937));
#151843=CARTESIAN_POINT('Ctrl Pts',(-10.9229452762603,14.4643171449067,
-669.092545883996));
#151844=CARTESIAN_POINT('Ctrl Pts',(-9.50104767561052,15.3447188656481,
-670.586663531055));
#151845=CARTESIAN_POINT('Ctrl Pts',(-8.07915007496071,16.2251205863895,
-672.080781178114));
#151846=CARTESIAN_POINT('Ctrl Pts',(-6.51968959134574,16.8292587962898,
-673.574898825172));
#151847=CARTESIAN_POINT('Ctrl Pts',(-4.96022910773078,17.4333970061901,
-675.069016472231));
#151848=CARTESIAN_POINT('Ctrl Pts',(-3.31631129755346,17.7406985030951,
-676.56313411929));
#151849=CARTESIAN_POINT('Ctrl Pts',(-1.67239348737615,18.048,-678.057251766349));
#151850=CARTESIAN_POINT('Ctrl Pts',(-2.21024254310115E-15,18.048,-679.551369413408));
#151851=CARTESIAN_POINT('Ctrl Pts',(1.67239348737616,18.048,-681.045487060467));
#151852=CARTESIAN_POINT('Ctrl Pts',(3.31631129755346,17.7406985030951,-682.539604707525));
#151853=CARTESIAN_POINT('Ctrl Pts',(4.96022910773077,17.4333970061901,-684.033722354584));
#151854=CARTESIAN_POINT('Ctrl Pts',(6.51968959134575,16.8292587962898,-685.527840001643));
#151855=CARTESIAN_POINT('Ctrl Pts',(8.07915007496071,16.2251205863895,-687.021957648702));
#151856=CARTESIAN_POINT('Ctrl Pts',(9.50104767561053,15.3447188656481,-688.516075295761));
#151857=CARTESIAN_POINT('Ctrl Pts',(10.9229452762603,14.4643171449067,-690.01019294282));
#151858=CARTESIAN_POINT('Ctrl Pts',(12.1588589765331,13.3376329379985,-691.504310589879));
#151859=CARTESIAN_POINT('Ctrl Pts',(13.3947726768058,12.2109487310903,-692.998428236937));
#151860=CARTESIAN_POINT('Ctrl Pts',(14.4026149179538,10.8763499173728,-694.492545883996));
#151861=CARTESIAN_POINT('Ctrl Pts',(15.4104571591017,9.54175110365538,-695.986663531055));
#151862=CARTESIAN_POINT('Ctrl Pts',(16.1559070823762,8.04468584505496,-697.480781178113));
#151863=CARTESIAN_POINT('Ctrl Pts',(16.9013570056506,6.54762058645456,-698.974898825172));
#151864=CARTESIAN_POINT('Ctrl Pts',(17.3590292079831,4.93906964482096,-700.469016472231));
#151865=CARTESIAN_POINT('Ctrl Pts',(17.8167014103155,3.33051870318735,-701.96313411929));
#151866=CARTESIAN_POINT('Ctrl Pts',(17.9710104137728,1.66525935159367,-703.457251766349));
#151867=CARTESIAN_POINT('Ctrl Pts',(18.1253194172301,3.32956716117513E-15,
-704.951369413408));
#151868=CARTESIAN_POINT('Ctrl Pts',(17.9710104137728,-1.66525935159367,
-706.445487060467));
#151869=CARTESIAN_POINT('Ctrl Pts',(17.8167014103155,-3.33051870318736,
-707.939604707526));
#151870=CARTESIAN_POINT('Ctrl Pts',(17.3590292079831,-4.93906964482095,
-709.433722354584));
#151871=CARTESIAN_POINT('Ctrl Pts',(16.9013570056506,-6.54762058645456,
-710.927840001643));
#151872=CARTESIAN_POINT('Ctrl Pts',(16.1559070823762,-8.04468584505497,
-712.421957648702));
#151873=CARTESIAN_POINT('Ctrl Pts',(15.4104571591017,-9.54175110365538,
-713.91607529576));
#151874=CARTESIAN_POINT('Ctrl Pts',(14.4026149179538,-10.8763499173728,
-715.410192942819));
#151875=CARTESIAN_POINT('Ctrl Pts',(13.3947726768058,-12.2109487310903,
-716.904310589879));
#151876=CARTESIAN_POINT('Ctrl Pts',(12.1588589765331,-13.3376329379985,
-718.398428236937));
#151877=CARTESIAN_POINT('Ctrl Pts',(10.9229452762603,-14.4643171449067,
-719.892545883996));
#151878=CARTESIAN_POINT('Ctrl Pts',(9.50104767561053,-15.3447188656481,
-721.386663531055));
#151879=CARTESIAN_POINT('Ctrl Pts',(8.07915007496071,-16.2251205863895,
-722.880781178114));
#151880=CARTESIAN_POINT('Ctrl Pts',(6.51968959134574,-16.8292587962898,
-724.374898825173));
#151881=CARTESIAN_POINT('Ctrl Pts',(4.96022910773078,-17.4333970061901,
-725.869016472232));
#151882=CARTESIAN_POINT('Ctrl Pts',(3.31631129755346,-17.7406985030951,
-727.36313411929));
#151883=CARTESIAN_POINT('Ctrl Pts',(1.67239348737615,-18.048,-728.857251766349));
#151884=CARTESIAN_POINT('Ctrl Pts',(0.,-18.048,-730.351369413408));
#151885=CARTESIAN_POINT('Ctrl Pts',(-1.67239348737615,-18.048,-731.845487060467));
#151886=CARTESIAN_POINT('Ctrl Pts',(-3.31631129755346,-17.7406985030951,
-733.339604707525));
#151887=CARTESIAN_POINT('Ctrl Pts',(-4.96022910773077,-17.4333970061901,
-734.833722354584));
#151888=CARTESIAN_POINT('Ctrl Pts',(-6.51968959134574,-16.8292587962898,
-736.327840001643));
#151889=CARTESIAN_POINT('Ctrl Pts',(-8.07915007496071,-16.2251205863895,
-737.821957648702));
#151890=CARTESIAN_POINT('Ctrl Pts',(-9.50104767561052,-15.3447188656481,
-739.316075295761));
#151891=CARTESIAN_POINT('Ctrl Pts',(-10.9229452762603,-14.4643171449067,
-740.81019294282));
#151892=CARTESIAN_POINT('Ctrl Pts',(-12.1588589765331,-13.3376329379985,
-742.304310589878));
#151893=CARTESIAN_POINT('Ctrl Pts',(-13.3947726768058,-12.2109487310903,
-743.798428236937));
#151894=CARTESIAN_POINT('Ctrl Pts',(-14.4026149179538,-10.8763499173728,
-745.292545883996));
#151895=CARTESIAN_POINT('Ctrl Pts',(-15.4104571591017,-9.54175110365538,
-746.786663531055));
#151896=CARTESIAN_POINT('Ctrl Pts',(-16.1559070823762,-8.04468584505497,
-748.280781178114));
#151897=CARTESIAN_POINT('Ctrl Pts',(-16.9013570056506,-6.54762058645456,
-749.774898825172));
#151898=CARTESIAN_POINT('Ctrl Pts',(-17.3590292079831,-4.93906964482095,
-751.269016472231));
#151899=CARTESIAN_POINT('Ctrl Pts',(-17.8167014103155,-3.33051870318735,
-752.76313411929));
#151900=CARTESIAN_POINT('Ctrl Pts',(-17.9710104137728,-1.66525935159368,
-754.257251766349));
#151901=CARTESIAN_POINT('Ctrl Pts',(-18.1253194172301,-1.10985572039171E-15,
-755.751369413408));
#151902=CARTESIAN_POINT('Ctrl Pts',(-17.9710104137728,1.66525935159367,
-757.245487060466));
#151903=CARTESIAN_POINT('Ctrl Pts',(-17.8167014103155,3.33051870318735,
-758.739604707525));
#151904=CARTESIAN_POINT('Ctrl Pts',(-17.3590292079831,4.93906964482096,
-760.233722354584));
#151905=CARTESIAN_POINT('Ctrl Pts',(-16.9013570056506,6.54762058645456,
-761.727840001643));
#151906=CARTESIAN_POINT('Ctrl Pts',(-16.1559070823762,8.04468584505497,
-763.221957648702));
#151907=CARTESIAN_POINT('Ctrl Pts',(-15.4104571591017,9.54175110365538,
-764.716075295761));
#151908=CARTESIAN_POINT('Ctrl Pts',(-14.4026149179538,10.8763499173728,
-766.21019294282));
#151909=CARTESIAN_POINT('Ctrl Pts',(-13.3947726768058,12.2109487310903,
-767.704310589879));
#151910=CARTESIAN_POINT('Ctrl Pts',(-12.1588589765331,13.3376329379985,
-769.198428236937));
#151911=CARTESIAN_POINT('Ctrl Pts',(-10.9229452762603,14.4643171449067,
-770.692545883996));
#151912=CARTESIAN_POINT('Ctrl Pts',(-9.50104767561052,15.3447188656481,
-772.186663531055));
#151913=CARTESIAN_POINT('Ctrl Pts',(-8.07915007496071,16.2251205863895,
-773.680781178114));
#151914=CARTESIAN_POINT('Ctrl Pts',(-6.51968959134574,16.8292587962898,
-775.174898825172));
#151915=CARTESIAN_POINT('Ctrl Pts',(-4.96022910773078,17.4333970061901,
-776.669016472231));
#151916=CARTESIAN_POINT('Ctrl Pts',(-3.31631129755346,17.7406985030951,
-778.16313411929));
#151917=CARTESIAN_POINT('Ctrl Pts',(-1.67239348737615,18.048,-779.657251766349));
#151918=CARTESIAN_POINT('Ctrl Pts',(-2.21024254310115E-15,18.048,-781.151369413408));
#151919=CARTESIAN_POINT('Ctrl Pts',(1.67239348737616,18.048,-782.645487060467));
#151920=CARTESIAN_POINT('Ctrl Pts',(3.31631129755346,17.7406985030951,-784.139604707526));
#151921=CARTESIAN_POINT('Ctrl Pts',(4.96022910773077,17.4333970061901,-785.633722354585));
#151922=CARTESIAN_POINT('Ctrl Pts',(6.51968959134575,16.8292587962898,-787.127840001643));
#151923=CARTESIAN_POINT('Ctrl Pts',(8.07915007496071,16.2251205863895,-788.621957648702));
#151924=CARTESIAN_POINT('Ctrl Pts',(9.50104767561053,15.3447188656481,-790.116075295761));
#151925=CARTESIAN_POINT('Ctrl Pts',(10.9229452762603,14.4643171449067,-791.61019294282));
#151926=CARTESIAN_POINT('Ctrl Pts',(12.1588589765331,13.3376329379985,-793.104310589878));
#151927=CARTESIAN_POINT('Ctrl Pts',(13.3947726768058,12.2109487310903,-794.598428236937));
#151928=CARTESIAN_POINT('Ctrl Pts',(14.4026149179538,10.8763499173728,-796.092545883996));
#151929=CARTESIAN_POINT('Ctrl Pts',(15.4104571591017,9.54175110365538,-797.586663531055));
#151930=CARTESIAN_POINT('Ctrl Pts',(16.1559070823762,8.04468584505496,-799.080781178114));
#151931=CARTESIAN_POINT('Ctrl Pts',(16.9013570056506,6.54762058645456,-800.574898825173));
#151932=CARTESIAN_POINT('Ctrl Pts',(17.3590292079831,4.93906964482096,-802.069016472231));
#151933=CARTESIAN_POINT('Ctrl Pts',(17.8167014103155,3.33051870318735,-803.56313411929));
#151934=CARTESIAN_POINT('Ctrl Pts',(17.9710104137728,1.66525935159367,-805.057251766349));
#151935=CARTESIAN_POINT('Ctrl Pts',(18.1253194172301,3.32956716117513E-15,
-806.551369413408));
#151936=CARTESIAN_POINT('Ctrl Pts',(17.9710104137728,-1.66525935159367,
-808.045487060467));
#151937=CARTESIAN_POINT('Ctrl Pts',(17.8167014103155,-3.33051870318736,
-809.539604707526));
#151938=CARTESIAN_POINT('Ctrl Pts',(17.3590292079831,-4.93906964482095,
-811.033722354584));
#151939=CARTESIAN_POINT('Ctrl Pts',(16.9013570056506,-6.54762058645456,
-812.527840001643));
#151940=CARTESIAN_POINT('Ctrl Pts',(16.1559070823762,-8.04468584505497,
-814.021957648702));
#151941=CARTESIAN_POINT('Ctrl Pts',(15.4104571591017,-9.54175110365538,
-815.516075295761));
#151942=CARTESIAN_POINT('Ctrl Pts',(14.4026149179538,-10.8763499173728,
-817.010192942819));
#151943=CARTESIAN_POINT('Ctrl Pts',(13.3947726768058,-12.2109487310903,
-818.504310589878));
#151944=CARTESIAN_POINT('Ctrl Pts',(12.1588589765331,-13.3376329379985,
-819.998428236937));
#151945=CARTESIAN_POINT('Ctrl Pts',(10.9229452762603,-14.4643171449067,
-821.492545883996));
#151946=CARTESIAN_POINT('Ctrl Pts',(9.50104767561053,-15.3447188656481,
-822.986663531055));
#151947=CARTESIAN_POINT('Ctrl Pts',(8.07915007496071,-16.2251205863895,
-824.480781178114));
#151948=CARTESIAN_POINT('Ctrl Pts',(6.51968959134574,-16.8292587962898,
-825.974898825173));
#151949=CARTESIAN_POINT('Ctrl Pts',(4.96022910773078,-17.4333970061901,
-827.469016472232));
#151950=CARTESIAN_POINT('Ctrl Pts',(3.31631129755346,-17.7406985030951,
-828.96313411929));
#151951=CARTESIAN_POINT('Ctrl Pts',(1.67239348737615,-18.048,-830.457251766349));
#151952=CARTESIAN_POINT('Ctrl Pts',(0.,-18.048,-831.951369413408));
#151953=CARTESIAN_POINT('Ctrl Pts',(-1.67239348737615,-18.048,-833.445487060467));
#151954=CARTESIAN_POINT('Ctrl Pts',(-3.31631129755346,-17.7406985030951,
-834.939604707525));
#151955=CARTESIAN_POINT('Ctrl Pts',(-4.96022910773077,-17.4333970061901,
-836.433722354584));
#151956=CARTESIAN_POINT('Ctrl Pts',(-6.51968959134574,-16.8292587962898,
-837.927840001643));
#151957=CARTESIAN_POINT('Ctrl Pts',(-8.07915007496071,-16.2251205863895,
-839.421957648702));
#151958=CARTESIAN_POINT('Ctrl Pts',(-9.50104767561052,-15.3447188656481,
-840.916075295761));
#151959=CARTESIAN_POINT('Ctrl Pts',(-10.9229452762603,-14.4643171449067,
-842.41019294282));
#151960=CARTESIAN_POINT('Ctrl Pts',(-12.1588589765331,-13.3376329379985,
-843.904310589879));
#151961=CARTESIAN_POINT('Ctrl Pts',(-13.3947726768058,-12.2109487310903,
-845.398428236937));
#151962=CARTESIAN_POINT('Ctrl Pts',(-14.4026149179538,-10.8763499173728,
-846.892545883996));
#151963=CARTESIAN_POINT('Ctrl Pts',(-15.4104571591017,-9.54175110365538,
-848.386663531055));
#151964=CARTESIAN_POINT('Ctrl Pts',(-16.1559070823762,-8.04468584505497,
-849.880781178114));
#151965=CARTESIAN_POINT('Ctrl Pts',(-16.9013570056506,-6.54762058645456,
-851.374898825173));
#151966=CARTESIAN_POINT('Ctrl Pts',(-17.3590292079831,-4.93906964482095,
-852.869016472231));
#151967=CARTESIAN_POINT('Ctrl Pts',(-17.8167014103155,-3.33051870318735,
-854.36313411929));
#151968=CARTESIAN_POINT('Ctrl Pts',(-17.9710104137728,-1.66525935159368,
-855.857251766349));
#151969=CARTESIAN_POINT('Ctrl Pts',(-18.1253194172301,-1.10985572039171E-15,
-857.351369413408));
#151970=CARTESIAN_POINT('Ctrl Pts',(-17.9710104137728,1.66525935159367,
-858.845487060467));
#151971=CARTESIAN_POINT('Ctrl Pts',(-17.8167014103155,3.33051870318735,
-860.339604707526));
#151972=CARTESIAN_POINT('Ctrl Pts',(-17.3590292079831,4.93906964482096,
-861.833722354584));
#151973=CARTESIAN_POINT('Ctrl Pts',(-16.9013570056506,6.54762058645456,
-863.327840001643));
#151974=CARTESIAN_POINT('Ctrl Pts',(-16.1559070823762,8.04468584505497,
-864.821957648702));
#151975=CARTESIAN_POINT('Ctrl Pts',(-15.4104571591017,9.54175110365538,
-866.316075295761));
#151976=CARTESIAN_POINT('Ctrl Pts',(-14.4026149179538,10.8763499173728,
-867.810192942819));
#151977=CARTESIAN_POINT('Ctrl Pts',(-13.3947726768058,12.2109487310903,
-869.304310589878));
#151978=CARTESIAN_POINT('Ctrl Pts',(-12.1588589765331,13.3376329379985,
-870.798428236937));
#151979=CARTESIAN_POINT('Ctrl Pts',(-10.9229452762603,14.4643171449067,
-872.292545883996));
#151980=CARTESIAN_POINT('Ctrl Pts',(-9.50104767561052,15.3447188656481,
-873.786663531055));
#151981=CARTESIAN_POINT('Ctrl Pts',(-8.07915007496071,16.2251205863895,
-875.280781178114));
#151982=CARTESIAN_POINT('Ctrl Pts',(-6.51968959134574,16.8292587962898,
-876.774898825172));
#151983=CARTESIAN_POINT('Ctrl Pts',(-4.96022910773078,17.4333970061901,
-878.269016472231));
#151984=CARTESIAN_POINT('Ctrl Pts',(-3.31631129755346,17.7406985030951,
-879.76313411929));
#151985=CARTESIAN_POINT('Ctrl Pts',(-1.67239348737615,18.048,-881.257251766349));
#151986=CARTESIAN_POINT('Ctrl Pts',(-2.21024254310115E-15,18.048,-882.751369413408));
#151987=CARTESIAN_POINT('Ctrl Pts',(1.67239348737616,18.048,-884.245487060467));
#151988=CARTESIAN_POINT('Ctrl Pts',(3.31631129755346,17.7406985030951,-885.739604707526));
#151989=CARTESIAN_POINT('Ctrl Pts',(4.96022910773077,17.4333970061901,-887.233722354585));
#151990=CARTESIAN_POINT('Ctrl Pts',(6.51968959134575,16.8292587962898,-888.727840001643));
#151991=CARTESIAN_POINT('Ctrl Pts',(8.07915007496071,16.2251205863895,-890.221957648702));
#151992=CARTESIAN_POINT('Ctrl Pts',(9.50104767561053,15.3447188656481,-891.71607529576));
#151993=CARTESIAN_POINT('Ctrl Pts',(10.9229452762603,14.4643171449067,-893.21019294282));
#151994=CARTESIAN_POINT('Ctrl Pts',(12.1588589765331,13.3376329379985,-894.704310589878));
#151995=CARTESIAN_POINT('Ctrl Pts',(13.3947726768058,12.2109487310903,-896.198428236937));
#151996=CARTESIAN_POINT('Ctrl Pts',(14.4026149179538,10.8763499173728,-897.692545883996));
#151997=CARTESIAN_POINT('Ctrl Pts',(15.4104571591017,9.54175110365538,-899.186663531055));
#151998=CARTESIAN_POINT('Ctrl Pts',(16.1559070823762,8.04468584505496,-900.680781178114));
#151999=CARTESIAN_POINT('Ctrl Pts',(16.9013570056506,6.54762058645456,-902.174898825173));
#152000=CARTESIAN_POINT('Ctrl Pts',(17.3590292079831,4.93906964482096,-903.669016472231));
#152001=CARTESIAN_POINT('Ctrl Pts',(17.8167014103155,3.33051870318735,-905.16313411929));
#152002=CARTESIAN_POINT('Ctrl Pts',(17.9710104137728,1.66525935159367,-906.657251766349));
#152003=CARTESIAN_POINT('Ctrl Pts',(18.1253194172301,3.32956716117513E-15,
-908.151369413408));
#152004=CARTESIAN_POINT('Ctrl Pts',(17.9710104137728,-1.66525935159367,
-909.645487060466));
#152005=CARTESIAN_POINT('Ctrl Pts',(17.8167014103155,-3.33051870318736,
-911.139604707525));
#152006=CARTESIAN_POINT('Ctrl Pts',(17.3590292079831,-4.93906964482095,
-912.633722354584));
#152007=CARTESIAN_POINT('Ctrl Pts',(16.9013570056506,-6.54762058645456,
-914.127840001643));
#152008=CARTESIAN_POINT('Ctrl Pts',(16.1559070823762,-8.04468584505497,
-915.621957648702));
#152009=CARTESIAN_POINT('Ctrl Pts',(15.4104571591017,-9.54175110365538,
-917.116075295761));
#152010=CARTESIAN_POINT('Ctrl Pts',(14.4026149179538,-10.8763499173728,
-918.61019294282));
#152011=CARTESIAN_POINT('Ctrl Pts',(13.3947726768058,-12.2109487310903,
-920.104310589879));
#152012=CARTESIAN_POINT('Ctrl Pts',(12.1588589765331,-13.3376329379985,
-921.598428236937));
#152013=CARTESIAN_POINT('Ctrl Pts',(10.9229452762603,-14.4643171449067,
-923.092545883996));
#152014=CARTESIAN_POINT('Ctrl Pts',(9.50104767561053,-15.3447188656481,
-924.586663531055));
#152015=CARTESIAN_POINT('Ctrl Pts',(8.07915007496071,-16.2251205863895,
-926.080781178114));
#152016=CARTESIAN_POINT('Ctrl Pts',(6.51968959134574,-16.8292587962898,
-927.574898825172));
#152017=CARTESIAN_POINT('Ctrl Pts',(4.96022910773078,-17.4333970061901,
-929.069016472232));
#152018=CARTESIAN_POINT('Ctrl Pts',(3.31631129755346,-17.7406985030951,
-930.56313411929));
#152019=CARTESIAN_POINT('Ctrl Pts',(1.67239348737615,-18.048,-932.057251766349));
#152020=CARTESIAN_POINT('Ctrl Pts',(0.,-18.048,-933.551369413408));
#152021=CARTESIAN_POINT('Ctrl Pts',(-1.67239348737615,-18.048,-935.045487060467));
#152022=CARTESIAN_POINT('Ctrl Pts',(-3.31631129755346,-17.7406985030951,
-936.539604707525));
#152023=CARTESIAN_POINT('Ctrl Pts',(-4.96022910773077,-17.4333970061901,
-938.033722354584));
#152024=CARTESIAN_POINT('Ctrl Pts',(-6.51968959134574,-16.8292587962898,
-939.527840001643));
#152025=CARTESIAN_POINT('Ctrl Pts',(-8.07915007496071,-16.2251205863895,
-941.021957648702));
#152026=CARTESIAN_POINT('Ctrl Pts',(-9.50104767561052,-15.3447188656481,
-942.516075295761));
#152027=CARTESIAN_POINT('Ctrl Pts',(-10.9229452762603,-14.4643171449067,
-944.01019294282));
#152028=CARTESIAN_POINT('Ctrl Pts',(-12.1588589765331,-13.3376329379985,
-945.504310589878));
#152029=CARTESIAN_POINT('Ctrl Pts',(-13.3947726768058,-12.2109487310903,
-946.998428236937));
#152030=CARTESIAN_POINT('Ctrl Pts',(-14.4026149179538,-10.8763499173728,
-948.492545883996));
#152031=CARTESIAN_POINT('Ctrl Pts',(-15.4104571591017,-9.54175110365538,
-949.986663531055));
#152032=CARTESIAN_POINT('Ctrl Pts',(-16.1559070823762,-8.04468584505497,
-951.480781178113));
#152033=CARTESIAN_POINT('Ctrl Pts',(-16.9013570056506,-6.54762058645456,
-952.974898825173));
#152034=CARTESIAN_POINT('Ctrl Pts',(-17.3590292079831,-4.93906964482095,
-954.469016472231));
#152035=CARTESIAN_POINT('Ctrl Pts',(-17.8167014103155,-3.33051870318735,
-955.96313411929));
#152036=CARTESIAN_POINT('Ctrl Pts',(-17.9710104137728,-1.66525935159368,
-957.457251766349));
#152037=CARTESIAN_POINT('Ctrl Pts',(-18.1253194172301,-1.10985572039171E-15,
-958.951369413408));
#152038=CARTESIAN_POINT('Ctrl Pts',(-17.9710104137728,1.66525935159367,
-960.445487060467));
#152039=CARTESIAN_POINT('Ctrl Pts',(-17.8167014103155,3.33051870318735,
-961.939604707526));
#152040=CARTESIAN_POINT('Ctrl Pts',(-17.3590292079831,4.93906964482096,
-963.433722354584));
#152041=CARTESIAN_POINT('Ctrl Pts',(-16.9013570056506,6.54762058645456,
-964.927840001643));
#152042=CARTESIAN_POINT('Ctrl Pts',(-16.1559070823762,8.04468584505497,
-966.421957648702));
#152043=CARTESIAN_POINT('Ctrl Pts',(-15.4104571591017,9.54175110365538,
-967.916075295761));
#152044=CARTESIAN_POINT('Ctrl Pts',(-14.4026149179538,10.8763499173728,
-969.410192942819));
#152045=CARTESIAN_POINT('Ctrl Pts',(-13.3947726768058,12.2109487310903,
-970.904310589878));
#152046=CARTESIAN_POINT('Ctrl Pts',(-12.1588589765331,13.3376329379985,
-972.398428236937));
#152047=CARTESIAN_POINT('Ctrl Pts',(-10.9229452762603,14.4643171449067,
-973.892545883996));
#152048=CARTESIAN_POINT('Ctrl Pts',(-9.50104767561052,15.3447188656481,
-975.386663531055));
#152049=CARTESIAN_POINT('Ctrl Pts',(-8.07915007496071,16.2251205863895,
-976.880781178114));
#152050=CARTESIAN_POINT('Ctrl Pts',(-6.51968959134574,16.8292587962898,
-978.374898825173));
#152051=CARTESIAN_POINT('Ctrl Pts',(-4.96022910773078,17.4333970061901,
-979.869016472231));
#152052=CARTESIAN_POINT('Ctrl Pts',(-3.31631129755346,17.7406985030951,
-981.36313411929));
#152053=CARTESIAN_POINT('Ctrl Pts',(-1.67239348737615,18.048,-982.857251766349));
#152054=CARTESIAN_POINT('Ctrl Pts',(-2.21024254310115E-15,18.048,-984.351369413408));
#152055=CARTESIAN_POINT('Ctrl Pts',(1.67239348737616,18.048,-985.845487060466));
#152056=CARTESIAN_POINT('Ctrl Pts',(3.31631129755346,17.7406985030951,-987.339604707525));
#152057=CARTESIAN_POINT('Ctrl Pts',(4.96022910773077,17.4333970061901,-988.833722354585));
#152058=CARTESIAN_POINT('Ctrl Pts',(6.51968959134575,16.8292587962898,-990.327840001643));
#152059=CARTESIAN_POINT('Ctrl Pts',(8.07915007496071,16.2251205863895,-991.821957648702));
#152060=CARTESIAN_POINT('Ctrl Pts',(9.50104767561053,15.3447188656481,-993.316075295761));
#152061=CARTESIAN_POINT('Ctrl Pts',(10.9229452762603,14.4643171449067,-994.81019294282));
#152062=CARTESIAN_POINT('Ctrl Pts',(12.1588589765331,13.3376329379985,-996.304310589878));
#152063=CARTESIAN_POINT('Ctrl Pts',(13.3947726768058,12.2109487310903,-997.798428236937));
#152064=CARTESIAN_POINT('Ctrl Pts',(14.4026149179538,10.8763499173728,-999.292545883996));
#152065=CARTESIAN_POINT('Ctrl Pts',(15.4104571591017,9.54175110365538,-1000.78666353105));
#152066=CARTESIAN_POINT('Ctrl Pts',(16.1559070823762,8.04468584505496,-1002.28078117811));
#152067=CARTESIAN_POINT('Ctrl Pts',(16.9013570056506,6.54762058645456,-1003.77489882517));
#152068=CARTESIAN_POINT('Ctrl Pts',(17.3590292079831,4.93906964482096,-1005.26901647223));
#152069=CARTESIAN_POINT('Ctrl Pts',(17.8167014103155,3.33051870318735,-1006.76313411929));
#152070=CARTESIAN_POINT('Ctrl Pts',(17.9710104137728,1.66525935159367,-1008.25725176635));
#152071=CARTESIAN_POINT('Ctrl Pts',(18.1253194172301,3.32956716117513E-15,
-1009.75136941341));
#152072=CARTESIAN_POINT('Ctrl Pts',(17.9710104137728,-1.66525935159367,
-1011.24548706047));
#152073=CARTESIAN_POINT('Ctrl Pts',(17.8167014103155,-3.33051870318736,
-1012.73960470753));
#152074=CARTESIAN_POINT('Ctrl Pts',(17.3590292079831,-4.93906964482095,
-1014.23372235458));
#152075=CARTESIAN_POINT('Ctrl Pts',(16.9013570056506,-6.54762058645456,
-1015.72784000164));
#152076=CARTESIAN_POINT('Ctrl Pts',(16.1559070823762,-8.04468584505497,
-1017.2219576487));
#152077=CARTESIAN_POINT('Ctrl Pts',(15.4104571591017,-9.54175110365538,
-1018.71607529576));
#152078=CARTESIAN_POINT('Ctrl Pts',(14.4026149179538,-10.8763499173728,
-1020.21019294282));
#152079=CARTESIAN_POINT('Ctrl Pts',(13.3947726768058,-12.2109487310903,
-1021.70431058988));
#152080=CARTESIAN_POINT('Ctrl Pts',(12.1588589765331,-13.3376329379985,
-1023.19842823694));
#152081=CARTESIAN_POINT('Ctrl Pts',(10.9229452762603,-14.4643171449067,
-1024.692545884));
#152082=CARTESIAN_POINT('Ctrl Pts',(9.50104767561053,-15.3447188656481,
-1026.18666353105));
#152083=CARTESIAN_POINT('Ctrl Pts',(8.07915007496071,-16.2251205863895,
-1027.68078117811));
#152084=CARTESIAN_POINT('Ctrl Pts',(6.51968959134574,-16.8292587962898,
-1029.17489882517));
#152085=CARTESIAN_POINT('Ctrl Pts',(4.96022910773078,-17.4333970061901,
-1030.66901647223));
#152086=CARTESIAN_POINT('Ctrl Pts',(3.31631129755346,-17.7406985030951,
-1032.16313411929));
#152087=CARTESIAN_POINT('Ctrl Pts',(1.67239348737615,-18.048,-1033.65725176635));
#152088=CARTESIAN_POINT('Ctrl Pts',(0.,-18.048,-1035.15136941341));
#152089=CARTESIAN_POINT('Ctrl Pts',(-1.67239348737615,-18.048,-1036.64548706047));
#152090=CARTESIAN_POINT('Ctrl Pts',(-3.31631129755346,-17.7406985030951,
-1038.13960470753));
#152091=CARTESIAN_POINT('Ctrl Pts',(-4.96022910773077,-17.4333970061901,
-1039.63372235458));
#152092=CARTESIAN_POINT('Ctrl Pts',(-6.51968959134574,-16.8292587962898,
-1041.12784000164));
#152093=CARTESIAN_POINT('Ctrl Pts',(-8.07915007496071,-16.2251205863895,
-1042.6219576487));
#152094=CARTESIAN_POINT('Ctrl Pts',(-9.50104767561052,-15.3447188656481,
-1044.11607529576));
#152095=CARTESIAN_POINT('Ctrl Pts',(-10.9229452762603,-14.4643171449067,
-1045.61019294282));
#152096=CARTESIAN_POINT('Ctrl Pts',(-12.1588589765331,-13.3376329379985,
-1047.10431058988));
#152097=CARTESIAN_POINT('Ctrl Pts',(-13.3947726768058,-12.2109487310903,
-1048.59842823694));
#152098=CARTESIAN_POINT('Ctrl Pts',(-14.4026149179538,-10.8763499173728,
-1050.092545884));
#152099=CARTESIAN_POINT('Ctrl Pts',(-15.4104571591017,-9.54175110365538,
-1051.58666353105));
#152100=CARTESIAN_POINT('Ctrl Pts',(-16.1559070823762,-8.04468584505497,
-1053.08078117811));
#152101=CARTESIAN_POINT('Ctrl Pts',(-16.9013570056506,-6.54762058645456,
-1054.57489882517));
#152102=CARTESIAN_POINT('Ctrl Pts',(-17.3590292079831,-4.93906964482095,
-1056.06901647223));
#152103=CARTESIAN_POINT('Ctrl Pts',(-17.8167014103155,-3.33051870318735,
-1057.56313411929));
#152104=CARTESIAN_POINT('Ctrl Pts',(-17.9710104137728,-1.66525935159368,
-1059.05725176635));
#152105=CARTESIAN_POINT('Ctrl Pts',(-18.1253194172301,-1.10985572039171E-15,
-1060.55136941341));
#152106=CARTESIAN_POINT('Ctrl Pts',(-17.9710104137728,1.66525935159367,
-1062.04548706047));
#152107=CARTESIAN_POINT('Ctrl Pts',(-17.8167014103155,3.33051870318735,
-1063.53960470753));
#152108=CARTESIAN_POINT('Ctrl Pts',(-17.3590292079831,4.93906964482096,
-1065.03372235458));
#152109=CARTESIAN_POINT('Ctrl Pts',(-16.9013570056506,6.54762058645456,
-1066.52784000164));
#152110=CARTESIAN_POINT('Ctrl Pts',(-16.1559070823762,8.04468584505497,
-1068.0219576487));
#152111=CARTESIAN_POINT('Ctrl Pts',(-15.4104571591017,9.54175110365538,
-1069.51607529576));
#152112=CARTESIAN_POINT('Ctrl Pts',(-14.4026149179538,10.8763499173728,
-1071.01019294282));
#152113=CARTESIAN_POINT('Ctrl Pts',(-13.3947726768058,12.2109487310903,
-1072.50431058988));
#152114=CARTESIAN_POINT('Ctrl Pts',(-12.1588589765331,13.3376329379985,
-1073.99842823694));
#152115=CARTESIAN_POINT('Ctrl Pts',(-10.9229452762603,14.4643171449067,
-1075.492545884));
#152116=CARTESIAN_POINT('Ctrl Pts',(-9.50104767561052,15.3447188656481,
-1076.98666353105));
#152117=CARTESIAN_POINT('Ctrl Pts',(-8.07915007496071,16.2251205863895,
-1078.48078117811));
#152118=CARTESIAN_POINT('Ctrl Pts',(-6.51968959134574,16.8292587962898,
-1079.97489882517));
#152119=CARTESIAN_POINT('Ctrl Pts',(-4.96022910773078,17.4333970061901,
-1081.46901647223));
#152120=CARTESIAN_POINT('Ctrl Pts',(-3.31631129755346,17.7406985030951,
-1082.96313411929));
#152121=CARTESIAN_POINT('Ctrl Pts',(-1.67239348737615,18.048,-1084.45725176635));
#152122=CARTESIAN_POINT('Ctrl Pts',(-2.21024254310115E-15,18.048,-1085.95136941341));
#152123=CARTESIAN_POINT('Ctrl Pts',(1.67239348737616,18.048,-1087.44548706047));
#152124=CARTESIAN_POINT('Ctrl Pts',(3.31631129755346,17.7406985030951,-1088.93960470753));
#152125=CARTESIAN_POINT('Ctrl Pts',(4.96022910773077,17.4333970061901,-1090.43372235458));
#152126=CARTESIAN_POINT('Ctrl Pts',(6.51968959134575,16.8292587962898,-1091.92784000164));
#152127=CARTESIAN_POINT('Ctrl Pts',(8.07915007496071,16.2251205863895,-1093.4219576487));
#152128=CARTESIAN_POINT('Ctrl Pts',(9.50104767561053,15.3447188656481,-1094.91607529576));
#152129=CARTESIAN_POINT('Ctrl Pts',(10.9229452762603,14.4643171449067,-1096.41019294282));
#152130=CARTESIAN_POINT('Ctrl Pts',(12.1588589765331,13.3376329379985,-1097.90431058988));
#152131=CARTESIAN_POINT('Ctrl Pts',(13.3947726768058,12.2109487310903,-1099.39842823694));
#152132=CARTESIAN_POINT('Ctrl Pts',(14.4026149179538,10.8763499173728,-1100.892545884));
#152133=CARTESIAN_POINT('Ctrl Pts',(15.4104571591017,9.54175110365538,-1102.38666353105));
#152134=CARTESIAN_POINT('Ctrl Pts',(16.1559070823762,8.04468584505496,-1103.88078117811));
#152135=CARTESIAN_POINT('Ctrl Pts',(16.9013570056506,6.54762058645456,-1105.37489882517));
#152136=CARTESIAN_POINT('Ctrl Pts',(17.3590292079831,4.93906964482096,-1106.86901647223));
#152137=CARTESIAN_POINT('Ctrl Pts',(17.8167014103155,3.33051870318735,-1108.36313411929));
#152138=CARTESIAN_POINT('Ctrl Pts',(17.9710104137728,1.66525935159367,-1109.85725176635));
#152139=CARTESIAN_POINT('Ctrl Pts',(18.1253194172301,3.32956716117513E-15,
-1111.35136941341));
#152140=CARTESIAN_POINT('Ctrl Pts',(17.9710104137728,-1.66525935159367,
-1112.84548706047));
#152141=CARTESIAN_POINT('Ctrl Pts',(17.8167014103155,-3.33051870318736,
-1114.33960470753));
#152142=CARTESIAN_POINT('Ctrl Pts',(17.3590292079831,-4.93906964482095,
-1115.83372235458));
#152143=CARTESIAN_POINT('Ctrl Pts',(16.9013570056506,-6.54762058645456,
-1117.32784000164));
#152144=CARTESIAN_POINT('Ctrl Pts',(16.1559070823762,-8.04468584505497,
-1118.8219576487));
#152145=CARTESIAN_POINT('Ctrl Pts',(15.4104571591017,-9.54175110365538,
-1120.31607529576));
#152146=CARTESIAN_POINT('Ctrl Pts',(14.4026149179538,-10.8763499173728,
-1121.81019294282));
#152147=CARTESIAN_POINT('Ctrl Pts',(13.3947726768058,-12.2109487310903,
-1123.30431058988));
#152148=CARTESIAN_POINT('Ctrl Pts',(12.1588589765331,-13.3376329379985,
-1124.79842823694));
#152149=CARTESIAN_POINT('Ctrl Pts',(10.9229452762603,-14.4643171449067,
-1126.292545884));
#152150=CARTESIAN_POINT('Ctrl Pts',(9.50104767561053,-15.3447188656481,
-1127.78666353106));
#152151=CARTESIAN_POINT('Ctrl Pts',(8.07915007496071,-16.2251205863895,
-1129.28078117811));
#152152=CARTESIAN_POINT('Ctrl Pts',(6.51968959134574,-16.8292587962898,
-1130.77489882517));
#152153=CARTESIAN_POINT('Ctrl Pts',(4.96022910773078,-17.4333970061901,
-1132.26901647223));
#152154=CARTESIAN_POINT('Ctrl Pts',(3.31631129755346,-17.7406985030951,
-1133.76313411929));
#152155=CARTESIAN_POINT('Ctrl Pts',(1.67239348737615,-18.048,-1135.25725176635));
#152156=CARTESIAN_POINT('Ctrl Pts',(0.,-18.048,-1136.75136941341));
#152157=CARTESIAN_POINT('Ctrl Pts',(-1.67239348737615,-18.048,-1138.24548706047));
#152158=CARTESIAN_POINT('Ctrl Pts',(-3.31631129755346,-17.7406985030951,
-1139.73960470753));
#152159=CARTESIAN_POINT('Ctrl Pts',(-4.96022910773077,-17.4333970061901,
-1141.23372235458));
#152160=CARTESIAN_POINT('Ctrl Pts',(-6.51968959134574,-16.8292587962898,
-1142.72784000164));
#152161=CARTESIAN_POINT('Ctrl Pts',(-8.07915007496071,-16.2251205863895,
-1144.2219576487));
#152162=CARTESIAN_POINT('Ctrl Pts',(-9.50104767561052,-15.3447188656481,
-1145.71607529576));
#152163=CARTESIAN_POINT('Ctrl Pts',(-10.9229452762603,-14.4643171449067,
-1147.21019294282));
#152164=CARTESIAN_POINT('Ctrl Pts',(-12.1588589765331,-13.3376329379985,
-1148.70431058988));
#152165=CARTESIAN_POINT('Ctrl Pts',(-13.3947726768058,-12.2109487310903,
-1150.19842823694));
#152166=CARTESIAN_POINT('Ctrl Pts',(-14.4026149179538,-10.8763499173728,
-1151.692545884));
#152167=CARTESIAN_POINT('Ctrl Pts',(-15.4104571591017,-9.54175110365538,
-1153.18666353105));
#152168=CARTESIAN_POINT('Ctrl Pts',(-16.1559070823762,-8.04468584505497,
-1154.68078117811));
#152169=CARTESIAN_POINT('Ctrl Pts',(-16.9013570056506,-6.54762058645456,
-1156.17489882517));
#152170=CARTESIAN_POINT('Ctrl Pts',(-17.3590292079831,-4.93906964482095,
-1157.66901647223));
#152171=CARTESIAN_POINT('Ctrl Pts',(-17.8167014103155,-3.33051870318735,
-1159.16313411929));
#152172=CARTESIAN_POINT('Ctrl Pts',(-17.9710104137728,-1.66525935159368,
-1160.65725176635));
#152173=CARTESIAN_POINT('Ctrl Pts',(-18.1253194172301,-1.10985572039171E-15,
-1162.15136941341));
#152174=CARTESIAN_POINT('Ctrl Pts',(-17.9710104137728,1.66525935159367,
-1163.64548706047));
#152175=CARTESIAN_POINT('Ctrl Pts',(-17.8167014103155,3.33051870318735,
-1165.13960470753));
#152176=CARTESIAN_POINT('Ctrl Pts',(-17.3590292079831,4.93906964482096,
-1166.63372235458));
#152177=CARTESIAN_POINT('Ctrl Pts',(-16.9013570056506,6.54762058645456,
-1168.12784000164));
#152178=CARTESIAN_POINT('Ctrl Pts',(-16.1559070823762,8.04468584505497,
-1169.6219576487));
#152179=CARTESIAN_POINT('Ctrl Pts',(-15.4104571591017,9.54175110365538,
-1171.11607529576));
#152180=CARTESIAN_POINT('Ctrl Pts',(-14.4026149179538,10.8763499173728,
-1172.61019294282));
#152181=CARTESIAN_POINT('Ctrl Pts',(-13.3947726768058,12.2109487310903,
-1174.10431058988));
#152182=CARTESIAN_POINT('Ctrl Pts',(-12.1588589765331,13.3376329379985,
-1175.59842823694));
#152183=CARTESIAN_POINT('Ctrl Pts',(-10.9229452762603,14.4643171449067,
-1177.092545884));
#152184=CARTESIAN_POINT('Ctrl Pts',(-9.50104767561052,15.3447188656481,
-1178.58666353105));
#152185=CARTESIAN_POINT('Ctrl Pts',(-8.07915007496071,16.2251205863895,
-1180.08078117811));
#152186=CARTESIAN_POINT('Ctrl Pts',(-6.51968959134574,16.8292587962898,
-1181.57489882517));
#152187=CARTESIAN_POINT('Ctrl Pts',(-4.96022910773078,17.4333970061901,
-1183.06901647223));
#152188=CARTESIAN_POINT('Ctrl Pts',(-3.31631129755346,17.7406985030951,
-1184.56313411929));
#152189=CARTESIAN_POINT('Ctrl Pts',(-1.67239348737615,18.048,-1186.05725176635));
#152190=CARTESIAN_POINT('Ctrl Pts',(-2.21024254310115E-15,18.048,-1187.55136941341));
#152191=CARTESIAN_POINT('Ctrl Pts',(1.67239348737616,18.048,-1189.04548706047));
#152192=CARTESIAN_POINT('Ctrl Pts',(3.31631129755346,17.7406985030951,-1190.53960470753));
#152193=CARTESIAN_POINT('Ctrl Pts',(4.96022910773077,17.4333970061901,-1192.03372235458));
#152194=CARTESIAN_POINT('Ctrl Pts',(6.51968959134575,16.8292587962898,-1193.52784000164));
#152195=CARTESIAN_POINT('Ctrl Pts',(8.07915007496071,16.2251205863895,-1195.0219576487));
#152196=CARTESIAN_POINT('Ctrl Pts',(9.50104767561053,15.3447188656481,-1196.51607529576));
#152197=CARTESIAN_POINT('Ctrl Pts',(10.9229452762603,14.4643171449067,-1198.01019294282));
#152198=CARTESIAN_POINT('Ctrl Pts',(12.1588589765331,13.3376329379985,-1199.50431058988));
#152199=CARTESIAN_POINT('Ctrl Pts',(13.3947726768058,12.2109487310903,-1200.99842823694));
#152200=CARTESIAN_POINT('Ctrl Pts',(14.4026149179538,10.8763499173728,-1202.492545884));
#152201=CARTESIAN_POINT('Ctrl Pts',(15.4104571591017,9.54175110365538,-1203.98666353106));
#152202=CARTESIAN_POINT('Ctrl Pts',(16.1559070823762,8.04468584505496,-1205.48078117811));
#152203=CARTESIAN_POINT('Ctrl Pts',(16.9013570056506,6.54762058645456,-1206.97489882517));
#152204=CARTESIAN_POINT('Ctrl Pts',(17.3590292079831,4.93906964482096,-1208.46901647223));
#152205=CARTESIAN_POINT('Ctrl Pts',(17.8167014103155,3.33051870318735,-1209.96313411929));
#152206=CARTESIAN_POINT('Ctrl Pts',(17.9710104137728,1.66525935159367,-1211.45725176635));
#152207=CARTESIAN_POINT('Ctrl Pts',(18.1253194172301,3.32956716117513E-15,
-1212.95136941341));
#152208=CARTESIAN_POINT('Ctrl Pts',(17.9710104137728,-1.66525935159367,
-1214.44548706047));
#152209=CARTESIAN_POINT('Ctrl Pts',(17.8167014103155,-3.33051870318736,
-1215.93960470753));
#152210=CARTESIAN_POINT('Ctrl Pts',(17.3590292079831,-4.93906964482095,
-1217.43372235458));
#152211=CARTESIAN_POINT('Ctrl Pts',(16.9013570056506,-6.54762058645456,
-1218.92784000164));
#152212=CARTESIAN_POINT('Ctrl Pts',(16.1559070823762,-8.04468584505497,
-1220.4219576487));
#152213=CARTESIAN_POINT('Ctrl Pts',(15.4104571591017,-9.54175110365538,
-1221.91607529576));
#152214=CARTESIAN_POINT('Ctrl Pts',(14.4026149179538,-10.8763499173728,
-1223.41019294282));
#152215=CARTESIAN_POINT('Ctrl Pts',(13.3947726768058,-12.2109487310903,
-1224.90431058988));
#152216=CARTESIAN_POINT('Ctrl Pts',(12.1588589765331,-13.3376329379985,
-1226.39842823694));
#152217=CARTESIAN_POINT('Ctrl Pts',(10.9229452762603,-14.4643171449067,
-1227.892545884));
#152218=CARTESIAN_POINT('Ctrl Pts',(9.50104767561053,-15.3447188656481,
-1229.38666353105));
#152219=CARTESIAN_POINT('Ctrl Pts',(8.07915007496071,-16.2251205863895,
-1230.88078117811));
#152220=CARTESIAN_POINT('Ctrl Pts',(6.51968959134574,-16.8292587962898,
-1232.37489882517));
#152221=CARTESIAN_POINT('Ctrl Pts',(4.96022910773078,-17.4333970061901,
-1233.86901647223));
#152222=CARTESIAN_POINT('Ctrl Pts',(3.31631129755346,-17.7406985030951,
-1235.36313411929));
#152223=CARTESIAN_POINT('Ctrl Pts',(1.67239348737615,-18.048,-1236.85725176635));
#152224=CARTESIAN_POINT('Ctrl Pts',(0.,-18.048,-1238.35136941341));
#152225=CARTESIAN_POINT('Ctrl Pts',(-1.67239348737615,-18.048,-1239.84548706047));
#152226=CARTESIAN_POINT('Ctrl Pts',(-3.31631129755346,-17.7406985030951,
-1241.33960470753));
#152227=CARTESIAN_POINT('Ctrl Pts',(-4.96022910773077,-17.4333970061901,
-1242.83372235458));
#152228=CARTESIAN_POINT('Ctrl Pts',(-6.51968959134574,-16.8292587962898,
-1244.32784000164));
#152229=CARTESIAN_POINT('Ctrl Pts',(-8.07915007496071,-16.2251205863895,
-1245.8219576487));
#152230=CARTESIAN_POINT('Ctrl Pts',(-9.50104767561052,-15.3447188656481,
-1247.31607529576));
#152231=CARTESIAN_POINT('Ctrl Pts',(-10.9229452762603,-14.4643171449067,
-1248.81019294282));
#152232=CARTESIAN_POINT('Ctrl Pts',(-12.1588589765331,-13.3376329379985,
-1250.30431058988));
#152233=CARTESIAN_POINT('Ctrl Pts',(-13.3947726768058,-12.2109487310903,
-1251.79842823694));
#152234=CARTESIAN_POINT('Ctrl Pts',(-14.4026149179538,-10.8763499173728,
-1253.292545884));
#152235=CARTESIAN_POINT('Ctrl Pts',(-15.4104571591017,-9.54175110365538,
-1254.78666353105));
#152236=CARTESIAN_POINT('Ctrl Pts',(-16.1559070823762,-8.04468584505497,
-1256.28078117811));
#152237=CARTESIAN_POINT('Ctrl Pts',(-16.9013570056506,-6.54762058645456,
-1257.77489882517));
#152238=CARTESIAN_POINT('Ctrl Pts',(-17.3590292079831,-4.93906964482095,
-1259.26901647223));
#152239=CARTESIAN_POINT('Ctrl Pts',(-17.8167014103155,-3.33051870318735,
-1260.76313411929));
#152240=CARTESIAN_POINT('Ctrl Pts',(-17.9710104137728,-1.66525935159368,
-1262.25725176635));
#152241=CARTESIAN_POINT('Ctrl Pts',(-18.1253194172301,-1.10985572039171E-15,
-1263.75136941341));
#152242=CARTESIAN_POINT('Ctrl Pts',(-17.9710104137728,1.66525935159367,
-1265.24548706047));
#152243=CARTESIAN_POINT('Ctrl Pts',(-17.8167014103155,3.33051870318735,
-1266.73960470753));
#152244=CARTESIAN_POINT('Ctrl Pts',(-17.3590292079831,4.93906964482096,
-1268.23372235458));
#152245=CARTESIAN_POINT('Ctrl Pts',(-16.9013570056506,6.54762058645456,
-1269.72784000164));
#152246=CARTESIAN_POINT('Ctrl Pts',(-16.1559070823762,8.04468584505497,
-1271.2219576487));
#152247=CARTESIAN_POINT('Ctrl Pts',(-15.4104571591017,9.54175110365538,
-1272.71607529576));
#152248=CARTESIAN_POINT('Ctrl Pts',(-14.4026149179538,10.8763499173728,
-1274.21019294282));
#152249=CARTESIAN_POINT('Ctrl Pts',(-13.3947726768058,12.2109487310903,
-1275.70431058988));
#152250=CARTESIAN_POINT('Ctrl Pts',(-12.1588589765331,13.3376329379985,
-1277.19842823694));
#152251=CARTESIAN_POINT('Ctrl Pts',(-10.9229452762603,14.4643171449067,
-1278.692545884));
#152252=CARTESIAN_POINT('Ctrl Pts',(-9.50104767561052,15.3447188656481,
-1280.18666353105));
#152253=CARTESIAN_POINT('Ctrl Pts',(-8.07915007496071,16.2251205863895,
-1281.68078117811));
#152254=CARTESIAN_POINT('Ctrl Pts',(-6.51968959134574,16.8292587962898,
-1283.17489882517));
#152255=CARTESIAN_POINT('Ctrl Pts',(-4.96022910773078,17.4333970061901,
-1284.66901647223));
#152256=CARTESIAN_POINT('Ctrl Pts',(-3.31631129755346,17.7406985030951,
-1286.16313411929));
#152257=CARTESIAN_POINT('Ctrl Pts',(-1.67239348737615,18.048,-1287.65725176635));
#152258=CARTESIAN_POINT('Ctrl Pts',(-2.21024254310115E-15,18.048,-1289.15136941341));
#152259=CARTESIAN_POINT('Ctrl Pts',(1.67239348737616,18.048,-1290.64548706047));
#152260=CARTESIAN_POINT('Ctrl Pts',(3.31631129755346,17.7406985030951,-1292.13960470753));
#152261=CARTESIAN_POINT('Ctrl Pts',(4.96022910773077,17.4333970061901,-1293.63372235458));
#152262=CARTESIAN_POINT('Ctrl Pts',(6.51968959134575,16.8292587962898,-1295.12784000164));
#152263=CARTESIAN_POINT('Ctrl Pts',(8.07915007496071,16.2251205863895,-1296.6219576487));
#152264=CARTESIAN_POINT('Ctrl Pts',(9.50104767561053,15.3447188656481,-1298.11607529576));
#152265=CARTESIAN_POINT('Ctrl Pts',(10.9229452762603,14.4643171449067,-1299.61019294282));
#152266=CARTESIAN_POINT('Ctrl Pts',(12.1588589765331,13.3376329379985,-1301.10431058988));
#152267=CARTESIAN_POINT('Ctrl Pts',(13.3947726768058,12.2109487310903,-1302.59842823694));
#152268=CARTESIAN_POINT('Ctrl Pts',(14.4026149179538,10.8763499173728,-1304.092545884));
#152269=CARTESIAN_POINT('Ctrl Pts',(15.4104571591017,9.54175110365538,-1305.58666353106));
#152270=CARTESIAN_POINT('Ctrl Pts',(16.1559070823762,8.04468584505496,-1307.08078117811));
#152271=CARTESIAN_POINT('Ctrl Pts',(16.9013570056506,6.54762058645456,-1308.57489882517));
#152272=CARTESIAN_POINT('Ctrl Pts',(17.3590292079831,4.93906964482096,-1310.06901647223));
#152273=CARTESIAN_POINT('Ctrl Pts',(17.8167014103155,3.33051870318735,-1311.56313411929));
#152274=CARTESIAN_POINT('Ctrl Pts',(17.9710104137728,1.66525935159367,-1313.05725176635));
#152275=CARTESIAN_POINT('Ctrl Pts',(18.1253194172301,3.32956716117513E-15,
-1314.55136941341));
#152276=CARTESIAN_POINT('Ctrl Pts',(17.9710104137728,-1.66525935159367,
-1316.04548706047));
#152277=CARTESIAN_POINT('Ctrl Pts',(17.8167014103155,-3.33051870318736,
-1317.53960470753));
#152278=CARTESIAN_POINT('Ctrl Pts',(17.3590292079831,-4.93906964482095,
-1319.03372235458));
#152279=CARTESIAN_POINT('Ctrl Pts',(16.9013570056506,-6.54762058645456,
-1320.52784000164));
#152280=CARTESIAN_POINT('Ctrl Pts',(16.1559070823762,-8.04468584505497,
-1322.0219576487));
#152281=CARTESIAN_POINT('Ctrl Pts',(15.4104571591017,-9.54175110365538,
-1323.51607529576));
#152282=CARTESIAN_POINT('Ctrl Pts',(14.4026149179538,-10.8763499173728,
-1325.01019294282));
#152283=CARTESIAN_POINT('Ctrl Pts',(13.3947726768058,-12.2109487310903,
-1326.50431058988));
#152284=CARTESIAN_POINT('Ctrl Pts',(12.1588589765331,-13.3376329379985,
-1327.99842823694));
#152285=CARTESIAN_POINT('Ctrl Pts',(10.9229452762603,-14.4643171449067,
-1329.492545884));
#152286=CARTESIAN_POINT('Ctrl Pts',(9.50104767561053,-15.3447188656481,
-1330.98666353105));
#152287=CARTESIAN_POINT('Ctrl Pts',(8.07915007496071,-16.2251205863895,
-1332.48078117811));
#152288=CARTESIAN_POINT('Ctrl Pts',(6.51968959134574,-16.8292587962898,
-1333.97489882517));
#152289=CARTESIAN_POINT('Ctrl Pts',(4.96022910773078,-17.4333970061901,
-1335.46901647223));
#152290=CARTESIAN_POINT('Ctrl Pts',(3.31631129755346,-17.7406985030951,
-1336.96313411929));
#152291=CARTESIAN_POINT('Ctrl Pts',(1.67239348737615,-18.048,-1338.45725176635));
#152292=CARTESIAN_POINT('Ctrl Pts',(0.,-18.048,-1339.95136941341));
#152293=CARTESIAN_POINT('Ctrl Pts',(-1.67239348737615,-18.048,-1341.44548706047));
#152294=CARTESIAN_POINT('Ctrl Pts',(-3.31631129755346,-17.7406985030951,
-1342.93960470753));
#152295=CARTESIAN_POINT('Ctrl Pts',(-4.96022910773077,-17.4333970061901,
-1344.43372235458));
#152296=CARTESIAN_POINT('Ctrl Pts',(-6.51968959134574,-16.8292587962898,
-1345.92784000164));
#152297=CARTESIAN_POINT('Ctrl Pts',(-8.07915007496071,-16.2251205863895,
-1347.4219576487));
#152298=CARTESIAN_POINT('Ctrl Pts',(-9.50104767561052,-15.3447188656481,
-1348.91607529576));
#152299=CARTESIAN_POINT('Ctrl Pts',(-10.9229452762603,-14.4643171449067,
-1350.41019294282));
#152300=CARTESIAN_POINT('Ctrl Pts',(-12.1588589765331,-13.3376329379985,
-1351.90431058988));
#152301=CARTESIAN_POINT('Ctrl Pts',(-13.3947726768058,-12.2109487310903,
-1353.39842823694));
#152302=CARTESIAN_POINT('Ctrl Pts',(-14.4026149179538,-10.8763499173728,
-1354.892545884));
#152303=CARTESIAN_POINT('Ctrl Pts',(-15.4104571591017,-9.54175110365538,
-1356.38666353105));
#152304=CARTESIAN_POINT('Ctrl Pts',(-16.1559070823762,-8.04468584505497,
-1357.88078117811));
#152305=CARTESIAN_POINT('Ctrl Pts',(-16.9013570056506,-6.54762058645456,
-1359.37489882517));
#152306=CARTESIAN_POINT('Ctrl Pts',(-17.3590292079831,-4.93906964482095,
-1360.86901647223));
#152307=CARTESIAN_POINT('Ctrl Pts',(-17.8167014103155,-3.33051870318735,
-1362.36313411929));
#152308=CARTESIAN_POINT('Ctrl Pts',(-17.9710104137728,-1.66525935159368,
-1363.85725176635));
#152309=CARTESIAN_POINT('Ctrl Pts',(-18.1253194172301,-1.10985572039171E-15,
-1365.35136941341));
#152310=CARTESIAN_POINT('Ctrl Pts',(-17.9710104137728,1.66525935159367,
-1366.84548706047));
#152311=CARTESIAN_POINT('Ctrl Pts',(-17.8167014103155,3.33051870318735,
-1368.33960470753));
#152312=CARTESIAN_POINT('Ctrl Pts',(-17.3590292079831,4.93906964482096,
-1369.83372235458));
#152313=CARTESIAN_POINT('Ctrl Pts',(-16.9013570056506,6.54762058645456,
-1371.32784000164));
#152314=CARTESIAN_POINT('Ctrl Pts',(-16.1559070823762,8.04468584505497,
-1372.8219576487));
#152315=CARTESIAN_POINT('Ctrl Pts',(-15.4104571591017,9.54175110365538,
-1374.31607529576));
#152316=CARTESIAN_POINT('Ctrl Pts',(-14.4026149179538,10.8763499173728,
-1375.81019294282));
#152317=CARTESIAN_POINT('Ctrl Pts',(-13.3947726768058,12.2109487310903,
-1377.30431058988));
#152318=CARTESIAN_POINT('Ctrl Pts',(-12.1588589765331,13.3376329379985,
-1378.79842823694));
#152319=CARTESIAN_POINT('Ctrl Pts',(-10.9229452762603,14.4643171449067,
-1380.292545884));
#152320=CARTESIAN_POINT('Ctrl Pts',(-9.50104767561052,15.3447188656481,
-1381.78666353106));
#152321=CARTESIAN_POINT('Ctrl Pts',(-8.07915007496071,16.2251205863895,
-1383.28078117811));
#152322=CARTESIAN_POINT('Ctrl Pts',(-6.51968959134574,16.8292587962898,
-1384.77489882517));
#152323=CARTESIAN_POINT('Ctrl Pts',(-4.96022910773078,17.4333970061901,
-1386.26901647223));
#152324=CARTESIAN_POINT('Ctrl Pts',(-3.31631129755346,17.7406985030951,
-1387.76313411929));
#152325=CARTESIAN_POINT('Ctrl Pts',(-1.67239348737615,18.048,-1389.25725176635));
#152326=CARTESIAN_POINT('Ctrl Pts',(-2.21024254310115E-15,18.048,-1390.75136941341));
#152327=CARTESIAN_POINT('Ctrl Pts',(1.67239348737616,18.048,-1392.24548706047));
#152328=CARTESIAN_POINT('Ctrl Pts',(3.31631129755346,17.7406985030951,-1393.73960470753));
#152329=CARTESIAN_POINT('Ctrl Pts',(4.96022910773077,17.4333970061901,-1395.23372235458));
#152330=CARTESIAN_POINT('Ctrl Pts',(6.51968959134575,16.8292587962898,-1396.72784000164));
#152331=CARTESIAN_POINT('Ctrl Pts',(8.07915007496071,16.2251205863895,-1398.2219576487));
#152332=CARTESIAN_POINT('Ctrl Pts',(9.50104767561053,15.3447188656481,-1399.71607529576));
#152333=CARTESIAN_POINT('Ctrl Pts',(10.9229452762603,14.4643171449067,-1401.21019294282));
#152334=CARTESIAN_POINT('Ctrl Pts',(12.1588589765331,13.3376329379985,-1402.70431058988));
#152335=CARTESIAN_POINT('Ctrl Pts',(13.3947726768058,12.2109487310903,-1404.19842823694));
#152336=CARTESIAN_POINT('Ctrl Pts',(14.4026149179538,10.8763499173728,-1405.692545884));
#152337=CARTESIAN_POINT('Ctrl Pts',(15.4104571591017,9.54175110365538,-1407.18666353106));
#152338=CARTESIAN_POINT('Ctrl Pts',(16.1559070823762,8.04468584505496,-1408.68078117811));
#152339=CARTESIAN_POINT('Ctrl Pts',(16.9013570056506,6.54762058645456,-1410.17489882517));
#152340=CARTESIAN_POINT('Ctrl Pts',(17.3590292079831,4.93906964482096,-1411.66901647223));
#152341=CARTESIAN_POINT('Ctrl Pts',(17.8167014103155,3.33051870318735,-1413.16313411929));
#152342=CARTESIAN_POINT('Ctrl Pts',(17.9710104137728,1.66525935159367,-1414.65725176635));
#152343=CARTESIAN_POINT('Ctrl Pts',(18.1253194172301,3.32956716117513E-15,
-1416.15136941341));
#152344=CARTESIAN_POINT('Ctrl Pts',(17.9710104137728,-1.66525935159367,
-1417.64548706047));
#152345=CARTESIAN_POINT('Ctrl Pts',(17.8167014103155,-3.33051870318736,
-1419.13960470753));
#152346=CARTESIAN_POINT('Ctrl Pts',(17.3590292079831,-4.93906964482095,
-1420.63372235458));
#152347=CARTESIAN_POINT('Ctrl Pts',(16.9013570056506,-6.54762058645456,
-1422.12784000164));
#152348=CARTESIAN_POINT('Ctrl Pts',(16.1559070823762,-8.04468584505497,
-1423.6219576487));
#152349=CARTESIAN_POINT('Ctrl Pts',(15.4104571591017,-9.54175110365538,
-1425.11607529576));
#152350=CARTESIAN_POINT('Ctrl Pts',(14.4026149179538,-10.8763499173728,
-1426.61019294282));
#152351=CARTESIAN_POINT('Ctrl Pts',(13.3947726768058,-12.2109487310903,
-1428.10431058988));
#152352=CARTESIAN_POINT('Ctrl Pts',(12.1588589765331,-13.3376329379985,
-1429.59842823694));
#152353=CARTESIAN_POINT('Ctrl Pts',(10.9229452762603,-14.4643171449067,
-1431.092545884));
#152354=CARTESIAN_POINT('Ctrl Pts',(9.50104767561053,-15.3447188656481,
-1432.58666353105));
#152355=CARTESIAN_POINT('Ctrl Pts',(8.07915007496071,-16.2251205863895,
-1434.08078117811));
#152356=CARTESIAN_POINT('Ctrl Pts',(6.51968959134574,-16.8292587962898,
-1435.57489882517));
#152357=CARTESIAN_POINT('Ctrl Pts',(4.96022910773078,-17.4333970061901,
-1437.06901647223));
#152358=CARTESIAN_POINT('Ctrl Pts',(3.31631129755346,-17.7406985030951,
-1438.56313411929));
#152359=CARTESIAN_POINT('Ctrl Pts',(1.67239348737615,-18.048,-1440.05725176635));
#152360=CARTESIAN_POINT('Ctrl Pts',(0.,-18.048,-1441.55136941341));
#152361=CARTESIAN_POINT('Ctrl Pts',(-1.67239348737615,-18.048,-1443.04548706047));
#152362=CARTESIAN_POINT('Ctrl Pts',(-3.31631129755346,-17.7406985030951,
-1444.53960470753));
#152363=CARTESIAN_POINT('Ctrl Pts',(-4.96022910773077,-17.4333970061901,
-1446.03372235458));
#152364=CARTESIAN_POINT('Ctrl Pts',(-6.51968959134574,-16.8292587962898,
-1447.52784000164));
#152365=CARTESIAN_POINT('Ctrl Pts',(-8.07915007496071,-16.2251205863895,
-1449.0219576487));
#152366=CARTESIAN_POINT('Ctrl Pts',(-9.50104767561052,-15.3447188656481,
-1450.51607529576));
#152367=CARTESIAN_POINT('Ctrl Pts',(-10.9229452762603,-14.4643171449067,
-1452.01019294282));
#152368=CARTESIAN_POINT('Ctrl Pts',(-12.1588589765331,-13.3376329379985,
-1453.50431058988));
#152369=CARTESIAN_POINT('Ctrl Pts',(-13.3947726768058,-12.2109487310903,
-1454.99842823694));
#152370=CARTESIAN_POINT('Ctrl Pts',(-14.4026149179538,-10.8763499173728,
-1456.492545884));
#152371=CARTESIAN_POINT('Ctrl Pts',(-15.4104571591017,-9.54175110365538,
-1457.98666353106));
#152372=CARTESIAN_POINT('Ctrl Pts',(-16.1559070823762,-8.04468584505497,
-1459.48078117811));
#152373=CARTESIAN_POINT('Ctrl Pts',(-16.9013570056506,-6.54762058645456,
-1460.97489882517));
#152374=CARTESIAN_POINT('Ctrl Pts',(-17.3590292079831,-4.93906964482095,
-1462.46901647223));
#152375=CARTESIAN_POINT('Ctrl Pts',(-17.8167014103155,-3.33051870318735,
-1463.96313411929));
#152376=CARTESIAN_POINT('Ctrl Pts',(-17.9710104137728,-1.66525935159368,
-1465.45725176635));
#152377=CARTESIAN_POINT('Ctrl Pts',(-18.1253194172301,-1.10985572039171E-15,
-1466.95136941341));
#152378=CARTESIAN_POINT('Ctrl Pts',(-17.9710104137728,1.66525935159367,
-1468.44548706047));
#152379=CARTESIAN_POINT('Ctrl Pts',(-17.8167014103155,3.33051870318735,
-1469.93960470753));
#152380=CARTESIAN_POINT('Ctrl Pts',(-17.3590292079831,4.93906964482096,
-1471.43372235458));
#152381=CARTESIAN_POINT('Ctrl Pts',(-16.9013570056506,6.54762058645456,
-1472.92784000164));
#152382=CARTESIAN_POINT('Ctrl Pts',(-16.1559070823762,8.04468584505497,
-1474.4219576487));
#152383=CARTESIAN_POINT('Ctrl Pts',(-15.4104571591017,9.54175110365538,
-1475.91607529576));
#152384=CARTESIAN_POINT('Ctrl Pts',(-14.4026149179538,10.8763499173728,
-1477.41019294282));
#152385=CARTESIAN_POINT('Ctrl Pts',(-13.3947726768058,12.2109487310903,
-1478.90431058988));
#152386=CARTESIAN_POINT('Ctrl Pts',(-12.1588589765331,13.3376329379985,
-1480.39842823694));
#152387=CARTESIAN_POINT('Ctrl Pts',(-10.9229452762603,14.4643171449067,
-1481.892545884));
#152388=CARTESIAN_POINT('Ctrl Pts',(-9.50104767561052,15.3447188656481,
-1483.38666353105));
#152389=CARTESIAN_POINT('Ctrl Pts',(-8.07915007496071,16.2251205863895,
-1484.88078117811));
#152390=CARTESIAN_POINT('Ctrl Pts',(-6.51968959134574,16.8292587962898,
-1486.37489882517));
#152391=CARTESIAN_POINT('Ctrl Pts',(-4.96022910773078,17.4333970061901,
-1487.86901647223));
#152392=CARTESIAN_POINT('Ctrl Pts',(-3.31631129755346,17.7406985030951,
-1489.36313411929));
#152393=CARTESIAN_POINT('Ctrl Pts',(-1.67239348737615,18.048,-1490.85725176635));
#152394=CARTESIAN_POINT('Ctrl Pts',(-2.21024254310115E-15,18.048,-1492.35136941341));
#152395=CARTESIAN_POINT('Ctrl Pts',(1.67239348737616,18.048,-1493.84548706047));
#152396=CARTESIAN_POINT('Ctrl Pts',(3.31631129755346,17.7406985030951,-1495.33960470753));
#152397=CARTESIAN_POINT('Ctrl Pts',(4.96022910773077,17.4333970061901,-1496.83372235458));
#152398=CARTESIAN_POINT('Ctrl Pts',(6.51968959134575,16.8292587962898,-1498.32784000164));
#152399=CARTESIAN_POINT('Ctrl Pts',(7.54128438222279,16.4334908658494,-1499.30662902594));
#152400=CARTESIAN_POINT('Ctrl Pts',(8.50750525179214,15.9170555816938,-1500.28920199011));
#152401=CARTESIAN_POINT('Ctrl Pts',(0.,-50.8,1503.759375));
#152402=CARTESIAN_POINT('Ctrl Pts',(-4.70731322909511,-50.8,1502.26525735294));
#152403=CARTESIAN_POINT('Ctrl Pts',(-9.33447550508177,-49.9350334639422,
1500.77113970588));
#152404=CARTESIAN_POINT('Ctrl Pts',(-13.9616377810684,-49.0700669278844,
1499.27702205882));
#152405=CARTESIAN_POINT('Ctrl Pts',(-18.3510766423074,-47.3695892537413,
1497.78290441177));
#152406=CARTESIAN_POINT('Ctrl Pts',(-22.7405155035463,-45.6691115795981,
1496.28878676471));
#152407=CARTESIAN_POINT('Ctrl Pts',(-26.7427538741697,-43.1910304950644,
1494.79466911765));
#152408=CARTESIAN_POINT('Ctrl Pts',(-30.744992244793,-40.7129494105307,
1493.30055147059));
#152409=CARTESIAN_POINT('Ctrl Pts',(-34.2237386972451,-37.5416529948095,
1491.80643382353));
#152410=CARTESIAN_POINT('Ctrl Pts',(-37.7024851496972,-34.3703565790883,
1490.31231617647));
#152411=CARTESIAN_POINT('Ctrl Pts',(-40.5392751458362,-30.6138395280662,
1488.81819852941));
#152412=CARTESIAN_POINT('Ctrl Pts',(-43.3760651419751,-26.8573224770441,
1487.32408088235));
#152413=CARTESIAN_POINT('Ctrl Pts',(-45.4742952008371,-22.6435084734481,
1485.82996323529));
#152414=CARTESIAN_POINT('Ctrl Pts',(-47.5725252596992,-18.4296944698521,
1484.33584558824));
#152415=CARTESIAN_POINT('Ctrl Pts',(-48.8607426731792,-13.9020798956618,
1482.84172794118));
#152416=CARTESIAN_POINT('Ctrl Pts',(-50.1489600866593,-9.37446532147148,
1481.34761029412));
#152417=CARTESIAN_POINT('Ctrl Pts',(-50.5832961557877,-4.68723266073574,
1479.85349264706));
#152418=CARTESIAN_POINT('Ctrl Pts',(-51.0176322249162,-3.12392900021603E-15,
1478.359375));
#152419=CARTESIAN_POINT('Ctrl Pts',(-50.5832961557877,4.68723266073573,
1476.86525735294));
#152420=CARTESIAN_POINT('Ctrl Pts',(-50.1489600866593,9.37446532147149,
1475.37113970588));
#152421=CARTESIAN_POINT('Ctrl Pts',(-48.8607426731792,13.9020798956618,
1473.87702205882));
#152422=CARTESIAN_POINT('Ctrl Pts',(-47.5725252596992,18.4296944698521,
1472.38290441176));
#152423=CARTESIAN_POINT('Ctrl Pts',(-45.4742952008371,22.6435084734481,
1470.88878676471));
#152424=CARTESIAN_POINT('Ctrl Pts',(-43.3760651419751,26.8573224770442,
1469.39466911765));
#152425=CARTESIAN_POINT('Ctrl Pts',(-40.5392751458362,30.6138395280662,
1467.90055147059));
#152426=CARTESIAN_POINT('Ctrl Pts',(-37.7024851496972,34.3703565790883,
1466.40643382353));
#152427=CARTESIAN_POINT('Ctrl Pts',(-34.2237386972451,37.5416529948095,
1464.91231617647));
#152428=CARTESIAN_POINT('Ctrl Pts',(-30.744992244793,40.7129494105307,1463.41819852941));
#152429=CARTESIAN_POINT('Ctrl Pts',(-26.7427538741697,43.1910304950644,
1461.92408088235));
#152430=CARTESIAN_POINT('Ctrl Pts',(-22.7405155035463,45.6691115795981,
1460.42996323529));
#152431=CARTESIAN_POINT('Ctrl Pts',(-18.3510766423074,47.3695892537413,
1458.93584558824));
#152432=CARTESIAN_POINT('Ctrl Pts',(-13.9616377810684,49.0700669278844,
1457.44172794118));
#152433=CARTESIAN_POINT('Ctrl Pts',(-9.33447550508177,49.9350334639422,
1455.94761029412));
#152434=CARTESIAN_POINT('Ctrl Pts',(-4.7073132290951,50.8,1454.45349264706));
#152435=CARTESIAN_POINT('Ctrl Pts',(-6.22120573966855E-15,50.8,1452.959375));
#152436=CARTESIAN_POINT('Ctrl Pts',(4.70731322909511,50.8,1451.46525735294));
#152437=CARTESIAN_POINT('Ctrl Pts',(9.33447550508176,49.9350334639422,1449.97113970588));
#152438=CARTESIAN_POINT('Ctrl Pts',(13.9616377810684,49.0700669278844,1448.47702205882));
#152439=CARTESIAN_POINT('Ctrl Pts',(18.3510766423074,47.3695892537413,1446.98290441176));
#152440=CARTESIAN_POINT('Ctrl Pts',(22.7405155035463,45.6691115795981,1445.48878676471));
#152441=CARTESIAN_POINT('Ctrl Pts',(26.7427538741697,43.1910304950644,1443.99466911765));
#152442=CARTESIAN_POINT('Ctrl Pts',(30.744992244793,40.7129494105307,1442.50055147059));
#152443=CARTESIAN_POINT('Ctrl Pts',(34.2237386972451,37.5416529948095,1441.00643382353));
#152444=CARTESIAN_POINT('Ctrl Pts',(37.7024851496972,34.3703565790883,1439.51231617647));
#152445=CARTESIAN_POINT('Ctrl Pts',(40.5392751458362,30.6138395280662,1438.01819852941));
#152446=CARTESIAN_POINT('Ctrl Pts',(43.3760651419751,26.8573224770442,1436.52408088235));
#152447=CARTESIAN_POINT('Ctrl Pts',(45.4742952008372,22.6435084734481,1435.02996323529));
#152448=CARTESIAN_POINT('Ctrl Pts',(47.5725252596992,18.4296944698521,1433.53584558824));
#152449=CARTESIAN_POINT('Ctrl Pts',(48.8607426731792,13.9020798956618,1432.04172794118));
#152450=CARTESIAN_POINT('Ctrl Pts',(50.1489600866593,9.37446532147146,1430.54761029412));
#152451=CARTESIAN_POINT('Ctrl Pts',(50.5832961557877,4.68723266073574,1429.05349264706));
#152452=CARTESIAN_POINT('Ctrl Pts',(51.0176322249162,9.37178700064808E-15,
1427.559375));
#152453=CARTESIAN_POINT('Ctrl Pts',(50.5832961557877,-4.68723266073572,
1426.06525735294));
#152454=CARTESIAN_POINT('Ctrl Pts',(50.1489600866593,-9.37446532147149,
1424.57113970588));
#152455=CARTESIAN_POINT('Ctrl Pts',(48.8607426731792,-13.9020798956618,
1423.07702205882));
#152456=CARTESIAN_POINT('Ctrl Pts',(47.5725252596992,-18.4296944698521,
1421.58290441176));
#152457=CARTESIAN_POINT('Ctrl Pts',(45.4742952008371,-22.6435084734482,
1420.08878676471));
#152458=CARTESIAN_POINT('Ctrl Pts',(43.3760651419751,-26.8573224770441,
1418.59466911765));
#152459=CARTESIAN_POINT('Ctrl Pts',(40.5392751458362,-30.6138395280662,
1417.10055147059));
#152460=CARTESIAN_POINT('Ctrl Pts',(37.7024851496972,-34.3703565790883,
1415.60643382353));
#152461=CARTESIAN_POINT('Ctrl Pts',(34.2237386972451,-37.5416529948095,
1414.11231617647));
#152462=CARTESIAN_POINT('Ctrl Pts',(30.744992244793,-40.7129494105307,1412.61819852941));
#152463=CARTESIAN_POINT('Ctrl Pts',(26.7427538741697,-43.1910304950644,
1411.12408088235));
#152464=CARTESIAN_POINT('Ctrl Pts',(22.7405155035463,-45.6691115795981,
1409.62996323529));
#152465=CARTESIAN_POINT('Ctrl Pts',(18.3510766423074,-47.3695892537413,
1408.13584558824));
#152466=CARTESIAN_POINT('Ctrl Pts',(13.9616377810684,-49.0700669278844,
1406.64172794118));
#152467=CARTESIAN_POINT('Ctrl Pts',(9.33447550508176,-49.9350334639422,
1405.14761029412));
#152468=CARTESIAN_POINT('Ctrl Pts',(4.70731322909511,-50.8,1403.65349264706));
#152469=CARTESIAN_POINT('Ctrl Pts',(0.,-50.8,1402.159375));
#152470=CARTESIAN_POINT('Ctrl Pts',(-4.70731322909511,-50.8,1400.66525735294));
#152471=CARTESIAN_POINT('Ctrl Pts',(-9.33447550508177,-49.9350334639422,
1399.17113970588));
#152472=CARTESIAN_POINT('Ctrl Pts',(-13.9616377810684,-49.0700669278844,
1397.67702205882));
#152473=CARTESIAN_POINT('Ctrl Pts',(-18.3510766423074,-47.3695892537413,
1396.18290441176));
#152474=CARTESIAN_POINT('Ctrl Pts',(-22.7405155035463,-45.6691115795981,
1394.68878676471));
#152475=CARTESIAN_POINT('Ctrl Pts',(-26.7427538741697,-43.1910304950644,
1393.19466911765));
#152476=CARTESIAN_POINT('Ctrl Pts',(-30.744992244793,-40.7129494105307,
1391.70055147059));
#152477=CARTESIAN_POINT('Ctrl Pts',(-34.2237386972451,-37.5416529948095,
1390.20643382353));
#152478=CARTESIAN_POINT('Ctrl Pts',(-37.7024851496972,-34.3703565790883,
1388.71231617647));
#152479=CARTESIAN_POINT('Ctrl Pts',(-40.5392751458362,-30.6138395280662,
1387.21819852941));
#152480=CARTESIAN_POINT('Ctrl Pts',(-43.3760651419751,-26.8573224770441,
1385.72408088235));
#152481=CARTESIAN_POINT('Ctrl Pts',(-45.4742952008371,-22.6435084734481,
1384.22996323529));
#152482=CARTESIAN_POINT('Ctrl Pts',(-47.5725252596992,-18.4296944698521,
1382.73584558824));
#152483=CARTESIAN_POINT('Ctrl Pts',(-48.8607426731792,-13.9020798956618,
1381.24172794118));
#152484=CARTESIAN_POINT('Ctrl Pts',(-50.1489600866593,-9.37446532147148,
1379.74761029412));
#152485=CARTESIAN_POINT('Ctrl Pts',(-50.5832961557877,-4.68723266073574,
1378.25349264706));
#152486=CARTESIAN_POINT('Ctrl Pts',(-51.0176322249162,-3.12392900021603E-15,
1376.759375));
#152487=CARTESIAN_POINT('Ctrl Pts',(-50.5832961557877,4.68723266073573,
1375.26525735294));
#152488=CARTESIAN_POINT('Ctrl Pts',(-50.1489600866593,9.37446532147149,
1373.77113970588));
#152489=CARTESIAN_POINT('Ctrl Pts',(-48.8607426731792,13.9020798956618,
1372.27702205882));
#152490=CARTESIAN_POINT('Ctrl Pts',(-47.5725252596992,18.4296944698521,
1370.78290441177));
#152491=CARTESIAN_POINT('Ctrl Pts',(-45.4742952008371,22.6435084734481,
1369.28878676471));
#152492=CARTESIAN_POINT('Ctrl Pts',(-43.3760651419751,26.8573224770442,
1367.79466911765));
#152493=CARTESIAN_POINT('Ctrl Pts',(-40.5392751458362,30.6138395280662,
1366.30055147059));
#152494=CARTESIAN_POINT('Ctrl Pts',(-37.7024851496972,34.3703565790883,
1364.80643382353));
#152495=CARTESIAN_POINT('Ctrl Pts',(-34.2237386972451,37.5416529948095,
1363.31231617647));
#152496=CARTESIAN_POINT('Ctrl Pts',(-30.744992244793,40.7129494105307,1361.81819852941));
#152497=CARTESIAN_POINT('Ctrl Pts',(-26.7427538741697,43.1910304950644,
1360.32408088235));
#152498=CARTESIAN_POINT('Ctrl Pts',(-22.7405155035463,45.6691115795981,
1358.82996323529));
#152499=CARTESIAN_POINT('Ctrl Pts',(-18.3510766423074,47.3695892537413,
1357.33584558824));
#152500=CARTESIAN_POINT('Ctrl Pts',(-13.9616377810684,49.0700669278844,
1355.84172794118));
#152501=CARTESIAN_POINT('Ctrl Pts',(-9.33447550508177,49.9350334639422,
1354.34761029412));
#152502=CARTESIAN_POINT('Ctrl Pts',(-4.7073132290951,50.8,1352.85349264706));
#152503=CARTESIAN_POINT('Ctrl Pts',(-6.22120573966855E-15,50.8,1351.359375));
#152504=CARTESIAN_POINT('Ctrl Pts',(4.70731322909511,50.8,1349.86525735294));
#152505=CARTESIAN_POINT('Ctrl Pts',(9.33447550508176,49.9350334639422,1348.37113970588));
#152506=CARTESIAN_POINT('Ctrl Pts',(13.9616377810684,49.0700669278844,1346.87702205882));
#152507=CARTESIAN_POINT('Ctrl Pts',(18.3510766423074,47.3695892537413,1345.38290441176));
#152508=CARTESIAN_POINT('Ctrl Pts',(22.7405155035463,45.6691115795981,1343.88878676471));
#152509=CARTESIAN_POINT('Ctrl Pts',(26.7427538741697,43.1910304950644,1342.39466911765));
#152510=CARTESIAN_POINT('Ctrl Pts',(30.744992244793,40.7129494105307,1340.90055147059));
#152511=CARTESIAN_POINT('Ctrl Pts',(34.2237386972451,37.5416529948095,1339.40643382353));
#152512=CARTESIAN_POINT('Ctrl Pts',(37.7024851496972,34.3703565790883,1337.91231617647));
#152513=CARTESIAN_POINT('Ctrl Pts',(40.5392751458362,30.6138395280662,1336.41819852941));
#152514=CARTESIAN_POINT('Ctrl Pts',(43.3760651419751,26.8573224770442,1334.92408088235));
#152515=CARTESIAN_POINT('Ctrl Pts',(45.4742952008372,22.6435084734481,1333.42996323529));
#152516=CARTESIAN_POINT('Ctrl Pts',(47.5725252596992,18.4296944698521,1331.93584558824));
#152517=CARTESIAN_POINT('Ctrl Pts',(48.8607426731792,13.9020798956618,1330.44172794118));
#152518=CARTESIAN_POINT('Ctrl Pts',(50.1489600866593,9.37446532147146,1328.94761029412));
#152519=CARTESIAN_POINT('Ctrl Pts',(50.5832961557877,4.68723266073574,1327.45349264706));
#152520=CARTESIAN_POINT('Ctrl Pts',(51.0176322249162,9.37178700064808E-15,
1325.959375));
#152521=CARTESIAN_POINT('Ctrl Pts',(50.5832961557877,-4.68723266073572,
1324.46525735294));
#152522=CARTESIAN_POINT('Ctrl Pts',(50.1489600866593,-9.37446532147149,
1322.97113970588));
#152523=CARTESIAN_POINT('Ctrl Pts',(48.8607426731792,-13.9020798956618,
1321.47702205882));
#152524=CARTESIAN_POINT('Ctrl Pts',(47.5725252596992,-18.4296944698521,
1319.98290441177));
#152525=CARTESIAN_POINT('Ctrl Pts',(45.4742952008371,-22.6435084734482,
1318.48878676471));
#152526=CARTESIAN_POINT('Ctrl Pts',(43.3760651419751,-26.8573224770441,
1316.99466911765));
#152527=CARTESIAN_POINT('Ctrl Pts',(40.5392751458362,-30.6138395280662,
1315.50055147059));
#152528=CARTESIAN_POINT('Ctrl Pts',(37.7024851496972,-34.3703565790883,
1314.00643382353));
#152529=CARTESIAN_POINT('Ctrl Pts',(34.2237386972451,-37.5416529948095,
1312.51231617647));
#152530=CARTESIAN_POINT('Ctrl Pts',(30.744992244793,-40.7129494105307,1311.01819852941));
#152531=CARTESIAN_POINT('Ctrl Pts',(26.7427538741697,-43.1910304950644,
1309.52408088235));
#152532=CARTESIAN_POINT('Ctrl Pts',(22.7405155035463,-45.6691115795981,
1308.02996323529));
#152533=CARTESIAN_POINT('Ctrl Pts',(18.3510766423074,-47.3695892537413,
1306.53584558824));
#152534=CARTESIAN_POINT('Ctrl Pts',(13.9616377810684,-49.0700669278844,
1305.04172794118));
#152535=CARTESIAN_POINT('Ctrl Pts',(9.33447550508176,-49.9350334639422,
1303.54761029412));
#152536=CARTESIAN_POINT('Ctrl Pts',(4.70731322909511,-50.8,1302.05349264706));
#152537=CARTESIAN_POINT('Ctrl Pts',(0.,-50.8,1300.559375));
#152538=CARTESIAN_POINT('Ctrl Pts',(-4.70731322909511,-50.8,1299.06525735294));
#152539=CARTESIAN_POINT('Ctrl Pts',(-9.33447550508177,-49.9350334639422,
1297.57113970588));
#152540=CARTESIAN_POINT('Ctrl Pts',(-13.9616377810684,-49.0700669278844,
1296.07702205882));
#152541=CARTESIAN_POINT('Ctrl Pts',(-18.3510766423074,-47.3695892537413,
1294.58290441176));
#152542=CARTESIAN_POINT('Ctrl Pts',(-22.7405155035463,-45.6691115795981,
1293.08878676471));
#152543=CARTESIAN_POINT('Ctrl Pts',(-26.7427538741697,-43.1910304950644,
1291.59466911765));
#152544=CARTESIAN_POINT('Ctrl Pts',(-30.744992244793,-40.7129494105307,
1290.10055147059));
#152545=CARTESIAN_POINT('Ctrl Pts',(-34.2237386972451,-37.5416529948095,
1288.60643382353));
#152546=CARTESIAN_POINT('Ctrl Pts',(-37.7024851496972,-34.3703565790883,
1287.11231617647));
#152547=CARTESIAN_POINT('Ctrl Pts',(-40.5392751458362,-30.6138395280662,
1285.61819852941));
#152548=CARTESIAN_POINT('Ctrl Pts',(-43.3760651419751,-26.8573224770441,
1284.12408088235));
#152549=CARTESIAN_POINT('Ctrl Pts',(-45.4742952008371,-22.6435084734481,
1282.62996323529));
#152550=CARTESIAN_POINT('Ctrl Pts',(-47.5725252596992,-18.4296944698521,
1281.13584558824));
#152551=CARTESIAN_POINT('Ctrl Pts',(-48.8607426731792,-13.9020798956618,
1279.64172794118));
#152552=CARTESIAN_POINT('Ctrl Pts',(-50.1489600866593,-9.37446532147148,
1278.14761029412));
#152553=CARTESIAN_POINT('Ctrl Pts',(-50.5832961557877,-4.68723266073574,
1276.65349264706));
#152554=CARTESIAN_POINT('Ctrl Pts',(-51.0176322249162,-3.12392900021603E-15,
1275.159375));
#152555=CARTESIAN_POINT('Ctrl Pts',(-50.5832961557877,4.68723266073573,
1273.66525735294));
#152556=CARTESIAN_POINT('Ctrl Pts',(-50.1489600866593,9.37446532147149,
1272.17113970588));
#152557=CARTESIAN_POINT('Ctrl Pts',(-48.8607426731792,13.9020798956618,
1270.67702205882));
#152558=CARTESIAN_POINT('Ctrl Pts',(-47.5725252596992,18.4296944698521,
1269.18290441176));
#152559=CARTESIAN_POINT('Ctrl Pts',(-45.4742952008371,22.6435084734481,
1267.68878676471));
#152560=CARTESIAN_POINT('Ctrl Pts',(-43.3760651419751,26.8573224770442,
1266.19466911765));
#152561=CARTESIAN_POINT('Ctrl Pts',(-40.5392751458362,30.6138395280662,
1264.70055147059));
#152562=CARTESIAN_POINT('Ctrl Pts',(-37.7024851496972,34.3703565790883,
1263.20643382353));
#152563=CARTESIAN_POINT('Ctrl Pts',(-34.2237386972451,37.5416529948095,
1261.71231617647));
#152564=CARTESIAN_POINT('Ctrl Pts',(-30.744992244793,40.7129494105307,1260.21819852941));
#152565=CARTESIAN_POINT('Ctrl Pts',(-26.7427538741697,43.1910304950644,
1258.72408088235));
#152566=CARTESIAN_POINT('Ctrl Pts',(-22.7405155035463,45.6691115795981,
1257.22996323529));
#152567=CARTESIAN_POINT('Ctrl Pts',(-18.3510766423074,47.3695892537413,
1255.73584558824));
#152568=CARTESIAN_POINT('Ctrl Pts',(-13.9616377810684,49.0700669278844,
1254.24172794118));
#152569=CARTESIAN_POINT('Ctrl Pts',(-9.33447550508177,49.9350334639422,
1252.74761029412));
#152570=CARTESIAN_POINT('Ctrl Pts',(-4.7073132290951,50.8,1251.25349264706));
#152571=CARTESIAN_POINT('Ctrl Pts',(-6.22120573966855E-15,50.8,1249.759375));
#152572=CARTESIAN_POINT('Ctrl Pts',(4.70731322909511,50.8,1248.26525735294));
#152573=CARTESIAN_POINT('Ctrl Pts',(9.33447550508176,49.9350334639422,1246.77113970588));
#152574=CARTESIAN_POINT('Ctrl Pts',(13.9616377810684,49.0700669278844,1245.27702205882));
#152575=CARTESIAN_POINT('Ctrl Pts',(18.3510766423074,47.3695892537413,1243.78290441176));
#152576=CARTESIAN_POINT('Ctrl Pts',(22.7405155035463,45.6691115795981,1242.28878676471));
#152577=CARTESIAN_POINT('Ctrl Pts',(26.7427538741697,43.1910304950644,1240.79466911765));
#152578=CARTESIAN_POINT('Ctrl Pts',(30.744992244793,40.7129494105307,1239.30055147059));
#152579=CARTESIAN_POINT('Ctrl Pts',(34.2237386972451,37.5416529948095,1237.80643382353));
#152580=CARTESIAN_POINT('Ctrl Pts',(37.7024851496972,34.3703565790883,1236.31231617647));
#152581=CARTESIAN_POINT('Ctrl Pts',(40.5392751458362,30.6138395280662,1234.81819852941));
#152582=CARTESIAN_POINT('Ctrl Pts',(43.3760651419751,26.8573224770442,1233.32408088235));
#152583=CARTESIAN_POINT('Ctrl Pts',(45.4742952008372,22.6435084734481,1231.82996323529));
#152584=CARTESIAN_POINT('Ctrl Pts',(47.5725252596992,18.4296944698521,1230.33584558824));
#152585=CARTESIAN_POINT('Ctrl Pts',(48.8607426731792,13.9020798956618,1228.84172794118));
#152586=CARTESIAN_POINT('Ctrl Pts',(50.1489600866593,9.37446532147146,1227.34761029412));
#152587=CARTESIAN_POINT('Ctrl Pts',(50.5832961557877,4.68723266073574,1225.85349264706));
#152588=CARTESIAN_POINT('Ctrl Pts',(51.0176322249162,9.37178700064808E-15,
1224.359375));
#152589=CARTESIAN_POINT('Ctrl Pts',(50.5832961557877,-4.68723266073572,
1222.86525735294));
#152590=CARTESIAN_POINT('Ctrl Pts',(50.1489600866593,-9.37446532147149,
1221.37113970588));
#152591=CARTESIAN_POINT('Ctrl Pts',(48.8607426731792,-13.9020798956618,
1219.87702205882));
#152592=CARTESIAN_POINT('Ctrl Pts',(47.5725252596992,-18.4296944698521,
1218.38290441176));
#152593=CARTESIAN_POINT('Ctrl Pts',(45.4742952008371,-22.6435084734482,
1216.88878676471));
#152594=CARTESIAN_POINT('Ctrl Pts',(43.3760651419751,-26.8573224770441,
1215.39466911765));
#152595=CARTESIAN_POINT('Ctrl Pts',(40.5392751458362,-30.6138395280662,
1213.90055147059));
#152596=CARTESIAN_POINT('Ctrl Pts',(37.7024851496972,-34.3703565790883,
1212.40643382353));
#152597=CARTESIAN_POINT('Ctrl Pts',(34.2237386972451,-37.5416529948095,
1210.91231617647));
#152598=CARTESIAN_POINT('Ctrl Pts',(30.744992244793,-40.7129494105307,1209.41819852941));
#152599=CARTESIAN_POINT('Ctrl Pts',(26.7427538741697,-43.1910304950644,
1207.92408088235));
#152600=CARTESIAN_POINT('Ctrl Pts',(22.7405155035463,-45.6691115795981,
1206.42996323529));
#152601=CARTESIAN_POINT('Ctrl Pts',(18.3510766423074,-47.3695892537413,
1204.93584558824));
#152602=CARTESIAN_POINT('Ctrl Pts',(13.9616377810684,-49.0700669278844,
1203.44172794118));
#152603=CARTESIAN_POINT('Ctrl Pts',(9.33447550508176,-49.9350334639422,
1201.94761029412));
#152604=CARTESIAN_POINT('Ctrl Pts',(4.70731322909511,-50.8,1200.45349264706));
#152605=CARTESIAN_POINT('Ctrl Pts',(0.,-50.8,1198.959375));
#152606=CARTESIAN_POINT('Ctrl Pts',(-4.70731322909511,-50.8,1197.46525735294));
#152607=CARTESIAN_POINT('Ctrl Pts',(-9.33447550508177,-49.9350334639422,
1195.97113970588));
#152608=CARTESIAN_POINT('Ctrl Pts',(-13.9616377810684,-49.0700669278844,
1194.47702205882));
#152609=CARTESIAN_POINT('Ctrl Pts',(-18.3510766423074,-47.3695892537413,
1192.98290441176));
#152610=CARTESIAN_POINT('Ctrl Pts',(-22.7405155035463,-45.6691115795981,
1191.48878676471));
#152611=CARTESIAN_POINT('Ctrl Pts',(-26.7427538741697,-43.1910304950644,
1189.99466911765));
#152612=CARTESIAN_POINT('Ctrl Pts',(-30.744992244793,-40.7129494105307,
1188.50055147059));
#152613=CARTESIAN_POINT('Ctrl Pts',(-34.2237386972451,-37.5416529948095,
1187.00643382353));
#152614=CARTESIAN_POINT('Ctrl Pts',(-37.7024851496972,-34.3703565790883,
1185.51231617647));
#152615=CARTESIAN_POINT('Ctrl Pts',(-40.5392751458362,-30.6138395280662,
1184.01819852941));
#152616=CARTESIAN_POINT('Ctrl Pts',(-43.3760651419751,-26.8573224770441,
1182.52408088235));
#152617=CARTESIAN_POINT('Ctrl Pts',(-45.4742952008371,-22.6435084734481,
1181.02996323529));
#152618=CARTESIAN_POINT('Ctrl Pts',(-47.5725252596992,-18.4296944698521,
1179.53584558824));
#152619=CARTESIAN_POINT('Ctrl Pts',(-48.8607426731792,-13.9020798956618,
1178.04172794118));
#152620=CARTESIAN_POINT('Ctrl Pts',(-50.1489600866593,-9.37446532147148,
1176.54761029412));
#152621=CARTESIAN_POINT('Ctrl Pts',(-50.5832961557877,-4.68723266073574,
1175.05349264706));
#152622=CARTESIAN_POINT('Ctrl Pts',(-51.0176322249162,-3.12392900021603E-15,
1173.559375));
#152623=CARTESIAN_POINT('Ctrl Pts',(-50.5832961557877,4.68723266073573,
1172.06525735294));
#152624=CARTESIAN_POINT('Ctrl Pts',(-50.1489600866593,9.37446532147149,
1170.57113970588));
#152625=CARTESIAN_POINT('Ctrl Pts',(-48.8607426731792,13.9020798956618,
1169.07702205882));
#152626=CARTESIAN_POINT('Ctrl Pts',(-47.5725252596992,18.4296944698521,
1167.58290441176));
#152627=CARTESIAN_POINT('Ctrl Pts',(-45.4742952008371,22.6435084734481,
1166.08878676471));
#152628=CARTESIAN_POINT('Ctrl Pts',(-43.3760651419751,26.8573224770442,
1164.59466911765));
#152629=CARTESIAN_POINT('Ctrl Pts',(-40.5392751458362,30.6138395280662,
1163.10055147059));
#152630=CARTESIAN_POINT('Ctrl Pts',(-37.7024851496972,34.3703565790883,
1161.60643382353));
#152631=CARTESIAN_POINT('Ctrl Pts',(-34.2237386972451,37.5416529948095,
1160.11231617647));
#152632=CARTESIAN_POINT('Ctrl Pts',(-30.744992244793,40.7129494105307,1158.61819852941));
#152633=CARTESIAN_POINT('Ctrl Pts',(-26.7427538741697,43.1910304950644,
1157.12408088235));
#152634=CARTESIAN_POINT('Ctrl Pts',(-22.7405155035463,45.6691115795981,
1155.62996323529));
#152635=CARTESIAN_POINT('Ctrl Pts',(-18.3510766423074,47.3695892537413,
1154.13584558824));
#152636=CARTESIAN_POINT('Ctrl Pts',(-13.9616377810684,49.0700669278844,
1152.64172794118));
#152637=CARTESIAN_POINT('Ctrl Pts',(-9.33447550508177,49.9350334639422,
1151.14761029412));
#152638=CARTESIAN_POINT('Ctrl Pts',(-4.7073132290951,50.8,1149.65349264706));
#152639=CARTESIAN_POINT('Ctrl Pts',(-6.22120573966855E-15,50.8,1148.159375));
#152640=CARTESIAN_POINT('Ctrl Pts',(4.70731322909511,50.8,1146.66525735294));
#152641=CARTESIAN_POINT('Ctrl Pts',(9.33447550508176,49.9350334639422,1145.17113970588));
#152642=CARTESIAN_POINT('Ctrl Pts',(13.9616377810684,49.0700669278844,1143.67702205882));
#152643=CARTESIAN_POINT('Ctrl Pts',(18.3510766423074,47.3695892537413,1142.18290441176));
#152644=CARTESIAN_POINT('Ctrl Pts',(22.7405155035463,45.6691115795981,1140.68878676471));
#152645=CARTESIAN_POINT('Ctrl Pts',(26.7427538741697,43.1910304950644,1139.19466911765));
#152646=CARTESIAN_POINT('Ctrl Pts',(30.744992244793,40.7129494105307,1137.70055147059));
#152647=CARTESIAN_POINT('Ctrl Pts',(34.2237386972451,37.5416529948095,1136.20643382353));
#152648=CARTESIAN_POINT('Ctrl Pts',(37.7024851496972,34.3703565790883,1134.71231617647));
#152649=CARTESIAN_POINT('Ctrl Pts',(40.5392751458362,30.6138395280662,1133.21819852941));
#152650=CARTESIAN_POINT('Ctrl Pts',(43.3760651419751,26.8573224770442,1131.72408088235));
#152651=CARTESIAN_POINT('Ctrl Pts',(45.4742952008372,22.6435084734481,1130.22996323529));
#152652=CARTESIAN_POINT('Ctrl Pts',(47.5725252596992,18.4296944698521,1128.73584558824));
#152653=CARTESIAN_POINT('Ctrl Pts',(48.8607426731792,13.9020798956618,1127.24172794118));
#152654=CARTESIAN_POINT('Ctrl Pts',(50.1489600866593,9.37446532147146,1125.74761029412));
#152655=CARTESIAN_POINT('Ctrl Pts',(50.5832961557877,4.68723266073574,1124.25349264706));
#152656=CARTESIAN_POINT('Ctrl Pts',(51.0176322249162,9.37178700064808E-15,
1122.759375));
#152657=CARTESIAN_POINT('Ctrl Pts',(50.5832961557877,-4.68723266073572,
1121.26525735294));
#152658=CARTESIAN_POINT('Ctrl Pts',(50.1489600866593,-9.37446532147149,
1119.77113970588));
#152659=CARTESIAN_POINT('Ctrl Pts',(48.8607426731792,-13.9020798956618,
1118.27702205882));
#152660=CARTESIAN_POINT('Ctrl Pts',(47.5725252596992,-18.4296944698521,
1116.78290441177));
#152661=CARTESIAN_POINT('Ctrl Pts',(45.4742952008371,-22.6435084734482,
1115.28878676471));
#152662=CARTESIAN_POINT('Ctrl Pts',(43.3760651419751,-26.8573224770441,
1113.79466911765));
#152663=CARTESIAN_POINT('Ctrl Pts',(40.5392751458362,-30.6138395280662,
1112.30055147059));
#152664=CARTESIAN_POINT('Ctrl Pts',(37.7024851496972,-34.3703565790883,
1110.80643382353));
#152665=CARTESIAN_POINT('Ctrl Pts',(34.2237386972451,-37.5416529948095,
1109.31231617647));
#152666=CARTESIAN_POINT('Ctrl Pts',(30.744992244793,-40.7129494105307,1107.81819852941));
#152667=CARTESIAN_POINT('Ctrl Pts',(26.7427538741697,-43.1910304950644,
1106.32408088235));
#152668=CARTESIAN_POINT('Ctrl Pts',(22.7405155035463,-45.6691115795981,
1104.82996323529));
#152669=CARTESIAN_POINT('Ctrl Pts',(18.3510766423074,-47.3695892537413,
1103.33584558824));
#152670=CARTESIAN_POINT('Ctrl Pts',(13.9616377810684,-49.0700669278844,
1101.84172794118));
#152671=CARTESIAN_POINT('Ctrl Pts',(9.33447550508176,-49.9350334639422,
1100.34761029412));
#152672=CARTESIAN_POINT('Ctrl Pts',(4.70731322909511,-50.8,1098.85349264706));
#152673=CARTESIAN_POINT('Ctrl Pts',(0.,-50.8,1097.359375));
#152674=CARTESIAN_POINT('Ctrl Pts',(-4.70731322909511,-50.8,1095.86525735294));
#152675=CARTESIAN_POINT('Ctrl Pts',(-9.33447550508177,-49.9350334639422,
1094.37113970588));
#152676=CARTESIAN_POINT('Ctrl Pts',(-13.9616377810684,-49.0700669278844,
1092.87702205882));
#152677=CARTESIAN_POINT('Ctrl Pts',(-18.3510766423074,-47.3695892537413,
1091.38290441176));
#152678=CARTESIAN_POINT('Ctrl Pts',(-22.7405155035463,-45.6691115795981,
1089.88878676471));
#152679=CARTESIAN_POINT('Ctrl Pts',(-26.7427538741697,-43.1910304950644,
1088.39466911765));
#152680=CARTESIAN_POINT('Ctrl Pts',(-30.744992244793,-40.7129494105307,
1086.90055147059));
#152681=CARTESIAN_POINT('Ctrl Pts',(-34.2237386972451,-37.5416529948095,
1085.40643382353));
#152682=CARTESIAN_POINT('Ctrl Pts',(-37.7024851496972,-34.3703565790883,
1083.91231617647));
#152683=CARTESIAN_POINT('Ctrl Pts',(-40.5392751458362,-30.6138395280662,
1082.41819852941));
#152684=CARTESIAN_POINT('Ctrl Pts',(-43.3760651419751,-26.8573224770441,
1080.92408088235));
#152685=CARTESIAN_POINT('Ctrl Pts',(-45.4742952008371,-22.6435084734481,
1079.42996323529));
#152686=CARTESIAN_POINT('Ctrl Pts',(-47.5725252596992,-18.4296944698521,
1077.93584558824));
#152687=CARTESIAN_POINT('Ctrl Pts',(-48.8607426731792,-13.9020798956618,
1076.44172794118));
#152688=CARTESIAN_POINT('Ctrl Pts',(-50.1489600866593,-9.37446532147148,
1074.94761029412));
#152689=CARTESIAN_POINT('Ctrl Pts',(-50.5832961557877,-4.68723266073574,
1073.45349264706));
#152690=CARTESIAN_POINT('Ctrl Pts',(-51.0176322249162,-3.12392900021603E-15,
1071.959375));
#152691=CARTESIAN_POINT('Ctrl Pts',(-50.5832961557877,4.68723266073573,
1070.46525735294));
#152692=CARTESIAN_POINT('Ctrl Pts',(-50.1489600866593,9.37446532147149,
1068.97113970588));
#152693=CARTESIAN_POINT('Ctrl Pts',(-48.8607426731792,13.9020798956618,
1067.47702205882));
#152694=CARTESIAN_POINT('Ctrl Pts',(-47.5725252596992,18.4296944698521,
1065.98290441176));
#152695=CARTESIAN_POINT('Ctrl Pts',(-45.4742952008371,22.6435084734481,
1064.48878676471));
#152696=CARTESIAN_POINT('Ctrl Pts',(-43.3760651419751,26.8573224770442,
1062.99466911765));
#152697=CARTESIAN_POINT('Ctrl Pts',(-40.5392751458362,30.6138395280662,
1061.50055147059));
#152698=CARTESIAN_POINT('Ctrl Pts',(-37.7024851496972,34.3703565790883,
1060.00643382353));
#152699=CARTESIAN_POINT('Ctrl Pts',(-34.2237386972451,37.5416529948095,
1058.51231617647));
#152700=CARTESIAN_POINT('Ctrl Pts',(-30.744992244793,40.7129494105307,1057.01819852941));
#152701=CARTESIAN_POINT('Ctrl Pts',(-26.7427538741697,43.1910304950644,
1055.52408088235));
#152702=CARTESIAN_POINT('Ctrl Pts',(-22.7405155035463,45.6691115795981,
1054.02996323529));
#152703=CARTESIAN_POINT('Ctrl Pts',(-18.3510766423074,47.3695892537413,
1052.53584558824));
#152704=CARTESIAN_POINT('Ctrl Pts',(-13.9616377810684,49.0700669278844,
1051.04172794118));
#152705=CARTESIAN_POINT('Ctrl Pts',(-9.33447550508177,49.9350334639422,
1049.54761029412));
#152706=CARTESIAN_POINT('Ctrl Pts',(-4.7073132290951,50.8,1048.05349264706));
#152707=CARTESIAN_POINT('Ctrl Pts',(-6.22120573966855E-15,50.8,1046.559375));
#152708=CARTESIAN_POINT('Ctrl Pts',(4.70731322909511,50.8,1045.06525735294));
#152709=CARTESIAN_POINT('Ctrl Pts',(9.33447550508176,49.9350334639422,1043.57113970588));
#152710=CARTESIAN_POINT('Ctrl Pts',(13.9616377810684,49.0700669278844,1042.07702205882));
#152711=CARTESIAN_POINT('Ctrl Pts',(18.3510766423074,47.3695892537413,1040.58290441176));
#152712=CARTESIAN_POINT('Ctrl Pts',(22.7405155035463,45.6691115795981,1039.08878676471));
#152713=CARTESIAN_POINT('Ctrl Pts',(26.7427538741697,43.1910304950644,1037.59466911765));
#152714=CARTESIAN_POINT('Ctrl Pts',(30.744992244793,40.7129494105307,1036.10055147059));
#152715=CARTESIAN_POINT('Ctrl Pts',(34.2237386972451,37.5416529948095,1034.60643382353));
#152716=CARTESIAN_POINT('Ctrl Pts',(37.7024851496972,34.3703565790883,1033.11231617647));
#152717=CARTESIAN_POINT('Ctrl Pts',(40.5392751458362,30.6138395280662,1031.61819852941));
#152718=CARTESIAN_POINT('Ctrl Pts',(43.3760651419751,26.8573224770442,1030.12408088235));
#152719=CARTESIAN_POINT('Ctrl Pts',(45.4742952008372,22.6435084734481,1028.62996323529));
#152720=CARTESIAN_POINT('Ctrl Pts',(47.5725252596992,18.4296944698521,1027.13584558824));
#152721=CARTESIAN_POINT('Ctrl Pts',(48.8607426731792,13.9020798956618,1025.64172794118));
#152722=CARTESIAN_POINT('Ctrl Pts',(50.1489600866593,9.37446532147146,1024.14761029412));
#152723=CARTESIAN_POINT('Ctrl Pts',(50.5832961557877,4.68723266073574,1022.65349264706));
#152724=CARTESIAN_POINT('Ctrl Pts',(51.0176322249162,9.37178700064808E-15,
1021.159375));
#152725=CARTESIAN_POINT('Ctrl Pts',(50.5832961557877,-4.68723266073572,
1019.66525735294));
#152726=CARTESIAN_POINT('Ctrl Pts',(50.1489600866593,-9.37446532147149,
1018.17113970588));
#152727=CARTESIAN_POINT('Ctrl Pts',(48.8607426731792,-13.9020798956618,
1016.67702205882));
#152728=CARTESIAN_POINT('Ctrl Pts',(47.5725252596992,-18.4296944698521,
1015.18290441177));
#152729=CARTESIAN_POINT('Ctrl Pts',(45.4742952008371,-22.6435084734482,
1013.68878676471));
#152730=CARTESIAN_POINT('Ctrl Pts',(43.3760651419751,-26.8573224770441,
1012.19466911765));
#152731=CARTESIAN_POINT('Ctrl Pts',(40.5392751458362,-30.6138395280662,
1010.70055147059));
#152732=CARTESIAN_POINT('Ctrl Pts',(37.7024851496972,-34.3703565790883,
1009.20643382353));
#152733=CARTESIAN_POINT('Ctrl Pts',(34.2237386972451,-37.5416529948095,
1007.71231617647));
#152734=CARTESIAN_POINT('Ctrl Pts',(30.744992244793,-40.7129494105307,1006.21819852941));
#152735=CARTESIAN_POINT('Ctrl Pts',(26.7427538741697,-43.1910304950644,
1004.72408088235));
#152736=CARTESIAN_POINT('Ctrl Pts',(22.7405155035463,-45.6691115795981,
1003.22996323529));
#152737=CARTESIAN_POINT('Ctrl Pts',(18.3510766423074,-47.3695892537413,
1001.73584558824));
#152738=CARTESIAN_POINT('Ctrl Pts',(13.9616377810684,-49.0700669278844,
1000.24172794118));
#152739=CARTESIAN_POINT('Ctrl Pts',(9.33447550508176,-49.9350334639422,
998.747610294118));
#152740=CARTESIAN_POINT('Ctrl Pts',(4.70731322909511,-50.8,997.253492647059));
#152741=CARTESIAN_POINT('Ctrl Pts',(0.,-50.8,995.759375));
#152742=CARTESIAN_POINT('Ctrl Pts',(-4.70731322909511,-50.8,994.265257352941));
#152743=CARTESIAN_POINT('Ctrl Pts',(-9.33447550508177,-49.9350334639422,
992.771139705882));
#152744=CARTESIAN_POINT('Ctrl Pts',(-13.9616377810684,-49.0700669278844,
991.277022058824));
#152745=CARTESIAN_POINT('Ctrl Pts',(-18.3510766423074,-47.3695892537413,
989.782904411765));
#152746=CARTESIAN_POINT('Ctrl Pts',(-22.7405155035463,-45.6691115795981,
988.288786764706));
#152747=CARTESIAN_POINT('Ctrl Pts',(-26.7427538741697,-43.1910304950644,
986.794669117647));
#152748=CARTESIAN_POINT('Ctrl Pts',(-30.744992244793,-40.7129494105307,
985.300551470589));
#152749=CARTESIAN_POINT('Ctrl Pts',(-34.2237386972451,-37.5416529948095,
983.806433823529));
#152750=CARTESIAN_POINT('Ctrl Pts',(-37.7024851496972,-34.3703565790883,
982.312316176471));
#152751=CARTESIAN_POINT('Ctrl Pts',(-40.5392751458362,-30.6138395280662,
980.818198529412));
#152752=CARTESIAN_POINT('Ctrl Pts',(-43.3760651419751,-26.8573224770441,
979.324080882353));
#152753=CARTESIAN_POINT('Ctrl Pts',(-45.4742952008371,-22.6435084734481,
977.829963235294));
#152754=CARTESIAN_POINT('Ctrl Pts',(-47.5725252596992,-18.4296944698521,
976.335845588235));
#152755=CARTESIAN_POINT('Ctrl Pts',(-48.8607426731792,-13.9020798956618,
974.841727941176));
#152756=CARTESIAN_POINT('Ctrl Pts',(-50.1489600866593,-9.37446532147148,
973.347610294118));
#152757=CARTESIAN_POINT('Ctrl Pts',(-50.5832961557877,-4.68723266073574,
971.853492647059));
#152758=CARTESIAN_POINT('Ctrl Pts',(-51.0176322249162,-3.12392900021603E-15,
970.359375));
#152759=CARTESIAN_POINT('Ctrl Pts',(-50.5832961557877,4.68723266073573,
968.865257352941));
#152760=CARTESIAN_POINT('Ctrl Pts',(-50.1489600866593,9.37446532147149,
967.371139705883));
#152761=CARTESIAN_POINT('Ctrl Pts',(-48.8607426731792,13.9020798956618,
965.877022058824));
#152762=CARTESIAN_POINT('Ctrl Pts',(-47.5725252596992,18.4296944698521,
964.382904411765));
#152763=CARTESIAN_POINT('Ctrl Pts',(-45.4742952008371,22.6435084734481,
962.888786764706));
#152764=CARTESIAN_POINT('Ctrl Pts',(-43.3760651419751,26.8573224770442,
961.394669117647));
#152765=CARTESIAN_POINT('Ctrl Pts',(-40.5392751458362,30.6138395280662,
959.900551470588));
#152766=CARTESIAN_POINT('Ctrl Pts',(-37.7024851496972,34.3703565790883,
958.40643382353));
#152767=CARTESIAN_POINT('Ctrl Pts',(-34.2237386972451,37.5416529948095,
956.912316176471));
#152768=CARTESIAN_POINT('Ctrl Pts',(-30.744992244793,40.7129494105307,955.418198529412));
#152769=CARTESIAN_POINT('Ctrl Pts',(-26.7427538741697,43.1910304950644,
953.924080882353));
#152770=CARTESIAN_POINT('Ctrl Pts',(-22.7405155035463,45.6691115795981,
952.429963235294));
#152771=CARTESIAN_POINT('Ctrl Pts',(-18.3510766423074,47.3695892537413,
950.935845588235));
#152772=CARTESIAN_POINT('Ctrl Pts',(-13.9616377810684,49.0700669278844,
949.441727941177));
#152773=CARTESIAN_POINT('Ctrl Pts',(-9.33447550508177,49.9350334639422,
947.947610294118));
#152774=CARTESIAN_POINT('Ctrl Pts',(-4.7073132290951,50.8,946.453492647059));
#152775=CARTESIAN_POINT('Ctrl Pts',(-6.22120573966855E-15,50.8,944.959375));
#152776=CARTESIAN_POINT('Ctrl Pts',(4.70731322909511,50.8,943.465257352941));
#152777=CARTESIAN_POINT('Ctrl Pts',(9.33447550508176,49.9350334639422,941.971139705882));
#152778=CARTESIAN_POINT('Ctrl Pts',(13.9616377810684,49.0700669278844,940.477022058824));
#152779=CARTESIAN_POINT('Ctrl Pts',(18.3510766423074,47.3695892537413,938.982904411765));
#152780=CARTESIAN_POINT('Ctrl Pts',(22.7405155035463,45.6691115795981,937.488786764706));
#152781=CARTESIAN_POINT('Ctrl Pts',(26.7427538741697,43.1910304950644,935.994669117647));
#152782=CARTESIAN_POINT('Ctrl Pts',(30.744992244793,40.7129494105307,934.500551470588));
#152783=CARTESIAN_POINT('Ctrl Pts',(34.2237386972451,37.5416529948095,933.00643382353));
#152784=CARTESIAN_POINT('Ctrl Pts',(37.7024851496972,34.3703565790883,931.512316176471));
#152785=CARTESIAN_POINT('Ctrl Pts',(40.5392751458362,30.6138395280662,930.018198529412));
#152786=CARTESIAN_POINT('Ctrl Pts',(43.3760651419751,26.8573224770442,928.524080882353));
#152787=CARTESIAN_POINT('Ctrl Pts',(45.4742952008372,22.6435084734481,927.029963235294));
#152788=CARTESIAN_POINT('Ctrl Pts',(47.5725252596992,18.4296944698521,925.535845588235));
#152789=CARTESIAN_POINT('Ctrl Pts',(48.8607426731792,13.9020798956618,924.041727941176));
#152790=CARTESIAN_POINT('Ctrl Pts',(50.1489600866593,9.37446532147146,922.547610294118));
#152791=CARTESIAN_POINT('Ctrl Pts',(50.5832961557877,4.68723266073574,921.053492647059));
#152792=CARTESIAN_POINT('Ctrl Pts',(51.0176322249162,9.37178700064808E-15,
919.559375));
#152793=CARTESIAN_POINT('Ctrl Pts',(50.5832961557877,-4.68723266073572,
918.065257352941));
#152794=CARTESIAN_POINT('Ctrl Pts',(50.1489600866593,-9.37446532147149,
916.571139705882));
#152795=CARTESIAN_POINT('Ctrl Pts',(48.8607426731792,-13.9020798956618,
915.077022058824));
#152796=CARTESIAN_POINT('Ctrl Pts',(47.5725252596992,-18.4296944698521,
913.582904411765));
#152797=CARTESIAN_POINT('Ctrl Pts',(45.4742952008371,-22.6435084734482,
912.088786764706));
#152798=CARTESIAN_POINT('Ctrl Pts',(43.3760651419751,-26.8573224770441,
910.594669117647));
#152799=CARTESIAN_POINT('Ctrl Pts',(40.5392751458362,-30.6138395280662,
909.100551470588));
#152800=CARTESIAN_POINT('Ctrl Pts',(37.7024851496972,-34.3703565790883,
907.60643382353));
#152801=CARTESIAN_POINT('Ctrl Pts',(34.2237386972451,-37.5416529948095,
906.112316176471));
#152802=CARTESIAN_POINT('Ctrl Pts',(30.744992244793,-40.7129494105307,904.618198529412));
#152803=CARTESIAN_POINT('Ctrl Pts',(26.7427538741697,-43.1910304950644,
903.124080882353));
#152804=CARTESIAN_POINT('Ctrl Pts',(22.7405155035463,-45.6691115795981,
901.629963235294));
#152805=CARTESIAN_POINT('Ctrl Pts',(18.3510766423074,-47.3695892537413,
900.135845588235));
#152806=CARTESIAN_POINT('Ctrl Pts',(13.9616377810684,-49.0700669278844,
898.641727941177));
#152807=CARTESIAN_POINT('Ctrl Pts',(9.33447550508176,-49.9350334639422,
897.147610294118));
#152808=CARTESIAN_POINT('Ctrl Pts',(4.70731322909511,-50.8,895.653492647059));
#152809=CARTESIAN_POINT('Ctrl Pts',(0.,-50.8,894.159375));
#152810=CARTESIAN_POINT('Ctrl Pts',(-4.70731322909511,-50.8,892.665257352941));
#152811=CARTESIAN_POINT('Ctrl Pts',(-9.33447550508177,-49.9350334639422,
891.171139705882));
#152812=CARTESIAN_POINT('Ctrl Pts',(-13.9616377810684,-49.0700669278844,
889.677022058824));
#152813=CARTESIAN_POINT('Ctrl Pts',(-18.3510766423074,-47.3695892537413,
888.182904411765));
#152814=CARTESIAN_POINT('Ctrl Pts',(-22.7405155035463,-45.6691115795981,
886.688786764706));
#152815=CARTESIAN_POINT('Ctrl Pts',(-26.7427538741697,-43.1910304950644,
885.194669117647));
#152816=CARTESIAN_POINT('Ctrl Pts',(-30.744992244793,-40.7129494105307,
883.700551470588));
#152817=CARTESIAN_POINT('Ctrl Pts',(-34.2237386972451,-37.5416529948095,
882.206433823529));
#152818=CARTESIAN_POINT('Ctrl Pts',(-37.7024851496972,-34.3703565790883,
880.712316176471));
#152819=CARTESIAN_POINT('Ctrl Pts',(-40.5392751458362,-30.6138395280662,
879.218198529412));
#152820=CARTESIAN_POINT('Ctrl Pts',(-43.3760651419751,-26.8573224770441,
877.724080882353));
#152821=CARTESIAN_POINT('Ctrl Pts',(-45.4742952008371,-22.6435084734481,
876.229963235294));
#152822=CARTESIAN_POINT('Ctrl Pts',(-47.5725252596992,-18.4296944698521,
874.735845588236));
#152823=CARTESIAN_POINT('Ctrl Pts',(-48.8607426731792,-13.9020798956618,
873.241727941177));
#152824=CARTESIAN_POINT('Ctrl Pts',(-50.1489600866593,-9.37446532147148,
871.747610294118));
#152825=CARTESIAN_POINT('Ctrl Pts',(-50.5832961557877,-4.68723266073574,
870.253492647059));
#152826=CARTESIAN_POINT('Ctrl Pts',(-51.0176322249162,-3.12392900021603E-15,
868.759375));
#152827=CARTESIAN_POINT('Ctrl Pts',(-50.5832961557877,4.68723266073573,
867.265257352941));
#152828=CARTESIAN_POINT('Ctrl Pts',(-50.1489600866593,9.37446532147149,
865.771139705882));
#152829=CARTESIAN_POINT('Ctrl Pts',(-48.8607426731792,13.9020798956618,
864.277022058824));
#152830=CARTESIAN_POINT('Ctrl Pts',(-47.5725252596992,18.4296944698521,
862.782904411765));
#152831=CARTESIAN_POINT('Ctrl Pts',(-45.4742952008371,22.6435084734481,
861.288786764706));
#152832=CARTESIAN_POINT('Ctrl Pts',(-43.3760651419751,26.8573224770442,
859.794669117647));
#152833=CARTESIAN_POINT('Ctrl Pts',(-40.5392751458362,30.6138395280662,
858.300551470588));
#152834=CARTESIAN_POINT('Ctrl Pts',(-37.7024851496972,34.3703565790883,
856.80643382353));
#152835=CARTESIAN_POINT('Ctrl Pts',(-34.2237386972451,37.5416529948095,
855.312316176471));
#152836=CARTESIAN_POINT('Ctrl Pts',(-30.744992244793,40.7129494105307,853.818198529412));
#152837=CARTESIAN_POINT('Ctrl Pts',(-26.7427538741697,43.1910304950644,
852.324080882353));
#152838=CARTESIAN_POINT('Ctrl Pts',(-22.7405155035463,45.6691115795981,
850.829963235294));
#152839=CARTESIAN_POINT('Ctrl Pts',(-18.3510766423074,47.3695892537413,
849.335845588235));
#152840=CARTESIAN_POINT('Ctrl Pts',(-13.9616377810684,49.0700669278844,
847.841727941177));
#152841=CARTESIAN_POINT('Ctrl Pts',(-9.33447550508177,49.9350334639422,
846.347610294118));
#152842=CARTESIAN_POINT('Ctrl Pts',(-4.7073132290951,50.8,844.853492647059));
#152843=CARTESIAN_POINT('Ctrl Pts',(-6.22120573966855E-15,50.8,843.359375));
#152844=CARTESIAN_POINT('Ctrl Pts',(4.70731322909511,50.8,841.865257352941));
#152845=CARTESIAN_POINT('Ctrl Pts',(9.33447550508176,49.9350334639422,840.371139705882));
#152846=CARTESIAN_POINT('Ctrl Pts',(13.9616377810684,49.0700669278844,838.877022058824));
#152847=CARTESIAN_POINT('Ctrl Pts',(18.3510766423074,47.3695892537413,837.382904411765));
#152848=CARTESIAN_POINT('Ctrl Pts',(22.7405155035463,45.6691115795981,835.888786764706));
#152849=CARTESIAN_POINT('Ctrl Pts',(26.7427538741697,43.1910304950644,834.394669117647));
#152850=CARTESIAN_POINT('Ctrl Pts',(30.744992244793,40.7129494105307,832.900551470589));
#152851=CARTESIAN_POINT('Ctrl Pts',(34.2237386972451,37.5416529948095,831.406433823529));
#152852=CARTESIAN_POINT('Ctrl Pts',(37.7024851496972,34.3703565790883,829.912316176471));
#152853=CARTESIAN_POINT('Ctrl Pts',(40.5392751458362,30.6138395280662,828.418198529412));
#152854=CARTESIAN_POINT('Ctrl Pts',(43.3760651419751,26.8573224770442,826.924080882353));
#152855=CARTESIAN_POINT('Ctrl Pts',(45.4742952008372,22.6435084734481,825.429963235294));
#152856=CARTESIAN_POINT('Ctrl Pts',(47.5725252596992,18.4296944698521,823.935845588235));
#152857=CARTESIAN_POINT('Ctrl Pts',(48.8607426731792,13.9020798956618,822.441727941177));
#152858=CARTESIAN_POINT('Ctrl Pts',(50.1489600866593,9.37446532147146,820.947610294118));
#152859=CARTESIAN_POINT('Ctrl Pts',(50.5832961557877,4.68723266073574,819.453492647059));
#152860=CARTESIAN_POINT('Ctrl Pts',(51.0176322249162,9.37178700064808E-15,
817.959375));
#152861=CARTESIAN_POINT('Ctrl Pts',(50.5832961557877,-4.68723266073572,
816.465257352941));
#152862=CARTESIAN_POINT('Ctrl Pts',(50.1489600866593,-9.37446532147149,
814.971139705883));
#152863=CARTESIAN_POINT('Ctrl Pts',(48.8607426731792,-13.9020798956618,
813.477022058824));
#152864=CARTESIAN_POINT('Ctrl Pts',(47.5725252596992,-18.4296944698521,
811.982904411765));
#152865=CARTESIAN_POINT('Ctrl Pts',(45.4742952008371,-22.6435084734482,
810.488786764706));
#152866=CARTESIAN_POINT('Ctrl Pts',(43.3760651419751,-26.8573224770441,
808.994669117647));
#152867=CARTESIAN_POINT('Ctrl Pts',(40.5392751458362,-30.6138395280662,
807.500551470588));
#152868=CARTESIAN_POINT('Ctrl Pts',(37.7024851496972,-34.3703565790883,
806.00643382353));
#152869=CARTESIAN_POINT('Ctrl Pts',(34.2237386972451,-37.5416529948095,
804.512316176471));
#152870=CARTESIAN_POINT('Ctrl Pts',(30.744992244793,-40.7129494105307,803.018198529412));
#152871=CARTESIAN_POINT('Ctrl Pts',(26.7427538741697,-43.1910304950644,
801.524080882353));
#152872=CARTESIAN_POINT('Ctrl Pts',(22.7405155035463,-45.6691115795981,
800.029963235294));
#152873=CARTESIAN_POINT('Ctrl Pts',(18.3510766423074,-47.3695892537413,
798.535845588235));
#152874=CARTESIAN_POINT('Ctrl Pts',(13.9616377810684,-49.0700669278844,
797.041727941177));
#152875=CARTESIAN_POINT('Ctrl Pts',(9.33447550508176,-49.9350334639422,
795.547610294118));
#152876=CARTESIAN_POINT('Ctrl Pts',(4.70731322909511,-50.8,794.053492647059));
#152877=CARTESIAN_POINT('Ctrl Pts',(0.,-50.8,792.559375));
#152878=CARTESIAN_POINT('Ctrl Pts',(-4.70731322909511,-50.8,791.065257352941));
#152879=CARTESIAN_POINT('Ctrl Pts',(-9.33447550508177,-49.9350334639422,
789.571139705882));
#152880=CARTESIAN_POINT('Ctrl Pts',(-13.9616377810684,-49.0700669278844,
788.077022058824));
#152881=CARTESIAN_POINT('Ctrl Pts',(-18.3510766423074,-47.3695892537413,
786.582904411765));
#152882=CARTESIAN_POINT('Ctrl Pts',(-22.7405155035463,-45.6691115795981,
785.088786764706));
#152883=CARTESIAN_POINT('Ctrl Pts',(-26.7427538741697,-43.1910304950644,
783.594669117647));
#152884=CARTESIAN_POINT('Ctrl Pts',(-30.744992244793,-40.7129494105307,
782.100551470588));
#152885=CARTESIAN_POINT('Ctrl Pts',(-34.2237386972451,-37.5416529948095,
780.60643382353));
#152886=CARTESIAN_POINT('Ctrl Pts',(-37.7024851496972,-34.3703565790883,
779.112316176471));
#152887=CARTESIAN_POINT('Ctrl Pts',(-40.5392751458362,-30.6138395280662,
777.618198529412));
#152888=CARTESIAN_POINT('Ctrl Pts',(-43.3760651419751,-26.8573224770441,
776.124080882353));
#152889=CARTESIAN_POINT('Ctrl Pts',(-45.4742952008371,-22.6435084734481,
774.629963235294));
#152890=CARTESIAN_POINT('Ctrl Pts',(-47.5725252596992,-18.4296944698521,
773.135845588235));
#152891=CARTESIAN_POINT('Ctrl Pts',(-48.8607426731792,-13.9020798956618,
771.641727941176));
#152892=CARTESIAN_POINT('Ctrl Pts',(-50.1489600866593,-9.37446532147148,
770.147610294118));
#152893=CARTESIAN_POINT('Ctrl Pts',(-50.5832961557877,-4.68723266073574,
768.653492647059));
#152894=CARTESIAN_POINT('Ctrl Pts',(-51.0176322249162,-3.12392900021603E-15,
767.159375));
#152895=CARTESIAN_POINT('Ctrl Pts',(-50.5832961557877,4.68723266073573,
765.665257352941));
#152896=CARTESIAN_POINT('Ctrl Pts',(-50.1489600866593,9.37446532147149,
764.171139705882));
#152897=CARTESIAN_POINT('Ctrl Pts',(-48.8607426731792,13.9020798956618,
762.677022058824));
#152898=CARTESIAN_POINT('Ctrl Pts',(-47.5725252596992,18.4296944698521,
761.182904411765));
#152899=CARTESIAN_POINT('Ctrl Pts',(-45.4742952008371,22.6435084734481,
759.688786764706));
#152900=CARTESIAN_POINT('Ctrl Pts',(-43.3760651419751,26.8573224770442,
758.194669117647));
#152901=CARTESIAN_POINT('Ctrl Pts',(-40.5392751458362,30.6138395280662,
756.700551470588));
#152902=CARTESIAN_POINT('Ctrl Pts',(-37.7024851496972,34.3703565790883,
755.206433823529));
#152903=CARTESIAN_POINT('Ctrl Pts',(-34.2237386972451,37.5416529948095,
753.712316176471));
#152904=CARTESIAN_POINT('Ctrl Pts',(-30.744992244793,40.7129494105307,752.218198529412));
#152905=CARTESIAN_POINT('Ctrl Pts',(-26.7427538741697,43.1910304950644,
750.724080882353));
#152906=CARTESIAN_POINT('Ctrl Pts',(-22.7405155035463,45.6691115795981,
749.229963235294));
#152907=CARTESIAN_POINT('Ctrl Pts',(-18.3510766423074,47.3695892537413,
747.735845588235));
#152908=CARTESIAN_POINT('Ctrl Pts',(-13.9616377810684,49.0700669278844,
746.241727941177));
#152909=CARTESIAN_POINT('Ctrl Pts',(-9.33447550508177,49.9350334639422,
744.747610294118));
#152910=CARTESIAN_POINT('Ctrl Pts',(-4.7073132290951,50.8,743.253492647059));
#152911=CARTESIAN_POINT('Ctrl Pts',(-6.22120573966855E-15,50.8,741.759375));
#152912=CARTESIAN_POINT('Ctrl Pts',(4.70731322909511,50.8,740.265257352941));
#152913=CARTESIAN_POINT('Ctrl Pts',(9.33447550508176,49.9350334639422,738.771139705882));
#152914=CARTESIAN_POINT('Ctrl Pts',(13.9616377810684,49.0700669278844,737.277022058824));
#152915=CARTESIAN_POINT('Ctrl Pts',(18.3510766423074,47.3695892537413,735.782904411765));
#152916=CARTESIAN_POINT('Ctrl Pts',(22.7405155035463,45.6691115795981,734.288786764706));
#152917=CARTESIAN_POINT('Ctrl Pts',(26.7427538741697,43.1910304950644,732.794669117647));
#152918=CARTESIAN_POINT('Ctrl Pts',(30.744992244793,40.7129494105307,731.300551470588));
#152919=CARTESIAN_POINT('Ctrl Pts',(34.2237386972451,37.5416529948095,729.806433823529));
#152920=CARTESIAN_POINT('Ctrl Pts',(37.7024851496972,34.3703565790883,728.312316176471));
#152921=CARTESIAN_POINT('Ctrl Pts',(40.5392751458362,30.6138395280662,726.818198529412));
#152922=CARTESIAN_POINT('Ctrl Pts',(43.3760651419751,26.8573224770442,725.324080882353));
#152923=CARTESIAN_POINT('Ctrl Pts',(45.4742952008372,22.6435084734481,723.829963235294));
#152924=CARTESIAN_POINT('Ctrl Pts',(47.5725252596992,18.4296944698521,722.335845588235));
#152925=CARTESIAN_POINT('Ctrl Pts',(48.8607426731792,13.9020798956618,720.841727941176));
#152926=CARTESIAN_POINT('Ctrl Pts',(50.1489600866593,9.37446532147146,719.347610294118));
#152927=CARTESIAN_POINT('Ctrl Pts',(50.5832961557877,4.68723266073574,717.853492647059));
#152928=CARTESIAN_POINT('Ctrl Pts',(51.0176322249162,9.37178700064808E-15,
716.359375));
#152929=CARTESIAN_POINT('Ctrl Pts',(50.5832961557877,-4.68723266073572,
714.865257352941));
#152930=CARTESIAN_POINT('Ctrl Pts',(50.1489600866593,-9.37446532147149,
713.371139705882));
#152931=CARTESIAN_POINT('Ctrl Pts',(48.8607426731792,-13.9020798956618,
711.877022058824));
#152932=CARTESIAN_POINT('Ctrl Pts',(47.5725252596992,-18.4296944698521,
710.382904411765));
#152933=CARTESIAN_POINT('Ctrl Pts',(45.4742952008371,-22.6435084734482,
708.888786764706));
#152934=CARTESIAN_POINT('Ctrl Pts',(43.3760651419751,-26.8573224770441,
707.394669117647));
#152935=CARTESIAN_POINT('Ctrl Pts',(40.5392751458362,-30.6138395280662,
705.900551470588));
#152936=CARTESIAN_POINT('Ctrl Pts',(37.7024851496972,-34.3703565790883,
704.406433823529));
#152937=CARTESIAN_POINT('Ctrl Pts',(34.2237386972451,-37.5416529948095,
702.912316176471));
#152938=CARTESIAN_POINT('Ctrl Pts',(30.744992244793,-40.7129494105307,701.418198529412));
#152939=CARTESIAN_POINT('Ctrl Pts',(26.7427538741697,-43.1910304950644,
699.924080882353));
#152940=CARTESIAN_POINT('Ctrl Pts',(22.7405155035463,-45.6691115795981,
698.429963235294));
#152941=CARTESIAN_POINT('Ctrl Pts',(18.3510766423074,-47.3695892537413,
696.935845588235));
#152942=CARTESIAN_POINT('Ctrl Pts',(13.9616377810684,-49.0700669278844,
695.441727941177));
#152943=CARTESIAN_POINT('Ctrl Pts',(9.33447550508176,-49.9350334639422,
693.947610294118));
#152944=CARTESIAN_POINT('Ctrl Pts',(4.70731322909511,-50.8,692.453492647059));
#152945=CARTESIAN_POINT('Ctrl Pts',(0.,-50.8,690.959375));
#152946=CARTESIAN_POINT('Ctrl Pts',(-4.70731322909511,-50.8,689.465257352941));
#152947=CARTESIAN_POINT('Ctrl Pts',(-9.33447550508177,-49.9350334639422,
687.971139705882));
#152948=CARTESIAN_POINT('Ctrl Pts',(-13.9616377810684,-49.0700669278844,
686.477022058824));
#152949=CARTESIAN_POINT('Ctrl Pts',(-18.3510766423074,-47.3695892537413,
684.982904411765));
#152950=CARTESIAN_POINT('Ctrl Pts',(-22.7405155035463,-45.6691115795981,
683.488786764706));
#152951=CARTESIAN_POINT('Ctrl Pts',(-26.7427538741697,-43.1910304950644,
681.994669117647));
#152952=CARTESIAN_POINT('Ctrl Pts',(-30.744992244793,-40.7129494105307,
680.500551470588));
#152953=CARTESIAN_POINT('Ctrl Pts',(-34.2237386972451,-37.5416529948095,
679.006433823529));
#152954=CARTESIAN_POINT('Ctrl Pts',(-37.7024851496972,-34.3703565790883,
677.512316176471));
#152955=CARTESIAN_POINT('Ctrl Pts',(-40.5392751458362,-30.6138395280662,
676.018198529412));
#152956=CARTESIAN_POINT('Ctrl Pts',(-43.3760651419751,-26.8573224770441,
674.524080882353));
#152957=CARTESIAN_POINT('Ctrl Pts',(-45.4742952008371,-22.6435084734481,
673.029963235294));
#152958=CARTESIAN_POINT('Ctrl Pts',(-47.5725252596992,-18.4296944698521,
671.535845588235));
#152959=CARTESIAN_POINT('Ctrl Pts',(-48.8607426731792,-13.9020798956618,
670.041727941177));
#152960=CARTESIAN_POINT('Ctrl Pts',(-50.1489600866593,-9.37446532147148,
668.547610294118));
#152961=CARTESIAN_POINT('Ctrl Pts',(-50.5832961557877,-4.68723266073574,
667.053492647059));
#152962=CARTESIAN_POINT('Ctrl Pts',(-51.0176322249162,-3.12392900021603E-15,
665.559375));
#152963=CARTESIAN_POINT('Ctrl Pts',(-50.5832961557877,4.68723266073573,
664.065257352941));
#152964=CARTESIAN_POINT('Ctrl Pts',(-50.1489600866593,9.37446532147149,
662.571139705882));
#152965=CARTESIAN_POINT('Ctrl Pts',(-48.8607426731792,13.9020798956618,
661.077022058824));
#152966=CARTESIAN_POINT('Ctrl Pts',(-47.5725252596992,18.4296944698521,
659.582904411765));
#152967=CARTESIAN_POINT('Ctrl Pts',(-45.4742952008371,22.6435084734481,
658.088786764706));
#152968=CARTESIAN_POINT('Ctrl Pts',(-43.3760651419751,26.8573224770442,
656.594669117647));
#152969=CARTESIAN_POINT('Ctrl Pts',(-40.5392751458362,30.6138395280662,
655.100551470588));
#152970=CARTESIAN_POINT('Ctrl Pts',(-37.7024851496972,34.3703565790883,
653.606433823529));
#152971=CARTESIAN_POINT('Ctrl Pts',(-34.2237386972451,37.5416529948095,
652.112316176471));
#152972=CARTESIAN_POINT('Ctrl Pts',(-30.744992244793,40.7129494105307,650.618198529412));
#152973=CARTESIAN_POINT('Ctrl Pts',(-26.7427538741697,43.1910304950644,
649.124080882353));
#152974=CARTESIAN_POINT('Ctrl Pts',(-22.7405155035463,45.6691115795981,
647.629963235294));
#152975=CARTESIAN_POINT('Ctrl Pts',(-18.3510766423074,47.3695892537413,
646.135845588235));
#152976=CARTESIAN_POINT('Ctrl Pts',(-13.9616377810684,49.0700669278844,
644.641727941176));
#152977=CARTESIAN_POINT('Ctrl Pts',(-9.33447550508177,49.9350334639422,
643.147610294118));
#152978=CARTESIAN_POINT('Ctrl Pts',(-4.7073132290951,50.8,641.653492647059));
#152979=CARTESIAN_POINT('Ctrl Pts',(-6.22120573966855E-15,50.8,640.159375));
#152980=CARTESIAN_POINT('Ctrl Pts',(4.70731322909511,50.8,638.665257352941));
#152981=CARTESIAN_POINT('Ctrl Pts',(9.33447550508176,49.9350334639422,637.171139705882));
#152982=CARTESIAN_POINT('Ctrl Pts',(13.9616377810684,49.0700669278844,635.677022058824));
#152983=CARTESIAN_POINT('Ctrl Pts',(18.3510766423074,47.3695892537413,634.182904411765));
#152984=CARTESIAN_POINT('Ctrl Pts',(22.7405155035463,45.6691115795981,632.688786764706));
#152985=CARTESIAN_POINT('Ctrl Pts',(26.7427538741697,43.1910304950644,631.194669117647));
#152986=CARTESIAN_POINT('Ctrl Pts',(30.744992244793,40.7129494105307,629.700551470588));
#152987=CARTESIAN_POINT('Ctrl Pts',(34.2237386972451,37.5416529948095,628.206433823529));
#152988=CARTESIAN_POINT('Ctrl Pts',(37.7024851496972,34.3703565790883,626.712316176471));
#152989=CARTESIAN_POINT('Ctrl Pts',(40.5392751458362,30.6138395280662,625.218198529412));
#152990=CARTESIAN_POINT('Ctrl Pts',(43.3760651419751,26.8573224770442,623.724080882353));
#152991=CARTESIAN_POINT('Ctrl Pts',(45.4742952008372,22.6435084734481,622.229963235294));
#152992=CARTESIAN_POINT('Ctrl Pts',(47.5725252596992,18.4296944698521,620.735845588235));
#152993=CARTESIAN_POINT('Ctrl Pts',(48.8607426731792,13.9020798956618,619.241727941177));
#152994=CARTESIAN_POINT('Ctrl Pts',(50.1489600866593,9.37446532147146,617.747610294118));
#152995=CARTESIAN_POINT('Ctrl Pts',(50.5832961557877,4.68723266073574,616.253492647059));
#152996=CARTESIAN_POINT('Ctrl Pts',(51.0176322249162,9.37178700064808E-15,
614.759375));
#152997=CARTESIAN_POINT('Ctrl Pts',(50.5832961557877,-4.68723266073572,
613.265257352941));
#152998=CARTESIAN_POINT('Ctrl Pts',(50.1489600866593,-9.37446532147149,
611.771139705882));
#152999=CARTESIAN_POINT('Ctrl Pts',(48.8607426731792,-13.9020798956618,
610.277022058823));
#153000=CARTESIAN_POINT('Ctrl Pts',(47.5725252596992,-18.4296944698521,
608.782904411765));
#153001=CARTESIAN_POINT('Ctrl Pts',(45.4742952008371,-22.6435084734482,
607.288786764706));
#153002=CARTESIAN_POINT('Ctrl Pts',(43.3760651419751,-26.8573224770441,
605.794669117647));
#153003=CARTESIAN_POINT('Ctrl Pts',(40.5392751458362,-30.6138395280662,
604.300551470588));
#153004=CARTESIAN_POINT('Ctrl Pts',(37.7024851496972,-34.3703565790883,
602.806433823529));
#153005=CARTESIAN_POINT('Ctrl Pts',(34.2237386972451,-37.5416529948095,
601.312316176471));
#153006=CARTESIAN_POINT('Ctrl Pts',(30.744992244793,-40.7129494105307,599.818198529412));
#153007=CARTESIAN_POINT('Ctrl Pts',(26.7427538741697,-43.1910304950644,
598.324080882353));
#153008=CARTESIAN_POINT('Ctrl Pts',(22.7405155035463,-45.6691115795981,
596.829963235294));
#153009=CARTESIAN_POINT('Ctrl Pts',(18.3510766423074,-47.3695892537413,
595.335845588235));
#153010=CARTESIAN_POINT('Ctrl Pts',(13.9616377810684,-49.0700669278844,
593.841727941176));
#153011=CARTESIAN_POINT('Ctrl Pts',(9.33447550508176,-49.9350334639422,
592.347610294118));
#153012=CARTESIAN_POINT('Ctrl Pts',(4.70731322909511,-50.8,590.853492647059));
#153013=CARTESIAN_POINT('Ctrl Pts',(0.,-50.8,589.359375));
#153014=CARTESIAN_POINT('Ctrl Pts',(-4.70731322909511,-50.8,587.865257352941));
#153015=CARTESIAN_POINT('Ctrl Pts',(-9.33447550508177,-49.9350334639422,
586.371139705882));
#153016=CARTESIAN_POINT('Ctrl Pts',(-13.9616377810684,-49.0700669278844,
584.877022058824));
#153017=CARTESIAN_POINT('Ctrl Pts',(-18.3510766423074,-47.3695892537413,
583.382904411765));
#153018=CARTESIAN_POINT('Ctrl Pts',(-22.7405155035463,-45.6691115795981,
581.888786764706));
#153019=CARTESIAN_POINT('Ctrl Pts',(-26.7427538741697,-43.1910304950644,
580.394669117647));
#153020=CARTESIAN_POINT('Ctrl Pts',(-30.744992244793,-40.7129494105307,
578.900551470588));
#153021=CARTESIAN_POINT('Ctrl Pts',(-34.2237386972451,-37.5416529948095,
577.406433823529));
#153022=CARTESIAN_POINT('Ctrl Pts',(-37.7024851496972,-34.3703565790883,
575.912316176471));
#153023=CARTESIAN_POINT('Ctrl Pts',(-40.5392751458362,-30.6138395280662,
574.418198529412));
#153024=CARTESIAN_POINT('Ctrl Pts',(-43.3760651419751,-26.8573224770441,
572.924080882353));
#153025=CARTESIAN_POINT('Ctrl Pts',(-45.4742952008371,-22.6435084734481,
571.429963235294));
#153026=CARTESIAN_POINT('Ctrl Pts',(-47.5725252596992,-18.4296944698521,
569.935845588235));
#153027=CARTESIAN_POINT('Ctrl Pts',(-48.8607426731792,-13.9020798956618,
568.441727941177));
#153028=CARTESIAN_POINT('Ctrl Pts',(-50.1489600866593,-9.37446532147148,
566.947610294118));
#153029=CARTESIAN_POINT('Ctrl Pts',(-50.5832961557877,-4.68723266073574,
565.453492647059));
#153030=CARTESIAN_POINT('Ctrl Pts',(-51.0176322249162,-3.12392900021603E-15,
563.959375));
#153031=CARTESIAN_POINT('Ctrl Pts',(-50.5832961557877,4.68723266073573,
562.465257352941));
#153032=CARTESIAN_POINT('Ctrl Pts',(-50.1489600866593,9.37446532147149,
560.971139705882));
#153033=CARTESIAN_POINT('Ctrl Pts',(-48.8607426731792,13.9020798956618,
559.477022058824));
#153034=CARTESIAN_POINT('Ctrl Pts',(-47.5725252596992,18.4296944698521,
557.982904411765));
#153035=CARTESIAN_POINT('Ctrl Pts',(-45.4742952008371,22.6435084734481,
556.488786764706));
#153036=CARTESIAN_POINT('Ctrl Pts',(-43.3760651419751,26.8573224770442,
554.994669117647));
#153037=CARTESIAN_POINT('Ctrl Pts',(-40.5392751458362,30.6138395280662,
553.500551470588));
#153038=CARTESIAN_POINT('Ctrl Pts',(-37.7024851496972,34.3703565790883,
552.00643382353));
#153039=CARTESIAN_POINT('Ctrl Pts',(-34.2237386972451,37.5416529948095,
550.512316176471));
#153040=CARTESIAN_POINT('Ctrl Pts',(-30.744992244793,40.7129494105307,549.018198529412));
#153041=CARTESIAN_POINT('Ctrl Pts',(-26.7427538741697,43.1910304950644,
547.524080882353));
#153042=CARTESIAN_POINT('Ctrl Pts',(-22.7405155035463,45.6691115795981,
546.029963235294));
#153043=CARTESIAN_POINT('Ctrl Pts',(-18.3510766423074,47.3695892537413,
544.535845588235));
#153044=CARTESIAN_POINT('Ctrl Pts',(-13.9616377810684,49.0700669278844,
543.041727941176));
#153045=CARTESIAN_POINT('Ctrl Pts',(-9.33447550508177,49.9350334639422,
541.547610294118));
#153046=CARTESIAN_POINT('Ctrl Pts',(-4.7073132290951,50.8,540.053492647059));
#153047=CARTESIAN_POINT('Ctrl Pts',(-6.22120573966855E-15,50.8,538.559375));
#153048=CARTESIAN_POINT('Ctrl Pts',(4.70731322909511,50.8,537.065257352941));
#153049=CARTESIAN_POINT('Ctrl Pts',(9.33447550508176,49.9350334639422,535.571139705882));
#153050=CARTESIAN_POINT('Ctrl Pts',(13.9616377810684,49.0700669278844,534.077022058824));
#153051=CARTESIAN_POINT('Ctrl Pts',(18.3510766423074,47.3695892537413,532.582904411765));
#153052=CARTESIAN_POINT('Ctrl Pts',(22.7405155035463,45.6691115795981,531.088786764706));
#153053=CARTESIAN_POINT('Ctrl Pts',(26.7427538741697,43.1910304950644,529.594669117647));
#153054=CARTESIAN_POINT('Ctrl Pts',(30.744992244793,40.7129494105307,528.100551470588));
#153055=CARTESIAN_POINT('Ctrl Pts',(34.2237386972451,37.5416529948095,526.606433823529));
#153056=CARTESIAN_POINT('Ctrl Pts',(37.7024851496972,34.3703565790883,525.112316176471));
#153057=CARTESIAN_POINT('Ctrl Pts',(40.5392751458362,30.6138395280662,523.618198529412));
#153058=CARTESIAN_POINT('Ctrl Pts',(43.3760651419751,26.8573224770442,522.124080882353));
#153059=CARTESIAN_POINT('Ctrl Pts',(45.4742952008372,22.6435084734481,520.629963235294));
#153060=CARTESIAN_POINT('Ctrl Pts',(47.5725252596992,18.4296944698521,519.135845588235));
#153061=CARTESIAN_POINT('Ctrl Pts',(48.8607426731792,13.9020798956618,517.641727941176));
#153062=CARTESIAN_POINT('Ctrl Pts',(50.1489600866593,9.37446532147146,516.147610294118));
#153063=CARTESIAN_POINT('Ctrl Pts',(50.5832961557877,4.68723266073574,514.653492647059));
#153064=CARTESIAN_POINT('Ctrl Pts',(51.0176322249162,9.37178700064808E-15,
513.159375));
#153065=CARTESIAN_POINT('Ctrl Pts',(50.5832961557877,-4.68723266073572,
511.665257352941));
#153066=CARTESIAN_POINT('Ctrl Pts',(50.1489600866593,-9.37446532147149,
510.171139705882));
#153067=CARTESIAN_POINT('Ctrl Pts',(48.8607426731792,-13.9020798956618,
508.677022058824));
#153068=CARTESIAN_POINT('Ctrl Pts',(47.5725252596992,-18.4296944698521,
507.182904411765));
#153069=CARTESIAN_POINT('Ctrl Pts',(45.4742952008371,-22.6435084734482,
505.688786764706));
#153070=CARTESIAN_POINT('Ctrl Pts',(43.3760651419751,-26.8573224770441,
504.194669117647));
#153071=CARTESIAN_POINT('Ctrl Pts',(40.5392751458362,-30.6138395280662,
502.700551470588));
#153072=CARTESIAN_POINT('Ctrl Pts',(37.7024851496972,-34.3703565790883,
501.206433823529));
#153073=CARTESIAN_POINT('Ctrl Pts',(34.2237386972451,-37.5416529948095,
499.712316176471));
#153074=CARTESIAN_POINT('Ctrl Pts',(30.744992244793,-40.7129494105307,498.218198529412));
#153075=CARTESIAN_POINT('Ctrl Pts',(26.7427538741697,-43.1910304950644,
496.724080882353));
#153076=CARTESIAN_POINT('Ctrl Pts',(22.7405155035463,-45.6691115795981,
495.229963235294));
#153077=CARTESIAN_POINT('Ctrl Pts',(18.3510766423074,-47.3695892537413,
493.735845588235));
#153078=CARTESIAN_POINT('Ctrl Pts',(13.9616377810684,-49.0700669278844,
492.241727941177));
#153079=CARTESIAN_POINT('Ctrl Pts',(9.33447550508176,-49.9350334639422,
490.747610294118));
#153080=CARTESIAN_POINT('Ctrl Pts',(4.70731322909511,-50.8,489.253492647059));
#153081=CARTESIAN_POINT('Ctrl Pts',(0.,-50.8,487.759375));
#153082=CARTESIAN_POINT('Ctrl Pts',(-4.70731322909511,-50.8,486.265257352941));
#153083=CARTESIAN_POINT('Ctrl Pts',(-9.33447550508177,-49.9350334639422,
484.771139705882));
#153084=CARTESIAN_POINT('Ctrl Pts',(-13.9616377810684,-49.0700669278844,
483.277022058824));
#153085=CARTESIAN_POINT('Ctrl Pts',(-18.3510766423074,-47.3695892537413,
481.782904411765));
#153086=CARTESIAN_POINT('Ctrl Pts',(-22.7405155035463,-45.6691115795981,
480.288786764706));
#153087=CARTESIAN_POINT('Ctrl Pts',(-26.7427538741697,-43.1910304950644,
478.794669117647));
#153088=CARTESIAN_POINT('Ctrl Pts',(-30.744992244793,-40.7129494105307,
477.300551470589));
#153089=CARTESIAN_POINT('Ctrl Pts',(-34.2237386972451,-37.5416529948095,
475.80643382353));
#153090=CARTESIAN_POINT('Ctrl Pts',(-37.7024851496972,-34.3703565790883,
474.312316176471));
#153091=CARTESIAN_POINT('Ctrl Pts',(-40.5392751458362,-30.6138395280662,
472.818198529412));
#153092=CARTESIAN_POINT('Ctrl Pts',(-43.3760651419751,-26.8573224770441,
471.324080882353));
#153093=CARTESIAN_POINT('Ctrl Pts',(-45.4742952008371,-22.6435084734481,
469.829963235294));
#153094=CARTESIAN_POINT('Ctrl Pts',(-47.5725252596992,-18.4296944698521,
468.335845588235));
#153095=CARTESIAN_POINT('Ctrl Pts',(-48.8607426731792,-13.9020798956618,
466.841727941176));
#153096=CARTESIAN_POINT('Ctrl Pts',(-50.1489600866593,-9.37446532147148,
465.347610294118));
#153097=CARTESIAN_POINT('Ctrl Pts',(-50.5832961557877,-4.68723266073574,
463.853492647059));
#153098=CARTESIAN_POINT('Ctrl Pts',(-51.0176322249162,-3.12392900021603E-15,
462.359375));
#153099=CARTESIAN_POINT('Ctrl Pts',(-50.5832961557877,4.68723266073573,
460.865257352941));
#153100=CARTESIAN_POINT('Ctrl Pts',(-50.1489600866593,9.37446532147149,
459.371139705883));
#153101=CARTESIAN_POINT('Ctrl Pts',(-48.8607426731792,13.9020798956618,
457.877022058824));
#153102=CARTESIAN_POINT('Ctrl Pts',(-47.5725252596992,18.4296944698521,
456.382904411765));
#153103=CARTESIAN_POINT('Ctrl Pts',(-45.4742952008371,22.6435084734481,
454.888786764706));
#153104=CARTESIAN_POINT('Ctrl Pts',(-43.3760651419751,26.8573224770442,
453.394669117647));
#153105=CARTESIAN_POINT('Ctrl Pts',(-40.5392751458362,30.6138395280662,
451.900551470588));
#153106=CARTESIAN_POINT('Ctrl Pts',(-37.7024851496972,34.3703565790883,
450.406433823529));
#153107=CARTESIAN_POINT('Ctrl Pts',(-34.2237386972451,37.5416529948095,
448.912316176471));
#153108=CARTESIAN_POINT('Ctrl Pts',(-30.744992244793,40.7129494105307,447.418198529412));
#153109=CARTESIAN_POINT('Ctrl Pts',(-26.7427538741697,43.1910304950644,
445.924080882353));
#153110=CARTESIAN_POINT('Ctrl Pts',(-22.7405155035463,45.6691115795981,
444.429963235294));
#153111=CARTESIAN_POINT('Ctrl Pts',(-18.3510766423074,47.3695892537413,
442.935845588235));
#153112=CARTESIAN_POINT('Ctrl Pts',(-13.9616377810684,49.0700669278844,
441.441727941177));
#153113=CARTESIAN_POINT('Ctrl Pts',(-9.33447550508177,49.9350334639422,
439.947610294118));
#153114=CARTESIAN_POINT('Ctrl Pts',(-4.7073132290951,50.8,438.453492647059));
#153115=CARTESIAN_POINT('Ctrl Pts',(-6.22120573966855E-15,50.8,436.959375));
#153116=CARTESIAN_POINT('Ctrl Pts',(4.70731322909511,50.8,435.465257352941));
#153117=CARTESIAN_POINT('Ctrl Pts',(9.33447550508176,49.9350334639422,433.971139705882));
#153118=CARTESIAN_POINT('Ctrl Pts',(13.9616377810684,49.0700669278844,432.477022058824));
#153119=CARTESIAN_POINT('Ctrl Pts',(18.3510766423074,47.3695892537413,430.982904411765));
#153120=CARTESIAN_POINT('Ctrl Pts',(22.7405155035463,45.6691115795981,429.488786764706));
#153121=CARTESIAN_POINT('Ctrl Pts',(26.7427538741697,43.1910304950644,427.994669117647));
#153122=CARTESIAN_POINT('Ctrl Pts',(30.744992244793,40.7129494105307,426.500551470588));
#153123=CARTESIAN_POINT('Ctrl Pts',(34.2237386972451,37.5416529948095,425.00643382353));
#153124=CARTESIAN_POINT('Ctrl Pts',(37.7024851496972,34.3703565790883,423.512316176471));
#153125=CARTESIAN_POINT('Ctrl Pts',(40.5392751458362,30.6138395280662,422.018198529412));
#153126=CARTESIAN_POINT('Ctrl Pts',(43.3760651419751,26.8573224770442,420.524080882353));
#153127=CARTESIAN_POINT('Ctrl Pts',(45.4742952008372,22.6435084734481,419.029963235294));
#153128=CARTESIAN_POINT('Ctrl Pts',(47.5725252596992,18.4296944698521,417.535845588235));
#153129=CARTESIAN_POINT('Ctrl Pts',(48.8607426731792,13.9020798956618,416.041727941177));
#153130=CARTESIAN_POINT('Ctrl Pts',(50.1489600866593,9.37446532147146,414.547610294118));
#153131=CARTESIAN_POINT('Ctrl Pts',(50.5832961557877,4.68723266073574,413.053492647059));
#153132=CARTESIAN_POINT('Ctrl Pts',(51.0176322249162,9.37178700064808E-15,
411.559375));
#153133=CARTESIAN_POINT('Ctrl Pts',(50.5832961557877,-4.68723266073572,
410.065257352941));
#153134=CARTESIAN_POINT('Ctrl Pts',(50.1489600866593,-9.37446532147149,
408.571139705882));
#153135=CARTESIAN_POINT('Ctrl Pts',(48.8607426731792,-13.9020798956618,
407.077022058824));
#153136=CARTESIAN_POINT('Ctrl Pts',(47.5725252596992,-18.4296944698521,
405.582904411765));
#153137=CARTESIAN_POINT('Ctrl Pts',(45.4742952008371,-22.6435084734482,
404.088786764706));
#153138=CARTESIAN_POINT('Ctrl Pts',(43.3760651419751,-26.8573224770441,
402.594669117647));
#153139=CARTESIAN_POINT('Ctrl Pts',(40.5392751458362,-30.6138395280662,
401.100551470588));
#153140=CARTESIAN_POINT('Ctrl Pts',(37.7024851496972,-34.3703565790883,
399.60643382353));
#153141=CARTESIAN_POINT('Ctrl Pts',(34.2237386972451,-37.5416529948095,
398.112316176471));
#153142=CARTESIAN_POINT('Ctrl Pts',(30.744992244793,-40.7129494105307,396.618198529412));
#153143=CARTESIAN_POINT('Ctrl Pts',(26.7427538741697,-43.1910304950644,
395.124080882353));
#153144=CARTESIAN_POINT('Ctrl Pts',(22.7405155035463,-45.6691115795981,
393.629963235294));
#153145=CARTESIAN_POINT('Ctrl Pts',(18.3510766423074,-47.3695892537413,
392.135845588235));
#153146=CARTESIAN_POINT('Ctrl Pts',(13.9616377810684,-49.0700669278844,
390.641727941176));
#153147=CARTESIAN_POINT('Ctrl Pts',(9.33447550508176,-49.9350334639422,
389.147610294118));
#153148=CARTESIAN_POINT('Ctrl Pts',(4.70731322909511,-50.8,387.653492647059));
#153149=CARTESIAN_POINT('Ctrl Pts',(0.,-50.8,386.159375));
#153150=CARTESIAN_POINT('Ctrl Pts',(-4.70731322909511,-50.8,384.665257352941));
#153151=CARTESIAN_POINT('Ctrl Pts',(-9.33447550508177,-49.9350334639422,
383.171139705882));
#153152=CARTESIAN_POINT('Ctrl Pts',(-13.9616377810684,-49.0700669278844,
381.677022058824));
#153153=CARTESIAN_POINT('Ctrl Pts',(-18.3510766423074,-47.3695892537413,
380.182904411765));
#153154=CARTESIAN_POINT('Ctrl Pts',(-22.7405155035463,-45.6691115795981,
378.688786764706));
#153155=CARTESIAN_POINT('Ctrl Pts',(-26.7427538741697,-43.1910304950644,
377.194669117647));
#153156=CARTESIAN_POINT('Ctrl Pts',(-30.744992244793,-40.7129494105307,
375.700551470588));
#153157=CARTESIAN_POINT('Ctrl Pts',(-34.2237386972451,-37.5416529948095,
374.206433823529));
#153158=CARTESIAN_POINT('Ctrl Pts',(-37.7024851496972,-34.3703565790883,
372.712316176471));
#153159=CARTESIAN_POINT('Ctrl Pts',(-40.5392751458362,-30.6138395280662,
371.218198529412));
#153160=CARTESIAN_POINT('Ctrl Pts',(-43.3760651419751,-26.8573224770441,
369.724080882353));
#153161=CARTESIAN_POINT('Ctrl Pts',(-45.4742952008371,-22.6435084734481,
368.229963235294));
#153162=CARTESIAN_POINT('Ctrl Pts',(-47.5725252596992,-18.4296944698521,
366.735845588235));
#153163=CARTESIAN_POINT('Ctrl Pts',(-48.8607426731792,-13.9020798956618,
365.241727941177));
#153164=CARTESIAN_POINT('Ctrl Pts',(-50.1489600866593,-9.37446532147148,
363.747610294118));
#153165=CARTESIAN_POINT('Ctrl Pts',(-50.5832961557877,-4.68723266073574,
362.253492647059));
#153166=CARTESIAN_POINT('Ctrl Pts',(-51.0176322249162,-3.12392900021603E-15,
360.759375));
#153167=CARTESIAN_POINT('Ctrl Pts',(-50.5832961557877,4.68723266073573,
359.265257352941));
#153168=CARTESIAN_POINT('Ctrl Pts',(-50.1489600866593,9.37446532147149,
357.771139705883));
#153169=CARTESIAN_POINT('Ctrl Pts',(-48.8607426731792,13.9020798956618,
356.277022058824));
#153170=CARTESIAN_POINT('Ctrl Pts',(-47.5725252596992,18.4296944698521,
354.782904411765));
#153171=CARTESIAN_POINT('Ctrl Pts',(-45.4742952008371,22.6435084734481,
353.288786764706));
#153172=CARTESIAN_POINT('Ctrl Pts',(-43.3760651419751,26.8573224770442,
351.794669117647));
#153173=CARTESIAN_POINT('Ctrl Pts',(-40.5392751458362,30.6138395280662,
350.300551470588));
#153174=CARTESIAN_POINT('Ctrl Pts',(-37.7024851496972,34.3703565790883,
348.80643382353));
#153175=CARTESIAN_POINT('Ctrl Pts',(-34.2237386972451,37.5416529948095,
347.312316176471));
#153176=CARTESIAN_POINT('Ctrl Pts',(-30.744992244793,40.7129494105307,345.818198529412));
#153177=CARTESIAN_POINT('Ctrl Pts',(-26.7427538741697,43.1910304950644,
344.324080882353));
#153178=CARTESIAN_POINT('Ctrl Pts',(-22.7405155035463,45.6691115795981,
342.829963235294));
#153179=CARTESIAN_POINT('Ctrl Pts',(-18.3510766423074,47.3695892537413,
341.335845588235));
#153180=CARTESIAN_POINT('Ctrl Pts',(-13.9616377810684,49.0700669278844,
339.841727941176));
#153181=CARTESIAN_POINT('Ctrl Pts',(-9.33447550508177,49.9350334639422,
338.347610294118));
#153182=CARTESIAN_POINT('Ctrl Pts',(-4.7073132290951,50.8,336.853492647059));
#153183=CARTESIAN_POINT('Ctrl Pts',(-6.22120573966855E-15,50.8,335.359375));
#153184=CARTESIAN_POINT('Ctrl Pts',(4.70731322909511,50.8,333.865257352941));
#153185=CARTESIAN_POINT('Ctrl Pts',(9.33447550508176,49.9350334639422,332.371139705882));
#153186=CARTESIAN_POINT('Ctrl Pts',(13.9616377810684,49.0700669278844,330.877022058824));
#153187=CARTESIAN_POINT('Ctrl Pts',(18.3510766423074,47.3695892537413,329.382904411765));
#153188=CARTESIAN_POINT('Ctrl Pts',(22.7405155035463,45.6691115795981,327.888786764706));
#153189=CARTESIAN_POINT('Ctrl Pts',(26.7427538741697,43.1910304950644,326.394669117647));
#153190=CARTESIAN_POINT('Ctrl Pts',(30.744992244793,40.7129494105307,324.900551470588));
#153191=CARTESIAN_POINT('Ctrl Pts',(34.2237386972451,37.5416529948095,323.406433823529));
#153192=CARTESIAN_POINT('Ctrl Pts',(37.7024851496972,34.3703565790883,321.912316176471));
#153193=CARTESIAN_POINT('Ctrl Pts',(40.5392751458362,30.6138395280662,320.418198529412));
#153194=CARTESIAN_POINT('Ctrl Pts',(43.3760651419751,26.8573224770442,318.924080882353));
#153195=CARTESIAN_POINT('Ctrl Pts',(45.4742952008372,22.6435084734481,317.429963235294));
#153196=CARTESIAN_POINT('Ctrl Pts',(47.5725252596992,18.4296944698521,315.935845588235));
#153197=CARTESIAN_POINT('Ctrl Pts',(48.8607426731792,13.9020798956618,314.441727941176));
#153198=CARTESIAN_POINT('Ctrl Pts',(50.1489600866593,9.37446532147146,312.947610294118));
#153199=CARTESIAN_POINT('Ctrl Pts',(50.5832961557877,4.68723266073574,311.453492647059));
#153200=CARTESIAN_POINT('Ctrl Pts',(51.0176322249162,9.37178700064808E-15,
309.959375));
#153201=CARTESIAN_POINT('Ctrl Pts',(50.5832961557877,-4.68723266073572,
308.465257352941));
#153202=CARTESIAN_POINT('Ctrl Pts',(50.1489600866593,-9.37446532147149,
306.971139705882));
#153203=CARTESIAN_POINT('Ctrl Pts',(48.8607426731792,-13.9020798956618,
305.477022058824));
#153204=CARTESIAN_POINT('Ctrl Pts',(47.5725252596992,-18.4296944698521,
303.982904411765));
#153205=CARTESIAN_POINT('Ctrl Pts',(45.4742952008371,-22.6435084734482,
302.488786764706));
#153206=CARTESIAN_POINT('Ctrl Pts',(43.3760651419751,-26.8573224770441,
300.994669117647));
#153207=CARTESIAN_POINT('Ctrl Pts',(40.5392751458362,-30.6138395280662,
299.500551470588));
#153208=CARTESIAN_POINT('Ctrl Pts',(37.7024851496972,-34.3703565790883,
298.00643382353));
#153209=CARTESIAN_POINT('Ctrl Pts',(34.2237386972451,-37.5416529948095,
296.512316176471));
#153210=CARTESIAN_POINT('Ctrl Pts',(30.744992244793,-40.7129494105307,295.018198529412));
#153211=CARTESIAN_POINT('Ctrl Pts',(26.7427538741697,-43.1910304950644,
293.524080882353));
#153212=CARTESIAN_POINT('Ctrl Pts',(22.7405155035463,-45.6691115795981,
292.029963235294));
#153213=CARTESIAN_POINT('Ctrl Pts',(18.3510766423074,-47.3695892537413,
290.535845588235));
#153214=CARTESIAN_POINT('Ctrl Pts',(13.9616377810684,-49.0700669278844,
289.041727941177));
#153215=CARTESIAN_POINT('Ctrl Pts',(9.33447550508176,-49.9350334639422,
287.547610294118));
#153216=CARTESIAN_POINT('Ctrl Pts',(4.70731322909511,-50.8,286.053492647059));
#153217=CARTESIAN_POINT('Ctrl Pts',(0.,-50.8,284.559375));
#153218=CARTESIAN_POINT('Ctrl Pts',(-4.70731322909511,-50.8,283.065257352941));
#153219=CARTESIAN_POINT('Ctrl Pts',(-9.33447550508177,-49.9350334639422,
281.571139705882));
#153220=CARTESIAN_POINT('Ctrl Pts',(-13.9616377810684,-49.0700669278844,
280.077022058824));
#153221=CARTESIAN_POINT('Ctrl Pts',(-18.3510766423074,-47.3695892537413,
278.582904411765));
#153222=CARTESIAN_POINT('Ctrl Pts',(-22.7405155035463,-45.6691115795981,
277.088786764706));
#153223=CARTESIAN_POINT('Ctrl Pts',(-26.7427538741697,-43.1910304950644,
275.594669117647));
#153224=CARTESIAN_POINT('Ctrl Pts',(-30.744992244793,-40.7129494105307,
274.100551470588));
#153225=CARTESIAN_POINT('Ctrl Pts',(-34.2237386972451,-37.5416529948095,
272.606433823529));
#153226=CARTESIAN_POINT('Ctrl Pts',(-37.7024851496972,-34.3703565790883,
271.112316176471));
#153227=CARTESIAN_POINT('Ctrl Pts',(-40.5392751458362,-30.6138395280662,
269.618198529412));
#153228=CARTESIAN_POINT('Ctrl Pts',(-43.3760651419751,-26.8573224770441,
268.124080882353));
#153229=CARTESIAN_POINT('Ctrl Pts',(-45.4742952008371,-22.6435084734481,
266.629963235294));
#153230=CARTESIAN_POINT('Ctrl Pts',(-47.5725252596992,-18.4296944698521,
265.135845588235));
#153231=CARTESIAN_POINT('Ctrl Pts',(-48.8607426731792,-13.9020798956618,
263.641727941176));
#153232=CARTESIAN_POINT('Ctrl Pts',(-50.1489600866593,-9.37446532147148,
262.147610294118));
#153233=CARTESIAN_POINT('Ctrl Pts',(-50.5832961557877,-4.68723266073574,
260.653492647059));
#153234=CARTESIAN_POINT('Ctrl Pts',(-51.0176322249162,-3.12392900021603E-15,
259.159375));
#153235=CARTESIAN_POINT('Ctrl Pts',(-50.5832961557877,4.68723266073573,
257.665257352941));
#153236=CARTESIAN_POINT('Ctrl Pts',(-50.1489600866593,9.37446532147149,
256.171139705882));
#153237=CARTESIAN_POINT('Ctrl Pts',(-48.8607426731792,13.9020798956618,
254.677022058823));
#153238=CARTESIAN_POINT('Ctrl Pts',(-47.5725252596992,18.4296944698521,
253.182904411765));
#153239=CARTESIAN_POINT('Ctrl Pts',(-45.4742952008371,22.6435084734481,
251.688786764706));
#153240=CARTESIAN_POINT('Ctrl Pts',(-43.3760651419751,26.8573224770442,
250.194669117647));
#153241=CARTESIAN_POINT('Ctrl Pts',(-40.5392751458362,30.6138395280662,
248.700551470588));
#153242=CARTESIAN_POINT('Ctrl Pts',(-37.7024851496972,34.3703565790883,
247.206433823529));
#153243=CARTESIAN_POINT('Ctrl Pts',(-34.2237386972451,37.5416529948095,
245.712316176471));
#153244=CARTESIAN_POINT('Ctrl Pts',(-30.744992244793,40.7129494105307,244.218198529412));
#153245=CARTESIAN_POINT('Ctrl Pts',(-26.7427538741697,43.1910304950644,
242.724080882353));
#153246=CARTESIAN_POINT('Ctrl Pts',(-22.7405155035463,45.6691115795981,
241.229963235294));
#153247=CARTESIAN_POINT('Ctrl Pts',(-18.3510766423074,47.3695892537413,
239.735845588235));
#153248=CARTESIAN_POINT('Ctrl Pts',(-13.9616377810684,49.0700669278844,
238.241727941177));
#153249=CARTESIAN_POINT('Ctrl Pts',(-9.33447550508177,49.9350334639422,
236.747610294118));
#153250=CARTESIAN_POINT('Ctrl Pts',(-4.7073132290951,50.8,235.253492647059));
#153251=CARTESIAN_POINT('Ctrl Pts',(-6.22120573966855E-15,50.8,233.759375));
#153252=CARTESIAN_POINT('Ctrl Pts',(4.70731322909511,50.8,232.265257352941));
#153253=CARTESIAN_POINT('Ctrl Pts',(9.33447550508176,49.9350334639422,230.771139705882));
#153254=CARTESIAN_POINT('Ctrl Pts',(13.9616377810684,49.0700669278844,229.277022058824));
#153255=CARTESIAN_POINT('Ctrl Pts',(18.3510766423074,47.3695892537413,227.782904411765));
#153256=CARTESIAN_POINT('Ctrl Pts',(22.7405155035463,45.6691115795981,226.288786764706));
#153257=CARTESIAN_POINT('Ctrl Pts',(26.7427538741697,43.1910304950644,224.794669117647));
#153258=CARTESIAN_POINT('Ctrl Pts',(30.744992244793,40.7129494105307,223.300551470588));
#153259=CARTESIAN_POINT('Ctrl Pts',(34.2237386972451,37.5416529948095,221.80643382353));
#153260=CARTESIAN_POINT('Ctrl Pts',(37.7024851496972,34.3703565790883,220.312316176471));
#153261=CARTESIAN_POINT('Ctrl Pts',(40.5392751458362,30.6138395280662,218.818198529412));
#153262=CARTESIAN_POINT('Ctrl Pts',(43.3760651419751,26.8573224770442,217.324080882353));
#153263=CARTESIAN_POINT('Ctrl Pts',(45.4742952008372,22.6435084734481,215.829963235294));
#153264=CARTESIAN_POINT('Ctrl Pts',(47.5725252596992,18.4296944698521,214.335845588235));
#153265=CARTESIAN_POINT('Ctrl Pts',(48.8607426731792,13.9020798956618,212.841727941177));
#153266=CARTESIAN_POINT('Ctrl Pts',(50.1489600866593,9.37446532147146,211.347610294118));
#153267=CARTESIAN_POINT('Ctrl Pts',(50.5832961557877,4.68723266073574,209.853492647059));
#153268=CARTESIAN_POINT('Ctrl Pts',(51.0176322249162,9.37178700064808E-15,
208.359375));
#153269=CARTESIAN_POINT('Ctrl Pts',(50.5832961557877,-4.68723266073572,
206.865257352941));
#153270=CARTESIAN_POINT('Ctrl Pts',(50.1489600866593,-9.37446532147149,
205.371139705882));
#153271=CARTESIAN_POINT('Ctrl Pts',(48.8607426731792,-13.9020798956618,
203.877022058824));
#153272=CARTESIAN_POINT('Ctrl Pts',(47.5725252596992,-18.4296944698521,
202.382904411765));
#153273=CARTESIAN_POINT('Ctrl Pts',(45.4742952008371,-22.6435084734482,
200.888786764706));
#153274=CARTESIAN_POINT('Ctrl Pts',(43.3760651419751,-26.8573224770441,
199.394669117647));
#153275=CARTESIAN_POINT('Ctrl Pts',(40.5392751458362,-30.6138395280662,
197.900551470588));
#153276=CARTESIAN_POINT('Ctrl Pts',(37.7024851496972,-34.3703565790883,
196.406433823529));
#153277=CARTESIAN_POINT('Ctrl Pts',(34.2237386972451,-37.5416529948095,
194.912316176471));
#153278=CARTESIAN_POINT('Ctrl Pts',(30.744992244793,-40.7129494105307,193.418198529412));
#153279=CARTESIAN_POINT('Ctrl Pts',(26.7427538741697,-43.1910304950644,
191.924080882353));
#153280=CARTESIAN_POINT('Ctrl Pts',(22.7405155035463,-45.6691115795981,
190.429963235294));
#153281=CARTESIAN_POINT('Ctrl Pts',(18.3510766423074,-47.3695892537413,
188.935845588235));
#153282=CARTESIAN_POINT('Ctrl Pts',(13.9616377810684,-49.0700669278844,
187.441727941176));
#153283=CARTESIAN_POINT('Ctrl Pts',(9.33447550508176,-49.9350334639422,
185.947610294118));
#153284=CARTESIAN_POINT('Ctrl Pts',(4.70731322909511,-50.8,184.453492647059));
#153285=CARTESIAN_POINT('Ctrl Pts',(0.,-50.8,182.959375));
#153286=CARTESIAN_POINT('Ctrl Pts',(-4.70731322909511,-50.8,181.465257352941));
#153287=CARTESIAN_POINT('Ctrl Pts',(-9.33447550508177,-49.9350334639422,
179.971139705882));
#153288=CARTESIAN_POINT('Ctrl Pts',(-13.9616377810684,-49.0700669278844,
178.477022058824));
#153289=CARTESIAN_POINT('Ctrl Pts',(-18.3510766423074,-47.3695892537413,
176.982904411765));
#153290=CARTESIAN_POINT('Ctrl Pts',(-22.7405155035463,-45.6691115795981,
175.488786764706));
#153291=CARTESIAN_POINT('Ctrl Pts',(-26.7427538741697,-43.1910304950644,
173.994669117647));
#153292=CARTESIAN_POINT('Ctrl Pts',(-30.744992244793,-40.7129494105307,
172.500551470588));
#153293=CARTESIAN_POINT('Ctrl Pts',(-34.2237386972451,-37.5416529948095,
171.00643382353));
#153294=CARTESIAN_POINT('Ctrl Pts',(-37.7024851496972,-34.3703565790883,
169.512316176471));
#153295=CARTESIAN_POINT('Ctrl Pts',(-40.5392751458362,-30.6138395280662,
168.018198529412));
#153296=CARTESIAN_POINT('Ctrl Pts',(-43.3760651419751,-26.8573224770441,
166.524080882353));
#153297=CARTESIAN_POINT('Ctrl Pts',(-45.4742952008371,-22.6435084734481,
165.029963235294));
#153298=CARTESIAN_POINT('Ctrl Pts',(-47.5725252596992,-18.4296944698521,
163.535845588235));
#153299=CARTESIAN_POINT('Ctrl Pts',(-48.8607426731792,-13.9020798956618,
162.041727941177));
#153300=CARTESIAN_POINT('Ctrl Pts',(-50.1489600866593,-9.37446532147148,
160.547610294118));
#153301=CARTESIAN_POINT('Ctrl Pts',(-50.5832961557877,-4.68723266073574,
159.053492647059));
#153302=CARTESIAN_POINT('Ctrl Pts',(-51.0176322249162,-3.12392900021603E-15,
157.559375));
#153303=CARTESIAN_POINT('Ctrl Pts',(-50.5832961557877,4.68723266073573,
156.065257352941));
#153304=CARTESIAN_POINT('Ctrl Pts',(-50.1489600866593,9.37446532147149,
154.571139705882));
#153305=CARTESIAN_POINT('Ctrl Pts',(-48.8607426731792,13.9020798956618,
153.077022058824));
#153306=CARTESIAN_POINT('Ctrl Pts',(-47.5725252596992,18.4296944698521,
151.582904411765));
#153307=CARTESIAN_POINT('Ctrl Pts',(-45.4742952008371,22.6435084734481,
150.088786764706));
#153308=CARTESIAN_POINT('Ctrl Pts',(-43.3760651419751,26.8573224770442,
148.594669117647));
#153309=CARTESIAN_POINT('Ctrl Pts',(-40.5392751458362,30.6138395280662,
147.100551470588));
#153310=CARTESIAN_POINT('Ctrl Pts',(-37.7024851496972,34.3703565790883,
145.606433823529));
#153311=CARTESIAN_POINT('Ctrl Pts',(-34.2237386972451,37.5416529948095,
144.112316176471));
#153312=CARTESIAN_POINT('Ctrl Pts',(-30.744992244793,40.7129494105307,142.618198529412));
#153313=CARTESIAN_POINT('Ctrl Pts',(-26.7427538741697,43.1910304950644,
141.124080882353));
#153314=CARTESIAN_POINT('Ctrl Pts',(-22.7405155035463,45.6691115795981,
139.629963235294));
#153315=CARTESIAN_POINT('Ctrl Pts',(-18.3510766423074,47.3695892537413,
138.135845588235));
#153316=CARTESIAN_POINT('Ctrl Pts',(-13.9616377810684,49.0700669278844,
136.641727941176));
#153317=CARTESIAN_POINT('Ctrl Pts',(-9.33447550508177,49.9350334639422,
135.147610294118));
#153318=CARTESIAN_POINT('Ctrl Pts',(-4.7073132290951,50.8,133.653492647059));
#153319=CARTESIAN_POINT('Ctrl Pts',(-6.22120573966855E-15,50.8,132.159375));
#153320=CARTESIAN_POINT('Ctrl Pts',(4.70731322909511,50.8,130.665257352941));
#153321=CARTESIAN_POINT('Ctrl Pts',(9.33447550508176,49.9350334639422,129.171139705882));
#153322=CARTESIAN_POINT('Ctrl Pts',(13.9616377810684,49.0700669278844,127.677022058823));
#153323=CARTESIAN_POINT('Ctrl Pts',(18.3510766423074,47.3695892537413,126.182904411765));
#153324=CARTESIAN_POINT('Ctrl Pts',(22.7405155035463,45.6691115795981,124.688786764706));
#153325=CARTESIAN_POINT('Ctrl Pts',(26.7427538741697,43.1910304950644,123.194669117647));
#153326=CARTESIAN_POINT('Ctrl Pts',(30.744992244793,40.7129494105307,121.700551470588));
#153327=CARTESIAN_POINT('Ctrl Pts',(34.2237386972451,37.5416529948095,120.206433823529));
#153328=CARTESIAN_POINT('Ctrl Pts',(37.7024851496972,34.3703565790883,118.712316176471));
#153329=CARTESIAN_POINT('Ctrl Pts',(40.5392751458362,30.6138395280662,117.218198529412));
#153330=CARTESIAN_POINT('Ctrl Pts',(43.3760651419751,26.8573224770442,115.724080882353));
#153331=CARTESIAN_POINT('Ctrl Pts',(45.4742952008372,22.6435084734481,114.229963235294));
#153332=CARTESIAN_POINT('Ctrl Pts',(47.5725252596992,18.4296944698521,112.735845588235));
#153333=CARTESIAN_POINT('Ctrl Pts',(48.8607426731792,13.9020798956618,111.241727941177));
#153334=CARTESIAN_POINT('Ctrl Pts',(50.1489600866593,9.37446532147146,109.747610294118));
#153335=CARTESIAN_POINT('Ctrl Pts',(50.5832961557877,4.68723266073574,108.253492647059));
#153336=CARTESIAN_POINT('Ctrl Pts',(51.0176322249162,9.37178700064808E-15,
106.759375));
#153337=CARTESIAN_POINT('Ctrl Pts',(50.5832961557877,-4.68723266073572,
105.265257352941));
#153338=CARTESIAN_POINT('Ctrl Pts',(50.1489600866593,-9.37446532147149,
103.771139705883));
#153339=CARTESIAN_POINT('Ctrl Pts',(48.8607426731792,-13.9020798956618,
102.277022058824));
#153340=CARTESIAN_POINT('Ctrl Pts',(47.5725252596992,-18.4296944698521,
100.782904411765));
#153341=CARTESIAN_POINT('Ctrl Pts',(45.4742952008371,-22.6435084734482,
99.2887867647059));
#153342=CARTESIAN_POINT('Ctrl Pts',(43.3760651419751,-26.8573224770441,
97.794669117647));
#153343=CARTESIAN_POINT('Ctrl Pts',(40.5392751458362,-30.6138395280662,
96.3005514705884));
#153344=CARTESIAN_POINT('Ctrl Pts',(37.7024851496972,-34.3703565790883,
94.8064338235295));
#153345=CARTESIAN_POINT('Ctrl Pts',(34.2237386972451,-37.5416529948095,
93.3123161764706));
#153346=CARTESIAN_POINT('Ctrl Pts',(30.744992244793,-40.7129494105307,91.8181985294118));
#153347=CARTESIAN_POINT('Ctrl Pts',(26.7427538741697,-43.1910304950644,
90.3240808823529));
#153348=CARTESIAN_POINT('Ctrl Pts',(22.7405155035463,-45.6691115795981,
88.8299632352943));
#153349=CARTESIAN_POINT('Ctrl Pts',(18.3510766423074,-47.3695892537413,
87.3358455882354));
#153350=CARTESIAN_POINT('Ctrl Pts',(13.9616377810684,-49.0700669278844,
85.8417279411765));
#153351=CARTESIAN_POINT('Ctrl Pts',(9.33447550508176,-49.9350334639422,
84.3476102941176));
#153352=CARTESIAN_POINT('Ctrl Pts',(4.70731322909511,-50.8,82.8534926470588));
#153353=CARTESIAN_POINT('Ctrl Pts',(0.,-50.8,81.3593750000001));
#153354=CARTESIAN_POINT('Ctrl Pts',(-4.70731322909511,-50.8,79.8652573529413));
#153355=CARTESIAN_POINT('Ctrl Pts',(-9.33447550508177,-49.9350334639422,
78.3711397058824));
#153356=CARTESIAN_POINT('Ctrl Pts',(-13.9616377810684,-49.0700669278844,
76.8770220588235));
#153357=CARTESIAN_POINT('Ctrl Pts',(-18.3510766423074,-47.3695892537413,
75.3829044117647));
#153358=CARTESIAN_POINT('Ctrl Pts',(-22.7405155035463,-45.6691115795981,
73.888786764706));
#153359=CARTESIAN_POINT('Ctrl Pts',(-26.7427538741697,-43.1910304950644,
72.3946691176471));
#153360=CARTESIAN_POINT('Ctrl Pts',(-30.744992244793,-40.7129494105307,
70.9005514705883));
#153361=CARTESIAN_POINT('Ctrl Pts',(-34.2237386972451,-37.5416529948095,
69.4064338235294));
#153362=CARTESIAN_POINT('Ctrl Pts',(-37.7024851496972,-34.3703565790883,
67.9123161764705));
#153363=CARTESIAN_POINT('Ctrl Pts',(-40.5392751458362,-30.6138395280662,
66.4181985294119));
#153364=CARTESIAN_POINT('Ctrl Pts',(-43.3760651419751,-26.8573224770441,
64.9240808823531));
#153365=CARTESIAN_POINT('Ctrl Pts',(-45.4742952008371,-22.6435084734481,
63.4299632352942));
#153366=CARTESIAN_POINT('Ctrl Pts',(-47.5725252596992,-18.4296944698521,
61.9358455882353));
#153367=CARTESIAN_POINT('Ctrl Pts',(-48.8607426731792,-13.9020798956618,
60.4417279411764));
#153368=CARTESIAN_POINT('Ctrl Pts',(-50.1489600866593,-9.37446532147148,
58.9476102941178));
#153369=CARTESIAN_POINT('Ctrl Pts',(-50.5832961557877,-4.68723266073574,
57.4534926470589));
#153370=CARTESIAN_POINT('Ctrl Pts',(-51.0176322249162,-3.12392900021603E-15,
55.9593750000001));
#153371=CARTESIAN_POINT('Ctrl Pts',(-50.5832961557877,4.68723266073573,
54.4652573529412));
#153372=CARTESIAN_POINT('Ctrl Pts',(-50.1489600866593,9.37446532147149,
52.9711397058823));
#153373=CARTESIAN_POINT('Ctrl Pts',(-48.8607426731792,13.9020798956618,
51.4770220588236));
#153374=CARTESIAN_POINT('Ctrl Pts',(-47.5725252596992,18.4296944698521,
49.9829044117648));
#153375=CARTESIAN_POINT('Ctrl Pts',(-45.4742952008371,22.6435084734481,
48.4887867647059));
#153376=CARTESIAN_POINT('Ctrl Pts',(-43.3760651419751,26.8573224770442,
46.994669117647));
#153377=CARTESIAN_POINT('Ctrl Pts',(-40.5392751458362,30.6138395280662,
45.5005514705882));
#153378=CARTESIAN_POINT('Ctrl Pts',(-37.7024851496972,34.3703565790883,
44.0064338235295));
#153379=CARTESIAN_POINT('Ctrl Pts',(-34.2237386972451,37.5416529948095,
42.5123161764707));
#153380=CARTESIAN_POINT('Ctrl Pts',(-30.744992244793,40.7129494105307,41.0181985294118));
#153381=CARTESIAN_POINT('Ctrl Pts',(-26.7427538741697,43.1910304950644,
39.5240808823529));
#153382=CARTESIAN_POINT('Ctrl Pts',(-22.7405155035463,45.6691115795981,
38.0299632352941));
#153383=CARTESIAN_POINT('Ctrl Pts',(-18.3510766423074,47.3695892537413,
36.5358455882354));
#153384=CARTESIAN_POINT('Ctrl Pts',(-13.9616377810684,49.0700669278844,
35.0417279411765));
#153385=CARTESIAN_POINT('Ctrl Pts',(-9.33447550508177,49.9350334639422,
33.5476102941177));
#153386=CARTESIAN_POINT('Ctrl Pts',(-4.7073132290951,50.8,32.0534926470588));
#153387=CARTESIAN_POINT('Ctrl Pts',(-6.22120573966855E-15,50.8,30.5593749999999));
#153388=CARTESIAN_POINT('Ctrl Pts',(4.70731322909511,50.8,29.0652573529413));
#153389=CARTESIAN_POINT('Ctrl Pts',(9.33447550508176,49.9350334639422,27.5711397058824));
#153390=CARTESIAN_POINT('Ctrl Pts',(13.9616377810684,49.0700669278844,26.0770220588236));
#153391=CARTESIAN_POINT('Ctrl Pts',(18.3510766423074,47.3695892537413,24.5829044117647));
#153392=CARTESIAN_POINT('Ctrl Pts',(22.7405155035463,45.6691115795981,23.0887867647058));
#153393=CARTESIAN_POINT('Ctrl Pts',(26.7427538741697,43.1910304950644,21.5946691176472));
#153394=CARTESIAN_POINT('Ctrl Pts',(30.744992244793,40.7129494105307,20.1005514705883));
#153395=CARTESIAN_POINT('Ctrl Pts',(34.2237386972451,37.5416529948095,18.6064338235294));
#153396=CARTESIAN_POINT('Ctrl Pts',(37.7024851496972,34.3703565790883,17.1123161764706));
#153397=CARTESIAN_POINT('Ctrl Pts',(40.5392751458362,30.6138395280662,15.6181985294117));
#153398=CARTESIAN_POINT('Ctrl Pts',(43.3760651419751,26.8573224770442,14.1240808823531));
#153399=CARTESIAN_POINT('Ctrl Pts',(45.4742952008372,22.6435084734481,12.6299632352942));
#153400=CARTESIAN_POINT('Ctrl Pts',(47.5725252596992,18.4296944698521,11.1358455882353));
#153401=CARTESIAN_POINT('Ctrl Pts',(48.8607426731792,13.9020798956618,9.64172794117646));
#153402=CARTESIAN_POINT('Ctrl Pts',(50.1489600866593,9.37446532147146,8.14761029411759));
#153403=CARTESIAN_POINT('Ctrl Pts',(50.5832961557877,4.68723266073574,6.65349264705895));
#153404=CARTESIAN_POINT('Ctrl Pts',(51.0176322249162,9.37178700064808E-15,
5.15937500000008));
#153405=CARTESIAN_POINT('Ctrl Pts',(50.5832961557877,-4.68723266073572,
3.66525735294121));
#153406=CARTESIAN_POINT('Ctrl Pts',(50.1489600866593,-9.37446532147149,
2.17113970588234));
#153407=CARTESIAN_POINT('Ctrl Pts',(48.8607426731792,-13.9020798956618,
0.677022058823473));
#153408=CARTESIAN_POINT('Ctrl Pts',(47.5725252596992,-18.4296944698521,
-0.817095588235173));
#153409=CARTESIAN_POINT('Ctrl Pts',(45.4742952008371,-22.6435084734482,
-2.31121323529404));
#153410=CARTESIAN_POINT('Ctrl Pts',(43.3760651419751,-26.8573224770441,
-3.80533088235291));
#153411=CARTESIAN_POINT('Ctrl Pts',(40.5392751458362,-30.6138395280662,
-5.29944852941178));
#153412=CARTESIAN_POINT('Ctrl Pts',(37.7024851496972,-34.3703565790883,
-6.79356617647064));
#153413=CARTESIAN_POINT('Ctrl Pts',(34.2237386972451,-37.5416529948095,
-8.28768382352929));
#153414=CARTESIAN_POINT('Ctrl Pts',(30.744992244793,-40.7129494105307,-9.78180147058816));
#153415=CARTESIAN_POINT('Ctrl Pts',(26.7427538741697,-43.1910304950644,
-11.275919117647));
#153416=CARTESIAN_POINT('Ctrl Pts',(22.7405155035463,-45.6691115795981,
-12.7700367647059));
#153417=CARTESIAN_POINT('Ctrl Pts',(18.3510766423074,-47.3695892537413,
-14.2641544117648));
#153418=CARTESIAN_POINT('Ctrl Pts',(13.9616377810684,-49.0700669278844,
-15.7582720588234));
#153419=CARTESIAN_POINT('Ctrl Pts',(9.33447550508176,-49.9350334639422,
-17.2523897058823));
#153420=CARTESIAN_POINT('Ctrl Pts',(4.70731322909511,-50.8,-18.7465073529412));
#153421=CARTESIAN_POINT('Ctrl Pts',(0.,-50.8,-20.240625));
#153422=CARTESIAN_POINT('Ctrl Pts',(-4.70731322909511,-50.8,-21.7347426470589));
#153423=CARTESIAN_POINT('Ctrl Pts',(-9.33447550508177,-49.9350334639422,
-23.2288602941175));
#153424=CARTESIAN_POINT('Ctrl Pts',(-13.9616377810684,-49.0700669278844,
-24.7229779411764));
#153425=CARTESIAN_POINT('Ctrl Pts',(-18.3510766423074,-47.3695892537413,
-26.2170955882353));
#153426=CARTESIAN_POINT('Ctrl Pts',(-22.7405155035463,-45.6691115795981,
-27.7112132352941));
#153427=CARTESIAN_POINT('Ctrl Pts',(-26.7427538741697,-43.1910304950644,
-29.205330882353));
#153428=CARTESIAN_POINT('Ctrl Pts',(-30.744992244793,-40.7129494105307,
-30.6994485294116));
#153429=CARTESIAN_POINT('Ctrl Pts',(-34.2237386972451,-37.5416529948095,
-32.1935661764705));
#153430=CARTESIAN_POINT('Ctrl Pts',(-37.7024851496972,-34.3703565790883,
-33.6876838235294));
#153431=CARTESIAN_POINT('Ctrl Pts',(-40.5392751458362,-30.6138395280662,
-35.1818014705882));
#153432=CARTESIAN_POINT('Ctrl Pts',(-43.3760651419751,-26.8573224770441,
-36.6759191176471));
#153433=CARTESIAN_POINT('Ctrl Pts',(-45.4742952008371,-22.6435084734481,
-38.1700367647058));
#153434=CARTESIAN_POINT('Ctrl Pts',(-47.5725252596992,-18.4296944698521,
-39.6641544117646));
#153435=CARTESIAN_POINT('Ctrl Pts',(-48.8607426731792,-13.9020798956618,
-41.1582720588235));
#153436=CARTESIAN_POINT('Ctrl Pts',(-50.1489600866593,-9.37446532147148,
-42.6523897058824));
#153437=CARTESIAN_POINT('Ctrl Pts',(-50.5832961557877,-4.68723266073574,
-44.1465073529412));
#153438=CARTESIAN_POINT('Ctrl Pts',(-51.0176322249162,-3.12392900021603E-15,
-45.6406249999999));
#153439=CARTESIAN_POINT('Ctrl Pts',(-50.5832961557877,4.68723266073573,
-47.1347426470587));
#153440=CARTESIAN_POINT('Ctrl Pts',(-50.1489600866593,9.37446532147149,
-48.6288602941176));
#153441=CARTESIAN_POINT('Ctrl Pts',(-48.8607426731792,13.9020798956618,
-50.1229779411765));
#153442=CARTESIAN_POINT('Ctrl Pts',(-47.5725252596992,18.4296944698521,
-51.6170955882354));
#153443=CARTESIAN_POINT('Ctrl Pts',(-45.4742952008371,22.6435084734481,
-53.111213235294));
#153444=CARTESIAN_POINT('Ctrl Pts',(-43.3760651419751,26.8573224770442,
-54.6053308823529));
#153445=CARTESIAN_POINT('Ctrl Pts',(-40.5392751458362,30.6138395280662,
-56.0994485294117));
#153446=CARTESIAN_POINT('Ctrl Pts',(-37.7024851496972,34.3703565790883,
-57.5935661764706));
#153447=CARTESIAN_POINT('Ctrl Pts',(-34.2237386972451,37.5416529948095,
-59.0876838235295));
#153448=CARTESIAN_POINT('Ctrl Pts',(-30.744992244793,40.7129494105307,-60.5818014705881));
#153449=CARTESIAN_POINT('Ctrl Pts',(-26.7427538741697,43.1910304950644,
-62.075919117647));
#153450=CARTESIAN_POINT('Ctrl Pts',(-22.7405155035463,45.6691115795981,
-63.5700367647058));
#153451=CARTESIAN_POINT('Ctrl Pts',(-18.3510766423074,47.3695892537413,
-65.0641544117647));
#153452=CARTESIAN_POINT('Ctrl Pts',(-13.9616377810684,49.0700669278844,
-66.5582720588236));
#153453=CARTESIAN_POINT('Ctrl Pts',(-9.33447550508177,49.9350334639422,
-68.0523897058822));
#153454=CARTESIAN_POINT('Ctrl Pts',(-4.7073132290951,50.8,-69.5465073529411));
#153455=CARTESIAN_POINT('Ctrl Pts',(-6.22120573966855E-15,50.8,-71.040625));
#153456=CARTESIAN_POINT('Ctrl Pts',(4.70731322909511,50.8,-72.5347426470588));
#153457=CARTESIAN_POINT('Ctrl Pts',(9.33447550508176,49.9350334639422,-74.0288602941177));
#153458=CARTESIAN_POINT('Ctrl Pts',(13.9616377810684,49.0700669278844,-75.5229779411764));
#153459=CARTESIAN_POINT('Ctrl Pts',(18.3510766423074,47.3695892537413,-77.0170955882352));
#153460=CARTESIAN_POINT('Ctrl Pts',(22.7405155035463,45.6691115795981,-78.5112132352941));
#153461=CARTESIAN_POINT('Ctrl Pts',(26.7427538741697,43.1910304950644,-80.005330882353));
#153462=CARTESIAN_POINT('Ctrl Pts',(30.744992244793,40.7129494105307,-81.4994485294118));
#153463=CARTESIAN_POINT('Ctrl Pts',(34.2237386972451,37.5416529948095,-82.9935661764705));
#153464=CARTESIAN_POINT('Ctrl Pts',(37.7024851496972,34.3703565790883,-84.4876838235294));
#153465=CARTESIAN_POINT('Ctrl Pts',(40.5392751458362,30.6138395280662,-85.9818014705882));
#153466=CARTESIAN_POINT('Ctrl Pts',(43.3760651419751,26.8573224770442,-87.4759191176471));
#153467=CARTESIAN_POINT('Ctrl Pts',(45.4742952008372,22.6435084734481,-88.970036764706));
#153468=CARTESIAN_POINT('Ctrl Pts',(47.5725252596992,18.4296944698521,-90.4641544117646));
#153469=CARTESIAN_POINT('Ctrl Pts',(48.8607426731792,13.9020798956618,-91.9582720588235));
#153470=CARTESIAN_POINT('Ctrl Pts',(50.1489600866593,9.37446532147146,-93.4523897058823));
#153471=CARTESIAN_POINT('Ctrl Pts',(50.5832961557877,4.68723266073574,-94.9465073529412));
#153472=CARTESIAN_POINT('Ctrl Pts',(51.0176322249162,9.37178700064808E-15,
-96.4406250000001));
#153473=CARTESIAN_POINT('Ctrl Pts',(50.5832961557877,-4.68723266073572,
-97.9347426470587));
#153474=CARTESIAN_POINT('Ctrl Pts',(50.1489600866593,-9.37446532147149,
-99.4288602941176));
#153475=CARTESIAN_POINT('Ctrl Pts',(48.8607426731792,-13.9020798956618,
-100.922977941176));
#153476=CARTESIAN_POINT('Ctrl Pts',(47.5725252596992,-18.4296944698521,
-102.417095588235));
#153477=CARTESIAN_POINT('Ctrl Pts',(45.4742952008371,-22.6435084734482,
-103.911213235294));
#153478=CARTESIAN_POINT('Ctrl Pts',(43.3760651419751,-26.8573224770441,
-105.405330882353));
#153479=CARTESIAN_POINT('Ctrl Pts',(40.5392751458362,-30.6138395280662,
-106.899448529412));
#153480=CARTESIAN_POINT('Ctrl Pts',(37.7024851496972,-34.3703565790883,
-108.393566176471));
#153481=CARTESIAN_POINT('Ctrl Pts',(34.2237386972451,-37.5416529948095,
-109.887683823529));
#153482=CARTESIAN_POINT('Ctrl Pts',(30.744992244793,-40.7129494105307,-111.381801470588));
#153483=CARTESIAN_POINT('Ctrl Pts',(26.7427538741697,-43.1910304950644,
-112.875919117647));
#153484=CARTESIAN_POINT('Ctrl Pts',(22.7405155035463,-45.6691115795981,
-114.370036764706));
#153485=CARTESIAN_POINT('Ctrl Pts',(18.3510766423074,-47.3695892537413,
-115.864154411765));
#153486=CARTESIAN_POINT('Ctrl Pts',(13.9616377810684,-49.0700669278844,
-117.358272058824));
#153487=CARTESIAN_POINT('Ctrl Pts',(9.33447550508176,-49.9350334639422,
-118.852389705882));
#153488=CARTESIAN_POINT('Ctrl Pts',(4.70731322909511,-50.8,-120.346507352941));
#153489=CARTESIAN_POINT('Ctrl Pts',(0.,-50.8,-121.840625));
#153490=CARTESIAN_POINT('Ctrl Pts',(-4.70731322909511,-50.8,-123.334742647059));
#153491=CARTESIAN_POINT('Ctrl Pts',(-9.33447550508177,-49.9350334639422,
-124.828860294118));
#153492=CARTESIAN_POINT('Ctrl Pts',(-13.9616377810684,-49.0700669278844,
-126.322977941177));
#153493=CARTESIAN_POINT('Ctrl Pts',(-18.3510766423074,-47.3695892537413,
-127.817095588235));
#153494=CARTESIAN_POINT('Ctrl Pts',(-22.7405155035463,-45.6691115795981,
-129.311213235294));
#153495=CARTESIAN_POINT('Ctrl Pts',(-26.7427538741697,-43.1910304950644,
-130.805330882353));
#153496=CARTESIAN_POINT('Ctrl Pts',(-30.744992244793,-40.7129494105307,
-132.299448529412));
#153497=CARTESIAN_POINT('Ctrl Pts',(-34.2237386972451,-37.5416529948095,
-133.793566176471));
#153498=CARTESIAN_POINT('Ctrl Pts',(-37.7024851496972,-34.3703565790883,
-135.287683823529));
#153499=CARTESIAN_POINT('Ctrl Pts',(-40.5392751458362,-30.6138395280662,
-136.781801470588));
#153500=CARTESIAN_POINT('Ctrl Pts',(-43.3760651419751,-26.8573224770441,
-138.275919117647));
#153501=CARTESIAN_POINT('Ctrl Pts',(-45.4742952008371,-22.6435084734481,
-139.770036764706));
#153502=CARTESIAN_POINT('Ctrl Pts',(-47.5725252596992,-18.4296944698521,
-141.264154411765));
#153503=CARTESIAN_POINT('Ctrl Pts',(-48.8607426731792,-13.9020798956618,
-142.758272058823));
#153504=CARTESIAN_POINT('Ctrl Pts',(-50.1489600866593,-9.37446532147148,
-144.252389705882));
#153505=CARTESIAN_POINT('Ctrl Pts',(-50.5832961557877,-4.68723266073574,
-145.746507352941));
#153506=CARTESIAN_POINT('Ctrl Pts',(-51.0176322249162,-3.12392900021603E-15,
-147.240625));
#153507=CARTESIAN_POINT('Ctrl Pts',(-50.5832961557877,4.68723266073573,
-148.734742647059));
#153508=CARTESIAN_POINT('Ctrl Pts',(-50.1489600866593,9.37446532147149,
-150.228860294118));
#153509=CARTESIAN_POINT('Ctrl Pts',(-48.8607426731792,13.9020798956618,
-151.722977941176));
#153510=CARTESIAN_POINT('Ctrl Pts',(-47.5725252596992,18.4296944698521,
-153.217095588235));
#153511=CARTESIAN_POINT('Ctrl Pts',(-45.4742952008371,22.6435084734481,
-154.711213235294));
#153512=CARTESIAN_POINT('Ctrl Pts',(-43.3760651419751,26.8573224770442,
-156.205330882353));
#153513=CARTESIAN_POINT('Ctrl Pts',(-40.5392751458362,30.6138395280662,
-157.699448529412));
#153514=CARTESIAN_POINT('Ctrl Pts',(-37.7024851496972,34.3703565790883,
-159.193566176471));
#153515=CARTESIAN_POINT('Ctrl Pts',(-34.2237386972451,37.5416529948095,
-160.687683823529));
#153516=CARTESIAN_POINT('Ctrl Pts',(-30.744992244793,40.7129494105307,-162.181801470588));
#153517=CARTESIAN_POINT('Ctrl Pts',(-26.7427538741697,43.1910304950644,
-163.675919117647));
#153518=CARTESIAN_POINT('Ctrl Pts',(-22.7405155035463,45.6691115795981,
-165.170036764706));
#153519=CARTESIAN_POINT('Ctrl Pts',(-18.3510766423074,47.3695892537413,
-166.664154411765));
#153520=CARTESIAN_POINT('Ctrl Pts',(-13.9616377810684,49.0700669278844,
-168.158272058824));
#153521=CARTESIAN_POINT('Ctrl Pts',(-9.33447550508177,49.9350334639422,
-169.652389705882));
#153522=CARTESIAN_POINT('Ctrl Pts',(-4.7073132290951,50.8,-171.146507352941));
#153523=CARTESIAN_POINT('Ctrl Pts',(-6.22120573966855E-15,50.8,-172.640625));
#153524=CARTESIAN_POINT('Ctrl Pts',(4.70731322909511,50.8,-174.134742647059));
#153525=CARTESIAN_POINT('Ctrl Pts',(9.33447550508176,49.9350334639422,-175.628860294118));
#153526=CARTESIAN_POINT('Ctrl Pts',(13.9616377810684,49.0700669278844,-177.122977941176));
#153527=CARTESIAN_POINT('Ctrl Pts',(18.3510766423074,47.3695892537413,-178.617095588235));
#153528=CARTESIAN_POINT('Ctrl Pts',(22.7405155035463,45.6691115795981,-180.111213235294));
#153529=CARTESIAN_POINT('Ctrl Pts',(26.7427538741697,43.1910304950644,-181.605330882353));
#153530=CARTESIAN_POINT('Ctrl Pts',(30.744992244793,40.7129494105307,-183.099448529412));
#153531=CARTESIAN_POINT('Ctrl Pts',(34.2237386972451,37.5416529948095,-184.593566176471));
#153532=CARTESIAN_POINT('Ctrl Pts',(37.7024851496972,34.3703565790883,-186.087683823529));
#153533=CARTESIAN_POINT('Ctrl Pts',(40.5392751458362,30.6138395280662,-187.581801470588));
#153534=CARTESIAN_POINT('Ctrl Pts',(43.3760651419751,26.8573224770442,-189.075919117647));
#153535=CARTESIAN_POINT('Ctrl Pts',(45.4742952008372,22.6435084734481,-190.570036764706));
#153536=CARTESIAN_POINT('Ctrl Pts',(47.5725252596992,18.4296944698521,-192.064154411765));
#153537=CARTESIAN_POINT('Ctrl Pts',(48.8607426731792,13.9020798956618,-193.558272058824));
#153538=CARTESIAN_POINT('Ctrl Pts',(50.1489600866593,9.37446532147146,-195.052389705882));
#153539=CARTESIAN_POINT('Ctrl Pts',(50.5832961557877,4.68723266073574,-196.546507352941));
#153540=CARTESIAN_POINT('Ctrl Pts',(51.0176322249162,9.37178700064808E-15,
-198.040625));
#153541=CARTESIAN_POINT('Ctrl Pts',(50.5832961557877,-4.68723266073572,
-199.534742647059));
#153542=CARTESIAN_POINT('Ctrl Pts',(50.1489600866593,-9.37446532147149,
-201.028860294118));
#153543=CARTESIAN_POINT('Ctrl Pts',(48.8607426731792,-13.9020798956618,
-202.522977941176));
#153544=CARTESIAN_POINT('Ctrl Pts',(47.5725252596992,-18.4296944698521,
-204.017095588235));
#153545=CARTESIAN_POINT('Ctrl Pts',(45.4742952008371,-22.6435084734482,
-205.511213235294));
#153546=CARTESIAN_POINT('Ctrl Pts',(43.3760651419751,-26.8573224770441,
-207.005330882353));
#153547=CARTESIAN_POINT('Ctrl Pts',(40.5392751458362,-30.6138395280662,
-208.499448529412));
#153548=CARTESIAN_POINT('Ctrl Pts',(37.7024851496972,-34.3703565790883,
-209.99356617647));
#153549=CARTESIAN_POINT('Ctrl Pts',(34.2237386972451,-37.5416529948095,
-211.487683823529));
#153550=CARTESIAN_POINT('Ctrl Pts',(30.744992244793,-40.7129494105307,-212.981801470588));
#153551=CARTESIAN_POINT('Ctrl Pts',(26.7427538741697,-43.1910304950644,
-214.475919117647));
#153552=CARTESIAN_POINT('Ctrl Pts',(22.7405155035463,-45.6691115795981,
-215.970036764706));
#153553=CARTESIAN_POINT('Ctrl Pts',(18.3510766423074,-47.3695892537413,
-217.464154411765));
#153554=CARTESIAN_POINT('Ctrl Pts',(13.9616377810684,-49.0700669278844,
-218.958272058824));
#153555=CARTESIAN_POINT('Ctrl Pts',(9.33447550508176,-49.9350334639422,
-220.452389705882));
#153556=CARTESIAN_POINT('Ctrl Pts',(4.70731322909511,-50.8,-221.946507352941));
#153557=CARTESIAN_POINT('Ctrl Pts',(0.,-50.8,-223.440625));
#153558=CARTESIAN_POINT('Ctrl Pts',(-4.70731322909511,-50.8,-224.934742647059));
#153559=CARTESIAN_POINT('Ctrl Pts',(-9.33447550508177,-49.9350334639422,
-226.428860294118));
#153560=CARTESIAN_POINT('Ctrl Pts',(-13.9616377810684,-49.0700669278844,
-227.922977941176));
#153561=CARTESIAN_POINT('Ctrl Pts',(-18.3510766423074,-47.3695892537413,
-229.417095588235));
#153562=CARTESIAN_POINT('Ctrl Pts',(-22.7405155035463,-45.6691115795981,
-230.911213235294));
#153563=CARTESIAN_POINT('Ctrl Pts',(-26.7427538741697,-43.1910304950644,
-232.405330882353));
#153564=CARTESIAN_POINT('Ctrl Pts',(-30.744992244793,-40.7129494105307,
-233.899448529412));
#153565=CARTESIAN_POINT('Ctrl Pts',(-34.2237386972451,-37.5416529948095,
-235.393566176471));
#153566=CARTESIAN_POINT('Ctrl Pts',(-37.7024851496972,-34.3703565790883,
-236.887683823529));
#153567=CARTESIAN_POINT('Ctrl Pts',(-40.5392751458362,-30.6138395280662,
-238.381801470588));
#153568=CARTESIAN_POINT('Ctrl Pts',(-43.3760651419751,-26.8573224770441,
-239.875919117647));
#153569=CARTESIAN_POINT('Ctrl Pts',(-45.4742952008371,-22.6435084734481,
-241.370036764706));
#153570=CARTESIAN_POINT('Ctrl Pts',(-47.5725252596992,-18.4296944698521,
-242.864154411765));
#153571=CARTESIAN_POINT('Ctrl Pts',(-48.8607426731792,-13.9020798956618,
-244.358272058824));
#153572=CARTESIAN_POINT('Ctrl Pts',(-50.1489600866593,-9.37446532147148,
-245.852389705882));
#153573=CARTESIAN_POINT('Ctrl Pts',(-50.5832961557877,-4.68723266073574,
-247.346507352941));
#153574=CARTESIAN_POINT('Ctrl Pts',(-51.0176322249162,-3.12392900021603E-15,
-248.840625));
#153575=CARTESIAN_POINT('Ctrl Pts',(-50.5832961557877,4.68723266073573,
-250.334742647059));
#153576=CARTESIAN_POINT('Ctrl Pts',(-50.1489600866593,9.37446532147149,
-251.828860294118));
#153577=CARTESIAN_POINT('Ctrl Pts',(-48.8607426731792,13.9020798956618,
-253.322977941177));
#153578=CARTESIAN_POINT('Ctrl Pts',(-47.5725252596992,18.4296944698521,
-254.817095588235));
#153579=CARTESIAN_POINT('Ctrl Pts',(-45.4742952008371,22.6435084734481,
-256.311213235294));
#153580=CARTESIAN_POINT('Ctrl Pts',(-43.3760651419751,26.8573224770442,
-257.805330882353));
#153581=CARTESIAN_POINT('Ctrl Pts',(-40.5392751458362,30.6138395280662,
-259.299448529412));
#153582=CARTESIAN_POINT('Ctrl Pts',(-37.7024851496972,34.3703565790883,
-260.793566176471));
#153583=CARTESIAN_POINT('Ctrl Pts',(-34.2237386972451,37.5416529948095,
-262.287683823529));
#153584=CARTESIAN_POINT('Ctrl Pts',(-30.744992244793,40.7129494105307,-263.781801470588));
#153585=CARTESIAN_POINT('Ctrl Pts',(-26.7427538741697,43.1910304950644,
-265.275919117647));
#153586=CARTESIAN_POINT('Ctrl Pts',(-22.7405155035463,45.6691115795981,
-266.770036764706));
#153587=CARTESIAN_POINT('Ctrl Pts',(-18.3510766423074,47.3695892537413,
-268.264154411765));
#153588=CARTESIAN_POINT('Ctrl Pts',(-13.9616377810684,49.0700669278844,
-269.758272058823));
#153589=CARTESIAN_POINT('Ctrl Pts',(-9.33447550508177,49.9350334639422,
-271.252389705882));
#153590=CARTESIAN_POINT('Ctrl Pts',(-4.7073132290951,50.8,-272.746507352941));
#153591=CARTESIAN_POINT('Ctrl Pts',(-6.22120573966855E-15,50.8,-274.240625));
#153592=CARTESIAN_POINT('Ctrl Pts',(4.70731322909511,50.8,-275.734742647059));
#153593=CARTESIAN_POINT('Ctrl Pts',(9.33447550508176,49.9350334639422,-277.228860294118));
#153594=CARTESIAN_POINT('Ctrl Pts',(13.9616377810684,49.0700669278844,-278.722977941176));
#153595=CARTESIAN_POINT('Ctrl Pts',(18.3510766423074,47.3695892537413,-280.217095588235));
#153596=CARTESIAN_POINT('Ctrl Pts',(22.7405155035463,45.6691115795981,-281.711213235294));
#153597=CARTESIAN_POINT('Ctrl Pts',(26.7427538741697,43.1910304950644,-283.205330882353));
#153598=CARTESIAN_POINT('Ctrl Pts',(30.744992244793,40.7129494105307,-284.699448529412));
#153599=CARTESIAN_POINT('Ctrl Pts',(34.2237386972451,37.5416529948095,-286.193566176471));
#153600=CARTESIAN_POINT('Ctrl Pts',(37.7024851496972,34.3703565790883,-287.687683823529));
#153601=CARTESIAN_POINT('Ctrl Pts',(40.5392751458362,30.6138395280662,-289.181801470588));
#153602=CARTESIAN_POINT('Ctrl Pts',(43.3760651419751,26.8573224770442,-290.675919117647));
#153603=CARTESIAN_POINT('Ctrl Pts',(45.4742952008372,22.6435084734481,-292.170036764706));
#153604=CARTESIAN_POINT('Ctrl Pts',(47.5725252596992,18.4296944698521,-293.664154411765));
#153605=CARTESIAN_POINT('Ctrl Pts',(48.8607426731792,13.9020798956618,-295.158272058824));
#153606=CARTESIAN_POINT('Ctrl Pts',(50.1489600866593,9.37446532147146,-296.652389705882));
#153607=CARTESIAN_POINT('Ctrl Pts',(50.5832961557877,4.68723266073574,-298.146507352941));
#153608=CARTESIAN_POINT('Ctrl Pts',(51.0176322249162,9.37178700064808E-15,
-299.640625));
#153609=CARTESIAN_POINT('Ctrl Pts',(50.5832961557877,-4.68723266073572,
-301.134742647059));
#153610=CARTESIAN_POINT('Ctrl Pts',(50.1489600866593,-9.37446532147149,
-302.628860294118));
#153611=CARTESIAN_POINT('Ctrl Pts',(48.8607426731792,-13.9020798956618,
-304.122977941176));
#153612=CARTESIAN_POINT('Ctrl Pts',(47.5725252596992,-18.4296944698521,
-305.617095588235));
#153613=CARTESIAN_POINT('Ctrl Pts',(45.4742952008371,-22.6435084734482,
-307.111213235294));
#153614=CARTESIAN_POINT('Ctrl Pts',(43.3760651419751,-26.8573224770441,
-308.605330882353));
#153615=CARTESIAN_POINT('Ctrl Pts',(40.5392751458362,-30.6138395280662,
-310.099448529412));
#153616=CARTESIAN_POINT('Ctrl Pts',(37.7024851496972,-34.3703565790883,
-311.593566176471));
#153617=CARTESIAN_POINT('Ctrl Pts',(34.2237386972451,-37.5416529948095,
-313.087683823529));
#153618=CARTESIAN_POINT('Ctrl Pts',(30.744992244793,-40.7129494105307,-314.581801470588));
#153619=CARTESIAN_POINT('Ctrl Pts',(26.7427538741697,-43.1910304950644,
-316.075919117647));
#153620=CARTESIAN_POINT('Ctrl Pts',(22.7405155035463,-45.6691115795981,
-317.570036764706));
#153621=CARTESIAN_POINT('Ctrl Pts',(18.3510766423074,-47.3695892537413,
-319.064154411765));
#153622=CARTESIAN_POINT('Ctrl Pts',(13.9616377810684,-49.0700669278844,
-320.558272058824));
#153623=CARTESIAN_POINT('Ctrl Pts',(9.33447550508176,-49.9350334639422,
-322.052389705882));
#153624=CARTESIAN_POINT('Ctrl Pts',(4.70731322909511,-50.8,-323.546507352941));
#153625=CARTESIAN_POINT('Ctrl Pts',(0.,-50.8,-325.040625));
#153626=CARTESIAN_POINT('Ctrl Pts',(-4.70731322909511,-50.8,-326.534742647059));
#153627=CARTESIAN_POINT('Ctrl Pts',(-9.33447550508177,-49.9350334639422,
-328.028860294118));
#153628=CARTESIAN_POINT('Ctrl Pts',(-13.9616377810684,-49.0700669278844,
-329.522977941176));
#153629=CARTESIAN_POINT('Ctrl Pts',(-18.3510766423074,-47.3695892537413,
-331.017095588235));
#153630=CARTESIAN_POINT('Ctrl Pts',(-22.7405155035463,-45.6691115795981,
-332.511213235294));
#153631=CARTESIAN_POINT('Ctrl Pts',(-26.7427538741697,-43.1910304950644,
-334.005330882353));
#153632=CARTESIAN_POINT('Ctrl Pts',(-30.744992244793,-40.7129494105307,
-335.499448529412));
#153633=CARTESIAN_POINT('Ctrl Pts',(-34.2237386972451,-37.5416529948095,
-336.99356617647));
#153634=CARTESIAN_POINT('Ctrl Pts',(-37.7024851496972,-34.3703565790883,
-338.487683823529));
#153635=CARTESIAN_POINT('Ctrl Pts',(-40.5392751458362,-30.6138395280662,
-339.981801470588));
#153636=CARTESIAN_POINT('Ctrl Pts',(-43.3760651419751,-26.8573224770441,
-341.475919117647));
#153637=CARTESIAN_POINT('Ctrl Pts',(-45.4742952008371,-22.6435084734481,
-342.970036764706));
#153638=CARTESIAN_POINT('Ctrl Pts',(-47.5725252596992,-18.4296944698521,
-344.464154411765));
#153639=CARTESIAN_POINT('Ctrl Pts',(-48.8607426731792,-13.9020798956618,
-345.958272058824));
#153640=CARTESIAN_POINT('Ctrl Pts',(-50.1489600866593,-9.37446532147148,
-347.452389705882));
#153641=CARTESIAN_POINT('Ctrl Pts',(-50.5832961557877,-4.68723266073574,
-348.946507352941));
#153642=CARTESIAN_POINT('Ctrl Pts',(-51.0176322249162,-3.12392900021603E-15,
-350.440625));
#153643=CARTESIAN_POINT('Ctrl Pts',(-50.5832961557877,4.68723266073573,
-351.934742647059));
#153644=CARTESIAN_POINT('Ctrl Pts',(-50.1489600866593,9.37446532147149,
-353.428860294118));
#153645=CARTESIAN_POINT('Ctrl Pts',(-48.8607426731792,13.9020798956618,
-354.922977941176));
#153646=CARTESIAN_POINT('Ctrl Pts',(-47.5725252596992,18.4296944698521,
-356.417095588235));
#153647=CARTESIAN_POINT('Ctrl Pts',(-45.4742952008371,22.6435084734481,
-357.911213235294));
#153648=CARTESIAN_POINT('Ctrl Pts',(-43.3760651419751,26.8573224770442,
-359.405330882353));
#153649=CARTESIAN_POINT('Ctrl Pts',(-40.5392751458362,30.6138395280662,
-360.899448529412));
#153650=CARTESIAN_POINT('Ctrl Pts',(-37.7024851496972,34.3703565790883,
-362.393566176471));
#153651=CARTESIAN_POINT('Ctrl Pts',(-34.2237386972451,37.5416529948095,
-363.887683823529));
#153652=CARTESIAN_POINT('Ctrl Pts',(-30.744992244793,40.7129494105307,-365.381801470588));
#153653=CARTESIAN_POINT('Ctrl Pts',(-26.7427538741697,43.1910304950644,
-366.875919117647));
#153654=CARTESIAN_POINT('Ctrl Pts',(-22.7405155035463,45.6691115795981,
-368.370036764706));
#153655=CARTESIAN_POINT('Ctrl Pts',(-18.3510766423074,47.3695892537413,
-369.864154411765));
#153656=CARTESIAN_POINT('Ctrl Pts',(-13.9616377810684,49.0700669278844,
-371.358272058824));
#153657=CARTESIAN_POINT('Ctrl Pts',(-9.33447550508177,49.9350334639422,
-372.852389705882));
#153658=CARTESIAN_POINT('Ctrl Pts',(-4.7073132290951,50.8,-374.346507352941));
#153659=CARTESIAN_POINT('Ctrl Pts',(-6.22120573966855E-15,50.8,-375.840625));
#153660=CARTESIAN_POINT('Ctrl Pts',(4.70731322909511,50.8,-377.334742647059));
#153661=CARTESIAN_POINT('Ctrl Pts',(9.33447550508176,49.9350334639422,-378.828860294118));
#153662=CARTESIAN_POINT('Ctrl Pts',(13.9616377810684,49.0700669278844,-380.322977941177));
#153663=CARTESIAN_POINT('Ctrl Pts',(18.3510766423074,47.3695892537413,-381.817095588235));
#153664=CARTESIAN_POINT('Ctrl Pts',(22.7405155035463,45.6691115795981,-383.311213235294));
#153665=CARTESIAN_POINT('Ctrl Pts',(26.7427538741697,43.1910304950644,-384.805330882353));
#153666=CARTESIAN_POINT('Ctrl Pts',(30.744992244793,40.7129494105307,-386.299448529412));
#153667=CARTESIAN_POINT('Ctrl Pts',(34.2237386972451,37.5416529948095,-387.793566176471));
#153668=CARTESIAN_POINT('Ctrl Pts',(37.7024851496972,34.3703565790883,-389.287683823529));
#153669=CARTESIAN_POINT('Ctrl Pts',(40.5392751458362,30.6138395280662,-390.781801470588));
#153670=CARTESIAN_POINT('Ctrl Pts',(43.3760651419751,26.8573224770442,-392.275919117647));
#153671=CARTESIAN_POINT('Ctrl Pts',(45.4742952008372,22.6435084734481,-393.770036764706));
#153672=CARTESIAN_POINT('Ctrl Pts',(47.5725252596992,18.4296944698521,-395.264154411765));
#153673=CARTESIAN_POINT('Ctrl Pts',(48.8607426731792,13.9020798956618,-396.758272058823));
#153674=CARTESIAN_POINT('Ctrl Pts',(50.1489600866593,9.37446532147146,-398.252389705882));
#153675=CARTESIAN_POINT('Ctrl Pts',(50.5832961557877,4.68723266073574,-399.746507352941));
#153676=CARTESIAN_POINT('Ctrl Pts',(51.0176322249162,9.37178700064808E-15,
-401.240625));
#153677=CARTESIAN_POINT('Ctrl Pts',(50.5832961557877,-4.68723266073572,
-402.734742647059));
#153678=CARTESIAN_POINT('Ctrl Pts',(50.1489600866593,-9.37446532147149,
-404.228860294118));
#153679=CARTESIAN_POINT('Ctrl Pts',(48.8607426731792,-13.9020798956618,
-405.722977941176));
#153680=CARTESIAN_POINT('Ctrl Pts',(47.5725252596992,-18.4296944698521,
-407.217095588235));
#153681=CARTESIAN_POINT('Ctrl Pts',(45.4742952008371,-22.6435084734482,
-408.711213235294));
#153682=CARTESIAN_POINT('Ctrl Pts',(43.3760651419751,-26.8573224770441,
-410.205330882353));
#153683=CARTESIAN_POINT('Ctrl Pts',(40.5392751458362,-30.6138395280662,
-411.699448529412));
#153684=CARTESIAN_POINT('Ctrl Pts',(37.7024851496972,-34.3703565790883,
-413.193566176471));
#153685=CARTESIAN_POINT('Ctrl Pts',(34.2237386972451,-37.5416529948095,
-414.687683823529));
#153686=CARTESIAN_POINT('Ctrl Pts',(30.744992244793,-40.7129494105307,-416.181801470588));
#153687=CARTESIAN_POINT('Ctrl Pts',(26.7427538741697,-43.1910304950644,
-417.675919117647));
#153688=CARTESIAN_POINT('Ctrl Pts',(22.7405155035463,-45.6691115795981,
-419.170036764706));
#153689=CARTESIAN_POINT('Ctrl Pts',(18.3510766423074,-47.3695892537413,
-420.664154411765));
#153690=CARTESIAN_POINT('Ctrl Pts',(13.9616377810684,-49.0700669278844,
-422.158272058824));
#153691=CARTESIAN_POINT('Ctrl Pts',(9.33447550508176,-49.9350334639422,
-423.652389705882));
#153692=CARTESIAN_POINT('Ctrl Pts',(4.70731322909511,-50.8,-425.146507352941));
#153693=CARTESIAN_POINT('Ctrl Pts',(0.,-50.8,-426.640625));
#153694=CARTESIAN_POINT('Ctrl Pts',(-4.70731322909511,-50.8,-428.134742647059));
#153695=CARTESIAN_POINT('Ctrl Pts',(-9.33447550508177,-49.9350334639422,
-429.628860294118));
#153696=CARTESIAN_POINT('Ctrl Pts',(-13.9616377810684,-49.0700669278844,
-431.122977941177));
#153697=CARTESIAN_POINT('Ctrl Pts',(-18.3510766423074,-47.3695892537413,
-432.617095588235));
#153698=CARTESIAN_POINT('Ctrl Pts',(-22.7405155035463,-45.6691115795981,
-434.111213235294));
#153699=CARTESIAN_POINT('Ctrl Pts',(-26.7427538741697,-43.1910304950644,
-435.605330882353));
#153700=CARTESIAN_POINT('Ctrl Pts',(-30.744992244793,-40.7129494105307,
-437.099448529412));
#153701=CARTESIAN_POINT('Ctrl Pts',(-34.2237386972451,-37.5416529948095,
-438.593566176471));
#153702=CARTESIAN_POINT('Ctrl Pts',(-37.7024851496972,-34.3703565790883,
-440.087683823529));
#153703=CARTESIAN_POINT('Ctrl Pts',(-40.5392751458362,-30.6138395280662,
-441.581801470588));
#153704=CARTESIAN_POINT('Ctrl Pts',(-43.3760651419751,-26.8573224770441,
-443.075919117647));
#153705=CARTESIAN_POINT('Ctrl Pts',(-45.4742952008371,-22.6435084734481,
-444.570036764706));
#153706=CARTESIAN_POINT('Ctrl Pts',(-47.5725252596992,-18.4296944698521,
-446.064154411765));
#153707=CARTESIAN_POINT('Ctrl Pts',(-48.8607426731792,-13.9020798956618,
-447.558272058824));
#153708=CARTESIAN_POINT('Ctrl Pts',(-50.1489600866593,-9.37446532147148,
-449.052389705882));
#153709=CARTESIAN_POINT('Ctrl Pts',(-50.5832961557877,-4.68723266073574,
-450.546507352941));
#153710=CARTESIAN_POINT('Ctrl Pts',(-51.0176322249162,-3.12392900021603E-15,
-452.040625));
#153711=CARTESIAN_POINT('Ctrl Pts',(-50.5832961557877,4.68723266073573,
-453.534742647059));
#153712=CARTESIAN_POINT('Ctrl Pts',(-50.1489600866593,9.37446532147149,
-455.028860294118));
#153713=CARTESIAN_POINT('Ctrl Pts',(-48.8607426731792,13.9020798956618,
-456.522977941176));
#153714=CARTESIAN_POINT('Ctrl Pts',(-47.5725252596992,18.4296944698521,
-458.017095588235));
#153715=CARTESIAN_POINT('Ctrl Pts',(-45.4742952008371,22.6435084734481,
-459.511213235294));
#153716=CARTESIAN_POINT('Ctrl Pts',(-43.3760651419751,26.8573224770442,
-461.005330882353));
#153717=CARTESIAN_POINT('Ctrl Pts',(-40.5392751458362,30.6138395280662,
-462.499448529412));
#153718=CARTESIAN_POINT('Ctrl Pts',(-37.7024851496972,34.3703565790883,
-463.993566176471));
#153719=CARTESIAN_POINT('Ctrl Pts',(-34.2237386972451,37.5416529948095,
-465.487683823529));
#153720=CARTESIAN_POINT('Ctrl Pts',(-30.744992244793,40.7129494105307,-466.981801470588));
#153721=CARTESIAN_POINT('Ctrl Pts',(-26.7427538741697,43.1910304950644,
-468.475919117647));
#153722=CARTESIAN_POINT('Ctrl Pts',(-22.7405155035463,45.6691115795981,
-469.970036764706));
#153723=CARTESIAN_POINT('Ctrl Pts',(-18.3510766423074,47.3695892537413,
-471.464154411765));
#153724=CARTESIAN_POINT('Ctrl Pts',(-13.9616377810684,49.0700669278844,
-472.958272058823));
#153725=CARTESIAN_POINT('Ctrl Pts',(-9.33447550508177,49.9350334639422,
-474.452389705882));
#153726=CARTESIAN_POINT('Ctrl Pts',(-4.7073132290951,50.8,-475.946507352941));
#153727=CARTESIAN_POINT('Ctrl Pts',(-6.22120573966855E-15,50.8,-477.440625));
#153728=CARTESIAN_POINT('Ctrl Pts',(4.70731322909511,50.8,-478.934742647059));
#153729=CARTESIAN_POINT('Ctrl Pts',(9.33447550508176,49.9350334639422,-480.428860294118));
#153730=CARTESIAN_POINT('Ctrl Pts',(13.9616377810684,49.0700669278844,-481.922977941177));
#153731=CARTESIAN_POINT('Ctrl Pts',(18.3510766423074,47.3695892537413,-483.417095588235));
#153732=CARTESIAN_POINT('Ctrl Pts',(22.7405155035463,45.6691115795981,-484.911213235294));
#153733=CARTESIAN_POINT('Ctrl Pts',(26.7427538741697,43.1910304950644,-486.405330882353));
#153734=CARTESIAN_POINT('Ctrl Pts',(30.744992244793,40.7129494105307,-487.899448529412));
#153735=CARTESIAN_POINT('Ctrl Pts',(34.2237386972451,37.5416529948095,-489.393566176471));
#153736=CARTESIAN_POINT('Ctrl Pts',(37.7024851496972,34.3703565790883,-490.88768382353));
#153737=CARTESIAN_POINT('Ctrl Pts',(40.5392751458362,30.6138395280662,-492.381801470588));
#153738=CARTESIAN_POINT('Ctrl Pts',(43.3760651419751,26.8573224770442,-493.875919117647));
#153739=CARTESIAN_POINT('Ctrl Pts',(45.4742952008372,22.6435084734481,-495.370036764706));
#153740=CARTESIAN_POINT('Ctrl Pts',(47.5725252596992,18.4296944698521,-496.864154411765));
#153741=CARTESIAN_POINT('Ctrl Pts',(48.8607426731792,13.9020798956618,-498.358272058824));
#153742=CARTESIAN_POINT('Ctrl Pts',(50.1489600866593,9.37446532147146,-499.852389705883));
#153743=CARTESIAN_POINT('Ctrl Pts',(50.5832961557877,4.68723266073574,-501.346507352941));
#153744=CARTESIAN_POINT('Ctrl Pts',(51.0176322249162,9.37178700064808E-15,
-502.840625));
#153745=CARTESIAN_POINT('Ctrl Pts',(50.5832961557877,-4.68723266073572,
-504.334742647059));
#153746=CARTESIAN_POINT('Ctrl Pts',(50.1489600866593,-9.37446532147149,
-505.828860294118));
#153747=CARTESIAN_POINT('Ctrl Pts',(48.8607426731792,-13.9020798956618,
-507.322977941176));
#153748=CARTESIAN_POINT('Ctrl Pts',(47.5725252596992,-18.4296944698521,
-508.817095588235));
#153749=CARTESIAN_POINT('Ctrl Pts',(45.4742952008371,-22.6435084734482,
-510.311213235294));
#153750=CARTESIAN_POINT('Ctrl Pts',(43.3760651419751,-26.8573224770441,
-511.805330882353));
#153751=CARTESIAN_POINT('Ctrl Pts',(40.5392751458362,-30.6138395280662,
-513.299448529412));
#153752=CARTESIAN_POINT('Ctrl Pts',(37.7024851496972,-34.3703565790883,
-514.793566176471));
#153753=CARTESIAN_POINT('Ctrl Pts',(34.2237386972451,-37.5416529948095,
-516.28768382353));
#153754=CARTESIAN_POINT('Ctrl Pts',(30.744992244793,-40.7129494105307,-517.781801470588));
#153755=CARTESIAN_POINT('Ctrl Pts',(26.7427538741697,-43.1910304950644,
-519.275919117647));
#153756=CARTESIAN_POINT('Ctrl Pts',(22.7405155035463,-45.6691115795981,
-520.770036764706));
#153757=CARTESIAN_POINT('Ctrl Pts',(18.3510766423074,-47.3695892537413,
-522.264154411765));
#153758=CARTESIAN_POINT('Ctrl Pts',(13.9616377810684,-49.0700669278844,
-523.758272058823));
#153759=CARTESIAN_POINT('Ctrl Pts',(9.33447550508176,-49.9350334639422,
-525.252389705882));
#153760=CARTESIAN_POINT('Ctrl Pts',(4.70731322909511,-50.8,-526.746507352941));
#153761=CARTESIAN_POINT('Ctrl Pts',(0.,-50.8,-528.240625));
#153762=CARTESIAN_POINT('Ctrl Pts',(-4.70731322909511,-50.8,-529.734742647059));
#153763=CARTESIAN_POINT('Ctrl Pts',(-9.33447550508177,-49.9350334639422,
-531.228860294118));
#153764=CARTESIAN_POINT('Ctrl Pts',(-13.9616377810684,-49.0700669278844,
-532.722977941177));
#153765=CARTESIAN_POINT('Ctrl Pts',(-18.3510766423074,-47.3695892537413,
-534.217095588235));
#153766=CARTESIAN_POINT('Ctrl Pts',(-22.7405155035463,-45.6691115795981,
-535.711213235294));
#153767=CARTESIAN_POINT('Ctrl Pts',(-26.7427538741697,-43.1910304950644,
-537.205330882353));
#153768=CARTESIAN_POINT('Ctrl Pts',(-30.744992244793,-40.7129494105307,
-538.699448529412));
#153769=CARTESIAN_POINT('Ctrl Pts',(-34.2237386972451,-37.5416529948095,
-540.193566176471));
#153770=CARTESIAN_POINT('Ctrl Pts',(-37.7024851496972,-34.3703565790883,
-541.687683823529));
#153771=CARTESIAN_POINT('Ctrl Pts',(-40.5392751458362,-30.6138395280662,
-543.181801470588));
#153772=CARTESIAN_POINT('Ctrl Pts',(-43.3760651419751,-26.8573224770441,
-544.675919117647));
#153773=CARTESIAN_POINT('Ctrl Pts',(-45.4742952008371,-22.6435084734481,
-546.170036764706));
#153774=CARTESIAN_POINT('Ctrl Pts',(-47.5725252596992,-18.4296944698521,
-547.664154411765));
#153775=CARTESIAN_POINT('Ctrl Pts',(-48.8607426731792,-13.9020798956618,
-549.158272058823));
#153776=CARTESIAN_POINT('Ctrl Pts',(-50.1489600866593,-9.37446532147148,
-550.652389705882));
#153777=CARTESIAN_POINT('Ctrl Pts',(-50.5832961557877,-4.68723266073574,
-552.146507352941));
#153778=CARTESIAN_POINT('Ctrl Pts',(-51.0176322249162,-3.12392900021603E-15,
-553.640625));
#153779=CARTESIAN_POINT('Ctrl Pts',(-50.5832961557877,4.68723266073573,
-555.134742647059));
#153780=CARTESIAN_POINT('Ctrl Pts',(-50.1489600866593,9.37446532147149,
-556.628860294118));
#153781=CARTESIAN_POINT('Ctrl Pts',(-48.8607426731792,13.9020798956618,
-558.122977941176));
#153782=CARTESIAN_POINT('Ctrl Pts',(-47.5725252596992,18.4296944698521,
-559.617095588235));
#153783=CARTESIAN_POINT('Ctrl Pts',(-45.4742952008371,22.6435084734481,
-561.111213235294));
#153784=CARTESIAN_POINT('Ctrl Pts',(-43.3760651419751,26.8573224770442,
-562.605330882353));
#153785=CARTESIAN_POINT('Ctrl Pts',(-40.5392751458362,30.6138395280662,
-564.099448529412));
#153786=CARTESIAN_POINT('Ctrl Pts',(-37.7024851496972,34.3703565790883,
-565.593566176471));
#153787=CARTESIAN_POINT('Ctrl Pts',(-34.2237386972451,37.5416529948095,
-567.087683823529));
#153788=CARTESIAN_POINT('Ctrl Pts',(-30.744992244793,40.7129494105307,-568.581801470588));
#153789=CARTESIAN_POINT('Ctrl Pts',(-26.7427538741697,43.1910304950644,
-570.075919117647));
#153790=CARTESIAN_POINT('Ctrl Pts',(-22.7405155035463,45.6691115795981,
-571.570036764706));
#153791=CARTESIAN_POINT('Ctrl Pts',(-18.3510766423074,47.3695892537413,
-573.064154411765));
#153792=CARTESIAN_POINT('Ctrl Pts',(-13.9616377810684,49.0700669278844,
-574.558272058824));
#153793=CARTESIAN_POINT('Ctrl Pts',(-9.33447550508177,49.9350334639422,
-576.052389705882));
#153794=CARTESIAN_POINT('Ctrl Pts',(-4.7073132290951,50.8,-577.546507352941));
#153795=CARTESIAN_POINT('Ctrl Pts',(-6.22120573966855E-15,50.8,-579.040625));
#153796=CARTESIAN_POINT('Ctrl Pts',(4.70731322909511,50.8,-580.534742647059));
#153797=CARTESIAN_POINT('Ctrl Pts',(9.33447550508176,49.9350334639422,-582.028860294118));
#153798=CARTESIAN_POINT('Ctrl Pts',(13.9616377810684,49.0700669278844,-583.522977941176));
#153799=CARTESIAN_POINT('Ctrl Pts',(18.3510766423074,47.3695892537413,-585.017095588235));
#153800=CARTESIAN_POINT('Ctrl Pts',(22.7405155035463,45.6691115795981,-586.511213235294));
#153801=CARTESIAN_POINT('Ctrl Pts',(26.7427538741697,43.1910304950644,-588.005330882353));
#153802=CARTESIAN_POINT('Ctrl Pts',(30.744992244793,40.7129494105307,-589.499448529412));
#153803=CARTESIAN_POINT('Ctrl Pts',(34.2237386972451,37.5416529948095,-590.993566176471));
#153804=CARTESIAN_POINT('Ctrl Pts',(37.7024851496972,34.3703565790883,-592.48768382353));
#153805=CARTESIAN_POINT('Ctrl Pts',(40.5392751458362,30.6138395280662,-593.981801470588));
#153806=CARTESIAN_POINT('Ctrl Pts',(43.3760651419751,26.8573224770442,-595.475919117647));
#153807=CARTESIAN_POINT('Ctrl Pts',(45.4742952008372,22.6435084734481,-596.970036764706));
#153808=CARTESIAN_POINT('Ctrl Pts',(47.5725252596992,18.4296944698521,-598.464154411765));
#153809=CARTESIAN_POINT('Ctrl Pts',(48.8607426731792,13.9020798956618,-599.958272058823));
#153810=CARTESIAN_POINT('Ctrl Pts',(50.1489600866593,9.37446532147146,-601.452389705883));
#153811=CARTESIAN_POINT('Ctrl Pts',(50.5832961557877,4.68723266073574,-602.946507352941));
#153812=CARTESIAN_POINT('Ctrl Pts',(51.0176322249162,9.37178700064808E-15,
-604.440625));
#153813=CARTESIAN_POINT('Ctrl Pts',(50.5832961557877,-4.68723266073572,
-605.934742647059));
#153814=CARTESIAN_POINT('Ctrl Pts',(50.1489600866593,-9.37446532147149,
-607.428860294118));
#153815=CARTESIAN_POINT('Ctrl Pts',(48.8607426731792,-13.9020798956618,
-608.922977941176));
#153816=CARTESIAN_POINT('Ctrl Pts',(47.5725252596992,-18.4296944698521,
-610.417095588235));
#153817=CARTESIAN_POINT('Ctrl Pts',(45.4742952008371,-22.6435084734482,
-611.911213235294));
#153818=CARTESIAN_POINT('Ctrl Pts',(43.3760651419751,-26.8573224770441,
-613.405330882353));
#153819=CARTESIAN_POINT('Ctrl Pts',(40.5392751458362,-30.6138395280662,
-614.899448529412));
#153820=CARTESIAN_POINT('Ctrl Pts',(37.7024851496972,-34.3703565790883,
-616.393566176471));
#153821=CARTESIAN_POINT('Ctrl Pts',(34.2237386972451,-37.5416529948095,
-617.887683823529));
#153822=CARTESIAN_POINT('Ctrl Pts',(30.744992244793,-40.7129494105307,-619.381801470588));
#153823=CARTESIAN_POINT('Ctrl Pts',(26.7427538741697,-43.1910304950644,
-620.875919117647));
#153824=CARTESIAN_POINT('Ctrl Pts',(22.7405155035463,-45.6691115795981,
-622.370036764706));
#153825=CARTESIAN_POINT('Ctrl Pts',(18.3510766423074,-47.3695892537413,
-623.864154411765));
#153826=CARTESIAN_POINT('Ctrl Pts',(13.9616377810684,-49.0700669278844,
-625.358272058823));
#153827=CARTESIAN_POINT('Ctrl Pts',(9.33447550508176,-49.9350334639422,
-626.852389705882));
#153828=CARTESIAN_POINT('Ctrl Pts',(4.70731322909511,-50.8,-628.346507352941));
#153829=CARTESIAN_POINT('Ctrl Pts',(0.,-50.8,-629.840625));
#153830=CARTESIAN_POINT('Ctrl Pts',(-4.70731322909511,-50.8,-631.334742647059));
#153831=CARTESIAN_POINT('Ctrl Pts',(-9.33447550508177,-49.9350334639422,
-632.828860294118));
#153832=CARTESIAN_POINT('Ctrl Pts',(-13.9616377810684,-49.0700669278844,
-634.322977941177));
#153833=CARTESIAN_POINT('Ctrl Pts',(-18.3510766423074,-47.3695892537413,
-635.817095588235));
#153834=CARTESIAN_POINT('Ctrl Pts',(-22.7405155035463,-45.6691115795981,
-637.311213235294));
#153835=CARTESIAN_POINT('Ctrl Pts',(-26.7427538741697,-43.1910304950644,
-638.805330882353));
#153836=CARTESIAN_POINT('Ctrl Pts',(-30.744992244793,-40.7129494105307,
-640.299448529412));
#153837=CARTESIAN_POINT('Ctrl Pts',(-34.2237386972451,-37.5416529948095,
-641.79356617647));
#153838=CARTESIAN_POINT('Ctrl Pts',(-37.7024851496972,-34.3703565790883,
-643.287683823529));
#153839=CARTESIAN_POINT('Ctrl Pts',(-40.5392751458362,-30.6138395280662,
-644.781801470588));
#153840=CARTESIAN_POINT('Ctrl Pts',(-43.3760651419751,-26.8573224770441,
-646.275919117647));
#153841=CARTESIAN_POINT('Ctrl Pts',(-45.4742952008371,-22.6435084734481,
-647.770036764706));
#153842=CARTESIAN_POINT('Ctrl Pts',(-47.5725252596992,-18.4296944698521,
-649.264154411765));
#153843=CARTESIAN_POINT('Ctrl Pts',(-48.8607426731792,-13.9020798956618,
-650.758272058824));
#153844=CARTESIAN_POINT('Ctrl Pts',(-50.1489600866593,-9.37446532147148,
-652.252389705883));
#153845=CARTESIAN_POINT('Ctrl Pts',(-50.5832961557877,-4.68723266073574,
-653.746507352941));
#153846=CARTESIAN_POINT('Ctrl Pts',(-51.0176322249162,-3.12392900021603E-15,
-655.240625));
#153847=CARTESIAN_POINT('Ctrl Pts',(-50.5832961557877,4.68723266073573,
-656.734742647059));
#153848=CARTESIAN_POINT('Ctrl Pts',(-50.1489600866593,9.37446532147149,
-658.228860294118));
#153849=CARTESIAN_POINT('Ctrl Pts',(-48.8607426731792,13.9020798956618,
-659.722977941176));
#153850=CARTESIAN_POINT('Ctrl Pts',(-47.5725252596992,18.4296944698521,
-661.217095588236));
#153851=CARTESIAN_POINT('Ctrl Pts',(-45.4742952008371,22.6435084734481,
-662.711213235294));
#153852=CARTESIAN_POINT('Ctrl Pts',(-43.3760651419751,26.8573224770442,
-664.205330882353));
#153853=CARTESIAN_POINT('Ctrl Pts',(-40.5392751458362,30.6138395280662,
-665.699448529412));
#153854=CARTESIAN_POINT('Ctrl Pts',(-37.7024851496972,34.3703565790883,
-667.193566176471));
#153855=CARTESIAN_POINT('Ctrl Pts',(-34.2237386972451,37.5416529948095,
-668.687683823529));
#153856=CARTESIAN_POINT('Ctrl Pts',(-30.744992244793,40.7129494105307,-670.181801470588));
#153857=CARTESIAN_POINT('Ctrl Pts',(-26.7427538741697,43.1910304950644,
-671.675919117647));
#153858=CARTESIAN_POINT('Ctrl Pts',(-22.7405155035463,45.6691115795981,
-673.170036764706));
#153859=CARTESIAN_POINT('Ctrl Pts',(-18.3510766423074,47.3695892537413,
-674.664154411765));
#153860=CARTESIAN_POINT('Ctrl Pts',(-13.9616377810684,49.0700669278844,
-676.158272058824));
#153861=CARTESIAN_POINT('Ctrl Pts',(-9.33447550508177,49.9350334639422,
-677.652389705882));
#153862=CARTESIAN_POINT('Ctrl Pts',(-4.7073132290951,50.8,-679.146507352941));
#153863=CARTESIAN_POINT('Ctrl Pts',(-6.22120573966855E-15,50.8,-680.640625));
#153864=CARTESIAN_POINT('Ctrl Pts',(4.70731322909511,50.8,-682.134742647059));
#153865=CARTESIAN_POINT('Ctrl Pts',(9.33447550508176,49.9350334639422,-683.628860294117));
#153866=CARTESIAN_POINT('Ctrl Pts',(13.9616377810684,49.0700669278844,-685.122977941176));
#153867=CARTESIAN_POINT('Ctrl Pts',(18.3510766423074,47.3695892537413,-686.617095588235));
#153868=CARTESIAN_POINT('Ctrl Pts',(22.7405155035463,45.6691115795981,-688.111213235294));
#153869=CARTESIAN_POINT('Ctrl Pts',(26.7427538741697,43.1910304950644,-689.605330882353));
#153870=CARTESIAN_POINT('Ctrl Pts',(30.744992244793,40.7129494105307,-691.099448529412));
#153871=CARTESIAN_POINT('Ctrl Pts',(34.2237386972451,37.5416529948095,-692.593566176471));
#153872=CARTESIAN_POINT('Ctrl Pts',(37.7024851496972,34.3703565790883,-694.087683823529));
#153873=CARTESIAN_POINT('Ctrl Pts',(40.5392751458362,30.6138395280662,-695.581801470588));
#153874=CARTESIAN_POINT('Ctrl Pts',(43.3760651419751,26.8573224770442,-697.075919117647));
#153875=CARTESIAN_POINT('Ctrl Pts',(45.4742952008372,22.6435084734481,-698.570036764706));
#153876=CARTESIAN_POINT('Ctrl Pts',(47.5725252596992,18.4296944698521,-700.064154411765));
#153877=CARTESIAN_POINT('Ctrl Pts',(48.8607426731792,13.9020798956618,-701.558272058823));
#153878=CARTESIAN_POINT('Ctrl Pts',(50.1489600866593,9.37446532147146,-703.052389705882));
#153879=CARTESIAN_POINT('Ctrl Pts',(50.5832961557877,4.68723266073574,-704.546507352941));
#153880=CARTESIAN_POINT('Ctrl Pts',(51.0176322249162,9.37178700064808E-15,
-706.040625));
#153881=CARTESIAN_POINT('Ctrl Pts',(50.5832961557877,-4.68723266073572,
-707.534742647059));
#153882=CARTESIAN_POINT('Ctrl Pts',(50.1489600866593,-9.37446532147149,
-709.028860294118));
#153883=CARTESIAN_POINT('Ctrl Pts',(48.8607426731792,-13.9020798956618,
-710.522977941177));
#153884=CARTESIAN_POINT('Ctrl Pts',(47.5725252596992,-18.4296944698521,
-712.017095588236));
#153885=CARTESIAN_POINT('Ctrl Pts',(45.4742952008371,-22.6435084734482,
-713.511213235294));
#153886=CARTESIAN_POINT('Ctrl Pts',(43.3760651419751,-26.8573224770441,
-715.005330882353));
#153887=CARTESIAN_POINT('Ctrl Pts',(40.5392751458362,-30.6138395280662,
-716.499448529412));
#153888=CARTESIAN_POINT('Ctrl Pts',(37.7024851496972,-34.3703565790883,
-717.99356617647));
#153889=CARTESIAN_POINT('Ctrl Pts',(34.2237386972451,-37.5416529948095,
-719.487683823529));
#153890=CARTESIAN_POINT('Ctrl Pts',(30.744992244793,-40.7129494105307,-720.981801470588));
#153891=CARTESIAN_POINT('Ctrl Pts',(26.7427538741697,-43.1910304950644,
-722.475919117647));
#153892=CARTESIAN_POINT('Ctrl Pts',(22.7405155035463,-45.6691115795981,
-723.970036764706));
#153893=CARTESIAN_POINT('Ctrl Pts',(18.3510766423074,-47.3695892537413,
-725.464154411765));
#153894=CARTESIAN_POINT('Ctrl Pts',(13.9616377810684,-49.0700669278844,
-726.958272058824));
#153895=CARTESIAN_POINT('Ctrl Pts',(9.33447550508176,-49.9350334639422,
-728.452389705882));
#153896=CARTESIAN_POINT('Ctrl Pts',(4.70731322909511,-50.8,-729.946507352941));
#153897=CARTESIAN_POINT('Ctrl Pts',(0.,-50.8,-731.440625));
#153898=CARTESIAN_POINT('Ctrl Pts',(-4.70731322909511,-50.8,-732.934742647059));
#153899=CARTESIAN_POINT('Ctrl Pts',(-9.33447550508177,-49.9350334639422,
-734.428860294118));
#153900=CARTESIAN_POINT('Ctrl Pts',(-13.9616377810684,-49.0700669278844,
-735.922977941176));
#153901=CARTESIAN_POINT('Ctrl Pts',(-18.3510766423074,-47.3695892537413,
-737.417095588235));
#153902=CARTESIAN_POINT('Ctrl Pts',(-22.7405155035463,-45.6691115795981,
-738.911213235294));
#153903=CARTESIAN_POINT('Ctrl Pts',(-26.7427538741697,-43.1910304950644,
-740.405330882353));
#153904=CARTESIAN_POINT('Ctrl Pts',(-30.744992244793,-40.7129494105307,
-741.899448529412));
#153905=CARTESIAN_POINT('Ctrl Pts',(-34.2237386972451,-37.5416529948095,
-743.39356617647));
#153906=CARTESIAN_POINT('Ctrl Pts',(-37.7024851496972,-34.3703565790883,
-744.887683823529));
#153907=CARTESIAN_POINT('Ctrl Pts',(-40.5392751458362,-30.6138395280662,
-746.381801470588));
#153908=CARTESIAN_POINT('Ctrl Pts',(-43.3760651419751,-26.8573224770441,
-747.875919117647));
#153909=CARTESIAN_POINT('Ctrl Pts',(-45.4742952008371,-22.6435084734481,
-749.370036764706));
#153910=CARTESIAN_POINT('Ctrl Pts',(-47.5725252596992,-18.4296944698521,
-750.864154411765));
#153911=CARTESIAN_POINT('Ctrl Pts',(-48.8607426731792,-13.9020798956618,
-752.358272058824));
#153912=CARTESIAN_POINT('Ctrl Pts',(-50.1489600866593,-9.37446532147148,
-753.852389705883));
#153913=CARTESIAN_POINT('Ctrl Pts',(-50.5832961557877,-4.68723266073574,
-755.346507352941));
#153914=CARTESIAN_POINT('Ctrl Pts',(-51.0176322249162,-3.12392900021603E-15,
-756.840625));
#153915=CARTESIAN_POINT('Ctrl Pts',(-50.5832961557877,4.68723266073573,
-758.334742647059));
#153916=CARTESIAN_POINT('Ctrl Pts',(-50.1489600866593,9.37446532147149,
-759.828860294117));
#153917=CARTESIAN_POINT('Ctrl Pts',(-48.8607426731792,13.9020798956618,
-761.322977941176));
#153918=CARTESIAN_POINT('Ctrl Pts',(-47.5725252596992,18.4296944698521,
-762.817095588235));
#153919=CARTESIAN_POINT('Ctrl Pts',(-45.4742952008371,22.6435084734481,
-764.311213235294));
#153920=CARTESIAN_POINT('Ctrl Pts',(-43.3760651419751,26.8573224770442,
-765.805330882353));
#153921=CARTESIAN_POINT('Ctrl Pts',(-40.5392751458362,30.6138395280662,
-767.299448529412));
#153922=CARTESIAN_POINT('Ctrl Pts',(-37.7024851496972,34.3703565790883,
-768.793566176471));
#153923=CARTESIAN_POINT('Ctrl Pts',(-34.2237386972451,37.5416529948095,
-770.28768382353));
#153924=CARTESIAN_POINT('Ctrl Pts',(-30.744992244793,40.7129494105307,-771.781801470589));
#153925=CARTESIAN_POINT('Ctrl Pts',(-26.7427538741697,43.1910304950644,
-773.275919117647));
#153926=CARTESIAN_POINT('Ctrl Pts',(-22.7405155035463,45.6691115795981,
-774.770036764706));
#153927=CARTESIAN_POINT('Ctrl Pts',(-18.3510766423074,47.3695892537413,
-776.264154411765));
#153928=CARTESIAN_POINT('Ctrl Pts',(-13.9616377810684,49.0700669278844,
-777.758272058824));
#153929=CARTESIAN_POINT('Ctrl Pts',(-9.33447550508177,49.9350334639422,
-779.252389705882));
#153930=CARTESIAN_POINT('Ctrl Pts',(-4.7073132290951,50.8,-780.746507352941));
#153931=CARTESIAN_POINT('Ctrl Pts',(-6.22120573966855E-15,50.8,-782.240625));
#153932=CARTESIAN_POINT('Ctrl Pts',(4.70731322909511,50.8,-783.734742647059));
#153933=CARTESIAN_POINT('Ctrl Pts',(9.33447550508176,49.9350334639422,-785.228860294118));
#153934=CARTESIAN_POINT('Ctrl Pts',(13.9616377810684,49.0700669278844,-786.722977941177));
#153935=CARTESIAN_POINT('Ctrl Pts',(18.3510766423074,47.3695892537413,-788.217095588235));
#153936=CARTESIAN_POINT('Ctrl Pts',(22.7405155035463,45.6691115795981,-789.711213235294));
#153937=CARTESIAN_POINT('Ctrl Pts',(26.7427538741697,43.1910304950644,-791.205330882353));
#153938=CARTESIAN_POINT('Ctrl Pts',(30.744992244793,40.7129494105307,-792.699448529412));
#153939=CARTESIAN_POINT('Ctrl Pts',(34.2237386972451,37.5416529948095,-794.193566176471));
#153940=CARTESIAN_POINT('Ctrl Pts',(37.7024851496972,34.3703565790883,-795.687683823529));
#153941=CARTESIAN_POINT('Ctrl Pts',(40.5392751458362,30.6138395280662,-797.181801470588));
#153942=CARTESIAN_POINT('Ctrl Pts',(43.3760651419751,26.8573224770442,-798.675919117647));
#153943=CARTESIAN_POINT('Ctrl Pts',(45.4742952008372,22.6435084734481,-800.170036764706));
#153944=CARTESIAN_POINT('Ctrl Pts',(47.5725252596992,18.4296944698521,-801.664154411765));
#153945=CARTESIAN_POINT('Ctrl Pts',(48.8607426731792,13.9020798956618,-803.158272058823));
#153946=CARTESIAN_POINT('Ctrl Pts',(50.1489600866593,9.37446532147146,-804.652389705882));
#153947=CARTESIAN_POINT('Ctrl Pts',(50.5832961557877,4.68723266073574,-806.146507352941));
#153948=CARTESIAN_POINT('Ctrl Pts',(51.0176322249162,9.37178700064808E-15,
-807.640625));
#153949=CARTESIAN_POINT('Ctrl Pts',(50.5832961557877,-4.68723266073572,
-809.134742647059));
#153950=CARTESIAN_POINT('Ctrl Pts',(50.1489600866593,-9.37446532147149,
-810.628860294118));
#153951=CARTESIAN_POINT('Ctrl Pts',(48.8607426731792,-13.9020798956618,
-812.122977941177));
#153952=CARTESIAN_POINT('Ctrl Pts',(47.5725252596992,-18.4296944698521,
-813.617095588236));
#153953=CARTESIAN_POINT('Ctrl Pts',(45.4742952008371,-22.6435084734482,
-815.111213235294));
#153954=CARTESIAN_POINT('Ctrl Pts',(43.3760651419751,-26.8573224770441,
-816.605330882353));
#153955=CARTESIAN_POINT('Ctrl Pts',(40.5392751458362,-30.6138395280662,
-818.099448529412));
#153956=CARTESIAN_POINT('Ctrl Pts',(37.7024851496972,-34.3703565790883,
-819.59356617647));
#153957=CARTESIAN_POINT('Ctrl Pts',(34.2237386972451,-37.5416529948095,
-821.087683823529));
#153958=CARTESIAN_POINT('Ctrl Pts',(30.744992244793,-40.7129494105307,-822.581801470588));
#153959=CARTESIAN_POINT('Ctrl Pts',(26.7427538741697,-43.1910304950644,
-824.075919117647));
#153960=CARTESIAN_POINT('Ctrl Pts',(22.7405155035463,-45.6691115795981,
-825.570036764706));
#153961=CARTESIAN_POINT('Ctrl Pts',(18.3510766423074,-47.3695892537413,
-827.064154411765));
#153962=CARTESIAN_POINT('Ctrl Pts',(13.9616377810684,-49.0700669278844,
-828.558272058824));
#153963=CARTESIAN_POINT('Ctrl Pts',(9.33447550508176,-49.9350334639422,
-830.052389705883));
#153964=CARTESIAN_POINT('Ctrl Pts',(4.70731322909511,-50.8,-831.546507352941));
#153965=CARTESIAN_POINT('Ctrl Pts',(0.,-50.8,-833.040625));
#153966=CARTESIAN_POINT('Ctrl Pts',(-4.70731322909511,-50.8,-834.534742647059));
#153967=CARTESIAN_POINT('Ctrl Pts',(-9.33447550508177,-49.9350334639422,
-836.028860294118));
#153968=CARTESIAN_POINT('Ctrl Pts',(-13.9616377810684,-49.0700669278844,
-837.522977941177));
#153969=CARTESIAN_POINT('Ctrl Pts',(-18.3510766423074,-47.3695892537413,
-839.017095588235));
#153970=CARTESIAN_POINT('Ctrl Pts',(-22.7405155035463,-45.6691115795981,
-840.511213235294));
#153971=CARTESIAN_POINT('Ctrl Pts',(-26.7427538741697,-43.1910304950644,
-842.005330882353));
#153972=CARTESIAN_POINT('Ctrl Pts',(-30.744992244793,-40.7129494105307,
-843.499448529412));
#153973=CARTESIAN_POINT('Ctrl Pts',(-34.2237386972451,-37.5416529948095,
-844.993566176471));
#153974=CARTESIAN_POINT('Ctrl Pts',(-37.7024851496972,-34.3703565790883,
-846.48768382353));
#153975=CARTESIAN_POINT('Ctrl Pts',(-40.5392751458362,-30.6138395280662,
-847.981801470588));
#153976=CARTESIAN_POINT('Ctrl Pts',(-43.3760651419751,-26.8573224770441,
-849.475919117647));
#153977=CARTESIAN_POINT('Ctrl Pts',(-45.4742952008371,-22.6435084734481,
-850.970036764706));
#153978=CARTESIAN_POINT('Ctrl Pts',(-47.5725252596992,-18.4296944698521,
-852.464154411765));
#153979=CARTESIAN_POINT('Ctrl Pts',(-48.8607426731792,-13.9020798956618,
-853.958272058824));
#153980=CARTESIAN_POINT('Ctrl Pts',(-50.1489600866593,-9.37446532147148,
-855.452389705882));
#153981=CARTESIAN_POINT('Ctrl Pts',(-50.5832961557877,-4.68723266073574,
-856.946507352941));
#153982=CARTESIAN_POINT('Ctrl Pts',(-51.0176322249162,-3.12392900021603E-15,
-858.440625));
#153983=CARTESIAN_POINT('Ctrl Pts',(-50.5832961557877,4.68723266073573,
-859.934742647059));
#153984=CARTESIAN_POINT('Ctrl Pts',(-50.1489600866593,9.37446532147149,
-861.428860294118));
#153985=CARTESIAN_POINT('Ctrl Pts',(-48.8607426731792,13.9020798956618,
-862.922977941176));
#153986=CARTESIAN_POINT('Ctrl Pts',(-47.5725252596992,18.4296944698521,
-864.417095588235));
#153987=CARTESIAN_POINT('Ctrl Pts',(-45.4742952008371,22.6435084734481,
-865.911213235294));
#153988=CARTESIAN_POINT('Ctrl Pts',(-43.3760651419751,26.8573224770442,
-867.405330882353));
#153989=CARTESIAN_POINT('Ctrl Pts',(-40.5392751458362,30.6138395280662,
-868.899448529412));
#153990=CARTESIAN_POINT('Ctrl Pts',(-37.7024851496972,34.3703565790883,
-870.393566176471));
#153991=CARTESIAN_POINT('Ctrl Pts',(-34.2237386972451,37.5416529948095,
-871.887683823529));
#153992=CARTESIAN_POINT('Ctrl Pts',(-30.744992244793,40.7129494105307,-873.381801470588));
#153993=CARTESIAN_POINT('Ctrl Pts',(-26.7427538741697,43.1910304950644,
-874.875919117647));
#153994=CARTESIAN_POINT('Ctrl Pts',(-22.7405155035463,45.6691115795981,
-876.370036764706));
#153995=CARTESIAN_POINT('Ctrl Pts',(-18.3510766423074,47.3695892537413,
-877.864154411765));
#153996=CARTESIAN_POINT('Ctrl Pts',(-13.9616377810684,49.0700669278844,
-879.358272058823));
#153997=CARTESIAN_POINT('Ctrl Pts',(-9.33447550508177,49.9350334639422,
-880.852389705882));
#153998=CARTESIAN_POINT('Ctrl Pts',(-4.7073132290951,50.8,-882.346507352941));
#153999=CARTESIAN_POINT('Ctrl Pts',(-6.22120573966855E-15,50.8,-883.840625));
#154000=CARTESIAN_POINT('Ctrl Pts',(4.70731322909511,50.8,-885.334742647059));
#154001=CARTESIAN_POINT('Ctrl Pts',(9.33447550508176,49.9350334639422,-886.828860294118));
#154002=CARTESIAN_POINT('Ctrl Pts',(13.9616377810684,49.0700669278844,-888.322977941177));
#154003=CARTESIAN_POINT('Ctrl Pts',(18.3510766423074,47.3695892537413,-889.817095588235));
#154004=CARTESIAN_POINT('Ctrl Pts',(22.7405155035463,45.6691115795981,-891.311213235294));
#154005=CARTESIAN_POINT('Ctrl Pts',(26.7427538741697,43.1910304950644,-892.805330882353));
#154006=CARTESIAN_POINT('Ctrl Pts',(30.744992244793,40.7129494105307,-894.299448529412));
#154007=CARTESIAN_POINT('Ctrl Pts',(34.2237386972451,37.5416529948095,-895.79356617647));
#154008=CARTESIAN_POINT('Ctrl Pts',(37.7024851496972,34.3703565790883,-897.287683823529));
#154009=CARTESIAN_POINT('Ctrl Pts',(40.5392751458362,30.6138395280662,-898.781801470588));
#154010=CARTESIAN_POINT('Ctrl Pts',(43.3760651419751,26.8573224770442,-900.275919117647));
#154011=CARTESIAN_POINT('Ctrl Pts',(45.4742952008372,22.6435084734481,-901.770036764706));
#154012=CARTESIAN_POINT('Ctrl Pts',(47.5725252596992,18.4296944698521,-903.264154411765));
#154013=CARTESIAN_POINT('Ctrl Pts',(48.8607426731792,13.9020798956618,-904.758272058824));
#154014=CARTESIAN_POINT('Ctrl Pts',(50.1489600866593,9.37446532147146,-906.252389705883));
#154015=CARTESIAN_POINT('Ctrl Pts',(50.5832961557877,4.68723266073574,-907.746507352941));
#154016=CARTESIAN_POINT('Ctrl Pts',(51.0176322249162,9.37178700064808E-15,
-909.240625));
#154017=CARTESIAN_POINT('Ctrl Pts',(50.5832961557877,-4.68723266073572,
-910.734742647059));
#154018=CARTESIAN_POINT('Ctrl Pts',(50.1489600866593,-9.37446532147149,
-912.228860294118));
#154019=CARTESIAN_POINT('Ctrl Pts',(48.8607426731792,-13.9020798956618,
-913.722977941176));
#154020=CARTESIAN_POINT('Ctrl Pts',(47.5725252596992,-18.4296944698521,
-915.217095588235));
#154021=CARTESIAN_POINT('Ctrl Pts',(45.4742952008371,-22.6435084734482,
-916.711213235294));
#154022=CARTESIAN_POINT('Ctrl Pts',(43.3760651419751,-26.8573224770441,
-918.205330882353));
#154023=CARTESIAN_POINT('Ctrl Pts',(40.5392751458362,-30.6138395280662,
-919.699448529412));
#154024=CARTESIAN_POINT('Ctrl Pts',(37.7024851496972,-34.3703565790883,
-921.193566176471));
#154025=CARTESIAN_POINT('Ctrl Pts',(34.2237386972451,-37.5416529948095,
-922.687683823529));
#154026=CARTESIAN_POINT('Ctrl Pts',(30.744992244793,-40.7129494105307,-924.181801470588));
#154027=CARTESIAN_POINT('Ctrl Pts',(26.7427538741697,-43.1910304950644,
-925.675919117647));
#154028=CARTESIAN_POINT('Ctrl Pts',(22.7405155035463,-45.6691115795981,
-927.170036764706));
#154029=CARTESIAN_POINT('Ctrl Pts',(18.3510766423074,-47.3695892537413,
-928.664154411765));
#154030=CARTESIAN_POINT('Ctrl Pts',(13.9616377810684,-49.0700669278844,
-930.158272058824));
#154031=CARTESIAN_POINT('Ctrl Pts',(9.33447550508176,-49.9350334639422,
-931.652389705882));
#154032=CARTESIAN_POINT('Ctrl Pts',(4.70731322909511,-50.8,-933.146507352942));
#154033=CARTESIAN_POINT('Ctrl Pts',(0.,-50.8,-934.640625));
#154034=CARTESIAN_POINT('Ctrl Pts',(-4.70731322909511,-50.8,-936.134742647059));
#154035=CARTESIAN_POINT('Ctrl Pts',(-9.33447550508177,-49.9350334639422,
-937.628860294117));
#154036=CARTESIAN_POINT('Ctrl Pts',(-13.9616377810684,-49.0700669278844,
-939.122977941176));
#154037=CARTESIAN_POINT('Ctrl Pts',(-18.3510766423074,-47.3695892537413,
-940.617095588235));
#154038=CARTESIAN_POINT('Ctrl Pts',(-22.7405155035463,-45.6691115795981,
-942.111213235294));
#154039=CARTESIAN_POINT('Ctrl Pts',(-26.7427538741697,-43.1910304950644,
-943.605330882353));
#154040=CARTESIAN_POINT('Ctrl Pts',(-30.744992244793,-40.7129494105307,
-945.099448529412));
#154041=CARTESIAN_POINT('Ctrl Pts',(-34.2237386972451,-37.5416529948095,
-946.593566176471));
#154042=CARTESIAN_POINT('Ctrl Pts',(-37.7024851496972,-34.3703565790883,
-948.08768382353));
#154043=CARTESIAN_POINT('Ctrl Pts',(-40.5392751458362,-30.6138395280662,
-949.581801470588));
#154044=CARTESIAN_POINT('Ctrl Pts',(-43.3760651419751,-26.8573224770441,
-951.075919117647));
#154045=CARTESIAN_POINT('Ctrl Pts',(-45.4742952008371,-22.6435084734481,
-952.570036764706));
#154046=CARTESIAN_POINT('Ctrl Pts',(-47.5725252596992,-18.4296944698521,
-954.064154411765));
#154047=CARTESIAN_POINT('Ctrl Pts',(-48.8607426731792,-13.9020798956618,
-955.558272058823));
#154048=CARTESIAN_POINT('Ctrl Pts',(-50.1489600866593,-9.37446532147148,
-957.052389705882));
#154049=CARTESIAN_POINT('Ctrl Pts',(-50.5832961557877,-4.68723266073574,
-958.546507352941));
#154050=CARTESIAN_POINT('Ctrl Pts',(-51.0176322249162,-3.12392900021603E-15,
-960.040625));
#154051=CARTESIAN_POINT('Ctrl Pts',(-50.5832961557877,4.68723266073573,
-961.534742647059));
#154052=CARTESIAN_POINT('Ctrl Pts',(-50.1489600866593,9.37446532147149,
-963.028860294118));
#154053=CARTESIAN_POINT('Ctrl Pts',(-48.8607426731792,13.9020798956618,
-964.522977941177));
#154054=CARTESIAN_POINT('Ctrl Pts',(-47.5725252596992,18.4296944698521,
-966.017095588235));
#154055=CARTESIAN_POINT('Ctrl Pts',(-45.4742952008371,22.6435084734481,
-967.511213235294));
#154056=CARTESIAN_POINT('Ctrl Pts',(-43.3760651419751,26.8573224770442,
-969.005330882353));
#154057=CARTESIAN_POINT('Ctrl Pts',(-40.5392751458362,30.6138395280662,
-970.499448529412));
#154058=CARTESIAN_POINT('Ctrl Pts',(-37.7024851496972,34.3703565790883,
-971.99356617647));
#154059=CARTESIAN_POINT('Ctrl Pts',(-34.2237386972451,37.5416529948095,
-973.487683823529));
#154060=CARTESIAN_POINT('Ctrl Pts',(-30.744992244793,40.7129494105307,-974.981801470588));
#154061=CARTESIAN_POINT('Ctrl Pts',(-26.7427538741697,43.1910304950644,
-976.475919117647));
#154062=CARTESIAN_POINT('Ctrl Pts',(-22.7405155035463,45.6691115795981,
-977.970036764706));
#154063=CARTESIAN_POINT('Ctrl Pts',(-18.3510766423074,47.3695892537413,
-979.464154411765));
#154064=CARTESIAN_POINT('Ctrl Pts',(-13.9616377810684,49.0700669278844,
-980.958272058824));
#154065=CARTESIAN_POINT('Ctrl Pts',(-9.33447550508177,49.9350334639422,
-982.452389705882));
#154066=CARTESIAN_POINT('Ctrl Pts',(-4.7073132290951,50.8,-983.946507352941));
#154067=CARTESIAN_POINT('Ctrl Pts',(-6.22120573966855E-15,50.8,-985.440625));
#154068=CARTESIAN_POINT('Ctrl Pts',(4.70731322909511,50.8,-986.934742647059));
#154069=CARTESIAN_POINT('Ctrl Pts',(9.33447550508176,49.9350334639422,-988.428860294118));
#154070=CARTESIAN_POINT('Ctrl Pts',(13.9616377810684,49.0700669278844,-989.922977941177));
#154071=CARTESIAN_POINT('Ctrl Pts',(18.3510766423074,47.3695892537413,-991.417095588235));
#154072=CARTESIAN_POINT('Ctrl Pts',(22.7405155035463,45.6691115795981,-992.911213235294));
#154073=CARTESIAN_POINT('Ctrl Pts',(26.7427538741697,43.1910304950644,-994.405330882353));
#154074=CARTESIAN_POINT('Ctrl Pts',(30.744992244793,40.7129494105307,-995.899448529412));
#154075=CARTESIAN_POINT('Ctrl Pts',(34.2237386972451,37.5416529948095,-997.39356617647));
#154076=CARTESIAN_POINT('Ctrl Pts',(37.7024851496972,34.3703565790883,-998.887683823529));
#154077=CARTESIAN_POINT('Ctrl Pts',(40.5392751458362,30.6138395280662,-1000.38180147059));
#154078=CARTESIAN_POINT('Ctrl Pts',(43.3760651419751,26.8573224770442,-1001.87591911765));
#154079=CARTESIAN_POINT('Ctrl Pts',(45.4742952008372,22.6435084734481,-1003.37003676471));
#154080=CARTESIAN_POINT('Ctrl Pts',(47.5725252596992,18.4296944698521,-1004.86415441176));
#154081=CARTESIAN_POINT('Ctrl Pts',(48.8607426731792,13.9020798956618,-1006.35827205882));
#154082=CARTESIAN_POINT('Ctrl Pts',(50.1489600866593,9.37446532147146,-1007.85238970588));
#154083=CARTESIAN_POINT('Ctrl Pts',(50.5832961557877,4.68723266073574,-1009.34650735294));
#154084=CARTESIAN_POINT('Ctrl Pts',(51.0176322249162,9.37178700064808E-15,
-1010.840625));
#154085=CARTESIAN_POINT('Ctrl Pts',(50.5832961557877,-4.68723266073572,
-1012.33474264706));
#154086=CARTESIAN_POINT('Ctrl Pts',(50.1489600866593,-9.37446532147149,
-1013.82886029412));
#154087=CARTESIAN_POINT('Ctrl Pts',(48.8607426731792,-13.9020798956618,
-1015.32297794118));
#154088=CARTESIAN_POINT('Ctrl Pts',(47.5725252596992,-18.4296944698521,
-1016.81709558824));
#154089=CARTESIAN_POINT('Ctrl Pts',(45.4742952008371,-22.6435084734482,
-1018.31121323529));
#154090=CARTESIAN_POINT('Ctrl Pts',(43.3760651419751,-26.8573224770441,
-1019.80533088235));
#154091=CARTESIAN_POINT('Ctrl Pts',(40.5392751458362,-30.6138395280662,
-1021.29944852941));
#154092=CARTESIAN_POINT('Ctrl Pts',(37.7024851496972,-34.3703565790883,
-1022.79356617647));
#154093=CARTESIAN_POINT('Ctrl Pts',(34.2237386972451,-37.5416529948095,
-1024.28768382353));
#154094=CARTESIAN_POINT('Ctrl Pts',(30.744992244793,-40.7129494105307,-1025.78180147059));
#154095=CARTESIAN_POINT('Ctrl Pts',(26.7427538741697,-43.1910304950644,
-1027.27591911765));
#154096=CARTESIAN_POINT('Ctrl Pts',(22.7405155035463,-45.6691115795981,
-1028.77003676471));
#154097=CARTESIAN_POINT('Ctrl Pts',(18.3510766423074,-47.3695892537413,
-1030.26415441176));
#154098=CARTESIAN_POINT('Ctrl Pts',(13.9616377810684,-49.0700669278844,
-1031.75827205882));
#154099=CARTESIAN_POINT('Ctrl Pts',(9.33447550508176,-49.9350334639422,
-1033.25238970588));
#154100=CARTESIAN_POINT('Ctrl Pts',(4.70731322909511,-50.8,-1034.74650735294));
#154101=CARTESIAN_POINT('Ctrl Pts',(0.,-50.8,-1036.240625));
#154102=CARTESIAN_POINT('Ctrl Pts',(-4.70731322909511,-50.8,-1037.73474264706));
#154103=CARTESIAN_POINT('Ctrl Pts',(-9.33447550508177,-49.9350334639422,
-1039.22886029412));
#154104=CARTESIAN_POINT('Ctrl Pts',(-13.9616377810684,-49.0700669278844,
-1040.72297794118));
#154105=CARTESIAN_POINT('Ctrl Pts',(-18.3510766423074,-47.3695892537413,
-1042.21709558823));
#154106=CARTESIAN_POINT('Ctrl Pts',(-22.7405155035463,-45.6691115795981,
-1043.71121323529));
#154107=CARTESIAN_POINT('Ctrl Pts',(-26.7427538741697,-43.1910304950644,
-1045.20533088235));
#154108=CARTESIAN_POINT('Ctrl Pts',(-30.744992244793,-40.7129494105307,
-1046.69944852941));
#154109=CARTESIAN_POINT('Ctrl Pts',(-34.2237386972451,-37.5416529948095,
-1048.19356617647));
#154110=CARTESIAN_POINT('Ctrl Pts',(-37.7024851496972,-34.3703565790883,
-1049.68768382353));
#154111=CARTESIAN_POINT('Ctrl Pts',(-40.5392751458362,-30.6138395280662,
-1051.18180147059));
#154112=CARTESIAN_POINT('Ctrl Pts',(-43.3760651419751,-26.8573224770441,
-1052.67591911765));
#154113=CARTESIAN_POINT('Ctrl Pts',(-45.4742952008371,-22.6435084734481,
-1054.17003676471));
#154114=CARTESIAN_POINT('Ctrl Pts',(-47.5725252596992,-18.4296944698521,
-1055.66415441177));
#154115=CARTESIAN_POINT('Ctrl Pts',(-48.8607426731792,-13.9020798956618,
-1057.15827205882));
#154116=CARTESIAN_POINT('Ctrl Pts',(-50.1489600866593,-9.37446532147148,
-1058.65238970588));
#154117=CARTESIAN_POINT('Ctrl Pts',(-50.5832961557877,-4.68723266073574,
-1060.14650735294));
#154118=CARTESIAN_POINT('Ctrl Pts',(-51.0176322249162,-3.12392900021603E-15,
-1061.640625));
#154119=CARTESIAN_POINT('Ctrl Pts',(-50.5832961557877,4.68723266073573,
-1063.13474264706));
#154120=CARTESIAN_POINT('Ctrl Pts',(-50.1489600866593,9.37446532147149,
-1064.62886029412));
#154121=CARTESIAN_POINT('Ctrl Pts',(-48.8607426731792,13.9020798956618,
-1066.12297794118));
#154122=CARTESIAN_POINT('Ctrl Pts',(-47.5725252596992,18.4296944698521,
-1067.61709558824));
#154123=CARTESIAN_POINT('Ctrl Pts',(-45.4742952008371,22.6435084734481,
-1069.11121323529));
#154124=CARTESIAN_POINT('Ctrl Pts',(-43.3760651419751,26.8573224770442,
-1070.60533088235));
#154125=CARTESIAN_POINT('Ctrl Pts',(-40.5392751458362,30.6138395280662,
-1072.09944852941));
#154126=CARTESIAN_POINT('Ctrl Pts',(-37.7024851496972,34.3703565790883,
-1073.59356617647));
#154127=CARTESIAN_POINT('Ctrl Pts',(-34.2237386972451,37.5416529948095,
-1075.08768382353));
#154128=CARTESIAN_POINT('Ctrl Pts',(-30.744992244793,40.7129494105307,-1076.58180147059));
#154129=CARTESIAN_POINT('Ctrl Pts',(-26.7427538741697,43.1910304950644,
-1078.07591911765));
#154130=CARTESIAN_POINT('Ctrl Pts',(-22.7405155035463,45.6691115795981,
-1079.57003676471));
#154131=CARTESIAN_POINT('Ctrl Pts',(-18.3510766423074,47.3695892537413,
-1081.06415441176));
#154132=CARTESIAN_POINT('Ctrl Pts',(-13.9616377810684,49.0700669278844,
-1082.55827205882));
#154133=CARTESIAN_POINT('Ctrl Pts',(-9.33447550508177,49.9350334639422,
-1084.05238970588));
#154134=CARTESIAN_POINT('Ctrl Pts',(-4.7073132290951,50.8,-1085.54650735294));
#154135=CARTESIAN_POINT('Ctrl Pts',(-6.22120573966855E-15,50.8,-1087.040625));
#154136=CARTESIAN_POINT('Ctrl Pts',(4.70731322909511,50.8,-1088.53474264706));
#154137=CARTESIAN_POINT('Ctrl Pts',(9.33447550508176,49.9350334639422,-1090.02886029412));
#154138=CARTESIAN_POINT('Ctrl Pts',(13.9616377810684,49.0700669278844,-1091.52297794118));
#154139=CARTESIAN_POINT('Ctrl Pts',(18.3510766423074,47.3695892537413,-1093.01709558824));
#154140=CARTESIAN_POINT('Ctrl Pts',(22.7405155035463,45.6691115795981,-1094.51121323529));
#154141=CARTESIAN_POINT('Ctrl Pts',(26.7427538741697,43.1910304950644,-1096.00533088235));
#154142=CARTESIAN_POINT('Ctrl Pts',(30.744992244793,40.7129494105307,-1097.49944852941));
#154143=CARTESIAN_POINT('Ctrl Pts',(34.2237386972451,37.5416529948095,-1098.99356617647));
#154144=CARTESIAN_POINT('Ctrl Pts',(37.7024851496972,34.3703565790883,-1100.48768382353));
#154145=CARTESIAN_POINT('Ctrl Pts',(40.5392751458362,30.6138395280662,-1101.98180147059));
#154146=CARTESIAN_POINT('Ctrl Pts',(43.3760651419751,26.8573224770442,-1103.47591911765));
#154147=CARTESIAN_POINT('Ctrl Pts',(45.4742952008372,22.6435084734481,-1104.97003676471));
#154148=CARTESIAN_POINT('Ctrl Pts',(47.5725252596992,18.4296944698521,-1106.46415441176));
#154149=CARTESIAN_POINT('Ctrl Pts',(48.8607426731792,13.9020798956618,-1107.95827205882));
#154150=CARTESIAN_POINT('Ctrl Pts',(50.1489600866593,9.37446532147146,-1109.45238970588));
#154151=CARTESIAN_POINT('Ctrl Pts',(50.5832961557877,4.68723266073574,-1110.94650735294));
#154152=CARTESIAN_POINT('Ctrl Pts',(51.0176322249162,9.37178700064808E-15,
-1112.440625));
#154153=CARTESIAN_POINT('Ctrl Pts',(50.5832961557877,-4.68723266073572,
-1113.93474264706));
#154154=CARTESIAN_POINT('Ctrl Pts',(50.1489600866593,-9.37446532147149,
-1115.42886029412));
#154155=CARTESIAN_POINT('Ctrl Pts',(48.8607426731792,-13.9020798956618,
-1116.92297794118));
#154156=CARTESIAN_POINT('Ctrl Pts',(47.5725252596992,-18.4296944698521,
-1118.41709558824));
#154157=CARTESIAN_POINT('Ctrl Pts',(45.4742952008371,-22.6435084734482,
-1119.91121323529));
#154158=CARTESIAN_POINT('Ctrl Pts',(43.3760651419751,-26.8573224770441,
-1121.40533088235));
#154159=CARTESIAN_POINT('Ctrl Pts',(40.5392751458362,-30.6138395280662,
-1122.89944852941));
#154160=CARTESIAN_POINT('Ctrl Pts',(37.7024851496972,-34.3703565790883,
-1124.39356617647));
#154161=CARTESIAN_POINT('Ctrl Pts',(34.2237386972451,-37.5416529948095,
-1125.88768382353));
#154162=CARTESIAN_POINT('Ctrl Pts',(30.744992244793,-40.7129494105307,-1127.38180147059));
#154163=CARTESIAN_POINT('Ctrl Pts',(26.7427538741697,-43.1910304950644,
-1128.87591911765));
#154164=CARTESIAN_POINT('Ctrl Pts',(22.7405155035463,-45.6691115795981,
-1130.37003676471));
#154165=CARTESIAN_POINT('Ctrl Pts',(18.3510766423074,-47.3695892537413,
-1131.86415441176));
#154166=CARTESIAN_POINT('Ctrl Pts',(13.9616377810684,-49.0700669278844,
-1133.35827205882));
#154167=CARTESIAN_POINT('Ctrl Pts',(9.33447550508176,-49.9350334639422,
-1134.85238970588));
#154168=CARTESIAN_POINT('Ctrl Pts',(4.70731322909511,-50.8,-1136.34650735294));
#154169=CARTESIAN_POINT('Ctrl Pts',(0.,-50.8,-1137.840625));
#154170=CARTESIAN_POINT('Ctrl Pts',(-4.70731322909511,-50.8,-1139.33474264706));
#154171=CARTESIAN_POINT('Ctrl Pts',(-9.33447550508177,-49.9350334639422,
-1140.82886029412));
#154172=CARTESIAN_POINT('Ctrl Pts',(-13.9616377810684,-49.0700669278844,
-1142.32297794118));
#154173=CARTESIAN_POINT('Ctrl Pts',(-18.3510766423074,-47.3695892537413,
-1143.81709558824));
#154174=CARTESIAN_POINT('Ctrl Pts',(-22.7405155035463,-45.6691115795981,
-1145.31121323529));
#154175=CARTESIAN_POINT('Ctrl Pts',(-26.7427538741697,-43.1910304950644,
-1146.80533088235));
#154176=CARTESIAN_POINT('Ctrl Pts',(-30.744992244793,-40.7129494105307,
-1148.29944852941));
#154177=CARTESIAN_POINT('Ctrl Pts',(-34.2237386972451,-37.5416529948095,
-1149.79356617647));
#154178=CARTESIAN_POINT('Ctrl Pts',(-37.7024851496972,-34.3703565790883,
-1151.28768382353));
#154179=CARTESIAN_POINT('Ctrl Pts',(-40.5392751458362,-30.6138395280662,
-1152.78180147059));
#154180=CARTESIAN_POINT('Ctrl Pts',(-43.3760651419751,-26.8573224770441,
-1154.27591911765));
#154181=CARTESIAN_POINT('Ctrl Pts',(-45.4742952008371,-22.6435084734481,
-1155.77003676471));
#154182=CARTESIAN_POINT('Ctrl Pts',(-47.5725252596992,-18.4296944698521,
-1157.26415441177));
#154183=CARTESIAN_POINT('Ctrl Pts',(-48.8607426731792,-13.9020798956618,
-1158.75827205882));
#154184=CARTESIAN_POINT('Ctrl Pts',(-50.1489600866593,-9.37446532147148,
-1160.25238970588));
#154185=CARTESIAN_POINT('Ctrl Pts',(-50.5832961557877,-4.68723266073574,
-1161.74650735294));
#154186=CARTESIAN_POINT('Ctrl Pts',(-51.0176322249162,-3.12392900021603E-15,
-1163.240625));
#154187=CARTESIAN_POINT('Ctrl Pts',(-50.5832961557877,4.68723266073573,
-1164.73474264706));
#154188=CARTESIAN_POINT('Ctrl Pts',(-50.1489600866593,9.37446532147149,
-1166.22886029412));
#154189=CARTESIAN_POINT('Ctrl Pts',(-48.8607426731792,13.9020798956618,
-1167.72297794118));
#154190=CARTESIAN_POINT('Ctrl Pts',(-47.5725252596992,18.4296944698521,
-1169.21709558824));
#154191=CARTESIAN_POINT('Ctrl Pts',(-45.4742952008371,22.6435084734481,
-1170.71121323529));
#154192=CARTESIAN_POINT('Ctrl Pts',(-43.3760651419751,26.8573224770442,
-1172.20533088235));
#154193=CARTESIAN_POINT('Ctrl Pts',(-40.5392751458362,30.6138395280662,
-1173.69944852941));
#154194=CARTESIAN_POINT('Ctrl Pts',(-37.7024851496972,34.3703565790883,
-1175.19356617647));
#154195=CARTESIAN_POINT('Ctrl Pts',(-34.2237386972451,37.5416529948095,
-1176.68768382353));
#154196=CARTESIAN_POINT('Ctrl Pts',(-30.744992244793,40.7129494105307,-1178.18180147059));
#154197=CARTESIAN_POINT('Ctrl Pts',(-26.7427538741697,43.1910304950644,
-1179.67591911765));
#154198=CARTESIAN_POINT('Ctrl Pts',(-22.7405155035463,45.6691115795981,
-1181.17003676471));
#154199=CARTESIAN_POINT('Ctrl Pts',(-18.3510766423074,47.3695892537413,
-1182.66415441176));
#154200=CARTESIAN_POINT('Ctrl Pts',(-13.9616377810684,49.0700669278844,
-1184.15827205882));
#154201=CARTESIAN_POINT('Ctrl Pts',(-9.33447550508177,49.9350334639422,
-1185.65238970588));
#154202=CARTESIAN_POINT('Ctrl Pts',(-4.7073132290951,50.8,-1187.14650735294));
#154203=CARTESIAN_POINT('Ctrl Pts',(-6.22120573966855E-15,50.8,-1188.640625));
#154204=CARTESIAN_POINT('Ctrl Pts',(4.70731322909511,50.8,-1190.13474264706));
#154205=CARTESIAN_POINT('Ctrl Pts',(9.33447550508176,49.9350334639422,-1191.62886029412));
#154206=CARTESIAN_POINT('Ctrl Pts',(13.9616377810684,49.0700669278844,-1193.12297794118));
#154207=CARTESIAN_POINT('Ctrl Pts',(18.3510766423074,47.3695892537413,-1194.61709558824));
#154208=CARTESIAN_POINT('Ctrl Pts',(22.7405155035463,45.6691115795981,-1196.11121323529));
#154209=CARTESIAN_POINT('Ctrl Pts',(26.7427538741697,43.1910304950644,-1197.60533088235));
#154210=CARTESIAN_POINT('Ctrl Pts',(30.744992244793,40.7129494105307,-1199.09944852941));
#154211=CARTESIAN_POINT('Ctrl Pts',(34.2237386972451,37.5416529948095,-1200.59356617647));
#154212=CARTESIAN_POINT('Ctrl Pts',(37.7024851496972,34.3703565790883,-1202.08768382353));
#154213=CARTESIAN_POINT('Ctrl Pts',(40.5392751458362,30.6138395280662,-1203.58180147059));
#154214=CARTESIAN_POINT('Ctrl Pts',(43.3760651419751,26.8573224770442,-1205.07591911765));
#154215=CARTESIAN_POINT('Ctrl Pts',(45.4742952008372,22.6435084734481,-1206.57003676471));
#154216=CARTESIAN_POINT('Ctrl Pts',(47.5725252596992,18.4296944698521,-1208.06415441176));
#154217=CARTESIAN_POINT('Ctrl Pts',(48.8607426731792,13.9020798956618,-1209.55827205882));
#154218=CARTESIAN_POINT('Ctrl Pts',(50.1489600866593,9.37446532147146,-1211.05238970588));
#154219=CARTESIAN_POINT('Ctrl Pts',(50.5832961557877,4.68723266073574,-1212.54650735294));
#154220=CARTESIAN_POINT('Ctrl Pts',(51.0176322249162,9.37178700064808E-15,
-1214.040625));
#154221=CARTESIAN_POINT('Ctrl Pts',(50.5832961557877,-4.68723266073572,
-1215.53474264706));
#154222=CARTESIAN_POINT('Ctrl Pts',(50.1489600866593,-9.37446532147149,
-1217.02886029412));
#154223=CARTESIAN_POINT('Ctrl Pts',(48.8607426731792,-13.9020798956618,
-1218.52297794118));
#154224=CARTESIAN_POINT('Ctrl Pts',(47.5725252596992,-18.4296944698521,
-1220.01709558824));
#154225=CARTESIAN_POINT('Ctrl Pts',(45.4742952008371,-22.6435084734482,
-1221.51121323529));
#154226=CARTESIAN_POINT('Ctrl Pts',(43.3760651419751,-26.8573224770441,
-1223.00533088235));
#154227=CARTESIAN_POINT('Ctrl Pts',(40.5392751458362,-30.6138395280662,
-1224.49944852941));
#154228=CARTESIAN_POINT('Ctrl Pts',(37.7024851496972,-34.3703565790883,
-1225.99356617647));
#154229=CARTESIAN_POINT('Ctrl Pts',(34.2237386972451,-37.5416529948095,
-1227.48768382353));
#154230=CARTESIAN_POINT('Ctrl Pts',(30.744992244793,-40.7129494105307,-1228.98180147059));
#154231=CARTESIAN_POINT('Ctrl Pts',(26.7427538741697,-43.1910304950644,
-1230.47591911765));
#154232=CARTESIAN_POINT('Ctrl Pts',(22.7405155035463,-45.6691115795981,
-1231.97003676471));
#154233=CARTESIAN_POINT('Ctrl Pts',(18.3510766423074,-47.3695892537413,
-1233.46415441176));
#154234=CARTESIAN_POINT('Ctrl Pts',(13.9616377810684,-49.0700669278844,
-1234.95827205882));
#154235=CARTESIAN_POINT('Ctrl Pts',(9.33447550508176,-49.9350334639422,
-1236.45238970588));
#154236=CARTESIAN_POINT('Ctrl Pts',(4.70731322909511,-50.8,-1237.94650735294));
#154237=CARTESIAN_POINT('Ctrl Pts',(0.,-50.8,-1239.440625));
#154238=CARTESIAN_POINT('Ctrl Pts',(-4.70731322909511,-50.8,-1240.93474264706));
#154239=CARTESIAN_POINT('Ctrl Pts',(-9.33447550508177,-49.9350334639422,
-1242.42886029412));
#154240=CARTESIAN_POINT('Ctrl Pts',(-13.9616377810684,-49.0700669278844,
-1243.92297794118));
#154241=CARTESIAN_POINT('Ctrl Pts',(-18.3510766423074,-47.3695892537413,
-1245.41709558824));
#154242=CARTESIAN_POINT('Ctrl Pts',(-22.7405155035463,-45.6691115795981,
-1246.91121323529));
#154243=CARTESIAN_POINT('Ctrl Pts',(-26.7427538741697,-43.1910304950644,
-1248.40533088235));
#154244=CARTESIAN_POINT('Ctrl Pts',(-30.744992244793,-40.7129494105307,
-1249.89944852941));
#154245=CARTESIAN_POINT('Ctrl Pts',(-34.2237386972451,-37.5416529948095,
-1251.39356617647));
#154246=CARTESIAN_POINT('Ctrl Pts',(-37.7024851496972,-34.3703565790883,
-1252.88768382353));
#154247=CARTESIAN_POINT('Ctrl Pts',(-40.5392751458362,-30.6138395280662,
-1254.38180147059));
#154248=CARTESIAN_POINT('Ctrl Pts',(-43.3760651419751,-26.8573224770441,
-1255.87591911765));
#154249=CARTESIAN_POINT('Ctrl Pts',(-45.4742952008371,-22.6435084734481,
-1257.37003676471));
#154250=CARTESIAN_POINT('Ctrl Pts',(-47.5725252596992,-18.4296944698521,
-1258.86415441177));
#154251=CARTESIAN_POINT('Ctrl Pts',(-48.8607426731792,-13.9020798956618,
-1260.35827205882));
#154252=CARTESIAN_POINT('Ctrl Pts',(-50.1489600866593,-9.37446532147148,
-1261.85238970588));
#154253=CARTESIAN_POINT('Ctrl Pts',(-50.5832961557877,-4.68723266073574,
-1263.34650735294));
#154254=CARTESIAN_POINT('Ctrl Pts',(-51.0176322249162,-3.12392900021603E-15,
-1264.840625));
#154255=CARTESIAN_POINT('Ctrl Pts',(-50.5832961557877,4.68723266073573,
-1266.33474264706));
#154256=CARTESIAN_POINT('Ctrl Pts',(-50.1489600866593,9.37446532147149,
-1267.82886029412));
#154257=CARTESIAN_POINT('Ctrl Pts',(-48.8607426731792,13.9020798956618,
-1269.32297794118));
#154258=CARTESIAN_POINT('Ctrl Pts',(-47.5725252596992,18.4296944698521,
-1270.81709558824));
#154259=CARTESIAN_POINT('Ctrl Pts',(-45.4742952008371,22.6435084734481,
-1272.31121323529));
#154260=CARTESIAN_POINT('Ctrl Pts',(-43.3760651419751,26.8573224770442,
-1273.80533088235));
#154261=CARTESIAN_POINT('Ctrl Pts',(-40.5392751458362,30.6138395280662,
-1275.29944852941));
#154262=CARTESIAN_POINT('Ctrl Pts',(-37.7024851496972,34.3703565790883,
-1276.79356617647));
#154263=CARTESIAN_POINT('Ctrl Pts',(-34.2237386972451,37.5416529948095,
-1278.28768382353));
#154264=CARTESIAN_POINT('Ctrl Pts',(-30.744992244793,40.7129494105307,-1279.78180147059));
#154265=CARTESIAN_POINT('Ctrl Pts',(-26.7427538741697,43.1910304950644,
-1281.27591911765));
#154266=CARTESIAN_POINT('Ctrl Pts',(-22.7405155035463,45.6691115795981,
-1282.77003676471));
#154267=CARTESIAN_POINT('Ctrl Pts',(-18.3510766423074,47.3695892537413,
-1284.26415441176));
#154268=CARTESIAN_POINT('Ctrl Pts',(-13.9616377810684,49.0700669278844,
-1285.75827205882));
#154269=CARTESIAN_POINT('Ctrl Pts',(-9.33447550508177,49.9350334639422,
-1287.25238970588));
#154270=CARTESIAN_POINT('Ctrl Pts',(-4.7073132290951,50.8,-1288.74650735294));
#154271=CARTESIAN_POINT('Ctrl Pts',(-6.22120573966855E-15,50.8,-1290.240625));
#154272=CARTESIAN_POINT('Ctrl Pts',(4.70731322909511,50.8,-1291.73474264706));
#154273=CARTESIAN_POINT('Ctrl Pts',(9.33447550508176,49.9350334639422,-1293.22886029412));
#154274=CARTESIAN_POINT('Ctrl Pts',(13.9616377810684,49.0700669278844,-1294.72297794118));
#154275=CARTESIAN_POINT('Ctrl Pts',(18.3510766423074,47.3695892537413,-1296.21709558824));
#154276=CARTESIAN_POINT('Ctrl Pts',(22.7405155035463,45.6691115795981,-1297.71121323529));
#154277=CARTESIAN_POINT('Ctrl Pts',(26.7427538741697,43.1910304950644,-1299.20533088235));
#154278=CARTESIAN_POINT('Ctrl Pts',(30.744992244793,40.7129494105307,-1300.69944852941));
#154279=CARTESIAN_POINT('Ctrl Pts',(34.2237386972451,37.5416529948095,-1302.19356617647));
#154280=CARTESIAN_POINT('Ctrl Pts',(37.7024851496972,34.3703565790883,-1303.68768382353));
#154281=CARTESIAN_POINT('Ctrl Pts',(40.5392751458362,30.6138395280662,-1305.18180147059));
#154282=CARTESIAN_POINT('Ctrl Pts',(43.3760651419751,26.8573224770442,-1306.67591911765));
#154283=CARTESIAN_POINT('Ctrl Pts',(45.4742952008372,22.6435084734481,-1308.17003676471));
#154284=CARTESIAN_POINT('Ctrl Pts',(47.5725252596992,18.4296944698521,-1309.66415441177));
#154285=CARTESIAN_POINT('Ctrl Pts',(48.8607426731792,13.9020798956618,-1311.15827205882));
#154286=CARTESIAN_POINT('Ctrl Pts',(50.1489600866593,9.37446532147146,-1312.65238970588));
#154287=CARTESIAN_POINT('Ctrl Pts',(50.5832961557877,4.68723266073574,-1314.14650735294));
#154288=CARTESIAN_POINT('Ctrl Pts',(51.0176322249162,9.37178700064808E-15,
-1315.640625));
#154289=CARTESIAN_POINT('Ctrl Pts',(50.5832961557877,-4.68723266073572,
-1317.13474264706));
#154290=CARTESIAN_POINT('Ctrl Pts',(50.1489600866593,-9.37446532147149,
-1318.62886029412));
#154291=CARTESIAN_POINT('Ctrl Pts',(48.8607426731792,-13.9020798956618,
-1320.12297794118));
#154292=CARTESIAN_POINT('Ctrl Pts',(47.5725252596992,-18.4296944698521,
-1321.61709558824));
#154293=CARTESIAN_POINT('Ctrl Pts',(45.4742952008371,-22.6435084734482,
-1323.11121323529));
#154294=CARTESIAN_POINT('Ctrl Pts',(43.3760651419751,-26.8573224770441,
-1324.60533088235));
#154295=CARTESIAN_POINT('Ctrl Pts',(40.5392751458362,-30.6138395280662,
-1326.09944852941));
#154296=CARTESIAN_POINT('Ctrl Pts',(37.7024851496972,-34.3703565790883,
-1327.59356617647));
#154297=CARTESIAN_POINT('Ctrl Pts',(34.2237386972451,-37.5416529948095,
-1329.08768382353));
#154298=CARTESIAN_POINT('Ctrl Pts',(30.744992244793,-40.7129494105307,-1330.58180147059));
#154299=CARTESIAN_POINT('Ctrl Pts',(26.7427538741697,-43.1910304950644,
-1332.07591911765));
#154300=CARTESIAN_POINT('Ctrl Pts',(22.7405155035463,-45.6691115795981,
-1333.57003676471));
#154301=CARTESIAN_POINT('Ctrl Pts',(18.3510766423074,-47.3695892537413,
-1335.06415441176));
#154302=CARTESIAN_POINT('Ctrl Pts',(13.9616377810684,-49.0700669278844,
-1336.55827205882));
#154303=CARTESIAN_POINT('Ctrl Pts',(9.33447550508176,-49.9350334639422,
-1338.05238970588));
#154304=CARTESIAN_POINT('Ctrl Pts',(4.70731322909511,-50.8,-1339.54650735294));
#154305=CARTESIAN_POINT('Ctrl Pts',(0.,-50.8,-1341.040625));
#154306=CARTESIAN_POINT('Ctrl Pts',(-4.70731322909511,-50.8,-1342.53474264706));
#154307=CARTESIAN_POINT('Ctrl Pts',(-9.33447550508177,-49.9350334639422,
-1344.02886029412));
#154308=CARTESIAN_POINT('Ctrl Pts',(-13.9616377810684,-49.0700669278844,
-1345.52297794118));
#154309=CARTESIAN_POINT('Ctrl Pts',(-18.3510766423074,-47.3695892537413,
-1347.01709558824));
#154310=CARTESIAN_POINT('Ctrl Pts',(-22.7405155035463,-45.6691115795981,
-1348.51121323529));
#154311=CARTESIAN_POINT('Ctrl Pts',(-26.7427538741697,-43.1910304950644,
-1350.00533088235));
#154312=CARTESIAN_POINT('Ctrl Pts',(-30.744992244793,-40.7129494105307,
-1351.49944852941));
#154313=CARTESIAN_POINT('Ctrl Pts',(-34.2237386972451,-37.5416529948095,
-1352.99356617647));
#154314=CARTESIAN_POINT('Ctrl Pts',(-37.7024851496972,-34.3703565790883,
-1354.48768382353));
#154315=CARTESIAN_POINT('Ctrl Pts',(-40.5392751458362,-30.6138395280662,
-1355.98180147059));
#154316=CARTESIAN_POINT('Ctrl Pts',(-43.3760651419751,-26.8573224770441,
-1357.47591911765));
#154317=CARTESIAN_POINT('Ctrl Pts',(-45.4742952008371,-22.6435084734481,
-1358.97003676471));
#154318=CARTESIAN_POINT('Ctrl Pts',(-47.5725252596992,-18.4296944698521,
-1360.46415441177));
#154319=CARTESIAN_POINT('Ctrl Pts',(-48.8607426731792,-13.9020798956618,
-1361.95827205882));
#154320=CARTESIAN_POINT('Ctrl Pts',(-50.1489600866593,-9.37446532147148,
-1363.45238970588));
#154321=CARTESIAN_POINT('Ctrl Pts',(-50.5832961557877,-4.68723266073574,
-1364.94650735294));
#154322=CARTESIAN_POINT('Ctrl Pts',(-51.0176322249162,-3.12392900021603E-15,
-1366.440625));
#154323=CARTESIAN_POINT('Ctrl Pts',(-50.5832961557877,4.68723266073573,
-1367.93474264706));
#154324=CARTESIAN_POINT('Ctrl Pts',(-50.1489600866593,9.37446532147149,
-1369.42886029412));
#154325=CARTESIAN_POINT('Ctrl Pts',(-48.8607426731792,13.9020798956618,
-1370.92297794118));
#154326=CARTESIAN_POINT('Ctrl Pts',(-47.5725252596992,18.4296944698521,
-1372.41709558824));
#154327=CARTESIAN_POINT('Ctrl Pts',(-45.4742952008371,22.6435084734481,
-1373.91121323529));
#154328=CARTESIAN_POINT('Ctrl Pts',(-43.3760651419751,26.8573224770442,
-1375.40533088235));
#154329=CARTESIAN_POINT('Ctrl Pts',(-40.5392751458362,30.6138395280662,
-1376.89944852941));
#154330=CARTESIAN_POINT('Ctrl Pts',(-37.7024851496972,34.3703565790883,
-1378.39356617647));
#154331=CARTESIAN_POINT('Ctrl Pts',(-34.2237386972451,37.5416529948095,
-1379.88768382353));
#154332=CARTESIAN_POINT('Ctrl Pts',(-30.744992244793,40.7129494105307,-1381.38180147059));
#154333=CARTESIAN_POINT('Ctrl Pts',(-26.7427538741697,43.1910304950644,
-1382.87591911765));
#154334=CARTESIAN_POINT('Ctrl Pts',(-22.7405155035463,45.6691115795981,
-1384.37003676471));
#154335=CARTESIAN_POINT('Ctrl Pts',(-18.3510766423074,47.3695892537413,
-1385.86415441176));
#154336=CARTESIAN_POINT('Ctrl Pts',(-13.9616377810684,49.0700669278844,
-1387.35827205882));
#154337=CARTESIAN_POINT('Ctrl Pts',(-9.33447550508177,49.9350334639422,
-1388.85238970588));
#154338=CARTESIAN_POINT('Ctrl Pts',(-4.7073132290951,50.8,-1390.34650735294));
#154339=CARTESIAN_POINT('Ctrl Pts',(-6.22120573966855E-15,50.8,-1391.840625));
#154340=CARTESIAN_POINT('Ctrl Pts',(4.70731322909511,50.8,-1393.33474264706));
#154341=CARTESIAN_POINT('Ctrl Pts',(9.33447550508176,49.9350334639422,-1394.82886029412));
#154342=CARTESIAN_POINT('Ctrl Pts',(13.9616377810684,49.0700669278844,-1396.32297794118));
#154343=CARTESIAN_POINT('Ctrl Pts',(18.3510766423074,47.3695892537413,-1397.81709558824));
#154344=CARTESIAN_POINT('Ctrl Pts',(22.7405155035463,45.6691115795981,-1399.31121323529));
#154345=CARTESIAN_POINT('Ctrl Pts',(26.7427538741697,43.1910304950644,-1400.80533088235));
#154346=CARTESIAN_POINT('Ctrl Pts',(30.744992244793,40.7129494105307,-1402.29944852941));
#154347=CARTESIAN_POINT('Ctrl Pts',(34.2237386972451,37.5416529948095,-1403.79356617647));
#154348=CARTESIAN_POINT('Ctrl Pts',(37.7024851496972,34.3703565790883,-1405.28768382353));
#154349=CARTESIAN_POINT('Ctrl Pts',(40.5392751458362,30.6138395280662,-1406.78180147059));
#154350=CARTESIAN_POINT('Ctrl Pts',(43.3760651419751,26.8573224770442,-1408.27591911765));
#154351=CARTESIAN_POINT('Ctrl Pts',(45.4742952008372,22.6435084734481,-1409.77003676471));
#154352=CARTESIAN_POINT('Ctrl Pts',(47.5725252596992,18.4296944698521,-1411.26415441176));
#154353=CARTESIAN_POINT('Ctrl Pts',(48.8607426731792,13.9020798956618,-1412.75827205882));
#154354=CARTESIAN_POINT('Ctrl Pts',(50.1489600866593,9.37446532147146,-1414.25238970588));
#154355=CARTESIAN_POINT('Ctrl Pts',(50.5832961557877,4.68723266073574,-1415.74650735294));
#154356=CARTESIAN_POINT('Ctrl Pts',(51.0176322249162,9.37178700064808E-15,
-1417.240625));
#154357=CARTESIAN_POINT('Ctrl Pts',(50.5832961557877,-4.68723266073572,
-1418.73474264706));
#154358=CARTESIAN_POINT('Ctrl Pts',(50.1489600866593,-9.37446532147149,
-1420.22886029412));
#154359=CARTESIAN_POINT('Ctrl Pts',(48.8607426731792,-13.9020798956618,
-1421.72297794118));
#154360=CARTESIAN_POINT('Ctrl Pts',(47.5725252596992,-18.4296944698521,
-1423.21709558824));
#154361=CARTESIAN_POINT('Ctrl Pts',(45.4742952008371,-22.6435084734482,
-1424.71121323529));
#154362=CARTESIAN_POINT('Ctrl Pts',(43.3760651419751,-26.8573224770441,
-1426.20533088235));
#154363=CARTESIAN_POINT('Ctrl Pts',(40.5392751458362,-30.6138395280662,
-1427.69944852941));
#154364=CARTESIAN_POINT('Ctrl Pts',(37.7024851496972,-34.3703565790883,
-1429.19356617647));
#154365=CARTESIAN_POINT('Ctrl Pts',(34.2237386972451,-37.5416529948095,
-1430.68768382353));
#154366=CARTESIAN_POINT('Ctrl Pts',(30.744992244793,-40.7129494105307,-1432.18180147059));
#154367=CARTESIAN_POINT('Ctrl Pts',(26.7427538741697,-43.1910304950644,
-1433.67591911765));
#154368=CARTESIAN_POINT('Ctrl Pts',(22.7405155035463,-45.6691115795981,
-1435.17003676471));
#154369=CARTESIAN_POINT('Ctrl Pts',(18.3510766423074,-47.3695892537413,
-1436.66415441176));
#154370=CARTESIAN_POINT('Ctrl Pts',(13.9616377810684,-49.0700669278844,
-1438.15827205882));
#154371=CARTESIAN_POINT('Ctrl Pts',(9.33447550508176,-49.9350334639422,
-1439.65238970588));
#154372=CARTESIAN_POINT('Ctrl Pts',(4.70731322909511,-50.8,-1441.14650735294));
#154373=CARTESIAN_POINT('Ctrl Pts',(0.,-50.8,-1442.640625));
#154374=CARTESIAN_POINT('Ctrl Pts',(-4.70731322909511,-50.8,-1444.13474264706));
#154375=CARTESIAN_POINT('Ctrl Pts',(-9.33447550508177,-49.9350334639422,
-1445.62886029412));
#154376=CARTESIAN_POINT('Ctrl Pts',(-13.9616377810684,-49.0700669278844,
-1447.12297794118));
#154377=CARTESIAN_POINT('Ctrl Pts',(-18.3510766423074,-47.3695892537413,
-1448.61709558824));
#154378=CARTESIAN_POINT('Ctrl Pts',(-22.7405155035463,-45.6691115795981,
-1450.11121323529));
#154379=CARTESIAN_POINT('Ctrl Pts',(-26.7427538741697,-43.1910304950644,
-1451.60533088235));
#154380=CARTESIAN_POINT('Ctrl Pts',(-30.744992244793,-40.7129494105307,
-1453.09944852941));
#154381=CARTESIAN_POINT('Ctrl Pts',(-34.2237386972451,-37.5416529948095,
-1454.59356617647));
#154382=CARTESIAN_POINT('Ctrl Pts',(-37.7024851496972,-34.3703565790883,
-1456.08768382353));
#154383=CARTESIAN_POINT('Ctrl Pts',(-40.5392751458362,-30.6138395280662,
-1457.58180147059));
#154384=CARTESIAN_POINT('Ctrl Pts',(-43.3760651419751,-26.8573224770441,
-1459.07591911765));
#154385=CARTESIAN_POINT('Ctrl Pts',(-45.4742952008371,-22.6435084734481,
-1460.57003676471));
#154386=CARTESIAN_POINT('Ctrl Pts',(-47.5725252596992,-18.4296944698521,
-1462.06415441176));
#154387=CARTESIAN_POINT('Ctrl Pts',(-48.8607426731792,-13.9020798956618,
-1463.55827205882));
#154388=CARTESIAN_POINT('Ctrl Pts',(-50.1489600866593,-9.37446532147148,
-1465.05238970588));
#154389=CARTESIAN_POINT('Ctrl Pts',(-50.5832961557877,-4.68723266073574,
-1466.54650735294));
#154390=CARTESIAN_POINT('Ctrl Pts',(-51.0176322249162,-3.12392900021603E-15,
-1468.040625));
#154391=CARTESIAN_POINT('Ctrl Pts',(-50.5832961557877,4.68723266073573,
-1469.53474264706));
#154392=CARTESIAN_POINT('Ctrl Pts',(-50.1489600866593,9.37446532147149,
-1471.02886029412));
#154393=CARTESIAN_POINT('Ctrl Pts',(-48.8607426731792,13.9020798956618,
-1472.52297794118));
#154394=CARTESIAN_POINT('Ctrl Pts',(-47.5725252596992,18.4296944698521,
-1474.01709558824));
#154395=CARTESIAN_POINT('Ctrl Pts',(-45.4742952008371,22.6435084734481,
-1475.51121323529));
#154396=CARTESIAN_POINT('Ctrl Pts',(-43.3760651419751,26.8573224770442,
-1477.00533088235));
#154397=CARTESIAN_POINT('Ctrl Pts',(-40.5392751458362,30.6138395280662,
-1478.49944852941));
#154398=CARTESIAN_POINT('Ctrl Pts',(-37.7024851496972,34.3703565790883,
-1479.99356617647));
#154399=CARTESIAN_POINT('Ctrl Pts',(-34.2237386972451,37.5416529948095,
-1481.48768382353));
#154400=CARTESIAN_POINT('Ctrl Pts',(-30.744992244793,40.7129494105307,-1482.98180147059));
#154401=CARTESIAN_POINT('Ctrl Pts',(-26.7427538741697,43.1910304950644,
-1484.47591911765));
#154402=CARTESIAN_POINT('Ctrl Pts',(-22.7405155035463,45.6691115795981,
-1485.97003676471));
#154403=CARTESIAN_POINT('Ctrl Pts',(-18.3510766423074,47.3695892537413,
-1487.46415441176));
#154404=CARTESIAN_POINT('Ctrl Pts',(-13.9616377810684,49.0700669278844,
-1488.95827205882));
#154405=CARTESIAN_POINT('Ctrl Pts',(-9.33447550508177,49.9350334639422,
-1490.45238970588));
#154406=CARTESIAN_POINT('Ctrl Pts',(-4.7073132290951,50.8,-1491.94650735294));
#154407=CARTESIAN_POINT('Ctrl Pts',(-6.22120573966855E-15,50.8,-1493.440625));
#154408=CARTESIAN_POINT('Ctrl Pts',(4.70731322909511,50.8,-1494.93474264706));
#154409=CARTESIAN_POINT('Ctrl Pts',(9.33447550508176,49.9350334639422,-1496.42886029412));
#154410=CARTESIAN_POINT('Ctrl Pts',(13.9616377810684,49.0700669278844,-1497.92297794118));
#154411=CARTESIAN_POINT('Ctrl Pts',(18.3510766423074,47.3695892537413,-1499.41709558824));
#154412=CARTESIAN_POINT('Ctrl Pts',(21.2265761645012,46.2556148041416,-1500.39588461254));
#154413=CARTESIAN_POINT('Ctrl Pts',(23.9462138071277,44.8019959857072,-1501.3784575767));
#154414=CARTESIAN_POINT('',(-0.0544255098126717,-18.0479179370885,692.));
#154415=CARTESIAN_POINT('Ctrl Pts',(1.56487907968285,-38.9685918845674,
692.));
#154416=CARTESIAN_POINT('Ctrl Pts',(1.14513258304983,-35.4925583907916,
692.));
#154417=CARTESIAN_POINT('Ctrl Pts',(0.79988902048975,-32.0079330910613,
692.000000000004));
#154418=CARTESIAN_POINT('Ctrl Pts',(0.259957461376307,-25.0319090278082,
692.000000000004));
#154419=CARTESIAN_POINT('Ctrl Pts',(0.0649945143077899,-21.5401136171893,
692.));
#154420=CARTESIAN_POINT('Ctrl Pts',(-0.0544255098127947,-18.0479179370885,
692.));
#154421=CARTESIAN_POINT('',(0.,-18.048,1504.84863058659));
#154422=CARTESIAN_POINT('Ctrl Pts',(-2.21024254310115E-15,18.048,742.848630586592));
#154423=CARTESIAN_POINT('Ctrl Pts',(1.67239348737616,18.048,741.354512939533));
#154424=CARTESIAN_POINT('Ctrl Pts',(3.31631129755346,17.7406985030951,739.860395292475));
#154425=CARTESIAN_POINT('Ctrl Pts',(4.96022910773077,17.4333970061901,738.366277645416));
#154426=CARTESIAN_POINT('Ctrl Pts',(6.51968959134575,16.8292587962898,736.872159998357));
#154427=CARTESIAN_POINT('Ctrl Pts',(8.07915007496071,16.2251205863895,735.378042351298));
#154428=CARTESIAN_POINT('Ctrl Pts',(9.50104767561053,15.3447188656481,733.883924704239));
#154429=CARTESIAN_POINT('Ctrl Pts',(10.9229452762603,14.4643171449067,732.389807057181));
#154430=CARTESIAN_POINT('Ctrl Pts',(12.1588589765331,13.3376329379985,730.895689410122));
#154431=CARTESIAN_POINT('Ctrl Pts',(13.3947726768058,12.2109487310903,729.401571763063));
#154432=CARTESIAN_POINT('Ctrl Pts',(14.4026149179538,10.8763499173728,727.907454116004));
#154433=CARTESIAN_POINT('Ctrl Pts',(15.4104571591017,9.54175110365539,726.413336468945));
#154434=CARTESIAN_POINT('Ctrl Pts',(16.1559070823762,8.04468584505496,724.919218821886));
#154435=CARTESIAN_POINT('Ctrl Pts',(16.9013570056506,6.54762058645456,723.425101174828));
#154436=CARTESIAN_POINT('Ctrl Pts',(17.3590292079831,4.93906964482096,721.930983527769));
#154437=CARTESIAN_POINT('Ctrl Pts',(17.8167014103155,3.33051870318735,720.43686588071));
#154438=CARTESIAN_POINT('Ctrl Pts',(17.9710104137728,1.66525935159367,718.942748233651));
#154439=CARTESIAN_POINT('Ctrl Pts',(18.1253194172301,3.32956716117513E-15,
717.448630586592));
#154440=CARTESIAN_POINT('Ctrl Pts',(17.9710104137728,-1.66525935159367,
715.954512939534));
#154441=CARTESIAN_POINT('Ctrl Pts',(17.8167014103155,-3.33051870318736,
714.460395292475));
#154442=CARTESIAN_POINT('Ctrl Pts',(17.3590292079831,-4.93906964482095,
712.966277645416));
#154443=CARTESIAN_POINT('Ctrl Pts',(16.9013570056506,-6.54762058645456,
711.472159998357));
#154444=CARTESIAN_POINT('Ctrl Pts',(16.1559070823762,-8.04468584505497,
709.978042351298));
#154445=CARTESIAN_POINT('Ctrl Pts',(15.4104571591017,-9.54175110365538,
708.483924704239));
#154446=CARTESIAN_POINT('Ctrl Pts',(14.4026149179538,-10.8763499173728,
706.989807057181));
#154447=CARTESIAN_POINT('Ctrl Pts',(13.3947726768058,-12.2109487310903,
705.495689410122));
#154448=CARTESIAN_POINT('Ctrl Pts',(12.1588589765331,-13.3376329379985,
704.001571763063));
#154449=CARTESIAN_POINT('Ctrl Pts',(10.9229452762603,-14.4643171449067,
702.507454116004));
#154450=CARTESIAN_POINT('Ctrl Pts',(9.50104767561053,-15.3447188656481,
701.013336468945));
#154451=CARTESIAN_POINT('Ctrl Pts',(8.07915007496071,-16.2251205863895,
699.519218821886));
#154452=CARTESIAN_POINT('Ctrl Pts',(6.51968959134574,-16.8292587962898,
698.025101174828));
#154453=CARTESIAN_POINT('Ctrl Pts',(4.96022910773078,-17.4333970061901,
696.530983527769));
#154454=CARTESIAN_POINT('Ctrl Pts',(3.31631129755346,-17.7406985030951,
695.03686588071));
#154455=CARTESIAN_POINT('Ctrl Pts',(1.67239348737615,-18.048,693.542748233651));
#154456=CARTESIAN_POINT('Ctrl Pts',(0.,-18.048,692.048630586592));
#154457=CARTESIAN_POINT('Ctrl Pts',(-0.0272128167736711,-18.048,692.024318634845));
#154458=CARTESIAN_POINT('Ctrl Pts',(-0.0544255098126717,-18.0479179370885,
692.000000000001));
#154459=CARTESIAN_POINT('Ctrl Pts',(0.,-15.,1504.95));
#154460=CARTESIAN_POINT('Ctrl Pts',(-1.38995469363045,-15.,1503.45588235294));
#154461=CARTESIAN_POINT('Ctrl Pts',(-2.75624276724856,-14.7445964952585,
1501.96176470588));
#154462=CARTESIAN_POINT('Ctrl Pts',(-4.12253084086666,-14.4891929905171,
1500.46764705882));
#154463=CARTESIAN_POINT('Ctrl Pts',(-5.41862499280729,-13.9870834410653,
1498.97352941176));
#154464=CARTESIAN_POINT('Ctrl Pts',(-6.71471914474793,-13.4849738916136,
1497.47941176471));
#154465=CARTESIAN_POINT('Ctrl Pts',(-7.89648244316034,-12.7532570359442,
1495.98529411765));
#154466=CARTESIAN_POINT('Ctrl Pts',(-9.07824574157275,-12.0215401802748,
1494.49117647059));
#154467=CARTESIAN_POINT('Ctrl Pts',(-10.1054346546984,-11.0851337583099,
1492.99705882353));
#154468=CARTESIAN_POINT('Ctrl Pts',(-11.132623567824,-10.148727336345,1491.50294117647));
#154469=CARTESIAN_POINT('Ctrl Pts',(-11.9702584092036,-9.03951954568885,
1490.00882352941));
#154470=CARTESIAN_POINT('Ctrl Pts',(-12.8078932505832,-7.93031175503273,
1488.51470588235));
#154471=CARTESIAN_POINT('Ctrl Pts',(-13.4274493703259,-6.68607533664808,
1487.02058823529));
#154472=CARTESIAN_POINT('Ctrl Pts',(-14.0470054900687,-5.44183891826343,
1485.52647058824));
#154473=CARTESIAN_POINT('Ctrl Pts',(-14.4273846475923,-4.10494485108124,
1484.03235294118));
#154474=CARTESIAN_POINT('Ctrl Pts',(-14.8077638051159,-2.76805078389906,
1482.53823529412));
#154475=CARTESIAN_POINT('Ctrl Pts',(-14.9360126444255,-1.38402539194953,
1481.04411764706));
#154476=CARTESIAN_POINT('Ctrl Pts',(-15.0642614837351,-9.22419980378748E-16,
1479.55));
#154477=CARTESIAN_POINT('Ctrl Pts',(-14.9360126444255,1.38402539194953,
1478.05588235294));
#154478=CARTESIAN_POINT('Ctrl Pts',(-14.8077638051159,2.76805078389906,
1476.56176470588));
#154479=CARTESIAN_POINT('Ctrl Pts',(-14.4273846475923,4.10494485108124,
1475.06764705882));
#154480=CARTESIAN_POINT('Ctrl Pts',(-14.0470054900687,5.44183891826343,
1473.57352941176));
#154481=CARTESIAN_POINT('Ctrl Pts',(-13.4274493703259,6.68607533664807,
1472.07941176471));
#154482=CARTESIAN_POINT('Ctrl Pts',(-12.8078932505832,7.93031175503273,
1470.58529411765));
#154483=CARTESIAN_POINT('Ctrl Pts',(-11.9702584092036,9.03951954568884,
1469.09117647059));
#154484=CARTESIAN_POINT('Ctrl Pts',(-11.132623567824,10.148727336345,1467.59705882353));
#154485=CARTESIAN_POINT('Ctrl Pts',(-10.1054346546984,11.0851337583099,
1466.10294117647));
#154486=CARTESIAN_POINT('Ctrl Pts',(-9.07824574157275,12.0215401802748,
1464.60882352941));
#154487=CARTESIAN_POINT('Ctrl Pts',(-7.89648244316034,12.7532570359442,
1463.11470588235));
#154488=CARTESIAN_POINT('Ctrl Pts',(-6.71471914474793,13.4849738916136,
1461.62058823529));
#154489=CARTESIAN_POINT('Ctrl Pts',(-5.41862499280729,13.9870834410653,
1460.12647058824));
#154490=CARTESIAN_POINT('Ctrl Pts',(-4.12253084086667,14.4891929905171,
1458.63235294118));
#154491=CARTESIAN_POINT('Ctrl Pts',(-2.75624276724856,14.7445964952585,
1457.13823529412));
#154492=CARTESIAN_POINT('Ctrl Pts',(-1.38995469363044,15.,1455.64411764706));
#154493=CARTESIAN_POINT('Ctrl Pts',(-1.83697019872103E-15,15.,1454.15));
#154494=CARTESIAN_POINT('Ctrl Pts',(1.38995469363045,15.,1452.65588235294));
#154495=CARTESIAN_POINT('Ctrl Pts',(2.75624276724855,14.7445964952585,1451.16176470588));
#154496=CARTESIAN_POINT('Ctrl Pts',(4.12253084086666,14.4891929905171,1449.66764705882));
#154497=CARTESIAN_POINT('Ctrl Pts',(5.4186249928073,13.9870834410653,1448.17352941177));
#154498=CARTESIAN_POINT('Ctrl Pts',(6.71471914474792,13.4849738916136,1446.67941176471));
#154499=CARTESIAN_POINT('Ctrl Pts',(7.89648244316034,12.7532570359442,1445.18529411765));
#154500=CARTESIAN_POINT('Ctrl Pts',(9.07824574157275,12.0215401802748,1443.69117647059));
#154501=CARTESIAN_POINT('Ctrl Pts',(10.1054346546984,11.0851337583099,1442.19705882353));
#154502=CARTESIAN_POINT('Ctrl Pts',(11.132623567824,10.148727336345,1440.70294117647));
#154503=CARTESIAN_POINT('Ctrl Pts',(11.9702584092036,9.03951954568885,1439.20882352941));
#154504=CARTESIAN_POINT('Ctrl Pts',(12.8078932505832,7.93031175503273,1437.71470588235));
#154505=CARTESIAN_POINT('Ctrl Pts',(13.4274493703259,6.68607533664807,1436.22058823529));
#154506=CARTESIAN_POINT('Ctrl Pts',(14.0470054900687,5.44183891826343,1434.72647058824));
#154507=CARTESIAN_POINT('Ctrl Pts',(14.4273846475923,4.10494485108125,1433.23235294118));
#154508=CARTESIAN_POINT('Ctrl Pts',(14.8077638051159,2.76805078389905,1431.73823529412));
#154509=CARTESIAN_POINT('Ctrl Pts',(14.9360126444255,1.38402539194953,1430.24411764706));
#154510=CARTESIAN_POINT('Ctrl Pts',(15.0642614837351,2.76725994113625E-15,
1428.75));
#154511=CARTESIAN_POINT('Ctrl Pts',(14.9360126444255,-1.38402539194952,
1427.25588235294));
#154512=CARTESIAN_POINT('Ctrl Pts',(14.8077638051159,-2.76805078389906,
1425.76176470588));
#154513=CARTESIAN_POINT('Ctrl Pts',(14.4273846475923,-4.10494485108124,
1424.26764705882));
#154514=CARTESIAN_POINT('Ctrl Pts',(14.0470054900687,-5.44183891826342,
1422.77352941176));
#154515=CARTESIAN_POINT('Ctrl Pts',(13.4274493703259,-6.68607533664808,
1421.27941176471));
#154516=CARTESIAN_POINT('Ctrl Pts',(12.8078932505832,-7.93031175503273,
1419.78529411765));
#154517=CARTESIAN_POINT('Ctrl Pts',(11.9702584092036,-9.03951954568884,
1418.29117647059));
#154518=CARTESIAN_POINT('Ctrl Pts',(11.132623567824,-10.148727336345,1416.79705882353));
#154519=CARTESIAN_POINT('Ctrl Pts',(10.1054346546984,-11.0851337583099,
1415.30294117647));
#154520=CARTESIAN_POINT('Ctrl Pts',(9.07824574157275,-12.0215401802748,
1413.80882352941));
#154521=CARTESIAN_POINT('Ctrl Pts',(7.89648244316034,-12.7532570359442,
1412.31470588235));
#154522=CARTESIAN_POINT('Ctrl Pts',(6.71471914474792,-13.4849738916136,
1410.82058823529));
#154523=CARTESIAN_POINT('Ctrl Pts',(5.4186249928073,-13.9870834410653,1409.32647058824));
#154524=CARTESIAN_POINT('Ctrl Pts',(4.12253084086667,-14.4891929905171,
1407.83235294118));
#154525=CARTESIAN_POINT('Ctrl Pts',(2.75624276724855,-14.7445964952585,
1406.33823529412));
#154526=CARTESIAN_POINT('Ctrl Pts',(1.38995469363045,-15.,1404.84411764706));
#154527=CARTESIAN_POINT('Ctrl Pts',(0.,-15.,1403.35));
#154528=CARTESIAN_POINT('Ctrl Pts',(-1.38995469363045,-15.,1401.85588235294));
#154529=CARTESIAN_POINT('Ctrl Pts',(-2.75624276724856,-14.7445964952585,
1400.36176470588));
#154530=CARTESIAN_POINT('Ctrl Pts',(-4.12253084086666,-14.4891929905171,
1398.86764705882));
#154531=CARTESIAN_POINT('Ctrl Pts',(-5.41862499280729,-13.9870834410653,
1397.37352941176));
#154532=CARTESIAN_POINT('Ctrl Pts',(-6.71471914474793,-13.4849738916136,
1395.87941176471));
#154533=CARTESIAN_POINT('Ctrl Pts',(-7.89648244316034,-12.7532570359442,
1394.38529411765));
#154534=CARTESIAN_POINT('Ctrl Pts',(-9.07824574157275,-12.0215401802748,
1392.89117647059));
#154535=CARTESIAN_POINT('Ctrl Pts',(-10.1054346546984,-11.0851337583099,
1391.39705882353));
#154536=CARTESIAN_POINT('Ctrl Pts',(-11.132623567824,-10.148727336345,1389.90294117647));
#154537=CARTESIAN_POINT('Ctrl Pts',(-11.9702584092036,-9.03951954568885,
1388.40882352941));
#154538=CARTESIAN_POINT('Ctrl Pts',(-12.8078932505832,-7.93031175503273,
1386.91470588235));
#154539=CARTESIAN_POINT('Ctrl Pts',(-13.4274493703259,-6.68607533664808,
1385.42058823529));
#154540=CARTESIAN_POINT('Ctrl Pts',(-14.0470054900687,-5.44183891826343,
1383.92647058824));
#154541=CARTESIAN_POINT('Ctrl Pts',(-14.4273846475923,-4.10494485108124,
1382.43235294118));
#154542=CARTESIAN_POINT('Ctrl Pts',(-14.8077638051159,-2.76805078389906,
1380.93823529412));
#154543=CARTESIAN_POINT('Ctrl Pts',(-14.9360126444255,-1.38402539194953,
1379.44411764706));
#154544=CARTESIAN_POINT('Ctrl Pts',(-15.0642614837351,-9.22419980378748E-16,
1377.95));
#154545=CARTESIAN_POINT('Ctrl Pts',(-14.9360126444255,1.38402539194953,
1376.45588235294));
#154546=CARTESIAN_POINT('Ctrl Pts',(-14.8077638051159,2.76805078389906,
1374.96176470588));
#154547=CARTESIAN_POINT('Ctrl Pts',(-14.4273846475923,4.10494485108124,
1373.46764705882));
#154548=CARTESIAN_POINT('Ctrl Pts',(-14.0470054900687,5.44183891826343,
1371.97352941176));
#154549=CARTESIAN_POINT('Ctrl Pts',(-13.4274493703259,6.68607533664807,
1370.47941176471));
#154550=CARTESIAN_POINT('Ctrl Pts',(-12.8078932505832,7.93031175503273,
1368.98529411765));
#154551=CARTESIAN_POINT('Ctrl Pts',(-11.9702584092036,9.03951954568884,
1367.49117647059));
#154552=CARTESIAN_POINT('Ctrl Pts',(-11.132623567824,10.148727336345,1365.99705882353));
#154553=CARTESIAN_POINT('Ctrl Pts',(-10.1054346546984,11.0851337583099,
1364.50294117647));
#154554=CARTESIAN_POINT('Ctrl Pts',(-9.07824574157275,12.0215401802748,
1363.00882352941));
#154555=CARTESIAN_POINT('Ctrl Pts',(-7.89648244316034,12.7532570359442,
1361.51470588235));
#154556=CARTESIAN_POINT('Ctrl Pts',(-6.71471914474793,13.4849738916136,
1360.02058823529));
#154557=CARTESIAN_POINT('Ctrl Pts',(-5.41862499280729,13.9870834410653,
1358.52647058824));
#154558=CARTESIAN_POINT('Ctrl Pts',(-4.12253084086667,14.4891929905171,
1357.03235294118));
#154559=CARTESIAN_POINT('Ctrl Pts',(-2.75624276724856,14.7445964952585,
1355.53823529412));
#154560=CARTESIAN_POINT('Ctrl Pts',(-1.38995469363044,15.,1354.04411764706));
#154561=CARTESIAN_POINT('Ctrl Pts',(-1.83697019872103E-15,15.,1352.55));
#154562=CARTESIAN_POINT('Ctrl Pts',(1.38995469363045,15.,1351.05588235294));
#154563=CARTESIAN_POINT('Ctrl Pts',(2.75624276724855,14.7445964952585,1349.56176470588));
#154564=CARTESIAN_POINT('Ctrl Pts',(4.12253084086666,14.4891929905171,1348.06764705882));
#154565=CARTESIAN_POINT('Ctrl Pts',(5.4186249928073,13.9870834410653,1346.57352941176));
#154566=CARTESIAN_POINT('Ctrl Pts',(6.71471914474792,13.4849738916136,1345.07941176471));
#154567=CARTESIAN_POINT('Ctrl Pts',(7.89648244316034,12.7532570359442,1343.58529411765));
#154568=CARTESIAN_POINT('Ctrl Pts',(9.07824574157275,12.0215401802748,1342.09117647059));
#154569=CARTESIAN_POINT('Ctrl Pts',(10.1054346546984,11.0851337583099,1340.59705882353));
#154570=CARTESIAN_POINT('Ctrl Pts',(11.132623567824,10.148727336345,1339.10294117647));
#154571=CARTESIAN_POINT('Ctrl Pts',(11.9702584092036,9.03951954568885,1337.60882352941));
#154572=CARTESIAN_POINT('Ctrl Pts',(12.8078932505832,7.93031175503273,1336.11470588235));
#154573=CARTESIAN_POINT('Ctrl Pts',(13.4274493703259,6.68607533664807,1334.62058823529));
#154574=CARTESIAN_POINT('Ctrl Pts',(14.0470054900687,5.44183891826343,1333.12647058824));
#154575=CARTESIAN_POINT('Ctrl Pts',(14.4273846475923,4.10494485108125,1331.63235294118));
#154576=CARTESIAN_POINT('Ctrl Pts',(14.8077638051159,2.76805078389905,1330.13823529412));
#154577=CARTESIAN_POINT('Ctrl Pts',(14.9360126444255,1.38402539194953,1328.64411764706));
#154578=CARTESIAN_POINT('Ctrl Pts',(15.0642614837351,2.76725994113625E-15,
1327.15));
#154579=CARTESIAN_POINT('Ctrl Pts',(14.9360126444255,-1.38402539194952,
1325.65588235294));
#154580=CARTESIAN_POINT('Ctrl Pts',(14.8077638051159,-2.76805078389906,
1324.16176470588));
#154581=CARTESIAN_POINT('Ctrl Pts',(14.4273846475923,-4.10494485108124,
1322.66764705882));
#154582=CARTESIAN_POINT('Ctrl Pts',(14.0470054900687,-5.44183891826342,
1321.17352941176));
#154583=CARTESIAN_POINT('Ctrl Pts',(13.4274493703259,-6.68607533664808,
1319.67941176471));
#154584=CARTESIAN_POINT('Ctrl Pts',(12.8078932505832,-7.93031175503273,
1318.18529411765));
#154585=CARTESIAN_POINT('Ctrl Pts',(11.9702584092036,-9.03951954568884,
1316.69117647059));
#154586=CARTESIAN_POINT('Ctrl Pts',(11.132623567824,-10.148727336345,1315.19705882353));
#154587=CARTESIAN_POINT('Ctrl Pts',(10.1054346546984,-11.0851337583099,
1313.70294117647));
#154588=CARTESIAN_POINT('Ctrl Pts',(9.07824574157275,-12.0215401802748,
1312.20882352941));
#154589=CARTESIAN_POINT('Ctrl Pts',(7.89648244316034,-12.7532570359442,
1310.71470588235));
#154590=CARTESIAN_POINT('Ctrl Pts',(6.71471914474792,-13.4849738916136,
1309.22058823529));
#154591=CARTESIAN_POINT('Ctrl Pts',(5.4186249928073,-13.9870834410653,1307.72647058824));
#154592=CARTESIAN_POINT('Ctrl Pts',(4.12253084086667,-14.4891929905171,
1306.23235294118));
#154593=CARTESIAN_POINT('Ctrl Pts',(2.75624276724855,-14.7445964952585,
1304.73823529412));
#154594=CARTESIAN_POINT('Ctrl Pts',(1.38995469363045,-15.,1303.24411764706));
#154595=CARTESIAN_POINT('Ctrl Pts',(0.,-15.,1301.75));
#154596=CARTESIAN_POINT('Ctrl Pts',(-1.38995469363045,-15.,1300.25588235294));
#154597=CARTESIAN_POINT('Ctrl Pts',(-2.75624276724856,-14.7445964952585,
1298.76176470588));
#154598=CARTESIAN_POINT('Ctrl Pts',(-4.12253084086666,-14.4891929905171,
1297.26764705882));
#154599=CARTESIAN_POINT('Ctrl Pts',(-5.41862499280729,-13.9870834410653,
1295.77352941176));
#154600=CARTESIAN_POINT('Ctrl Pts',(-6.71471914474793,-13.4849738916136,
1294.27941176471));
#154601=CARTESIAN_POINT('Ctrl Pts',(-7.89648244316034,-12.7532570359442,
1292.78529411765));
#154602=CARTESIAN_POINT('Ctrl Pts',(-9.07824574157275,-12.0215401802748,
1291.29117647059));
#154603=CARTESIAN_POINT('Ctrl Pts',(-10.1054346546984,-11.0851337583099,
1289.79705882353));
#154604=CARTESIAN_POINT('Ctrl Pts',(-11.132623567824,-10.148727336345,1288.30294117647));
#154605=CARTESIAN_POINT('Ctrl Pts',(-11.9702584092036,-9.03951954568885,
1286.80882352941));
#154606=CARTESIAN_POINT('Ctrl Pts',(-12.8078932505832,-7.93031175503273,
1285.31470588235));
#154607=CARTESIAN_POINT('Ctrl Pts',(-13.4274493703259,-6.68607533664808,
1283.82058823529));
#154608=CARTESIAN_POINT('Ctrl Pts',(-14.0470054900687,-5.44183891826343,
1282.32647058824));
#154609=CARTESIAN_POINT('Ctrl Pts',(-14.4273846475923,-4.10494485108124,
1280.83235294118));
#154610=CARTESIAN_POINT('Ctrl Pts',(-14.8077638051159,-2.76805078389906,
1279.33823529412));
#154611=CARTESIAN_POINT('Ctrl Pts',(-14.9360126444255,-1.38402539194953,
1277.84411764706));
#154612=CARTESIAN_POINT('Ctrl Pts',(-15.0642614837351,-9.22419980378748E-16,
1276.35));
#154613=CARTESIAN_POINT('Ctrl Pts',(-14.9360126444255,1.38402539194953,
1274.85588235294));
#154614=CARTESIAN_POINT('Ctrl Pts',(-14.8077638051159,2.76805078389906,
1273.36176470588));
#154615=CARTESIAN_POINT('Ctrl Pts',(-14.4273846475923,4.10494485108124,
1271.86764705882));
#154616=CARTESIAN_POINT('Ctrl Pts',(-14.0470054900687,5.44183891826343,
1270.37352941176));
#154617=CARTESIAN_POINT('Ctrl Pts',(-13.4274493703259,6.68607533664807,
1268.87941176471));
#154618=CARTESIAN_POINT('Ctrl Pts',(-12.8078932505832,7.93031175503273,
1267.38529411765));
#154619=CARTESIAN_POINT('Ctrl Pts',(-11.9702584092036,9.03951954568884,
1265.89117647059));
#154620=CARTESIAN_POINT('Ctrl Pts',(-11.132623567824,10.148727336345,1264.39705882353));
#154621=CARTESIAN_POINT('Ctrl Pts',(-10.1054346546984,11.0851337583099,
1262.90294117647));
#154622=CARTESIAN_POINT('Ctrl Pts',(-9.07824574157275,12.0215401802748,
1261.40882352941));
#154623=CARTESIAN_POINT('Ctrl Pts',(-7.89648244316034,12.7532570359442,
1259.91470588235));
#154624=CARTESIAN_POINT('Ctrl Pts',(-6.71471914474793,13.4849738916136,
1258.42058823529));
#154625=CARTESIAN_POINT('Ctrl Pts',(-5.41862499280729,13.9870834410653,
1256.92647058824));
#154626=CARTESIAN_POINT('Ctrl Pts',(-4.12253084086667,14.4891929905171,
1255.43235294118));
#154627=CARTESIAN_POINT('Ctrl Pts',(-2.75624276724856,14.7445964952585,
1253.93823529412));
#154628=CARTESIAN_POINT('Ctrl Pts',(-1.38995469363044,15.,1252.44411764706));
#154629=CARTESIAN_POINT('Ctrl Pts',(-1.83697019872103E-15,15.,1250.95));
#154630=CARTESIAN_POINT('Ctrl Pts',(1.38995469363045,15.,1249.45588235294));
#154631=CARTESIAN_POINT('Ctrl Pts',(2.75624276724855,14.7445964952585,1247.96176470588));
#154632=CARTESIAN_POINT('Ctrl Pts',(4.12253084086666,14.4891929905171,1246.46764705882));
#154633=CARTESIAN_POINT('Ctrl Pts',(5.4186249928073,13.9870834410653,1244.97352941176));
#154634=CARTESIAN_POINT('Ctrl Pts',(6.71471914474792,13.4849738916136,1243.47941176471));
#154635=CARTESIAN_POINT('Ctrl Pts',(7.89648244316034,12.7532570359442,1241.98529411765));
#154636=CARTESIAN_POINT('Ctrl Pts',(9.07824574157275,12.0215401802748,1240.49117647059));
#154637=CARTESIAN_POINT('Ctrl Pts',(10.1054346546984,11.0851337583099,1238.99705882353));
#154638=CARTESIAN_POINT('Ctrl Pts',(11.132623567824,10.148727336345,1237.50294117647));
#154639=CARTESIAN_POINT('Ctrl Pts',(11.9702584092036,9.03951954568885,1236.00882352941));
#154640=CARTESIAN_POINT('Ctrl Pts',(12.8078932505832,7.93031175503273,1234.51470588235));
#154641=CARTESIAN_POINT('Ctrl Pts',(13.4274493703259,6.68607533664807,1233.02058823529));
#154642=CARTESIAN_POINT('Ctrl Pts',(14.0470054900687,5.44183891826343,1231.52647058824));
#154643=CARTESIAN_POINT('Ctrl Pts',(14.4273846475923,4.10494485108125,1230.03235294118));
#154644=CARTESIAN_POINT('Ctrl Pts',(14.8077638051159,2.76805078389905,1228.53823529412));
#154645=CARTESIAN_POINT('Ctrl Pts',(14.9360126444255,1.38402539194953,1227.04411764706));
#154646=CARTESIAN_POINT('Ctrl Pts',(15.0642614837351,2.76725994113625E-15,
1225.55));
#154647=CARTESIAN_POINT('Ctrl Pts',(14.9360126444255,-1.38402539194952,
1224.05588235294));
#154648=CARTESIAN_POINT('Ctrl Pts',(14.8077638051159,-2.76805078389906,
1222.56176470588));
#154649=CARTESIAN_POINT('Ctrl Pts',(14.4273846475923,-4.10494485108124,
1221.06764705882));
#154650=CARTESIAN_POINT('Ctrl Pts',(14.0470054900687,-5.44183891826342,
1219.57352941176));
#154651=CARTESIAN_POINT('Ctrl Pts',(13.4274493703259,-6.68607533664808,
1218.07941176471));
#154652=CARTESIAN_POINT('Ctrl Pts',(12.8078932505832,-7.93031175503273,
1216.58529411765));
#154653=CARTESIAN_POINT('Ctrl Pts',(11.9702584092036,-9.03951954568884,
1215.09117647059));
#154654=CARTESIAN_POINT('Ctrl Pts',(11.132623567824,-10.148727336345,1213.59705882353));
#154655=CARTESIAN_POINT('Ctrl Pts',(10.1054346546984,-11.0851337583099,
1212.10294117647));
#154656=CARTESIAN_POINT('Ctrl Pts',(9.07824574157275,-12.0215401802748,
1210.60882352941));
#154657=CARTESIAN_POINT('Ctrl Pts',(7.89648244316034,-12.7532570359442,
1209.11470588235));
#154658=CARTESIAN_POINT('Ctrl Pts',(6.71471914474792,-13.4849738916136,
1207.62058823529));
#154659=CARTESIAN_POINT('Ctrl Pts',(5.4186249928073,-13.9870834410653,1206.12647058824));
#154660=CARTESIAN_POINT('Ctrl Pts',(4.12253084086667,-14.4891929905171,
1204.63235294118));
#154661=CARTESIAN_POINT('Ctrl Pts',(2.75624276724855,-14.7445964952585,
1203.13823529412));
#154662=CARTESIAN_POINT('Ctrl Pts',(1.38995469363045,-15.,1201.64411764706));
#154663=CARTESIAN_POINT('Ctrl Pts',(0.,-15.,1200.15));
#154664=CARTESIAN_POINT('Ctrl Pts',(-1.38995469363045,-15.,1198.65588235294));
#154665=CARTESIAN_POINT('Ctrl Pts',(-2.75624276724856,-14.7445964952585,
1197.16176470588));
#154666=CARTESIAN_POINT('Ctrl Pts',(-4.12253084086666,-14.4891929905171,
1195.66764705882));
#154667=CARTESIAN_POINT('Ctrl Pts',(-5.41862499280729,-13.9870834410653,
1194.17352941176));
#154668=CARTESIAN_POINT('Ctrl Pts',(-6.71471914474793,-13.4849738916136,
1192.67941176471));
#154669=CARTESIAN_POINT('Ctrl Pts',(-7.89648244316034,-12.7532570359442,
1191.18529411765));
#154670=CARTESIAN_POINT('Ctrl Pts',(-9.07824574157275,-12.0215401802748,
1189.69117647059));
#154671=CARTESIAN_POINT('Ctrl Pts',(-10.1054346546984,-11.0851337583099,
1188.19705882353));
#154672=CARTESIAN_POINT('Ctrl Pts',(-11.132623567824,-10.148727336345,1186.70294117647));
#154673=CARTESIAN_POINT('Ctrl Pts',(-11.9702584092036,-9.03951954568885,
1185.20882352941));
#154674=CARTESIAN_POINT('Ctrl Pts',(-12.8078932505832,-7.93031175503273,
1183.71470588235));
#154675=CARTESIAN_POINT('Ctrl Pts',(-13.4274493703259,-6.68607533664808,
1182.22058823529));
#154676=CARTESIAN_POINT('Ctrl Pts',(-14.0470054900687,-5.44183891826343,
1180.72647058824));
#154677=CARTESIAN_POINT('Ctrl Pts',(-14.4273846475923,-4.10494485108124,
1179.23235294118));
#154678=CARTESIAN_POINT('Ctrl Pts',(-14.8077638051159,-2.76805078389906,
1177.73823529412));
#154679=CARTESIAN_POINT('Ctrl Pts',(-14.9360126444255,-1.38402539194953,
1176.24411764706));
#154680=CARTESIAN_POINT('Ctrl Pts',(-15.0642614837351,-9.22419980378748E-16,
1174.75));
#154681=CARTESIAN_POINT('Ctrl Pts',(-14.9360126444255,1.38402539194953,
1173.25588235294));
#154682=CARTESIAN_POINT('Ctrl Pts',(-14.8077638051159,2.76805078389906,
1171.76176470588));
#154683=CARTESIAN_POINT('Ctrl Pts',(-14.4273846475923,4.10494485108124,
1170.26764705882));
#154684=CARTESIAN_POINT('Ctrl Pts',(-14.0470054900687,5.44183891826343,
1168.77352941176));
#154685=CARTESIAN_POINT('Ctrl Pts',(-13.4274493703259,6.68607533664807,
1167.27941176471));
#154686=CARTESIAN_POINT('Ctrl Pts',(-12.8078932505832,7.93031175503273,
1165.78529411765));
#154687=CARTESIAN_POINT('Ctrl Pts',(-11.9702584092036,9.03951954568884,
1164.29117647059));
#154688=CARTESIAN_POINT('Ctrl Pts',(-11.132623567824,10.148727336345,1162.79705882353));
#154689=CARTESIAN_POINT('Ctrl Pts',(-10.1054346546984,11.0851337583099,
1161.30294117647));
#154690=CARTESIAN_POINT('Ctrl Pts',(-9.07824574157275,12.0215401802748,
1159.80882352941));
#154691=CARTESIAN_POINT('Ctrl Pts',(-7.89648244316034,12.7532570359442,
1158.31470588235));
#154692=CARTESIAN_POINT('Ctrl Pts',(-6.71471914474793,13.4849738916136,
1156.82058823529));
#154693=CARTESIAN_POINT('Ctrl Pts',(-5.41862499280729,13.9870834410653,
1155.32647058824));
#154694=CARTESIAN_POINT('Ctrl Pts',(-4.12253084086667,14.4891929905171,
1153.83235294118));
#154695=CARTESIAN_POINT('Ctrl Pts',(-2.75624276724856,14.7445964952585,
1152.33823529412));
#154696=CARTESIAN_POINT('Ctrl Pts',(-1.38995469363044,15.,1150.84411764706));
#154697=CARTESIAN_POINT('Ctrl Pts',(-1.83697019872103E-15,15.,1149.35));
#154698=CARTESIAN_POINT('Ctrl Pts',(1.38995469363045,15.,1147.85588235294));
#154699=CARTESIAN_POINT('Ctrl Pts',(2.75624276724855,14.7445964952585,1146.36176470588));
#154700=CARTESIAN_POINT('Ctrl Pts',(4.12253084086666,14.4891929905171,1144.86764705882));
#154701=CARTESIAN_POINT('Ctrl Pts',(5.4186249928073,13.9870834410653,1143.37352941176));
#154702=CARTESIAN_POINT('Ctrl Pts',(6.71471914474792,13.4849738916136,1141.87941176471));
#154703=CARTESIAN_POINT('Ctrl Pts',(7.89648244316034,12.7532570359442,1140.38529411765));
#154704=CARTESIAN_POINT('Ctrl Pts',(9.07824574157275,12.0215401802748,1138.89117647059));
#154705=CARTESIAN_POINT('Ctrl Pts',(10.1054346546984,11.0851337583099,1137.39705882353));
#154706=CARTESIAN_POINT('Ctrl Pts',(11.132623567824,10.148727336345,1135.90294117647));
#154707=CARTESIAN_POINT('Ctrl Pts',(11.9702584092036,9.03951954568885,1134.40882352941));
#154708=CARTESIAN_POINT('Ctrl Pts',(12.8078932505832,7.93031175503273,1132.91470588235));
#154709=CARTESIAN_POINT('Ctrl Pts',(13.4274493703259,6.68607533664807,1131.42058823529));
#154710=CARTESIAN_POINT('Ctrl Pts',(14.0470054900687,5.44183891826343,1129.92647058824));
#154711=CARTESIAN_POINT('Ctrl Pts',(14.4273846475923,4.10494485108125,1128.43235294118));
#154712=CARTESIAN_POINT('Ctrl Pts',(14.8077638051159,2.76805078389905,1126.93823529412));
#154713=CARTESIAN_POINT('Ctrl Pts',(14.9360126444255,1.38402539194953,1125.44411764706));
#154714=CARTESIAN_POINT('Ctrl Pts',(15.0642614837351,2.76725994113625E-15,
1123.95));
#154715=CARTESIAN_POINT('Ctrl Pts',(14.9360126444255,-1.38402539194952,
1122.45588235294));
#154716=CARTESIAN_POINT('Ctrl Pts',(14.8077638051159,-2.76805078389906,
1120.96176470588));
#154717=CARTESIAN_POINT('Ctrl Pts',(14.4273846475923,-4.10494485108124,
1119.46764705882));
#154718=CARTESIAN_POINT('Ctrl Pts',(14.0470054900687,-5.44183891826342,
1117.97352941176));
#154719=CARTESIAN_POINT('Ctrl Pts',(13.4274493703259,-6.68607533664808,
1116.47941176471));
#154720=CARTESIAN_POINT('Ctrl Pts',(12.8078932505832,-7.93031175503273,
1114.98529411765));
#154721=CARTESIAN_POINT('Ctrl Pts',(11.9702584092036,-9.03951954568884,
1113.49117647059));
#154722=CARTESIAN_POINT('Ctrl Pts',(11.132623567824,-10.148727336345,1111.99705882353));
#154723=CARTESIAN_POINT('Ctrl Pts',(10.1054346546984,-11.0851337583099,
1110.50294117647));
#154724=CARTESIAN_POINT('Ctrl Pts',(9.07824574157275,-12.0215401802748,
1109.00882352941));
#154725=CARTESIAN_POINT('Ctrl Pts',(7.89648244316034,-12.7532570359442,
1107.51470588235));
#154726=CARTESIAN_POINT('Ctrl Pts',(6.71471914474792,-13.4849738916136,
1106.02058823529));
#154727=CARTESIAN_POINT('Ctrl Pts',(5.4186249928073,-13.9870834410653,1104.52647058824));
#154728=CARTESIAN_POINT('Ctrl Pts',(4.12253084086667,-14.4891929905171,
1103.03235294118));
#154729=CARTESIAN_POINT('Ctrl Pts',(2.75624276724855,-14.7445964952585,
1101.53823529412));
#154730=CARTESIAN_POINT('Ctrl Pts',(1.38995469363045,-15.,1100.04411764706));
#154731=CARTESIAN_POINT('Ctrl Pts',(0.,-15.,1098.55));
#154732=CARTESIAN_POINT('Ctrl Pts',(-1.38995469363045,-15.,1097.05588235294));
#154733=CARTESIAN_POINT('Ctrl Pts',(-2.75624276724856,-14.7445964952585,
1095.56176470588));
#154734=CARTESIAN_POINT('Ctrl Pts',(-4.12253084086666,-14.4891929905171,
1094.06764705882));
#154735=CARTESIAN_POINT('Ctrl Pts',(-5.41862499280729,-13.9870834410653,
1092.57352941176));
#154736=CARTESIAN_POINT('Ctrl Pts',(-6.71471914474793,-13.4849738916136,
1091.07941176471));
#154737=CARTESIAN_POINT('Ctrl Pts',(-7.89648244316034,-12.7532570359442,
1089.58529411765));
#154738=CARTESIAN_POINT('Ctrl Pts',(-9.07824574157275,-12.0215401802748,
1088.09117647059));
#154739=CARTESIAN_POINT('Ctrl Pts',(-10.1054346546984,-11.0851337583099,
1086.59705882353));
#154740=CARTESIAN_POINT('Ctrl Pts',(-11.132623567824,-10.148727336345,1085.10294117647));
#154741=CARTESIAN_POINT('Ctrl Pts',(-11.9702584092036,-9.03951954568885,
1083.60882352941));
#154742=CARTESIAN_POINT('Ctrl Pts',(-12.8078932505832,-7.93031175503273,
1082.11470588235));
#154743=CARTESIAN_POINT('Ctrl Pts',(-13.4274493703259,-6.68607533664808,
1080.62058823529));
#154744=CARTESIAN_POINT('Ctrl Pts',(-14.0470054900687,-5.44183891826343,
1079.12647058824));
#154745=CARTESIAN_POINT('Ctrl Pts',(-14.4273846475923,-4.10494485108124,
1077.63235294118));
#154746=CARTESIAN_POINT('Ctrl Pts',(-14.8077638051159,-2.76805078389906,
1076.13823529412));
#154747=CARTESIAN_POINT('Ctrl Pts',(-14.9360126444255,-1.38402539194953,
1074.64411764706));
#154748=CARTESIAN_POINT('Ctrl Pts',(-15.0642614837351,-9.22419980378748E-16,
1073.15));
#154749=CARTESIAN_POINT('Ctrl Pts',(-14.9360126444255,1.38402539194953,
1071.65588235294));
#154750=CARTESIAN_POINT('Ctrl Pts',(-14.8077638051159,2.76805078389906,
1070.16176470588));
#154751=CARTESIAN_POINT('Ctrl Pts',(-14.4273846475923,4.10494485108124,
1068.66764705882));
#154752=CARTESIAN_POINT('Ctrl Pts',(-14.0470054900687,5.44183891826343,
1067.17352941176));
#154753=CARTESIAN_POINT('Ctrl Pts',(-13.4274493703259,6.68607533664807,
1065.67941176471));
#154754=CARTESIAN_POINT('Ctrl Pts',(-12.8078932505832,7.93031175503273,
1064.18529411765));
#154755=CARTESIAN_POINT('Ctrl Pts',(-11.9702584092036,9.03951954568884,
1062.69117647059));
#154756=CARTESIAN_POINT('Ctrl Pts',(-11.132623567824,10.148727336345,1061.19705882353));
#154757=CARTESIAN_POINT('Ctrl Pts',(-10.1054346546984,11.0851337583099,
1059.70294117647));
#154758=CARTESIAN_POINT('Ctrl Pts',(-9.07824574157275,12.0215401802748,
1058.20882352941));
#154759=CARTESIAN_POINT('Ctrl Pts',(-7.89648244316034,12.7532570359442,
1056.71470588235));
#154760=CARTESIAN_POINT('Ctrl Pts',(-6.71471914474793,13.4849738916136,
1055.22058823529));
#154761=CARTESIAN_POINT('Ctrl Pts',(-5.41862499280729,13.9870834410653,
1053.72647058824));
#154762=CARTESIAN_POINT('Ctrl Pts',(-4.12253084086667,14.4891929905171,
1052.23235294118));
#154763=CARTESIAN_POINT('Ctrl Pts',(-2.75624276724856,14.7445964952585,
1050.73823529412));
#154764=CARTESIAN_POINT('Ctrl Pts',(-1.38995469363044,15.,1049.24411764706));
#154765=CARTESIAN_POINT('Ctrl Pts',(-1.83697019872103E-15,15.,1047.75));
#154766=CARTESIAN_POINT('Ctrl Pts',(1.38995469363045,15.,1046.25588235294));
#154767=CARTESIAN_POINT('Ctrl Pts',(2.75624276724855,14.7445964952585,1044.76176470588));
#154768=CARTESIAN_POINT('Ctrl Pts',(4.12253084086666,14.4891929905171,1043.26764705882));
#154769=CARTESIAN_POINT('Ctrl Pts',(5.4186249928073,13.9870834410653,1041.77352941176));
#154770=CARTESIAN_POINT('Ctrl Pts',(6.71471914474792,13.4849738916136,1040.27941176471));
#154771=CARTESIAN_POINT('Ctrl Pts',(7.89648244316034,12.7532570359442,1038.78529411765));
#154772=CARTESIAN_POINT('Ctrl Pts',(9.07824574157275,12.0215401802748,1037.29117647059));
#154773=CARTESIAN_POINT('Ctrl Pts',(10.1054346546984,11.0851337583099,1035.79705882353));
#154774=CARTESIAN_POINT('Ctrl Pts',(11.132623567824,10.148727336345,1034.30294117647));
#154775=CARTESIAN_POINT('Ctrl Pts',(11.9702584092036,9.03951954568885,1032.80882352941));
#154776=CARTESIAN_POINT('Ctrl Pts',(12.8078932505832,7.93031175503273,1031.31470588235));
#154777=CARTESIAN_POINT('Ctrl Pts',(13.4274493703259,6.68607533664807,1029.82058823529));
#154778=CARTESIAN_POINT('Ctrl Pts',(14.0470054900687,5.44183891826343,1028.32647058824));
#154779=CARTESIAN_POINT('Ctrl Pts',(14.4273846475923,4.10494485108125,1026.83235294118));
#154780=CARTESIAN_POINT('Ctrl Pts',(14.8077638051159,2.76805078389905,1025.33823529412));
#154781=CARTESIAN_POINT('Ctrl Pts',(14.9360126444255,1.38402539194953,1023.84411764706));
#154782=CARTESIAN_POINT('Ctrl Pts',(15.0642614837351,2.76725994113625E-15,
1022.35));
#154783=CARTESIAN_POINT('Ctrl Pts',(14.9360126444255,-1.38402539194952,
1020.85588235294));
#154784=CARTESIAN_POINT('Ctrl Pts',(14.8077638051159,-2.76805078389906,
1019.36176470588));
#154785=CARTESIAN_POINT('Ctrl Pts',(14.4273846475923,-4.10494485108124,
1017.86764705882));
#154786=CARTESIAN_POINT('Ctrl Pts',(14.0470054900687,-5.44183891826342,
1016.37352941176));
#154787=CARTESIAN_POINT('Ctrl Pts',(13.4274493703259,-6.68607533664808,
1014.87941176471));
#154788=CARTESIAN_POINT('Ctrl Pts',(12.8078932505832,-7.93031175503273,
1013.38529411765));
#154789=CARTESIAN_POINT('Ctrl Pts',(11.9702584092036,-9.03951954568884,
1011.89117647059));
#154790=CARTESIAN_POINT('Ctrl Pts',(11.132623567824,-10.148727336345,1010.39705882353));
#154791=CARTESIAN_POINT('Ctrl Pts',(10.1054346546984,-11.0851337583099,
1008.90294117647));
#154792=CARTESIAN_POINT('Ctrl Pts',(9.07824574157275,-12.0215401802748,
1007.40882352941));
#154793=CARTESIAN_POINT('Ctrl Pts',(7.89648244316034,-12.7532570359442,
1005.91470588235));
#154794=CARTESIAN_POINT('Ctrl Pts',(6.71471914474792,-13.4849738916136,
1004.42058823529));
#154795=CARTESIAN_POINT('Ctrl Pts',(5.4186249928073,-13.9870834410653,1002.92647058824));
#154796=CARTESIAN_POINT('Ctrl Pts',(4.12253084086667,-14.4891929905171,
1001.43235294118));
#154797=CARTESIAN_POINT('Ctrl Pts',(2.75624276724855,-14.7445964952585,
999.938235294118));
#154798=CARTESIAN_POINT('Ctrl Pts',(1.38995469363045,-15.,998.444117647059));
#154799=CARTESIAN_POINT('Ctrl Pts',(0.,-15.,996.95));
#154800=CARTESIAN_POINT('Ctrl Pts',(-1.38995469363045,-15.,995.455882352941));
#154801=CARTESIAN_POINT('Ctrl Pts',(-2.75624276724856,-14.7445964952585,
993.961764705882));
#154802=CARTESIAN_POINT('Ctrl Pts',(-4.12253084086666,-14.4891929905171,
992.467647058824));
#154803=CARTESIAN_POINT('Ctrl Pts',(-5.41862499280729,-13.9870834410653,
990.973529411765));
#154804=CARTESIAN_POINT('Ctrl Pts',(-6.71471914474793,-13.4849738916136,
989.479411764706));
#154805=CARTESIAN_POINT('Ctrl Pts',(-7.89648244316034,-12.7532570359442,
987.985294117647));
#154806=CARTESIAN_POINT('Ctrl Pts',(-9.07824574157275,-12.0215401802748,
986.491176470588));
#154807=CARTESIAN_POINT('Ctrl Pts',(-10.1054346546984,-11.0851337583099,
984.997058823529));
#154808=CARTESIAN_POINT('Ctrl Pts',(-11.132623567824,-10.148727336345,983.502941176471));
#154809=CARTESIAN_POINT('Ctrl Pts',(-11.9702584092036,-9.03951954568885,
982.008823529412));
#154810=CARTESIAN_POINT('Ctrl Pts',(-12.8078932505832,-7.93031175503273,
980.514705882353));
#154811=CARTESIAN_POINT('Ctrl Pts',(-13.4274493703259,-6.68607533664808,
979.020588235294));
#154812=CARTESIAN_POINT('Ctrl Pts',(-14.0470054900687,-5.44183891826343,
977.526470588235));
#154813=CARTESIAN_POINT('Ctrl Pts',(-14.4273846475923,-4.10494485108124,
976.032352941177));
#154814=CARTESIAN_POINT('Ctrl Pts',(-14.8077638051159,-2.76805078389906,
974.538235294118));
#154815=CARTESIAN_POINT('Ctrl Pts',(-14.9360126444255,-1.38402539194953,
973.044117647059));
#154816=CARTESIAN_POINT('Ctrl Pts',(-15.0642614837351,-9.22419980378748E-16,
971.55));
#154817=CARTESIAN_POINT('Ctrl Pts',(-14.9360126444255,1.38402539194953,
970.055882352941));
#154818=CARTESIAN_POINT('Ctrl Pts',(-14.8077638051159,2.76805078389906,
968.561764705882));
#154819=CARTESIAN_POINT('Ctrl Pts',(-14.4273846475923,4.10494485108124,
967.067647058824));
#154820=CARTESIAN_POINT('Ctrl Pts',(-14.0470054900687,5.44183891826343,
965.573529411765));
#154821=CARTESIAN_POINT('Ctrl Pts',(-13.4274493703259,6.68607533664807,
964.079411764706));
#154822=CARTESIAN_POINT('Ctrl Pts',(-12.8078932505832,7.93031175503273,
962.585294117647));
#154823=CARTESIAN_POINT('Ctrl Pts',(-11.9702584092036,9.03951954568884,
961.091176470588));
#154824=CARTESIAN_POINT('Ctrl Pts',(-11.132623567824,10.148727336345,959.59705882353));
#154825=CARTESIAN_POINT('Ctrl Pts',(-10.1054346546984,11.0851337583099,
958.102941176471));
#154826=CARTESIAN_POINT('Ctrl Pts',(-9.07824574157275,12.0215401802748,
956.608823529412));
#154827=CARTESIAN_POINT('Ctrl Pts',(-7.89648244316034,12.7532570359442,
955.114705882353));
#154828=CARTESIAN_POINT('Ctrl Pts',(-6.71471914474793,13.4849738916136,
953.620588235294));
#154829=CARTESIAN_POINT('Ctrl Pts',(-5.41862499280729,13.9870834410653,
952.126470588235));
#154830=CARTESIAN_POINT('Ctrl Pts',(-4.12253084086667,14.4891929905171,
950.632352941177));
#154831=CARTESIAN_POINT('Ctrl Pts',(-2.75624276724856,14.7445964952585,
949.138235294118));
#154832=CARTESIAN_POINT('Ctrl Pts',(-1.38995469363044,15.,947.644117647059));
#154833=CARTESIAN_POINT('Ctrl Pts',(-1.83697019872103E-15,15.,946.15));
#154834=CARTESIAN_POINT('Ctrl Pts',(1.38995469363045,15.,944.655882352941));
#154835=CARTESIAN_POINT('Ctrl Pts',(2.75624276724855,14.7445964952585,943.161764705882));
#154836=CARTESIAN_POINT('Ctrl Pts',(4.12253084086666,14.4891929905171,941.667647058824));
#154837=CARTESIAN_POINT('Ctrl Pts',(5.4186249928073,13.9870834410653,940.173529411765));
#154838=CARTESIAN_POINT('Ctrl Pts',(6.71471914474792,13.4849738916136,938.679411764706));
#154839=CARTESIAN_POINT('Ctrl Pts',(7.89648244316034,12.7532570359442,937.185294117647));
#154840=CARTESIAN_POINT('Ctrl Pts',(9.07824574157275,12.0215401802748,935.691176470589));
#154841=CARTESIAN_POINT('Ctrl Pts',(10.1054346546984,11.0851337583099,934.19705882353));
#154842=CARTESIAN_POINT('Ctrl Pts',(11.132623567824,10.148727336345,932.702941176471));
#154843=CARTESIAN_POINT('Ctrl Pts',(11.9702584092036,9.03951954568885,931.208823529412));
#154844=CARTESIAN_POINT('Ctrl Pts',(12.8078932505832,7.93031175503273,929.714705882353));
#154845=CARTESIAN_POINT('Ctrl Pts',(13.4274493703259,6.68607533664807,928.220588235294));
#154846=CARTESIAN_POINT('Ctrl Pts',(14.0470054900687,5.44183891826343,926.726470588235));
#154847=CARTESIAN_POINT('Ctrl Pts',(14.4273846475923,4.10494485108125,925.232352941176));
#154848=CARTESIAN_POINT('Ctrl Pts',(14.8077638051159,2.76805078389905,923.738235294118));
#154849=CARTESIAN_POINT('Ctrl Pts',(14.9360126444255,1.38402539194953,922.244117647059));
#154850=CARTESIAN_POINT('Ctrl Pts',(15.0642614837351,2.76725994113625E-15,
920.75));
#154851=CARTESIAN_POINT('Ctrl Pts',(14.9360126444255,-1.38402539194952,
919.255882352941));
#154852=CARTESIAN_POINT('Ctrl Pts',(14.8077638051159,-2.76805078389906,
917.761764705882));
#154853=CARTESIAN_POINT('Ctrl Pts',(14.4273846475923,-4.10494485108124,
916.267647058824));
#154854=CARTESIAN_POINT('Ctrl Pts',(14.0470054900687,-5.44183891826342,
914.773529411765));
#154855=CARTESIAN_POINT('Ctrl Pts',(13.4274493703259,-6.68607533664808,
913.279411764706));
#154856=CARTESIAN_POINT('Ctrl Pts',(12.8078932505832,-7.93031175503273,
911.785294117647));
#154857=CARTESIAN_POINT('Ctrl Pts',(11.9702584092036,-9.03951954568884,
910.291176470588));
#154858=CARTESIAN_POINT('Ctrl Pts',(11.132623567824,-10.148727336345,908.797058823529));
#154859=CARTESIAN_POINT('Ctrl Pts',(10.1054346546984,-11.0851337583099,
907.302941176471));
#154860=CARTESIAN_POINT('Ctrl Pts',(9.07824574157275,-12.0215401802748,
905.808823529412));
#154861=CARTESIAN_POINT('Ctrl Pts',(7.89648244316034,-12.7532570359442,
904.314705882353));
#154862=CARTESIAN_POINT('Ctrl Pts',(6.71471914474792,-13.4849738916136,
902.820588235294));
#154863=CARTESIAN_POINT('Ctrl Pts',(5.4186249928073,-13.9870834410653,901.326470588235));
#154864=CARTESIAN_POINT('Ctrl Pts',(4.12253084086667,-14.4891929905171,
899.832352941177));
#154865=CARTESIAN_POINT('Ctrl Pts',(2.75624276724855,-14.7445964952585,
898.338235294118));
#154866=CARTESIAN_POINT('Ctrl Pts',(1.38995469363045,-15.,896.844117647059));
#154867=CARTESIAN_POINT('Ctrl Pts',(0.,-15.,895.35));
#154868=CARTESIAN_POINT('Ctrl Pts',(-1.38995469363045,-15.,893.855882352941));
#154869=CARTESIAN_POINT('Ctrl Pts',(-2.75624276724856,-14.7445964952585,
892.361764705882));
#154870=CARTESIAN_POINT('Ctrl Pts',(-4.12253084086666,-14.4891929905171,
890.867647058824));
#154871=CARTESIAN_POINT('Ctrl Pts',(-5.41862499280729,-13.9870834410653,
889.373529411765));
#154872=CARTESIAN_POINT('Ctrl Pts',(-6.71471914474793,-13.4849738916136,
887.879411764706));
#154873=CARTESIAN_POINT('Ctrl Pts',(-7.89648244316034,-12.7532570359442,
886.385294117647));
#154874=CARTESIAN_POINT('Ctrl Pts',(-9.07824574157275,-12.0215401802748,
884.891176470588));
#154875=CARTESIAN_POINT('Ctrl Pts',(-10.1054346546984,-11.0851337583099,
883.39705882353));
#154876=CARTESIAN_POINT('Ctrl Pts',(-11.132623567824,-10.148727336345,881.902941176471));
#154877=CARTESIAN_POINT('Ctrl Pts',(-11.9702584092036,-9.03951954568885,
880.408823529412));
#154878=CARTESIAN_POINT('Ctrl Pts',(-12.8078932505832,-7.93031175503273,
878.914705882353));
#154879=CARTESIAN_POINT('Ctrl Pts',(-13.4274493703259,-6.68607533664808,
877.420588235294));
#154880=CARTESIAN_POINT('Ctrl Pts',(-14.0470054900687,-5.44183891826343,
875.926470588235));
#154881=CARTESIAN_POINT('Ctrl Pts',(-14.4273846475923,-4.10494485108124,
874.432352941177));
#154882=CARTESIAN_POINT('Ctrl Pts',(-14.8077638051159,-2.76805078389906,
872.938235294118));
#154883=CARTESIAN_POINT('Ctrl Pts',(-14.9360126444255,-1.38402539194953,
871.444117647059));
#154884=CARTESIAN_POINT('Ctrl Pts',(-15.0642614837351,-9.22419980378748E-16,
869.95));
#154885=CARTESIAN_POINT('Ctrl Pts',(-14.9360126444255,1.38402539194953,
868.455882352941));
#154886=CARTESIAN_POINT('Ctrl Pts',(-14.8077638051159,2.76805078389906,
866.961764705882));
#154887=CARTESIAN_POINT('Ctrl Pts',(-14.4273846475923,4.10494485108124,
865.467647058824));
#154888=CARTESIAN_POINT('Ctrl Pts',(-14.0470054900687,5.44183891826343,
863.973529411765));
#154889=CARTESIAN_POINT('Ctrl Pts',(-13.4274493703259,6.68607533664807,
862.479411764706));
#154890=CARTESIAN_POINT('Ctrl Pts',(-12.8078932505832,7.93031175503273,
860.985294117647));
#154891=CARTESIAN_POINT('Ctrl Pts',(-11.9702584092036,9.03951954568884,
859.491176470588));
#154892=CARTESIAN_POINT('Ctrl Pts',(-11.132623567824,10.148727336345,857.997058823529));
#154893=CARTESIAN_POINT('Ctrl Pts',(-10.1054346546984,11.0851337583099,
856.502941176471));
#154894=CARTESIAN_POINT('Ctrl Pts',(-9.07824574157275,12.0215401802748,
855.008823529412));
#154895=CARTESIAN_POINT('Ctrl Pts',(-7.89648244316034,12.7532570359442,
853.514705882353));
#154896=CARTESIAN_POINT('Ctrl Pts',(-6.71471914474793,13.4849738916136,
852.020588235294));
#154897=CARTESIAN_POINT('Ctrl Pts',(-5.41862499280729,13.9870834410653,
850.526470588235));
#154898=CARTESIAN_POINT('Ctrl Pts',(-4.12253084086667,14.4891929905171,
849.032352941177));
#154899=CARTESIAN_POINT('Ctrl Pts',(-2.75624276724856,14.7445964952585,
847.538235294118));
#154900=CARTESIAN_POINT('Ctrl Pts',(-1.38995469363044,15.,846.044117647059));
#154901=CARTESIAN_POINT('Ctrl Pts',(-1.83697019872103E-15,15.,844.55));
#154902=CARTESIAN_POINT('Ctrl Pts',(1.38995469363045,15.,843.055882352941));
#154903=CARTESIAN_POINT('Ctrl Pts',(2.75624276724855,14.7445964952585,841.561764705883));
#154904=CARTESIAN_POINT('Ctrl Pts',(4.12253084086666,14.4891929905171,840.067647058824));
#154905=CARTESIAN_POINT('Ctrl Pts',(5.4186249928073,13.9870834410653,838.573529411765));
#154906=CARTESIAN_POINT('Ctrl Pts',(6.71471914474792,13.4849738916136,837.079411764706));
#154907=CARTESIAN_POINT('Ctrl Pts',(7.89648244316034,12.7532570359442,835.585294117647));
#154908=CARTESIAN_POINT('Ctrl Pts',(9.07824574157275,12.0215401802748,834.091176470588));
#154909=CARTESIAN_POINT('Ctrl Pts',(10.1054346546984,11.0851337583099,832.597058823529));
#154910=CARTESIAN_POINT('Ctrl Pts',(11.132623567824,10.148727336345,831.102941176471));
#154911=CARTESIAN_POINT('Ctrl Pts',(11.9702584092036,9.03951954568885,829.608823529412));
#154912=CARTESIAN_POINT('Ctrl Pts',(12.8078932505832,7.93031175503273,828.114705882353));
#154913=CARTESIAN_POINT('Ctrl Pts',(13.4274493703259,6.68607533664807,826.620588235294));
#154914=CARTESIAN_POINT('Ctrl Pts',(14.0470054900687,5.44183891826343,825.126470588235));
#154915=CARTESIAN_POINT('Ctrl Pts',(14.4273846475923,4.10494485108125,823.632352941177));
#154916=CARTESIAN_POINT('Ctrl Pts',(14.8077638051159,2.76805078389905,822.138235294118));
#154917=CARTESIAN_POINT('Ctrl Pts',(14.9360126444255,1.38402539194953,820.644117647059));
#154918=CARTESIAN_POINT('Ctrl Pts',(15.0642614837351,2.76725994113625E-15,
819.15));
#154919=CARTESIAN_POINT('Ctrl Pts',(14.9360126444255,-1.38402539194952,
817.655882352941));
#154920=CARTESIAN_POINT('Ctrl Pts',(14.8077638051159,-2.76805078389906,
816.161764705882));
#154921=CARTESIAN_POINT('Ctrl Pts',(14.4273846475923,-4.10494485108124,
814.667647058824));
#154922=CARTESIAN_POINT('Ctrl Pts',(14.0470054900687,-5.44183891826342,
813.173529411765));
#154923=CARTESIAN_POINT('Ctrl Pts',(13.4274493703259,-6.68607533664808,
811.679411764706));
#154924=CARTESIAN_POINT('Ctrl Pts',(12.8078932505832,-7.93031175503273,
810.185294117647));
#154925=CARTESIAN_POINT('Ctrl Pts',(11.9702584092036,-9.03951954568884,
808.691176470588));
#154926=CARTESIAN_POINT('Ctrl Pts',(11.132623567824,-10.148727336345,807.197058823529));
#154927=CARTESIAN_POINT('Ctrl Pts',(10.1054346546984,-11.0851337583099,
805.702941176471));
#154928=CARTESIAN_POINT('Ctrl Pts',(9.07824574157275,-12.0215401802748,
804.208823529412));
#154929=CARTESIAN_POINT('Ctrl Pts',(7.89648244316034,-12.7532570359442,
802.714705882353));
#154930=CARTESIAN_POINT('Ctrl Pts',(6.71471914474792,-13.4849738916136,
801.220588235294));
#154931=CARTESIAN_POINT('Ctrl Pts',(5.4186249928073,-13.9870834410653,799.726470588235));
#154932=CARTESIAN_POINT('Ctrl Pts',(4.12253084086667,-14.4891929905171,
798.232352941176));
#154933=CARTESIAN_POINT('Ctrl Pts',(2.75624276724855,-14.7445964952585,
796.738235294118));
#154934=CARTESIAN_POINT('Ctrl Pts',(1.38995469363045,-15.,795.244117647059));
#154935=CARTESIAN_POINT('Ctrl Pts',(0.,-15.,793.75));
#154936=CARTESIAN_POINT('Ctrl Pts',(-1.38995469363045,-15.,792.255882352941));
#154937=CARTESIAN_POINT('Ctrl Pts',(-2.75624276724856,-14.7445964952585,
790.761764705882));
#154938=CARTESIAN_POINT('Ctrl Pts',(-4.12253084086666,-14.4891929905171,
789.267647058824));
#154939=CARTESIAN_POINT('Ctrl Pts',(-5.41862499280729,-13.9870834410653,
787.773529411765));
#154940=CARTESIAN_POINT('Ctrl Pts',(-6.71471914474793,-13.4849738916136,
786.279411764706));
#154941=CARTESIAN_POINT('Ctrl Pts',(-7.89648244316034,-12.7532570359442,
784.785294117647));
#154942=CARTESIAN_POINT('Ctrl Pts',(-9.07824574157275,-12.0215401802748,
783.291176470588));
#154943=CARTESIAN_POINT('Ctrl Pts',(-10.1054346546984,-11.0851337583099,
781.797058823529));
#154944=CARTESIAN_POINT('Ctrl Pts',(-11.132623567824,-10.148727336345,780.302941176471));
#154945=CARTESIAN_POINT('Ctrl Pts',(-11.9702584092036,-9.03951954568885,
778.808823529412));
#154946=CARTESIAN_POINT('Ctrl Pts',(-12.8078932505832,-7.93031175503273,
777.314705882353));
#154947=CARTESIAN_POINT('Ctrl Pts',(-13.4274493703259,-6.68607533664808,
775.820588235294));
#154948=CARTESIAN_POINT('Ctrl Pts',(-14.0470054900687,-5.44183891826343,
774.326470588235));
#154949=CARTESIAN_POINT('Ctrl Pts',(-14.4273846475923,-4.10494485108124,
772.832352941177));
#154950=CARTESIAN_POINT('Ctrl Pts',(-14.8077638051159,-2.76805078389906,
771.338235294118));
#154951=CARTESIAN_POINT('Ctrl Pts',(-14.9360126444255,-1.38402539194953,
769.844117647059));
#154952=CARTESIAN_POINT('Ctrl Pts',(-15.0642614837351,-9.22419980378748E-16,
768.35));
#154953=CARTESIAN_POINT('Ctrl Pts',(-14.9360126444255,1.38402539194953,
766.855882352941));
#154954=CARTESIAN_POINT('Ctrl Pts',(-14.8077638051159,2.76805078389906,
765.361764705882));
#154955=CARTESIAN_POINT('Ctrl Pts',(-14.4273846475923,4.10494485108124,
763.867647058824));
#154956=CARTESIAN_POINT('Ctrl Pts',(-14.0470054900687,5.44183891826343,
762.373529411765));
#154957=CARTESIAN_POINT('Ctrl Pts',(-13.4274493703259,6.68607533664807,
760.879411764706));
#154958=CARTESIAN_POINT('Ctrl Pts',(-12.8078932505832,7.93031175503273,
759.385294117647));
#154959=CARTESIAN_POINT('Ctrl Pts',(-11.9702584092036,9.03951954568884,
757.891176470588));
#154960=CARTESIAN_POINT('Ctrl Pts',(-11.132623567824,10.148727336345,756.397058823529));
#154961=CARTESIAN_POINT('Ctrl Pts',(-10.1054346546984,11.0851337583099,
754.902941176471));
#154962=CARTESIAN_POINT('Ctrl Pts',(-9.07824574157275,12.0215401802748,
753.408823529412));
#154963=CARTESIAN_POINT('Ctrl Pts',(-7.89648244316034,12.7532570359442,
751.914705882353));
#154964=CARTESIAN_POINT('Ctrl Pts',(-6.71471914474793,13.4849738916136,
750.420588235294));
#154965=CARTESIAN_POINT('Ctrl Pts',(-5.41862499280729,13.9870834410653,
748.926470588235));
#154966=CARTESIAN_POINT('Ctrl Pts',(-4.12253084086667,14.4891929905171,
747.432352941176));
#154967=CARTESIAN_POINT('Ctrl Pts',(-2.75624276724856,14.7445964952585,
745.938235294118));
#154968=CARTESIAN_POINT('Ctrl Pts',(-1.38995469363044,15.,744.444117647059));
#154969=CARTESIAN_POINT('Ctrl Pts',(-1.83697019872103E-15,15.,742.95));
#154970=CARTESIAN_POINT('Ctrl Pts',(1.38995469363045,15.,741.455882352941));
#154971=CARTESIAN_POINT('Ctrl Pts',(2.75624276724855,14.7445964952585,739.961764705882));
#154972=CARTESIAN_POINT('Ctrl Pts',(4.12253084086666,14.4891929905171,738.467647058824));
#154973=CARTESIAN_POINT('Ctrl Pts',(5.4186249928073,13.9870834410653,736.973529411765));
#154974=CARTESIAN_POINT('Ctrl Pts',(6.71471914474792,13.4849738916136,735.479411764706));
#154975=CARTESIAN_POINT('Ctrl Pts',(7.89648244316034,12.7532570359442,733.985294117647));
#154976=CARTESIAN_POINT('Ctrl Pts',(9.07824574157275,12.0215401802748,732.491176470588));
#154977=CARTESIAN_POINT('Ctrl Pts',(10.1054346546984,11.0851337583099,730.99705882353));
#154978=CARTESIAN_POINT('Ctrl Pts',(11.132623567824,10.148727336345,729.502941176471));
#154979=CARTESIAN_POINT('Ctrl Pts',(11.9702584092036,9.03951954568885,728.008823529412));
#154980=CARTESIAN_POINT('Ctrl Pts',(12.8078932505832,7.93031175503273,726.514705882353));
#154981=CARTESIAN_POINT('Ctrl Pts',(13.4274493703259,6.68607533664807,725.020588235294));
#154982=CARTESIAN_POINT('Ctrl Pts',(14.0470054900687,5.44183891826343,723.526470588235));
#154983=CARTESIAN_POINT('Ctrl Pts',(14.4273846475923,4.10494485108125,722.032352941177));
#154984=CARTESIAN_POINT('Ctrl Pts',(14.8077638051159,2.76805078389905,720.538235294118));
#154985=CARTESIAN_POINT('Ctrl Pts',(14.9360126444255,1.38402539194953,719.044117647059));
#154986=CARTESIAN_POINT('Ctrl Pts',(15.0642614837351,2.76725994113625E-15,
717.55));
#154987=CARTESIAN_POINT('Ctrl Pts',(14.9360126444255,-1.38402539194952,
716.055882352941));
#154988=CARTESIAN_POINT('Ctrl Pts',(14.8077638051159,-2.76805078389906,
714.561764705882));
#154989=CARTESIAN_POINT('Ctrl Pts',(14.4273846475923,-4.10494485108124,
713.067647058824));
#154990=CARTESIAN_POINT('Ctrl Pts',(14.0470054900687,-5.44183891826342,
711.573529411765));
#154991=CARTESIAN_POINT('Ctrl Pts',(13.4274493703259,-6.68607533664808,
710.079411764706));
#154992=CARTESIAN_POINT('Ctrl Pts',(12.8078932505832,-7.93031175503273,
708.585294117647));
#154993=CARTESIAN_POINT('Ctrl Pts',(11.9702584092036,-9.03951954568884,
707.091176470588));
#154994=CARTESIAN_POINT('Ctrl Pts',(11.132623567824,-10.148727336345,705.597058823529));
#154995=CARTESIAN_POINT('Ctrl Pts',(10.1054346546984,-11.0851337583099,
704.102941176471));
#154996=CARTESIAN_POINT('Ctrl Pts',(9.07824574157275,-12.0215401802748,
702.608823529412));
#154997=CARTESIAN_POINT('Ctrl Pts',(7.89648244316034,-12.7532570359442,
701.114705882353));
#154998=CARTESIAN_POINT('Ctrl Pts',(6.71471914474792,-13.4849738916136,
699.620588235294));
#154999=CARTESIAN_POINT('Ctrl Pts',(5.4186249928073,-13.9870834410653,698.126470588235));
#155000=CARTESIAN_POINT('Ctrl Pts',(4.12253084086667,-14.4891929905171,
696.632352941177));
#155001=CARTESIAN_POINT('Ctrl Pts',(2.75624276724855,-14.7445964952585,
695.138235294118));
#155002=CARTESIAN_POINT('Ctrl Pts',(1.38995469363045,-15.,693.644117647059));
#155003=CARTESIAN_POINT('Ctrl Pts',(0.,-15.,692.15));
#155004=CARTESIAN_POINT('Ctrl Pts',(-1.38995469363045,-15.,690.655882352941));
#155005=CARTESIAN_POINT('Ctrl Pts',(-2.75624276724856,-14.7445964952585,
689.161764705882));
#155006=CARTESIAN_POINT('Ctrl Pts',(-4.12253084086666,-14.4891929905171,
687.667647058824));
#155007=CARTESIAN_POINT('Ctrl Pts',(-5.41862499280729,-13.9870834410653,
686.173529411765));
#155008=CARTESIAN_POINT('Ctrl Pts',(-6.71471914474793,-13.4849738916136,
684.679411764706));
#155009=CARTESIAN_POINT('Ctrl Pts',(-7.89648244316034,-12.7532570359442,
683.185294117647));
#155010=CARTESIAN_POINT('Ctrl Pts',(-9.07824574157275,-12.0215401802748,
681.691176470588));
#155011=CARTESIAN_POINT('Ctrl Pts',(-10.1054346546984,-11.0851337583099,
680.197058823529));
#155012=CARTESIAN_POINT('Ctrl Pts',(-11.132623567824,-10.148727336345,678.702941176471));
#155013=CARTESIAN_POINT('Ctrl Pts',(-11.9702584092036,-9.03951954568885,
677.208823529412));
#155014=CARTESIAN_POINT('Ctrl Pts',(-12.8078932505832,-7.93031175503273,
675.714705882353));
#155015=CARTESIAN_POINT('Ctrl Pts',(-13.4274493703259,-6.68607533664808,
674.220588235294));
#155016=CARTESIAN_POINT('Ctrl Pts',(-14.0470054900687,-5.44183891826343,
672.726470588236));
#155017=CARTESIAN_POINT('Ctrl Pts',(-14.4273846475923,-4.10494485108124,
671.232352941176));
#155018=CARTESIAN_POINT('Ctrl Pts',(-14.8077638051159,-2.76805078389906,
669.738235294118));
#155019=CARTESIAN_POINT('Ctrl Pts',(-14.9360126444255,-1.38402539194953,
668.244117647059));
#155020=CARTESIAN_POINT('Ctrl Pts',(-15.0642614837351,-9.22419980378748E-16,
666.75));
#155021=CARTESIAN_POINT('Ctrl Pts',(-14.9360126444255,1.38402539194953,
665.255882352941));
#155022=CARTESIAN_POINT('Ctrl Pts',(-14.8077638051159,2.76805078389906,
663.761764705882));
#155023=CARTESIAN_POINT('Ctrl Pts',(-14.4273846475923,4.10494485108124,
662.267647058824));
#155024=CARTESIAN_POINT('Ctrl Pts',(-14.0470054900687,5.44183891826343,
660.773529411765));
#155025=CARTESIAN_POINT('Ctrl Pts',(-13.4274493703259,6.68607533664807,
659.279411764706));
#155026=CARTESIAN_POINT('Ctrl Pts',(-12.8078932505832,7.93031175503273,
657.785294117647));
#155027=CARTESIAN_POINT('Ctrl Pts',(-11.9702584092036,9.03951954568884,
656.291176470588));
#155028=CARTESIAN_POINT('Ctrl Pts',(-11.132623567824,10.148727336345,654.797058823529));
#155029=CARTESIAN_POINT('Ctrl Pts',(-10.1054346546984,11.0851337583099,
653.302941176471));
#155030=CARTESIAN_POINT('Ctrl Pts',(-9.07824574157275,12.0215401802748,
651.808823529412));
#155031=CARTESIAN_POINT('Ctrl Pts',(-7.89648244316034,12.7532570359442,
650.314705882353));
#155032=CARTESIAN_POINT('Ctrl Pts',(-6.71471914474793,13.4849738916136,
648.820588235294));
#155033=CARTESIAN_POINT('Ctrl Pts',(-5.41862499280729,13.9870834410653,
647.326470588235));
#155034=CARTESIAN_POINT('Ctrl Pts',(-4.12253084086667,14.4891929905171,
645.832352941176));
#155035=CARTESIAN_POINT('Ctrl Pts',(-2.75624276724856,14.7445964952585,
644.338235294118));
#155036=CARTESIAN_POINT('Ctrl Pts',(-1.38995469363044,15.,642.844117647059));
#155037=CARTESIAN_POINT('Ctrl Pts',(-1.83697019872103E-15,15.,641.35));
#155038=CARTESIAN_POINT('Ctrl Pts',(1.38995469363045,15.,639.855882352941));
#155039=CARTESIAN_POINT('Ctrl Pts',(2.75624276724855,14.7445964952585,638.361764705882));
#155040=CARTESIAN_POINT('Ctrl Pts',(4.12253084086666,14.4891929905171,636.867647058824));
#155041=CARTESIAN_POINT('Ctrl Pts',(5.4186249928073,13.9870834410653,635.373529411765));
#155042=CARTESIAN_POINT('Ctrl Pts',(6.71471914474792,13.4849738916136,633.879411764706));
#155043=CARTESIAN_POINT('Ctrl Pts',(7.89648244316034,12.7532570359442,632.385294117647));
#155044=CARTESIAN_POINT('Ctrl Pts',(9.07824574157275,12.0215401802748,630.891176470588));
#155045=CARTESIAN_POINT('Ctrl Pts',(10.1054346546984,11.0851337583099,629.39705882353));
#155046=CARTESIAN_POINT('Ctrl Pts',(11.132623567824,10.148727336345,627.902941176471));
#155047=CARTESIAN_POINT('Ctrl Pts',(11.9702584092036,9.03951954568885,626.408823529412));
#155048=CARTESIAN_POINT('Ctrl Pts',(12.8078932505832,7.93031175503273,624.914705882353));
#155049=CARTESIAN_POINT('Ctrl Pts',(13.4274493703259,6.68607533664807,623.420588235294));
#155050=CARTESIAN_POINT('Ctrl Pts',(14.0470054900687,5.44183891826343,621.926470588235));
#155051=CARTESIAN_POINT('Ctrl Pts',(14.4273846475923,4.10494485108125,620.432352941177));
#155052=CARTESIAN_POINT('Ctrl Pts',(14.8077638051159,2.76805078389905,618.938235294118));
#155053=CARTESIAN_POINT('Ctrl Pts',(14.9360126444255,1.38402539194953,617.444117647059));
#155054=CARTESIAN_POINT('Ctrl Pts',(15.0642614837351,2.76725994113625E-15,
615.95));
#155055=CARTESIAN_POINT('Ctrl Pts',(14.9360126444255,-1.38402539194952,
614.455882352941));
#155056=CARTESIAN_POINT('Ctrl Pts',(14.8077638051159,-2.76805078389906,
612.961764705883));
#155057=CARTESIAN_POINT('Ctrl Pts',(14.4273846475923,-4.10494485108124,
611.467647058824));
#155058=CARTESIAN_POINT('Ctrl Pts',(14.0470054900687,-5.44183891826342,
609.973529411765));
#155059=CARTESIAN_POINT('Ctrl Pts',(13.4274493703259,-6.68607533664808,
608.479411764706));
#155060=CARTESIAN_POINT('Ctrl Pts',(12.8078932505832,-7.93031175503273,
606.985294117647));
#155061=CARTESIAN_POINT('Ctrl Pts',(11.9702584092036,-9.03951954568884,
605.491176470588));
#155062=CARTESIAN_POINT('Ctrl Pts',(11.132623567824,-10.148727336345,603.997058823529));
#155063=CARTESIAN_POINT('Ctrl Pts',(10.1054346546984,-11.0851337583099,
602.502941176471));
#155064=CARTESIAN_POINT('Ctrl Pts',(9.07824574157275,-12.0215401802748,
601.008823529412));
#155065=CARTESIAN_POINT('Ctrl Pts',(7.89648244316034,-12.7532570359442,
599.514705882353));
#155066=CARTESIAN_POINT('Ctrl Pts',(6.71471914474792,-13.4849738916136,
598.020588235294));
#155067=CARTESIAN_POINT('Ctrl Pts',(5.4186249928073,-13.9870834410653,596.526470588235));
#155068=CARTESIAN_POINT('Ctrl Pts',(4.12253084086667,-14.4891929905171,
595.032352941176));
#155069=CARTESIAN_POINT('Ctrl Pts',(2.75624276724855,-14.7445964952585,
593.538235294118));
#155070=CARTESIAN_POINT('Ctrl Pts',(1.38995469363045,-15.,592.044117647059));
#155071=CARTESIAN_POINT('Ctrl Pts',(0.,-15.,590.55));
#155072=CARTESIAN_POINT('Ctrl Pts',(-1.38995469363045,-15.,589.055882352941));
#155073=CARTESIAN_POINT('Ctrl Pts',(-2.75624276724856,-14.7445964952585,
587.561764705882));
#155074=CARTESIAN_POINT('Ctrl Pts',(-4.12253084086666,-14.4891929905171,
586.067647058823));
#155075=CARTESIAN_POINT('Ctrl Pts',(-5.41862499280729,-13.9870834410653,
584.573529411765));
#155076=CARTESIAN_POINT('Ctrl Pts',(-6.71471914474793,-13.4849738916136,
583.079411764706));
#155077=CARTESIAN_POINT('Ctrl Pts',(-7.89648244316034,-12.7532570359442,
581.585294117647));
#155078=CARTESIAN_POINT('Ctrl Pts',(-9.07824574157275,-12.0215401802748,
580.091176470588));
#155079=CARTESIAN_POINT('Ctrl Pts',(-10.1054346546984,-11.0851337583099,
578.597058823529));
#155080=CARTESIAN_POINT('Ctrl Pts',(-11.132623567824,-10.148727336345,577.102941176471));
#155081=CARTESIAN_POINT('Ctrl Pts',(-11.9702584092036,-9.03951954568885,
575.608823529412));
#155082=CARTESIAN_POINT('Ctrl Pts',(-12.8078932505832,-7.93031175503273,
574.114705882353));
#155083=CARTESIAN_POINT('Ctrl Pts',(-13.4274493703259,-6.68607533664808,
572.620588235294));
#155084=CARTESIAN_POINT('Ctrl Pts',(-14.0470054900687,-5.44183891826343,
571.126470588235));
#155085=CARTESIAN_POINT('Ctrl Pts',(-14.4273846475923,-4.10494485108124,
569.632352941177));
#155086=CARTESIAN_POINT('Ctrl Pts',(-14.8077638051159,-2.76805078389906,
568.138235294118));
#155087=CARTESIAN_POINT('Ctrl Pts',(-14.9360126444255,-1.38402539194953,
566.644117647059));
#155088=CARTESIAN_POINT('Ctrl Pts',(-15.0642614837351,-9.22419980378748E-16,
565.15));
#155089=CARTESIAN_POINT('Ctrl Pts',(-14.9360126444255,1.38402539194953,
563.655882352941));
#155090=CARTESIAN_POINT('Ctrl Pts',(-14.8077638051159,2.76805078389906,
562.161764705883));
#155091=CARTESIAN_POINT('Ctrl Pts',(-14.4273846475923,4.10494485108124,
560.667647058824));
#155092=CARTESIAN_POINT('Ctrl Pts',(-14.0470054900687,5.44183891826343,
559.173529411765));
#155093=CARTESIAN_POINT('Ctrl Pts',(-13.4274493703259,6.68607533664807,
557.679411764706));
#155094=CARTESIAN_POINT('Ctrl Pts',(-12.8078932505832,7.93031175503273,
556.185294117647));
#155095=CARTESIAN_POINT('Ctrl Pts',(-11.9702584092036,9.03951954568884,
554.691176470588));
#155096=CARTESIAN_POINT('Ctrl Pts',(-11.132623567824,10.148727336345,553.19705882353));
#155097=CARTESIAN_POINT('Ctrl Pts',(-10.1054346546984,11.0851337583099,
551.702941176471));
#155098=CARTESIAN_POINT('Ctrl Pts',(-9.07824574157275,12.0215401802748,
550.208823529412));
#155099=CARTESIAN_POINT('Ctrl Pts',(-7.89648244316034,12.7532570359442,
548.714705882353));
#155100=CARTESIAN_POINT('Ctrl Pts',(-6.71471914474793,13.4849738916136,
547.220588235294));
#155101=CARTESIAN_POINT('Ctrl Pts',(-5.41862499280729,13.9870834410653,
545.726470588235));
#155102=CARTESIAN_POINT('Ctrl Pts',(-4.12253084086667,14.4891929905171,
544.232352941176));
#155103=CARTESIAN_POINT('Ctrl Pts',(-2.75624276724856,14.7445964952585,
542.738235294118));
#155104=CARTESIAN_POINT('Ctrl Pts',(-1.38995469363044,15.,541.244117647059));
#155105=CARTESIAN_POINT('Ctrl Pts',(-1.83697019872103E-15,15.,539.75));
#155106=CARTESIAN_POINT('Ctrl Pts',(1.38995469363045,15.,538.255882352941));
#155107=CARTESIAN_POINT('Ctrl Pts',(2.75624276724855,14.7445964952585,536.761764705882));
#155108=CARTESIAN_POINT('Ctrl Pts',(4.12253084086666,14.4891929905171,535.267647058824));
#155109=CARTESIAN_POINT('Ctrl Pts',(5.4186249928073,13.9870834410653,533.773529411765));
#155110=CARTESIAN_POINT('Ctrl Pts',(6.71471914474792,13.4849738916136,532.279411764706));
#155111=CARTESIAN_POINT('Ctrl Pts',(7.89648244316034,12.7532570359442,530.785294117647));
#155112=CARTESIAN_POINT('Ctrl Pts',(9.07824574157275,12.0215401802748,529.291176470588));
#155113=CARTESIAN_POINT('Ctrl Pts',(10.1054346546984,11.0851337583099,527.797058823529));
#155114=CARTESIAN_POINT('Ctrl Pts',(11.132623567824,10.148727336345,526.302941176471));
#155115=CARTESIAN_POINT('Ctrl Pts',(11.9702584092036,9.03951954568885,524.808823529412));
#155116=CARTESIAN_POINT('Ctrl Pts',(12.8078932505832,7.93031175503273,523.314705882353));
#155117=CARTESIAN_POINT('Ctrl Pts',(13.4274493703259,6.68607533664807,521.820588235294));
#155118=CARTESIAN_POINT('Ctrl Pts',(14.0470054900687,5.44183891826343,520.326470588235));
#155119=CARTESIAN_POINT('Ctrl Pts',(14.4273846475923,4.10494485108125,518.832352941177));
#155120=CARTESIAN_POINT('Ctrl Pts',(14.8077638051159,2.76805078389905,517.338235294118));
#155121=CARTESIAN_POINT('Ctrl Pts',(14.9360126444255,1.38402539194953,515.844117647059));
#155122=CARTESIAN_POINT('Ctrl Pts',(15.0642614837351,2.76725994113625E-15,
514.35));
#155123=CARTESIAN_POINT('Ctrl Pts',(14.9360126444255,-1.38402539194952,
512.855882352941));
#155124=CARTESIAN_POINT('Ctrl Pts',(14.8077638051159,-2.76805078389906,
511.361764705882));
#155125=CARTESIAN_POINT('Ctrl Pts',(14.4273846475923,-4.10494485108124,
509.867647058824));
#155126=CARTESIAN_POINT('Ctrl Pts',(14.0470054900687,-5.44183891826342,
508.373529411765));
#155127=CARTESIAN_POINT('Ctrl Pts',(13.4274493703259,-6.68607533664808,
506.879411764706));
#155128=CARTESIAN_POINT('Ctrl Pts',(12.8078932505832,-7.93031175503273,
505.385294117647));
#155129=CARTESIAN_POINT('Ctrl Pts',(11.9702584092036,-9.03951954568884,
503.891176470588));
#155130=CARTESIAN_POINT('Ctrl Pts',(11.132623567824,-10.148727336345,502.39705882353));
#155131=CARTESIAN_POINT('Ctrl Pts',(10.1054346546984,-11.0851337583099,
500.902941176471));
#155132=CARTESIAN_POINT('Ctrl Pts',(9.07824574157275,-12.0215401802748,
499.408823529412));
#155133=CARTESIAN_POINT('Ctrl Pts',(7.89648244316034,-12.7532570359442,
497.914705882353));
#155134=CARTESIAN_POINT('Ctrl Pts',(6.71471914474792,-13.4849738916136,
496.420588235294));
#155135=CARTESIAN_POINT('Ctrl Pts',(5.4186249928073,-13.9870834410653,494.926470588235));
#155136=CARTESIAN_POINT('Ctrl Pts',(4.12253084086667,-14.4891929905171,
493.432352941177));
#155137=CARTESIAN_POINT('Ctrl Pts',(2.75624276724855,-14.7445964952585,
491.938235294118));
#155138=CARTESIAN_POINT('Ctrl Pts',(1.38995469363045,-15.,490.444117647059));
#155139=CARTESIAN_POINT('Ctrl Pts',(0.,-15.,488.95));
#155140=CARTESIAN_POINT('Ctrl Pts',(-1.38995469363045,-15.,487.455882352941));
#155141=CARTESIAN_POINT('Ctrl Pts',(-2.75624276724856,-14.7445964952585,
485.961764705883));
#155142=CARTESIAN_POINT('Ctrl Pts',(-4.12253084086666,-14.4891929905171,
484.467647058824));
#155143=CARTESIAN_POINT('Ctrl Pts',(-5.41862499280729,-13.9870834410653,
482.973529411765));
#155144=CARTESIAN_POINT('Ctrl Pts',(-6.71471914474793,-13.4849738916136,
481.479411764706));
#155145=CARTESIAN_POINT('Ctrl Pts',(-7.89648244316034,-12.7532570359442,
479.985294117647));
#155146=CARTESIAN_POINT('Ctrl Pts',(-9.07824574157275,-12.0215401802748,
478.491176470588));
#155147=CARTESIAN_POINT('Ctrl Pts',(-10.1054346546984,-11.0851337583099,
476.99705882353));
#155148=CARTESIAN_POINT('Ctrl Pts',(-11.132623567824,-10.148727336345,475.502941176471));
#155149=CARTESIAN_POINT('Ctrl Pts',(-11.9702584092036,-9.03951954568885,
474.008823529412));
#155150=CARTESIAN_POINT('Ctrl Pts',(-12.8078932505832,-7.93031175503273,
472.514705882353));
#155151=CARTESIAN_POINT('Ctrl Pts',(-13.4274493703259,-6.68607533664808,
471.020588235294));
#155152=CARTESIAN_POINT('Ctrl Pts',(-14.0470054900687,-5.44183891826343,
469.526470588235));
#155153=CARTESIAN_POINT('Ctrl Pts',(-14.4273846475923,-4.10494485108124,
468.032352941177));
#155154=CARTESIAN_POINT('Ctrl Pts',(-14.8077638051159,-2.76805078389906,
466.538235294118));
#155155=CARTESIAN_POINT('Ctrl Pts',(-14.9360126444255,-1.38402539194953,
465.044117647059));
#155156=CARTESIAN_POINT('Ctrl Pts',(-15.0642614837351,-9.22419980378748E-16,
463.55));
#155157=CARTESIAN_POINT('Ctrl Pts',(-14.9360126444255,1.38402539194953,
462.055882352941));
#155158=CARTESIAN_POINT('Ctrl Pts',(-14.8077638051159,2.76805078389906,
460.561764705882));
#155159=CARTESIAN_POINT('Ctrl Pts',(-14.4273846475923,4.10494485108124,
459.067647058824));
#155160=CARTESIAN_POINT('Ctrl Pts',(-14.0470054900687,5.44183891826343,
457.573529411765));
#155161=CARTESIAN_POINT('Ctrl Pts',(-13.4274493703259,6.68607533664807,
456.079411764706));
#155162=CARTESIAN_POINT('Ctrl Pts',(-12.8078932505832,7.93031175503273,
454.585294117647));
#155163=CARTESIAN_POINT('Ctrl Pts',(-11.9702584092036,9.03951954568884,
453.091176470588));
#155164=CARTESIAN_POINT('Ctrl Pts',(-11.132623567824,10.148727336345,451.597058823529));
#155165=CARTESIAN_POINT('Ctrl Pts',(-10.1054346546984,11.0851337583099,
450.102941176471));
#155166=CARTESIAN_POINT('Ctrl Pts',(-9.07824574157275,12.0215401802748,
448.608823529412));
#155167=CARTESIAN_POINT('Ctrl Pts',(-7.89648244316034,12.7532570359442,
447.114705882353));
#155168=CARTESIAN_POINT('Ctrl Pts',(-6.71471914474793,13.4849738916136,
445.620588235294));
#155169=CARTESIAN_POINT('Ctrl Pts',(-5.41862499280729,13.9870834410653,
444.126470588235));
#155170=CARTESIAN_POINT('Ctrl Pts',(-4.12253084086667,14.4891929905171,
442.632352941176));
#155171=CARTESIAN_POINT('Ctrl Pts',(-2.75624276724856,14.7445964952585,
441.138235294118));
#155172=CARTESIAN_POINT('Ctrl Pts',(-1.38995469363044,15.,439.644117647059));
#155173=CARTESIAN_POINT('Ctrl Pts',(-1.83697019872103E-15,15.,438.15));
#155174=CARTESIAN_POINT('Ctrl Pts',(1.38995469363045,15.,436.655882352941));
#155175=CARTESIAN_POINT('Ctrl Pts',(2.75624276724855,14.7445964952585,435.161764705882));
#155176=CARTESIAN_POINT('Ctrl Pts',(4.12253084086666,14.4891929905171,433.667647058824));
#155177=CARTESIAN_POINT('Ctrl Pts',(5.4186249928073,13.9870834410653,432.173529411765));
#155178=CARTESIAN_POINT('Ctrl Pts',(6.71471914474792,13.4849738916136,430.679411764706));
#155179=CARTESIAN_POINT('Ctrl Pts',(7.89648244316034,12.7532570359442,429.185294117647));
#155180=CARTESIAN_POINT('Ctrl Pts',(9.07824574157275,12.0215401802748,427.691176470588));
#155181=CARTESIAN_POINT('Ctrl Pts',(10.1054346546984,11.0851337583099,426.19705882353));
#155182=CARTESIAN_POINT('Ctrl Pts',(11.132623567824,10.148727336345,424.702941176471));
#155183=CARTESIAN_POINT('Ctrl Pts',(11.9702584092036,9.03951954568885,423.208823529412));
#155184=CARTESIAN_POINT('Ctrl Pts',(12.8078932505832,7.93031175503273,421.714705882353));
#155185=CARTESIAN_POINT('Ctrl Pts',(13.4274493703259,6.68607533664807,420.220588235294));
#155186=CARTESIAN_POINT('Ctrl Pts',(14.0470054900687,5.44183891826343,418.726470588235));
#155187=CARTESIAN_POINT('Ctrl Pts',(14.4273846475923,4.10494485108125,417.232352941177));
#155188=CARTESIAN_POINT('Ctrl Pts',(14.8077638051159,2.76805078389905,415.738235294118));
#155189=CARTESIAN_POINT('Ctrl Pts',(14.9360126444255,1.38402539194953,414.244117647059));
#155190=CARTESIAN_POINT('Ctrl Pts',(15.0642614837351,2.76725994113625E-15,
412.75));
#155191=CARTESIAN_POINT('Ctrl Pts',(14.9360126444255,-1.38402539194952,
411.255882352941));
#155192=CARTESIAN_POINT('Ctrl Pts',(14.8077638051159,-2.76805078389906,
409.761764705883));
#155193=CARTESIAN_POINT('Ctrl Pts',(14.4273846475923,-4.10494485108124,
408.267647058824));
#155194=CARTESIAN_POINT('Ctrl Pts',(14.0470054900687,-5.44183891826342,
406.773529411765));
#155195=CARTESIAN_POINT('Ctrl Pts',(13.4274493703259,-6.68607533664808,
405.279411764706));
#155196=CARTESIAN_POINT('Ctrl Pts',(12.8078932505832,-7.93031175503273,
403.785294117647));
#155197=CARTESIAN_POINT('Ctrl Pts',(11.9702584092036,-9.03951954568884,
402.291176470588));
#155198=CARTESIAN_POINT('Ctrl Pts',(11.132623567824,-10.148727336345,400.797058823529));
#155199=CARTESIAN_POINT('Ctrl Pts',(10.1054346546984,-11.0851337583099,
399.302941176471));
#155200=CARTESIAN_POINT('Ctrl Pts',(9.07824574157275,-12.0215401802748,
397.808823529412));
#155201=CARTESIAN_POINT('Ctrl Pts',(7.89648244316034,-12.7532570359442,
396.314705882353));
#155202=CARTESIAN_POINT('Ctrl Pts',(6.71471914474792,-13.4849738916136,
394.820588235294));
#155203=CARTESIAN_POINT('Ctrl Pts',(5.4186249928073,-13.9870834410653,393.326470588235));
#155204=CARTESIAN_POINT('Ctrl Pts',(4.12253084086667,-14.4891929905171,
391.832352941177));
#155205=CARTESIAN_POINT('Ctrl Pts',(2.75624276724855,-14.7445964952585,
390.338235294118));
#155206=CARTESIAN_POINT('Ctrl Pts',(1.38995469363045,-15.,388.844117647059));
#155207=CARTESIAN_POINT('Ctrl Pts',(0.,-15.,387.35));
#155208=CARTESIAN_POINT('Ctrl Pts',(-1.38995469363045,-15.,385.855882352941));
#155209=CARTESIAN_POINT('Ctrl Pts',(-2.75624276724856,-14.7445964952585,
384.361764705882));
#155210=CARTESIAN_POINT('Ctrl Pts',(-4.12253084086666,-14.4891929905171,
382.867647058824));
#155211=CARTESIAN_POINT('Ctrl Pts',(-5.41862499280729,-13.9870834410653,
381.373529411765));
#155212=CARTESIAN_POINT('Ctrl Pts',(-6.71471914474793,-13.4849738916136,
379.879411764706));
#155213=CARTESIAN_POINT('Ctrl Pts',(-7.89648244316034,-12.7532570359442,
378.385294117647));
#155214=CARTESIAN_POINT('Ctrl Pts',(-9.07824574157275,-12.0215401802748,
376.891176470588));
#155215=CARTESIAN_POINT('Ctrl Pts',(-10.1054346546984,-11.0851337583099,
375.397058823529));
#155216=CARTESIAN_POINT('Ctrl Pts',(-11.132623567824,-10.148727336345,373.902941176471));
#155217=CARTESIAN_POINT('Ctrl Pts',(-11.9702584092036,-9.03951954568885,
372.408823529412));
#155218=CARTESIAN_POINT('Ctrl Pts',(-12.8078932505832,-7.93031175503273,
370.914705882353));
#155219=CARTESIAN_POINT('Ctrl Pts',(-13.4274493703259,-6.68607533664808,
369.420588235294));
#155220=CARTESIAN_POINT('Ctrl Pts',(-14.0470054900687,-5.44183891826343,
367.926470588235));
#155221=CARTESIAN_POINT('Ctrl Pts',(-14.4273846475923,-4.10494485108124,
366.432352941177));
#155222=CARTESIAN_POINT('Ctrl Pts',(-14.8077638051159,-2.76805078389906,
364.938235294118));
#155223=CARTESIAN_POINT('Ctrl Pts',(-14.9360126444255,-1.38402539194953,
363.444117647059));
#155224=CARTESIAN_POINT('Ctrl Pts',(-15.0642614837351,-9.22419980378748E-16,
361.95));
#155225=CARTESIAN_POINT('Ctrl Pts',(-14.9360126444255,1.38402539194953,
360.455882352941));
#155226=CARTESIAN_POINT('Ctrl Pts',(-14.8077638051159,2.76805078389906,
358.961764705882));
#155227=CARTESIAN_POINT('Ctrl Pts',(-14.4273846475923,4.10494485108124,
357.467647058824));
#155228=CARTESIAN_POINT('Ctrl Pts',(-14.0470054900687,5.44183891826343,
355.973529411765));
#155229=CARTESIAN_POINT('Ctrl Pts',(-13.4274493703259,6.68607533664807,
354.479411764706));
#155230=CARTESIAN_POINT('Ctrl Pts',(-12.8078932505832,7.93031175503273,
352.985294117647));
#155231=CARTESIAN_POINT('Ctrl Pts',(-11.9702584092036,9.03951954568884,
351.491176470588));
#155232=CARTESIAN_POINT('Ctrl Pts',(-11.132623567824,10.148727336345,349.99705882353));
#155233=CARTESIAN_POINT('Ctrl Pts',(-10.1054346546984,11.0851337583099,
348.502941176471));
#155234=CARTESIAN_POINT('Ctrl Pts',(-9.07824574157275,12.0215401802748,
347.008823529412));
#155235=CARTESIAN_POINT('Ctrl Pts',(-7.89648244316034,12.7532570359442,
345.514705882353));
#155236=CARTESIAN_POINT('Ctrl Pts',(-6.71471914474793,13.4849738916136,
344.020588235294));
#155237=CARTESIAN_POINT('Ctrl Pts',(-5.41862499280729,13.9870834410653,
342.526470588235));
#155238=CARTESIAN_POINT('Ctrl Pts',(-4.12253084086667,14.4891929905171,
341.032352941177));
#155239=CARTESIAN_POINT('Ctrl Pts',(-2.75624276724856,14.7445964952585,
339.538235294118));
#155240=CARTESIAN_POINT('Ctrl Pts',(-1.38995469363044,15.,338.044117647059));
#155241=CARTESIAN_POINT('Ctrl Pts',(-1.83697019872103E-15,15.,336.55));
#155242=CARTESIAN_POINT('Ctrl Pts',(1.38995469363045,15.,335.055882352941));
#155243=CARTESIAN_POINT('Ctrl Pts',(2.75624276724855,14.7445964952585,333.561764705882));
#155244=CARTESIAN_POINT('Ctrl Pts',(4.12253084086666,14.4891929905171,332.067647058824));
#155245=CARTESIAN_POINT('Ctrl Pts',(5.4186249928073,13.9870834410653,330.573529411765));
#155246=CARTESIAN_POINT('Ctrl Pts',(6.71471914474792,13.4849738916136,329.079411764706));
#155247=CARTESIAN_POINT('Ctrl Pts',(7.89648244316034,12.7532570359442,327.585294117647));
#155248=CARTESIAN_POINT('Ctrl Pts',(9.07824574157275,12.0215401802748,326.091176470588));
#155249=CARTESIAN_POINT('Ctrl Pts',(10.1054346546984,11.0851337583099,324.597058823529));
#155250=CARTESIAN_POINT('Ctrl Pts',(11.132623567824,10.148727336345,323.102941176471));
#155251=CARTESIAN_POINT('Ctrl Pts',(11.9702584092036,9.03951954568885,321.608823529412));
#155252=CARTESIAN_POINT('Ctrl Pts',(12.8078932505832,7.93031175503273,320.114705882353));
#155253=CARTESIAN_POINT('Ctrl Pts',(13.4274493703259,6.68607533664807,318.620588235294));
#155254=CARTESIAN_POINT('Ctrl Pts',(14.0470054900687,5.44183891826343,317.126470588235));
#155255=CARTESIAN_POINT('Ctrl Pts',(14.4273846475923,4.10494485108125,315.632352941176));
#155256=CARTESIAN_POINT('Ctrl Pts',(14.8077638051159,2.76805078389905,314.138235294118));
#155257=CARTESIAN_POINT('Ctrl Pts',(14.9360126444255,1.38402539194953,312.644117647059));
#155258=CARTESIAN_POINT('Ctrl Pts',(15.0642614837351,2.76725994113625E-15,
311.15));
#155259=CARTESIAN_POINT('Ctrl Pts',(14.9360126444255,-1.38402539194952,
309.655882352941));
#155260=CARTESIAN_POINT('Ctrl Pts',(14.8077638051159,-2.76805078389906,
308.161764705882));
#155261=CARTESIAN_POINT('Ctrl Pts',(14.4273846475923,-4.10494485108124,
306.667647058824));
#155262=CARTESIAN_POINT('Ctrl Pts',(14.0470054900687,-5.44183891826342,
305.173529411765));
#155263=CARTESIAN_POINT('Ctrl Pts',(13.4274493703259,-6.68607533664808,
303.679411764706));
#155264=CARTESIAN_POINT('Ctrl Pts',(12.8078932505832,-7.93031175503273,
302.185294117647));
#155265=CARTESIAN_POINT('Ctrl Pts',(11.9702584092036,-9.03951954568884,
300.691176470588));
#155266=CARTESIAN_POINT('Ctrl Pts',(11.132623567824,-10.148727336345,299.19705882353));
#155267=CARTESIAN_POINT('Ctrl Pts',(10.1054346546984,-11.0851337583099,
297.702941176471));
#155268=CARTESIAN_POINT('Ctrl Pts',(9.07824574157275,-12.0215401802748,
296.208823529412));
#155269=CARTESIAN_POINT('Ctrl Pts',(7.89648244316034,-12.7532570359442,
294.714705882353));
#155270=CARTESIAN_POINT('Ctrl Pts',(6.71471914474792,-13.4849738916136,
293.220588235294));
#155271=CARTESIAN_POINT('Ctrl Pts',(5.4186249928073,-13.9870834410653,291.726470588235));
#155272=CARTESIAN_POINT('Ctrl Pts',(4.12253084086667,-14.4891929905171,
290.232352941176));
#155273=CARTESIAN_POINT('Ctrl Pts',(2.75624276724855,-14.7445964952585,
288.738235294118));
#155274=CARTESIAN_POINT('Ctrl Pts',(1.38995469363045,-15.,287.244117647059));
#155275=CARTESIAN_POINT('Ctrl Pts',(0.,-15.,285.75));
#155276=CARTESIAN_POINT('Ctrl Pts',(-1.38995469363045,-15.,284.255882352941));
#155277=CARTESIAN_POINT('Ctrl Pts',(-2.75624276724856,-14.7445964952585,
282.761764705882));
#155278=CARTESIAN_POINT('Ctrl Pts',(-4.12253084086666,-14.4891929905171,
281.267647058824));
#155279=CARTESIAN_POINT('Ctrl Pts',(-5.41862499280729,-13.9870834410653,
279.773529411765));
#155280=CARTESIAN_POINT('Ctrl Pts',(-6.71471914474793,-13.4849738916136,
278.279411764706));
#155281=CARTESIAN_POINT('Ctrl Pts',(-7.89648244316034,-12.7532570359442,
276.785294117647));
#155282=CARTESIAN_POINT('Ctrl Pts',(-9.07824574157275,-12.0215401802748,
275.291176470588));
#155283=CARTESIAN_POINT('Ctrl Pts',(-10.1054346546984,-11.0851337583099,
273.797058823529));
#155284=CARTESIAN_POINT('Ctrl Pts',(-11.132623567824,-10.148727336345,272.302941176471));
#155285=CARTESIAN_POINT('Ctrl Pts',(-11.9702584092036,-9.03951954568885,
270.808823529412));
#155286=CARTESIAN_POINT('Ctrl Pts',(-12.8078932505832,-7.93031175503273,
269.314705882353));
#155287=CARTESIAN_POINT('Ctrl Pts',(-13.4274493703259,-6.68607533664808,
267.820588235294));
#155288=CARTESIAN_POINT('Ctrl Pts',(-14.0470054900687,-5.44183891826343,
266.326470588235));
#155289=CARTESIAN_POINT('Ctrl Pts',(-14.4273846475923,-4.10494485108124,
264.832352941177));
#155290=CARTESIAN_POINT('Ctrl Pts',(-14.8077638051159,-2.76805078389906,
263.338235294118));
#155291=CARTESIAN_POINT('Ctrl Pts',(-14.9360126444255,-1.38402539194953,
261.844117647059));
#155292=CARTESIAN_POINT('Ctrl Pts',(-15.0642614837351,-9.22419980378748E-16,
260.35));
#155293=CARTESIAN_POINT('Ctrl Pts',(-14.9360126444255,1.38402539194953,
258.855882352941));
#155294=CARTESIAN_POINT('Ctrl Pts',(-14.8077638051159,2.76805078389906,
257.361764705882));
#155295=CARTESIAN_POINT('Ctrl Pts',(-14.4273846475923,4.10494485108124,
255.867647058823));
#155296=CARTESIAN_POINT('Ctrl Pts',(-14.0470054900687,5.44183891826343,
254.373529411765));
#155297=CARTESIAN_POINT('Ctrl Pts',(-13.4274493703259,6.68607533664807,
252.879411764706));
#155298=CARTESIAN_POINT('Ctrl Pts',(-12.8078932505832,7.93031175503273,
251.385294117647));
#155299=CARTESIAN_POINT('Ctrl Pts',(-11.9702584092036,9.03951954568884,
249.891176470588));
#155300=CARTESIAN_POINT('Ctrl Pts',(-11.132623567824,10.148727336345,248.397058823529));
#155301=CARTESIAN_POINT('Ctrl Pts',(-10.1054346546984,11.0851337583099,
246.902941176471));
#155302=CARTESIAN_POINT('Ctrl Pts',(-9.07824574157275,12.0215401802748,
245.408823529412));
#155303=CARTESIAN_POINT('Ctrl Pts',(-7.89648244316034,12.7532570359442,
243.914705882353));
#155304=CARTESIAN_POINT('Ctrl Pts',(-6.71471914474793,13.4849738916136,
242.420588235294));
#155305=CARTESIAN_POINT('Ctrl Pts',(-5.41862499280729,13.9870834410653,
240.926470588235));
#155306=CARTESIAN_POINT('Ctrl Pts',(-4.12253084086667,14.4891929905171,
239.432352941177));
#155307=CARTESIAN_POINT('Ctrl Pts',(-2.75624276724856,14.7445964952585,
237.938235294118));
#155308=CARTESIAN_POINT('Ctrl Pts',(-1.38995469363044,15.,236.444117647059));
#155309=CARTESIAN_POINT('Ctrl Pts',(-1.83697019872103E-15,15.,234.95));
#155310=CARTESIAN_POINT('Ctrl Pts',(1.38995469363045,15.,233.455882352941));
#155311=CARTESIAN_POINT('Ctrl Pts',(2.75624276724855,14.7445964952585,231.961764705883));
#155312=CARTESIAN_POINT('Ctrl Pts',(4.12253084086666,14.4891929905171,230.467647058824));
#155313=CARTESIAN_POINT('Ctrl Pts',(5.4186249928073,13.9870834410653,228.973529411765));
#155314=CARTESIAN_POINT('Ctrl Pts',(6.71471914474792,13.4849738916136,227.479411764706));
#155315=CARTESIAN_POINT('Ctrl Pts',(7.89648244316034,12.7532570359442,225.985294117647));
#155316=CARTESIAN_POINT('Ctrl Pts',(9.07824574157275,12.0215401802748,224.491176470588));
#155317=CARTESIAN_POINT('Ctrl Pts',(10.1054346546984,11.0851337583099,222.99705882353));
#155318=CARTESIAN_POINT('Ctrl Pts',(11.132623567824,10.148727336345,221.502941176471));
#155319=CARTESIAN_POINT('Ctrl Pts',(11.9702584092036,9.03951954568885,220.008823529412));
#155320=CARTESIAN_POINT('Ctrl Pts',(12.8078932505832,7.93031175503273,218.514705882353));
#155321=CARTESIAN_POINT('Ctrl Pts',(13.4274493703259,6.68607533664807,217.020588235294));
#155322=CARTESIAN_POINT('Ctrl Pts',(14.0470054900687,5.44183891826343,215.526470588235));
#155323=CARTESIAN_POINT('Ctrl Pts',(14.4273846475923,4.10494485108125,214.032352941176));
#155324=CARTESIAN_POINT('Ctrl Pts',(14.8077638051159,2.76805078389905,212.538235294118));
#155325=CARTESIAN_POINT('Ctrl Pts',(14.9360126444255,1.38402539194953,211.044117647059));
#155326=CARTESIAN_POINT('Ctrl Pts',(15.0642614837351,2.76725994113625E-15,
209.55));
#155327=CARTESIAN_POINT('Ctrl Pts',(14.9360126444255,-1.38402539194952,
208.055882352941));
#155328=CARTESIAN_POINT('Ctrl Pts',(14.8077638051159,-2.76805078389906,
206.561764705882));
#155329=CARTESIAN_POINT('Ctrl Pts',(14.4273846475923,-4.10494485108124,
205.067647058824));
#155330=CARTESIAN_POINT('Ctrl Pts',(14.0470054900687,-5.44183891826342,
203.573529411765));
#155331=CARTESIAN_POINT('Ctrl Pts',(13.4274493703259,-6.68607533664808,
202.079411764706));
#155332=CARTESIAN_POINT('Ctrl Pts',(12.8078932505832,-7.93031175503273,
200.585294117647));
#155333=CARTESIAN_POINT('Ctrl Pts',(11.9702584092036,-9.03951954568884,
199.091176470588));
#155334=CARTESIAN_POINT('Ctrl Pts',(11.132623567824,-10.148727336345,197.597058823529));
#155335=CARTESIAN_POINT('Ctrl Pts',(10.1054346546984,-11.0851337583099,
196.102941176471));
#155336=CARTESIAN_POINT('Ctrl Pts',(9.07824574157275,-12.0215401802748,
194.608823529412));
#155337=CARTESIAN_POINT('Ctrl Pts',(7.89648244316034,-12.7532570359442,
193.114705882353));
#155338=CARTESIAN_POINT('Ctrl Pts',(6.71471914474792,-13.4849738916136,
191.620588235294));
#155339=CARTESIAN_POINT('Ctrl Pts',(5.4186249928073,-13.9870834410653,190.126470588235));
#155340=CARTESIAN_POINT('Ctrl Pts',(4.12253084086667,-14.4891929905171,
188.632352941176));
#155341=CARTESIAN_POINT('Ctrl Pts',(2.75624276724855,-14.7445964952585,
187.138235294118));
#155342=CARTESIAN_POINT('Ctrl Pts',(1.38995469363045,-15.,185.644117647059));
#155343=CARTESIAN_POINT('Ctrl Pts',(0.,-15.,184.15));
#155344=CARTESIAN_POINT('Ctrl Pts',(-1.38995469363045,-15.,182.655882352941));
#155345=CARTESIAN_POINT('Ctrl Pts',(-2.75624276724856,-14.7445964952585,
181.161764705882));
#155346=CARTESIAN_POINT('Ctrl Pts',(-4.12253084086666,-14.4891929905171,
179.667647058824));
#155347=CARTESIAN_POINT('Ctrl Pts',(-5.41862499280729,-13.9870834410653,
178.173529411765));
#155348=CARTESIAN_POINT('Ctrl Pts',(-6.71471914474793,-13.4849738916136,
176.679411764706));
#155349=CARTESIAN_POINT('Ctrl Pts',(-7.89648244316034,-12.7532570359442,
175.185294117647));
#155350=CARTESIAN_POINT('Ctrl Pts',(-9.07824574157275,-12.0215401802748,
173.691176470588));
#155351=CARTESIAN_POINT('Ctrl Pts',(-10.1054346546984,-11.0851337583099,
172.19705882353));
#155352=CARTESIAN_POINT('Ctrl Pts',(-11.132623567824,-10.148727336345,170.702941176471));
#155353=CARTESIAN_POINT('Ctrl Pts',(-11.9702584092036,-9.03951954568885,
169.208823529412));
#155354=CARTESIAN_POINT('Ctrl Pts',(-12.8078932505832,-7.93031175503273,
167.714705882353));
#155355=CARTESIAN_POINT('Ctrl Pts',(-13.4274493703259,-6.68607533664808,
166.220588235294));
#155356=CARTESIAN_POINT('Ctrl Pts',(-14.0470054900687,-5.44183891826343,
164.726470588235));
#155357=CARTESIAN_POINT('Ctrl Pts',(-14.4273846475923,-4.10494485108124,
163.232352941177));
#155358=CARTESIAN_POINT('Ctrl Pts',(-14.8077638051159,-2.76805078389906,
161.738235294118));
#155359=CARTESIAN_POINT('Ctrl Pts',(-14.9360126444255,-1.38402539194953,
160.244117647059));
#155360=CARTESIAN_POINT('Ctrl Pts',(-15.0642614837351,-9.22419980378748E-16,
158.75));
#155361=CARTESIAN_POINT('Ctrl Pts',(-14.9360126444255,1.38402539194953,
157.255882352941));
#155362=CARTESIAN_POINT('Ctrl Pts',(-14.8077638051159,2.76805078389906,
155.761764705882));
#155363=CARTESIAN_POINT('Ctrl Pts',(-14.4273846475923,4.10494485108124,
154.267647058824));
#155364=CARTESIAN_POINT('Ctrl Pts',(-14.0470054900687,5.44183891826343,
152.773529411765));
#155365=CARTESIAN_POINT('Ctrl Pts',(-13.4274493703259,6.68607533664807,
151.279411764706));
#155366=CARTESIAN_POINT('Ctrl Pts',(-12.8078932505832,7.93031175503273,
149.785294117647));
#155367=CARTESIAN_POINT('Ctrl Pts',(-11.9702584092036,9.03951954568884,
148.291176470588));
#155368=CARTESIAN_POINT('Ctrl Pts',(-11.132623567824,10.148727336345,146.79705882353));
#155369=CARTESIAN_POINT('Ctrl Pts',(-10.1054346546984,11.0851337583099,
145.302941176471));
#155370=CARTESIAN_POINT('Ctrl Pts',(-9.07824574157275,12.0215401802748,
143.808823529412));
#155371=CARTESIAN_POINT('Ctrl Pts',(-7.89648244316034,12.7532570359442,
142.314705882353));
#155372=CARTESIAN_POINT('Ctrl Pts',(-6.71471914474793,13.4849738916136,
140.820588235294));
#155373=CARTESIAN_POINT('Ctrl Pts',(-5.41862499280729,13.9870834410653,
139.326470588235));
#155374=CARTESIAN_POINT('Ctrl Pts',(-4.12253084086667,14.4891929905171,
137.832352941177));
#155375=CARTESIAN_POINT('Ctrl Pts',(-2.75624276724856,14.7445964952585,
136.338235294118));
#155376=CARTESIAN_POINT('Ctrl Pts',(-1.38995469363044,15.,134.844117647059));
#155377=CARTESIAN_POINT('Ctrl Pts',(-1.83697019872103E-15,15.,133.35));
#155378=CARTESIAN_POINT('Ctrl Pts',(1.38995469363045,15.,131.855882352941));
#155379=CARTESIAN_POINT('Ctrl Pts',(2.75624276724855,14.7445964952585,130.361764705882));
#155380=CARTESIAN_POINT('Ctrl Pts',(4.12253084086666,14.4891929905171,128.867647058824));
#155381=CARTESIAN_POINT('Ctrl Pts',(5.4186249928073,13.9870834410653,127.373529411765));
#155382=CARTESIAN_POINT('Ctrl Pts',(6.71471914474792,13.4849738916136,125.879411764706));
#155383=CARTESIAN_POINT('Ctrl Pts',(7.89648244316034,12.7532570359442,124.385294117647));
#155384=CARTESIAN_POINT('Ctrl Pts',(9.07824574157275,12.0215401802748,122.891176470588));
#155385=CARTESIAN_POINT('Ctrl Pts',(10.1054346546984,11.0851337583099,121.397058823529));
#155386=CARTESIAN_POINT('Ctrl Pts',(11.132623567824,10.148727336345,119.902941176471));
#155387=CARTESIAN_POINT('Ctrl Pts',(11.9702584092036,9.03951954568885,118.408823529412));
#155388=CARTESIAN_POINT('Ctrl Pts',(12.8078932505832,7.93031175503273,116.914705882353));
#155389=CARTESIAN_POINT('Ctrl Pts',(13.4274493703259,6.68607533664807,115.420588235294));
#155390=CARTESIAN_POINT('Ctrl Pts',(14.0470054900687,5.44183891826343,113.926470588235));
#155391=CARTESIAN_POINT('Ctrl Pts',(14.4273846475923,4.10494485108125,112.432352941177));
#155392=CARTESIAN_POINT('Ctrl Pts',(14.8077638051159,2.76805078389905,110.938235294118));
#155393=CARTESIAN_POINT('Ctrl Pts',(14.9360126444255,1.38402539194953,109.444117647059));
#155394=CARTESIAN_POINT('Ctrl Pts',(15.0642614837351,2.76725994113625E-15,
107.95));
#155395=CARTESIAN_POINT('Ctrl Pts',(14.9360126444255,-1.38402539194952,
106.455882352941));
#155396=CARTESIAN_POINT('Ctrl Pts',(14.8077638051159,-2.76805078389906,
104.961764705882));
#155397=CARTESIAN_POINT('Ctrl Pts',(14.4273846475923,-4.10494485108124,
103.467647058824));
#155398=CARTESIAN_POINT('Ctrl Pts',(14.0470054900687,-5.44183891826342,
101.973529411765));
#155399=CARTESIAN_POINT('Ctrl Pts',(13.4274493703259,-6.68607533664808,
100.479411764706));
#155400=CARTESIAN_POINT('Ctrl Pts',(12.8078932505832,-7.93031175503273,
98.985294117647));
#155401=CARTESIAN_POINT('Ctrl Pts',(11.9702584092036,-9.03951954568884,
97.4911764705884));
#155402=CARTESIAN_POINT('Ctrl Pts',(11.132623567824,-10.148727336345,95.9970588235295));
#155403=CARTESIAN_POINT('Ctrl Pts',(10.1054346546984,-11.0851337583099,
94.5029411764706));
#155404=CARTESIAN_POINT('Ctrl Pts',(9.07824574157275,-12.0215401802748,
93.0088235294117));
#155405=CARTESIAN_POINT('Ctrl Pts',(7.89648244316034,-12.7532570359442,
91.5147058823529));
#155406=CARTESIAN_POINT('Ctrl Pts',(6.71471914474792,-13.4849738916136,
90.0205882352942));
#155407=CARTESIAN_POINT('Ctrl Pts',(5.4186249928073,-13.9870834410653,88.5264705882354));
#155408=CARTESIAN_POINT('Ctrl Pts',(4.12253084086667,-14.4891929905171,
87.0323529411765));
#155409=CARTESIAN_POINT('Ctrl Pts',(2.75624276724855,-14.7445964952585,
85.5382352941176));
#155410=CARTESIAN_POINT('Ctrl Pts',(1.38995469363045,-15.,84.0441176470588));
#155411=CARTESIAN_POINT('Ctrl Pts',(0.,-15.,82.5500000000001));
#155412=CARTESIAN_POINT('Ctrl Pts',(-1.38995469363045,-15.,81.0558823529413));
#155413=CARTESIAN_POINT('Ctrl Pts',(-2.75624276724856,-14.7445964952585,
79.5617647058824));
#155414=CARTESIAN_POINT('Ctrl Pts',(-4.12253084086666,-14.4891929905171,
78.0676470588235));
#155415=CARTESIAN_POINT('Ctrl Pts',(-5.41862499280729,-13.9870834410653,
76.5735294117647));
#155416=CARTESIAN_POINT('Ctrl Pts',(-6.71471914474793,-13.4849738916136,
75.079411764706));
#155417=CARTESIAN_POINT('Ctrl Pts',(-7.89648244316034,-12.7532570359442,
73.5852941176471));
#155418=CARTESIAN_POINT('Ctrl Pts',(-9.07824574157275,-12.0215401802748,
72.0911764705883));
#155419=CARTESIAN_POINT('Ctrl Pts',(-10.1054346546984,-11.0851337583099,
70.5970588235294));
#155420=CARTESIAN_POINT('Ctrl Pts',(-11.132623567824,-10.148727336345,69.1029411764705));
#155421=CARTESIAN_POINT('Ctrl Pts',(-11.9702584092036,-9.03951954568885,
67.6088235294119));
#155422=CARTESIAN_POINT('Ctrl Pts',(-12.8078932505832,-7.93031175503273,
66.114705882353));
#155423=CARTESIAN_POINT('Ctrl Pts',(-13.4274493703259,-6.68607533664808,
64.6205882352942));
#155424=CARTESIAN_POINT('Ctrl Pts',(-14.0470054900687,-5.44183891826343,
63.1264705882353));
#155425=CARTESIAN_POINT('Ctrl Pts',(-14.4273846475923,-4.10494485108124,
61.6323529411764));
#155426=CARTESIAN_POINT('Ctrl Pts',(-14.8077638051159,-2.76805078389906,
60.1382352941178));
#155427=CARTESIAN_POINT('Ctrl Pts',(-14.9360126444255,-1.38402539194953,
58.6441176470589));
#155428=CARTESIAN_POINT('Ctrl Pts',(-15.0642614837351,-9.22419980378748E-16,
57.15));
#155429=CARTESIAN_POINT('Ctrl Pts',(-14.9360126444255,1.38402539194953,
55.6558823529412));
#155430=CARTESIAN_POINT('Ctrl Pts',(-14.8077638051159,2.76805078389906,
54.1617647058823));
#155431=CARTESIAN_POINT('Ctrl Pts',(-14.4273846475923,4.10494485108124,
52.6676470588237));
#155432=CARTESIAN_POINT('Ctrl Pts',(-14.0470054900687,5.44183891826343,
51.1735294117648));
#155433=CARTESIAN_POINT('Ctrl Pts',(-13.4274493703259,6.68607533664807,
49.6794117647059));
#155434=CARTESIAN_POINT('Ctrl Pts',(-12.8078932505832,7.93031175503273,
48.185294117647));
#155435=CARTESIAN_POINT('Ctrl Pts',(-11.9702584092036,9.03951954568884,
46.6911764705882));
#155436=CARTESIAN_POINT('Ctrl Pts',(-11.132623567824,10.148727336345,45.1970588235295));
#155437=CARTESIAN_POINT('Ctrl Pts',(-10.1054346546984,11.0851337583099,
43.7029411764707));
#155438=CARTESIAN_POINT('Ctrl Pts',(-9.07824574157275,12.0215401802748,
42.2088235294118));
#155439=CARTESIAN_POINT('Ctrl Pts',(-7.89648244316034,12.7532570359442,
40.7147058823529));
#155440=CARTESIAN_POINT('Ctrl Pts',(-6.71471914474793,13.4849738916136,
39.2205882352941));
#155441=CARTESIAN_POINT('Ctrl Pts',(-5.41862499280729,13.9870834410653,
37.7264705882354));
#155442=CARTESIAN_POINT('Ctrl Pts',(-4.12253084086667,14.4891929905171,
36.2323529411766));
#155443=CARTESIAN_POINT('Ctrl Pts',(-2.75624276724856,14.7445964952585,
34.7382352941177));
#155444=CARTESIAN_POINT('Ctrl Pts',(-1.38995469363044,15.,33.2441176470588));
#155445=CARTESIAN_POINT('Ctrl Pts',(-1.83697019872103E-15,15.,31.7499999999999));
#155446=CARTESIAN_POINT('Ctrl Pts',(1.38995469363045,15.,30.2558823529413));
#155447=CARTESIAN_POINT('Ctrl Pts',(2.75624276724855,14.7445964952585,28.7617647058824));
#155448=CARTESIAN_POINT('Ctrl Pts',(4.12253084086666,14.4891929905171,27.2676470588236));
#155449=CARTESIAN_POINT('Ctrl Pts',(5.4186249928073,13.9870834410653,25.7735294117647));
#155450=CARTESIAN_POINT('Ctrl Pts',(6.71471914474792,13.4849738916136,24.2794117647058));
#155451=CARTESIAN_POINT('Ctrl Pts',(7.89648244316034,12.7532570359442,22.7852941176472));
#155452=CARTESIAN_POINT('Ctrl Pts',(9.07824574157275,12.0215401802748,21.2911764705883));
#155453=CARTESIAN_POINT('Ctrl Pts',(10.1054346546984,11.0851337583099,19.7970588235294));
#155454=CARTESIAN_POINT('Ctrl Pts',(11.132623567824,10.148727336345,18.3029411764706));
#155455=CARTESIAN_POINT('Ctrl Pts',(11.9702584092036,9.03951954568885,16.8088235294117));
#155456=CARTESIAN_POINT('Ctrl Pts',(12.8078932505832,7.93031175503273,15.3147058823531));
#155457=CARTESIAN_POINT('Ctrl Pts',(13.4274493703259,6.68607533664807,13.8205882352942));
#155458=CARTESIAN_POINT('Ctrl Pts',(14.0470054900687,5.44183891826343,12.3264705882353));
#155459=CARTESIAN_POINT('Ctrl Pts',(14.4273846475923,4.10494485108125,10.8323529411765));
#155460=CARTESIAN_POINT('Ctrl Pts',(14.8077638051159,2.76805078389905,9.33823529411759));
#155461=CARTESIAN_POINT('Ctrl Pts',(14.9360126444255,1.38402539194953,7.84411764705895));
#155462=CARTESIAN_POINT('Ctrl Pts',(15.0642614837351,2.76725994113625E-15,
6.35000000000008));
#155463=CARTESIAN_POINT('Ctrl Pts',(14.9360126444255,-1.38402539194952,
4.85588235294121));
#155464=CARTESIAN_POINT('Ctrl Pts',(14.8077638051159,-2.76805078389906,
3.36176470588234));
#155465=CARTESIAN_POINT('Ctrl Pts',(14.4273846475923,-4.10494485108124,
1.86764705882347));
#155466=CARTESIAN_POINT('Ctrl Pts',(14.0470054900687,-5.44183891826342,
0.373529411764828));
#155467=CARTESIAN_POINT('Ctrl Pts',(13.4274493703259,-6.68607533664808,
-1.12058823529404));
#155468=CARTESIAN_POINT('Ctrl Pts',(12.8078932505832,-7.93031175503273,
-2.61470588235291));
#155469=CARTESIAN_POINT('Ctrl Pts',(11.9702584092036,-9.03951954568884,
-4.10882352941178));
#155470=CARTESIAN_POINT('Ctrl Pts',(11.132623567824,-10.148727336345,-5.60294117647064));
#155471=CARTESIAN_POINT('Ctrl Pts',(10.1054346546984,-11.0851337583099,
-7.09705882352929));
#155472=CARTESIAN_POINT('Ctrl Pts',(9.07824574157275,-12.0215401802748,
-8.59117647058816));
#155473=CARTESIAN_POINT('Ctrl Pts',(7.89648244316034,-12.7532570359442,
-10.085294117647));
#155474=CARTESIAN_POINT('Ctrl Pts',(6.71471914474792,-13.4849738916136,
-11.5794117647059));
#155475=CARTESIAN_POINT('Ctrl Pts',(5.4186249928073,-13.9870834410653,-13.0735294117648));
#155476=CARTESIAN_POINT('Ctrl Pts',(4.12253084086667,-14.4891929905171,
-14.5676470588234));
#155477=CARTESIAN_POINT('Ctrl Pts',(2.75624276724855,-14.7445964952585,
-16.0617647058823));
#155478=CARTESIAN_POINT('Ctrl Pts',(1.38995469363045,-15.,-17.5558823529411));
#155479=CARTESIAN_POINT('Ctrl Pts',(0.,-15.,-19.05));
#155480=CARTESIAN_POINT('Ctrl Pts',(-1.38995469363045,-15.,-20.5441176470589));
#155481=CARTESIAN_POINT('Ctrl Pts',(-2.75624276724856,-14.7445964952585,
-22.0382352941175));
#155482=CARTESIAN_POINT('Ctrl Pts',(-4.12253084086666,-14.4891929905171,
-23.5323529411764));
#155483=CARTESIAN_POINT('Ctrl Pts',(-5.41862499280729,-13.9870834410653,
-25.0264705882353));
#155484=CARTESIAN_POINT('Ctrl Pts',(-6.71471914474793,-13.4849738916136,
-26.5205882352941));
#155485=CARTESIAN_POINT('Ctrl Pts',(-7.89648244316034,-12.7532570359442,
-28.014705882353));
#155486=CARTESIAN_POINT('Ctrl Pts',(-9.07824574157275,-12.0215401802748,
-29.5088235294116));
#155487=CARTESIAN_POINT('Ctrl Pts',(-10.1054346546984,-11.0851337583099,
-31.0029411764705));
#155488=CARTESIAN_POINT('Ctrl Pts',(-11.132623567824,-10.148727336345,-32.4970588235294));
#155489=CARTESIAN_POINT('Ctrl Pts',(-11.9702584092036,-9.03951954568885,
-33.9911764705882));
#155490=CARTESIAN_POINT('Ctrl Pts',(-12.8078932505832,-7.93031175503273,
-35.4852941176471));
#155491=CARTESIAN_POINT('Ctrl Pts',(-13.4274493703259,-6.68607533664808,
-36.9794117647058));
#155492=CARTESIAN_POINT('Ctrl Pts',(-14.0470054900687,-5.44183891826343,
-38.4735294117646));
#155493=CARTESIAN_POINT('Ctrl Pts',(-14.4273846475923,-4.10494485108124,
-39.9676470588235));
#155494=CARTESIAN_POINT('Ctrl Pts',(-14.8077638051159,-2.76805078389906,
-41.4617647058824));
#155495=CARTESIAN_POINT('Ctrl Pts',(-14.9360126444255,-1.38402539194953,
-42.9558823529412));
#155496=CARTESIAN_POINT('Ctrl Pts',(-15.0642614837351,-9.22419980378748E-16,
-44.4499999999999));
#155497=CARTESIAN_POINT('Ctrl Pts',(-14.9360126444255,1.38402539194953,
-45.9441176470587));
#155498=CARTESIAN_POINT('Ctrl Pts',(-14.8077638051159,2.76805078389906,
-47.4382352941176));
#155499=CARTESIAN_POINT('Ctrl Pts',(-14.4273846475923,4.10494485108124,
-48.9323529411765));
#155500=CARTESIAN_POINT('Ctrl Pts',(-14.0470054900687,5.44183891826343,
-50.4264705882354));
#155501=CARTESIAN_POINT('Ctrl Pts',(-13.4274493703259,6.68607533664807,
-51.920588235294));
#155502=CARTESIAN_POINT('Ctrl Pts',(-12.8078932505832,7.93031175503273,
-53.4147058823529));
#155503=CARTESIAN_POINT('Ctrl Pts',(-11.9702584092036,9.03951954568884,
-54.9088235294117));
#155504=CARTESIAN_POINT('Ctrl Pts',(-11.132623567824,10.148727336345,-56.4029411764706));
#155505=CARTESIAN_POINT('Ctrl Pts',(-10.1054346546984,11.0851337583099,
-57.8970588235295));
#155506=CARTESIAN_POINT('Ctrl Pts',(-9.07824574157275,12.0215401802748,
-59.3911764705881));
#155507=CARTESIAN_POINT('Ctrl Pts',(-7.89648244316034,12.7532570359442,
-60.885294117647));
#155508=CARTESIAN_POINT('Ctrl Pts',(-6.71471914474793,13.4849738916136,
-62.3794117647059));
#155509=CARTESIAN_POINT('Ctrl Pts',(-5.41862499280729,13.9870834410653,
-63.8735294117647));
#155510=CARTESIAN_POINT('Ctrl Pts',(-4.12253084086667,14.4891929905171,
-65.3676470588236));
#155511=CARTESIAN_POINT('Ctrl Pts',(-2.75624276724856,14.7445964952585,
-66.8617647058822));
#155512=CARTESIAN_POINT('Ctrl Pts',(-1.38995469363044,15.,-68.3558823529411));
#155513=CARTESIAN_POINT('Ctrl Pts',(-1.83697019872103E-15,15.,-69.85));
#155514=CARTESIAN_POINT('Ctrl Pts',(1.38995469363045,15.,-71.3441176470589));
#155515=CARTESIAN_POINT('Ctrl Pts',(2.75624276724855,14.7445964952585,-72.8382352941177));
#155516=CARTESIAN_POINT('Ctrl Pts',(4.12253084086666,14.4891929905171,-74.3323529411764));
#155517=CARTESIAN_POINT('Ctrl Pts',(5.4186249928073,13.9870834410653,-75.8264705882352));
#155518=CARTESIAN_POINT('Ctrl Pts',(6.71471914474792,13.4849738916136,-77.3205882352941));
#155519=CARTESIAN_POINT('Ctrl Pts',(7.89648244316034,12.7532570359442,-78.814705882353));
#155520=CARTESIAN_POINT('Ctrl Pts',(9.07824574157275,12.0215401802748,-80.3088235294118));
#155521=CARTESIAN_POINT('Ctrl Pts',(10.1054346546984,11.0851337583099,-81.8029411764705));
#155522=CARTESIAN_POINT('Ctrl Pts',(11.132623567824,10.148727336345,-83.2970588235294));
#155523=CARTESIAN_POINT('Ctrl Pts',(11.9702584092036,9.03951954568885,-84.7911764705882));
#155524=CARTESIAN_POINT('Ctrl Pts',(12.8078932505832,7.93031175503273,-86.2852941176471));
#155525=CARTESIAN_POINT('Ctrl Pts',(13.4274493703259,6.68607533664807,-87.7794117647059));
#155526=CARTESIAN_POINT('Ctrl Pts',(14.0470054900687,5.44183891826343,-89.2735294117646));
#155527=CARTESIAN_POINT('Ctrl Pts',(14.4273846475923,4.10494485108125,-90.7676470588235));
#155528=CARTESIAN_POINT('Ctrl Pts',(14.8077638051159,2.76805078389905,-92.2617647058823));
#155529=CARTESIAN_POINT('Ctrl Pts',(14.9360126444255,1.38402539194953,-93.7558823529412));
#155530=CARTESIAN_POINT('Ctrl Pts',(15.0642614837351,2.76725994113625E-15,
-95.2500000000001));
#155531=CARTESIAN_POINT('Ctrl Pts',(14.9360126444255,-1.38402539194952,
-96.7441176470587));
#155532=CARTESIAN_POINT('Ctrl Pts',(14.8077638051159,-2.76805078389906,
-98.2382352941176));
#155533=CARTESIAN_POINT('Ctrl Pts',(14.4273846475923,-4.10494485108124,
-99.7323529411764));
#155534=CARTESIAN_POINT('Ctrl Pts',(14.0470054900687,-5.44183891826342,
-101.226470588235));
#155535=CARTESIAN_POINT('Ctrl Pts',(13.4274493703259,-6.68607533664808,
-102.720588235294));
#155536=CARTESIAN_POINT('Ctrl Pts',(12.8078932505832,-7.93031175503273,
-104.214705882353));
#155537=CARTESIAN_POINT('Ctrl Pts',(11.9702584092036,-9.03951954568884,
-105.708823529412));
#155538=CARTESIAN_POINT('Ctrl Pts',(11.132623567824,-10.148727336345,-107.202941176471));
#155539=CARTESIAN_POINT('Ctrl Pts',(10.1054346546984,-11.0851337583099,
-108.697058823529));
#155540=CARTESIAN_POINT('Ctrl Pts',(9.07824574157275,-12.0215401802748,
-110.191176470588));
#155541=CARTESIAN_POINT('Ctrl Pts',(7.89648244316034,-12.7532570359442,
-111.685294117647));
#155542=CARTESIAN_POINT('Ctrl Pts',(6.71471914474792,-13.4849738916136,
-113.179411764706));
#155543=CARTESIAN_POINT('Ctrl Pts',(5.4186249928073,-13.9870834410653,-114.673529411765));
#155544=CARTESIAN_POINT('Ctrl Pts',(4.12253084086667,-14.4891929905171,
-116.167647058824));
#155545=CARTESIAN_POINT('Ctrl Pts',(2.75624276724855,-14.7445964952585,
-117.661764705882));
#155546=CARTESIAN_POINT('Ctrl Pts',(1.38995469363045,-15.,-119.155882352941));
#155547=CARTESIAN_POINT('Ctrl Pts',(0.,-15.,-120.65));
#155548=CARTESIAN_POINT('Ctrl Pts',(-1.38995469363045,-15.,-122.144117647059));
#155549=CARTESIAN_POINT('Ctrl Pts',(-2.75624276724856,-14.7445964952585,
-123.638235294118));
#155550=CARTESIAN_POINT('Ctrl Pts',(-4.12253084086666,-14.4891929905171,
-125.132352941177));
#155551=CARTESIAN_POINT('Ctrl Pts',(-5.41862499280729,-13.9870834410653,
-126.626470588235));
#155552=CARTESIAN_POINT('Ctrl Pts',(-6.71471914474793,-13.4849738916136,
-128.120588235294));
#155553=CARTESIAN_POINT('Ctrl Pts',(-7.89648244316034,-12.7532570359442,
-129.614705882353));
#155554=CARTESIAN_POINT('Ctrl Pts',(-9.07824574157275,-12.0215401802748,
-131.108823529412));
#155555=CARTESIAN_POINT('Ctrl Pts',(-10.1054346546984,-11.0851337583099,
-132.602941176471));
#155556=CARTESIAN_POINT('Ctrl Pts',(-11.132623567824,-10.148727336345,-134.097058823529));
#155557=CARTESIAN_POINT('Ctrl Pts',(-11.9702584092036,-9.03951954568885,
-135.591176470588));
#155558=CARTESIAN_POINT('Ctrl Pts',(-12.8078932505832,-7.93031175503273,
-137.085294117647));
#155559=CARTESIAN_POINT('Ctrl Pts',(-13.4274493703259,-6.68607533664808,
-138.579411764706));
#155560=CARTESIAN_POINT('Ctrl Pts',(-14.0470054900687,-5.44183891826343,
-140.073529411765));
#155561=CARTESIAN_POINT('Ctrl Pts',(-14.4273846475923,-4.10494485108124,
-141.567647058823));
#155562=CARTESIAN_POINT('Ctrl Pts',(-14.8077638051159,-2.76805078389906,
-143.061764705882));
#155563=CARTESIAN_POINT('Ctrl Pts',(-14.9360126444255,-1.38402539194953,
-144.555882352941));
#155564=CARTESIAN_POINT('Ctrl Pts',(-15.0642614837351,-9.22419980378748E-16,
-146.05));
#155565=CARTESIAN_POINT('Ctrl Pts',(-14.9360126444255,1.38402539194953,
-147.544117647059));
#155566=CARTESIAN_POINT('Ctrl Pts',(-14.8077638051159,2.76805078389906,
-149.038235294118));
#155567=CARTESIAN_POINT('Ctrl Pts',(-14.4273846475923,4.10494485108124,
-150.532352941176));
#155568=CARTESIAN_POINT('Ctrl Pts',(-14.0470054900687,5.44183891826343,
-152.026470588235));
#155569=CARTESIAN_POINT('Ctrl Pts',(-13.4274493703259,6.68607533664807,
-153.520588235294));
#155570=CARTESIAN_POINT('Ctrl Pts',(-12.8078932505832,7.93031175503273,
-155.014705882353));
#155571=CARTESIAN_POINT('Ctrl Pts',(-11.9702584092036,9.03951954568884,
-156.508823529412));
#155572=CARTESIAN_POINT('Ctrl Pts',(-11.132623567824,10.148727336345,-158.002941176471));
#155573=CARTESIAN_POINT('Ctrl Pts',(-10.1054346546984,11.0851337583099,
-159.497058823529));
#155574=CARTESIAN_POINT('Ctrl Pts',(-9.07824574157275,12.0215401802748,
-160.991176470588));
#155575=CARTESIAN_POINT('Ctrl Pts',(-7.89648244316034,12.7532570359442,
-162.485294117647));
#155576=CARTESIAN_POINT('Ctrl Pts',(-6.71471914474793,13.4849738916136,
-163.979411764706));
#155577=CARTESIAN_POINT('Ctrl Pts',(-5.41862499280729,13.9870834410653,
-165.473529411765));
#155578=CARTESIAN_POINT('Ctrl Pts',(-4.12253084086667,14.4891929905171,
-166.967647058824));
#155579=CARTESIAN_POINT('Ctrl Pts',(-2.75624276724856,14.7445964952585,
-168.461764705882));
#155580=CARTESIAN_POINT('Ctrl Pts',(-1.38995469363044,15.,-169.955882352941));
#155581=CARTESIAN_POINT('Ctrl Pts',(-1.83697019872103E-15,15.,-171.45));
#155582=CARTESIAN_POINT('Ctrl Pts',(1.38995469363045,15.,-172.944117647059));
#155583=CARTESIAN_POINT('Ctrl Pts',(2.75624276724855,14.7445964952585,-174.438235294118));
#155584=CARTESIAN_POINT('Ctrl Pts',(4.12253084086666,14.4891929905171,-175.932352941176));
#155585=CARTESIAN_POINT('Ctrl Pts',(5.4186249928073,13.9870834410653,-177.426470588235));
#155586=CARTESIAN_POINT('Ctrl Pts',(6.71471914474792,13.4849738916136,-178.920588235294));
#155587=CARTESIAN_POINT('Ctrl Pts',(7.89648244316034,12.7532570359442,-180.414705882353));
#155588=CARTESIAN_POINT('Ctrl Pts',(9.07824574157275,12.0215401802748,-181.908823529412));
#155589=CARTESIAN_POINT('Ctrl Pts',(10.1054346546984,11.0851337583099,-183.402941176471));
#155590=CARTESIAN_POINT('Ctrl Pts',(11.132623567824,10.148727336345,-184.897058823529));
#155591=CARTESIAN_POINT('Ctrl Pts',(11.9702584092036,9.03951954568885,-186.391176470588));
#155592=CARTESIAN_POINT('Ctrl Pts',(12.8078932505832,7.93031175503273,-187.885294117647));
#155593=CARTESIAN_POINT('Ctrl Pts',(13.4274493703259,6.68607533664807,-189.379411764706));
#155594=CARTESIAN_POINT('Ctrl Pts',(14.0470054900687,5.44183891826343,-190.873529411765));
#155595=CARTESIAN_POINT('Ctrl Pts',(14.4273846475923,4.10494485108125,-192.367647058824));
#155596=CARTESIAN_POINT('Ctrl Pts',(14.8077638051159,2.76805078389905,-193.861764705882));
#155597=CARTESIAN_POINT('Ctrl Pts',(14.9360126444255,1.38402539194953,-195.355882352941));
#155598=CARTESIAN_POINT('Ctrl Pts',(15.0642614837351,2.76725994113625E-15,
-196.85));
#155599=CARTESIAN_POINT('Ctrl Pts',(14.9360126444255,-1.38402539194952,
-198.344117647059));
#155600=CARTESIAN_POINT('Ctrl Pts',(14.8077638051159,-2.76805078389906,
-199.838235294118));
#155601=CARTESIAN_POINT('Ctrl Pts',(14.4273846475923,-4.10494485108124,
-201.332352941176));
#155602=CARTESIAN_POINT('Ctrl Pts',(14.0470054900687,-5.44183891826342,
-202.826470588235));
#155603=CARTESIAN_POINT('Ctrl Pts',(13.4274493703259,-6.68607533664808,
-204.320588235294));
#155604=CARTESIAN_POINT('Ctrl Pts',(12.8078932505832,-7.93031175503273,
-205.814705882353));
#155605=CARTESIAN_POINT('Ctrl Pts',(11.9702584092036,-9.03951954568884,
-207.308823529412));
#155606=CARTESIAN_POINT('Ctrl Pts',(11.132623567824,-10.148727336345,-208.80294117647));
#155607=CARTESIAN_POINT('Ctrl Pts',(10.1054346546984,-11.0851337583099,
-210.297058823529));
#155608=CARTESIAN_POINT('Ctrl Pts',(9.07824574157275,-12.0215401802748,
-211.791176470588));
#155609=CARTESIAN_POINT('Ctrl Pts',(7.89648244316034,-12.7532570359442,
-213.285294117647));
#155610=CARTESIAN_POINT('Ctrl Pts',(6.71471914474792,-13.4849738916136,
-214.779411764706));
#155611=CARTESIAN_POINT('Ctrl Pts',(5.4186249928073,-13.9870834410653,-216.273529411765));
#155612=CARTESIAN_POINT('Ctrl Pts',(4.12253084086667,-14.4891929905171,
-217.767647058823));
#155613=CARTESIAN_POINT('Ctrl Pts',(2.75624276724855,-14.7445964952585,
-219.261764705882));
#155614=CARTESIAN_POINT('Ctrl Pts',(1.38995469363045,-15.,-220.755882352941));
#155615=CARTESIAN_POINT('Ctrl Pts',(0.,-15.,-222.25));
#155616=CARTESIAN_POINT('Ctrl Pts',(-1.38995469363045,-15.,-223.744117647059));
#155617=CARTESIAN_POINT('Ctrl Pts',(-2.75624276724856,-14.7445964952585,
-225.238235294118));
#155618=CARTESIAN_POINT('Ctrl Pts',(-4.12253084086666,-14.4891929905171,
-226.732352941176));
#155619=CARTESIAN_POINT('Ctrl Pts',(-5.41862499280729,-13.9870834410653,
-228.226470588235));
#155620=CARTESIAN_POINT('Ctrl Pts',(-6.71471914474793,-13.4849738916136,
-229.720588235294));
#155621=CARTESIAN_POINT('Ctrl Pts',(-7.89648244316034,-12.7532570359442,
-231.214705882353));
#155622=CARTESIAN_POINT('Ctrl Pts',(-9.07824574157275,-12.0215401802748,
-232.708823529412));
#155623=CARTESIAN_POINT('Ctrl Pts',(-10.1054346546984,-11.0851337583099,
-234.202941176471));
#155624=CARTESIAN_POINT('Ctrl Pts',(-11.132623567824,-10.148727336345,-235.697058823529));
#155625=CARTESIAN_POINT('Ctrl Pts',(-11.9702584092036,-9.03951954568885,
-237.191176470588));
#155626=CARTESIAN_POINT('Ctrl Pts',(-12.8078932505832,-7.93031175503273,
-238.685294117647));
#155627=CARTESIAN_POINT('Ctrl Pts',(-13.4274493703259,-6.68607533664808,
-240.179411764706));
#155628=CARTESIAN_POINT('Ctrl Pts',(-14.0470054900687,-5.44183891826343,
-241.673529411765));
#155629=CARTESIAN_POINT('Ctrl Pts',(-14.4273846475923,-4.10494485108124,
-243.167647058824));
#155630=CARTESIAN_POINT('Ctrl Pts',(-14.8077638051159,-2.76805078389906,
-244.661764705882));
#155631=CARTESIAN_POINT('Ctrl Pts',(-14.9360126444255,-1.38402539194953,
-246.155882352941));
#155632=CARTESIAN_POINT('Ctrl Pts',(-15.0642614837351,-9.22419980378748E-16,
-247.65));
#155633=CARTESIAN_POINT('Ctrl Pts',(-14.9360126444255,1.38402539194953,
-249.144117647059));
#155634=CARTESIAN_POINT('Ctrl Pts',(-14.8077638051159,2.76805078389906,
-250.638235294118));
#155635=CARTESIAN_POINT('Ctrl Pts',(-14.4273846475923,4.10494485108124,
-252.132352941177));
#155636=CARTESIAN_POINT('Ctrl Pts',(-14.0470054900687,5.44183891826343,
-253.626470588235));
#155637=CARTESIAN_POINT('Ctrl Pts',(-13.4274493703259,6.68607533664807,
-255.120588235294));
#155638=CARTESIAN_POINT('Ctrl Pts',(-12.8078932505832,7.93031175503273,
-256.614705882353));
#155639=CARTESIAN_POINT('Ctrl Pts',(-11.9702584092036,9.03951954568884,
-258.108823529412));
#155640=CARTESIAN_POINT('Ctrl Pts',(-11.132623567824,10.148727336345,-259.602941176471));
#155641=CARTESIAN_POINT('Ctrl Pts',(-10.1054346546984,11.0851337583099,
-261.097058823529));
#155642=CARTESIAN_POINT('Ctrl Pts',(-9.07824574157275,12.0215401802748,
-262.591176470588));
#155643=CARTESIAN_POINT('Ctrl Pts',(-7.89648244316034,12.7532570359442,
-264.085294117647));
#155644=CARTESIAN_POINT('Ctrl Pts',(-6.71471914474793,13.4849738916136,
-265.579411764706));
#155645=CARTESIAN_POINT('Ctrl Pts',(-5.41862499280729,13.9870834410653,
-267.073529411765));
#155646=CARTESIAN_POINT('Ctrl Pts',(-4.12253084086667,14.4891929905171,
-268.567647058823));
#155647=CARTESIAN_POINT('Ctrl Pts',(-2.75624276724856,14.7445964952585,
-270.061764705882));
#155648=CARTESIAN_POINT('Ctrl Pts',(-1.38995469363044,15.,-271.555882352941));
#155649=CARTESIAN_POINT('Ctrl Pts',(-1.83697019872103E-15,15.,-273.05));
#155650=CARTESIAN_POINT('Ctrl Pts',(1.38995469363045,15.,-274.544117647059));
#155651=CARTESIAN_POINT('Ctrl Pts',(2.75624276724855,14.7445964952585,-276.038235294118));
#155652=CARTESIAN_POINT('Ctrl Pts',(4.12253084086666,14.4891929905171,-277.532352941176));
#155653=CARTESIAN_POINT('Ctrl Pts',(5.4186249928073,13.9870834410653,-279.026470588235));
#155654=CARTESIAN_POINT('Ctrl Pts',(6.71471914474792,13.4849738916136,-280.520588235294));
#155655=CARTESIAN_POINT('Ctrl Pts',(7.89648244316034,12.7532570359442,-282.014705882353));
#155656=CARTESIAN_POINT('Ctrl Pts',(9.07824574157275,12.0215401802748,-283.508823529412));
#155657=CARTESIAN_POINT('Ctrl Pts',(10.1054346546984,11.0851337583099,-285.002941176471));
#155658=CARTESIAN_POINT('Ctrl Pts',(11.132623567824,10.148727336345,-286.497058823529));
#155659=CARTESIAN_POINT('Ctrl Pts',(11.9702584092036,9.03951954568885,-287.991176470588));
#155660=CARTESIAN_POINT('Ctrl Pts',(12.8078932505832,7.93031175503273,-289.485294117647));
#155661=CARTESIAN_POINT('Ctrl Pts',(13.4274493703259,6.68607533664807,-290.979411764706));
#155662=CARTESIAN_POINT('Ctrl Pts',(14.0470054900687,5.44183891826343,-292.473529411765));
#155663=CARTESIAN_POINT('Ctrl Pts',(14.4273846475923,4.10494485108125,-293.967647058824));
#155664=CARTESIAN_POINT('Ctrl Pts',(14.8077638051159,2.76805078389905,-295.461764705882));
#155665=CARTESIAN_POINT('Ctrl Pts',(14.9360126444255,1.38402539194953,-296.955882352941));
#155666=CARTESIAN_POINT('Ctrl Pts',(15.0642614837351,2.76725994113625E-15,
-298.45));
#155667=CARTESIAN_POINT('Ctrl Pts',(14.9360126444255,-1.38402539194952,
-299.944117647059));
#155668=CARTESIAN_POINT('Ctrl Pts',(14.8077638051159,-2.76805078389906,
-301.438235294118));
#155669=CARTESIAN_POINT('Ctrl Pts',(14.4273846475923,-4.10494485108124,
-302.932352941177));
#155670=CARTESIAN_POINT('Ctrl Pts',(14.0470054900687,-5.44183891826342,
-304.426470588235));
#155671=CARTESIAN_POINT('Ctrl Pts',(13.4274493703259,-6.68607533664808,
-305.920588235294));
#155672=CARTESIAN_POINT('Ctrl Pts',(12.8078932505832,-7.93031175503273,
-307.414705882353));
#155673=CARTESIAN_POINT('Ctrl Pts',(11.9702584092036,-9.03951954568884,
-308.908823529412));
#155674=CARTESIAN_POINT('Ctrl Pts',(11.132623567824,-10.148727336345,-310.402941176471));
#155675=CARTESIAN_POINT('Ctrl Pts',(10.1054346546984,-11.0851337583099,
-311.897058823529));
#155676=CARTESIAN_POINT('Ctrl Pts',(9.07824574157275,-12.0215401802748,
-313.391176470588));
#155677=CARTESIAN_POINT('Ctrl Pts',(7.89648244316034,-12.7532570359442,
-314.885294117647));
#155678=CARTESIAN_POINT('Ctrl Pts',(6.71471914474792,-13.4849738916136,
-316.379411764706));
#155679=CARTESIAN_POINT('Ctrl Pts',(5.4186249928073,-13.9870834410653,-317.873529411765));
#155680=CARTESIAN_POINT('Ctrl Pts',(4.12253084086667,-14.4891929905171,
-319.367647058824));
#155681=CARTESIAN_POINT('Ctrl Pts',(2.75624276724855,-14.7445964952585,
-320.861764705882));
#155682=CARTESIAN_POINT('Ctrl Pts',(1.38995469363045,-15.,-322.355882352941));
#155683=CARTESIAN_POINT('Ctrl Pts',(0.,-15.,-323.85));
#155684=CARTESIAN_POINT('Ctrl Pts',(-1.38995469363045,-15.,-325.344117647059));
#155685=CARTESIAN_POINT('Ctrl Pts',(-2.75624276724856,-14.7445964952585,
-326.838235294118));
#155686=CARTESIAN_POINT('Ctrl Pts',(-4.12253084086666,-14.4891929905171,
-328.332352941176));
#155687=CARTESIAN_POINT('Ctrl Pts',(-5.41862499280729,-13.9870834410653,
-329.826470588235));
#155688=CARTESIAN_POINT('Ctrl Pts',(-6.71471914474793,-13.4849738916136,
-331.320588235294));
#155689=CARTESIAN_POINT('Ctrl Pts',(-7.89648244316034,-12.7532570359442,
-332.814705882353));
#155690=CARTESIAN_POINT('Ctrl Pts',(-9.07824574157275,-12.0215401802748,
-334.308823529412));
#155691=CARTESIAN_POINT('Ctrl Pts',(-10.1054346546984,-11.0851337583099,
-335.80294117647));
#155692=CARTESIAN_POINT('Ctrl Pts',(-11.132623567824,-10.148727336345,-337.297058823529));
#155693=CARTESIAN_POINT('Ctrl Pts',(-11.9702584092036,-9.03951954568885,
-338.791176470588));
#155694=CARTESIAN_POINT('Ctrl Pts',(-12.8078932505832,-7.93031175503273,
-340.285294117647));
#155695=CARTESIAN_POINT('Ctrl Pts',(-13.4274493703259,-6.68607533664808,
-341.779411764706));
#155696=CARTESIAN_POINT('Ctrl Pts',(-14.0470054900687,-5.44183891826343,
-343.273529411765));
#155697=CARTESIAN_POINT('Ctrl Pts',(-14.4273846475923,-4.10494485108124,
-344.767647058823));
#155698=CARTESIAN_POINT('Ctrl Pts',(-14.8077638051159,-2.76805078389906,
-346.261764705882));
#155699=CARTESIAN_POINT('Ctrl Pts',(-14.9360126444255,-1.38402539194953,
-347.755882352941));
#155700=CARTESIAN_POINT('Ctrl Pts',(-15.0642614837351,-9.22419980378748E-16,
-349.25));
#155701=CARTESIAN_POINT('Ctrl Pts',(-14.9360126444255,1.38402539194953,
-350.744117647059));
#155702=CARTESIAN_POINT('Ctrl Pts',(-14.8077638051159,2.76805078389906,
-352.238235294118));
#155703=CARTESIAN_POINT('Ctrl Pts',(-14.4273846475923,4.10494485108124,
-353.732352941176));
#155704=CARTESIAN_POINT('Ctrl Pts',(-14.0470054900687,5.44183891826343,
-355.226470588235));
#155705=CARTESIAN_POINT('Ctrl Pts',(-13.4274493703259,6.68607533664807,
-356.720588235294));
#155706=CARTESIAN_POINT('Ctrl Pts',(-12.8078932505832,7.93031175503273,
-358.214705882353));
#155707=CARTESIAN_POINT('Ctrl Pts',(-11.9702584092036,9.03951954568884,
-359.708823529412));
#155708=CARTESIAN_POINT('Ctrl Pts',(-11.132623567824,10.148727336345,-361.202941176471));
#155709=CARTESIAN_POINT('Ctrl Pts',(-10.1054346546984,11.0851337583099,
-362.697058823529));
#155710=CARTESIAN_POINT('Ctrl Pts',(-9.07824574157275,12.0215401802748,
-364.191176470588));
#155711=CARTESIAN_POINT('Ctrl Pts',(-7.89648244316034,12.7532570359442,
-365.685294117647));
#155712=CARTESIAN_POINT('Ctrl Pts',(-6.71471914474793,13.4849738916136,
-367.179411764706));
#155713=CARTESIAN_POINT('Ctrl Pts',(-5.41862499280729,13.9870834410653,
-368.673529411765));
#155714=CARTESIAN_POINT('Ctrl Pts',(-4.12253084086667,14.4891929905171,
-370.167647058824));
#155715=CARTESIAN_POINT('Ctrl Pts',(-2.75624276724856,14.7445964952585,
-371.661764705882));
#155716=CARTESIAN_POINT('Ctrl Pts',(-1.38995469363044,15.,-373.155882352941));
#155717=CARTESIAN_POINT('Ctrl Pts',(-1.83697019872103E-15,15.,-374.65));
#155718=CARTESIAN_POINT('Ctrl Pts',(1.38995469363045,15.,-376.144117647059));
#155719=CARTESIAN_POINT('Ctrl Pts',(2.75624276724855,14.7445964952585,-377.638235294118));
#155720=CARTESIAN_POINT('Ctrl Pts',(4.12253084086666,14.4891929905171,-379.132352941177));
#155721=CARTESIAN_POINT('Ctrl Pts',(5.4186249928073,13.9870834410653,-380.626470588235));
#155722=CARTESIAN_POINT('Ctrl Pts',(6.71471914474792,13.4849738916136,-382.120588235294));
#155723=CARTESIAN_POINT('Ctrl Pts',(7.89648244316034,12.7532570359442,-383.614705882353));
#155724=CARTESIAN_POINT('Ctrl Pts',(9.07824574157275,12.0215401802748,-385.108823529412));
#155725=CARTESIAN_POINT('Ctrl Pts',(10.1054346546984,11.0851337583099,-386.602941176471));
#155726=CARTESIAN_POINT('Ctrl Pts',(11.132623567824,10.148727336345,-388.097058823529));
#155727=CARTESIAN_POINT('Ctrl Pts',(11.9702584092036,9.03951954568885,-389.591176470588));
#155728=CARTESIAN_POINT('Ctrl Pts',(12.8078932505832,7.93031175503273,-391.085294117647));
#155729=CARTESIAN_POINT('Ctrl Pts',(13.4274493703259,6.68607533664807,-392.579411764706));
#155730=CARTESIAN_POINT('Ctrl Pts',(14.0470054900687,5.44183891826343,-394.073529411765));
#155731=CARTESIAN_POINT('Ctrl Pts',(14.4273846475923,4.10494485108125,-395.567647058823));
#155732=CARTESIAN_POINT('Ctrl Pts',(14.8077638051159,2.76805078389905,-397.061764705882));
#155733=CARTESIAN_POINT('Ctrl Pts',(14.9360126444255,1.38402539194953,-398.555882352941));
#155734=CARTESIAN_POINT('Ctrl Pts',(15.0642614837351,2.76725994113625E-15,
-400.05));
#155735=CARTESIAN_POINT('Ctrl Pts',(14.9360126444255,-1.38402539194952,
-401.544117647059));
#155736=CARTESIAN_POINT('Ctrl Pts',(14.8077638051159,-2.76805078389906,
-403.038235294118));
#155737=CARTESIAN_POINT('Ctrl Pts',(14.4273846475923,-4.10494485108124,
-404.532352941176));
#155738=CARTESIAN_POINT('Ctrl Pts',(14.0470054900687,-5.44183891826342,
-406.026470588235));
#155739=CARTESIAN_POINT('Ctrl Pts',(13.4274493703259,-6.68607533664808,
-407.520588235294));
#155740=CARTESIAN_POINT('Ctrl Pts',(12.8078932505832,-7.93031175503273,
-409.014705882353));
#155741=CARTESIAN_POINT('Ctrl Pts',(11.9702584092036,-9.03951954568884,
-410.508823529412));
#155742=CARTESIAN_POINT('Ctrl Pts',(11.132623567824,-10.148727336345,-412.002941176471));
#155743=CARTESIAN_POINT('Ctrl Pts',(10.1054346546984,-11.0851337583099,
-413.497058823529));
#155744=CARTESIAN_POINT('Ctrl Pts',(9.07824574157275,-12.0215401802748,
-414.991176470588));
#155745=CARTESIAN_POINT('Ctrl Pts',(7.89648244316034,-12.7532570359442,
-416.485294117647));
#155746=CARTESIAN_POINT('Ctrl Pts',(6.71471914474792,-13.4849738916136,
-417.979411764706));
#155747=CARTESIAN_POINT('Ctrl Pts',(5.4186249928073,-13.9870834410653,-419.473529411765));
#155748=CARTESIAN_POINT('Ctrl Pts',(4.12253084086667,-14.4891929905171,
-420.967647058824));
#155749=CARTESIAN_POINT('Ctrl Pts',(2.75624276724855,-14.7445964952585,
-422.461764705882));
#155750=CARTESIAN_POINT('Ctrl Pts',(1.38995469363045,-15.,-423.955882352941));
#155751=CARTESIAN_POINT('Ctrl Pts',(0.,-15.,-425.45));
#155752=CARTESIAN_POINT('Ctrl Pts',(-1.38995469363045,-15.,-426.944117647059));
#155753=CARTESIAN_POINT('Ctrl Pts',(-2.75624276724856,-14.7445964952585,
-428.438235294118));
#155754=CARTESIAN_POINT('Ctrl Pts',(-4.12253084086666,-14.4891929905171,
-429.932352941177));
#155755=CARTESIAN_POINT('Ctrl Pts',(-5.41862499280729,-13.9870834410653,
-431.426470588235));
#155756=CARTESIAN_POINT('Ctrl Pts',(-6.71471914474793,-13.4849738916136,
-432.920588235294));
#155757=CARTESIAN_POINT('Ctrl Pts',(-7.89648244316034,-12.7532570359442,
-434.414705882353));
#155758=CARTESIAN_POINT('Ctrl Pts',(-9.07824574157275,-12.0215401802748,
-435.908823529412));
#155759=CARTESIAN_POINT('Ctrl Pts',(-10.1054346546984,-11.0851337583099,
-437.402941176471));
#155760=CARTESIAN_POINT('Ctrl Pts',(-11.132623567824,-10.148727336345,-438.89705882353));
#155761=CARTESIAN_POINT('Ctrl Pts',(-11.9702584092036,-9.03951954568885,
-440.391176470588));
#155762=CARTESIAN_POINT('Ctrl Pts',(-12.8078932505832,-7.93031175503273,
-441.885294117647));
#155763=CARTESIAN_POINT('Ctrl Pts',(-13.4274493703259,-6.68607533664808,
-443.379411764706));
#155764=CARTESIAN_POINT('Ctrl Pts',(-14.0470054900687,-5.44183891826343,
-444.873529411765));
#155765=CARTESIAN_POINT('Ctrl Pts',(-14.4273846475923,-4.10494485108124,
-446.367647058824));
#155766=CARTESIAN_POINT('Ctrl Pts',(-14.8077638051159,-2.76805078389906,
-447.861764705882));
#155767=CARTESIAN_POINT('Ctrl Pts',(-14.9360126444255,-1.38402539194953,
-449.355882352941));
#155768=CARTESIAN_POINT('Ctrl Pts',(-15.0642614837351,-9.22419980378748E-16,
-450.85));
#155769=CARTESIAN_POINT('Ctrl Pts',(-14.9360126444255,1.38402539194953,
-452.344117647059));
#155770=CARTESIAN_POINT('Ctrl Pts',(-14.8077638051159,2.76805078389906,
-453.838235294118));
#155771=CARTESIAN_POINT('Ctrl Pts',(-14.4273846475923,4.10494485108124,
-455.332352941176));
#155772=CARTESIAN_POINT('Ctrl Pts',(-14.0470054900687,5.44183891826343,
-456.826470588235));
#155773=CARTESIAN_POINT('Ctrl Pts',(-13.4274493703259,6.68607533664807,
-458.320588235294));
#155774=CARTESIAN_POINT('Ctrl Pts',(-12.8078932505832,7.93031175503273,
-459.814705882353));
#155775=CARTESIAN_POINT('Ctrl Pts',(-11.9702584092036,9.03951954568884,
-461.308823529412));
#155776=CARTESIAN_POINT('Ctrl Pts',(-11.132623567824,10.148727336345,-462.802941176471));
#155777=CARTESIAN_POINT('Ctrl Pts',(-10.1054346546984,11.0851337583099,
-464.297058823529));
#155778=CARTESIAN_POINT('Ctrl Pts',(-9.07824574157275,12.0215401802748,
-465.791176470588));
#155779=CARTESIAN_POINT('Ctrl Pts',(-7.89648244316034,12.7532570359442,
-467.285294117647));
#155780=CARTESIAN_POINT('Ctrl Pts',(-6.71471914474793,13.4849738916136,
-468.779411764706));
#155781=CARTESIAN_POINT('Ctrl Pts',(-5.41862499280729,13.9870834410653,
-470.273529411765));
#155782=CARTESIAN_POINT('Ctrl Pts',(-4.12253084086667,14.4891929905171,
-471.767647058824));
#155783=CARTESIAN_POINT('Ctrl Pts',(-2.75624276724856,14.7445964952585,
-473.261764705882));
#155784=CARTESIAN_POINT('Ctrl Pts',(-1.38995469363044,15.,-474.755882352941));
#155785=CARTESIAN_POINT('Ctrl Pts',(-1.83697019872103E-15,15.,-476.25));
#155786=CARTESIAN_POINT('Ctrl Pts',(1.38995469363045,15.,-477.744117647059));
#155787=CARTESIAN_POINT('Ctrl Pts',(2.75624276724855,14.7445964952585,-479.238235294118));
#155788=CARTESIAN_POINT('Ctrl Pts',(4.12253084086666,14.4891929905171,-480.732352941176));
#155789=CARTESIAN_POINT('Ctrl Pts',(5.4186249928073,13.9870834410653,-482.226470588235));
#155790=CARTESIAN_POINT('Ctrl Pts',(6.71471914474792,13.4849738916136,-483.720588235294));
#155791=CARTESIAN_POINT('Ctrl Pts',(7.89648244316034,12.7532570359442,-485.214705882353));
#155792=CARTESIAN_POINT('Ctrl Pts',(9.07824574157275,12.0215401802748,-486.708823529412));
#155793=CARTESIAN_POINT('Ctrl Pts',(10.1054346546984,11.0851337583099,-488.202941176471));
#155794=CARTESIAN_POINT('Ctrl Pts',(11.132623567824,10.148727336345,-489.697058823529));
#155795=CARTESIAN_POINT('Ctrl Pts',(11.9702584092036,9.03951954568885,-491.191176470588));
#155796=CARTESIAN_POINT('Ctrl Pts',(12.8078932505832,7.93031175503273,-492.685294117647));
#155797=CARTESIAN_POINT('Ctrl Pts',(13.4274493703259,6.68607533664807,-494.179411764706));
#155798=CARTESIAN_POINT('Ctrl Pts',(14.0470054900687,5.44183891826343,-495.673529411765));
#155799=CARTESIAN_POINT('Ctrl Pts',(14.4273846475923,4.10494485108125,-497.167647058824));
#155800=CARTESIAN_POINT('Ctrl Pts',(14.8077638051159,2.76805078389905,-498.661764705882));
#155801=CARTESIAN_POINT('Ctrl Pts',(14.9360126444255,1.38402539194953,-500.155882352941));
#155802=CARTESIAN_POINT('Ctrl Pts',(15.0642614837351,2.76725994113625E-15,
-501.65));
#155803=CARTESIAN_POINT('Ctrl Pts',(14.9360126444255,-1.38402539194952,
-503.144117647059));
#155804=CARTESIAN_POINT('Ctrl Pts',(14.8077638051159,-2.76805078389906,
-504.638235294118));
#155805=CARTESIAN_POINT('Ctrl Pts',(14.4273846475923,-4.10494485108124,
-506.132352941176));
#155806=CARTESIAN_POINT('Ctrl Pts',(14.0470054900687,-5.44183891826342,
-507.626470588235));
#155807=CARTESIAN_POINT('Ctrl Pts',(13.4274493703259,-6.68607533664808,
-509.120588235294));
#155808=CARTESIAN_POINT('Ctrl Pts',(12.8078932505832,-7.93031175503273,
-510.614705882353));
#155809=CARTESIAN_POINT('Ctrl Pts',(11.9702584092036,-9.03951954568884,
-512.108823529412));
#155810=CARTESIAN_POINT('Ctrl Pts',(11.132623567824,-10.148727336345,-513.602941176471));
#155811=CARTESIAN_POINT('Ctrl Pts',(10.1054346546984,-11.0851337583099,
-515.09705882353));
#155812=CARTESIAN_POINT('Ctrl Pts',(9.07824574157275,-12.0215401802748,
-516.591176470588));
#155813=CARTESIAN_POINT('Ctrl Pts',(7.89648244316034,-12.7532570359442,
-518.085294117647));
#155814=CARTESIAN_POINT('Ctrl Pts',(6.71471914474792,-13.4849738916136,
-519.579411764706));
#155815=CARTESIAN_POINT('Ctrl Pts',(5.4186249928073,-13.9870834410653,-521.073529411765));
#155816=CARTESIAN_POINT('Ctrl Pts',(4.12253084086667,-14.4891929905171,
-522.567647058823));
#155817=CARTESIAN_POINT('Ctrl Pts',(2.75624276724855,-14.7445964952585,
-524.061764705882));
#155818=CARTESIAN_POINT('Ctrl Pts',(1.38995469363045,-15.,-525.555882352941));
#155819=CARTESIAN_POINT('Ctrl Pts',(0.,-15.,-527.05));
#155820=CARTESIAN_POINT('Ctrl Pts',(-1.38995469363045,-15.,-528.544117647059));
#155821=CARTESIAN_POINT('Ctrl Pts',(-2.75624276724856,-14.7445964952585,
-530.038235294118));
#155822=CARTESIAN_POINT('Ctrl Pts',(-4.12253084086666,-14.4891929905171,
-531.532352941177));
#155823=CARTESIAN_POINT('Ctrl Pts',(-5.41862499280729,-13.9870834410653,
-533.026470588235));
#155824=CARTESIAN_POINT('Ctrl Pts',(-6.71471914474793,-13.4849738916136,
-534.520588235294));
#155825=CARTESIAN_POINT('Ctrl Pts',(-7.89648244316034,-12.7532570359442,
-536.014705882353));
#155826=CARTESIAN_POINT('Ctrl Pts',(-9.07824574157275,-12.0215401802748,
-537.508823529412));
#155827=CARTESIAN_POINT('Ctrl Pts',(-10.1054346546984,-11.0851337583099,
-539.00294117647));
#155828=CARTESIAN_POINT('Ctrl Pts',(-11.132623567824,-10.148727336345,-540.49705882353));
#155829=CARTESIAN_POINT('Ctrl Pts',(-11.9702584092036,-9.03951954568885,
-541.991176470588));
#155830=CARTESIAN_POINT('Ctrl Pts',(-12.8078932505832,-7.93031175503273,
-543.485294117647));
#155831=CARTESIAN_POINT('Ctrl Pts',(-13.4274493703259,-6.68607533664808,
-544.979411764706));
#155832=CARTESIAN_POINT('Ctrl Pts',(-14.0470054900687,-5.44183891826343,
-546.473529411765));
#155833=CARTESIAN_POINT('Ctrl Pts',(-14.4273846475923,-4.10494485108124,
-547.967647058823));
#155834=CARTESIAN_POINT('Ctrl Pts',(-14.8077638051159,-2.76805078389906,
-549.461764705882));
#155835=CARTESIAN_POINT('Ctrl Pts',(-14.9360126444255,-1.38402539194953,
-550.955882352941));
#155836=CARTESIAN_POINT('Ctrl Pts',(-15.0642614837351,-9.22419980378748E-16,
-552.45));
#155837=CARTESIAN_POINT('Ctrl Pts',(-14.9360126444255,1.38402539194953,
-553.944117647059));
#155838=CARTESIAN_POINT('Ctrl Pts',(-14.8077638051159,2.76805078389906,
-555.438235294118));
#155839=CARTESIAN_POINT('Ctrl Pts',(-14.4273846475923,4.10494485108124,
-556.932352941177));
#155840=CARTESIAN_POINT('Ctrl Pts',(-14.0470054900687,5.44183891826343,
-558.426470588235));
#155841=CARTESIAN_POINT('Ctrl Pts',(-13.4274493703259,6.68607533664807,
-559.920588235294));
#155842=CARTESIAN_POINT('Ctrl Pts',(-12.8078932505832,7.93031175503273,
-561.414705882353));
#155843=CARTESIAN_POINT('Ctrl Pts',(-11.9702584092036,9.03951954568884,
-562.908823529412));
#155844=CARTESIAN_POINT('Ctrl Pts',(-11.132623567824,10.148727336345,-564.402941176471));
#155845=CARTESIAN_POINT('Ctrl Pts',(-10.1054346546984,11.0851337583099,
-565.897058823529));
#155846=CARTESIAN_POINT('Ctrl Pts',(-9.07824574157275,12.0215401802748,
-567.391176470588));
#155847=CARTESIAN_POINT('Ctrl Pts',(-7.89648244316034,12.7532570359442,
-568.885294117647));
#155848=CARTESIAN_POINT('Ctrl Pts',(-6.71471914474793,13.4849738916136,
-570.379411764706));
#155849=CARTESIAN_POINT('Ctrl Pts',(-5.41862499280729,13.9870834410653,
-571.873529411765));
#155850=CARTESIAN_POINT('Ctrl Pts',(-4.12253084086667,14.4891929905171,
-573.367647058824));
#155851=CARTESIAN_POINT('Ctrl Pts',(-2.75624276724856,14.7445964952585,
-574.861764705882));
#155852=CARTESIAN_POINT('Ctrl Pts',(-1.38995469363044,15.,-576.355882352941));
#155853=CARTESIAN_POINT('Ctrl Pts',(-1.83697019872103E-15,15.,-577.85));
#155854=CARTESIAN_POINT('Ctrl Pts',(1.38995469363045,15.,-579.344117647059));
#155855=CARTESIAN_POINT('Ctrl Pts',(2.75624276724855,14.7445964952585,-580.838235294117));
#155856=CARTESIAN_POINT('Ctrl Pts',(4.12253084086666,14.4891929905171,-582.332352941176));
#155857=CARTESIAN_POINT('Ctrl Pts',(5.4186249928073,13.9870834410653,-583.826470588235));
#155858=CARTESIAN_POINT('Ctrl Pts',(6.71471914474792,13.4849738916136,-585.320588235294));
#155859=CARTESIAN_POINT('Ctrl Pts',(7.89648244316034,12.7532570359442,-586.814705882353));
#155860=CARTESIAN_POINT('Ctrl Pts',(9.07824574157275,12.0215401802748,-588.308823529412));
#155861=CARTESIAN_POINT('Ctrl Pts',(10.1054346546984,11.0851337583099,-589.802941176471));
#155862=CARTESIAN_POINT('Ctrl Pts',(11.132623567824,10.148727336345,-591.297058823529));
#155863=CARTESIAN_POINT('Ctrl Pts',(11.9702584092036,9.03951954568885,-592.791176470588));
#155864=CARTESIAN_POINT('Ctrl Pts',(12.8078932505832,7.93031175503273,-594.285294117647));
#155865=CARTESIAN_POINT('Ctrl Pts',(13.4274493703259,6.68607533664807,-595.779411764706));
#155866=CARTESIAN_POINT('Ctrl Pts',(14.0470054900687,5.44183891826343,-597.273529411765));
#155867=CARTESIAN_POINT('Ctrl Pts',(14.4273846475923,4.10494485108125,-598.767647058824));
#155868=CARTESIAN_POINT('Ctrl Pts',(14.8077638051159,2.76805078389905,-600.261764705882));
#155869=CARTESIAN_POINT('Ctrl Pts',(14.9360126444255,1.38402539194953,-601.755882352941));
#155870=CARTESIAN_POINT('Ctrl Pts',(15.0642614837351,2.76725994113625E-15,
-603.25));
#155871=CARTESIAN_POINT('Ctrl Pts',(14.9360126444255,-1.38402539194952,
-604.744117647059));
#155872=CARTESIAN_POINT('Ctrl Pts',(14.8077638051159,-2.76805078389906,
-606.238235294118));
#155873=CARTESIAN_POINT('Ctrl Pts',(14.4273846475923,-4.10494485108124,
-607.732352941176));
#155874=CARTESIAN_POINT('Ctrl Pts',(14.0470054900687,-5.44183891826342,
-609.226470588235));
#155875=CARTESIAN_POINT('Ctrl Pts',(13.4274493703259,-6.68607533664808,
-610.720588235294));
#155876=CARTESIAN_POINT('Ctrl Pts',(12.8078932505832,-7.93031175503273,
-612.214705882353));
#155877=CARTESIAN_POINT('Ctrl Pts',(11.9702584092036,-9.03951954568884,
-613.708823529412));
#155878=CARTESIAN_POINT('Ctrl Pts',(11.132623567824,-10.148727336345,-615.202941176471));
#155879=CARTESIAN_POINT('Ctrl Pts',(10.1054346546984,-11.0851337583099,
-616.697058823529));
#155880=CARTESIAN_POINT('Ctrl Pts',(9.07824574157275,-12.0215401802748,
-618.191176470588));
#155881=CARTESIAN_POINT('Ctrl Pts',(7.89648244316034,-12.7532570359442,
-619.685294117647));
#155882=CARTESIAN_POINT('Ctrl Pts',(6.71471914474792,-13.4849738916136,
-621.179411764706));
#155883=CARTESIAN_POINT('Ctrl Pts',(5.4186249928073,-13.9870834410653,-622.673529411764));
#155884=CARTESIAN_POINT('Ctrl Pts',(4.12253084086667,-14.4891929905171,
-624.167647058823));
#155885=CARTESIAN_POINT('Ctrl Pts',(2.75624276724855,-14.7445964952585,
-625.661764705882));
#155886=CARTESIAN_POINT('Ctrl Pts',(1.38995469363045,-15.,-627.155882352941));
#155887=CARTESIAN_POINT('Ctrl Pts',(0.,-15.,-628.65));
#155888=CARTESIAN_POINT('Ctrl Pts',(-1.38995469363045,-15.,-630.144117647059));
#155889=CARTESIAN_POINT('Ctrl Pts',(-2.75624276724856,-14.7445964952585,
-631.638235294118));
#155890=CARTESIAN_POINT('Ctrl Pts',(-4.12253084086666,-14.4891929905171,
-633.132352941176));
#155891=CARTESIAN_POINT('Ctrl Pts',(-5.41862499280729,-13.9870834410653,
-634.626470588235));
#155892=CARTESIAN_POINT('Ctrl Pts',(-6.71471914474793,-13.4849738916136,
-636.120588235294));
#155893=CARTESIAN_POINT('Ctrl Pts',(-7.89648244316034,-12.7532570359442,
-637.614705882353));
#155894=CARTESIAN_POINT('Ctrl Pts',(-9.07824574157275,-12.0215401802748,
-639.108823529412));
#155895=CARTESIAN_POINT('Ctrl Pts',(-10.1054346546984,-11.0851337583099,
-640.60294117647));
#155896=CARTESIAN_POINT('Ctrl Pts',(-11.132623567824,-10.148727336345,-642.097058823529));
#155897=CARTESIAN_POINT('Ctrl Pts',(-11.9702584092036,-9.03951954568885,
-643.591176470588));
#155898=CARTESIAN_POINT('Ctrl Pts',(-12.8078932505832,-7.93031175503273,
-645.085294117647));
#155899=CARTESIAN_POINT('Ctrl Pts',(-13.4274493703259,-6.68607533664808,
-646.579411764706));
#155900=CARTESIAN_POINT('Ctrl Pts',(-14.0470054900687,-5.44183891826343,
-648.073529411765));
#155901=CARTESIAN_POINT('Ctrl Pts',(-14.4273846475923,-4.10494485108124,
-649.567647058824));
#155902=CARTESIAN_POINT('Ctrl Pts',(-14.8077638051159,-2.76805078389906,
-651.061764705883));
#155903=CARTESIAN_POINT('Ctrl Pts',(-14.9360126444255,-1.38402539194953,
-652.555882352941));
#155904=CARTESIAN_POINT('Ctrl Pts',(-15.0642614837351,-9.22419980378748E-16,
-654.05));
#155905=CARTESIAN_POINT('Ctrl Pts',(-14.9360126444255,1.38402539194953,
-655.544117647059));
#155906=CARTESIAN_POINT('Ctrl Pts',(-14.8077638051159,2.76805078389906,
-657.038235294117));
#155907=CARTESIAN_POINT('Ctrl Pts',(-14.4273846475923,4.10494485108124,
-658.532352941177));
#155908=CARTESIAN_POINT('Ctrl Pts',(-14.0470054900687,5.44183891826343,
-660.026470588235));
#155909=CARTESIAN_POINT('Ctrl Pts',(-13.4274493703259,6.68607533664807,
-661.520588235294));
#155910=CARTESIAN_POINT('Ctrl Pts',(-12.8078932505832,7.93031175503273,
-663.014705882353));
#155911=CARTESIAN_POINT('Ctrl Pts',(-11.9702584092036,9.03951954568884,
-664.508823529412));
#155912=CARTESIAN_POINT('Ctrl Pts',(-11.132623567824,10.148727336345,-666.002941176471));
#155913=CARTESIAN_POINT('Ctrl Pts',(-10.1054346546984,11.0851337583099,
-667.497058823529));
#155914=CARTESIAN_POINT('Ctrl Pts',(-9.07824574157275,12.0215401802748,
-668.991176470588));
#155915=CARTESIAN_POINT('Ctrl Pts',(-7.89648244316034,12.7532570359442,
-670.485294117647));
#155916=CARTESIAN_POINT('Ctrl Pts',(-6.71471914474793,13.4849738916136,
-671.979411764706));
#155917=CARTESIAN_POINT('Ctrl Pts',(-5.41862499280729,13.9870834410653,
-673.473529411765));
#155918=CARTESIAN_POINT('Ctrl Pts',(-4.12253084086667,14.4891929905171,
-674.967647058824));
#155919=CARTESIAN_POINT('Ctrl Pts',(-2.75624276724856,14.7445964952585,
-676.461764705882));
#155920=CARTESIAN_POINT('Ctrl Pts',(-1.38995469363044,15.,-677.955882352941));
#155921=CARTESIAN_POINT('Ctrl Pts',(-1.83697019872103E-15,15.,-679.45));
#155922=CARTESIAN_POINT('Ctrl Pts',(1.38995469363045,15.,-680.944117647059));
#155923=CARTESIAN_POINT('Ctrl Pts',(2.75624276724855,14.7445964952585,-682.438235294117));
#155924=CARTESIAN_POINT('Ctrl Pts',(4.12253084086666,14.4891929905171,-683.932352941176));
#155925=CARTESIAN_POINT('Ctrl Pts',(5.4186249928073,13.9870834410653,-685.426470588235));
#155926=CARTESIAN_POINT('Ctrl Pts',(6.71471914474792,13.4849738916136,-686.920588235294));
#155927=CARTESIAN_POINT('Ctrl Pts',(7.89648244316034,12.7532570359442,-688.414705882353));
#155928=CARTESIAN_POINT('Ctrl Pts',(9.07824574157275,12.0215401802748,-689.908823529412));
#155929=CARTESIAN_POINT('Ctrl Pts',(10.1054346546984,11.0851337583099,-691.402941176471));
#155930=CARTESIAN_POINT('Ctrl Pts',(11.132623567824,10.148727336345,-692.89705882353));
#155931=CARTESIAN_POINT('Ctrl Pts',(11.9702584092036,9.03951954568885,-694.391176470588));
#155932=CARTESIAN_POINT('Ctrl Pts',(12.8078932505832,7.93031175503273,-695.885294117647));
#155933=CARTESIAN_POINT('Ctrl Pts',(13.4274493703259,6.68607533664807,-697.379411764706));
#155934=CARTESIAN_POINT('Ctrl Pts',(14.0470054900687,5.44183891826343,-698.873529411764));
#155935=CARTESIAN_POINT('Ctrl Pts',(14.4273846475923,4.10494485108125,-700.367647058823));
#155936=CARTESIAN_POINT('Ctrl Pts',(14.8077638051159,2.76805078389905,-701.861764705882));
#155937=CARTESIAN_POINT('Ctrl Pts',(14.9360126444255,1.38402539194953,-703.355882352941));
#155938=CARTESIAN_POINT('Ctrl Pts',(15.0642614837351,2.76725994113625E-15,
-704.85));
#155939=CARTESIAN_POINT('Ctrl Pts',(14.9360126444255,-1.38402539194952,
-706.344117647059));
#155940=CARTESIAN_POINT('Ctrl Pts',(14.8077638051159,-2.76805078389906,
-707.838235294118));
#155941=CARTESIAN_POINT('Ctrl Pts',(14.4273846475923,-4.10494485108124,
-709.332352941177));
#155942=CARTESIAN_POINT('Ctrl Pts',(14.0470054900687,-5.44183891826342,
-710.826470588236));
#155943=CARTESIAN_POINT('Ctrl Pts',(13.4274493703259,-6.68607533664808,
-712.320588235294));
#155944=CARTESIAN_POINT('Ctrl Pts',(12.8078932505832,-7.93031175503273,
-713.814705882353));
#155945=CARTESIAN_POINT('Ctrl Pts',(11.9702584092036,-9.03951954568884,
-715.308823529412));
#155946=CARTESIAN_POINT('Ctrl Pts',(11.132623567824,-10.148727336345,-716.802941176471));
#155947=CARTESIAN_POINT('Ctrl Pts',(10.1054346546984,-11.0851337583099,
-718.297058823529));
#155948=CARTESIAN_POINT('Ctrl Pts',(9.07824574157275,-12.0215401802748,
-719.791176470588));
#155949=CARTESIAN_POINT('Ctrl Pts',(7.89648244316034,-12.7532570359442,
-721.285294117647));
#155950=CARTESIAN_POINT('Ctrl Pts',(6.71471914474792,-13.4849738916136,
-722.779411764706));
#155951=CARTESIAN_POINT('Ctrl Pts',(5.4186249928073,-13.9870834410653,-724.273529411765));
#155952=CARTESIAN_POINT('Ctrl Pts',(4.12253084086667,-14.4891929905171,
-725.767647058824));
#155953=CARTESIAN_POINT('Ctrl Pts',(2.75624276724855,-14.7445964952585,
-727.261764705882));
#155954=CARTESIAN_POINT('Ctrl Pts',(1.38995469363045,-15.,-728.755882352941));
#155955=CARTESIAN_POINT('Ctrl Pts',(0.,-15.,-730.25));
#155956=CARTESIAN_POINT('Ctrl Pts',(-1.38995469363045,-15.,-731.744117647059));
#155957=CARTESIAN_POINT('Ctrl Pts',(-2.75624276724856,-14.7445964952585,
-733.238235294118));
#155958=CARTESIAN_POINT('Ctrl Pts',(-4.12253084086666,-14.4891929905171,
-734.732352941177));
#155959=CARTESIAN_POINT('Ctrl Pts',(-5.41862499280729,-13.9870834410653,
-736.226470588235));
#155960=CARTESIAN_POINT('Ctrl Pts',(-6.71471914474793,-13.4849738916136,
-737.720588235294));
#155961=CARTESIAN_POINT('Ctrl Pts',(-7.89648244316034,-12.7532570359442,
-739.214705882353));
#155962=CARTESIAN_POINT('Ctrl Pts',(-9.07824574157275,-12.0215401802748,
-740.708823529412));
#155963=CARTESIAN_POINT('Ctrl Pts',(-10.1054346546984,-11.0851337583099,
-742.20294117647));
#155964=CARTESIAN_POINT('Ctrl Pts',(-11.132623567824,-10.148727336345,-743.697058823529));
#155965=CARTESIAN_POINT('Ctrl Pts',(-11.9702584092036,-9.03951954568885,
-745.191176470588));
#155966=CARTESIAN_POINT('Ctrl Pts',(-12.8078932505832,-7.93031175503273,
-746.685294117647));
#155967=CARTESIAN_POINT('Ctrl Pts',(-13.4274493703259,-6.68607533664808,
-748.179411764706));
#155968=CARTESIAN_POINT('Ctrl Pts',(-14.0470054900687,-5.44183891826343,
-749.673529411765));
#155969=CARTESIAN_POINT('Ctrl Pts',(-14.4273846475923,-4.10494485108124,
-751.167647058824));
#155970=CARTESIAN_POINT('Ctrl Pts',(-14.8077638051159,-2.76805078389906,
-752.661764705882));
#155971=CARTESIAN_POINT('Ctrl Pts',(-14.9360126444255,-1.38402539194953,
-754.155882352941));
#155972=CARTESIAN_POINT('Ctrl Pts',(-15.0642614837351,-9.22419980378748E-16,
-755.65));
#155973=CARTESIAN_POINT('Ctrl Pts',(-14.9360126444255,1.38402539194953,
-757.144117647059));
#155974=CARTESIAN_POINT('Ctrl Pts',(-14.8077638051159,2.76805078389906,
-758.638235294118));
#155975=CARTESIAN_POINT('Ctrl Pts',(-14.4273846475923,4.10494485108124,
-760.132352941176));
#155976=CARTESIAN_POINT('Ctrl Pts',(-14.0470054900687,5.44183891826343,
-761.626470588235));
#155977=CARTESIAN_POINT('Ctrl Pts',(-13.4274493703259,6.68607533664807,
-763.120588235294));
#155978=CARTESIAN_POINT('Ctrl Pts',(-12.8078932505832,7.93031175503273,
-764.614705882353));
#155979=CARTESIAN_POINT('Ctrl Pts',(-11.9702584092036,9.03951954568884,
-766.108823529412));
#155980=CARTESIAN_POINT('Ctrl Pts',(-11.132623567824,10.148727336345,-767.602941176471));
#155981=CARTESIAN_POINT('Ctrl Pts',(-10.1054346546984,11.0851337583099,
-769.09705882353));
#155982=CARTESIAN_POINT('Ctrl Pts',(-9.07824574157275,12.0215401802748,
-770.591176470589));
#155983=CARTESIAN_POINT('Ctrl Pts',(-7.89648244316034,12.7532570359442,
-772.085294117647));
#155984=CARTESIAN_POINT('Ctrl Pts',(-6.71471914474793,13.4849738916136,
-773.579411764706));
#155985=CARTESIAN_POINT('Ctrl Pts',(-5.41862499280729,13.9870834410653,
-775.073529411765));
#155986=CARTESIAN_POINT('Ctrl Pts',(-4.12253084086667,14.4891929905171,
-776.567647058824));
#155987=CARTESIAN_POINT('Ctrl Pts',(-2.75624276724856,14.7445964952585,
-778.061764705882));
#155988=CARTESIAN_POINT('Ctrl Pts',(-1.38995469363044,15.,-779.555882352941));
#155989=CARTESIAN_POINT('Ctrl Pts',(-1.83697019872103E-15,15.,-781.05));
#155990=CARTESIAN_POINT('Ctrl Pts',(1.38995469363045,15.,-782.544117647059));
#155991=CARTESIAN_POINT('Ctrl Pts',(2.75624276724855,14.7445964952585,-784.038235294118));
#155992=CARTESIAN_POINT('Ctrl Pts',(4.12253084086666,14.4891929905171,-785.532352941177));
#155993=CARTESIAN_POINT('Ctrl Pts',(5.4186249928073,13.9870834410653,-787.026470588235));
#155994=CARTESIAN_POINT('Ctrl Pts',(6.71471914474792,13.4849738916136,-788.520588235294));
#155995=CARTESIAN_POINT('Ctrl Pts',(7.89648244316034,12.7532570359442,-790.014705882353));
#155996=CARTESIAN_POINT('Ctrl Pts',(9.07824574157275,12.0215401802748,-791.508823529412));
#155997=CARTESIAN_POINT('Ctrl Pts',(10.1054346546984,11.0851337583099,-793.002941176471));
#155998=CARTESIAN_POINT('Ctrl Pts',(11.132623567824,10.148727336345,-794.497058823529));
#155999=CARTESIAN_POINT('Ctrl Pts',(11.9702584092036,9.03951954568885,-795.991176470588));
#156000=CARTESIAN_POINT('Ctrl Pts',(12.8078932505832,7.93031175503273,-797.485294117647));
#156001=CARTESIAN_POINT('Ctrl Pts',(13.4274493703259,6.68607533664807,-798.979411764706));
#156002=CARTESIAN_POINT('Ctrl Pts',(14.0470054900687,5.44183891826343,-800.473529411765));
#156003=CARTESIAN_POINT('Ctrl Pts',(14.4273846475923,4.10494485108125,-801.967647058823));
#156004=CARTESIAN_POINT('Ctrl Pts',(14.8077638051159,2.76805078389905,-803.461764705882));
#156005=CARTESIAN_POINT('Ctrl Pts',(14.9360126444255,1.38402539194953,-804.955882352941));
#156006=CARTESIAN_POINT('Ctrl Pts',(15.0642614837351,2.76725994113625E-15,
-806.45));
#156007=CARTESIAN_POINT('Ctrl Pts',(14.9360126444255,-1.38402539194952,
-807.944117647059));
#156008=CARTESIAN_POINT('Ctrl Pts',(14.8077638051159,-2.76805078389906,
-809.438235294118));
#156009=CARTESIAN_POINT('Ctrl Pts',(14.4273846475923,-4.10494485108124,
-810.932352941177));
#156010=CARTESIAN_POINT('Ctrl Pts',(14.0470054900687,-5.44183891826342,
-812.426470588235));
#156011=CARTESIAN_POINT('Ctrl Pts',(13.4274493703259,-6.68607533664808,
-813.920588235294));
#156012=CARTESIAN_POINT('Ctrl Pts',(12.8078932505832,-7.93031175503273,
-815.414705882353));
#156013=CARTESIAN_POINT('Ctrl Pts',(11.9702584092036,-9.03951954568884,
-816.908823529412));
#156014=CARTESIAN_POINT('Ctrl Pts',(11.132623567824,-10.148727336345,-818.40294117647));
#156015=CARTESIAN_POINT('Ctrl Pts',(10.1054346546984,-11.0851337583099,
-819.897058823529));
#156016=CARTESIAN_POINT('Ctrl Pts',(9.07824574157275,-12.0215401802748,
-821.391176470588));
#156017=CARTESIAN_POINT('Ctrl Pts',(7.89648244316034,-12.7532570359442,
-822.885294117647));
#156018=CARTESIAN_POINT('Ctrl Pts',(6.71471914474792,-13.4849738916136,
-824.379411764706));
#156019=CARTESIAN_POINT('Ctrl Pts',(5.4186249928073,-13.9870834410653,-825.873529411765));
#156020=CARTESIAN_POINT('Ctrl Pts',(4.12253084086667,-14.4891929905171,
-827.367647058824));
#156021=CARTESIAN_POINT('Ctrl Pts',(2.75624276724855,-14.7445964952585,
-828.861764705882));
#156022=CARTESIAN_POINT('Ctrl Pts',(1.38995469363045,-15.,-830.355882352941));
#156023=CARTESIAN_POINT('Ctrl Pts',(0.,-15.,-831.85));
#156024=CARTESIAN_POINT('Ctrl Pts',(-1.38995469363045,-15.,-833.344117647059));
#156025=CARTESIAN_POINT('Ctrl Pts',(-2.75624276724856,-14.7445964952585,
-834.838235294118));
#156026=CARTESIAN_POINT('Ctrl Pts',(-4.12253084086666,-14.4891929905171,
-836.332352941177));
#156027=CARTESIAN_POINT('Ctrl Pts',(-5.41862499280729,-13.9870834410653,
-837.826470588235));
#156028=CARTESIAN_POINT('Ctrl Pts',(-6.71471914474793,-13.4849738916136,
-839.320588235294));
#156029=CARTESIAN_POINT('Ctrl Pts',(-7.89648244316034,-12.7532570359442,
-840.814705882353));
#156030=CARTESIAN_POINT('Ctrl Pts',(-9.07824574157275,-12.0215401802748,
-842.308823529412));
#156031=CARTESIAN_POINT('Ctrl Pts',(-10.1054346546984,-11.0851337583099,
-843.802941176471));
#156032=CARTESIAN_POINT('Ctrl Pts',(-11.132623567824,-10.148727336345,-845.29705882353));
#156033=CARTESIAN_POINT('Ctrl Pts',(-11.9702584092036,-9.03951954568885,
-846.791176470588));
#156034=CARTESIAN_POINT('Ctrl Pts',(-12.8078932505832,-7.93031175503273,
-848.285294117647));
#156035=CARTESIAN_POINT('Ctrl Pts',(-13.4274493703259,-6.68607533664808,
-849.779411764706));
#156036=CARTESIAN_POINT('Ctrl Pts',(-14.0470054900687,-5.44183891826343,
-851.273529411765));
#156037=CARTESIAN_POINT('Ctrl Pts',(-14.4273846475923,-4.10494485108124,
-852.767647058824));
#156038=CARTESIAN_POINT('Ctrl Pts',(-14.8077638051159,-2.76805078389906,
-854.261764705882));
#156039=CARTESIAN_POINT('Ctrl Pts',(-14.9360126444255,-1.38402539194953,
-855.755882352941));
#156040=CARTESIAN_POINT('Ctrl Pts',(-15.0642614837351,-9.22419980378748E-16,
-857.25));
#156041=CARTESIAN_POINT('Ctrl Pts',(-14.9360126444255,1.38402539194953,
-858.744117647059));
#156042=CARTESIAN_POINT('Ctrl Pts',(-14.8077638051159,2.76805078389906,
-860.238235294118));
#156043=CARTESIAN_POINT('Ctrl Pts',(-14.4273846475923,4.10494485108124,
-861.732352941176));
#156044=CARTESIAN_POINT('Ctrl Pts',(-14.0470054900687,5.44183891826343,
-863.226470588235));
#156045=CARTESIAN_POINT('Ctrl Pts',(-13.4274493703259,6.68607533664807,
-864.720588235294));
#156046=CARTESIAN_POINT('Ctrl Pts',(-12.8078932505832,7.93031175503273,
-866.214705882353));
#156047=CARTESIAN_POINT('Ctrl Pts',(-11.9702584092036,9.03951954568884,
-867.708823529412));
#156048=CARTESIAN_POINT('Ctrl Pts',(-11.132623567824,10.148727336345,-869.202941176471));
#156049=CARTESIAN_POINT('Ctrl Pts',(-10.1054346546984,11.0851337583099,
-870.697058823529));
#156050=CARTESIAN_POINT('Ctrl Pts',(-9.07824574157275,12.0215401802748,
-872.191176470589));
#156051=CARTESIAN_POINT('Ctrl Pts',(-7.89648244316034,12.7532570359442,
-873.685294117647));
#156052=CARTESIAN_POINT('Ctrl Pts',(-6.71471914474793,13.4849738916136,
-875.179411764706));
#156053=CARTESIAN_POINT('Ctrl Pts',(-5.41862499280729,13.9870834410653,
-876.673529411764));
#156054=CARTESIAN_POINT('Ctrl Pts',(-4.12253084086667,14.4891929905171,
-878.167647058823));
#156055=CARTESIAN_POINT('Ctrl Pts',(-2.75624276724856,14.7445964952585,
-879.661764705882));
#156056=CARTESIAN_POINT('Ctrl Pts',(-1.38995469363044,15.,-881.155882352941));
#156057=CARTESIAN_POINT('Ctrl Pts',(-1.83697019872103E-15,15.,-882.65));
#156058=CARTESIAN_POINT('Ctrl Pts',(1.38995469363045,15.,-884.144117647059));
#156059=CARTESIAN_POINT('Ctrl Pts',(2.75624276724855,14.7445964952585,-885.638235294118));
#156060=CARTESIAN_POINT('Ctrl Pts',(4.12253084086666,14.4891929905171,-887.132352941177));
#156061=CARTESIAN_POINT('Ctrl Pts',(5.4186249928073,13.9870834410653,-888.626470588235));
#156062=CARTESIAN_POINT('Ctrl Pts',(6.71471914474792,13.4849738916136,-890.120588235294));
#156063=CARTESIAN_POINT('Ctrl Pts',(7.89648244316034,12.7532570359442,-891.614705882353));
#156064=CARTESIAN_POINT('Ctrl Pts',(9.07824574157275,12.0215401802748,-893.108823529412));
#156065=CARTESIAN_POINT('Ctrl Pts',(10.1054346546984,11.0851337583099,-894.60294117647));
#156066=CARTESIAN_POINT('Ctrl Pts',(11.132623567824,10.148727336345,-896.09705882353));
#156067=CARTESIAN_POINT('Ctrl Pts',(11.9702584092036,9.03951954568885,-897.591176470588));
#156068=CARTESIAN_POINT('Ctrl Pts',(12.8078932505832,7.93031175503273,-899.085294117647));
#156069=CARTESIAN_POINT('Ctrl Pts',(13.4274493703259,6.68607533664807,-900.579411764706));
#156070=CARTESIAN_POINT('Ctrl Pts',(14.0470054900687,5.44183891826343,-902.073529411765));
#156071=CARTESIAN_POINT('Ctrl Pts',(14.4273846475923,4.10494485108125,-903.567647058824));
#156072=CARTESIAN_POINT('Ctrl Pts',(14.8077638051159,2.76805078389905,-905.061764705883));
#156073=CARTESIAN_POINT('Ctrl Pts',(14.9360126444255,1.38402539194953,-906.555882352941));
#156074=CARTESIAN_POINT('Ctrl Pts',(15.0642614837351,2.76725994113625E-15,
-908.05));
#156075=CARTESIAN_POINT('Ctrl Pts',(14.9360126444255,-1.38402539194952,
-909.544117647059));
#156076=CARTESIAN_POINT('Ctrl Pts',(14.8077638051159,-2.76805078389906,
-911.038235294118));
#156077=CARTESIAN_POINT('Ctrl Pts',(14.4273846475923,-4.10494485108124,
-912.532352941176));
#156078=CARTESIAN_POINT('Ctrl Pts',(14.0470054900687,-5.44183891826342,
-914.026470588235));
#156079=CARTESIAN_POINT('Ctrl Pts',(13.4274493703259,-6.68607533664808,
-915.520588235294));
#156080=CARTESIAN_POINT('Ctrl Pts',(12.8078932505832,-7.93031175503273,
-917.014705882353));
#156081=CARTESIAN_POINT('Ctrl Pts',(11.9702584092036,-9.03951954568884,
-918.508823529412));
#156082=CARTESIAN_POINT('Ctrl Pts',(11.132623567824,-10.148727336345,-920.002941176471));
#156083=CARTESIAN_POINT('Ctrl Pts',(10.1054346546984,-11.0851337583099,
-921.497058823529));
#156084=CARTESIAN_POINT('Ctrl Pts',(9.07824574157275,-12.0215401802748,
-922.991176470588));
#156085=CARTESIAN_POINT('Ctrl Pts',(7.89648244316034,-12.7532570359442,
-924.485294117647));
#156086=CARTESIAN_POINT('Ctrl Pts',(6.71471914474792,-13.4849738916136,
-925.979411764706));
#156087=CARTESIAN_POINT('Ctrl Pts',(5.4186249928073,-13.9870834410653,-927.473529411765));
#156088=CARTESIAN_POINT('Ctrl Pts',(4.12253084086667,-14.4891929905171,
-928.967647058823));
#156089=CARTESIAN_POINT('Ctrl Pts',(2.75624276724855,-14.7445964952585,
-930.461764705883));
#156090=CARTESIAN_POINT('Ctrl Pts',(1.38995469363045,-15.,-931.955882352941));
#156091=CARTESIAN_POINT('Ctrl Pts',(0.,-15.,-933.45));
#156092=CARTESIAN_POINT('Ctrl Pts',(-1.38995469363045,-15.,-934.944117647059));
#156093=CARTESIAN_POINT('Ctrl Pts',(-2.75624276724856,-14.7445964952585,
-936.438235294117));
#156094=CARTESIAN_POINT('Ctrl Pts',(-4.12253084086666,-14.4891929905171,
-937.932352941177));
#156095=CARTESIAN_POINT('Ctrl Pts',(-5.41862499280729,-13.9870834410653,
-939.426470588235));
#156096=CARTESIAN_POINT('Ctrl Pts',(-6.71471914474793,-13.4849738916136,
-940.920588235294));
#156097=CARTESIAN_POINT('Ctrl Pts',(-7.89648244316034,-12.7532570359442,
-942.414705882353));
#156098=CARTESIAN_POINT('Ctrl Pts',(-9.07824574157275,-12.0215401802748,
-943.908823529412));
#156099=CARTESIAN_POINT('Ctrl Pts',(-10.1054346546984,-11.0851337583099,
-945.402941176471));
#156100=CARTESIAN_POINT('Ctrl Pts',(-11.132623567824,-10.148727336345,-946.89705882353));
#156101=CARTESIAN_POINT('Ctrl Pts',(-11.9702584092036,-9.03951954568885,
-948.391176470588));
#156102=CARTESIAN_POINT('Ctrl Pts',(-12.8078932505832,-7.93031175503273,
-949.885294117647));
#156103=CARTESIAN_POINT('Ctrl Pts',(-13.4274493703259,-6.68607533664808,
-951.379411764706));
#156104=CARTESIAN_POINT('Ctrl Pts',(-14.0470054900687,-5.44183891826343,
-952.873529411765));
#156105=CARTESIAN_POINT('Ctrl Pts',(-14.4273846475923,-4.10494485108124,
-954.367647058824));
#156106=CARTESIAN_POINT('Ctrl Pts',(-14.8077638051159,-2.76805078389906,
-955.861764705882));
#156107=CARTESIAN_POINT('Ctrl Pts',(-14.9360126444255,-1.38402539194953,
-957.355882352941));
#156108=CARTESIAN_POINT('Ctrl Pts',(-15.0642614837351,-9.22419980378748E-16,
-958.85));
#156109=CARTESIAN_POINT('Ctrl Pts',(-14.9360126444255,1.38402539194953,
-960.344117647059));
#156110=CARTESIAN_POINT('Ctrl Pts',(-14.8077638051159,2.76805078389906,
-961.838235294118));
#156111=CARTESIAN_POINT('Ctrl Pts',(-14.4273846475923,4.10494485108124,
-963.332352941177));
#156112=CARTESIAN_POINT('Ctrl Pts',(-14.0470054900687,5.44183891826343,
-964.826470588235));
#156113=CARTESIAN_POINT('Ctrl Pts',(-13.4274493703259,6.68607533664807,
-966.320588235294));
#156114=CARTESIAN_POINT('Ctrl Pts',(-12.8078932505832,7.93031175503273,
-967.814705882353));
#156115=CARTESIAN_POINT('Ctrl Pts',(-11.9702584092036,9.03951954568884,
-969.308823529412));
#156116=CARTESIAN_POINT('Ctrl Pts',(-11.132623567824,10.148727336345,-970.80294117647));
#156117=CARTESIAN_POINT('Ctrl Pts',(-10.1054346546984,11.0851337583099,
-972.297058823529));
#156118=CARTESIAN_POINT('Ctrl Pts',(-9.07824574157275,12.0215401802748,
-973.791176470588));
#156119=CARTESIAN_POINT('Ctrl Pts',(-7.89648244316034,12.7532570359442,
-975.285294117647));
#156120=CARTESIAN_POINT('Ctrl Pts',(-6.71471914474793,13.4849738916136,
-976.779411764706));
#156121=CARTESIAN_POINT('Ctrl Pts',(-5.41862499280729,13.9870834410653,
-978.273529411765));
#156122=CARTESIAN_POINT('Ctrl Pts',(-4.12253084086667,14.4891929905171,
-979.767647058824));
#156123=CARTESIAN_POINT('Ctrl Pts',(-2.75624276724856,14.7445964952585,
-981.261764705882));
#156124=CARTESIAN_POINT('Ctrl Pts',(-1.38995469363044,15.,-982.755882352941));
#156125=CARTESIAN_POINT('Ctrl Pts',(-1.83697019872103E-15,15.,-984.25));
#156126=CARTESIAN_POINT('Ctrl Pts',(1.38995469363045,15.,-985.744117647059));
#156127=CARTESIAN_POINT('Ctrl Pts',(2.75624276724855,14.7445964952585,-987.238235294118));
#156128=CARTESIAN_POINT('Ctrl Pts',(4.12253084086666,14.4891929905171,-988.732352941177));
#156129=CARTESIAN_POINT('Ctrl Pts',(5.4186249928073,13.9870834410653,-990.226470588235));
#156130=CARTESIAN_POINT('Ctrl Pts',(6.71471914474792,13.4849738916136,-991.720588235294));
#156131=CARTESIAN_POINT('Ctrl Pts',(7.89648244316034,12.7532570359442,-993.214705882353));
#156132=CARTESIAN_POINT('Ctrl Pts',(9.07824574157275,12.0215401802748,-994.708823529412));
#156133=CARTESIAN_POINT('Ctrl Pts',(10.1054346546984,11.0851337583099,-996.202941176471));
#156134=CARTESIAN_POINT('Ctrl Pts',(11.132623567824,10.148727336345,-997.697058823529));
#156135=CARTESIAN_POINT('Ctrl Pts',(11.9702584092036,9.03951954568885,-999.191176470588));
#156136=CARTESIAN_POINT('Ctrl Pts',(12.8078932505832,7.93031175503273,-1000.68529411765));
#156137=CARTESIAN_POINT('Ctrl Pts',(13.4274493703259,6.68607533664807,-1002.17941176471));
#156138=CARTESIAN_POINT('Ctrl Pts',(14.0470054900687,5.44183891826343,-1003.67352941176));
#156139=CARTESIAN_POINT('Ctrl Pts',(14.4273846475923,4.10494485108125,-1005.16764705882));
#156140=CARTESIAN_POINT('Ctrl Pts',(14.8077638051159,2.76805078389905,-1006.66176470588));
#156141=CARTESIAN_POINT('Ctrl Pts',(14.9360126444255,1.38402539194953,-1008.15588235294));
#156142=CARTESIAN_POINT('Ctrl Pts',(15.0642614837351,2.76725994113625E-15,
-1009.65));
#156143=CARTESIAN_POINT('Ctrl Pts',(14.9360126444255,-1.38402539194952,
-1011.14411764706));
#156144=CARTESIAN_POINT('Ctrl Pts',(14.8077638051159,-2.76805078389906,
-1012.63823529412));
#156145=CARTESIAN_POINT('Ctrl Pts',(14.4273846475923,-4.10494485108124,
-1014.13235294118));
#156146=CARTESIAN_POINT('Ctrl Pts',(14.0470054900687,-5.44183891826342,
-1015.62647058824));
#156147=CARTESIAN_POINT('Ctrl Pts',(13.4274493703259,-6.68607533664808,
-1017.12058823529));
#156148=CARTESIAN_POINT('Ctrl Pts',(12.8078932505832,-7.93031175503273,
-1018.61470588235));
#156149=CARTESIAN_POINT('Ctrl Pts',(11.9702584092036,-9.03951954568884,
-1020.10882352941));
#156150=CARTESIAN_POINT('Ctrl Pts',(11.132623567824,-10.148727336345,-1021.60294117647));
#156151=CARTESIAN_POINT('Ctrl Pts',(10.1054346546984,-11.0851337583099,
-1023.09705882353));
#156152=CARTESIAN_POINT('Ctrl Pts',(9.07824574157275,-12.0215401802748,
-1024.59117647059));
#156153=CARTESIAN_POINT('Ctrl Pts',(7.89648244316034,-12.7532570359442,
-1026.08529411765));
#156154=CARTESIAN_POINT('Ctrl Pts',(6.71471914474792,-13.4849738916136,
-1027.57941176471));
#156155=CARTESIAN_POINT('Ctrl Pts',(5.4186249928073,-13.9870834410653,-1029.07352941176));
#156156=CARTESIAN_POINT('Ctrl Pts',(4.12253084086667,-14.4891929905171,
-1030.56764705882));
#156157=CARTESIAN_POINT('Ctrl Pts',(2.75624276724855,-14.7445964952585,
-1032.06176470588));
#156158=CARTESIAN_POINT('Ctrl Pts',(1.38995469363045,-15.,-1033.55588235294));
#156159=CARTESIAN_POINT('Ctrl Pts',(0.,-15.,-1035.05));
#156160=CARTESIAN_POINT('Ctrl Pts',(-1.38995469363045,-15.,-1036.54411764706));
#156161=CARTESIAN_POINT('Ctrl Pts',(-2.75624276724856,-14.7445964952585,
-1038.03823529412));
#156162=CARTESIAN_POINT('Ctrl Pts',(-4.12253084086666,-14.4891929905171,
-1039.53235294118));
#156163=CARTESIAN_POINT('Ctrl Pts',(-5.41862499280729,-13.9870834410653,
-1041.02647058824));
#156164=CARTESIAN_POINT('Ctrl Pts',(-6.71471914474793,-13.4849738916136,
-1042.52058823529));
#156165=CARTESIAN_POINT('Ctrl Pts',(-7.89648244316034,-12.7532570359442,
-1044.01470588235));
#156166=CARTESIAN_POINT('Ctrl Pts',(-9.07824574157275,-12.0215401802748,
-1045.50882352941));
#156167=CARTESIAN_POINT('Ctrl Pts',(-10.1054346546984,-11.0851337583099,
-1047.00294117647));
#156168=CARTESIAN_POINT('Ctrl Pts',(-11.132623567824,-10.148727336345,-1048.49705882353));
#156169=CARTESIAN_POINT('Ctrl Pts',(-11.9702584092036,-9.03951954568885,
-1049.99117647059));
#156170=CARTESIAN_POINT('Ctrl Pts',(-12.8078932505832,-7.93031175503273,
-1051.48529411765));
#156171=CARTESIAN_POINT('Ctrl Pts',(-13.4274493703259,-6.68607533664808,
-1052.97941176471));
#156172=CARTESIAN_POINT('Ctrl Pts',(-14.0470054900687,-5.44183891826343,
-1054.47352941176));
#156173=CARTESIAN_POINT('Ctrl Pts',(-14.4273846475923,-4.10494485108124,
-1055.96764705882));
#156174=CARTESIAN_POINT('Ctrl Pts',(-14.8077638051159,-2.76805078389906,
-1057.46176470588));
#156175=CARTESIAN_POINT('Ctrl Pts',(-14.9360126444255,-1.38402539194953,
-1058.95588235294));
#156176=CARTESIAN_POINT('Ctrl Pts',(-15.0642614837351,-9.22419980378748E-16,
-1060.45));
#156177=CARTESIAN_POINT('Ctrl Pts',(-14.9360126444255,1.38402539194953,
-1061.94411764706));
#156178=CARTESIAN_POINT('Ctrl Pts',(-14.8077638051159,2.76805078389906,
-1063.43823529412));
#156179=CARTESIAN_POINT('Ctrl Pts',(-14.4273846475923,4.10494485108124,
-1064.93235294118));
#156180=CARTESIAN_POINT('Ctrl Pts',(-14.0470054900687,5.44183891826343,
-1066.42647058824));
#156181=CARTESIAN_POINT('Ctrl Pts',(-13.4274493703259,6.68607533664807,
-1067.92058823529));
#156182=CARTESIAN_POINT('Ctrl Pts',(-12.8078932505832,7.93031175503273,
-1069.41470588235));
#156183=CARTESIAN_POINT('Ctrl Pts',(-11.9702584092036,9.03951954568884,
-1070.90882352941));
#156184=CARTESIAN_POINT('Ctrl Pts',(-11.132623567824,10.148727336345,-1072.40294117647));
#156185=CARTESIAN_POINT('Ctrl Pts',(-10.1054346546984,11.0851337583099,
-1073.89705882353));
#156186=CARTESIAN_POINT('Ctrl Pts',(-9.07824574157275,12.0215401802748,
-1075.39117647059));
#156187=CARTESIAN_POINT('Ctrl Pts',(-7.89648244316034,12.7532570359442,
-1076.88529411765));
#156188=CARTESIAN_POINT('Ctrl Pts',(-6.71471914474793,13.4849738916136,
-1078.37941176471));
#156189=CARTESIAN_POINT('Ctrl Pts',(-5.41862499280729,13.9870834410653,
-1079.87352941176));
#156190=CARTESIAN_POINT('Ctrl Pts',(-4.12253084086667,14.4891929905171,
-1081.36764705882));
#156191=CARTESIAN_POINT('Ctrl Pts',(-2.75624276724856,14.7445964952585,
-1082.86176470588));
#156192=CARTESIAN_POINT('Ctrl Pts',(-1.38995469363044,15.,-1084.35588235294));
#156193=CARTESIAN_POINT('Ctrl Pts',(-1.83697019872103E-15,15.,-1085.85));
#156194=CARTESIAN_POINT('Ctrl Pts',(1.38995469363045,15.,-1087.34411764706));
#156195=CARTESIAN_POINT('Ctrl Pts',(2.75624276724855,14.7445964952585,-1088.83823529412));
#156196=CARTESIAN_POINT('Ctrl Pts',(4.12253084086666,14.4891929905171,-1090.33235294118));
#156197=CARTESIAN_POINT('Ctrl Pts',(5.4186249928073,13.9870834410653,-1091.82647058824));
#156198=CARTESIAN_POINT('Ctrl Pts',(6.71471914474792,13.4849738916136,-1093.32058823529));
#156199=CARTESIAN_POINT('Ctrl Pts',(7.89648244316034,12.7532570359442,-1094.81470588235));
#156200=CARTESIAN_POINT('Ctrl Pts',(9.07824574157275,12.0215401802748,-1096.30882352941));
#156201=CARTESIAN_POINT('Ctrl Pts',(10.1054346546984,11.0851337583099,-1097.80294117647));
#156202=CARTESIAN_POINT('Ctrl Pts',(11.132623567824,10.148727336345,-1099.29705882353));
#156203=CARTESIAN_POINT('Ctrl Pts',(11.9702584092036,9.03951954568885,-1100.79117647059));
#156204=CARTESIAN_POINT('Ctrl Pts',(12.8078932505832,7.93031175503273,-1102.28529411765));
#156205=CARTESIAN_POINT('Ctrl Pts',(13.4274493703259,6.68607533664807,-1103.77941176471));
#156206=CARTESIAN_POINT('Ctrl Pts',(14.0470054900687,5.44183891826343,-1105.27352941176));
#156207=CARTESIAN_POINT('Ctrl Pts',(14.4273846475923,4.10494485108125,-1106.76764705882));
#156208=CARTESIAN_POINT('Ctrl Pts',(14.8077638051159,2.76805078389905,-1108.26176470588));
#156209=CARTESIAN_POINT('Ctrl Pts',(14.9360126444255,1.38402539194953,-1109.75588235294));
#156210=CARTESIAN_POINT('Ctrl Pts',(15.0642614837351,2.76725994113625E-15,
-1111.25));
#156211=CARTESIAN_POINT('Ctrl Pts',(14.9360126444255,-1.38402539194952,
-1112.74411764706));
#156212=CARTESIAN_POINT('Ctrl Pts',(14.8077638051159,-2.76805078389906,
-1114.23823529412));
#156213=CARTESIAN_POINT('Ctrl Pts',(14.4273846475923,-4.10494485108124,
-1115.73235294118));
#156214=CARTESIAN_POINT('Ctrl Pts',(14.0470054900687,-5.44183891826342,
-1117.22647058824));
#156215=CARTESIAN_POINT('Ctrl Pts',(13.4274493703259,-6.68607533664808,
-1118.72058823529));
#156216=CARTESIAN_POINT('Ctrl Pts',(12.8078932505832,-7.93031175503273,
-1120.21470588235));
#156217=CARTESIAN_POINT('Ctrl Pts',(11.9702584092036,-9.03951954568884,
-1121.70882352941));
#156218=CARTESIAN_POINT('Ctrl Pts',(11.132623567824,-10.148727336345,-1123.20294117647));
#156219=CARTESIAN_POINT('Ctrl Pts',(10.1054346546984,-11.0851337583099,
-1124.69705882353));
#156220=CARTESIAN_POINT('Ctrl Pts',(9.07824574157275,-12.0215401802748,
-1126.19117647059));
#156221=CARTESIAN_POINT('Ctrl Pts',(7.89648244316034,-12.7532570359442,
-1127.68529411765));
#156222=CARTESIAN_POINT('Ctrl Pts',(6.71471914474792,-13.4849738916136,
-1129.17941176471));
#156223=CARTESIAN_POINT('Ctrl Pts',(5.4186249928073,-13.9870834410653,-1130.67352941176));
#156224=CARTESIAN_POINT('Ctrl Pts',(4.12253084086667,-14.4891929905171,
-1132.16764705882));
#156225=CARTESIAN_POINT('Ctrl Pts',(2.75624276724855,-14.7445964952585,
-1133.66176470588));
#156226=CARTESIAN_POINT('Ctrl Pts',(1.38995469363045,-15.,-1135.15588235294));
#156227=CARTESIAN_POINT('Ctrl Pts',(0.,-15.,-1136.65));
#156228=CARTESIAN_POINT('Ctrl Pts',(-1.38995469363045,-15.,-1138.14411764706));
#156229=CARTESIAN_POINT('Ctrl Pts',(-2.75624276724856,-14.7445964952585,
-1139.63823529412));
#156230=CARTESIAN_POINT('Ctrl Pts',(-4.12253084086666,-14.4891929905171,
-1141.13235294118));
#156231=CARTESIAN_POINT('Ctrl Pts',(-5.41862499280729,-13.9870834410653,
-1142.62647058824));
#156232=CARTESIAN_POINT('Ctrl Pts',(-6.71471914474793,-13.4849738916136,
-1144.12058823529));
#156233=CARTESIAN_POINT('Ctrl Pts',(-7.89648244316034,-12.7532570359442,
-1145.61470588235));
#156234=CARTESIAN_POINT('Ctrl Pts',(-9.07824574157275,-12.0215401802748,
-1147.10882352941));
#156235=CARTESIAN_POINT('Ctrl Pts',(-10.1054346546984,-11.0851337583099,
-1148.60294117647));
#156236=CARTESIAN_POINT('Ctrl Pts',(-11.132623567824,-10.148727336345,-1150.09705882353));
#156237=CARTESIAN_POINT('Ctrl Pts',(-11.9702584092036,-9.03951954568885,
-1151.59117647059));
#156238=CARTESIAN_POINT('Ctrl Pts',(-12.8078932505832,-7.93031175503273,
-1153.08529411765));
#156239=CARTESIAN_POINT('Ctrl Pts',(-13.4274493703259,-6.68607533664808,
-1154.57941176471));
#156240=CARTESIAN_POINT('Ctrl Pts',(-14.0470054900687,-5.44183891826343,
-1156.07352941176));
#156241=CARTESIAN_POINT('Ctrl Pts',(-14.4273846475923,-4.10494485108124,
-1157.56764705882));
#156242=CARTESIAN_POINT('Ctrl Pts',(-14.8077638051159,-2.76805078389906,
-1159.06176470588));
#156243=CARTESIAN_POINT('Ctrl Pts',(-14.9360126444255,-1.38402539194953,
-1160.55588235294));
#156244=CARTESIAN_POINT('Ctrl Pts',(-15.0642614837351,-9.22419980378748E-16,
-1162.05));
#156245=CARTESIAN_POINT('Ctrl Pts',(-14.9360126444255,1.38402539194953,
-1163.54411764706));
#156246=CARTESIAN_POINT('Ctrl Pts',(-14.8077638051159,2.76805078389906,
-1165.03823529412));
#156247=CARTESIAN_POINT('Ctrl Pts',(-14.4273846475923,4.10494485108124,
-1166.53235294118));
#156248=CARTESIAN_POINT('Ctrl Pts',(-14.0470054900687,5.44183891826343,
-1168.02647058824));
#156249=CARTESIAN_POINT('Ctrl Pts',(-13.4274493703259,6.68607533664807,
-1169.52058823529));
#156250=CARTESIAN_POINT('Ctrl Pts',(-12.8078932505832,7.93031175503273,
-1171.01470588235));
#156251=CARTESIAN_POINT('Ctrl Pts',(-11.9702584092036,9.03951954568884,
-1172.50882352941));
#156252=CARTESIAN_POINT('Ctrl Pts',(-11.132623567824,10.148727336345,-1174.00294117647));
#156253=CARTESIAN_POINT('Ctrl Pts',(-10.1054346546984,11.0851337583099,
-1175.49705882353));
#156254=CARTESIAN_POINT('Ctrl Pts',(-9.07824574157275,12.0215401802748,
-1176.99117647059));
#156255=CARTESIAN_POINT('Ctrl Pts',(-7.89648244316034,12.7532570359442,
-1178.48529411765));
#156256=CARTESIAN_POINT('Ctrl Pts',(-6.71471914474793,13.4849738916136,
-1179.97941176471));
#156257=CARTESIAN_POINT('Ctrl Pts',(-5.41862499280729,13.9870834410653,
-1181.47352941176));
#156258=CARTESIAN_POINT('Ctrl Pts',(-4.12253084086667,14.4891929905171,
-1182.96764705882));
#156259=CARTESIAN_POINT('Ctrl Pts',(-2.75624276724856,14.7445964952585,
-1184.46176470588));
#156260=CARTESIAN_POINT('Ctrl Pts',(-1.38995469363044,15.,-1185.95588235294));
#156261=CARTESIAN_POINT('Ctrl Pts',(-1.83697019872103E-15,15.,-1187.45));
#156262=CARTESIAN_POINT('Ctrl Pts',(1.38995469363045,15.,-1188.94411764706));
#156263=CARTESIAN_POINT('Ctrl Pts',(2.75624276724855,14.7445964952585,-1190.43823529412));
#156264=CARTESIAN_POINT('Ctrl Pts',(4.12253084086666,14.4891929905171,-1191.93235294118));
#156265=CARTESIAN_POINT('Ctrl Pts',(5.4186249928073,13.9870834410653,-1193.42647058824));
#156266=CARTESIAN_POINT('Ctrl Pts',(6.71471914474792,13.4849738916136,-1194.92058823529));
#156267=CARTESIAN_POINT('Ctrl Pts',(7.89648244316034,12.7532570359442,-1196.41470588235));
#156268=CARTESIAN_POINT('Ctrl Pts',(9.07824574157275,12.0215401802748,-1197.90882352941));
#156269=CARTESIAN_POINT('Ctrl Pts',(10.1054346546984,11.0851337583099,-1199.40294117647));
#156270=CARTESIAN_POINT('Ctrl Pts',(11.132623567824,10.148727336345,-1200.89705882353));
#156271=CARTESIAN_POINT('Ctrl Pts',(11.9702584092036,9.03951954568885,-1202.39117647059));
#156272=CARTESIAN_POINT('Ctrl Pts',(12.8078932505832,7.93031175503273,-1203.88529411765));
#156273=CARTESIAN_POINT('Ctrl Pts',(13.4274493703259,6.68607533664807,-1205.37941176471));
#156274=CARTESIAN_POINT('Ctrl Pts',(14.0470054900687,5.44183891826343,-1206.87352941176));
#156275=CARTESIAN_POINT('Ctrl Pts',(14.4273846475923,4.10494485108125,-1208.36764705882));
#156276=CARTESIAN_POINT('Ctrl Pts',(14.8077638051159,2.76805078389905,-1209.86176470588));
#156277=CARTESIAN_POINT('Ctrl Pts',(14.9360126444255,1.38402539194953,-1211.35588235294));
#156278=CARTESIAN_POINT('Ctrl Pts',(15.0642614837351,2.76725994113625E-15,
-1212.85));
#156279=CARTESIAN_POINT('Ctrl Pts',(14.9360126444255,-1.38402539194952,
-1214.34411764706));
#156280=CARTESIAN_POINT('Ctrl Pts',(14.8077638051159,-2.76805078389906,
-1215.83823529412));
#156281=CARTESIAN_POINT('Ctrl Pts',(14.4273846475923,-4.10494485108124,
-1217.33235294118));
#156282=CARTESIAN_POINT('Ctrl Pts',(14.0470054900687,-5.44183891826342,
-1218.82647058824));
#156283=CARTESIAN_POINT('Ctrl Pts',(13.4274493703259,-6.68607533664808,
-1220.32058823529));
#156284=CARTESIAN_POINT('Ctrl Pts',(12.8078932505832,-7.93031175503273,
-1221.81470588235));
#156285=CARTESIAN_POINT('Ctrl Pts',(11.9702584092036,-9.03951954568884,
-1223.30882352941));
#156286=CARTESIAN_POINT('Ctrl Pts',(11.132623567824,-10.148727336345,-1224.80294117647));
#156287=CARTESIAN_POINT('Ctrl Pts',(10.1054346546984,-11.0851337583099,
-1226.29705882353));
#156288=CARTESIAN_POINT('Ctrl Pts',(9.07824574157275,-12.0215401802748,
-1227.79117647059));
#156289=CARTESIAN_POINT('Ctrl Pts',(7.89648244316034,-12.7532570359442,
-1229.28529411765));
#156290=CARTESIAN_POINT('Ctrl Pts',(6.71471914474792,-13.4849738916136,
-1230.77941176471));
#156291=CARTESIAN_POINT('Ctrl Pts',(5.4186249928073,-13.9870834410653,-1232.27352941176));
#156292=CARTESIAN_POINT('Ctrl Pts',(4.12253084086667,-14.4891929905171,
-1233.76764705882));
#156293=CARTESIAN_POINT('Ctrl Pts',(2.75624276724855,-14.7445964952585,
-1235.26176470588));
#156294=CARTESIAN_POINT('Ctrl Pts',(1.38995469363045,-15.,-1236.75588235294));
#156295=CARTESIAN_POINT('Ctrl Pts',(0.,-15.,-1238.25));
#156296=CARTESIAN_POINT('Ctrl Pts',(-1.38995469363045,-15.,-1239.74411764706));
#156297=CARTESIAN_POINT('Ctrl Pts',(-2.75624276724856,-14.7445964952585,
-1241.23823529412));
#156298=CARTESIAN_POINT('Ctrl Pts',(-4.12253084086666,-14.4891929905171,
-1242.73235294118));
#156299=CARTESIAN_POINT('Ctrl Pts',(-5.41862499280729,-13.9870834410653,
-1244.22647058824));
#156300=CARTESIAN_POINT('Ctrl Pts',(-6.71471914474793,-13.4849738916136,
-1245.72058823529));
#156301=CARTESIAN_POINT('Ctrl Pts',(-7.89648244316034,-12.7532570359442,
-1247.21470588235));
#156302=CARTESIAN_POINT('Ctrl Pts',(-9.07824574157275,-12.0215401802748,
-1248.70882352941));
#156303=CARTESIAN_POINT('Ctrl Pts',(-10.1054346546984,-11.0851337583099,
-1250.20294117647));
#156304=CARTESIAN_POINT('Ctrl Pts',(-11.132623567824,-10.148727336345,-1251.69705882353));
#156305=CARTESIAN_POINT('Ctrl Pts',(-11.9702584092036,-9.03951954568885,
-1253.19117647059));
#156306=CARTESIAN_POINT('Ctrl Pts',(-12.8078932505832,-7.93031175503273,
-1254.68529411765));
#156307=CARTESIAN_POINT('Ctrl Pts',(-13.4274493703259,-6.68607533664808,
-1256.17941176471));
#156308=CARTESIAN_POINT('Ctrl Pts',(-14.0470054900687,-5.44183891826343,
-1257.67352941176));
#156309=CARTESIAN_POINT('Ctrl Pts',(-14.4273846475923,-4.10494485108124,
-1259.16764705882));
#156310=CARTESIAN_POINT('Ctrl Pts',(-14.8077638051159,-2.76805078389906,
-1260.66176470588));
#156311=CARTESIAN_POINT('Ctrl Pts',(-14.9360126444255,-1.38402539194953,
-1262.15588235294));
#156312=CARTESIAN_POINT('Ctrl Pts',(-15.0642614837351,-9.22419980378748E-16,
-1263.65));
#156313=CARTESIAN_POINT('Ctrl Pts',(-14.9360126444255,1.38402539194953,
-1265.14411764706));
#156314=CARTESIAN_POINT('Ctrl Pts',(-14.8077638051159,2.76805078389906,
-1266.63823529412));
#156315=CARTESIAN_POINT('Ctrl Pts',(-14.4273846475923,4.10494485108124,
-1268.13235294118));
#156316=CARTESIAN_POINT('Ctrl Pts',(-14.0470054900687,5.44183891826343,
-1269.62647058824));
#156317=CARTESIAN_POINT('Ctrl Pts',(-13.4274493703259,6.68607533664807,
-1271.12058823529));
#156318=CARTESIAN_POINT('Ctrl Pts',(-12.8078932505832,7.93031175503273,
-1272.61470588235));
#156319=CARTESIAN_POINT('Ctrl Pts',(-11.9702584092036,9.03951954568884,
-1274.10882352941));
#156320=CARTESIAN_POINT('Ctrl Pts',(-11.132623567824,10.148727336345,-1275.60294117647));
#156321=CARTESIAN_POINT('Ctrl Pts',(-10.1054346546984,11.0851337583099,
-1277.09705882353));
#156322=CARTESIAN_POINT('Ctrl Pts',(-9.07824574157275,12.0215401802748,
-1278.59117647059));
#156323=CARTESIAN_POINT('Ctrl Pts',(-7.89648244316034,12.7532570359442,
-1280.08529411765));
#156324=CARTESIAN_POINT('Ctrl Pts',(-6.71471914474793,13.4849738916136,
-1281.57941176471));
#156325=CARTESIAN_POINT('Ctrl Pts',(-5.41862499280729,13.9870834410653,
-1283.07352941176));
#156326=CARTESIAN_POINT('Ctrl Pts',(-4.12253084086667,14.4891929905171,
-1284.56764705882));
#156327=CARTESIAN_POINT('Ctrl Pts',(-2.75624276724856,14.7445964952585,
-1286.06176470588));
#156328=CARTESIAN_POINT('Ctrl Pts',(-1.38995469363044,15.,-1287.55588235294));
#156329=CARTESIAN_POINT('Ctrl Pts',(-1.83697019872103E-15,15.,-1289.05));
#156330=CARTESIAN_POINT('Ctrl Pts',(1.38995469363045,15.,-1290.54411764706));
#156331=CARTESIAN_POINT('Ctrl Pts',(2.75624276724855,14.7445964952585,-1292.03823529412));
#156332=CARTESIAN_POINT('Ctrl Pts',(4.12253084086666,14.4891929905171,-1293.53235294118));
#156333=CARTESIAN_POINT('Ctrl Pts',(5.4186249928073,13.9870834410653,-1295.02647058824));
#156334=CARTESIAN_POINT('Ctrl Pts',(6.71471914474792,13.4849738916136,-1296.52058823529));
#156335=CARTESIAN_POINT('Ctrl Pts',(7.89648244316034,12.7532570359442,-1298.01470588235));
#156336=CARTESIAN_POINT('Ctrl Pts',(9.07824574157275,12.0215401802748,-1299.50882352941));
#156337=CARTESIAN_POINT('Ctrl Pts',(10.1054346546984,11.0851337583099,-1301.00294117647));
#156338=CARTESIAN_POINT('Ctrl Pts',(11.132623567824,10.148727336345,-1302.49705882353));
#156339=CARTESIAN_POINT('Ctrl Pts',(11.9702584092036,9.03951954568885,-1303.99117647059));
#156340=CARTESIAN_POINT('Ctrl Pts',(12.8078932505832,7.93031175503273,-1305.48529411765));
#156341=CARTESIAN_POINT('Ctrl Pts',(13.4274493703259,6.68607533664807,-1306.97941176471));
#156342=CARTESIAN_POINT('Ctrl Pts',(14.0470054900687,5.44183891826343,-1308.47352941176));
#156343=CARTESIAN_POINT('Ctrl Pts',(14.4273846475923,4.10494485108125,-1309.96764705882));
#156344=CARTESIAN_POINT('Ctrl Pts',(14.8077638051159,2.76805078389905,-1311.46176470588));
#156345=CARTESIAN_POINT('Ctrl Pts',(14.9360126444255,1.38402539194953,-1312.95588235294));
#156346=CARTESIAN_POINT('Ctrl Pts',(15.0642614837351,2.76725994113625E-15,
-1314.45));
#156347=CARTESIAN_POINT('Ctrl Pts',(14.9360126444255,-1.38402539194952,
-1315.94411764706));
#156348=CARTESIAN_POINT('Ctrl Pts',(14.8077638051159,-2.76805078389906,
-1317.43823529412));
#156349=CARTESIAN_POINT('Ctrl Pts',(14.4273846475923,-4.10494485108124,
-1318.93235294118));
#156350=CARTESIAN_POINT('Ctrl Pts',(14.0470054900687,-5.44183891826342,
-1320.42647058824));
#156351=CARTESIAN_POINT('Ctrl Pts',(13.4274493703259,-6.68607533664808,
-1321.92058823529));
#156352=CARTESIAN_POINT('Ctrl Pts',(12.8078932505832,-7.93031175503273,
-1323.41470588235));
#156353=CARTESIAN_POINT('Ctrl Pts',(11.9702584092036,-9.03951954568884,
-1324.90882352941));
#156354=CARTESIAN_POINT('Ctrl Pts',(11.132623567824,-10.148727336345,-1326.40294117647));
#156355=CARTESIAN_POINT('Ctrl Pts',(10.1054346546984,-11.0851337583099,
-1327.89705882353));
#156356=CARTESIAN_POINT('Ctrl Pts',(9.07824574157275,-12.0215401802748,
-1329.39117647059));
#156357=CARTESIAN_POINT('Ctrl Pts',(7.89648244316034,-12.7532570359442,
-1330.88529411765));
#156358=CARTESIAN_POINT('Ctrl Pts',(6.71471914474792,-13.4849738916136,
-1332.37941176471));
#156359=CARTESIAN_POINT('Ctrl Pts',(5.4186249928073,-13.9870834410653,-1333.87352941176));
#156360=CARTESIAN_POINT('Ctrl Pts',(4.12253084086667,-14.4891929905171,
-1335.36764705882));
#156361=CARTESIAN_POINT('Ctrl Pts',(2.75624276724855,-14.7445964952585,
-1336.86176470588));
#156362=CARTESIAN_POINT('Ctrl Pts',(1.38995469363045,-15.,-1338.35588235294));
#156363=CARTESIAN_POINT('Ctrl Pts',(0.,-15.,-1339.85));
#156364=CARTESIAN_POINT('Ctrl Pts',(-1.38995469363045,-15.,-1341.34411764706));
#156365=CARTESIAN_POINT('Ctrl Pts',(-2.75624276724856,-14.7445964952585,
-1342.83823529412));
#156366=CARTESIAN_POINT('Ctrl Pts',(-4.12253084086666,-14.4891929905171,
-1344.33235294118));
#156367=CARTESIAN_POINT('Ctrl Pts',(-5.41862499280729,-13.9870834410653,
-1345.82647058824));
#156368=CARTESIAN_POINT('Ctrl Pts',(-6.71471914474793,-13.4849738916136,
-1347.32058823529));
#156369=CARTESIAN_POINT('Ctrl Pts',(-7.89648244316034,-12.7532570359442,
-1348.81470588235));
#156370=CARTESIAN_POINT('Ctrl Pts',(-9.07824574157275,-12.0215401802748,
-1350.30882352941));
#156371=CARTESIAN_POINT('Ctrl Pts',(-10.1054346546984,-11.0851337583099,
-1351.80294117647));
#156372=CARTESIAN_POINT('Ctrl Pts',(-11.132623567824,-10.148727336345,-1353.29705882353));
#156373=CARTESIAN_POINT('Ctrl Pts',(-11.9702584092036,-9.03951954568885,
-1354.79117647059));
#156374=CARTESIAN_POINT('Ctrl Pts',(-12.8078932505832,-7.93031175503273,
-1356.28529411765));
#156375=CARTESIAN_POINT('Ctrl Pts',(-13.4274493703259,-6.68607533664808,
-1357.77941176471));
#156376=CARTESIAN_POINT('Ctrl Pts',(-14.0470054900687,-5.44183891826343,
-1359.27352941176));
#156377=CARTESIAN_POINT('Ctrl Pts',(-14.4273846475923,-4.10494485108124,
-1360.76764705882));
#156378=CARTESIAN_POINT('Ctrl Pts',(-14.8077638051159,-2.76805078389906,
-1362.26176470588));
#156379=CARTESIAN_POINT('Ctrl Pts',(-14.9360126444255,-1.38402539194953,
-1363.75588235294));
#156380=CARTESIAN_POINT('Ctrl Pts',(-15.0642614837351,-9.22419980378748E-16,
-1365.25));
#156381=CARTESIAN_POINT('Ctrl Pts',(-14.9360126444255,1.38402539194953,
-1366.74411764706));
#156382=CARTESIAN_POINT('Ctrl Pts',(-14.8077638051159,2.76805078389906,
-1368.23823529412));
#156383=CARTESIAN_POINT('Ctrl Pts',(-14.4273846475923,4.10494485108124,
-1369.73235294118));
#156384=CARTESIAN_POINT('Ctrl Pts',(-14.0470054900687,5.44183891826343,
-1371.22647058824));
#156385=CARTESIAN_POINT('Ctrl Pts',(-13.4274493703259,6.68607533664807,
-1372.72058823529));
#156386=CARTESIAN_POINT('Ctrl Pts',(-12.8078932505832,7.93031175503273,
-1374.21470588235));
#156387=CARTESIAN_POINT('Ctrl Pts',(-11.9702584092036,9.03951954568884,
-1375.70882352941));
#156388=CARTESIAN_POINT('Ctrl Pts',(-11.132623567824,10.148727336345,-1377.20294117647));
#156389=CARTESIAN_POINT('Ctrl Pts',(-10.1054346546984,11.0851337583099,
-1378.69705882353));
#156390=CARTESIAN_POINT('Ctrl Pts',(-9.07824574157275,12.0215401802748,
-1380.19117647059));
#156391=CARTESIAN_POINT('Ctrl Pts',(-7.89648244316034,12.7532570359442,
-1381.68529411765));
#156392=CARTESIAN_POINT('Ctrl Pts',(-6.71471914474793,13.4849738916136,
-1383.17941176471));
#156393=CARTESIAN_POINT('Ctrl Pts',(-5.41862499280729,13.9870834410653,
-1384.67352941176));
#156394=CARTESIAN_POINT('Ctrl Pts',(-4.12253084086667,14.4891929905171,
-1386.16764705882));
#156395=CARTESIAN_POINT('Ctrl Pts',(-2.75624276724856,14.7445964952585,
-1387.66176470588));
#156396=CARTESIAN_POINT('Ctrl Pts',(-1.38995469363044,15.,-1389.15588235294));
#156397=CARTESIAN_POINT('Ctrl Pts',(-1.83697019872103E-15,15.,-1390.65));
#156398=CARTESIAN_POINT('Ctrl Pts',(1.38995469363045,15.,-1392.14411764706));
#156399=CARTESIAN_POINT('Ctrl Pts',(2.75624276724855,14.7445964952585,-1393.63823529412));
#156400=CARTESIAN_POINT('Ctrl Pts',(4.12253084086666,14.4891929905171,-1395.13235294118));
#156401=CARTESIAN_POINT('Ctrl Pts',(5.4186249928073,13.9870834410653,-1396.62647058824));
#156402=CARTESIAN_POINT('Ctrl Pts',(6.71471914474792,13.4849738916136,-1398.12058823529));
#156403=CARTESIAN_POINT('Ctrl Pts',(7.89648244316034,12.7532570359442,-1399.61470588235));
#156404=CARTESIAN_POINT('Ctrl Pts',(9.07824574157275,12.0215401802748,-1401.10882352941));
#156405=CARTESIAN_POINT('Ctrl Pts',(10.1054346546984,11.0851337583099,-1402.60294117647));
#156406=CARTESIAN_POINT('Ctrl Pts',(11.132623567824,10.148727336345,-1404.09705882353));
#156407=CARTESIAN_POINT('Ctrl Pts',(11.9702584092036,9.03951954568885,-1405.59117647059));
#156408=CARTESIAN_POINT('Ctrl Pts',(12.8078932505832,7.93031175503273,-1407.08529411765));
#156409=CARTESIAN_POINT('Ctrl Pts',(13.4274493703259,6.68607533664807,-1408.57941176471));
#156410=CARTESIAN_POINT('Ctrl Pts',(14.0470054900687,5.44183891826343,-1410.07352941176));
#156411=CARTESIAN_POINT('Ctrl Pts',(14.4273846475923,4.10494485108125,-1411.56764705882));
#156412=CARTESIAN_POINT('Ctrl Pts',(14.8077638051159,2.76805078389905,-1413.06176470588));
#156413=CARTESIAN_POINT('Ctrl Pts',(14.9360126444255,1.38402539194953,-1414.55588235294));
#156414=CARTESIAN_POINT('Ctrl Pts',(15.0642614837351,2.76725994113625E-15,
-1416.05));
#156415=CARTESIAN_POINT('Ctrl Pts',(14.9360126444255,-1.38402539194952,
-1417.54411764706));
#156416=CARTESIAN_POINT('Ctrl Pts',(14.8077638051159,-2.76805078389906,
-1419.03823529412));
#156417=CARTESIAN_POINT('Ctrl Pts',(14.4273846475923,-4.10494485108124,
-1420.53235294118));
#156418=CARTESIAN_POINT('Ctrl Pts',(14.0470054900687,-5.44183891826342,
-1422.02647058824));
#156419=CARTESIAN_POINT('Ctrl Pts',(13.4274493703259,-6.68607533664808,
-1423.52058823529));
#156420=CARTESIAN_POINT('Ctrl Pts',(12.8078932505832,-7.93031175503273,
-1425.01470588235));
#156421=CARTESIAN_POINT('Ctrl Pts',(11.9702584092036,-9.03951954568884,
-1426.50882352941));
#156422=CARTESIAN_POINT('Ctrl Pts',(11.132623567824,-10.148727336345,-1428.00294117647));
#156423=CARTESIAN_POINT('Ctrl Pts',(10.1054346546984,-11.0851337583099,
-1429.49705882353));
#156424=CARTESIAN_POINT('Ctrl Pts',(9.07824574157275,-12.0215401802748,
-1430.99117647059));
#156425=CARTESIAN_POINT('Ctrl Pts',(7.89648244316034,-12.7532570359442,
-1432.48529411765));
#156426=CARTESIAN_POINT('Ctrl Pts',(6.71471914474792,-13.4849738916136,
-1433.97941176471));
#156427=CARTESIAN_POINT('Ctrl Pts',(5.4186249928073,-13.9870834410653,-1435.47352941176));
#156428=CARTESIAN_POINT('Ctrl Pts',(4.12253084086667,-14.4891929905171,
-1436.96764705882));
#156429=CARTESIAN_POINT('Ctrl Pts',(2.75624276724855,-14.7445964952585,
-1438.46176470588));
#156430=CARTESIAN_POINT('Ctrl Pts',(1.38995469363045,-15.,-1439.95588235294));
#156431=CARTESIAN_POINT('Ctrl Pts',(0.,-15.,-1441.45));
#156432=CARTESIAN_POINT('Ctrl Pts',(-1.38995469363045,-15.,-1442.94411764706));
#156433=CARTESIAN_POINT('Ctrl Pts',(-2.75624276724856,-14.7445964952585,
-1444.43823529412));
#156434=CARTESIAN_POINT('Ctrl Pts',(-4.12253084086666,-14.4891929905171,
-1445.93235294118));
#156435=CARTESIAN_POINT('Ctrl Pts',(-5.41862499280729,-13.9870834410653,
-1447.42647058824));
#156436=CARTESIAN_POINT('Ctrl Pts',(-6.71471914474793,-13.4849738916136,
-1448.92058823529));
#156437=CARTESIAN_POINT('Ctrl Pts',(-7.89648244316034,-12.7532570359442,
-1450.41470588235));
#156438=CARTESIAN_POINT('Ctrl Pts',(-9.07824574157275,-12.0215401802748,
-1451.90882352941));
#156439=CARTESIAN_POINT('Ctrl Pts',(-10.1054346546984,-11.0851337583099,
-1453.40294117647));
#156440=CARTESIAN_POINT('Ctrl Pts',(-11.132623567824,-10.148727336345,-1454.89705882353));
#156441=CARTESIAN_POINT('Ctrl Pts',(-11.9702584092036,-9.03951954568885,
-1456.39117647059));
#156442=CARTESIAN_POINT('Ctrl Pts',(-12.8078932505832,-7.93031175503273,
-1457.88529411765));
#156443=CARTESIAN_POINT('Ctrl Pts',(-13.4274493703259,-6.68607533664808,
-1459.37941176471));
#156444=CARTESIAN_POINT('Ctrl Pts',(-14.0470054900687,-5.44183891826343,
-1460.87352941176));
#156445=CARTESIAN_POINT('Ctrl Pts',(-14.4273846475923,-4.10494485108124,
-1462.36764705882));
#156446=CARTESIAN_POINT('Ctrl Pts',(-14.8077638051159,-2.76805078389906,
-1463.86176470588));
#156447=CARTESIAN_POINT('Ctrl Pts',(-14.9360126444255,-1.38402539194953,
-1465.35588235294));
#156448=CARTESIAN_POINT('Ctrl Pts',(-15.0642614837351,-9.22419980378748E-16,
-1466.85));
#156449=CARTESIAN_POINT('Ctrl Pts',(-14.9360126444255,1.38402539194953,
-1468.34411764706));
#156450=CARTESIAN_POINT('Ctrl Pts',(-14.8077638051159,2.76805078389906,
-1469.83823529412));
#156451=CARTESIAN_POINT('Ctrl Pts',(-14.4273846475923,4.10494485108124,
-1471.33235294118));
#156452=CARTESIAN_POINT('Ctrl Pts',(-14.0470054900687,5.44183891826343,
-1472.82647058824));
#156453=CARTESIAN_POINT('Ctrl Pts',(-13.4274493703259,6.68607533664807,
-1474.32058823529));
#156454=CARTESIAN_POINT('Ctrl Pts',(-12.8078932505832,7.93031175503273,
-1475.81470588235));
#156455=CARTESIAN_POINT('Ctrl Pts',(-11.9702584092036,9.03951954568884,
-1477.30882352941));
#156456=CARTESIAN_POINT('Ctrl Pts',(-11.132623567824,10.148727336345,-1478.80294117647));
#156457=CARTESIAN_POINT('Ctrl Pts',(-10.1054346546984,11.0851337583099,
-1480.29705882353));
#156458=CARTESIAN_POINT('Ctrl Pts',(-9.07824574157275,12.0215401802748,
-1481.79117647059));
#156459=CARTESIAN_POINT('Ctrl Pts',(-7.89648244316034,12.7532570359442,
-1483.28529411765));
#156460=CARTESIAN_POINT('Ctrl Pts',(-6.71471914474793,13.4849738916136,
-1484.77941176471));
#156461=CARTESIAN_POINT('Ctrl Pts',(-5.41862499280729,13.9870834410653,
-1486.27352941176));
#156462=CARTESIAN_POINT('Ctrl Pts',(-4.12253084086667,14.4891929905171,
-1487.76764705882));
#156463=CARTESIAN_POINT('Ctrl Pts',(-2.75624276724856,14.7445964952585,
-1489.26176470588));
#156464=CARTESIAN_POINT('Ctrl Pts',(-1.38995469363044,15.,-1490.75588235294));
#156465=CARTESIAN_POINT('Ctrl Pts',(-1.83697019872103E-15,15.,-1492.25));
#156466=CARTESIAN_POINT('Ctrl Pts',(1.38995469363045,15.,-1493.74411764706));
#156467=CARTESIAN_POINT('Ctrl Pts',(2.75624276724855,14.7445964952585,-1495.23823529412));
#156468=CARTESIAN_POINT('Ctrl Pts',(4.12253084086666,14.4891929905171,-1496.73235294118));
#156469=CARTESIAN_POINT('Ctrl Pts',(5.4186249928073,13.9870834410653,-1498.22647058824));
#156470=CARTESIAN_POINT('Ctrl Pts',(6.26766581794969,13.6581632730821,-1499.20523195215));
#156471=CARTESIAN_POINT('Ctrl Pts',(7.0706872023049,13.228959992651,-1500.18777724595));
#156472=CARTESIAN_POINT('Ctrl Pts',(19.3695474754025,6.6553975974033,-1515.23617759469));
#156473=CARTESIAN_POINT('Ctrl Pts',(31.6684077485001,0.0818352021555714,
-1530.28457794343));
#156474=CARTESIAN_POINT('Ctrl Pts',(0.,-18.048,1504.95));
#156475=CARTESIAN_POINT('Ctrl Pts',(-1.67239348737615,-18.048,1503.45588235294));
#156476=CARTESIAN_POINT('Ctrl Pts',(-3.31631129755346,-17.7406985030951,
1501.96176470588));
#156477=CARTESIAN_POINT('Ctrl Pts',(-4.96022910773077,-17.4333970061901,
1500.46764705882));
#156478=CARTESIAN_POINT('Ctrl Pts',(-6.51968959134574,-16.8292587962898,
1498.97352941176));
#156479=CARTESIAN_POINT('Ctrl Pts',(-8.07915007496071,-16.2251205863895,
1497.47941176471));
#156480=CARTESIAN_POINT('Ctrl Pts',(-9.50104767561052,-15.3447188656481,
1495.98529411765));
#156481=CARTESIAN_POINT('Ctrl Pts',(-10.9229452762603,-14.4643171449067,
1494.49117647059));
#156482=CARTESIAN_POINT('Ctrl Pts',(-12.1588589765331,-13.3376329379985,
1492.99705882353));
#156483=CARTESIAN_POINT('Ctrl Pts',(-13.3947726768058,-12.2109487310903,
1491.50294117647));
#156484=CARTESIAN_POINT('Ctrl Pts',(-14.4026149179538,-10.8763499173728,
1490.00882352941));
#156485=CARTESIAN_POINT('Ctrl Pts',(-15.4104571591017,-9.54175110365538,
1488.51470588235));
#156486=CARTESIAN_POINT('Ctrl Pts',(-16.1559070823762,-8.04468584505497,
1487.02058823529));
#156487=CARTESIAN_POINT('Ctrl Pts',(-16.9013570056506,-6.54762058645456,
1485.52647058824));
#156488=CARTESIAN_POINT('Ctrl Pts',(-17.3590292079831,-4.93906964482095,
1484.03235294118));
#156489=CARTESIAN_POINT('Ctrl Pts',(-17.8167014103155,-3.33051870318735,
1482.53823529412));
#156490=CARTESIAN_POINT('Ctrl Pts',(-17.9710104137728,-1.66525935159368,
1481.04411764706));
#156491=CARTESIAN_POINT('Ctrl Pts',(-18.1253194172301,-1.10985572039171E-15,
1479.55));
#156492=CARTESIAN_POINT('Ctrl Pts',(-17.9710104137728,1.66525935159367,
1478.05588235294));
#156493=CARTESIAN_POINT('Ctrl Pts',(-17.8167014103155,3.33051870318735,
1476.56176470588));
#156494=CARTESIAN_POINT('Ctrl Pts',(-17.3590292079831,4.93906964482096,
1475.06764705882));
#156495=CARTESIAN_POINT('Ctrl Pts',(-16.9013570056506,6.54762058645456,
1473.57352941176));
#156496=CARTESIAN_POINT('Ctrl Pts',(-16.1559070823762,8.04468584505497,
1472.07941176471));
#156497=CARTESIAN_POINT('Ctrl Pts',(-15.4104571591017,9.54175110365538,
1470.58529411765));
#156498=CARTESIAN_POINT('Ctrl Pts',(-14.4026149179538,10.8763499173728,
1469.09117647059));
#156499=CARTESIAN_POINT('Ctrl Pts',(-13.3947726768058,12.2109487310903,
1467.59705882353));
#156500=CARTESIAN_POINT('Ctrl Pts',(-12.1588589765331,13.3376329379985,
1466.10294117647));
#156501=CARTESIAN_POINT('Ctrl Pts',(-10.9229452762603,14.4643171449067,
1464.60882352941));
#156502=CARTESIAN_POINT('Ctrl Pts',(-9.50104767561052,15.3447188656481,
1463.11470588235));
#156503=CARTESIAN_POINT('Ctrl Pts',(-8.07915007496071,16.2251205863895,
1461.62058823529));
#156504=CARTESIAN_POINT('Ctrl Pts',(-6.51968959134574,16.8292587962898,
1460.12647058824));
#156505=CARTESIAN_POINT('Ctrl Pts',(-4.96022910773078,17.4333970061901,
1458.63235294118));
#156506=CARTESIAN_POINT('Ctrl Pts',(-3.31631129755346,17.7406985030951,
1457.13823529412));
#156507=CARTESIAN_POINT('Ctrl Pts',(-1.67239348737615,18.048,1455.64411764706));
#156508=CARTESIAN_POINT('Ctrl Pts',(-2.21024254310115E-15,18.048,1454.15));
#156509=CARTESIAN_POINT('Ctrl Pts',(1.67239348737616,18.048,1452.65588235294));
#156510=CARTESIAN_POINT('Ctrl Pts',(3.31631129755346,17.7406985030951,1451.16176470588));
#156511=CARTESIAN_POINT('Ctrl Pts',(4.96022910773077,17.4333970061901,1449.66764705882));
#156512=CARTESIAN_POINT('Ctrl Pts',(6.51968959134575,16.8292587962898,1448.17352941177));
#156513=CARTESIAN_POINT('Ctrl Pts',(8.07915007496071,16.2251205863895,1446.67941176471));
#156514=CARTESIAN_POINT('Ctrl Pts',(9.50104767561053,15.3447188656481,1445.18529411765));
#156515=CARTESIAN_POINT('Ctrl Pts',(10.9229452762603,14.4643171449067,1443.69117647059));
#156516=CARTESIAN_POINT('Ctrl Pts',(12.1588589765331,13.3376329379985,1442.19705882353));
#156517=CARTESIAN_POINT('Ctrl Pts',(13.3947726768058,12.2109487310903,1440.70294117647));
#156518=CARTESIAN_POINT('Ctrl Pts',(14.4026149179538,10.8763499173728,1439.20882352941));
#156519=CARTESIAN_POINT('Ctrl Pts',(15.4104571591017,9.54175110365538,1437.71470588235));
#156520=CARTESIAN_POINT('Ctrl Pts',(16.1559070823762,8.04468584505496,1436.22058823529));
#156521=CARTESIAN_POINT('Ctrl Pts',(16.9013570056506,6.54762058645456,1434.72647058824));
#156522=CARTESIAN_POINT('Ctrl Pts',(17.3590292079831,4.93906964482096,1433.23235294118));
#156523=CARTESIAN_POINT('Ctrl Pts',(17.8167014103155,3.33051870318735,1431.73823529412));
#156524=CARTESIAN_POINT('Ctrl Pts',(17.9710104137728,1.66525935159367,1430.24411764706));
#156525=CARTESIAN_POINT('Ctrl Pts',(18.1253194172301,3.32956716117513E-15,
1428.75));
#156526=CARTESIAN_POINT('Ctrl Pts',(17.9710104137728,-1.66525935159367,
1427.25588235294));
#156527=CARTESIAN_POINT('Ctrl Pts',(17.8167014103155,-3.33051870318736,
1425.76176470588));
#156528=CARTESIAN_POINT('Ctrl Pts',(17.3590292079831,-4.93906964482095,
1424.26764705882));
#156529=CARTESIAN_POINT('Ctrl Pts',(16.9013570056506,-6.54762058645456,
1422.77352941176));
#156530=CARTESIAN_POINT('Ctrl Pts',(16.1559070823762,-8.04468584505497,
1421.27941176471));
#156531=CARTESIAN_POINT('Ctrl Pts',(15.4104571591017,-9.54175110365538,
1419.78529411765));
#156532=CARTESIAN_POINT('Ctrl Pts',(14.4026149179538,-10.8763499173728,
1418.29117647059));
#156533=CARTESIAN_POINT('Ctrl Pts',(13.3947726768058,-12.2109487310903,
1416.79705882353));
#156534=CARTESIAN_POINT('Ctrl Pts',(12.1588589765331,-13.3376329379985,
1415.30294117647));
#156535=CARTESIAN_POINT('Ctrl Pts',(10.9229452762603,-14.4643171449067,
1413.80882352941));
#156536=CARTESIAN_POINT('Ctrl Pts',(9.50104767561053,-15.3447188656481,
1412.31470588235));
#156537=CARTESIAN_POINT('Ctrl Pts',(8.07915007496071,-16.2251205863895,
1410.82058823529));
#156538=CARTESIAN_POINT('Ctrl Pts',(6.51968959134574,-16.8292587962898,
1409.32647058824));
#156539=CARTESIAN_POINT('Ctrl Pts',(4.96022910773078,-17.4333970061901,
1407.83235294118));
#156540=CARTESIAN_POINT('Ctrl Pts',(3.31631129755346,-17.7406985030951,
1406.33823529412));
#156541=CARTESIAN_POINT('Ctrl Pts',(1.67239348737615,-18.048,1404.84411764706));
#156542=CARTESIAN_POINT('Ctrl Pts',(0.,-18.048,1403.35));
#156543=CARTESIAN_POINT('Ctrl Pts',(-1.67239348737615,-18.048,1401.85588235294));
#156544=CARTESIAN_POINT('Ctrl Pts',(-3.31631129755346,-17.7406985030951,
1400.36176470588));
#156545=CARTESIAN_POINT('Ctrl Pts',(-4.96022910773077,-17.4333970061901,
1398.86764705882));
#156546=CARTESIAN_POINT('Ctrl Pts',(-6.51968959134574,-16.8292587962898,
1397.37352941176));
#156547=CARTESIAN_POINT('Ctrl Pts',(-8.07915007496071,-16.2251205863895,
1395.87941176471));
#156548=CARTESIAN_POINT('Ctrl Pts',(-9.50104767561052,-15.3447188656481,
1394.38529411765));
#156549=CARTESIAN_POINT('Ctrl Pts',(-10.9229452762603,-14.4643171449067,
1392.89117647059));
#156550=CARTESIAN_POINT('Ctrl Pts',(-12.1588589765331,-13.3376329379985,
1391.39705882353));
#156551=CARTESIAN_POINT('Ctrl Pts',(-13.3947726768058,-12.2109487310903,
1389.90294117647));
#156552=CARTESIAN_POINT('Ctrl Pts',(-14.4026149179538,-10.8763499173728,
1388.40882352941));
#156553=CARTESIAN_POINT('Ctrl Pts',(-15.4104571591017,-9.54175110365538,
1386.91470588235));
#156554=CARTESIAN_POINT('Ctrl Pts',(-16.1559070823762,-8.04468584505497,
1385.42058823529));
#156555=CARTESIAN_POINT('Ctrl Pts',(-16.9013570056506,-6.54762058645456,
1383.92647058824));
#156556=CARTESIAN_POINT('Ctrl Pts',(-17.3590292079831,-4.93906964482095,
1382.43235294118));
#156557=CARTESIAN_POINT('Ctrl Pts',(-17.8167014103155,-3.33051870318735,
1380.93823529412));
#156558=CARTESIAN_POINT('Ctrl Pts',(-17.9710104137728,-1.66525935159368,
1379.44411764706));
#156559=CARTESIAN_POINT('Ctrl Pts',(-18.1253194172301,-1.10985572039171E-15,
1377.95));
#156560=CARTESIAN_POINT('Ctrl Pts',(-17.9710104137728,1.66525935159367,
1376.45588235294));
#156561=CARTESIAN_POINT('Ctrl Pts',(-17.8167014103155,3.33051870318735,
1374.96176470588));
#156562=CARTESIAN_POINT('Ctrl Pts',(-17.3590292079831,4.93906964482096,
1373.46764705882));
#156563=CARTESIAN_POINT('Ctrl Pts',(-16.9013570056506,6.54762058645456,
1371.97352941176));
#156564=CARTESIAN_POINT('Ctrl Pts',(-16.1559070823762,8.04468584505497,
1370.47941176471));
#156565=CARTESIAN_POINT('Ctrl Pts',(-15.4104571591017,9.54175110365538,
1368.98529411765));
#156566=CARTESIAN_POINT('Ctrl Pts',(-14.4026149179538,10.8763499173728,
1367.49117647059));
#156567=CARTESIAN_POINT('Ctrl Pts',(-13.3947726768058,12.2109487310903,
1365.99705882353));
#156568=CARTESIAN_POINT('Ctrl Pts',(-12.1588589765331,13.3376329379985,
1364.50294117647));
#156569=CARTESIAN_POINT('Ctrl Pts',(-10.9229452762603,14.4643171449067,
1363.00882352941));
#156570=CARTESIAN_POINT('Ctrl Pts',(-9.50104767561052,15.3447188656481,
1361.51470588235));
#156571=CARTESIAN_POINT('Ctrl Pts',(-8.07915007496071,16.2251205863895,
1360.02058823529));
#156572=CARTESIAN_POINT('Ctrl Pts',(-6.51968959134574,16.8292587962898,
1358.52647058824));
#156573=CARTESIAN_POINT('Ctrl Pts',(-4.96022910773078,17.4333970061901,
1357.03235294118));
#156574=CARTESIAN_POINT('Ctrl Pts',(-3.31631129755346,17.7406985030951,
1355.53823529412));
#156575=CARTESIAN_POINT('Ctrl Pts',(-1.67239348737615,18.048,1354.04411764706));
#156576=CARTESIAN_POINT('Ctrl Pts',(-2.21024254310115E-15,18.048,1352.55));
#156577=CARTESIAN_POINT('Ctrl Pts',(1.67239348737616,18.048,1351.05588235294));
#156578=CARTESIAN_POINT('Ctrl Pts',(3.31631129755346,17.7406985030951,1349.56176470588));
#156579=CARTESIAN_POINT('Ctrl Pts',(4.96022910773077,17.4333970061901,1348.06764705882));
#156580=CARTESIAN_POINT('Ctrl Pts',(6.51968959134575,16.8292587962898,1346.57352941176));
#156581=CARTESIAN_POINT('Ctrl Pts',(8.07915007496071,16.2251205863895,1345.07941176471));
#156582=CARTESIAN_POINT('Ctrl Pts',(9.50104767561053,15.3447188656481,1343.58529411765));
#156583=CARTESIAN_POINT('Ctrl Pts',(10.9229452762603,14.4643171449067,1342.09117647059));
#156584=CARTESIAN_POINT('Ctrl Pts',(12.1588589765331,13.3376329379985,1340.59705882353));
#156585=CARTESIAN_POINT('Ctrl Pts',(13.3947726768058,12.2109487310903,1339.10294117647));
#156586=CARTESIAN_POINT('Ctrl Pts',(14.4026149179538,10.8763499173728,1337.60882352941));
#156587=CARTESIAN_POINT('Ctrl Pts',(15.4104571591017,9.54175110365538,1336.11470588235));
#156588=CARTESIAN_POINT('Ctrl Pts',(16.1559070823762,8.04468584505496,1334.62058823529));
#156589=CARTESIAN_POINT('Ctrl Pts',(16.9013570056506,6.54762058645456,1333.12647058824));
#156590=CARTESIAN_POINT('Ctrl Pts',(17.3590292079831,4.93906964482096,1331.63235294118));
#156591=CARTESIAN_POINT('Ctrl Pts',(17.8167014103155,3.33051870318735,1330.13823529412));
#156592=CARTESIAN_POINT('Ctrl Pts',(17.9710104137728,1.66525935159367,1328.64411764706));
#156593=CARTESIAN_POINT('Ctrl Pts',(18.1253194172301,3.32956716117513E-15,
1327.15));
#156594=CARTESIAN_POINT('Ctrl Pts',(17.9710104137728,-1.66525935159367,
1325.65588235294));
#156595=CARTESIAN_POINT('Ctrl Pts',(17.8167014103155,-3.33051870318736,
1324.16176470588));
#156596=CARTESIAN_POINT('Ctrl Pts',(17.3590292079831,-4.93906964482095,
1322.66764705882));
#156597=CARTESIAN_POINT('Ctrl Pts',(16.9013570056506,-6.54762058645456,
1321.17352941176));
#156598=CARTESIAN_POINT('Ctrl Pts',(16.1559070823762,-8.04468584505497,
1319.67941176471));
#156599=CARTESIAN_POINT('Ctrl Pts',(15.4104571591017,-9.54175110365538,
1318.18529411765));
#156600=CARTESIAN_POINT('Ctrl Pts',(14.4026149179538,-10.8763499173728,
1316.69117647059));
#156601=CARTESIAN_POINT('Ctrl Pts',(13.3947726768058,-12.2109487310903,
1315.19705882353));
#156602=CARTESIAN_POINT('Ctrl Pts',(12.1588589765331,-13.3376329379985,
1313.70294117647));
#156603=CARTESIAN_POINT('Ctrl Pts',(10.9229452762603,-14.4643171449067,
1312.20882352941));
#156604=CARTESIAN_POINT('Ctrl Pts',(9.50104767561053,-15.3447188656481,
1310.71470588235));
#156605=CARTESIAN_POINT('Ctrl Pts',(8.07915007496071,-16.2251205863895,
1309.22058823529));
#156606=CARTESIAN_POINT('Ctrl Pts',(6.51968959134574,-16.8292587962898,
1307.72647058824));
#156607=CARTESIAN_POINT('Ctrl Pts',(4.96022910773078,-17.4333970061901,
1306.23235294118));
#156608=CARTESIAN_POINT('Ctrl Pts',(3.31631129755346,-17.7406985030951,
1304.73823529412));
#156609=CARTESIAN_POINT('Ctrl Pts',(1.67239348737615,-18.048,1303.24411764706));
#156610=CARTESIAN_POINT('Ctrl Pts',(0.,-18.048,1301.75));
#156611=CARTESIAN_POINT('Ctrl Pts',(-1.67239348737615,-18.048,1300.25588235294));
#156612=CARTESIAN_POINT('Ctrl Pts',(-3.31631129755346,-17.7406985030951,
1298.76176470588));
#156613=CARTESIAN_POINT('Ctrl Pts',(-4.96022910773077,-17.4333970061901,
1297.26764705882));
#156614=CARTESIAN_POINT('Ctrl Pts',(-6.51968959134574,-16.8292587962898,
1295.77352941176));
#156615=CARTESIAN_POINT('Ctrl Pts',(-8.07915007496071,-16.2251205863895,
1294.27941176471));
#156616=CARTESIAN_POINT('Ctrl Pts',(-9.50104767561052,-15.3447188656481,
1292.78529411765));
#156617=CARTESIAN_POINT('Ctrl Pts',(-10.9229452762603,-14.4643171449067,
1291.29117647059));
#156618=CARTESIAN_POINT('Ctrl Pts',(-12.1588589765331,-13.3376329379985,
1289.79705882353));
#156619=CARTESIAN_POINT('Ctrl Pts',(-13.3947726768058,-12.2109487310903,
1288.30294117647));
#156620=CARTESIAN_POINT('Ctrl Pts',(-14.4026149179538,-10.8763499173728,
1286.80882352941));
#156621=CARTESIAN_POINT('Ctrl Pts',(-15.4104571591017,-9.54175110365538,
1285.31470588235));
#156622=CARTESIAN_POINT('Ctrl Pts',(-16.1559070823762,-8.04468584505497,
1283.82058823529));
#156623=CARTESIAN_POINT('Ctrl Pts',(-16.9013570056506,-6.54762058645456,
1282.32647058824));
#156624=CARTESIAN_POINT('Ctrl Pts',(-17.3590292079831,-4.93906964482095,
1280.83235294118));
#156625=CARTESIAN_POINT('Ctrl Pts',(-17.8167014103155,-3.33051870318735,
1279.33823529412));
#156626=CARTESIAN_POINT('Ctrl Pts',(-17.9710104137728,-1.66525935159368,
1277.84411764706));
#156627=CARTESIAN_POINT('Ctrl Pts',(-18.1253194172301,-1.10985572039171E-15,
1276.35));
#156628=CARTESIAN_POINT('Ctrl Pts',(-17.9710104137728,1.66525935159367,
1274.85588235294));
#156629=CARTESIAN_POINT('Ctrl Pts',(-17.8167014103155,3.33051870318735,
1273.36176470588));
#156630=CARTESIAN_POINT('Ctrl Pts',(-17.3590292079831,4.93906964482096,
1271.86764705882));
#156631=CARTESIAN_POINT('Ctrl Pts',(-16.9013570056506,6.54762058645456,
1270.37352941176));
#156632=CARTESIAN_POINT('Ctrl Pts',(-16.1559070823762,8.04468584505497,
1268.87941176471));
#156633=CARTESIAN_POINT('Ctrl Pts',(-15.4104571591017,9.54175110365538,
1267.38529411765));
#156634=CARTESIAN_POINT('Ctrl Pts',(-14.4026149179538,10.8763499173728,
1265.89117647059));
#156635=CARTESIAN_POINT('Ctrl Pts',(-13.3947726768058,12.2109487310903,
1264.39705882353));
#156636=CARTESIAN_POINT('Ctrl Pts',(-12.1588589765331,13.3376329379985,
1262.90294117647));
#156637=CARTESIAN_POINT('Ctrl Pts',(-10.9229452762603,14.4643171449067,
1261.40882352941));
#156638=CARTESIAN_POINT('Ctrl Pts',(-9.50104767561052,15.3447188656481,
1259.91470588235));
#156639=CARTESIAN_POINT('Ctrl Pts',(-8.07915007496071,16.2251205863895,
1258.42058823529));
#156640=CARTESIAN_POINT('Ctrl Pts',(-6.51968959134574,16.8292587962898,
1256.92647058824));
#156641=CARTESIAN_POINT('Ctrl Pts',(-4.96022910773078,17.4333970061901,
1255.43235294118));
#156642=CARTESIAN_POINT('Ctrl Pts',(-3.31631129755346,17.7406985030951,
1253.93823529412));
#156643=CARTESIAN_POINT('Ctrl Pts',(-1.67239348737615,18.048,1252.44411764706));
#156644=CARTESIAN_POINT('Ctrl Pts',(-2.21024254310115E-15,18.048,1250.95));
#156645=CARTESIAN_POINT('Ctrl Pts',(1.67239348737616,18.048,1249.45588235294));
#156646=CARTESIAN_POINT('Ctrl Pts',(3.31631129755346,17.7406985030951,1247.96176470588));
#156647=CARTESIAN_POINT('Ctrl Pts',(4.96022910773077,17.4333970061901,1246.46764705882));
#156648=CARTESIAN_POINT('Ctrl Pts',(6.51968959134575,16.8292587962898,1244.97352941176));
#156649=CARTESIAN_POINT('Ctrl Pts',(8.07915007496071,16.2251205863895,1243.47941176471));
#156650=CARTESIAN_POINT('Ctrl Pts',(9.50104767561053,15.3447188656481,1241.98529411765));
#156651=CARTESIAN_POINT('Ctrl Pts',(10.9229452762603,14.4643171449067,1240.49117647059));
#156652=CARTESIAN_POINT('Ctrl Pts',(12.1588589765331,13.3376329379985,1238.99705882353));
#156653=CARTESIAN_POINT('Ctrl Pts',(13.3947726768058,12.2109487310903,1237.50294117647));
#156654=CARTESIAN_POINT('Ctrl Pts',(14.4026149179538,10.8763499173728,1236.00882352941));
#156655=CARTESIAN_POINT('Ctrl Pts',(15.4104571591017,9.54175110365538,1234.51470588235));
#156656=CARTESIAN_POINT('Ctrl Pts',(16.1559070823762,8.04468584505496,1233.02058823529));
#156657=CARTESIAN_POINT('Ctrl Pts',(16.9013570056506,6.54762058645456,1231.52647058824));
#156658=CARTESIAN_POINT('Ctrl Pts',(17.3590292079831,4.93906964482096,1230.03235294118));
#156659=CARTESIAN_POINT('Ctrl Pts',(17.8167014103155,3.33051870318735,1228.53823529412));
#156660=CARTESIAN_POINT('Ctrl Pts',(17.9710104137728,1.66525935159367,1227.04411764706));
#156661=CARTESIAN_POINT('Ctrl Pts',(18.1253194172301,3.32956716117513E-15,
1225.55));
#156662=CARTESIAN_POINT('Ctrl Pts',(17.9710104137728,-1.66525935159367,
1224.05588235294));
#156663=CARTESIAN_POINT('Ctrl Pts',(17.8167014103155,-3.33051870318736,
1222.56176470588));
#156664=CARTESIAN_POINT('Ctrl Pts',(17.3590292079831,-4.93906964482095,
1221.06764705882));
#156665=CARTESIAN_POINT('Ctrl Pts',(16.9013570056506,-6.54762058645456,
1219.57352941176));
#156666=CARTESIAN_POINT('Ctrl Pts',(16.1559070823762,-8.04468584505497,
1218.07941176471));
#156667=CARTESIAN_POINT('Ctrl Pts',(15.4104571591017,-9.54175110365538,
1216.58529411765));
#156668=CARTESIAN_POINT('Ctrl Pts',(14.4026149179538,-10.8763499173728,
1215.09117647059));
#156669=CARTESIAN_POINT('Ctrl Pts',(13.3947726768058,-12.2109487310903,
1213.59705882353));
#156670=CARTESIAN_POINT('Ctrl Pts',(12.1588589765331,-13.3376329379985,
1212.10294117647));
#156671=CARTESIAN_POINT('Ctrl Pts',(10.9229452762603,-14.4643171449067,
1210.60882352941));
#156672=CARTESIAN_POINT('Ctrl Pts',(9.50104767561053,-15.3447188656481,
1209.11470588235));
#156673=CARTESIAN_POINT('Ctrl Pts',(8.07915007496071,-16.2251205863895,
1207.62058823529));
#156674=CARTESIAN_POINT('Ctrl Pts',(6.51968959134574,-16.8292587962898,
1206.12647058824));
#156675=CARTESIAN_POINT('Ctrl Pts',(4.96022910773078,-17.4333970061901,
1204.63235294118));
#156676=CARTESIAN_POINT('Ctrl Pts',(3.31631129755346,-17.7406985030951,
1203.13823529412));
#156677=CARTESIAN_POINT('Ctrl Pts',(1.67239348737615,-18.048,1201.64411764706));
#156678=CARTESIAN_POINT('Ctrl Pts',(0.,-18.048,1200.15));
#156679=CARTESIAN_POINT('Ctrl Pts',(-1.67239348737615,-18.048,1198.65588235294));
#156680=CARTESIAN_POINT('Ctrl Pts',(-3.31631129755346,-17.7406985030951,
1197.16176470588));
#156681=CARTESIAN_POINT('Ctrl Pts',(-4.96022910773077,-17.4333970061901,
1195.66764705882));
#156682=CARTESIAN_POINT('Ctrl Pts',(-6.51968959134574,-16.8292587962898,
1194.17352941176));
#156683=CARTESIAN_POINT('Ctrl Pts',(-8.07915007496071,-16.2251205863895,
1192.67941176471));
#156684=CARTESIAN_POINT('Ctrl Pts',(-9.50104767561052,-15.3447188656481,
1191.18529411765));
#156685=CARTESIAN_POINT('Ctrl Pts',(-10.9229452762603,-14.4643171449067,
1189.69117647059));
#156686=CARTESIAN_POINT('Ctrl Pts',(-12.1588589765331,-13.3376329379985,
1188.19705882353));
#156687=CARTESIAN_POINT('Ctrl Pts',(-13.3947726768058,-12.2109487310903,
1186.70294117647));
#156688=CARTESIAN_POINT('Ctrl Pts',(-14.4026149179538,-10.8763499173728,
1185.20882352941));
#156689=CARTESIAN_POINT('Ctrl Pts',(-15.4104571591017,-9.54175110365538,
1183.71470588235));
#156690=CARTESIAN_POINT('Ctrl Pts',(-16.1559070823762,-8.04468584505497,
1182.22058823529));
#156691=CARTESIAN_POINT('Ctrl Pts',(-16.9013570056506,-6.54762058645456,
1180.72647058824));
#156692=CARTESIAN_POINT('Ctrl Pts',(-17.3590292079831,-4.93906964482095,
1179.23235294118));
#156693=CARTESIAN_POINT('Ctrl Pts',(-17.8167014103155,-3.33051870318735,
1177.73823529412));
#156694=CARTESIAN_POINT('Ctrl Pts',(-17.9710104137728,-1.66525935159368,
1176.24411764706));
#156695=CARTESIAN_POINT('Ctrl Pts',(-18.1253194172301,-1.10985572039171E-15,
1174.75));
#156696=CARTESIAN_POINT('Ctrl Pts',(-17.9710104137728,1.66525935159367,
1173.25588235294));
#156697=CARTESIAN_POINT('Ctrl Pts',(-17.8167014103155,3.33051870318735,
1171.76176470588));
#156698=CARTESIAN_POINT('Ctrl Pts',(-17.3590292079831,4.93906964482096,
1170.26764705882));
#156699=CARTESIAN_POINT('Ctrl Pts',(-16.9013570056506,6.54762058645456,
1168.77352941176));
#156700=CARTESIAN_POINT('Ctrl Pts',(-16.1559070823762,8.04468584505497,
1167.27941176471));
#156701=CARTESIAN_POINT('Ctrl Pts',(-15.4104571591017,9.54175110365538,
1165.78529411765));
#156702=CARTESIAN_POINT('Ctrl Pts',(-14.4026149179538,10.8763499173728,
1164.29117647059));
#156703=CARTESIAN_POINT('Ctrl Pts',(-13.3947726768058,12.2109487310903,
1162.79705882353));
#156704=CARTESIAN_POINT('Ctrl Pts',(-12.1588589765331,13.3376329379985,
1161.30294117647));
#156705=CARTESIAN_POINT('Ctrl Pts',(-10.9229452762603,14.4643171449067,
1159.80882352941));
#156706=CARTESIAN_POINT('Ctrl Pts',(-9.50104767561052,15.3447188656481,
1158.31470588235));
#156707=CARTESIAN_POINT('Ctrl Pts',(-8.07915007496071,16.2251205863895,
1156.82058823529));
#156708=CARTESIAN_POINT('Ctrl Pts',(-6.51968959134574,16.8292587962898,
1155.32647058824));
#156709=CARTESIAN_POINT('Ctrl Pts',(-4.96022910773078,17.4333970061901,
1153.83235294118));
#156710=CARTESIAN_POINT('Ctrl Pts',(-3.31631129755346,17.7406985030951,
1152.33823529412));
#156711=CARTESIAN_POINT('Ctrl Pts',(-1.67239348737615,18.048,1150.84411764706));
#156712=CARTESIAN_POINT('Ctrl Pts',(-2.21024254310115E-15,18.048,1149.35));
#156713=CARTESIAN_POINT('Ctrl Pts',(1.67239348737616,18.048,1147.85588235294));
#156714=CARTESIAN_POINT('Ctrl Pts',(3.31631129755346,17.7406985030951,1146.36176470588));
#156715=CARTESIAN_POINT('Ctrl Pts',(4.96022910773077,17.4333970061901,1144.86764705882));
#156716=CARTESIAN_POINT('Ctrl Pts',(6.51968959134575,16.8292587962898,1143.37352941176));
#156717=CARTESIAN_POINT('Ctrl Pts',(8.07915007496071,16.2251205863895,1141.87941176471));
#156718=CARTESIAN_POINT('Ctrl Pts',(9.50104767561053,15.3447188656481,1140.38529411765));
#156719=CARTESIAN_POINT('Ctrl Pts',(10.9229452762603,14.4643171449067,1138.89117647059));
#156720=CARTESIAN_POINT('Ctrl Pts',(12.1588589765331,13.3376329379985,1137.39705882353));
#156721=CARTESIAN_POINT('Ctrl Pts',(13.3947726768058,12.2109487310903,1135.90294117647));
#156722=CARTESIAN_POINT('Ctrl Pts',(14.4026149179538,10.8763499173728,1134.40882352941));
#156723=CARTESIAN_POINT('Ctrl Pts',(15.4104571591017,9.54175110365538,1132.91470588235));
#156724=CARTESIAN_POINT('Ctrl Pts',(16.1559070823762,8.04468584505496,1131.42058823529));
#156725=CARTESIAN_POINT('Ctrl Pts',(16.9013570056506,6.54762058645456,1129.92647058824));
#156726=CARTESIAN_POINT('Ctrl Pts',(17.3590292079831,4.93906964482096,1128.43235294118));
#156727=CARTESIAN_POINT('Ctrl Pts',(17.8167014103155,3.33051870318735,1126.93823529412));
#156728=CARTESIAN_POINT('Ctrl Pts',(17.9710104137728,1.66525935159367,1125.44411764706));
#156729=CARTESIAN_POINT('Ctrl Pts',(18.1253194172301,3.32956716117513E-15,
1123.95));
#156730=CARTESIAN_POINT('Ctrl Pts',(17.9710104137728,-1.66525935159367,
1122.45588235294));
#156731=CARTESIAN_POINT('Ctrl Pts',(17.8167014103155,-3.33051870318736,
1120.96176470588));
#156732=CARTESIAN_POINT('Ctrl Pts',(17.3590292079831,-4.93906964482095,
1119.46764705882));
#156733=CARTESIAN_POINT('Ctrl Pts',(16.9013570056506,-6.54762058645456,
1117.97352941176));
#156734=CARTESIAN_POINT('Ctrl Pts',(16.1559070823762,-8.04468584505497,
1116.47941176471));
#156735=CARTESIAN_POINT('Ctrl Pts',(15.4104571591017,-9.54175110365538,
1114.98529411765));
#156736=CARTESIAN_POINT('Ctrl Pts',(14.4026149179538,-10.8763499173728,
1113.49117647059));
#156737=CARTESIAN_POINT('Ctrl Pts',(13.3947726768058,-12.2109487310903,
1111.99705882353));
#156738=CARTESIAN_POINT('Ctrl Pts',(12.1588589765331,-13.3376329379985,
1110.50294117647));
#156739=CARTESIAN_POINT('Ctrl Pts',(10.9229452762603,-14.4643171449067,
1109.00882352941));
#156740=CARTESIAN_POINT('Ctrl Pts',(9.50104767561053,-15.3447188656481,
1107.51470588235));
#156741=CARTESIAN_POINT('Ctrl Pts',(8.07915007496071,-16.2251205863895,
1106.02058823529));
#156742=CARTESIAN_POINT('Ctrl Pts',(6.51968959134574,-16.8292587962898,
1104.52647058824));
#156743=CARTESIAN_POINT('Ctrl Pts',(4.96022910773078,-17.4333970061901,
1103.03235294118));
#156744=CARTESIAN_POINT('Ctrl Pts',(3.31631129755346,-17.7406985030951,
1101.53823529412));
#156745=CARTESIAN_POINT('Ctrl Pts',(1.67239348737615,-18.048,1100.04411764706));
#156746=CARTESIAN_POINT('Ctrl Pts',(0.,-18.048,1098.55));
#156747=CARTESIAN_POINT('Ctrl Pts',(-1.67239348737615,-18.048,1097.05588235294));
#156748=CARTESIAN_POINT('Ctrl Pts',(-3.31631129755346,-17.7406985030951,
1095.56176470588));
#156749=CARTESIAN_POINT('Ctrl Pts',(-4.96022910773077,-17.4333970061901,
1094.06764705882));
#156750=CARTESIAN_POINT('Ctrl Pts',(-6.51968959134574,-16.8292587962898,
1092.57352941176));
#156751=CARTESIAN_POINT('Ctrl Pts',(-8.07915007496071,-16.2251205863895,
1091.07941176471));
#156752=CARTESIAN_POINT('Ctrl Pts',(-9.50104767561052,-15.3447188656481,
1089.58529411765));
#156753=CARTESIAN_POINT('Ctrl Pts',(-10.9229452762603,-14.4643171449067,
1088.09117647059));
#156754=CARTESIAN_POINT('Ctrl Pts',(-12.1588589765331,-13.3376329379985,
1086.59705882353));
#156755=CARTESIAN_POINT('Ctrl Pts',(-13.3947726768058,-12.2109487310903,
1085.10294117647));
#156756=CARTESIAN_POINT('Ctrl Pts',(-14.4026149179538,-10.8763499173728,
1083.60882352941));
#156757=CARTESIAN_POINT('Ctrl Pts',(-15.4104571591017,-9.54175110365538,
1082.11470588235));
#156758=CARTESIAN_POINT('Ctrl Pts',(-16.1559070823762,-8.04468584505497,
1080.62058823529));
#156759=CARTESIAN_POINT('Ctrl Pts',(-16.9013570056506,-6.54762058645456,
1079.12647058824));
#156760=CARTESIAN_POINT('Ctrl Pts',(-17.3590292079831,-4.93906964482095,
1077.63235294118));
#156761=CARTESIAN_POINT('Ctrl Pts',(-17.8167014103155,-3.33051870318735,
1076.13823529412));
#156762=CARTESIAN_POINT('Ctrl Pts',(-17.9710104137728,-1.66525935159368,
1074.64411764706));
#156763=CARTESIAN_POINT('Ctrl Pts',(-18.1253194172301,-1.10985572039171E-15,
1073.15));
#156764=CARTESIAN_POINT('Ctrl Pts',(-17.9710104137728,1.66525935159367,
1071.65588235294));
#156765=CARTESIAN_POINT('Ctrl Pts',(-17.8167014103155,3.33051870318735,
1070.16176470588));
#156766=CARTESIAN_POINT('Ctrl Pts',(-17.3590292079831,4.93906964482096,
1068.66764705882));
#156767=CARTESIAN_POINT('Ctrl Pts',(-16.9013570056506,6.54762058645456,
1067.17352941176));
#156768=CARTESIAN_POINT('Ctrl Pts',(-16.1559070823762,8.04468584505497,
1065.67941176471));
#156769=CARTESIAN_POINT('Ctrl Pts',(-15.4104571591017,9.54175110365538,
1064.18529411765));
#156770=CARTESIAN_POINT('Ctrl Pts',(-14.4026149179538,10.8763499173728,
1062.69117647059));
#156771=CARTESIAN_POINT('Ctrl Pts',(-13.3947726768058,12.2109487310903,
1061.19705882353));
#156772=CARTESIAN_POINT('Ctrl Pts',(-12.1588589765331,13.3376329379985,
1059.70294117647));
#156773=CARTESIAN_POINT('Ctrl Pts',(-10.9229452762603,14.4643171449067,
1058.20882352941));
#156774=CARTESIAN_POINT('Ctrl Pts',(-9.50104767561052,15.3447188656481,
1056.71470588235));
#156775=CARTESIAN_POINT('Ctrl Pts',(-8.07915007496071,16.2251205863895,
1055.22058823529));
#156776=CARTESIAN_POINT('Ctrl Pts',(-6.51968959134574,16.8292587962898,
1053.72647058824));
#156777=CARTESIAN_POINT('Ctrl Pts',(-4.96022910773078,17.4333970061901,
1052.23235294118));
#156778=CARTESIAN_POINT('Ctrl Pts',(-3.31631129755346,17.7406985030951,
1050.73823529412));
#156779=CARTESIAN_POINT('Ctrl Pts',(-1.67239348737615,18.048,1049.24411764706));
#156780=CARTESIAN_POINT('Ctrl Pts',(-2.21024254310115E-15,18.048,1047.75));
#156781=CARTESIAN_POINT('Ctrl Pts',(1.67239348737616,18.048,1046.25588235294));
#156782=CARTESIAN_POINT('Ctrl Pts',(3.31631129755346,17.7406985030951,1044.76176470588));
#156783=CARTESIAN_POINT('Ctrl Pts',(4.96022910773077,17.4333970061901,1043.26764705882));
#156784=CARTESIAN_POINT('Ctrl Pts',(6.51968959134575,16.8292587962898,1041.77352941176));
#156785=CARTESIAN_POINT('Ctrl Pts',(8.07915007496071,16.2251205863895,1040.27941176471));
#156786=CARTESIAN_POINT('Ctrl Pts',(9.50104767561053,15.3447188656481,1038.78529411765));
#156787=CARTESIAN_POINT('Ctrl Pts',(10.9229452762603,14.4643171449067,1037.29117647059));
#156788=CARTESIAN_POINT('Ctrl Pts',(12.1588589765331,13.3376329379985,1035.79705882353));
#156789=CARTESIAN_POINT('Ctrl Pts',(13.3947726768058,12.2109487310903,1034.30294117647));
#156790=CARTESIAN_POINT('Ctrl Pts',(14.4026149179538,10.8763499173728,1032.80882352941));
#156791=CARTESIAN_POINT('Ctrl Pts',(15.4104571591017,9.54175110365538,1031.31470588235));
#156792=CARTESIAN_POINT('Ctrl Pts',(16.1559070823762,8.04468584505496,1029.82058823529));
#156793=CARTESIAN_POINT('Ctrl Pts',(16.9013570056506,6.54762058645456,1028.32647058824));
#156794=CARTESIAN_POINT('Ctrl Pts',(17.3590292079831,4.93906964482096,1026.83235294118));
#156795=CARTESIAN_POINT('Ctrl Pts',(17.8167014103155,3.33051870318735,1025.33823529412));
#156796=CARTESIAN_POINT('Ctrl Pts',(17.9710104137728,1.66525935159367,1023.84411764706));
#156797=CARTESIAN_POINT('Ctrl Pts',(18.1253194172301,3.32956716117513E-15,
1022.35));
#156798=CARTESIAN_POINT('Ctrl Pts',(17.9710104137728,-1.66525935159367,
1020.85588235294));
#156799=CARTESIAN_POINT('Ctrl Pts',(17.8167014103155,-3.33051870318736,
1019.36176470588));
#156800=CARTESIAN_POINT('Ctrl Pts',(17.3590292079831,-4.93906964482095,
1017.86764705882));
#156801=CARTESIAN_POINT('Ctrl Pts',(16.9013570056506,-6.54762058645456,
1016.37352941176));
#156802=CARTESIAN_POINT('Ctrl Pts',(16.1559070823762,-8.04468584505497,
1014.87941176471));
#156803=CARTESIAN_POINT('Ctrl Pts',(15.4104571591017,-9.54175110365538,
1013.38529411765));
#156804=CARTESIAN_POINT('Ctrl Pts',(14.4026149179538,-10.8763499173728,
1011.89117647059));
#156805=CARTESIAN_POINT('Ctrl Pts',(13.3947726768058,-12.2109487310903,
1010.39705882353));
#156806=CARTESIAN_POINT('Ctrl Pts',(12.1588589765331,-13.3376329379985,
1008.90294117647));
#156807=CARTESIAN_POINT('Ctrl Pts',(10.9229452762603,-14.4643171449067,
1007.40882352941));
#156808=CARTESIAN_POINT('Ctrl Pts',(9.50104767561053,-15.3447188656481,
1005.91470588235));
#156809=CARTESIAN_POINT('Ctrl Pts',(8.07915007496071,-16.2251205863895,
1004.42058823529));
#156810=CARTESIAN_POINT('Ctrl Pts',(6.51968959134574,-16.8292587962898,
1002.92647058824));
#156811=CARTESIAN_POINT('Ctrl Pts',(4.96022910773078,-17.4333970061901,
1001.43235294118));
#156812=CARTESIAN_POINT('Ctrl Pts',(3.31631129755346,-17.7406985030951,
999.938235294118));
#156813=CARTESIAN_POINT('Ctrl Pts',(1.67239348737615,-18.048,998.444117647059));
#156814=CARTESIAN_POINT('Ctrl Pts',(0.,-18.048,996.95));
#156815=CARTESIAN_POINT('Ctrl Pts',(-1.67239348737615,-18.048,995.455882352941));
#156816=CARTESIAN_POINT('Ctrl Pts',(-3.31631129755346,-17.7406985030951,
993.961764705882));
#156817=CARTESIAN_POINT('Ctrl Pts',(-4.96022910773077,-17.4333970061901,
992.467647058824));
#156818=CARTESIAN_POINT('Ctrl Pts',(-6.51968959134574,-16.8292587962898,
990.973529411765));
#156819=CARTESIAN_POINT('Ctrl Pts',(-8.07915007496071,-16.2251205863895,
989.479411764706));
#156820=CARTESIAN_POINT('Ctrl Pts',(-9.50104767561052,-15.3447188656481,
987.985294117647));
#156821=CARTESIAN_POINT('Ctrl Pts',(-10.9229452762603,-14.4643171449067,
986.491176470588));
#156822=CARTESIAN_POINT('Ctrl Pts',(-12.1588589765331,-13.3376329379985,
984.997058823529));
#156823=CARTESIAN_POINT('Ctrl Pts',(-13.3947726768058,-12.2109487310903,
983.502941176471));
#156824=CARTESIAN_POINT('Ctrl Pts',(-14.4026149179538,-10.8763499173728,
982.008823529412));
#156825=CARTESIAN_POINT('Ctrl Pts',(-15.4104571591017,-9.54175110365538,
980.514705882353));
#156826=CARTESIAN_POINT('Ctrl Pts',(-16.1559070823762,-8.04468584505497,
979.020588235294));
#156827=CARTESIAN_POINT('Ctrl Pts',(-16.9013570056506,-6.54762058645456,
977.526470588235));
#156828=CARTESIAN_POINT('Ctrl Pts',(-17.3590292079831,-4.93906964482095,
976.032352941177));
#156829=CARTESIAN_POINT('Ctrl Pts',(-17.8167014103155,-3.33051870318735,
974.538235294118));
#156830=CARTESIAN_POINT('Ctrl Pts',(-17.9710104137728,-1.66525935159368,
973.044117647059));
#156831=CARTESIAN_POINT('Ctrl Pts',(-18.1253194172301,-1.10985572039171E-15,
971.55));
#156832=CARTESIAN_POINT('Ctrl Pts',(-17.9710104137728,1.66525935159367,
970.055882352941));
#156833=CARTESIAN_POINT('Ctrl Pts',(-17.8167014103155,3.33051870318735,
968.561764705882));
#156834=CARTESIAN_POINT('Ctrl Pts',(-17.3590292079831,4.93906964482096,
967.067647058824));
#156835=CARTESIAN_POINT('Ctrl Pts',(-16.9013570056506,6.54762058645456,
965.573529411765));
#156836=CARTESIAN_POINT('Ctrl Pts',(-16.1559070823762,8.04468584505497,
964.079411764706));
#156837=CARTESIAN_POINT('Ctrl Pts',(-15.4104571591017,9.54175110365538,
962.585294117647));
#156838=CARTESIAN_POINT('Ctrl Pts',(-14.4026149179538,10.8763499173728,
961.091176470588));
#156839=CARTESIAN_POINT('Ctrl Pts',(-13.3947726768058,12.2109487310903,
959.59705882353));
#156840=CARTESIAN_POINT('Ctrl Pts',(-12.1588589765331,13.3376329379985,
958.102941176471));
#156841=CARTESIAN_POINT('Ctrl Pts',(-10.9229452762603,14.4643171449067,
956.608823529412));
#156842=CARTESIAN_POINT('Ctrl Pts',(-9.50104767561052,15.3447188656481,
955.114705882353));
#156843=CARTESIAN_POINT('Ctrl Pts',(-8.07915007496071,16.2251205863895,
953.620588235294));
#156844=CARTESIAN_POINT('Ctrl Pts',(-6.51968959134574,16.8292587962898,
952.126470588235));
#156845=CARTESIAN_POINT('Ctrl Pts',(-4.96022910773078,17.4333970061901,
950.632352941177));
#156846=CARTESIAN_POINT('Ctrl Pts',(-3.31631129755346,17.7406985030951,
949.138235294118));
#156847=CARTESIAN_POINT('Ctrl Pts',(-1.67239348737615,18.048,947.644117647059));
#156848=CARTESIAN_POINT('Ctrl Pts',(-2.21024254310115E-15,18.048,946.15));
#156849=CARTESIAN_POINT('Ctrl Pts',(1.67239348737616,18.048,944.655882352941));
#156850=CARTESIAN_POINT('Ctrl Pts',(3.31631129755346,17.7406985030951,943.161764705882));
#156851=CARTESIAN_POINT('Ctrl Pts',(4.96022910773077,17.4333970061901,941.667647058824));
#156852=CARTESIAN_POINT('Ctrl Pts',(6.51968959134575,16.8292587962898,940.173529411765));
#156853=CARTESIAN_POINT('Ctrl Pts',(8.07915007496071,16.2251205863895,938.679411764706));
#156854=CARTESIAN_POINT('Ctrl Pts',(9.50104767561053,15.3447188656481,937.185294117647));
#156855=CARTESIAN_POINT('Ctrl Pts',(10.9229452762603,14.4643171449067,935.691176470589));
#156856=CARTESIAN_POINT('Ctrl Pts',(12.1588589765331,13.3376329379985,934.19705882353));
#156857=CARTESIAN_POINT('Ctrl Pts',(13.3947726768058,12.2109487310903,932.702941176471));
#156858=CARTESIAN_POINT('Ctrl Pts',(14.4026149179538,10.8763499173728,931.208823529412));
#156859=CARTESIAN_POINT('Ctrl Pts',(15.4104571591017,9.54175110365538,929.714705882353));
#156860=CARTESIAN_POINT('Ctrl Pts',(16.1559070823762,8.04468584505496,928.220588235294));
#156861=CARTESIAN_POINT('Ctrl Pts',(16.9013570056506,6.54762058645456,926.726470588235));
#156862=CARTESIAN_POINT('Ctrl Pts',(17.3590292079831,4.93906964482096,925.232352941176));
#156863=CARTESIAN_POINT('Ctrl Pts',(17.8167014103155,3.33051870318735,923.738235294118));
#156864=CARTESIAN_POINT('Ctrl Pts',(17.9710104137728,1.66525935159367,922.244117647059));
#156865=CARTESIAN_POINT('Ctrl Pts',(18.1253194172301,3.32956716117513E-15,
920.75));
#156866=CARTESIAN_POINT('Ctrl Pts',(17.9710104137728,-1.66525935159367,
919.255882352941));
#156867=CARTESIAN_POINT('Ctrl Pts',(17.8167014103155,-3.33051870318736,
917.761764705882));
#156868=CARTESIAN_POINT('Ctrl Pts',(17.3590292079831,-4.93906964482095,
916.267647058824));
#156869=CARTESIAN_POINT('Ctrl Pts',(16.9013570056506,-6.54762058645456,
914.773529411765));
#156870=CARTESIAN_POINT('Ctrl Pts',(16.1559070823762,-8.04468584505497,
913.279411764706));
#156871=CARTESIAN_POINT('Ctrl Pts',(15.4104571591017,-9.54175110365538,
911.785294117647));
#156872=CARTESIAN_POINT('Ctrl Pts',(14.4026149179538,-10.8763499173728,
910.291176470588));
#156873=CARTESIAN_POINT('Ctrl Pts',(13.3947726768058,-12.2109487310903,
908.797058823529));
#156874=CARTESIAN_POINT('Ctrl Pts',(12.1588589765331,-13.3376329379985,
907.302941176471));
#156875=CARTESIAN_POINT('Ctrl Pts',(10.9229452762603,-14.4643171449067,
905.808823529412));
#156876=CARTESIAN_POINT('Ctrl Pts',(9.50104767561053,-15.3447188656481,
904.314705882353));
#156877=CARTESIAN_POINT('Ctrl Pts',(8.07915007496071,-16.2251205863895,
902.820588235294));
#156878=CARTESIAN_POINT('Ctrl Pts',(6.51968959134574,-16.8292587962898,
901.326470588235));
#156879=CARTESIAN_POINT('Ctrl Pts',(4.96022910773078,-17.4333970061901,
899.832352941177));
#156880=CARTESIAN_POINT('Ctrl Pts',(3.31631129755346,-17.7406985030951,
898.338235294118));
#156881=CARTESIAN_POINT('Ctrl Pts',(1.67239348737615,-18.048,896.844117647059));
#156882=CARTESIAN_POINT('Ctrl Pts',(0.,-18.048,895.35));
#156883=CARTESIAN_POINT('Ctrl Pts',(-1.67239348737615,-18.048,893.855882352941));
#156884=CARTESIAN_POINT('Ctrl Pts',(-3.31631129755346,-17.7406985030951,
892.361764705882));
#156885=CARTESIAN_POINT('Ctrl Pts',(-4.96022910773077,-17.4333970061901,
890.867647058824));
#156886=CARTESIAN_POINT('Ctrl Pts',(-6.51968959134574,-16.8292587962898,
889.373529411765));
#156887=CARTESIAN_POINT('Ctrl Pts',(-8.07915007496071,-16.2251205863895,
887.879411764706));
#156888=CARTESIAN_POINT('Ctrl Pts',(-9.50104767561052,-15.3447188656481,
886.385294117647));
#156889=CARTESIAN_POINT('Ctrl Pts',(-10.9229452762603,-14.4643171449067,
884.891176470588));
#156890=CARTESIAN_POINT('Ctrl Pts',(-12.1588589765331,-13.3376329379985,
883.39705882353));
#156891=CARTESIAN_POINT('Ctrl Pts',(-13.3947726768058,-12.2109487310903,
881.902941176471));
#156892=CARTESIAN_POINT('Ctrl Pts',(-14.4026149179538,-10.8763499173728,
880.408823529412));
#156893=CARTESIAN_POINT('Ctrl Pts',(-15.4104571591017,-9.54175110365538,
878.914705882353));
#156894=CARTESIAN_POINT('Ctrl Pts',(-16.1559070823762,-8.04468584505497,
877.420588235294));
#156895=CARTESIAN_POINT('Ctrl Pts',(-16.9013570056506,-6.54762058645456,
875.926470588235));
#156896=CARTESIAN_POINT('Ctrl Pts',(-17.3590292079831,-4.93906964482095,
874.432352941177));
#156897=CARTESIAN_POINT('Ctrl Pts',(-17.8167014103155,-3.33051870318735,
872.938235294118));
#156898=CARTESIAN_POINT('Ctrl Pts',(-17.9710104137728,-1.66525935159368,
871.444117647059));
#156899=CARTESIAN_POINT('Ctrl Pts',(-18.1253194172301,-1.10985572039171E-15,
869.95));
#156900=CARTESIAN_POINT('Ctrl Pts',(-17.9710104137728,1.66525935159367,
868.455882352941));
#156901=CARTESIAN_POINT('Ctrl Pts',(-17.8167014103155,3.33051870318735,
866.961764705882));
#156902=CARTESIAN_POINT('Ctrl Pts',(-17.3590292079831,4.93906964482096,
865.467647058824));
#156903=CARTESIAN_POINT('Ctrl Pts',(-16.9013570056506,6.54762058645456,
863.973529411765));
#156904=CARTESIAN_POINT('Ctrl Pts',(-16.1559070823762,8.04468584505497,
862.479411764706));
#156905=CARTESIAN_POINT('Ctrl Pts',(-15.4104571591017,9.54175110365538,
860.985294117647));
#156906=CARTESIAN_POINT('Ctrl Pts',(-14.4026149179538,10.8763499173728,
859.491176470588));
#156907=CARTESIAN_POINT('Ctrl Pts',(-13.3947726768058,12.2109487310903,
857.997058823529));
#156908=CARTESIAN_POINT('Ctrl Pts',(-12.1588589765331,13.3376329379985,
856.502941176471));
#156909=CARTESIAN_POINT('Ctrl Pts',(-10.9229452762603,14.4643171449067,
855.008823529412));
#156910=CARTESIAN_POINT('Ctrl Pts',(-9.50104767561052,15.3447188656481,
853.514705882353));
#156911=CARTESIAN_POINT('Ctrl Pts',(-8.07915007496071,16.2251205863895,
852.020588235294));
#156912=CARTESIAN_POINT('Ctrl Pts',(-6.51968959134574,16.8292587962898,
850.526470588235));
#156913=CARTESIAN_POINT('Ctrl Pts',(-4.96022910773078,17.4333970061901,
849.032352941177));
#156914=CARTESIAN_POINT('Ctrl Pts',(-3.31631129755346,17.7406985030951,
847.538235294118));
#156915=CARTESIAN_POINT('Ctrl Pts',(-1.67239348737615,18.048,846.044117647059));
#156916=CARTESIAN_POINT('Ctrl Pts',(-2.21024254310115E-15,18.048,844.55));
#156917=CARTESIAN_POINT('Ctrl Pts',(1.67239348737616,18.048,843.055882352941));
#156918=CARTESIAN_POINT('Ctrl Pts',(3.31631129755346,17.7406985030951,841.561764705883));
#156919=CARTESIAN_POINT('Ctrl Pts',(4.96022910773077,17.4333970061901,840.067647058824));
#156920=CARTESIAN_POINT('Ctrl Pts',(6.51968959134575,16.8292587962898,838.573529411765));
#156921=CARTESIAN_POINT('Ctrl Pts',(8.07915007496071,16.2251205863895,837.079411764706));
#156922=CARTESIAN_POINT('Ctrl Pts',(9.50104767561053,15.3447188656481,835.585294117647));
#156923=CARTESIAN_POINT('Ctrl Pts',(10.9229452762603,14.4643171449067,834.091176470588));
#156924=CARTESIAN_POINT('Ctrl Pts',(12.1588589765331,13.3376329379985,832.597058823529));
#156925=CARTESIAN_POINT('Ctrl Pts',(13.3947726768058,12.2109487310903,831.102941176471));
#156926=CARTESIAN_POINT('Ctrl Pts',(14.4026149179538,10.8763499173728,829.608823529412));
#156927=CARTESIAN_POINT('Ctrl Pts',(15.4104571591017,9.54175110365538,828.114705882353));
#156928=CARTESIAN_POINT('Ctrl Pts',(16.1559070823762,8.04468584505496,826.620588235294));
#156929=CARTESIAN_POINT('Ctrl Pts',(16.9013570056506,6.54762058645456,825.126470588235));
#156930=CARTESIAN_POINT('Ctrl Pts',(17.3590292079831,4.93906964482096,823.632352941177));
#156931=CARTESIAN_POINT('Ctrl Pts',(17.8167014103155,3.33051870318735,822.138235294118));
#156932=CARTESIAN_POINT('Ctrl Pts',(17.9710104137728,1.66525935159367,820.644117647059));
#156933=CARTESIAN_POINT('Ctrl Pts',(18.1253194172301,3.32956716117513E-15,
819.15));
#156934=CARTESIAN_POINT('Ctrl Pts',(17.9710104137728,-1.66525935159367,
817.655882352941));
#156935=CARTESIAN_POINT('Ctrl Pts',(17.8167014103155,-3.33051870318736,
816.161764705882));
#156936=CARTESIAN_POINT('Ctrl Pts',(17.3590292079831,-4.93906964482095,
814.667647058824));
#156937=CARTESIAN_POINT('Ctrl Pts',(16.9013570056506,-6.54762058645456,
813.173529411765));
#156938=CARTESIAN_POINT('Ctrl Pts',(16.1559070823762,-8.04468584505497,
811.679411764706));
#156939=CARTESIAN_POINT('Ctrl Pts',(15.4104571591017,-9.54175110365538,
810.185294117647));
#156940=CARTESIAN_POINT('Ctrl Pts',(14.4026149179538,-10.8763499173728,
808.691176470588));
#156941=CARTESIAN_POINT('Ctrl Pts',(13.3947726768058,-12.2109487310903,
807.197058823529));
#156942=CARTESIAN_POINT('Ctrl Pts',(12.1588589765331,-13.3376329379985,
805.702941176471));
#156943=CARTESIAN_POINT('Ctrl Pts',(10.9229452762603,-14.4643171449067,
804.208823529412));
#156944=CARTESIAN_POINT('Ctrl Pts',(9.50104767561053,-15.3447188656481,
802.714705882353));
#156945=CARTESIAN_POINT('Ctrl Pts',(8.07915007496071,-16.2251205863895,
801.220588235294));
#156946=CARTESIAN_POINT('Ctrl Pts',(6.51968959134574,-16.8292587962898,
799.726470588235));
#156947=CARTESIAN_POINT('Ctrl Pts',(4.96022910773078,-17.4333970061901,
798.232352941176));
#156948=CARTESIAN_POINT('Ctrl Pts',(3.31631129755346,-17.7406985030951,
796.738235294118));
#156949=CARTESIAN_POINT('Ctrl Pts',(1.67239348737615,-18.048,795.244117647059));
#156950=CARTESIAN_POINT('Ctrl Pts',(0.,-18.048,793.75));
#156951=CARTESIAN_POINT('Ctrl Pts',(-1.67239348737615,-18.048,792.255882352941));
#156952=CARTESIAN_POINT('Ctrl Pts',(-3.31631129755346,-17.7406985030951,
790.761764705882));
#156953=CARTESIAN_POINT('Ctrl Pts',(-4.96022910773077,-17.4333970061901,
789.267647058824));
#156954=CARTESIAN_POINT('Ctrl Pts',(-6.51968959134574,-16.8292587962898,
787.773529411765));
#156955=CARTESIAN_POINT('Ctrl Pts',(-8.07915007496071,-16.2251205863895,
786.279411764706));
#156956=CARTESIAN_POINT('Ctrl Pts',(-9.50104767561052,-15.3447188656481,
784.785294117647));
#156957=CARTESIAN_POINT('Ctrl Pts',(-10.9229452762603,-14.4643171449067,
783.291176470588));
#156958=CARTESIAN_POINT('Ctrl Pts',(-12.1588589765331,-13.3376329379985,
781.797058823529));
#156959=CARTESIAN_POINT('Ctrl Pts',(-13.3947726768058,-12.2109487310903,
780.302941176471));
#156960=CARTESIAN_POINT('Ctrl Pts',(-14.4026149179538,-10.8763499173728,
778.808823529412));
#156961=CARTESIAN_POINT('Ctrl Pts',(-15.4104571591017,-9.54175110365538,
777.314705882353));
#156962=CARTESIAN_POINT('Ctrl Pts',(-16.1559070823762,-8.04468584505497,
775.820588235294));
#156963=CARTESIAN_POINT('Ctrl Pts',(-16.9013570056506,-6.54762058645456,
774.326470588235));
#156964=CARTESIAN_POINT('Ctrl Pts',(-17.3590292079831,-4.93906964482095,
772.832352941177));
#156965=CARTESIAN_POINT('Ctrl Pts',(-17.8167014103155,-3.33051870318735,
771.338235294118));
#156966=CARTESIAN_POINT('Ctrl Pts',(-17.9710104137728,-1.66525935159368,
769.844117647059));
#156967=CARTESIAN_POINT('Ctrl Pts',(-18.1253194172301,-1.10985572039171E-15,
768.35));
#156968=CARTESIAN_POINT('Ctrl Pts',(-17.9710104137728,1.66525935159367,
766.855882352941));
#156969=CARTESIAN_POINT('Ctrl Pts',(-17.8167014103155,3.33051870318735,
765.361764705882));
#156970=CARTESIAN_POINT('Ctrl Pts',(-17.3590292079831,4.93906964482096,
763.867647058824));
#156971=CARTESIAN_POINT('Ctrl Pts',(-16.9013570056506,6.54762058645456,
762.373529411765));
#156972=CARTESIAN_POINT('Ctrl Pts',(-16.1559070823762,8.04468584505497,
760.879411764706));
#156973=CARTESIAN_POINT('Ctrl Pts',(-15.4104571591017,9.54175110365538,
759.385294117647));
#156974=CARTESIAN_POINT('Ctrl Pts',(-14.4026149179538,10.8763499173728,
757.891176470588));
#156975=CARTESIAN_POINT('Ctrl Pts',(-13.3947726768058,12.2109487310903,
756.397058823529));
#156976=CARTESIAN_POINT('Ctrl Pts',(-12.1588589765331,13.3376329379985,
754.902941176471));
#156977=CARTESIAN_POINT('Ctrl Pts',(-10.9229452762603,14.4643171449067,
753.408823529412));
#156978=CARTESIAN_POINT('Ctrl Pts',(-9.50104767561052,15.3447188656481,
751.914705882353));
#156979=CARTESIAN_POINT('Ctrl Pts',(-8.07915007496071,16.2251205863895,
750.420588235294));
#156980=CARTESIAN_POINT('Ctrl Pts',(-6.51968959134574,16.8292587962898,
748.926470588235));
#156981=CARTESIAN_POINT('Ctrl Pts',(-4.96022910773078,17.4333970061901,
747.432352941176));
#156982=CARTESIAN_POINT('Ctrl Pts',(-3.31631129755346,17.7406985030951,
745.938235294118));
#156983=CARTESIAN_POINT('Ctrl Pts',(-1.67239348737615,18.048,744.444117647059));
#156984=CARTESIAN_POINT('Ctrl Pts',(-2.21024254310115E-15,18.048,742.95));
#156985=CARTESIAN_POINT('Ctrl Pts',(1.67239348737616,18.048,741.455882352941));
#156986=CARTESIAN_POINT('Ctrl Pts',(3.31631129755346,17.7406985030951,739.961764705882));
#156987=CARTESIAN_POINT('Ctrl Pts',(4.96022910773077,17.4333970061901,738.467647058824));
#156988=CARTESIAN_POINT('Ctrl Pts',(6.51968959134575,16.8292587962898,736.973529411765));
#156989=CARTESIAN_POINT('Ctrl Pts',(8.07915007496071,16.2251205863895,735.479411764706));
#156990=CARTESIAN_POINT('Ctrl Pts',(9.50104767561053,15.3447188656481,733.985294117647));
#156991=CARTESIAN_POINT('Ctrl Pts',(10.9229452762603,14.4643171449067,732.491176470588));
#156992=CARTESIAN_POINT('Ctrl Pts',(12.1588589765331,13.3376329379985,730.99705882353));
#156993=CARTESIAN_POINT('Ctrl Pts',(13.3947726768058,12.2109487310903,729.502941176471));
#156994=CARTESIAN_POINT('Ctrl Pts',(14.4026149179538,10.8763499173728,728.008823529412));
#156995=CARTESIAN_POINT('Ctrl Pts',(15.4104571591017,9.54175110365538,726.514705882353));
#156996=CARTESIAN_POINT('Ctrl Pts',(16.1559070823762,8.04468584505496,725.020588235294));
#156997=CARTESIAN_POINT('Ctrl Pts',(16.9013570056506,6.54762058645456,723.526470588235));
#156998=CARTESIAN_POINT('Ctrl Pts',(17.3590292079831,4.93906964482096,722.032352941177));
#156999=CARTESIAN_POINT('Ctrl Pts',(17.8167014103155,3.33051870318735,720.538235294118));
#157000=CARTESIAN_POINT('Ctrl Pts',(17.9710104137728,1.66525935159367,719.044117647059));
#157001=CARTESIAN_POINT('Ctrl Pts',(18.1253194172301,3.32956716117513E-15,
717.55));
#157002=CARTESIAN_POINT('Ctrl Pts',(17.9710104137728,-1.66525935159367,
716.055882352941));
#157003=CARTESIAN_POINT('Ctrl Pts',(17.8167014103155,-3.33051870318736,
714.561764705882));
#157004=CARTESIAN_POINT('Ctrl Pts',(17.3590292079831,-4.93906964482095,
713.067647058824));
#157005=CARTESIAN_POINT('Ctrl Pts',(16.9013570056506,-6.54762058645456,
711.573529411765));
#157006=CARTESIAN_POINT('Ctrl Pts',(16.1559070823762,-8.04468584505497,
710.079411764706));
#157007=CARTESIAN_POINT('Ctrl Pts',(15.4104571591017,-9.54175110365538,
708.585294117647));
#157008=CARTESIAN_POINT('Ctrl Pts',(14.4026149179538,-10.8763499173728,
707.091176470588));
#157009=CARTESIAN_POINT('Ctrl Pts',(13.3947726768058,-12.2109487310903,
705.597058823529));
#157010=CARTESIAN_POINT('Ctrl Pts',(12.1588589765331,-13.3376329379985,
704.102941176471));
#157011=CARTESIAN_POINT('Ctrl Pts',(10.9229452762603,-14.4643171449067,
702.608823529412));
#157012=CARTESIAN_POINT('Ctrl Pts',(9.50104767561053,-15.3447188656481,
701.114705882353));
#157013=CARTESIAN_POINT('Ctrl Pts',(8.07915007496071,-16.2251205863895,
699.620588235294));
#157014=CARTESIAN_POINT('Ctrl Pts',(6.51968959134574,-16.8292587962898,
698.126470588235));
#157015=CARTESIAN_POINT('Ctrl Pts',(4.96022910773078,-17.4333970061901,
696.632352941177));
#157016=CARTESIAN_POINT('Ctrl Pts',(3.31631129755346,-17.7406985030951,
695.138235294118));
#157017=CARTESIAN_POINT('Ctrl Pts',(1.67239348737615,-18.048,693.644117647059));
#157018=CARTESIAN_POINT('Ctrl Pts',(0.,-18.048,692.15));
#157019=CARTESIAN_POINT('Ctrl Pts',(-1.67239348737615,-18.048,690.655882352941));
#157020=CARTESIAN_POINT('Ctrl Pts',(-3.31631129755346,-17.7406985030951,
689.161764705882));
#157021=CARTESIAN_POINT('Ctrl Pts',(-4.96022910773077,-17.4333970061901,
687.667647058824));
#157022=CARTESIAN_POINT('Ctrl Pts',(-6.51968959134574,-16.8292587962898,
686.173529411765));
#157023=CARTESIAN_POINT('Ctrl Pts',(-8.07915007496071,-16.2251205863895,
684.679411764706));
#157024=CARTESIAN_POINT('Ctrl Pts',(-9.50104767561052,-15.3447188656481,
683.185294117647));
#157025=CARTESIAN_POINT('Ctrl Pts',(-10.9229452762603,-14.4643171449067,
681.691176470588));
#157026=CARTESIAN_POINT('Ctrl Pts',(-12.1588589765331,-13.3376329379985,
680.197058823529));
#157027=CARTESIAN_POINT('Ctrl Pts',(-13.3947726768058,-12.2109487310903,
678.702941176471));
#157028=CARTESIAN_POINT('Ctrl Pts',(-14.4026149179538,-10.8763499173728,
677.208823529412));
#157029=CARTESIAN_POINT('Ctrl Pts',(-15.4104571591017,-9.54175110365538,
675.714705882353));
#157030=CARTESIAN_POINT('Ctrl Pts',(-16.1559070823762,-8.04468584505497,
674.220588235294));
#157031=CARTESIAN_POINT('Ctrl Pts',(-16.9013570056506,-6.54762058645456,
672.726470588236));
#157032=CARTESIAN_POINT('Ctrl Pts',(-17.3590292079831,-4.93906964482095,
671.232352941176));
#157033=CARTESIAN_POINT('Ctrl Pts',(-17.8167014103155,-3.33051870318735,
669.738235294118));
#157034=CARTESIAN_POINT('Ctrl Pts',(-17.9710104137728,-1.66525935159368,
668.244117647059));
#157035=CARTESIAN_POINT('Ctrl Pts',(-18.1253194172301,-1.10985572039171E-15,
666.75));
#157036=CARTESIAN_POINT('Ctrl Pts',(-17.9710104137728,1.66525935159367,
665.255882352941));
#157037=CARTESIAN_POINT('Ctrl Pts',(-17.8167014103155,3.33051870318735,
663.761764705882));
#157038=CARTESIAN_POINT('Ctrl Pts',(-17.3590292079831,4.93906964482096,
662.267647058824));
#157039=CARTESIAN_POINT('Ctrl Pts',(-16.9013570056506,6.54762058645456,
660.773529411765));
#157040=CARTESIAN_POINT('Ctrl Pts',(-16.1559070823762,8.04468584505497,
659.279411764706));
#157041=CARTESIAN_POINT('Ctrl Pts',(-15.4104571591017,9.54175110365538,
657.785294117647));
#157042=CARTESIAN_POINT('Ctrl Pts',(-14.4026149179538,10.8763499173728,
656.291176470588));
#157043=CARTESIAN_POINT('Ctrl Pts',(-13.3947726768058,12.2109487310903,
654.797058823529));
#157044=CARTESIAN_POINT('Ctrl Pts',(-12.1588589765331,13.3376329379985,
653.302941176471));
#157045=CARTESIAN_POINT('Ctrl Pts',(-10.9229452762603,14.4643171449067,
651.808823529412));
#157046=CARTESIAN_POINT('Ctrl Pts',(-9.50104767561052,15.3447188656481,
650.314705882353));
#157047=CARTESIAN_POINT('Ctrl Pts',(-8.07915007496071,16.2251205863895,
648.820588235294));
#157048=CARTESIAN_POINT('Ctrl Pts',(-6.51968959134574,16.8292587962898,
647.326470588235));
#157049=CARTESIAN_POINT('Ctrl Pts',(-4.96022910773078,17.4333970061901,
645.832352941176));
#157050=CARTESIAN_POINT('Ctrl Pts',(-3.31631129755346,17.7406985030951,
644.338235294118));
#157051=CARTESIAN_POINT('Ctrl Pts',(-1.67239348737615,18.048,642.844117647059));
#157052=CARTESIAN_POINT('Ctrl Pts',(-2.21024254310115E-15,18.048,641.35));
#157053=CARTESIAN_POINT('Ctrl Pts',(1.67239348737616,18.048,639.855882352941));
#157054=CARTESIAN_POINT('Ctrl Pts',(3.31631129755346,17.7406985030951,638.361764705882));
#157055=CARTESIAN_POINT('Ctrl Pts',(4.96022910773077,17.4333970061901,636.867647058824));
#157056=CARTESIAN_POINT('Ctrl Pts',(6.51968959134575,16.8292587962898,635.373529411765));
#157057=CARTESIAN_POINT('Ctrl Pts',(8.07915007496071,16.2251205863895,633.879411764706));
#157058=CARTESIAN_POINT('Ctrl Pts',(9.50104767561053,15.3447188656481,632.385294117647));
#157059=CARTESIAN_POINT('Ctrl Pts',(10.9229452762603,14.4643171449067,630.891176470588));
#157060=CARTESIAN_POINT('Ctrl Pts',(12.1588589765331,13.3376329379985,629.39705882353));
#157061=CARTESIAN_POINT('Ctrl Pts',(13.3947726768058,12.2109487310903,627.902941176471));
#157062=CARTESIAN_POINT('Ctrl Pts',(14.4026149179538,10.8763499173728,626.408823529412));
#157063=CARTESIAN_POINT('Ctrl Pts',(15.4104571591017,9.54175110365538,624.914705882353));
#157064=CARTESIAN_POINT('Ctrl Pts',(16.1559070823762,8.04468584505496,623.420588235294));
#157065=CARTESIAN_POINT('Ctrl Pts',(16.9013570056506,6.54762058645456,621.926470588235));
#157066=CARTESIAN_POINT('Ctrl Pts',(17.3590292079831,4.93906964482096,620.432352941177));
#157067=CARTESIAN_POINT('Ctrl Pts',(17.8167014103155,3.33051870318735,618.938235294118));
#157068=CARTESIAN_POINT('Ctrl Pts',(17.9710104137728,1.66525935159367,617.444117647059));
#157069=CARTESIAN_POINT('Ctrl Pts',(18.1253194172301,3.32956716117513E-15,
615.95));
#157070=CARTESIAN_POINT('Ctrl Pts',(17.9710104137728,-1.66525935159367,
614.455882352941));
#157071=CARTESIAN_POINT('Ctrl Pts',(17.8167014103155,-3.33051870318736,
612.961764705883));
#157072=CARTESIAN_POINT('Ctrl Pts',(17.3590292079831,-4.93906964482095,
611.467647058824));
#157073=CARTESIAN_POINT('Ctrl Pts',(16.9013570056506,-6.54762058645456,
609.973529411765));
#157074=CARTESIAN_POINT('Ctrl Pts',(16.1559070823762,-8.04468584505497,
608.479411764706));
#157075=CARTESIAN_POINT('Ctrl Pts',(15.4104571591017,-9.54175110365538,
606.985294117647));
#157076=CARTESIAN_POINT('Ctrl Pts',(14.4026149179538,-10.8763499173728,
605.491176470588));
#157077=CARTESIAN_POINT('Ctrl Pts',(13.3947726768058,-12.2109487310903,
603.997058823529));
#157078=CARTESIAN_POINT('Ctrl Pts',(12.1588589765331,-13.3376329379985,
602.502941176471));
#157079=CARTESIAN_POINT('Ctrl Pts',(10.9229452762603,-14.4643171449067,
601.008823529412));
#157080=CARTESIAN_POINT('Ctrl Pts',(9.50104767561053,-15.3447188656481,
599.514705882353));
#157081=CARTESIAN_POINT('Ctrl Pts',(8.07915007496071,-16.2251205863895,
598.020588235294));
#157082=CARTESIAN_POINT('Ctrl Pts',(6.51968959134574,-16.8292587962898,
596.526470588235));
#157083=CARTESIAN_POINT('Ctrl Pts',(4.96022910773078,-17.4333970061901,
595.032352941176));
#157084=CARTESIAN_POINT('Ctrl Pts',(3.31631129755346,-17.7406985030951,
593.538235294118));
#157085=CARTESIAN_POINT('Ctrl Pts',(1.67239348737615,-18.048,592.044117647059));
#157086=CARTESIAN_POINT('Ctrl Pts',(0.,-18.048,590.55));
#157087=CARTESIAN_POINT('Ctrl Pts',(-1.67239348737615,-18.048,589.055882352941));
#157088=CARTESIAN_POINT('Ctrl Pts',(-3.31631129755346,-17.7406985030951,
587.561764705882));
#157089=CARTESIAN_POINT('Ctrl Pts',(-4.96022910773077,-17.4333970061901,
586.067647058823));
#157090=CARTESIAN_POINT('Ctrl Pts',(-6.51968959134574,-16.8292587962898,
584.573529411765));
#157091=CARTESIAN_POINT('Ctrl Pts',(-8.07915007496071,-16.2251205863895,
583.079411764706));
#157092=CARTESIAN_POINT('Ctrl Pts',(-9.50104767561052,-15.3447188656481,
581.585294117647));
#157093=CARTESIAN_POINT('Ctrl Pts',(-10.9229452762603,-14.4643171449067,
580.091176470588));
#157094=CARTESIAN_POINT('Ctrl Pts',(-12.1588589765331,-13.3376329379985,
578.597058823529));
#157095=CARTESIAN_POINT('Ctrl Pts',(-13.3947726768058,-12.2109487310903,
577.102941176471));
#157096=CARTESIAN_POINT('Ctrl Pts',(-14.4026149179538,-10.8763499173728,
575.608823529412));
#157097=CARTESIAN_POINT('Ctrl Pts',(-15.4104571591017,-9.54175110365538,
574.114705882353));
#157098=CARTESIAN_POINT('Ctrl Pts',(-16.1559070823762,-8.04468584505497,
572.620588235294));
#157099=CARTESIAN_POINT('Ctrl Pts',(-16.9013570056506,-6.54762058645456,
571.126470588235));
#157100=CARTESIAN_POINT('Ctrl Pts',(-17.3590292079831,-4.93906964482095,
569.632352941177));
#157101=CARTESIAN_POINT('Ctrl Pts',(-17.8167014103155,-3.33051870318735,
568.138235294118));
#157102=CARTESIAN_POINT('Ctrl Pts',(-17.9710104137728,-1.66525935159368,
566.644117647059));
#157103=CARTESIAN_POINT('Ctrl Pts',(-18.1253194172301,-1.10985572039171E-15,
565.15));
#157104=CARTESIAN_POINT('Ctrl Pts',(-17.9710104137728,1.66525935159367,
563.655882352941));
#157105=CARTESIAN_POINT('Ctrl Pts',(-17.8167014103155,3.33051870318735,
562.161764705883));
#157106=CARTESIAN_POINT('Ctrl Pts',(-17.3590292079831,4.93906964482096,
560.667647058824));
#157107=CARTESIAN_POINT('Ctrl Pts',(-16.9013570056506,6.54762058645456,
559.173529411765));
#157108=CARTESIAN_POINT('Ctrl Pts',(-16.1559070823762,8.04468584505497,
557.679411764706));
#157109=CARTESIAN_POINT('Ctrl Pts',(-15.4104571591017,9.54175110365538,
556.185294117647));
#157110=CARTESIAN_POINT('Ctrl Pts',(-14.4026149179538,10.8763499173728,
554.691176470588));
#157111=CARTESIAN_POINT('Ctrl Pts',(-13.3947726768058,12.2109487310903,
553.19705882353));
#157112=CARTESIAN_POINT('Ctrl Pts',(-12.1588589765331,13.3376329379985,
551.702941176471));
#157113=CARTESIAN_POINT('Ctrl Pts',(-10.9229452762603,14.4643171449067,
550.208823529412));
#157114=CARTESIAN_POINT('Ctrl Pts',(-9.50104767561052,15.3447188656481,
548.714705882353));
#157115=CARTESIAN_POINT('Ctrl Pts',(-8.07915007496071,16.2251205863895,
547.220588235294));
#157116=CARTESIAN_POINT('Ctrl Pts',(-6.51968959134574,16.8292587962898,
545.726470588235));
#157117=CARTESIAN_POINT('Ctrl Pts',(-4.96022910773078,17.4333970061901,
544.232352941176));
#157118=CARTESIAN_POINT('Ctrl Pts',(-3.31631129755346,17.7406985030951,
542.738235294118));
#157119=CARTESIAN_POINT('Ctrl Pts',(-1.67239348737615,18.048,541.244117647059));
#157120=CARTESIAN_POINT('Ctrl Pts',(-2.21024254310115E-15,18.048,539.75));
#157121=CARTESIAN_POINT('Ctrl Pts',(1.67239348737616,18.048,538.255882352941));
#157122=CARTESIAN_POINT('Ctrl Pts',(3.31631129755346,17.7406985030951,536.761764705882));
#157123=CARTESIAN_POINT('Ctrl Pts',(4.96022910773077,17.4333970061901,535.267647058824));
#157124=CARTESIAN_POINT('Ctrl Pts',(6.51968959134575,16.8292587962898,533.773529411765));
#157125=CARTESIAN_POINT('Ctrl Pts',(8.07915007496071,16.2251205863895,532.279411764706));
#157126=CARTESIAN_POINT('Ctrl Pts',(9.50104767561053,15.3447188656481,530.785294117647));
#157127=CARTESIAN_POINT('Ctrl Pts',(10.9229452762603,14.4643171449067,529.291176470588));
#157128=CARTESIAN_POINT('Ctrl Pts',(12.1588589765331,13.3376329379985,527.797058823529));
#157129=CARTESIAN_POINT('Ctrl Pts',(13.3947726768058,12.2109487310903,526.302941176471));
#157130=CARTESIAN_POINT('Ctrl Pts',(14.4026149179538,10.8763499173728,524.808823529412));
#157131=CARTESIAN_POINT('Ctrl Pts',(15.4104571591017,9.54175110365538,523.314705882353));
#157132=CARTESIAN_POINT('Ctrl Pts',(16.1559070823762,8.04468584505496,521.820588235294));
#157133=CARTESIAN_POINT('Ctrl Pts',(16.9013570056506,6.54762058645456,520.326470588235));
#157134=CARTESIAN_POINT('Ctrl Pts',(17.3590292079831,4.93906964482096,518.832352941177));
#157135=CARTESIAN_POINT('Ctrl Pts',(17.8167014103155,3.33051870318735,517.338235294118));
#157136=CARTESIAN_POINT('Ctrl Pts',(17.9710104137728,1.66525935159367,515.844117647059));
#157137=CARTESIAN_POINT('Ctrl Pts',(18.1253194172301,3.32956716117513E-15,
514.35));
#157138=CARTESIAN_POINT('Ctrl Pts',(17.9710104137728,-1.66525935159367,
512.855882352941));
#157139=CARTESIAN_POINT('Ctrl Pts',(17.8167014103155,-3.33051870318736,
511.361764705882));
#157140=CARTESIAN_POINT('Ctrl Pts',(17.3590292079831,-4.93906964482095,
509.867647058824));
#157141=CARTESIAN_POINT('Ctrl Pts',(16.9013570056506,-6.54762058645456,
508.373529411765));
#157142=CARTESIAN_POINT('Ctrl Pts',(16.1559070823762,-8.04468584505497,
506.879411764706));
#157143=CARTESIAN_POINT('Ctrl Pts',(15.4104571591017,-9.54175110365538,
505.385294117647));
#157144=CARTESIAN_POINT('Ctrl Pts',(14.4026149179538,-10.8763499173728,
503.891176470588));
#157145=CARTESIAN_POINT('Ctrl Pts',(13.3947726768058,-12.2109487310903,
502.39705882353));
#157146=CARTESIAN_POINT('Ctrl Pts',(12.1588589765331,-13.3376329379985,
500.902941176471));
#157147=CARTESIAN_POINT('Ctrl Pts',(10.9229452762603,-14.4643171449067,
499.408823529412));
#157148=CARTESIAN_POINT('Ctrl Pts',(9.50104767561053,-15.3447188656481,
497.914705882353));
#157149=CARTESIAN_POINT('Ctrl Pts',(8.07915007496071,-16.2251205863895,
496.420588235294));
#157150=CARTESIAN_POINT('Ctrl Pts',(6.51968959134574,-16.8292587962898,
494.926470588235));
#157151=CARTESIAN_POINT('Ctrl Pts',(4.96022910773078,-17.4333970061901,
493.432352941177));
#157152=CARTESIAN_POINT('Ctrl Pts',(3.31631129755346,-17.7406985030951,
491.938235294118));
#157153=CARTESIAN_POINT('Ctrl Pts',(1.67239348737615,-18.048,490.444117647059));
#157154=CARTESIAN_POINT('Ctrl Pts',(0.,-18.048,488.95));
#157155=CARTESIAN_POINT('Ctrl Pts',(-1.67239348737615,-18.048,487.455882352941));
#157156=CARTESIAN_POINT('Ctrl Pts',(-3.31631129755346,-17.7406985030951,
485.961764705883));
#157157=CARTESIAN_POINT('Ctrl Pts',(-4.96022910773077,-17.4333970061901,
484.467647058824));
#157158=CARTESIAN_POINT('Ctrl Pts',(-6.51968959134574,-16.8292587962898,
482.973529411765));
#157159=CARTESIAN_POINT('Ctrl Pts',(-8.07915007496071,-16.2251205863895,
481.479411764706));
#157160=CARTESIAN_POINT('Ctrl Pts',(-9.50104767561052,-15.3447188656481,
479.985294117647));
#157161=CARTESIAN_POINT('Ctrl Pts',(-10.9229452762603,-14.4643171449067,
478.491176470588));
#157162=CARTESIAN_POINT('Ctrl Pts',(-12.1588589765331,-13.3376329379985,
476.99705882353));
#157163=CARTESIAN_POINT('Ctrl Pts',(-13.3947726768058,-12.2109487310903,
475.502941176471));
#157164=CARTESIAN_POINT('Ctrl Pts',(-14.4026149179538,-10.8763499173728,
474.008823529412));
#157165=CARTESIAN_POINT('Ctrl Pts',(-15.4104571591017,-9.54175110365538,
472.514705882353));
#157166=CARTESIAN_POINT('Ctrl Pts',(-16.1559070823762,-8.04468584505497,
471.020588235294));
#157167=CARTESIAN_POINT('Ctrl Pts',(-16.9013570056506,-6.54762058645456,
469.526470588235));
#157168=CARTESIAN_POINT('Ctrl Pts',(-17.3590292079831,-4.93906964482095,
468.032352941177));
#157169=CARTESIAN_POINT('Ctrl Pts',(-17.8167014103155,-3.33051870318735,
466.538235294118));
#157170=CARTESIAN_POINT('Ctrl Pts',(-17.9710104137728,-1.66525935159368,
465.044117647059));
#157171=CARTESIAN_POINT('Ctrl Pts',(-18.1253194172301,-1.10985572039171E-15,
463.55));
#157172=CARTESIAN_POINT('Ctrl Pts',(-17.9710104137728,1.66525935159367,
462.055882352941));
#157173=CARTESIAN_POINT('Ctrl Pts',(-17.8167014103155,3.33051870318735,
460.561764705882));
#157174=CARTESIAN_POINT('Ctrl Pts',(-17.3590292079831,4.93906964482096,
459.067647058824));
#157175=CARTESIAN_POINT('Ctrl Pts',(-16.9013570056506,6.54762058645456,
457.573529411765));
#157176=CARTESIAN_POINT('Ctrl Pts',(-16.1559070823762,8.04468584505497,
456.079411764706));
#157177=CARTESIAN_POINT('Ctrl Pts',(-15.4104571591017,9.54175110365538,
454.585294117647));
#157178=CARTESIAN_POINT('Ctrl Pts',(-14.4026149179538,10.8763499173728,
453.091176470588));
#157179=CARTESIAN_POINT('Ctrl Pts',(-13.3947726768058,12.2109487310903,
451.597058823529));
#157180=CARTESIAN_POINT('Ctrl Pts',(-12.1588589765331,13.3376329379985,
450.102941176471));
#157181=CARTESIAN_POINT('Ctrl Pts',(-10.9229452762603,14.4643171449067,
448.608823529412));
#157182=CARTESIAN_POINT('Ctrl Pts',(-9.50104767561052,15.3447188656481,
447.114705882353));
#157183=CARTESIAN_POINT('Ctrl Pts',(-8.07915007496071,16.2251205863895,
445.620588235294));
#157184=CARTESIAN_POINT('Ctrl Pts',(-6.51968959134574,16.8292587962898,
444.126470588235));
#157185=CARTESIAN_POINT('Ctrl Pts',(-4.96022910773078,17.4333970061901,
442.632352941176));
#157186=CARTESIAN_POINT('Ctrl Pts',(-3.31631129755346,17.7406985030951,
441.138235294118));
#157187=CARTESIAN_POINT('Ctrl Pts',(-1.67239348737615,18.048,439.644117647059));
#157188=CARTESIAN_POINT('Ctrl Pts',(-2.21024254310115E-15,18.048,438.15));
#157189=CARTESIAN_POINT('Ctrl Pts',(1.67239348737616,18.048,436.655882352941));
#157190=CARTESIAN_POINT('Ctrl Pts',(3.31631129755346,17.7406985030951,435.161764705882));
#157191=CARTESIAN_POINT('Ctrl Pts',(4.96022910773077,17.4333970061901,433.667647058824));
#157192=CARTESIAN_POINT('Ctrl Pts',(6.51968959134575,16.8292587962898,432.173529411765));
#157193=CARTESIAN_POINT('Ctrl Pts',(8.07915007496071,16.2251205863895,430.679411764706));
#157194=CARTESIAN_POINT('Ctrl Pts',(9.50104767561053,15.3447188656481,429.185294117647));
#157195=CARTESIAN_POINT('Ctrl Pts',(10.9229452762603,14.4643171449067,427.691176470588));
#157196=CARTESIAN_POINT('Ctrl Pts',(12.1588589765331,13.3376329379985,426.19705882353));
#157197=CARTESIAN_POINT('Ctrl Pts',(13.3947726768058,12.2109487310903,424.702941176471));
#157198=CARTESIAN_POINT('Ctrl Pts',(14.4026149179538,10.8763499173728,423.208823529412));
#157199=CARTESIAN_POINT('Ctrl Pts',(15.4104571591017,9.54175110365538,421.714705882353));
#157200=CARTESIAN_POINT('Ctrl Pts',(16.1559070823762,8.04468584505496,420.220588235294));
#157201=CARTESIAN_POINT('Ctrl Pts',(16.9013570056506,6.54762058645456,418.726470588235));
#157202=CARTESIAN_POINT('Ctrl Pts',(17.3590292079831,4.93906964482096,417.232352941177));
#157203=CARTESIAN_POINT('Ctrl Pts',(17.8167014103155,3.33051870318735,415.738235294118));
#157204=CARTESIAN_POINT('Ctrl Pts',(17.9710104137728,1.66525935159367,414.244117647059));
#157205=CARTESIAN_POINT('Ctrl Pts',(18.1253194172301,3.32956716117513E-15,
412.75));
#157206=CARTESIAN_POINT('Ctrl Pts',(17.9710104137728,-1.66525935159367,
411.255882352941));
#157207=CARTESIAN_POINT('Ctrl Pts',(17.8167014103155,-3.33051870318736,
409.761764705883));
#157208=CARTESIAN_POINT('Ctrl Pts',(17.3590292079831,-4.93906964482095,
408.267647058824));
#157209=CARTESIAN_POINT('Ctrl Pts',(16.9013570056506,-6.54762058645456,
406.773529411765));
#157210=CARTESIAN_POINT('Ctrl Pts',(16.1559070823762,-8.04468584505497,
405.279411764706));
#157211=CARTESIAN_POINT('Ctrl Pts',(15.4104571591017,-9.54175110365538,
403.785294117647));
#157212=CARTESIAN_POINT('Ctrl Pts',(14.4026149179538,-10.8763499173728,
402.291176470588));
#157213=CARTESIAN_POINT('Ctrl Pts',(13.3947726768058,-12.2109487310903,
400.797058823529));
#157214=CARTESIAN_POINT('Ctrl Pts',(12.1588589765331,-13.3376329379985,
399.302941176471));
#157215=CARTESIAN_POINT('Ctrl Pts',(10.9229452762603,-14.4643171449067,
397.808823529412));
#157216=CARTESIAN_POINT('Ctrl Pts',(9.50104767561053,-15.3447188656481,
396.314705882353));
#157217=CARTESIAN_POINT('Ctrl Pts',(8.07915007496071,-16.2251205863895,
394.820588235294));
#157218=CARTESIAN_POINT('Ctrl Pts',(6.51968959134574,-16.8292587962898,
393.326470588235));
#157219=CARTESIAN_POINT('Ctrl Pts',(4.96022910773078,-17.4333970061901,
391.832352941177));
#157220=CARTESIAN_POINT('Ctrl Pts',(3.31631129755346,-17.7406985030951,
390.338235294118));
#157221=CARTESIAN_POINT('Ctrl Pts',(1.67239348737615,-18.048,388.844117647059));
#157222=CARTESIAN_POINT('Ctrl Pts',(0.,-18.048,387.35));
#157223=CARTESIAN_POINT('Ctrl Pts',(-1.67239348737615,-18.048,385.855882352941));
#157224=CARTESIAN_POINT('Ctrl Pts',(-3.31631129755346,-17.7406985030951,
384.361764705882));
#157225=CARTESIAN_POINT('Ctrl Pts',(-4.96022910773077,-17.4333970061901,
382.867647058824));
#157226=CARTESIAN_POINT('Ctrl Pts',(-6.51968959134574,-16.8292587962898,
381.373529411765));
#157227=CARTESIAN_POINT('Ctrl Pts',(-8.07915007496071,-16.2251205863895,
379.879411764706));
#157228=CARTESIAN_POINT('Ctrl Pts',(-9.50104767561052,-15.3447188656481,
378.385294117647));
#157229=CARTESIAN_POINT('Ctrl Pts',(-10.9229452762603,-14.4643171449067,
376.891176470588));
#157230=CARTESIAN_POINT('Ctrl Pts',(-12.1588589765331,-13.3376329379985,
375.397058823529));
#157231=CARTESIAN_POINT('Ctrl Pts',(-13.3947726768058,-12.2109487310903,
373.902941176471));
#157232=CARTESIAN_POINT('Ctrl Pts',(-14.4026149179538,-10.8763499173728,
372.408823529412));
#157233=CARTESIAN_POINT('Ctrl Pts',(-15.4104571591017,-9.54175110365538,
370.914705882353));
#157234=CARTESIAN_POINT('Ctrl Pts',(-16.1559070823762,-8.04468584505497,
369.420588235294));
#157235=CARTESIAN_POINT('Ctrl Pts',(-16.9013570056506,-6.54762058645456,
367.926470588235));
#157236=CARTESIAN_POINT('Ctrl Pts',(-17.3590292079831,-4.93906964482095,
366.432352941177));
#157237=CARTESIAN_POINT('Ctrl Pts',(-17.8167014103155,-3.33051870318735,
364.938235294118));
#157238=CARTESIAN_POINT('Ctrl Pts',(-17.9710104137728,-1.66525935159368,
363.444117647059));
#157239=CARTESIAN_POINT('Ctrl Pts',(-18.1253194172301,-1.10985572039171E-15,
361.95));
#157240=CARTESIAN_POINT('Ctrl Pts',(-17.9710104137728,1.66525935159367,
360.455882352941));
#157241=CARTESIAN_POINT('Ctrl Pts',(-17.8167014103155,3.33051870318735,
358.961764705882));
#157242=CARTESIAN_POINT('Ctrl Pts',(-17.3590292079831,4.93906964482096,
357.467647058824));
#157243=CARTESIAN_POINT('Ctrl Pts',(-16.9013570056506,6.54762058645456,
355.973529411765));
#157244=CARTESIAN_POINT('Ctrl Pts',(-16.1559070823762,8.04468584505497,
354.479411764706));
#157245=CARTESIAN_POINT('Ctrl Pts',(-15.4104571591017,9.54175110365538,
352.985294117647));
#157246=CARTESIAN_POINT('Ctrl Pts',(-14.4026149179538,10.8763499173728,
351.491176470588));
#157247=CARTESIAN_POINT('Ctrl Pts',(-13.3947726768058,12.2109487310903,
349.99705882353));
#157248=CARTESIAN_POINT('Ctrl Pts',(-12.1588589765331,13.3376329379985,
348.502941176471));
#157249=CARTESIAN_POINT('Ctrl Pts',(-10.9229452762603,14.4643171449067,
347.008823529412));
#157250=CARTESIAN_POINT('Ctrl Pts',(-9.50104767561052,15.3447188656481,
345.514705882353));
#157251=CARTESIAN_POINT('Ctrl Pts',(-8.07915007496071,16.2251205863895,
344.020588235294));
#157252=CARTESIAN_POINT('Ctrl Pts',(-6.51968959134574,16.8292587962898,
342.526470588235));
#157253=CARTESIAN_POINT('Ctrl Pts',(-4.96022910773078,17.4333970061901,
341.032352941177));
#157254=CARTESIAN_POINT('Ctrl Pts',(-3.31631129755346,17.7406985030951,
339.538235294118));
#157255=CARTESIAN_POINT('Ctrl Pts',(-1.67239348737615,18.048,338.044117647059));
#157256=CARTESIAN_POINT('Ctrl Pts',(-2.21024254310115E-15,18.048,336.55));
#157257=CARTESIAN_POINT('Ctrl Pts',(1.67239348737616,18.048,335.055882352941));
#157258=CARTESIAN_POINT('Ctrl Pts',(3.31631129755346,17.7406985030951,333.561764705882));
#157259=CARTESIAN_POINT('Ctrl Pts',(4.96022910773077,17.4333970061901,332.067647058824));
#157260=CARTESIAN_POINT('Ctrl Pts',(6.51968959134575,16.8292587962898,330.573529411765));
#157261=CARTESIAN_POINT('Ctrl Pts',(8.07915007496071,16.2251205863895,329.079411764706));
#157262=CARTESIAN_POINT('Ctrl Pts',(9.50104767561053,15.3447188656481,327.585294117647));
#157263=CARTESIAN_POINT('Ctrl Pts',(10.9229452762603,14.4643171449067,326.091176470588));
#157264=CARTESIAN_POINT('Ctrl Pts',(12.1588589765331,13.3376329379985,324.597058823529));
#157265=CARTESIAN_POINT('Ctrl Pts',(13.3947726768058,12.2109487310903,323.102941176471));
#157266=CARTESIAN_POINT('Ctrl Pts',(14.4026149179538,10.8763499173728,321.608823529412));
#157267=CARTESIAN_POINT('Ctrl Pts',(15.4104571591017,9.54175110365538,320.114705882353));
#157268=CARTESIAN_POINT('Ctrl Pts',(16.1559070823762,8.04468584505496,318.620588235294));
#157269=CARTESIAN_POINT('Ctrl Pts',(16.9013570056506,6.54762058645456,317.126470588235));
#157270=CARTESIAN_POINT('Ctrl Pts',(17.3590292079831,4.93906964482096,315.632352941176));
#157271=CARTESIAN_POINT('Ctrl Pts',(17.8167014103155,3.33051870318735,314.138235294118));
#157272=CARTESIAN_POINT('Ctrl Pts',(17.9710104137728,1.66525935159367,312.644117647059));
#157273=CARTESIAN_POINT('Ctrl Pts',(18.1253194172301,3.32956716117513E-15,
311.15));
#157274=CARTESIAN_POINT('Ctrl Pts',(17.9710104137728,-1.66525935159367,
309.655882352941));
#157275=CARTESIAN_POINT('Ctrl Pts',(17.8167014103155,-3.33051870318736,
308.161764705882));
#157276=CARTESIAN_POINT('Ctrl Pts',(17.3590292079831,-4.93906964482095,
306.667647058824));
#157277=CARTESIAN_POINT('Ctrl Pts',(16.9013570056506,-6.54762058645456,
305.173529411765));
#157278=CARTESIAN_POINT('Ctrl Pts',(16.1559070823762,-8.04468584505497,
303.679411764706));
#157279=CARTESIAN_POINT('Ctrl Pts',(15.4104571591017,-9.54175110365538,
302.185294117647));
#157280=CARTESIAN_POINT('Ctrl Pts',(14.4026149179538,-10.8763499173728,
300.691176470588));
#157281=CARTESIAN_POINT('Ctrl Pts',(13.3947726768058,-12.2109487310903,
299.19705882353));
#157282=CARTESIAN_POINT('Ctrl Pts',(12.1588589765331,-13.3376329379985,
297.702941176471));
#157283=CARTESIAN_POINT('Ctrl Pts',(10.9229452762603,-14.4643171449067,
296.208823529412));
#157284=CARTESIAN_POINT('Ctrl Pts',(9.50104767561053,-15.3447188656481,
294.714705882353));
#157285=CARTESIAN_POINT('Ctrl Pts',(8.07915007496071,-16.2251205863895,
293.220588235294));
#157286=CARTESIAN_POINT('Ctrl Pts',(6.51968959134574,-16.8292587962898,
291.726470588235));
#157287=CARTESIAN_POINT('Ctrl Pts',(4.96022910773078,-17.4333970061901,
290.232352941176));
#157288=CARTESIAN_POINT('Ctrl Pts',(3.31631129755346,-17.7406985030951,
288.738235294118));
#157289=CARTESIAN_POINT('Ctrl Pts',(1.67239348737615,-18.048,287.244117647059));
#157290=CARTESIAN_POINT('Ctrl Pts',(0.,-18.048,285.75));
#157291=CARTESIAN_POINT('Ctrl Pts',(-1.67239348737615,-18.048,284.255882352941));
#157292=CARTESIAN_POINT('Ctrl Pts',(-3.31631129755346,-17.7406985030951,
282.761764705882));
#157293=CARTESIAN_POINT('Ctrl Pts',(-4.96022910773077,-17.4333970061901,
281.267647058824));
#157294=CARTESIAN_POINT('Ctrl Pts',(-6.51968959134574,-16.8292587962898,
279.773529411765));
#157295=CARTESIAN_POINT('Ctrl Pts',(-8.07915007496071,-16.2251205863895,
278.279411764706));
#157296=CARTESIAN_POINT('Ctrl Pts',(-9.50104767561052,-15.3447188656481,
276.785294117647));
#157297=CARTESIAN_POINT('Ctrl Pts',(-10.9229452762603,-14.4643171449067,
275.291176470588));
#157298=CARTESIAN_POINT('Ctrl Pts',(-12.1588589765331,-13.3376329379985,
273.797058823529));
#157299=CARTESIAN_POINT('Ctrl Pts',(-13.3947726768058,-12.2109487310903,
272.302941176471));
#157300=CARTESIAN_POINT('Ctrl Pts',(-14.4026149179538,-10.8763499173728,
270.808823529412));
#157301=CARTESIAN_POINT('Ctrl Pts',(-15.4104571591017,-9.54175110365538,
269.314705882353));
#157302=CARTESIAN_POINT('Ctrl Pts',(-16.1559070823762,-8.04468584505497,
267.820588235294));
#157303=CARTESIAN_POINT('Ctrl Pts',(-16.9013570056506,-6.54762058645456,
266.326470588235));
#157304=CARTESIAN_POINT('Ctrl Pts',(-17.3590292079831,-4.93906964482095,
264.832352941177));
#157305=CARTESIAN_POINT('Ctrl Pts',(-17.8167014103155,-3.33051870318735,
263.338235294118));
#157306=CARTESIAN_POINT('Ctrl Pts',(-17.9710104137728,-1.66525935159368,
261.844117647059));
#157307=CARTESIAN_POINT('Ctrl Pts',(-18.1253194172301,-1.10985572039171E-15,
260.35));
#157308=CARTESIAN_POINT('Ctrl Pts',(-17.9710104137728,1.66525935159367,
258.855882352941));
#157309=CARTESIAN_POINT('Ctrl Pts',(-17.8167014103155,3.33051870318735,
257.361764705882));
#157310=CARTESIAN_POINT('Ctrl Pts',(-17.3590292079831,4.93906964482096,
255.867647058823));
#157311=CARTESIAN_POINT('Ctrl Pts',(-16.9013570056506,6.54762058645456,
254.373529411765));
#157312=CARTESIAN_POINT('Ctrl Pts',(-16.1559070823762,8.04468584505497,
252.879411764706));
#157313=CARTESIAN_POINT('Ctrl Pts',(-15.4104571591017,9.54175110365538,
251.385294117647));
#157314=CARTESIAN_POINT('Ctrl Pts',(-14.4026149179538,10.8763499173728,
249.891176470588));
#157315=CARTESIAN_POINT('Ctrl Pts',(-13.3947726768058,12.2109487310903,
248.397058823529));
#157316=CARTESIAN_POINT('Ctrl Pts',(-12.1588589765331,13.3376329379985,
246.902941176471));
#157317=CARTESIAN_POINT('Ctrl Pts',(-10.9229452762603,14.4643171449067,
245.408823529412));
#157318=CARTESIAN_POINT('Ctrl Pts',(-9.50104767561052,15.3447188656481,
243.914705882353));
#157319=CARTESIAN_POINT('Ctrl Pts',(-8.07915007496071,16.2251205863895,
242.420588235294));
#157320=CARTESIAN_POINT('Ctrl Pts',(-6.51968959134574,16.8292587962898,
240.926470588235));
#157321=CARTESIAN_POINT('Ctrl Pts',(-4.96022910773078,17.4333970061901,
239.432352941177));
#157322=CARTESIAN_POINT('Ctrl Pts',(-3.31631129755346,17.7406985030951,
237.938235294118));
#157323=CARTESIAN_POINT('Ctrl Pts',(-1.67239348737615,18.048,236.444117647059));
#157324=CARTESIAN_POINT('Ctrl Pts',(-2.21024254310115E-15,18.048,234.95));
#157325=CARTESIAN_POINT('Ctrl Pts',(1.67239348737616,18.048,233.455882352941));
#157326=CARTESIAN_POINT('Ctrl Pts',(3.31631129755346,17.7406985030951,231.961764705883));
#157327=CARTESIAN_POINT('Ctrl Pts',(4.96022910773077,17.4333970061901,230.467647058824));
#157328=CARTESIAN_POINT('Ctrl Pts',(6.51968959134575,16.8292587962898,228.973529411765));
#157329=CARTESIAN_POINT('Ctrl Pts',(8.07915007496071,16.2251205863895,227.479411764706));
#157330=CARTESIAN_POINT('Ctrl Pts',(9.50104767561053,15.3447188656481,225.985294117647));
#157331=CARTESIAN_POINT('Ctrl Pts',(10.9229452762603,14.4643171449067,224.491176470588));
#157332=CARTESIAN_POINT('Ctrl Pts',(12.1588589765331,13.3376329379985,222.99705882353));
#157333=CARTESIAN_POINT('Ctrl Pts',(13.3947726768058,12.2109487310903,221.502941176471));
#157334=CARTESIAN_POINT('Ctrl Pts',(14.4026149179538,10.8763499173728,220.008823529412));
#157335=CARTESIAN_POINT('Ctrl Pts',(15.4104571591017,9.54175110365538,218.514705882353));
#157336=CARTESIAN_POINT('Ctrl Pts',(16.1559070823762,8.04468584505496,217.020588235294));
#157337=CARTESIAN_POINT('Ctrl Pts',(16.9013570056506,6.54762058645456,215.526470588235));
#157338=CARTESIAN_POINT('Ctrl Pts',(17.3590292079831,4.93906964482096,214.032352941176));
#157339=CARTESIAN_POINT('Ctrl Pts',(17.8167014103155,3.33051870318735,212.538235294118));
#157340=CARTESIAN_POINT('Ctrl Pts',(17.9710104137728,1.66525935159367,211.044117647059));
#157341=CARTESIAN_POINT('Ctrl Pts',(18.1253194172301,3.32956716117513E-15,
209.55));
#157342=CARTESIAN_POINT('Ctrl Pts',(17.9710104137728,-1.66525935159367,
208.055882352941));
#157343=CARTESIAN_POINT('Ctrl Pts',(17.8167014103155,-3.33051870318736,
206.561764705882));
#157344=CARTESIAN_POINT('Ctrl Pts',(17.3590292079831,-4.93906964482095,
205.067647058824));
#157345=CARTESIAN_POINT('Ctrl Pts',(16.9013570056506,-6.54762058645456,
203.573529411765));
#157346=CARTESIAN_POINT('Ctrl Pts',(16.1559070823762,-8.04468584505497,
202.079411764706));
#157347=CARTESIAN_POINT('Ctrl Pts',(15.4104571591017,-9.54175110365538,
200.585294117647));
#157348=CARTESIAN_POINT('Ctrl Pts',(14.4026149179538,-10.8763499173728,
199.091176470588));
#157349=CARTESIAN_POINT('Ctrl Pts',(13.3947726768058,-12.2109487310903,
197.597058823529));
#157350=CARTESIAN_POINT('Ctrl Pts',(12.1588589765331,-13.3376329379985,
196.102941176471));
#157351=CARTESIAN_POINT('Ctrl Pts',(10.9229452762603,-14.4643171449067,
194.608823529412));
#157352=CARTESIAN_POINT('Ctrl Pts',(9.50104767561053,-15.3447188656481,
193.114705882353));
#157353=CARTESIAN_POINT('Ctrl Pts',(8.07915007496071,-16.2251205863895,
191.620588235294));
#157354=CARTESIAN_POINT('Ctrl Pts',(6.51968959134574,-16.8292587962898,
190.126470588235));
#157355=CARTESIAN_POINT('Ctrl Pts',(4.96022910773078,-17.4333970061901,
188.632352941176));
#157356=CARTESIAN_POINT('Ctrl Pts',(3.31631129755346,-17.7406985030951,
187.138235294118));
#157357=CARTESIAN_POINT('Ctrl Pts',(1.67239348737615,-18.048,185.644117647059));
#157358=CARTESIAN_POINT('Ctrl Pts',(0.,-18.048,184.15));
#157359=CARTESIAN_POINT('Ctrl Pts',(-1.67239348737615,-18.048,182.655882352941));
#157360=CARTESIAN_POINT('Ctrl Pts',(-3.31631129755346,-17.7406985030951,
181.161764705882));
#157361=CARTESIAN_POINT('Ctrl Pts',(-4.96022910773077,-17.4333970061901,
179.667647058824));
#157362=CARTESIAN_POINT('Ctrl Pts',(-6.51968959134574,-16.8292587962898,
178.173529411765));
#157363=CARTESIAN_POINT('Ctrl Pts',(-8.07915007496071,-16.2251205863895,
176.679411764706));
#157364=CARTESIAN_POINT('Ctrl Pts',(-9.50104767561052,-15.3447188656481,
175.185294117647));
#157365=CARTESIAN_POINT('Ctrl Pts',(-10.9229452762603,-14.4643171449067,
173.691176470588));
#157366=CARTESIAN_POINT('Ctrl Pts',(-12.1588589765331,-13.3376329379985,
172.19705882353));
#157367=CARTESIAN_POINT('Ctrl Pts',(-13.3947726768058,-12.2109487310903,
170.702941176471));
#157368=CARTESIAN_POINT('Ctrl Pts',(-14.4026149179538,-10.8763499173728,
169.208823529412));
#157369=CARTESIAN_POINT('Ctrl Pts',(-15.4104571591017,-9.54175110365538,
167.714705882353));
#157370=CARTESIAN_POINT('Ctrl Pts',(-16.1559070823762,-8.04468584505497,
166.220588235294));
#157371=CARTESIAN_POINT('Ctrl Pts',(-16.9013570056506,-6.54762058645456,
164.726470588235));
#157372=CARTESIAN_POINT('Ctrl Pts',(-17.3590292079831,-4.93906964482095,
163.232352941177));
#157373=CARTESIAN_POINT('Ctrl Pts',(-17.8167014103155,-3.33051870318735,
161.738235294118));
#157374=CARTESIAN_POINT('Ctrl Pts',(-17.9710104137728,-1.66525935159368,
160.244117647059));
#157375=CARTESIAN_POINT('Ctrl Pts',(-18.1253194172301,-1.10985572039171E-15,
158.75));
#157376=CARTESIAN_POINT('Ctrl Pts',(-17.9710104137728,1.66525935159367,
157.255882352941));
#157377=CARTESIAN_POINT('Ctrl Pts',(-17.8167014103155,3.33051870318735,
155.761764705882));
#157378=CARTESIAN_POINT('Ctrl Pts',(-17.3590292079831,4.93906964482096,
154.267647058824));
#157379=CARTESIAN_POINT('Ctrl Pts',(-16.9013570056506,6.54762058645456,
152.773529411765));
#157380=CARTESIAN_POINT('Ctrl Pts',(-16.1559070823762,8.04468584505497,
151.279411764706));
#157381=CARTESIAN_POINT('Ctrl Pts',(-15.4104571591017,9.54175110365538,
149.785294117647));
#157382=CARTESIAN_POINT('Ctrl Pts',(-14.4026149179538,10.8763499173728,
148.291176470588));
#157383=CARTESIAN_POINT('Ctrl Pts',(-13.3947726768058,12.2109487310903,
146.79705882353));
#157384=CARTESIAN_POINT('Ctrl Pts',(-12.1588589765331,13.3376329379985,
145.302941176471));
#157385=CARTESIAN_POINT('Ctrl Pts',(-10.9229452762603,14.4643171449067,
143.808823529412));
#157386=CARTESIAN_POINT('Ctrl Pts',(-9.50104767561052,15.3447188656481,
142.314705882353));
#157387=CARTESIAN_POINT('Ctrl Pts',(-8.07915007496071,16.2251205863895,
140.820588235294));
#157388=CARTESIAN_POINT('Ctrl Pts',(-6.51968959134574,16.8292587962898,
139.326470588235));
#157389=CARTESIAN_POINT('Ctrl Pts',(-4.96022910773078,17.4333970061901,
137.832352941177));
#157390=CARTESIAN_POINT('Ctrl Pts',(-3.31631129755346,17.7406985030951,
136.338235294118));
#157391=CARTESIAN_POINT('Ctrl Pts',(-1.67239348737615,18.048,134.844117647059));
#157392=CARTESIAN_POINT('Ctrl Pts',(-2.21024254310115E-15,18.048,133.35));
#157393=CARTESIAN_POINT('Ctrl Pts',(1.67239348737616,18.048,131.855882352941));
#157394=CARTESIAN_POINT('Ctrl Pts',(3.31631129755346,17.7406985030951,130.361764705882));
#157395=CARTESIAN_POINT('Ctrl Pts',(4.96022910773077,17.4333970061901,128.867647058824));
#157396=CARTESIAN_POINT('Ctrl Pts',(6.51968959134575,16.8292587962898,127.373529411765));
#157397=CARTESIAN_POINT('Ctrl Pts',(8.07915007496071,16.2251205863895,125.879411764706));
#157398=CARTESIAN_POINT('Ctrl Pts',(9.50104767561053,15.3447188656481,124.385294117647));
#157399=CARTESIAN_POINT('Ctrl Pts',(10.9229452762603,14.4643171449067,122.891176470588));
#157400=CARTESIAN_POINT('Ctrl Pts',(12.1588589765331,13.3376329379985,121.397058823529));
#157401=CARTESIAN_POINT('Ctrl Pts',(13.3947726768058,12.2109487310903,119.902941176471));
#157402=CARTESIAN_POINT('Ctrl Pts',(14.4026149179538,10.8763499173728,118.408823529412));
#157403=CARTESIAN_POINT('Ctrl Pts',(15.4104571591017,9.54175110365538,116.914705882353));
#157404=CARTESIAN_POINT('Ctrl Pts',(16.1559070823762,8.04468584505496,115.420588235294));
#157405=CARTESIAN_POINT('Ctrl Pts',(16.9013570056506,6.54762058645456,113.926470588235));
#157406=CARTESIAN_POINT('Ctrl Pts',(17.3590292079831,4.93906964482096,112.432352941177));
#157407=CARTESIAN_POINT('Ctrl Pts',(17.8167014103155,3.33051870318735,110.938235294118));
#157408=CARTESIAN_POINT('Ctrl Pts',(17.9710104137728,1.66525935159367,109.444117647059));
#157409=CARTESIAN_POINT('Ctrl Pts',(18.1253194172301,3.32956716117513E-15,
107.95));
#157410=CARTESIAN_POINT('Ctrl Pts',(17.9710104137728,-1.66525935159367,
106.455882352941));
#157411=CARTESIAN_POINT('Ctrl Pts',(17.8167014103155,-3.33051870318736,
104.961764705882));
#157412=CARTESIAN_POINT('Ctrl Pts',(17.3590292079831,-4.93906964482095,
103.467647058824));
#157413=CARTESIAN_POINT('Ctrl Pts',(16.9013570056506,-6.54762058645456,
101.973529411765));
#157414=CARTESIAN_POINT('Ctrl Pts',(16.1559070823762,-8.04468584505497,
100.479411764706));
#157415=CARTESIAN_POINT('Ctrl Pts',(15.4104571591017,-9.54175110365538,
98.985294117647));
#157416=CARTESIAN_POINT('Ctrl Pts',(14.4026149179538,-10.8763499173728,
97.4911764705884));
#157417=CARTESIAN_POINT('Ctrl Pts',(13.3947726768058,-12.2109487310903,
95.9970588235295));
#157418=CARTESIAN_POINT('Ctrl Pts',(12.1588589765331,-13.3376329379985,
94.5029411764706));
#157419=CARTESIAN_POINT('Ctrl Pts',(10.9229452762603,-14.4643171449067,
93.0088235294117));
#157420=CARTESIAN_POINT('Ctrl Pts',(9.50104767561053,-15.3447188656481,
91.5147058823529));
#157421=CARTESIAN_POINT('Ctrl Pts',(8.07915007496071,-16.2251205863895,
90.0205882352942));
#157422=CARTESIAN_POINT('Ctrl Pts',(6.51968959134574,-16.8292587962898,
88.5264705882354));
#157423=CARTESIAN_POINT('Ctrl Pts',(4.96022910773078,-17.4333970061901,
87.0323529411765));
#157424=CARTESIAN_POINT('Ctrl Pts',(3.31631129755346,-17.7406985030951,
85.5382352941176));
#157425=CARTESIAN_POINT('Ctrl Pts',(1.67239348737615,-18.048,84.0441176470588));
#157426=CARTESIAN_POINT('Ctrl Pts',(0.,-18.048,82.5500000000001));
#157427=CARTESIAN_POINT('Ctrl Pts',(-1.67239348737615,-18.048,81.0558823529413));
#157428=CARTESIAN_POINT('Ctrl Pts',(-3.31631129755346,-17.7406985030951,
79.5617647058824));
#157429=CARTESIAN_POINT('Ctrl Pts',(-4.96022910773077,-17.4333970061901,
78.0676470588235));
#157430=CARTESIAN_POINT('Ctrl Pts',(-6.51968959134574,-16.8292587962898,
76.5735294117647));
#157431=CARTESIAN_POINT('Ctrl Pts',(-8.07915007496071,-16.2251205863895,
75.079411764706));
#157432=CARTESIAN_POINT('Ctrl Pts',(-9.50104767561052,-15.3447188656481,
73.5852941176471));
#157433=CARTESIAN_POINT('Ctrl Pts',(-10.9229452762603,-14.4643171449067,
72.0911764705883));
#157434=CARTESIAN_POINT('Ctrl Pts',(-12.1588589765331,-13.3376329379985,
70.5970588235294));
#157435=CARTESIAN_POINT('Ctrl Pts',(-13.3947726768058,-12.2109487310903,
69.1029411764705));
#157436=CARTESIAN_POINT('Ctrl Pts',(-14.4026149179538,-10.8763499173728,
67.6088235294119));
#157437=CARTESIAN_POINT('Ctrl Pts',(-15.4104571591017,-9.54175110365538,
66.114705882353));
#157438=CARTESIAN_POINT('Ctrl Pts',(-16.1559070823762,-8.04468584505497,
64.6205882352942));
#157439=CARTESIAN_POINT('Ctrl Pts',(-16.9013570056506,-6.54762058645456,
63.1264705882353));
#157440=CARTESIAN_POINT('Ctrl Pts',(-17.3590292079831,-4.93906964482095,
61.6323529411764));
#157441=CARTESIAN_POINT('Ctrl Pts',(-17.8167014103155,-3.33051870318735,
60.1382352941178));
#157442=CARTESIAN_POINT('Ctrl Pts',(-17.9710104137728,-1.66525935159368,
58.6441176470589));
#157443=CARTESIAN_POINT('Ctrl Pts',(-18.1253194172301,-1.10985572039171E-15,
57.15));
#157444=CARTESIAN_POINT('Ctrl Pts',(-17.9710104137728,1.66525935159367,
55.6558823529412));
#157445=CARTESIAN_POINT('Ctrl Pts',(-17.8167014103155,3.33051870318735,
54.1617647058823));
#157446=CARTESIAN_POINT('Ctrl Pts',(-17.3590292079831,4.93906964482096,
52.6676470588237));
#157447=CARTESIAN_POINT('Ctrl Pts',(-16.9013570056506,6.54762058645456,
51.1735294117648));
#157448=CARTESIAN_POINT('Ctrl Pts',(-16.1559070823762,8.04468584505497,
49.6794117647059));
#157449=CARTESIAN_POINT('Ctrl Pts',(-15.4104571591017,9.54175110365538,
48.185294117647));
#157450=CARTESIAN_POINT('Ctrl Pts',(-14.4026149179538,10.8763499173728,
46.6911764705882));
#157451=CARTESIAN_POINT('Ctrl Pts',(-13.3947726768058,12.2109487310903,
45.1970588235295));
#157452=CARTESIAN_POINT('Ctrl Pts',(-12.1588589765331,13.3376329379985,
43.7029411764707));
#157453=CARTESIAN_POINT('Ctrl Pts',(-10.9229452762603,14.4643171449067,
42.2088235294118));
#157454=CARTESIAN_POINT('Ctrl Pts',(-9.50104767561052,15.3447188656481,
40.7147058823529));
#157455=CARTESIAN_POINT('Ctrl Pts',(-8.07915007496071,16.2251205863895,
39.2205882352941));
#157456=CARTESIAN_POINT('Ctrl Pts',(-6.51968959134574,16.8292587962898,
37.7264705882354));
#157457=CARTESIAN_POINT('Ctrl Pts',(-4.96022910773078,17.4333970061901,
36.2323529411766));
#157458=CARTESIAN_POINT('Ctrl Pts',(-3.31631129755346,17.7406985030951,
34.7382352941177));
#157459=CARTESIAN_POINT('Ctrl Pts',(-1.67239348737615,18.048,33.2441176470588));
#157460=CARTESIAN_POINT('Ctrl Pts',(-2.21024254310115E-15,18.048,31.7499999999999));
#157461=CARTESIAN_POINT('Ctrl Pts',(1.67239348737616,18.048,30.2558823529413));
#157462=CARTESIAN_POINT('Ctrl Pts',(3.31631129755346,17.7406985030951,28.7617647058824));
#157463=CARTESIAN_POINT('Ctrl Pts',(4.96022910773077,17.4333970061901,27.2676470588236));
#157464=CARTESIAN_POINT('Ctrl Pts',(6.51968959134575,16.8292587962898,25.7735294117647));
#157465=CARTESIAN_POINT('Ctrl Pts',(8.07915007496071,16.2251205863895,24.2794117647058));
#157466=CARTESIAN_POINT('Ctrl Pts',(9.50104767561053,15.3447188656481,22.7852941176472));
#157467=CARTESIAN_POINT('Ctrl Pts',(10.9229452762603,14.4643171449067,21.2911764705883));
#157468=CARTESIAN_POINT('Ctrl Pts',(12.1588589765331,13.3376329379985,19.7970588235294));
#157469=CARTESIAN_POINT('Ctrl Pts',(13.3947726768058,12.2109487310903,18.3029411764706));
#157470=CARTESIAN_POINT('Ctrl Pts',(14.4026149179538,10.8763499173728,16.8088235294117));
#157471=CARTESIAN_POINT('Ctrl Pts',(15.4104571591017,9.54175110365538,15.3147058823531));
#157472=CARTESIAN_POINT('Ctrl Pts',(16.1559070823762,8.04468584505496,13.8205882352942));
#157473=CARTESIAN_POINT('Ctrl Pts',(16.9013570056506,6.54762058645456,12.3264705882353));
#157474=CARTESIAN_POINT('Ctrl Pts',(17.3590292079831,4.93906964482096,10.8323529411765));
#157475=CARTESIAN_POINT('Ctrl Pts',(17.8167014103155,3.33051870318735,9.33823529411759));
#157476=CARTESIAN_POINT('Ctrl Pts',(17.9710104137728,1.66525935159367,7.84411764705895));
#157477=CARTESIAN_POINT('Ctrl Pts',(18.1253194172301,3.32956716117513E-15,
6.35000000000008));
#157478=CARTESIAN_POINT('Ctrl Pts',(17.9710104137728,-1.66525935159367,
4.85588235294121));
#157479=CARTESIAN_POINT('Ctrl Pts',(17.8167014103155,-3.33051870318736,
3.36176470588234));
#157480=CARTESIAN_POINT('Ctrl Pts',(17.3590292079831,-4.93906964482095,
1.86764705882347));
#157481=CARTESIAN_POINT('Ctrl Pts',(16.9013570056506,-6.54762058645456,
0.373529411764828));
#157482=CARTESIAN_POINT('Ctrl Pts',(16.1559070823762,-8.04468584505497,
-1.12058823529404));
#157483=CARTESIAN_POINT('Ctrl Pts',(15.4104571591017,-9.54175110365538,
-2.61470588235291));
#157484=CARTESIAN_POINT('Ctrl Pts',(14.4026149179538,-10.8763499173728,
-4.10882352941178));
#157485=CARTESIAN_POINT('Ctrl Pts',(13.3947726768058,-12.2109487310903,
-5.60294117647064));
#157486=CARTESIAN_POINT('Ctrl Pts',(12.1588589765331,-13.3376329379985,
-7.09705882352929));
#157487=CARTESIAN_POINT('Ctrl Pts',(10.9229452762603,-14.4643171449067,
-8.59117647058816));
#157488=CARTESIAN_POINT('Ctrl Pts',(9.50104767561053,-15.3447188656481,
-10.085294117647));
#157489=CARTESIAN_POINT('Ctrl Pts',(8.07915007496071,-16.2251205863895,
-11.5794117647059));
#157490=CARTESIAN_POINT('Ctrl Pts',(6.51968959134574,-16.8292587962898,
-13.0735294117648));
#157491=CARTESIAN_POINT('Ctrl Pts',(4.96022910773078,-17.4333970061901,
-14.5676470588234));
#157492=CARTESIAN_POINT('Ctrl Pts',(3.31631129755346,-17.7406985030951,
-16.0617647058823));
#157493=CARTESIAN_POINT('Ctrl Pts',(1.67239348737615,-18.048,-17.5558823529411));
#157494=CARTESIAN_POINT('Ctrl Pts',(0.,-18.048,-19.05));
#157495=CARTESIAN_POINT('Ctrl Pts',(-1.67239348737615,-18.048,-20.5441176470589));
#157496=CARTESIAN_POINT('Ctrl Pts',(-3.31631129755346,-17.7406985030951,
-22.0382352941175));
#157497=CARTESIAN_POINT('Ctrl Pts',(-4.96022910773077,-17.4333970061901,
-23.5323529411764));
#157498=CARTESIAN_POINT('Ctrl Pts',(-6.51968959134574,-16.8292587962898,
-25.0264705882353));
#157499=CARTESIAN_POINT('Ctrl Pts',(-8.07915007496071,-16.2251205863895,
-26.5205882352941));
#157500=CARTESIAN_POINT('Ctrl Pts',(-9.50104767561052,-15.3447188656481,
-28.014705882353));
#157501=CARTESIAN_POINT('Ctrl Pts',(-10.9229452762603,-14.4643171449067,
-29.5088235294116));
#157502=CARTESIAN_POINT('Ctrl Pts',(-12.1588589765331,-13.3376329379985,
-31.0029411764705));
#157503=CARTESIAN_POINT('Ctrl Pts',(-13.3947726768058,-12.2109487310903,
-32.4970588235294));
#157504=CARTESIAN_POINT('Ctrl Pts',(-14.4026149179538,-10.8763499173728,
-33.9911764705882));
#157505=CARTESIAN_POINT('Ctrl Pts',(-15.4104571591017,-9.54175110365538,
-35.4852941176471));
#157506=CARTESIAN_POINT('Ctrl Pts',(-16.1559070823762,-8.04468584505497,
-36.9794117647058));
#157507=CARTESIAN_POINT('Ctrl Pts',(-16.9013570056506,-6.54762058645456,
-38.4735294117646));
#157508=CARTESIAN_POINT('Ctrl Pts',(-17.3590292079831,-4.93906964482095,
-39.9676470588235));
#157509=CARTESIAN_POINT('Ctrl Pts',(-17.8167014103155,-3.33051870318735,
-41.4617647058824));
#157510=CARTESIAN_POINT('Ctrl Pts',(-17.9710104137728,-1.66525935159368,
-42.9558823529412));
#157511=CARTESIAN_POINT('Ctrl Pts',(-18.1253194172301,-1.10985572039171E-15,
-44.4499999999999));
#157512=CARTESIAN_POINT('Ctrl Pts',(-17.9710104137728,1.66525935159367,
-45.9441176470587));
#157513=CARTESIAN_POINT('Ctrl Pts',(-17.8167014103155,3.33051870318735,
-47.4382352941176));
#157514=CARTESIAN_POINT('Ctrl Pts',(-17.3590292079831,4.93906964482096,
-48.9323529411765));
#157515=CARTESIAN_POINT('Ctrl Pts',(-16.9013570056506,6.54762058645456,
-50.4264705882354));
#157516=CARTESIAN_POINT('Ctrl Pts',(-16.1559070823762,8.04468584505497,
-51.920588235294));
#157517=CARTESIAN_POINT('Ctrl Pts',(-15.4104571591017,9.54175110365538,
-53.4147058823529));
#157518=CARTESIAN_POINT('Ctrl Pts',(-14.4026149179538,10.8763499173728,
-54.9088235294117));
#157519=CARTESIAN_POINT('Ctrl Pts',(-13.3947726768058,12.2109487310903,
-56.4029411764706));
#157520=CARTESIAN_POINT('Ctrl Pts',(-12.1588589765331,13.3376329379985,
-57.8970588235295));
#157521=CARTESIAN_POINT('Ctrl Pts',(-10.9229452762603,14.4643171449067,
-59.3911764705881));
#157522=CARTESIAN_POINT('Ctrl Pts',(-9.50104767561052,15.3447188656481,
-60.885294117647));
#157523=CARTESIAN_POINT('Ctrl Pts',(-8.07915007496071,16.2251205863895,
-62.3794117647059));
#157524=CARTESIAN_POINT('Ctrl Pts',(-6.51968959134574,16.8292587962898,
-63.8735294117647));
#157525=CARTESIAN_POINT('Ctrl Pts',(-4.96022910773078,17.4333970061901,
-65.3676470588236));
#157526=CARTESIAN_POINT('Ctrl Pts',(-3.31631129755346,17.7406985030951,
-66.8617647058822));
#157527=CARTESIAN_POINT('Ctrl Pts',(-1.67239348737615,18.048,-68.3558823529411));
#157528=CARTESIAN_POINT('Ctrl Pts',(-2.21024254310115E-15,18.048,-69.85));
#157529=CARTESIAN_POINT('Ctrl Pts',(1.67239348737616,18.048,-71.3441176470589));
#157530=CARTESIAN_POINT('Ctrl Pts',(3.31631129755346,17.7406985030951,-72.8382352941177));
#157531=CARTESIAN_POINT('Ctrl Pts',(4.96022910773077,17.4333970061901,-74.3323529411764));
#157532=CARTESIAN_POINT('Ctrl Pts',(6.51968959134575,16.8292587962898,-75.8264705882352));
#157533=CARTESIAN_POINT('Ctrl Pts',(8.07915007496071,16.2251205863895,-77.3205882352941));
#157534=CARTESIAN_POINT('Ctrl Pts',(9.50104767561053,15.3447188656481,-78.814705882353));
#157535=CARTESIAN_POINT('Ctrl Pts',(10.9229452762603,14.4643171449067,-80.3088235294118));
#157536=CARTESIAN_POINT('Ctrl Pts',(12.1588589765331,13.3376329379985,-81.8029411764705));
#157537=CARTESIAN_POINT('Ctrl Pts',(13.3947726768058,12.2109487310903,-83.2970588235294));
#157538=CARTESIAN_POINT('Ctrl Pts',(14.4026149179538,10.8763499173728,-84.7911764705882));
#157539=CARTESIAN_POINT('Ctrl Pts',(15.4104571591017,9.54175110365538,-86.2852941176471));
#157540=CARTESIAN_POINT('Ctrl Pts',(16.1559070823762,8.04468584505496,-87.7794117647059));
#157541=CARTESIAN_POINT('Ctrl Pts',(16.9013570056506,6.54762058645456,-89.2735294117646));
#157542=CARTESIAN_POINT('Ctrl Pts',(17.3590292079831,4.93906964482096,-90.7676470588235));
#157543=CARTESIAN_POINT('Ctrl Pts',(17.8167014103155,3.33051870318735,-92.2617647058823));
#157544=CARTESIAN_POINT('Ctrl Pts',(17.9710104137728,1.66525935159367,-93.7558823529412));
#157545=CARTESIAN_POINT('Ctrl Pts',(18.1253194172301,3.32956716117513E-15,
-95.2500000000001));
#157546=CARTESIAN_POINT('Ctrl Pts',(17.9710104137728,-1.66525935159367,
-96.7441176470587));
#157547=CARTESIAN_POINT('Ctrl Pts',(17.8167014103155,-3.33051870318736,
-98.2382352941176));
#157548=CARTESIAN_POINT('Ctrl Pts',(17.3590292079831,-4.93906964482095,
-99.7323529411764));
#157549=CARTESIAN_POINT('Ctrl Pts',(16.9013570056506,-6.54762058645456,
-101.226470588235));
#157550=CARTESIAN_POINT('Ctrl Pts',(16.1559070823762,-8.04468584505497,
-102.720588235294));
#157551=CARTESIAN_POINT('Ctrl Pts',(15.4104571591017,-9.54175110365538,
-104.214705882353));
#157552=CARTESIAN_POINT('Ctrl Pts',(14.4026149179538,-10.8763499173728,
-105.708823529412));
#157553=CARTESIAN_POINT('Ctrl Pts',(13.3947726768058,-12.2109487310903,
-107.202941176471));
#157554=CARTESIAN_POINT('Ctrl Pts',(12.1588589765331,-13.3376329379985,
-108.697058823529));
#157555=CARTESIAN_POINT('Ctrl Pts',(10.9229452762603,-14.4643171449067,
-110.191176470588));
#157556=CARTESIAN_POINT('Ctrl Pts',(9.50104767561053,-15.3447188656481,
-111.685294117647));
#157557=CARTESIAN_POINT('Ctrl Pts',(8.07915007496071,-16.2251205863895,
-113.179411764706));
#157558=CARTESIAN_POINT('Ctrl Pts',(6.51968959134574,-16.8292587962898,
-114.673529411765));
#157559=CARTESIAN_POINT('Ctrl Pts',(4.96022910773078,-17.4333970061901,
-116.167647058824));
#157560=CARTESIAN_POINT('Ctrl Pts',(3.31631129755346,-17.7406985030951,
-117.661764705882));
#157561=CARTESIAN_POINT('Ctrl Pts',(1.67239348737615,-18.048,-119.155882352941));
#157562=CARTESIAN_POINT('Ctrl Pts',(0.,-18.048,-120.65));
#157563=CARTESIAN_POINT('Ctrl Pts',(-1.67239348737615,-18.048,-122.144117647059));
#157564=CARTESIAN_POINT('Ctrl Pts',(-3.31631129755346,-17.7406985030951,
-123.638235294118));
#157565=CARTESIAN_POINT('Ctrl Pts',(-4.96022910773077,-17.4333970061901,
-125.132352941177));
#157566=CARTESIAN_POINT('Ctrl Pts',(-6.51968959134574,-16.8292587962898,
-126.626470588235));
#157567=CARTESIAN_POINT('Ctrl Pts',(-8.07915007496071,-16.2251205863895,
-128.120588235294));
#157568=CARTESIAN_POINT('Ctrl Pts',(-9.50104767561052,-15.3447188656481,
-129.614705882353));
#157569=CARTESIAN_POINT('Ctrl Pts',(-10.9229452762603,-14.4643171449067,
-131.108823529412));
#157570=CARTESIAN_POINT('Ctrl Pts',(-12.1588589765331,-13.3376329379985,
-132.602941176471));
#157571=CARTESIAN_POINT('Ctrl Pts',(-13.3947726768058,-12.2109487310903,
-134.097058823529));
#157572=CARTESIAN_POINT('Ctrl Pts',(-14.4026149179538,-10.8763499173728,
-135.591176470588));
#157573=CARTESIAN_POINT('Ctrl Pts',(-15.4104571591017,-9.54175110365538,
-137.085294117647));
#157574=CARTESIAN_POINT('Ctrl Pts',(-16.1559070823762,-8.04468584505497,
-138.579411764706));
#157575=CARTESIAN_POINT('Ctrl Pts',(-16.9013570056506,-6.54762058645456,
-140.073529411765));
#157576=CARTESIAN_POINT('Ctrl Pts',(-17.3590292079831,-4.93906964482095,
-141.567647058823));
#157577=CARTESIAN_POINT('Ctrl Pts',(-17.8167014103155,-3.33051870318735,
-143.061764705882));
#157578=CARTESIAN_POINT('Ctrl Pts',(-17.9710104137728,-1.66525935159368,
-144.555882352941));
#157579=CARTESIAN_POINT('Ctrl Pts',(-18.1253194172301,-1.10985572039171E-15,
-146.05));
#157580=CARTESIAN_POINT('Ctrl Pts',(-17.9710104137728,1.66525935159367,
-147.544117647059));
#157581=CARTESIAN_POINT('Ctrl Pts',(-17.8167014103155,3.33051870318735,
-149.038235294118));
#157582=CARTESIAN_POINT('Ctrl Pts',(-17.3590292079831,4.93906964482096,
-150.532352941176));
#157583=CARTESIAN_POINT('Ctrl Pts',(-16.9013570056506,6.54762058645456,
-152.026470588235));
#157584=CARTESIAN_POINT('Ctrl Pts',(-16.1559070823762,8.04468584505497,
-153.520588235294));
#157585=CARTESIAN_POINT('Ctrl Pts',(-15.4104571591017,9.54175110365538,
-155.014705882353));
#157586=CARTESIAN_POINT('Ctrl Pts',(-14.4026149179538,10.8763499173728,
-156.508823529412));
#157587=CARTESIAN_POINT('Ctrl Pts',(-13.3947726768058,12.2109487310903,
-158.002941176471));
#157588=CARTESIAN_POINT('Ctrl Pts',(-12.1588589765331,13.3376329379985,
-159.497058823529));
#157589=CARTESIAN_POINT('Ctrl Pts',(-10.9229452762603,14.4643171449067,
-160.991176470588));
#157590=CARTESIAN_POINT('Ctrl Pts',(-9.50104767561052,15.3447188656481,
-162.485294117647));
#157591=CARTESIAN_POINT('Ctrl Pts',(-8.07915007496071,16.2251205863895,
-163.979411764706));
#157592=CARTESIAN_POINT('Ctrl Pts',(-6.51968959134574,16.8292587962898,
-165.473529411765));
#157593=CARTESIAN_POINT('Ctrl Pts',(-4.96022910773078,17.4333970061901,
-166.967647058824));
#157594=CARTESIAN_POINT('Ctrl Pts',(-3.31631129755346,17.7406985030951,
-168.461764705882));
#157595=CARTESIAN_POINT('Ctrl Pts',(-1.67239348737615,18.048,-169.955882352941));
#157596=CARTESIAN_POINT('Ctrl Pts',(-2.21024254310115E-15,18.048,-171.45));
#157597=CARTESIAN_POINT('Ctrl Pts',(1.67239348737616,18.048,-172.944117647059));
#157598=CARTESIAN_POINT('Ctrl Pts',(3.31631129755346,17.7406985030951,-174.438235294118));
#157599=CARTESIAN_POINT('Ctrl Pts',(4.96022910773077,17.4333970061901,-175.932352941176));
#157600=CARTESIAN_POINT('Ctrl Pts',(6.51968959134575,16.8292587962898,-177.426470588235));
#157601=CARTESIAN_POINT('Ctrl Pts',(8.07915007496071,16.2251205863895,-178.920588235294));
#157602=CARTESIAN_POINT('Ctrl Pts',(9.50104767561053,15.3447188656481,-180.414705882353));
#157603=CARTESIAN_POINT('Ctrl Pts',(10.9229452762603,14.4643171449067,-181.908823529412));
#157604=CARTESIAN_POINT('Ctrl Pts',(12.1588589765331,13.3376329379985,-183.402941176471));
#157605=CARTESIAN_POINT('Ctrl Pts',(13.3947726768058,12.2109487310903,-184.897058823529));
#157606=CARTESIAN_POINT('Ctrl Pts',(14.4026149179538,10.8763499173728,-186.391176470588));
#157607=CARTESIAN_POINT('Ctrl Pts',(15.4104571591017,9.54175110365538,-187.885294117647));
#157608=CARTESIAN_POINT('Ctrl Pts',(16.1559070823762,8.04468584505496,-189.379411764706));
#157609=CARTESIAN_POINT('Ctrl Pts',(16.9013570056506,6.54762058645456,-190.873529411765));
#157610=CARTESIAN_POINT('Ctrl Pts',(17.3590292079831,4.93906964482096,-192.367647058824));
#157611=CARTESIAN_POINT('Ctrl Pts',(17.8167014103155,3.33051870318735,-193.861764705882));
#157612=CARTESIAN_POINT('Ctrl Pts',(17.9710104137728,1.66525935159367,-195.355882352941));
#157613=CARTESIAN_POINT('Ctrl Pts',(18.1253194172301,3.32956716117513E-15,
-196.85));
#157614=CARTESIAN_POINT('Ctrl Pts',(17.9710104137728,-1.66525935159367,
-198.344117647059));
#157615=CARTESIAN_POINT('Ctrl Pts',(17.8167014103155,-3.33051870318736,
-199.838235294118));
#157616=CARTESIAN_POINT('Ctrl Pts',(17.3590292079831,-4.93906964482095,
-201.332352941176));
#157617=CARTESIAN_POINT('Ctrl Pts',(16.9013570056506,-6.54762058645456,
-202.826470588235));
#157618=CARTESIAN_POINT('Ctrl Pts',(16.1559070823762,-8.04468584505497,
-204.320588235294));
#157619=CARTESIAN_POINT('Ctrl Pts',(15.4104571591017,-9.54175110365538,
-205.814705882353));
#157620=CARTESIAN_POINT('Ctrl Pts',(14.4026149179538,-10.8763499173728,
-207.308823529412));
#157621=CARTESIAN_POINT('Ctrl Pts',(13.3947726768058,-12.2109487310903,
-208.80294117647));
#157622=CARTESIAN_POINT('Ctrl Pts',(12.1588589765331,-13.3376329379985,
-210.297058823529));
#157623=CARTESIAN_POINT('Ctrl Pts',(10.9229452762603,-14.4643171449067,
-211.791176470588));
#157624=CARTESIAN_POINT('Ctrl Pts',(9.50104767561053,-15.3447188656481,
-213.285294117647));
#157625=CARTESIAN_POINT('Ctrl Pts',(8.07915007496071,-16.2251205863895,
-214.779411764706));
#157626=CARTESIAN_POINT('Ctrl Pts',(6.51968959134574,-16.8292587962898,
-216.273529411765));
#157627=CARTESIAN_POINT('Ctrl Pts',(4.96022910773078,-17.4333970061901,
-217.767647058823));
#157628=CARTESIAN_POINT('Ctrl Pts',(3.31631129755346,-17.7406985030951,
-219.261764705882));
#157629=CARTESIAN_POINT('Ctrl Pts',(1.67239348737615,-18.048,-220.755882352941));
#157630=CARTESIAN_POINT('Ctrl Pts',(0.,-18.048,-222.25));
#157631=CARTESIAN_POINT('Ctrl Pts',(-1.67239348737615,-18.048,-223.744117647059));
#157632=CARTESIAN_POINT('Ctrl Pts',(-3.31631129755346,-17.7406985030951,
-225.238235294118));
#157633=CARTESIAN_POINT('Ctrl Pts',(-4.96022910773077,-17.4333970061901,
-226.732352941176));
#157634=CARTESIAN_POINT('Ctrl Pts',(-6.51968959134574,-16.8292587962898,
-228.226470588235));
#157635=CARTESIAN_POINT('Ctrl Pts',(-8.07915007496071,-16.2251205863895,
-229.720588235294));
#157636=CARTESIAN_POINT('Ctrl Pts',(-9.50104767561052,-15.3447188656481,
-231.214705882353));
#157637=CARTESIAN_POINT('Ctrl Pts',(-10.9229452762603,-14.4643171449067,
-232.708823529412));
#157638=CARTESIAN_POINT('Ctrl Pts',(-12.1588589765331,-13.3376329379985,
-234.202941176471));
#157639=CARTESIAN_POINT('Ctrl Pts',(-13.3947726768058,-12.2109487310903,
-235.697058823529));
#157640=CARTESIAN_POINT('Ctrl Pts',(-14.4026149179538,-10.8763499173728,
-237.191176470588));
#157641=CARTESIAN_POINT('Ctrl Pts',(-15.4104571591017,-9.54175110365538,
-238.685294117647));
#157642=CARTESIAN_POINT('Ctrl Pts',(-16.1559070823762,-8.04468584505497,
-240.179411764706));
#157643=CARTESIAN_POINT('Ctrl Pts',(-16.9013570056506,-6.54762058645456,
-241.673529411765));
#157644=CARTESIAN_POINT('Ctrl Pts',(-17.3590292079831,-4.93906964482095,
-243.167647058824));
#157645=CARTESIAN_POINT('Ctrl Pts',(-17.8167014103155,-3.33051870318735,
-244.661764705882));
#157646=CARTESIAN_POINT('Ctrl Pts',(-17.9710104137728,-1.66525935159368,
-246.155882352941));
#157647=CARTESIAN_POINT('Ctrl Pts',(-18.1253194172301,-1.10985572039171E-15,
-247.65));
#157648=CARTESIAN_POINT('Ctrl Pts',(-17.9710104137728,1.66525935159367,
-249.144117647059));
#157649=CARTESIAN_POINT('Ctrl Pts',(-17.8167014103155,3.33051870318735,
-250.638235294118));
#157650=CARTESIAN_POINT('Ctrl Pts',(-17.3590292079831,4.93906964482096,
-252.132352941177));
#157651=CARTESIAN_POINT('Ctrl Pts',(-16.9013570056506,6.54762058645456,
-253.626470588235));
#157652=CARTESIAN_POINT('Ctrl Pts',(-16.1559070823762,8.04468584505497,
-255.120588235294));
#157653=CARTESIAN_POINT('Ctrl Pts',(-15.4104571591017,9.54175110365538,
-256.614705882353));
#157654=CARTESIAN_POINT('Ctrl Pts',(-14.4026149179538,10.8763499173728,
-258.108823529412));
#157655=CARTESIAN_POINT('Ctrl Pts',(-13.3947726768058,12.2109487310903,
-259.602941176471));
#157656=CARTESIAN_POINT('Ctrl Pts',(-12.1588589765331,13.3376329379985,
-261.097058823529));
#157657=CARTESIAN_POINT('Ctrl Pts',(-10.9229452762603,14.4643171449067,
-262.591176470588));
#157658=CARTESIAN_POINT('Ctrl Pts',(-9.50104767561052,15.3447188656481,
-264.085294117647));
#157659=CARTESIAN_POINT('Ctrl Pts',(-8.07915007496071,16.2251205863895,
-265.579411764706));
#157660=CARTESIAN_POINT('Ctrl Pts',(-6.51968959134574,16.8292587962898,
-267.073529411765));
#157661=CARTESIAN_POINT('Ctrl Pts',(-4.96022910773078,17.4333970061901,
-268.567647058823));
#157662=CARTESIAN_POINT('Ctrl Pts',(-3.31631129755346,17.7406985030951,
-270.061764705882));
#157663=CARTESIAN_POINT('Ctrl Pts',(-1.67239348737615,18.048,-271.555882352941));
#157664=CARTESIAN_POINT('Ctrl Pts',(-2.21024254310115E-15,18.048,-273.05));
#157665=CARTESIAN_POINT('Ctrl Pts',(1.67239348737616,18.048,-274.544117647059));
#157666=CARTESIAN_POINT('Ctrl Pts',(3.31631129755346,17.7406985030951,-276.038235294118));
#157667=CARTESIAN_POINT('Ctrl Pts',(4.96022910773077,17.4333970061901,-277.532352941176));
#157668=CARTESIAN_POINT('Ctrl Pts',(6.51968959134575,16.8292587962898,-279.026470588235));
#157669=CARTESIAN_POINT('Ctrl Pts',(8.07915007496071,16.2251205863895,-280.520588235294));
#157670=CARTESIAN_POINT('Ctrl Pts',(9.50104767561053,15.3447188656481,-282.014705882353));
#157671=CARTESIAN_POINT('Ctrl Pts',(10.9229452762603,14.4643171449067,-283.508823529412));
#157672=CARTESIAN_POINT('Ctrl Pts',(12.1588589765331,13.3376329379985,-285.002941176471));
#157673=CARTESIAN_POINT('Ctrl Pts',(13.3947726768058,12.2109487310903,-286.497058823529));
#157674=CARTESIAN_POINT('Ctrl Pts',(14.4026149179538,10.8763499173728,-287.991176470588));
#157675=CARTESIAN_POINT('Ctrl Pts',(15.4104571591017,9.54175110365538,-289.485294117647));
#157676=CARTESIAN_POINT('Ctrl Pts',(16.1559070823762,8.04468584505496,-290.979411764706));
#157677=CARTESIAN_POINT('Ctrl Pts',(16.9013570056506,6.54762058645456,-292.473529411765));
#157678=CARTESIAN_POINT('Ctrl Pts',(17.3590292079831,4.93906964482096,-293.967647058824));
#157679=CARTESIAN_POINT('Ctrl Pts',(17.8167014103155,3.33051870318735,-295.461764705882));
#157680=CARTESIAN_POINT('Ctrl Pts',(17.9710104137728,1.66525935159367,-296.955882352941));
#157681=CARTESIAN_POINT('Ctrl Pts',(18.1253194172301,3.32956716117513E-15,
-298.45));
#157682=CARTESIAN_POINT('Ctrl Pts',(17.9710104137728,-1.66525935159367,
-299.944117647059));
#157683=CARTESIAN_POINT('Ctrl Pts',(17.8167014103155,-3.33051870318736,
-301.438235294118));
#157684=CARTESIAN_POINT('Ctrl Pts',(17.3590292079831,-4.93906964482095,
-302.932352941177));
#157685=CARTESIAN_POINT('Ctrl Pts',(16.9013570056506,-6.54762058645456,
-304.426470588235));
#157686=CARTESIAN_POINT('Ctrl Pts',(16.1559070823762,-8.04468584505497,
-305.920588235294));
#157687=CARTESIAN_POINT('Ctrl Pts',(15.4104571591017,-9.54175110365538,
-307.414705882353));
#157688=CARTESIAN_POINT('Ctrl Pts',(14.4026149179538,-10.8763499173728,
-308.908823529412));
#157689=CARTESIAN_POINT('Ctrl Pts',(13.3947726768058,-12.2109487310903,
-310.402941176471));
#157690=CARTESIAN_POINT('Ctrl Pts',(12.1588589765331,-13.3376329379985,
-311.897058823529));
#157691=CARTESIAN_POINT('Ctrl Pts',(10.9229452762603,-14.4643171449067,
-313.391176470588));
#157692=CARTESIAN_POINT('Ctrl Pts',(9.50104767561053,-15.3447188656481,
-314.885294117647));
#157693=CARTESIAN_POINT('Ctrl Pts',(8.07915007496071,-16.2251205863895,
-316.379411764706));
#157694=CARTESIAN_POINT('Ctrl Pts',(6.51968959134574,-16.8292587962898,
-317.873529411765));
#157695=CARTESIAN_POINT('Ctrl Pts',(4.96022910773078,-17.4333970061901,
-319.367647058824));
#157696=CARTESIAN_POINT('Ctrl Pts',(3.31631129755346,-17.7406985030951,
-320.861764705882));
#157697=CARTESIAN_POINT('Ctrl Pts',(1.67239348737615,-18.048,-322.355882352941));
#157698=CARTESIAN_POINT('Ctrl Pts',(0.,-18.048,-323.85));
#157699=CARTESIAN_POINT('Ctrl Pts',(-1.67239348737615,-18.048,-325.344117647059));
#157700=CARTESIAN_POINT('Ctrl Pts',(-3.31631129755346,-17.7406985030951,
-326.838235294118));
#157701=CARTESIAN_POINT('Ctrl Pts',(-4.96022910773077,-17.4333970061901,
-328.332352941176));
#157702=CARTESIAN_POINT('Ctrl Pts',(-6.51968959134574,-16.8292587962898,
-329.826470588235));
#157703=CARTESIAN_POINT('Ctrl Pts',(-8.07915007496071,-16.2251205863895,
-331.320588235294));
#157704=CARTESIAN_POINT('Ctrl Pts',(-9.50104767561052,-15.3447188656481,
-332.814705882353));
#157705=CARTESIAN_POINT('Ctrl Pts',(-10.9229452762603,-14.4643171449067,
-334.308823529412));
#157706=CARTESIAN_POINT('Ctrl Pts',(-12.1588589765331,-13.3376329379985,
-335.80294117647));
#157707=CARTESIAN_POINT('Ctrl Pts',(-13.3947726768058,-12.2109487310903,
-337.297058823529));
#157708=CARTESIAN_POINT('Ctrl Pts',(-14.4026149179538,-10.8763499173728,
-338.791176470588));
#157709=CARTESIAN_POINT('Ctrl Pts',(-15.4104571591017,-9.54175110365538,
-340.285294117647));
#157710=CARTESIAN_POINT('Ctrl Pts',(-16.1559070823762,-8.04468584505497,
-341.779411764706));
#157711=CARTESIAN_POINT('Ctrl Pts',(-16.9013570056506,-6.54762058645456,
-343.273529411765));
#157712=CARTESIAN_POINT('Ctrl Pts',(-17.3590292079831,-4.93906964482095,
-344.767647058823));
#157713=CARTESIAN_POINT('Ctrl Pts',(-17.8167014103155,-3.33051870318735,
-346.261764705882));
#157714=CARTESIAN_POINT('Ctrl Pts',(-17.9710104137728,-1.66525935159368,
-347.755882352941));
#157715=CARTESIAN_POINT('Ctrl Pts',(-18.1253194172301,-1.10985572039171E-15,
-349.25));
#157716=CARTESIAN_POINT('Ctrl Pts',(-17.9710104137728,1.66525935159367,
-350.744117647059));
#157717=CARTESIAN_POINT('Ctrl Pts',(-17.8167014103155,3.33051870318735,
-352.238235294118));
#157718=CARTESIAN_POINT('Ctrl Pts',(-17.3590292079831,4.93906964482096,
-353.732352941176));
#157719=CARTESIAN_POINT('Ctrl Pts',(-16.9013570056506,6.54762058645456,
-355.226470588235));
#157720=CARTESIAN_POINT('Ctrl Pts',(-16.1559070823762,8.04468584505497,
-356.720588235294));
#157721=CARTESIAN_POINT('Ctrl Pts',(-15.4104571591017,9.54175110365538,
-358.214705882353));
#157722=CARTESIAN_POINT('Ctrl Pts',(-14.4026149179538,10.8763499173728,
-359.708823529412));
#157723=CARTESIAN_POINT('Ctrl Pts',(-13.3947726768058,12.2109487310903,
-361.202941176471));
#157724=CARTESIAN_POINT('Ctrl Pts',(-12.1588589765331,13.3376329379985,
-362.697058823529));
#157725=CARTESIAN_POINT('Ctrl Pts',(-10.9229452762603,14.4643171449067,
-364.191176470588));
#157726=CARTESIAN_POINT('Ctrl Pts',(-9.50104767561052,15.3447188656481,
-365.685294117647));
#157727=CARTESIAN_POINT('Ctrl Pts',(-8.07915007496071,16.2251205863895,
-367.179411764706));
#157728=CARTESIAN_POINT('Ctrl Pts',(-6.51968959134574,16.8292587962898,
-368.673529411765));
#157729=CARTESIAN_POINT('Ctrl Pts',(-4.96022910773078,17.4333970061901,
-370.167647058824));
#157730=CARTESIAN_POINT('Ctrl Pts',(-3.31631129755346,17.7406985030951,
-371.661764705882));
#157731=CARTESIAN_POINT('Ctrl Pts',(-1.67239348737615,18.048,-373.155882352941));
#157732=CARTESIAN_POINT('Ctrl Pts',(-2.21024254310115E-15,18.048,-374.65));
#157733=CARTESIAN_POINT('Ctrl Pts',(1.67239348737616,18.048,-376.144117647059));
#157734=CARTESIAN_POINT('Ctrl Pts',(3.31631129755346,17.7406985030951,-377.638235294118));
#157735=CARTESIAN_POINT('Ctrl Pts',(4.96022910773077,17.4333970061901,-379.132352941177));
#157736=CARTESIAN_POINT('Ctrl Pts',(6.51968959134575,16.8292587962898,-380.626470588235));
#157737=CARTESIAN_POINT('Ctrl Pts',(8.07915007496071,16.2251205863895,-382.120588235294));
#157738=CARTESIAN_POINT('Ctrl Pts',(9.50104767561053,15.3447188656481,-383.614705882353));
#157739=CARTESIAN_POINT('Ctrl Pts',(10.9229452762603,14.4643171449067,-385.108823529412));
#157740=CARTESIAN_POINT('Ctrl Pts',(12.1588589765331,13.3376329379985,-386.602941176471));
#157741=CARTESIAN_POINT('Ctrl Pts',(13.3947726768058,12.2109487310903,-388.097058823529));
#157742=CARTESIAN_POINT('Ctrl Pts',(14.4026149179538,10.8763499173728,-389.591176470588));
#157743=CARTESIAN_POINT('Ctrl Pts',(15.4104571591017,9.54175110365538,-391.085294117647));
#157744=CARTESIAN_POINT('Ctrl Pts',(16.1559070823762,8.04468584505496,-392.579411764706));
#157745=CARTESIAN_POINT('Ctrl Pts',(16.9013570056506,6.54762058645456,-394.073529411765));
#157746=CARTESIAN_POINT('Ctrl Pts',(17.3590292079831,4.93906964482096,-395.567647058823));
#157747=CARTESIAN_POINT('Ctrl Pts',(17.8167014103155,3.33051870318735,-397.061764705882));
#157748=CARTESIAN_POINT('Ctrl Pts',(17.9710104137728,1.66525935159367,-398.555882352941));
#157749=CARTESIAN_POINT('Ctrl Pts',(18.1253194172301,3.32956716117513E-15,
-400.05));
#157750=CARTESIAN_POINT('Ctrl Pts',(17.9710104137728,-1.66525935159367,
-401.544117647059));
#157751=CARTESIAN_POINT('Ctrl Pts',(17.8167014103155,-3.33051870318736,
-403.038235294118));
#157752=CARTESIAN_POINT('Ctrl Pts',(17.3590292079831,-4.93906964482095,
-404.532352941176));
#157753=CARTESIAN_POINT('Ctrl Pts',(16.9013570056506,-6.54762058645456,
-406.026470588235));
#157754=CARTESIAN_POINT('Ctrl Pts',(16.1559070823762,-8.04468584505497,
-407.520588235294));
#157755=CARTESIAN_POINT('Ctrl Pts',(15.4104571591017,-9.54175110365538,
-409.014705882353));
#157756=CARTESIAN_POINT('Ctrl Pts',(14.4026149179538,-10.8763499173728,
-410.508823529412));
#157757=CARTESIAN_POINT('Ctrl Pts',(13.3947726768058,-12.2109487310903,
-412.002941176471));
#157758=CARTESIAN_POINT('Ctrl Pts',(12.1588589765331,-13.3376329379985,
-413.497058823529));
#157759=CARTESIAN_POINT('Ctrl Pts',(10.9229452762603,-14.4643171449067,
-414.991176470588));
#157760=CARTESIAN_POINT('Ctrl Pts',(9.50104767561053,-15.3447188656481,
-416.485294117647));
#157761=CARTESIAN_POINT('Ctrl Pts',(8.07915007496071,-16.2251205863895,
-417.979411764706));
#157762=CARTESIAN_POINT('Ctrl Pts',(6.51968959134574,-16.8292587962898,
-419.473529411765));
#157763=CARTESIAN_POINT('Ctrl Pts',(4.96022910773078,-17.4333970061901,
-420.967647058824));
#157764=CARTESIAN_POINT('Ctrl Pts',(3.31631129755346,-17.7406985030951,
-422.461764705882));
#157765=CARTESIAN_POINT('Ctrl Pts',(1.67239348737615,-18.048,-423.955882352941));
#157766=CARTESIAN_POINT('Ctrl Pts',(0.,-18.048,-425.45));
#157767=CARTESIAN_POINT('Ctrl Pts',(-1.67239348737615,-18.048,-426.944117647059));
#157768=CARTESIAN_POINT('Ctrl Pts',(-3.31631129755346,-17.7406985030951,
-428.438235294118));
#157769=CARTESIAN_POINT('Ctrl Pts',(-4.96022910773077,-17.4333970061901,
-429.932352941177));
#157770=CARTESIAN_POINT('Ctrl Pts',(-6.51968959134574,-16.8292587962898,
-431.426470588235));
#157771=CARTESIAN_POINT('Ctrl Pts',(-8.07915007496071,-16.2251205863895,
-432.920588235294));
#157772=CARTESIAN_POINT('Ctrl Pts',(-9.50104767561052,-15.3447188656481,
-434.414705882353));
#157773=CARTESIAN_POINT('Ctrl Pts',(-10.9229452762603,-14.4643171449067,
-435.908823529412));
#157774=CARTESIAN_POINT('Ctrl Pts',(-12.1588589765331,-13.3376329379985,
-437.402941176471));
#157775=CARTESIAN_POINT('Ctrl Pts',(-13.3947726768058,-12.2109487310903,
-438.89705882353));
#157776=CARTESIAN_POINT('Ctrl Pts',(-14.4026149179538,-10.8763499173728,
-440.391176470588));
#157777=CARTESIAN_POINT('Ctrl Pts',(-15.4104571591017,-9.54175110365538,
-441.885294117647));
#157778=CARTESIAN_POINT('Ctrl Pts',(-16.1559070823762,-8.04468584505497,
-443.379411764706));
#157779=CARTESIAN_POINT('Ctrl Pts',(-16.9013570056506,-6.54762058645456,
-444.873529411765));
#157780=CARTESIAN_POINT('Ctrl Pts',(-17.3590292079831,-4.93906964482095,
-446.367647058824));
#157781=CARTESIAN_POINT('Ctrl Pts',(-17.8167014103155,-3.33051870318735,
-447.861764705882));
#157782=CARTESIAN_POINT('Ctrl Pts',(-17.9710104137728,-1.66525935159368,
-449.355882352941));
#157783=CARTESIAN_POINT('Ctrl Pts',(-18.1253194172301,-1.10985572039171E-15,
-450.85));
#157784=CARTESIAN_POINT('Ctrl Pts',(-17.9710104137728,1.66525935159367,
-452.344117647059));
#157785=CARTESIAN_POINT('Ctrl Pts',(-17.8167014103155,3.33051870318735,
-453.838235294118));
#157786=CARTESIAN_POINT('Ctrl Pts',(-17.3590292079831,4.93906964482096,
-455.332352941176));
#157787=CARTESIAN_POINT('Ctrl Pts',(-16.9013570056506,6.54762058645456,
-456.826470588235));
#157788=CARTESIAN_POINT('Ctrl Pts',(-16.1559070823762,8.04468584505497,
-458.320588235294));
#157789=CARTESIAN_POINT('Ctrl Pts',(-15.4104571591017,9.54175110365538,
-459.814705882353));
#157790=CARTESIAN_POINT('Ctrl Pts',(-14.4026149179538,10.8763499173728,
-461.308823529412));
#157791=CARTESIAN_POINT('Ctrl Pts',(-13.3947726768058,12.2109487310903,
-462.802941176471));
#157792=CARTESIAN_POINT('Ctrl Pts',(-12.1588589765331,13.3376329379985,
-464.297058823529));
#157793=CARTESIAN_POINT('Ctrl Pts',(-10.9229452762603,14.4643171449067,
-465.791176470588));
#157794=CARTESIAN_POINT('Ctrl Pts',(-9.50104767561052,15.3447188656481,
-467.285294117647));
#157795=CARTESIAN_POINT('Ctrl Pts',(-8.07915007496071,16.2251205863895,
-468.779411764706));
#157796=CARTESIAN_POINT('Ctrl Pts',(-6.51968959134574,16.8292587962898,
-470.273529411765));
#157797=CARTESIAN_POINT('Ctrl Pts',(-4.96022910773078,17.4333970061901,
-471.767647058824));
#157798=CARTESIAN_POINT('Ctrl Pts',(-3.31631129755346,17.7406985030951,
-473.261764705882));
#157799=CARTESIAN_POINT('Ctrl Pts',(-1.67239348737615,18.048,-474.755882352941));
#157800=CARTESIAN_POINT('Ctrl Pts',(-2.21024254310115E-15,18.048,-476.25));
#157801=CARTESIAN_POINT('Ctrl Pts',(1.67239348737616,18.048,-477.744117647059));
#157802=CARTESIAN_POINT('Ctrl Pts',(3.31631129755346,17.7406985030951,-479.238235294118));
#157803=CARTESIAN_POINT('Ctrl Pts',(4.96022910773077,17.4333970061901,-480.732352941176));
#157804=CARTESIAN_POINT('Ctrl Pts',(6.51968959134575,16.8292587962898,-482.226470588235));
#157805=CARTESIAN_POINT('Ctrl Pts',(8.07915007496071,16.2251205863895,-483.720588235294));
#157806=CARTESIAN_POINT('Ctrl Pts',(9.50104767561053,15.3447188656481,-485.214705882353));
#157807=CARTESIAN_POINT('Ctrl Pts',(10.9229452762603,14.4643171449067,-486.708823529412));
#157808=CARTESIAN_POINT('Ctrl Pts',(12.1588589765331,13.3376329379985,-488.202941176471));
#157809=CARTESIAN_POINT('Ctrl Pts',(13.3947726768058,12.2109487310903,-489.697058823529));
#157810=CARTESIAN_POINT('Ctrl Pts',(14.4026149179538,10.8763499173728,-491.191176470588));
#157811=CARTESIAN_POINT('Ctrl Pts',(15.4104571591017,9.54175110365538,-492.685294117647));
#157812=CARTESIAN_POINT('Ctrl Pts',(16.1559070823762,8.04468584505496,-494.179411764706));
#157813=CARTESIAN_POINT('Ctrl Pts',(16.9013570056506,6.54762058645456,-495.673529411765));
#157814=CARTESIAN_POINT('Ctrl Pts',(17.3590292079831,4.93906964482096,-497.167647058824));
#157815=CARTESIAN_POINT('Ctrl Pts',(17.8167014103155,3.33051870318735,-498.661764705882));
#157816=CARTESIAN_POINT('Ctrl Pts',(17.9710104137728,1.66525935159367,-500.155882352941));
#157817=CARTESIAN_POINT('Ctrl Pts',(18.1253194172301,3.32956716117513E-15,
-501.65));
#157818=CARTESIAN_POINT('Ctrl Pts',(17.9710104137728,-1.66525935159367,
-503.144117647059));
#157819=CARTESIAN_POINT('Ctrl Pts',(17.8167014103155,-3.33051870318736,
-504.638235294118));
#157820=CARTESIAN_POINT('Ctrl Pts',(17.3590292079831,-4.93906964482095,
-506.132352941176));
#157821=CARTESIAN_POINT('Ctrl Pts',(16.9013570056506,-6.54762058645456,
-507.626470588235));
#157822=CARTESIAN_POINT('Ctrl Pts',(16.1559070823762,-8.04468584505497,
-509.120588235294));
#157823=CARTESIAN_POINT('Ctrl Pts',(15.4104571591017,-9.54175110365538,
-510.614705882353));
#157824=CARTESIAN_POINT('Ctrl Pts',(14.4026149179538,-10.8763499173728,
-512.108823529412));
#157825=CARTESIAN_POINT('Ctrl Pts',(13.3947726768058,-12.2109487310903,
-513.602941176471));
#157826=CARTESIAN_POINT('Ctrl Pts',(12.1588589765331,-13.3376329379985,
-515.09705882353));
#157827=CARTESIAN_POINT('Ctrl Pts',(10.9229452762603,-14.4643171449067,
-516.591176470588));
#157828=CARTESIAN_POINT('Ctrl Pts',(9.50104767561053,-15.3447188656481,
-518.085294117647));
#157829=CARTESIAN_POINT('Ctrl Pts',(8.07915007496071,-16.2251205863895,
-519.579411764706));
#157830=CARTESIAN_POINT('Ctrl Pts',(6.51968959134574,-16.8292587962898,
-521.073529411765));
#157831=CARTESIAN_POINT('Ctrl Pts',(4.96022910773078,-17.4333970061901,
-522.567647058823));
#157832=CARTESIAN_POINT('Ctrl Pts',(3.31631129755346,-17.7406985030951,
-524.061764705882));
#157833=CARTESIAN_POINT('Ctrl Pts',(1.67239348737615,-18.048,-525.555882352941));
#157834=CARTESIAN_POINT('Ctrl Pts',(0.,-18.048,-527.05));
#157835=CARTESIAN_POINT('Ctrl Pts',(-1.67239348737615,-18.048,-528.544117647059));
#157836=CARTESIAN_POINT('Ctrl Pts',(-3.31631129755346,-17.7406985030951,
-530.038235294118));
#157837=CARTESIAN_POINT('Ctrl Pts',(-4.96022910773077,-17.4333970061901,
-531.532352941177));
#157838=CARTESIAN_POINT('Ctrl Pts',(-6.51968959134574,-16.8292587962898,
-533.026470588235));
#157839=CARTESIAN_POINT('Ctrl Pts',(-8.07915007496071,-16.2251205863895,
-534.520588235294));
#157840=CARTESIAN_POINT('Ctrl Pts',(-9.50104767561052,-15.3447188656481,
-536.014705882353));
#157841=CARTESIAN_POINT('Ctrl Pts',(-10.9229452762603,-14.4643171449067,
-537.508823529412));
#157842=CARTESIAN_POINT('Ctrl Pts',(-12.1588589765331,-13.3376329379985,
-539.00294117647));
#157843=CARTESIAN_POINT('Ctrl Pts',(-13.3947726768058,-12.2109487310903,
-540.49705882353));
#157844=CARTESIAN_POINT('Ctrl Pts',(-14.4026149179538,-10.8763499173728,
-541.991176470588));
#157845=CARTESIAN_POINT('Ctrl Pts',(-15.4104571591017,-9.54175110365538,
-543.485294117647));
#157846=CARTESIAN_POINT('Ctrl Pts',(-16.1559070823762,-8.04468584505497,
-544.979411764706));
#157847=CARTESIAN_POINT('Ctrl Pts',(-16.9013570056506,-6.54762058645456,
-546.473529411765));
#157848=CARTESIAN_POINT('Ctrl Pts',(-17.3590292079831,-4.93906964482095,
-547.967647058823));
#157849=CARTESIAN_POINT('Ctrl Pts',(-17.8167014103155,-3.33051870318735,
-549.461764705882));
#157850=CARTESIAN_POINT('Ctrl Pts',(-17.9710104137728,-1.66525935159368,
-550.955882352941));
#157851=CARTESIAN_POINT('Ctrl Pts',(-18.1253194172301,-1.10985572039171E-15,
-552.45));
#157852=CARTESIAN_POINT('Ctrl Pts',(-17.9710104137728,1.66525935159367,
-553.944117647059));
#157853=CARTESIAN_POINT('Ctrl Pts',(-17.8167014103155,3.33051870318735,
-555.438235294118));
#157854=CARTESIAN_POINT('Ctrl Pts',(-17.3590292079831,4.93906964482096,
-556.932352941177));
#157855=CARTESIAN_POINT('Ctrl Pts',(-16.9013570056506,6.54762058645456,
-558.426470588235));
#157856=CARTESIAN_POINT('Ctrl Pts',(-16.1559070823762,8.04468584505497,
-559.920588235294));
#157857=CARTESIAN_POINT('Ctrl Pts',(-15.4104571591017,9.54175110365538,
-561.414705882353));
#157858=CARTESIAN_POINT('Ctrl Pts',(-14.4026149179538,10.8763499173728,
-562.908823529412));
#157859=CARTESIAN_POINT('Ctrl Pts',(-13.3947726768058,12.2109487310903,
-564.402941176471));
#157860=CARTESIAN_POINT('Ctrl Pts',(-12.1588589765331,13.3376329379985,
-565.897058823529));
#157861=CARTESIAN_POINT('Ctrl Pts',(-10.9229452762603,14.4643171449067,
-567.391176470588));
#157862=CARTESIAN_POINT('Ctrl Pts',(-9.50104767561052,15.3447188656481,
-568.885294117647));
#157863=CARTESIAN_POINT('Ctrl Pts',(-8.07915007496071,16.2251205863895,
-570.379411764706));
#157864=CARTESIAN_POINT('Ctrl Pts',(-6.51968959134574,16.8292587962898,
-571.873529411765));
#157865=CARTESIAN_POINT('Ctrl Pts',(-4.96022910773078,17.4333970061901,
-573.367647058824));
#157866=CARTESIAN_POINT('Ctrl Pts',(-3.31631129755346,17.7406985030951,
-574.861764705882));
#157867=CARTESIAN_POINT('Ctrl Pts',(-1.67239348737615,18.048,-576.355882352941));
#157868=CARTESIAN_POINT('Ctrl Pts',(-2.21024254310115E-15,18.048,-577.85));
#157869=CARTESIAN_POINT('Ctrl Pts',(1.67239348737616,18.048,-579.344117647059));
#157870=CARTESIAN_POINT('Ctrl Pts',(3.31631129755346,17.7406985030951,-580.838235294117));
#157871=CARTESIAN_POINT('Ctrl Pts',(4.96022910773077,17.4333970061901,-582.332352941176));
#157872=CARTESIAN_POINT('Ctrl Pts',(6.51968959134575,16.8292587962898,-583.826470588235));
#157873=CARTESIAN_POINT('Ctrl Pts',(8.07915007496071,16.2251205863895,-585.320588235294));
#157874=CARTESIAN_POINT('Ctrl Pts',(9.50104767561053,15.3447188656481,-586.814705882353));
#157875=CARTESIAN_POINT('Ctrl Pts',(10.9229452762603,14.4643171449067,-588.308823529412));
#157876=CARTESIAN_POINT('Ctrl Pts',(12.1588589765331,13.3376329379985,-589.802941176471));
#157877=CARTESIAN_POINT('Ctrl Pts',(13.3947726768058,12.2109487310903,-591.297058823529));
#157878=CARTESIAN_POINT('Ctrl Pts',(14.4026149179538,10.8763499173728,-592.791176470588));
#157879=CARTESIAN_POINT('Ctrl Pts',(15.4104571591017,9.54175110365538,-594.285294117647));
#157880=CARTESIAN_POINT('Ctrl Pts',(16.1559070823762,8.04468584505496,-595.779411764706));
#157881=CARTESIAN_POINT('Ctrl Pts',(16.9013570056506,6.54762058645456,-597.273529411765));
#157882=CARTESIAN_POINT('Ctrl Pts',(17.3590292079831,4.93906964482096,-598.767647058824));
#157883=CARTESIAN_POINT('Ctrl Pts',(17.8167014103155,3.33051870318735,-600.261764705882));
#157884=CARTESIAN_POINT('Ctrl Pts',(17.9710104137728,1.66525935159367,-601.755882352941));
#157885=CARTESIAN_POINT('Ctrl Pts',(18.1253194172301,3.32956716117513E-15,
-603.25));
#157886=CARTESIAN_POINT('Ctrl Pts',(17.9710104137728,-1.66525935159367,
-604.744117647059));
#157887=CARTESIAN_POINT('Ctrl Pts',(17.8167014103155,-3.33051870318736,
-606.238235294118));
#157888=CARTESIAN_POINT('Ctrl Pts',(17.3590292079831,-4.93906964482095,
-607.732352941176));
#157889=CARTESIAN_POINT('Ctrl Pts',(16.9013570056506,-6.54762058645456,
-609.226470588235));
#157890=CARTESIAN_POINT('Ctrl Pts',(16.1559070823762,-8.04468584505497,
-610.720588235294));
#157891=CARTESIAN_POINT('Ctrl Pts',(15.4104571591017,-9.54175110365538,
-612.214705882353));
#157892=CARTESIAN_POINT('Ctrl Pts',(14.4026149179538,-10.8763499173728,
-613.708823529412));
#157893=CARTESIAN_POINT('Ctrl Pts',(13.3947726768058,-12.2109487310903,
-615.202941176471));
#157894=CARTESIAN_POINT('Ctrl Pts',(12.1588589765331,-13.3376329379985,
-616.697058823529));
#157895=CARTESIAN_POINT('Ctrl Pts',(10.9229452762603,-14.4643171449067,
-618.191176470588));
#157896=CARTESIAN_POINT('Ctrl Pts',(9.50104767561053,-15.3447188656481,
-619.685294117647));
#157897=CARTESIAN_POINT('Ctrl Pts',(8.07915007496071,-16.2251205863895,
-621.179411764706));
#157898=CARTESIAN_POINT('Ctrl Pts',(6.51968959134574,-16.8292587962898,
-622.673529411764));
#157899=CARTESIAN_POINT('Ctrl Pts',(4.96022910773078,-17.4333970061901,
-624.167647058823));
#157900=CARTESIAN_POINT('Ctrl Pts',(3.31631129755346,-17.7406985030951,
-625.661764705882));
#157901=CARTESIAN_POINT('Ctrl Pts',(1.67239348737615,-18.048,-627.155882352941));
#157902=CARTESIAN_POINT('Ctrl Pts',(0.,-18.048,-628.65));
#157903=CARTESIAN_POINT('Ctrl Pts',(-1.67239348737615,-18.048,-630.144117647059));
#157904=CARTESIAN_POINT('Ctrl Pts',(-3.31631129755346,-17.7406985030951,
-631.638235294118));
#157905=CARTESIAN_POINT('Ctrl Pts',(-4.96022910773077,-17.4333970061901,
-633.132352941176));
#157906=CARTESIAN_POINT('Ctrl Pts',(-6.51968959134574,-16.8292587962898,
-634.626470588235));
#157907=CARTESIAN_POINT('Ctrl Pts',(-8.07915007496071,-16.2251205863895,
-636.120588235294));
#157908=CARTESIAN_POINT('Ctrl Pts',(-9.50104767561052,-15.3447188656481,
-637.614705882353));
#157909=CARTESIAN_POINT('Ctrl Pts',(-10.9229452762603,-14.4643171449067,
-639.108823529412));
#157910=CARTESIAN_POINT('Ctrl Pts',(-12.1588589765331,-13.3376329379985,
-640.60294117647));
#157911=CARTESIAN_POINT('Ctrl Pts',(-13.3947726768058,-12.2109487310903,
-642.097058823529));
#157912=CARTESIAN_POINT('Ctrl Pts',(-14.4026149179538,-10.8763499173728,
-643.591176470588));
#157913=CARTESIAN_POINT('Ctrl Pts',(-15.4104571591017,-9.54175110365538,
-645.085294117647));
#157914=CARTESIAN_POINT('Ctrl Pts',(-16.1559070823762,-8.04468584505497,
-646.579411764706));
#157915=CARTESIAN_POINT('Ctrl Pts',(-16.9013570056506,-6.54762058645456,
-648.073529411765));
#157916=CARTESIAN_POINT('Ctrl Pts',(-17.3590292079831,-4.93906964482095,
-649.567647058824));
#157917=CARTESIAN_POINT('Ctrl Pts',(-17.8167014103155,-3.33051870318735,
-651.061764705883));
#157918=CARTESIAN_POINT('Ctrl Pts',(-17.9710104137728,-1.66525935159368,
-652.555882352941));
#157919=CARTESIAN_POINT('Ctrl Pts',(-18.1253194172301,-1.10985572039171E-15,
-654.05));
#157920=CARTESIAN_POINT('Ctrl Pts',(-17.9710104137728,1.66525935159367,
-655.544117647059));
#157921=CARTESIAN_POINT('Ctrl Pts',(-17.8167014103155,3.33051870318735,
-657.038235294117));
#157922=CARTESIAN_POINT('Ctrl Pts',(-17.3590292079831,4.93906964482096,
-658.532352941177));
#157923=CARTESIAN_POINT('Ctrl Pts',(-16.9013570056506,6.54762058645456,
-660.026470588235));
#157924=CARTESIAN_POINT('Ctrl Pts',(-16.1559070823762,8.04468584505497,
-661.520588235294));
#157925=CARTESIAN_POINT('Ctrl Pts',(-15.4104571591017,9.54175110365538,
-663.014705882353));
#157926=CARTESIAN_POINT('Ctrl Pts',(-14.4026149179538,10.8763499173728,
-664.508823529412));
#157927=CARTESIAN_POINT('Ctrl Pts',(-13.3947726768058,12.2109487310903,
-666.002941176471));
#157928=CARTESIAN_POINT('Ctrl Pts',(-12.1588589765331,13.3376329379985,
-667.497058823529));
#157929=CARTESIAN_POINT('Ctrl Pts',(-10.9229452762603,14.4643171449067,
-668.991176470588));
#157930=CARTESIAN_POINT('Ctrl Pts',(-9.50104767561052,15.3447188656481,
-670.485294117647));
#157931=CARTESIAN_POINT('Ctrl Pts',(-8.07915007496071,16.2251205863895,
-671.979411764706));
#157932=CARTESIAN_POINT('Ctrl Pts',(-6.51968959134574,16.8292587962898,
-673.473529411765));
#157933=CARTESIAN_POINT('Ctrl Pts',(-4.96022910773078,17.4333970061901,
-674.967647058824));
#157934=CARTESIAN_POINT('Ctrl Pts',(-3.31631129755346,17.7406985030951,
-676.461764705882));
#157935=CARTESIAN_POINT('Ctrl Pts',(-1.67239348737615,18.048,-677.955882352941));
#157936=CARTESIAN_POINT('Ctrl Pts',(-2.21024254310115E-15,18.048,-679.45));
#157937=CARTESIAN_POINT('Ctrl Pts',(1.67239348737616,18.048,-680.944117647059));
#157938=CARTESIAN_POINT('Ctrl Pts',(3.31631129755346,17.7406985030951,-682.438235294117));
#157939=CARTESIAN_POINT('Ctrl Pts',(4.96022910773077,17.4333970061901,-683.932352941176));
#157940=CARTESIAN_POINT('Ctrl Pts',(6.51968959134575,16.8292587962898,-685.426470588235));
#157941=CARTESIAN_POINT('Ctrl Pts',(8.07915007496071,16.2251205863895,-686.920588235294));
#157942=CARTESIAN_POINT('Ctrl Pts',(9.50104767561053,15.3447188656481,-688.414705882353));
#157943=CARTESIAN_POINT('Ctrl Pts',(10.9229452762603,14.4643171449067,-689.908823529412));
#157944=CARTESIAN_POINT('Ctrl Pts',(12.1588589765331,13.3376329379985,-691.402941176471));
#157945=CARTESIAN_POINT('Ctrl Pts',(13.3947726768058,12.2109487310903,-692.89705882353));
#157946=CARTESIAN_POINT('Ctrl Pts',(14.4026149179538,10.8763499173728,-694.391176470588));
#157947=CARTESIAN_POINT('Ctrl Pts',(15.4104571591017,9.54175110365538,-695.885294117647));
#157948=CARTESIAN_POINT('Ctrl Pts',(16.1559070823762,8.04468584505496,-697.379411764706));
#157949=CARTESIAN_POINT('Ctrl Pts',(16.9013570056506,6.54762058645456,-698.873529411764));
#157950=CARTESIAN_POINT('Ctrl Pts',(17.3590292079831,4.93906964482096,-700.367647058823));
#157951=CARTESIAN_POINT('Ctrl Pts',(17.8167014103155,3.33051870318735,-701.861764705882));
#157952=CARTESIAN_POINT('Ctrl Pts',(17.9710104137728,1.66525935159367,-703.355882352941));
#157953=CARTESIAN_POINT('Ctrl Pts',(18.1253194172301,3.32956716117513E-15,
-704.85));
#157954=CARTESIAN_POINT('Ctrl Pts',(17.9710104137728,-1.66525935159367,
-706.344117647059));
#157955=CARTESIAN_POINT('Ctrl Pts',(17.8167014103155,-3.33051870318736,
-707.838235294118));
#157956=CARTESIAN_POINT('Ctrl Pts',(17.3590292079831,-4.93906964482095,
-709.332352941177));
#157957=CARTESIAN_POINT('Ctrl Pts',(16.9013570056506,-6.54762058645456,
-710.826470588236));
#157958=CARTESIAN_POINT('Ctrl Pts',(16.1559070823762,-8.04468584505497,
-712.320588235294));
#157959=CARTESIAN_POINT('Ctrl Pts',(15.4104571591017,-9.54175110365538,
-713.814705882353));
#157960=CARTESIAN_POINT('Ctrl Pts',(14.4026149179538,-10.8763499173728,
-715.308823529412));
#157961=CARTESIAN_POINT('Ctrl Pts',(13.3947726768058,-12.2109487310903,
-716.802941176471));
#157962=CARTESIAN_POINT('Ctrl Pts',(12.1588589765331,-13.3376329379985,
-718.297058823529));
#157963=CARTESIAN_POINT('Ctrl Pts',(10.9229452762603,-14.4643171449067,
-719.791176470588));
#157964=CARTESIAN_POINT('Ctrl Pts',(9.50104767561053,-15.3447188656481,
-721.285294117647));
#157965=CARTESIAN_POINT('Ctrl Pts',(8.07915007496071,-16.2251205863895,
-722.779411764706));
#157966=CARTESIAN_POINT('Ctrl Pts',(6.51968959134574,-16.8292587962898,
-724.273529411765));
#157967=CARTESIAN_POINT('Ctrl Pts',(4.96022910773078,-17.4333970061901,
-725.767647058824));
#157968=CARTESIAN_POINT('Ctrl Pts',(3.31631129755346,-17.7406985030951,
-727.261764705882));
#157969=CARTESIAN_POINT('Ctrl Pts',(1.67239348737615,-18.048,-728.755882352941));
#157970=CARTESIAN_POINT('Ctrl Pts',(0.,-18.048,-730.25));
#157971=CARTESIAN_POINT('Ctrl Pts',(-1.67239348737615,-18.048,-731.744117647059));
#157972=CARTESIAN_POINT('Ctrl Pts',(-3.31631129755346,-17.7406985030951,
-733.238235294118));
#157973=CARTESIAN_POINT('Ctrl Pts',(-4.96022910773077,-17.4333970061901,
-734.732352941177));
#157974=CARTESIAN_POINT('Ctrl Pts',(-6.51968959134574,-16.8292587962898,
-736.226470588235));
#157975=CARTESIAN_POINT('Ctrl Pts',(-8.07915007496071,-16.2251205863895,
-737.720588235294));
#157976=CARTESIAN_POINT('Ctrl Pts',(-9.50104767561052,-15.3447188656481,
-739.214705882353));
#157977=CARTESIAN_POINT('Ctrl Pts',(-10.9229452762603,-14.4643171449067,
-740.708823529412));
#157978=CARTESIAN_POINT('Ctrl Pts',(-12.1588589765331,-13.3376329379985,
-742.20294117647));
#157979=CARTESIAN_POINT('Ctrl Pts',(-13.3947726768058,-12.2109487310903,
-743.697058823529));
#157980=CARTESIAN_POINT('Ctrl Pts',(-14.4026149179538,-10.8763499173728,
-745.191176470588));
#157981=CARTESIAN_POINT('Ctrl Pts',(-15.4104571591017,-9.54175110365538,
-746.685294117647));
#157982=CARTESIAN_POINT('Ctrl Pts',(-16.1559070823762,-8.04468584505497,
-748.179411764706));
#157983=CARTESIAN_POINT('Ctrl Pts',(-16.9013570056506,-6.54762058645456,
-749.673529411765));
#157984=CARTESIAN_POINT('Ctrl Pts',(-17.3590292079831,-4.93906964482095,
-751.167647058824));
#157985=CARTESIAN_POINT('Ctrl Pts',(-17.8167014103155,-3.33051870318735,
-752.661764705882));
#157986=CARTESIAN_POINT('Ctrl Pts',(-17.9710104137728,-1.66525935159368,
-754.155882352941));
#157987=CARTESIAN_POINT('Ctrl Pts',(-18.1253194172301,-1.10985572039171E-15,
-755.65));
#157988=CARTESIAN_POINT('Ctrl Pts',(-17.9710104137728,1.66525935159367,
-757.144117647059));
#157989=CARTESIAN_POINT('Ctrl Pts',(-17.8167014103155,3.33051870318735,
-758.638235294118));
#157990=CARTESIAN_POINT('Ctrl Pts',(-17.3590292079831,4.93906964482096,
-760.132352941176));
#157991=CARTESIAN_POINT('Ctrl Pts',(-16.9013570056506,6.54762058645456,
-761.626470588235));
#157992=CARTESIAN_POINT('Ctrl Pts',(-16.1559070823762,8.04468584505497,
-763.120588235294));
#157993=CARTESIAN_POINT('Ctrl Pts',(-15.4104571591017,9.54175110365538,
-764.614705882353));
#157994=CARTESIAN_POINT('Ctrl Pts',(-14.4026149179538,10.8763499173728,
-766.108823529412));
#157995=CARTESIAN_POINT('Ctrl Pts',(-13.3947726768058,12.2109487310903,
-767.602941176471));
#157996=CARTESIAN_POINT('Ctrl Pts',(-12.1588589765331,13.3376329379985,
-769.09705882353));
#157997=CARTESIAN_POINT('Ctrl Pts',(-10.9229452762603,14.4643171449067,
-770.591176470589));
#157998=CARTESIAN_POINT('Ctrl Pts',(-9.50104767561052,15.3447188656481,
-772.085294117647));
#157999=CARTESIAN_POINT('Ctrl Pts',(-8.07915007496071,16.2251205863895,
-773.579411764706));
#158000=CARTESIAN_POINT('Ctrl Pts',(-6.51968959134574,16.8292587962898,
-775.073529411765));
#158001=CARTESIAN_POINT('Ctrl Pts',(-4.96022910773078,17.4333970061901,
-776.567647058824));
#158002=CARTESIAN_POINT('Ctrl Pts',(-3.31631129755346,17.7406985030951,
-778.061764705882));
#158003=CARTESIAN_POINT('Ctrl Pts',(-1.67239348737615,18.048,-779.555882352941));
#158004=CARTESIAN_POINT('Ctrl Pts',(-2.21024254310115E-15,18.048,-781.05));
#158005=CARTESIAN_POINT('Ctrl Pts',(1.67239348737616,18.048,-782.544117647059));
#158006=CARTESIAN_POINT('Ctrl Pts',(3.31631129755346,17.7406985030951,-784.038235294118));
#158007=CARTESIAN_POINT('Ctrl Pts',(4.96022910773077,17.4333970061901,-785.532352941177));
#158008=CARTESIAN_POINT('Ctrl Pts',(6.51968959134575,16.8292587962898,-787.026470588235));
#158009=CARTESIAN_POINT('Ctrl Pts',(8.07915007496071,16.2251205863895,-788.520588235294));
#158010=CARTESIAN_POINT('Ctrl Pts',(9.50104767561053,15.3447188656481,-790.014705882353));
#158011=CARTESIAN_POINT('Ctrl Pts',(10.9229452762603,14.4643171449067,-791.508823529412));
#158012=CARTESIAN_POINT('Ctrl Pts',(12.1588589765331,13.3376329379985,-793.002941176471));
#158013=CARTESIAN_POINT('Ctrl Pts',(13.3947726768058,12.2109487310903,-794.497058823529));
#158014=CARTESIAN_POINT('Ctrl Pts',(14.4026149179538,10.8763499173728,-795.991176470588));
#158015=CARTESIAN_POINT('Ctrl Pts',(15.4104571591017,9.54175110365538,-797.485294117647));
#158016=CARTESIAN_POINT('Ctrl Pts',(16.1559070823762,8.04468584505496,-798.979411764706));
#158017=CARTESIAN_POINT('Ctrl Pts',(16.9013570056506,6.54762058645456,-800.473529411765));
#158018=CARTESIAN_POINT('Ctrl Pts',(17.3590292079831,4.93906964482096,-801.967647058823));
#158019=CARTESIAN_POINT('Ctrl Pts',(17.8167014103155,3.33051870318735,-803.461764705882));
#158020=CARTESIAN_POINT('Ctrl Pts',(17.9710104137728,1.66525935159367,-804.955882352941));
#158021=CARTESIAN_POINT('Ctrl Pts',(18.1253194172301,3.32956716117513E-15,
-806.45));
#158022=CARTESIAN_POINT('Ctrl Pts',(17.9710104137728,-1.66525935159367,
-807.944117647059));
#158023=CARTESIAN_POINT('Ctrl Pts',(17.8167014103155,-3.33051870318736,
-809.438235294118));
#158024=CARTESIAN_POINT('Ctrl Pts',(17.3590292079831,-4.93906964482095,
-810.932352941177));
#158025=CARTESIAN_POINT('Ctrl Pts',(16.9013570056506,-6.54762058645456,
-812.426470588235));
#158026=CARTESIAN_POINT('Ctrl Pts',(16.1559070823762,-8.04468584505497,
-813.920588235294));
#158027=CARTESIAN_POINT('Ctrl Pts',(15.4104571591017,-9.54175110365538,
-815.414705882353));
#158028=CARTESIAN_POINT('Ctrl Pts',(14.4026149179538,-10.8763499173728,
-816.908823529412));
#158029=CARTESIAN_POINT('Ctrl Pts',(13.3947726768058,-12.2109487310903,
-818.40294117647));
#158030=CARTESIAN_POINT('Ctrl Pts',(12.1588589765331,-13.3376329379985,
-819.897058823529));
#158031=CARTESIAN_POINT('Ctrl Pts',(10.9229452762603,-14.4643171449067,
-821.391176470588));
#158032=CARTESIAN_POINT('Ctrl Pts',(9.50104767561053,-15.3447188656481,
-822.885294117647));
#158033=CARTESIAN_POINT('Ctrl Pts',(8.07915007496071,-16.2251205863895,
-824.379411764706));
#158034=CARTESIAN_POINT('Ctrl Pts',(6.51968959134574,-16.8292587962898,
-825.873529411765));
#158035=CARTESIAN_POINT('Ctrl Pts',(4.96022910773078,-17.4333970061901,
-827.367647058824));
#158036=CARTESIAN_POINT('Ctrl Pts',(3.31631129755346,-17.7406985030951,
-828.861764705882));
#158037=CARTESIAN_POINT('Ctrl Pts',(1.67239348737615,-18.048,-830.355882352941));
#158038=CARTESIAN_POINT('Ctrl Pts',(0.,-18.048,-831.85));
#158039=CARTESIAN_POINT('Ctrl Pts',(-1.67239348737615,-18.048,-833.344117647059));
#158040=CARTESIAN_POINT('Ctrl Pts',(-3.31631129755346,-17.7406985030951,
-834.838235294118));
#158041=CARTESIAN_POINT('Ctrl Pts',(-4.96022910773077,-17.4333970061901,
-836.332352941177));
#158042=CARTESIAN_POINT('Ctrl Pts',(-6.51968959134574,-16.8292587962898,
-837.826470588235));
#158043=CARTESIAN_POINT('Ctrl Pts',(-8.07915007496071,-16.2251205863895,
-839.320588235294));
#158044=CARTESIAN_POINT('Ctrl Pts',(-9.50104767561052,-15.3447188656481,
-840.814705882353));
#158045=CARTESIAN_POINT('Ctrl Pts',(-10.9229452762603,-14.4643171449067,
-842.308823529412));
#158046=CARTESIAN_POINT('Ctrl Pts',(-12.1588589765331,-13.3376329379985,
-843.802941176471));
#158047=CARTESIAN_POINT('Ctrl Pts',(-13.3947726768058,-12.2109487310903,
-845.29705882353));
#158048=CARTESIAN_POINT('Ctrl Pts',(-14.4026149179538,-10.8763499173728,
-846.791176470588));
#158049=CARTESIAN_POINT('Ctrl Pts',(-15.4104571591017,-9.54175110365538,
-848.285294117647));
#158050=CARTESIAN_POINT('Ctrl Pts',(-16.1559070823762,-8.04468584505497,
-849.779411764706));
#158051=CARTESIAN_POINT('Ctrl Pts',(-16.9013570056506,-6.54762058645456,
-851.273529411765));
#158052=CARTESIAN_POINT('Ctrl Pts',(-17.3590292079831,-4.93906964482095,
-852.767647058824));
#158053=CARTESIAN_POINT('Ctrl Pts',(-17.8167014103155,-3.33051870318735,
-854.261764705882));
#158054=CARTESIAN_POINT('Ctrl Pts',(-17.9710104137728,-1.66525935159368,
-855.755882352941));
#158055=CARTESIAN_POINT('Ctrl Pts',(-18.1253194172301,-1.10985572039171E-15,
-857.25));
#158056=CARTESIAN_POINT('Ctrl Pts',(-17.9710104137728,1.66525935159367,
-858.744117647059));
#158057=CARTESIAN_POINT('Ctrl Pts',(-17.8167014103155,3.33051870318735,
-860.238235294118));
#158058=CARTESIAN_POINT('Ctrl Pts',(-17.3590292079831,4.93906964482096,
-861.732352941176));
#158059=CARTESIAN_POINT('Ctrl Pts',(-16.9013570056506,6.54762058645456,
-863.226470588235));
#158060=CARTESIAN_POINT('Ctrl Pts',(-16.1559070823762,8.04468584505497,
-864.720588235294));
#158061=CARTESIAN_POINT('Ctrl Pts',(-15.4104571591017,9.54175110365538,
-866.214705882353));
#158062=CARTESIAN_POINT('Ctrl Pts',(-14.4026149179538,10.8763499173728,
-867.708823529412));
#158063=CARTESIAN_POINT('Ctrl Pts',(-13.3947726768058,12.2109487310903,
-869.202941176471));
#158064=CARTESIAN_POINT('Ctrl Pts',(-12.1588589765331,13.3376329379985,
-870.697058823529));
#158065=CARTESIAN_POINT('Ctrl Pts',(-10.9229452762603,14.4643171449067,
-872.191176470589));
#158066=CARTESIAN_POINT('Ctrl Pts',(-9.50104767561052,15.3447188656481,
-873.685294117647));
#158067=CARTESIAN_POINT('Ctrl Pts',(-8.07915007496071,16.2251205863895,
-875.179411764706));
#158068=CARTESIAN_POINT('Ctrl Pts',(-6.51968959134574,16.8292587962898,
-876.673529411764));
#158069=CARTESIAN_POINT('Ctrl Pts',(-4.96022910773078,17.4333970061901,
-878.167647058823));
#158070=CARTESIAN_POINT('Ctrl Pts',(-3.31631129755346,17.7406985030951,
-879.661764705882));
#158071=CARTESIAN_POINT('Ctrl Pts',(-1.67239348737615,18.048,-881.155882352941));
#158072=CARTESIAN_POINT('Ctrl Pts',(-2.21024254310115E-15,18.048,-882.65));
#158073=CARTESIAN_POINT('Ctrl Pts',(1.67239348737616,18.048,-884.144117647059));
#158074=CARTESIAN_POINT('Ctrl Pts',(3.31631129755346,17.7406985030951,-885.638235294118));
#158075=CARTESIAN_POINT('Ctrl Pts',(4.96022910773077,17.4333970061901,-887.132352941177));
#158076=CARTESIAN_POINT('Ctrl Pts',(6.51968959134575,16.8292587962898,-888.626470588235));
#158077=CARTESIAN_POINT('Ctrl Pts',(8.07915007496071,16.2251205863895,-890.120588235294));
#158078=CARTESIAN_POINT('Ctrl Pts',(9.50104767561053,15.3447188656481,-891.614705882353));
#158079=CARTESIAN_POINT('Ctrl Pts',(10.9229452762603,14.4643171449067,-893.108823529412));
#158080=CARTESIAN_POINT('Ctrl Pts',(12.1588589765331,13.3376329379985,-894.60294117647));
#158081=CARTESIAN_POINT('Ctrl Pts',(13.3947726768058,12.2109487310903,-896.09705882353));
#158082=CARTESIAN_POINT('Ctrl Pts',(14.4026149179538,10.8763499173728,-897.591176470588));
#158083=CARTESIAN_POINT('Ctrl Pts',(15.4104571591017,9.54175110365538,-899.085294117647));
#158084=CARTESIAN_POINT('Ctrl Pts',(16.1559070823762,8.04468584505496,-900.579411764706));
#158085=CARTESIAN_POINT('Ctrl Pts',(16.9013570056506,6.54762058645456,-902.073529411765));
#158086=CARTESIAN_POINT('Ctrl Pts',(17.3590292079831,4.93906964482096,-903.567647058824));
#158087=CARTESIAN_POINT('Ctrl Pts',(17.8167014103155,3.33051870318735,-905.061764705883));
#158088=CARTESIAN_POINT('Ctrl Pts',(17.9710104137728,1.66525935159367,-906.555882352941));
#158089=CARTESIAN_POINT('Ctrl Pts',(18.1253194172301,3.32956716117513E-15,
-908.05));
#158090=CARTESIAN_POINT('Ctrl Pts',(17.9710104137728,-1.66525935159367,
-909.544117647059));
#158091=CARTESIAN_POINT('Ctrl Pts',(17.8167014103155,-3.33051870318736,
-911.038235294118));
#158092=CARTESIAN_POINT('Ctrl Pts',(17.3590292079831,-4.93906964482095,
-912.532352941176));
#158093=CARTESIAN_POINT('Ctrl Pts',(16.9013570056506,-6.54762058645456,
-914.026470588235));
#158094=CARTESIAN_POINT('Ctrl Pts',(16.1559070823762,-8.04468584505497,
-915.520588235294));
#158095=CARTESIAN_POINT('Ctrl Pts',(15.4104571591017,-9.54175110365538,
-917.014705882353));
#158096=CARTESIAN_POINT('Ctrl Pts',(14.4026149179538,-10.8763499173728,
-918.508823529412));
#158097=CARTESIAN_POINT('Ctrl Pts',(13.3947726768058,-12.2109487310903,
-920.002941176471));
#158098=CARTESIAN_POINT('Ctrl Pts',(12.1588589765331,-13.3376329379985,
-921.497058823529));
#158099=CARTESIAN_POINT('Ctrl Pts',(10.9229452762603,-14.4643171449067,
-922.991176470588));
#158100=CARTESIAN_POINT('Ctrl Pts',(9.50104767561053,-15.3447188656481,
-924.485294117647));
#158101=CARTESIAN_POINT('Ctrl Pts',(8.07915007496071,-16.2251205863895,
-925.979411764706));
#158102=CARTESIAN_POINT('Ctrl Pts',(6.51968959134574,-16.8292587962898,
-927.473529411765));
#158103=CARTESIAN_POINT('Ctrl Pts',(4.96022910773078,-17.4333970061901,
-928.967647058823));
#158104=CARTESIAN_POINT('Ctrl Pts',(3.31631129755346,-17.7406985030951,
-930.461764705883));
#158105=CARTESIAN_POINT('Ctrl Pts',(1.67239348737615,-18.048,-931.955882352941));
#158106=CARTESIAN_POINT('Ctrl Pts',(0.,-18.048,-933.45));
#158107=CARTESIAN_POINT('Ctrl Pts',(-1.67239348737615,-18.048,-934.944117647059));
#158108=CARTESIAN_POINT('Ctrl Pts',(-3.31631129755346,-17.7406985030951,
-936.438235294117));
#158109=CARTESIAN_POINT('Ctrl Pts',(-4.96022910773077,-17.4333970061901,
-937.932352941177));
#158110=CARTESIAN_POINT('Ctrl Pts',(-6.51968959134574,-16.8292587962898,
-939.426470588235));
#158111=CARTESIAN_POINT('Ctrl Pts',(-8.07915007496071,-16.2251205863895,
-940.920588235294));
#158112=CARTESIAN_POINT('Ctrl Pts',(-9.50104767561052,-15.3447188656481,
-942.414705882353));
#158113=CARTESIAN_POINT('Ctrl Pts',(-10.9229452762603,-14.4643171449067,
-943.908823529412));
#158114=CARTESIAN_POINT('Ctrl Pts',(-12.1588589765331,-13.3376329379985,
-945.402941176471));
#158115=CARTESIAN_POINT('Ctrl Pts',(-13.3947726768058,-12.2109487310903,
-946.89705882353));
#158116=CARTESIAN_POINT('Ctrl Pts',(-14.4026149179538,-10.8763499173728,
-948.391176470588));
#158117=CARTESIAN_POINT('Ctrl Pts',(-15.4104571591017,-9.54175110365538,
-949.885294117647));
#158118=CARTESIAN_POINT('Ctrl Pts',(-16.1559070823762,-8.04468584505497,
-951.379411764706));
#158119=CARTESIAN_POINT('Ctrl Pts',(-16.9013570056506,-6.54762058645456,
-952.873529411765));
#158120=CARTESIAN_POINT('Ctrl Pts',(-17.3590292079831,-4.93906964482095,
-954.367647058824));
#158121=CARTESIAN_POINT('Ctrl Pts',(-17.8167014103155,-3.33051870318735,
-955.861764705882));
#158122=CARTESIAN_POINT('Ctrl Pts',(-17.9710104137728,-1.66525935159368,
-957.355882352941));
#158123=CARTESIAN_POINT('Ctrl Pts',(-18.1253194172301,-1.10985572039171E-15,
-958.85));
#158124=CARTESIAN_POINT('Ctrl Pts',(-17.9710104137728,1.66525935159367,
-960.344117647059));
#158125=CARTESIAN_POINT('Ctrl Pts',(-17.8167014103155,3.33051870318735,
-961.838235294118));
#158126=CARTESIAN_POINT('Ctrl Pts',(-17.3590292079831,4.93906964482096,
-963.332352941177));
#158127=CARTESIAN_POINT('Ctrl Pts',(-16.9013570056506,6.54762058645456,
-964.826470588235));
#158128=CARTESIAN_POINT('Ctrl Pts',(-16.1559070823762,8.04468584505497,
-966.320588235294));
#158129=CARTESIAN_POINT('Ctrl Pts',(-15.4104571591017,9.54175110365538,
-967.814705882353));
#158130=CARTESIAN_POINT('Ctrl Pts',(-14.4026149179538,10.8763499173728,
-969.308823529412));
#158131=CARTESIAN_POINT('Ctrl Pts',(-13.3947726768058,12.2109487310903,
-970.80294117647));
#158132=CARTESIAN_POINT('Ctrl Pts',(-12.1588589765331,13.3376329379985,
-972.297058823529));
#158133=CARTESIAN_POINT('Ctrl Pts',(-10.9229452762603,14.4643171449067,
-973.791176470588));
#158134=CARTESIAN_POINT('Ctrl Pts',(-9.50104767561052,15.3447188656481,
-975.285294117647));
#158135=CARTESIAN_POINT('Ctrl Pts',(-8.07915007496071,16.2251205863895,
-976.779411764706));
#158136=CARTESIAN_POINT('Ctrl Pts',(-6.51968959134574,16.8292587962898,
-978.273529411765));
#158137=CARTESIAN_POINT('Ctrl Pts',(-4.96022910773078,17.4333970061901,
-979.767647058824));
#158138=CARTESIAN_POINT('Ctrl Pts',(-3.31631129755346,17.7406985030951,
-981.261764705882));
#158139=CARTESIAN_POINT('Ctrl Pts',(-1.67239348737615,18.048,-982.755882352941));
#158140=CARTESIAN_POINT('Ctrl Pts',(-2.21024254310115E-15,18.048,-984.25));
#158141=CARTESIAN_POINT('Ctrl Pts',(1.67239348737616,18.048,-985.744117647059));
#158142=CARTESIAN_POINT('Ctrl Pts',(3.31631129755346,17.7406985030951,-987.238235294118));
#158143=CARTESIAN_POINT('Ctrl Pts',(4.96022910773077,17.4333970061901,-988.732352941177));
#158144=CARTESIAN_POINT('Ctrl Pts',(6.51968959134575,16.8292587962898,-990.226470588235));
#158145=CARTESIAN_POINT('Ctrl Pts',(8.07915007496071,16.2251205863895,-991.720588235294));
#158146=CARTESIAN_POINT('Ctrl Pts',(9.50104767561053,15.3447188656481,-993.214705882353));
#158147=CARTESIAN_POINT('Ctrl Pts',(10.9229452762603,14.4643171449067,-994.708823529412));
#158148=CARTESIAN_POINT('Ctrl Pts',(12.1588589765331,13.3376329379985,-996.202941176471));
#158149=CARTESIAN_POINT('Ctrl Pts',(13.3947726768058,12.2109487310903,-997.697058823529));
#158150=CARTESIAN_POINT('Ctrl Pts',(14.4026149179538,10.8763499173728,-999.191176470588));
#158151=CARTESIAN_POINT('Ctrl Pts',(15.4104571591017,9.54175110365538,-1000.68529411765));
#158152=CARTESIAN_POINT('Ctrl Pts',(16.1559070823762,8.04468584505496,-1002.17941176471));
#158153=CARTESIAN_POINT('Ctrl Pts',(16.9013570056506,6.54762058645456,-1003.67352941176));
#158154=CARTESIAN_POINT('Ctrl Pts',(17.3590292079831,4.93906964482096,-1005.16764705882));
#158155=CARTESIAN_POINT('Ctrl Pts',(17.8167014103155,3.33051870318735,-1006.66176470588));
#158156=CARTESIAN_POINT('Ctrl Pts',(17.9710104137728,1.66525935159367,-1008.15588235294));
#158157=CARTESIAN_POINT('Ctrl Pts',(18.1253194172301,3.32956716117513E-15,
-1009.65));
#158158=CARTESIAN_POINT('Ctrl Pts',(17.9710104137728,-1.66525935159367,
-1011.14411764706));
#158159=CARTESIAN_POINT('Ctrl Pts',(17.8167014103155,-3.33051870318736,
-1012.63823529412));
#158160=CARTESIAN_POINT('Ctrl Pts',(17.3590292079831,-4.93906964482095,
-1014.13235294118));
#158161=CARTESIAN_POINT('Ctrl Pts',(16.9013570056506,-6.54762058645456,
-1015.62647058824));
#158162=CARTESIAN_POINT('Ctrl Pts',(16.1559070823762,-8.04468584505497,
-1017.12058823529));
#158163=CARTESIAN_POINT('Ctrl Pts',(15.4104571591017,-9.54175110365538,
-1018.61470588235));
#158164=CARTESIAN_POINT('Ctrl Pts',(14.4026149179538,-10.8763499173728,
-1020.10882352941));
#158165=CARTESIAN_POINT('Ctrl Pts',(13.3947726768058,-12.2109487310903,
-1021.60294117647));
#158166=CARTESIAN_POINT('Ctrl Pts',(12.1588589765331,-13.3376329379985,
-1023.09705882353));
#158167=CARTESIAN_POINT('Ctrl Pts',(10.9229452762603,-14.4643171449067,
-1024.59117647059));
#158168=CARTESIAN_POINT('Ctrl Pts',(9.50104767561053,-15.3447188656481,
-1026.08529411765));
#158169=CARTESIAN_POINT('Ctrl Pts',(8.07915007496071,-16.2251205863895,
-1027.57941176471));
#158170=CARTESIAN_POINT('Ctrl Pts',(6.51968959134574,-16.8292587962898,
-1029.07352941176));
#158171=CARTESIAN_POINT('Ctrl Pts',(4.96022910773078,-17.4333970061901,
-1030.56764705882));
#158172=CARTESIAN_POINT('Ctrl Pts',(3.31631129755346,-17.7406985030951,
-1032.06176470588));
#158173=CARTESIAN_POINT('Ctrl Pts',(1.67239348737615,-18.048,-1033.55588235294));
#158174=CARTESIAN_POINT('Ctrl Pts',(0.,-18.048,-1035.05));
#158175=CARTESIAN_POINT('Ctrl Pts',(-1.67239348737615,-18.048,-1036.54411764706));
#158176=CARTESIAN_POINT('Ctrl Pts',(-3.31631129755346,-17.7406985030951,
-1038.03823529412));
#158177=CARTESIAN_POINT('Ctrl Pts',(-4.96022910773077,-17.4333970061901,
-1039.53235294118));
#158178=CARTESIAN_POINT('Ctrl Pts',(-6.51968959134574,-16.8292587962898,
-1041.02647058824));
#158179=CARTESIAN_POINT('Ctrl Pts',(-8.07915007496071,-16.2251205863895,
-1042.52058823529));
#158180=CARTESIAN_POINT('Ctrl Pts',(-9.50104767561052,-15.3447188656481,
-1044.01470588235));
#158181=CARTESIAN_POINT('Ctrl Pts',(-10.9229452762603,-14.4643171449067,
-1045.50882352941));
#158182=CARTESIAN_POINT('Ctrl Pts',(-12.1588589765331,-13.3376329379985,
-1047.00294117647));
#158183=CARTESIAN_POINT('Ctrl Pts',(-13.3947726768058,-12.2109487310903,
-1048.49705882353));
#158184=CARTESIAN_POINT('Ctrl Pts',(-14.4026149179538,-10.8763499173728,
-1049.99117647059));
#158185=CARTESIAN_POINT('Ctrl Pts',(-15.4104571591017,-9.54175110365538,
-1051.48529411765));
#158186=CARTESIAN_POINT('Ctrl Pts',(-16.1559070823762,-8.04468584505497,
-1052.97941176471));
#158187=CARTESIAN_POINT('Ctrl Pts',(-16.9013570056506,-6.54762058645456,
-1054.47352941176));
#158188=CARTESIAN_POINT('Ctrl Pts',(-17.3590292079831,-4.93906964482095,
-1055.96764705882));
#158189=CARTESIAN_POINT('Ctrl Pts',(-17.8167014103155,-3.33051870318735,
-1057.46176470588));
#158190=CARTESIAN_POINT('Ctrl Pts',(-17.9710104137728,-1.66525935159368,
-1058.95588235294));
#158191=CARTESIAN_POINT('Ctrl Pts',(-18.1253194172301,-1.10985572039171E-15,
-1060.45));
#158192=CARTESIAN_POINT('Ctrl Pts',(-17.9710104137728,1.66525935159367,
-1061.94411764706));
#158193=CARTESIAN_POINT('Ctrl Pts',(-17.8167014103155,3.33051870318735,
-1063.43823529412));
#158194=CARTESIAN_POINT('Ctrl Pts',(-17.3590292079831,4.93906964482096,
-1064.93235294118));
#158195=CARTESIAN_POINT('Ctrl Pts',(-16.9013570056506,6.54762058645456,
-1066.42647058824));
#158196=CARTESIAN_POINT('Ctrl Pts',(-16.1559070823762,8.04468584505497,
-1067.92058823529));
#158197=CARTESIAN_POINT('Ctrl Pts',(-15.4104571591017,9.54175110365538,
-1069.41470588235));
#158198=CARTESIAN_POINT('Ctrl Pts',(-14.4026149179538,10.8763499173728,
-1070.90882352941));
#158199=CARTESIAN_POINT('Ctrl Pts',(-13.3947726768058,12.2109487310903,
-1072.40294117647));
#158200=CARTESIAN_POINT('Ctrl Pts',(-12.1588589765331,13.3376329379985,
-1073.89705882353));
#158201=CARTESIAN_POINT('Ctrl Pts',(-10.9229452762603,14.4643171449067,
-1075.39117647059));
#158202=CARTESIAN_POINT('Ctrl Pts',(-9.50104767561052,15.3447188656481,
-1076.88529411765));
#158203=CARTESIAN_POINT('Ctrl Pts',(-8.07915007496071,16.2251205863895,
-1078.37941176471));
#158204=CARTESIAN_POINT('Ctrl Pts',(-6.51968959134574,16.8292587962898,
-1079.87352941176));
#158205=CARTESIAN_POINT('Ctrl Pts',(-4.96022910773078,17.4333970061901,
-1081.36764705882));
#158206=CARTESIAN_POINT('Ctrl Pts',(-3.31631129755346,17.7406985030951,
-1082.86176470588));
#158207=CARTESIAN_POINT('Ctrl Pts',(-1.67239348737615,18.048,-1084.35588235294));
#158208=CARTESIAN_POINT('Ctrl Pts',(-2.21024254310115E-15,18.048,-1085.85));
#158209=CARTESIAN_POINT('Ctrl Pts',(1.67239348737616,18.048,-1087.34411764706));
#158210=CARTESIAN_POINT('Ctrl Pts',(3.31631129755346,17.7406985030951,-1088.83823529412));
#158211=CARTESIAN_POINT('Ctrl Pts',(4.96022910773077,17.4333970061901,-1090.33235294118));
#158212=CARTESIAN_POINT('Ctrl Pts',(6.51968959134575,16.8292587962898,-1091.82647058824));
#158213=CARTESIAN_POINT('Ctrl Pts',(8.07915007496071,16.2251205863895,-1093.32058823529));
#158214=CARTESIAN_POINT('Ctrl Pts',(9.50104767561053,15.3447188656481,-1094.81470588235));
#158215=CARTESIAN_POINT('Ctrl Pts',(10.9229452762603,14.4643171449067,-1096.30882352941));
#158216=CARTESIAN_POINT('Ctrl Pts',(12.1588589765331,13.3376329379985,-1097.80294117647));
#158217=CARTESIAN_POINT('Ctrl Pts',(13.3947726768058,12.2109487310903,-1099.29705882353));
#158218=CARTESIAN_POINT('Ctrl Pts',(14.4026149179538,10.8763499173728,-1100.79117647059));
#158219=CARTESIAN_POINT('Ctrl Pts',(15.4104571591017,9.54175110365538,-1102.28529411765));
#158220=CARTESIAN_POINT('Ctrl Pts',(16.1559070823762,8.04468584505496,-1103.77941176471));
#158221=CARTESIAN_POINT('Ctrl Pts',(16.9013570056506,6.54762058645456,-1105.27352941176));
#158222=CARTESIAN_POINT('Ctrl Pts',(17.3590292079831,4.93906964482096,-1106.76764705882));
#158223=CARTESIAN_POINT('Ctrl Pts',(17.8167014103155,3.33051870318735,-1108.26176470588));
#158224=CARTESIAN_POINT('Ctrl Pts',(17.9710104137728,1.66525935159367,-1109.75588235294));
#158225=CARTESIAN_POINT('Ctrl Pts',(18.1253194172301,3.32956716117513E-15,
-1111.25));
#158226=CARTESIAN_POINT('Ctrl Pts',(17.9710104137728,-1.66525935159367,
-1112.74411764706));
#158227=CARTESIAN_POINT('Ctrl Pts',(17.8167014103155,-3.33051870318736,
-1114.23823529412));
#158228=CARTESIAN_POINT('Ctrl Pts',(17.3590292079831,-4.93906964482095,
-1115.73235294118));
#158229=CARTESIAN_POINT('Ctrl Pts',(16.9013570056506,-6.54762058645456,
-1117.22647058824));
#158230=CARTESIAN_POINT('Ctrl Pts',(16.1559070823762,-8.04468584505497,
-1118.72058823529));
#158231=CARTESIAN_POINT('Ctrl Pts',(15.4104571591017,-9.54175110365538,
-1120.21470588235));
#158232=CARTESIAN_POINT('Ctrl Pts',(14.4026149179538,-10.8763499173728,
-1121.70882352941));
#158233=CARTESIAN_POINT('Ctrl Pts',(13.3947726768058,-12.2109487310903,
-1123.20294117647));
#158234=CARTESIAN_POINT('Ctrl Pts',(12.1588589765331,-13.3376329379985,
-1124.69705882353));
#158235=CARTESIAN_POINT('Ctrl Pts',(10.9229452762603,-14.4643171449067,
-1126.19117647059));
#158236=CARTESIAN_POINT('Ctrl Pts',(9.50104767561053,-15.3447188656481,
-1127.68529411765));
#158237=CARTESIAN_POINT('Ctrl Pts',(8.07915007496071,-16.2251205863895,
-1129.17941176471));
#158238=CARTESIAN_POINT('Ctrl Pts',(6.51968959134574,-16.8292587962898,
-1130.67352941176));
#158239=CARTESIAN_POINT('Ctrl Pts',(4.96022910773078,-17.4333970061901,
-1132.16764705882));
#158240=CARTESIAN_POINT('Ctrl Pts',(3.31631129755346,-17.7406985030951,
-1133.66176470588));
#158241=CARTESIAN_POINT('Ctrl Pts',(1.67239348737615,-18.048,-1135.15588235294));
#158242=CARTESIAN_POINT('Ctrl Pts',(0.,-18.048,-1136.65));
#158243=CARTESIAN_POINT('Ctrl Pts',(-1.67239348737615,-18.048,-1138.14411764706));
#158244=CARTESIAN_POINT('Ctrl Pts',(-3.31631129755346,-17.7406985030951,
-1139.63823529412));
#158245=CARTESIAN_POINT('Ctrl Pts',(-4.96022910773077,-17.4333970061901,
-1141.13235294118));
#158246=CARTESIAN_POINT('Ctrl Pts',(-6.51968959134574,-16.8292587962898,
-1142.62647058824));
#158247=CARTESIAN_POINT('Ctrl Pts',(-8.07915007496071,-16.2251205863895,
-1144.12058823529));
#158248=CARTESIAN_POINT('Ctrl Pts',(-9.50104767561052,-15.3447188656481,
-1145.61470588235));
#158249=CARTESIAN_POINT('Ctrl Pts',(-10.9229452762603,-14.4643171449067,
-1147.10882352941));
#158250=CARTESIAN_POINT('Ctrl Pts',(-12.1588589765331,-13.3376329379985,
-1148.60294117647));
#158251=CARTESIAN_POINT('Ctrl Pts',(-13.3947726768058,-12.2109487310903,
-1150.09705882353));
#158252=CARTESIAN_POINT('Ctrl Pts',(-14.4026149179538,-10.8763499173728,
-1151.59117647059));
#158253=CARTESIAN_POINT('Ctrl Pts',(-15.4104571591017,-9.54175110365538,
-1153.08529411765));
#158254=CARTESIAN_POINT('Ctrl Pts',(-16.1559070823762,-8.04468584505497,
-1154.57941176471));
#158255=CARTESIAN_POINT('Ctrl Pts',(-16.9013570056506,-6.54762058645456,
-1156.07352941176));
#158256=CARTESIAN_POINT('Ctrl Pts',(-17.3590292079831,-4.93906964482095,
-1157.56764705882));
#158257=CARTESIAN_POINT('Ctrl Pts',(-17.8167014103155,-3.33051870318735,
-1159.06176470588));
#158258=CARTESIAN_POINT('Ctrl Pts',(-17.9710104137728,-1.66525935159368,
-1160.55588235294));
#158259=CARTESIAN_POINT('Ctrl Pts',(-18.1253194172301,-1.10985572039171E-15,
-1162.05));
#158260=CARTESIAN_POINT('Ctrl Pts',(-17.9710104137728,1.66525935159367,
-1163.54411764706));
#158261=CARTESIAN_POINT('Ctrl Pts',(-17.8167014103155,3.33051870318735,
-1165.03823529412));
#158262=CARTESIAN_POINT('Ctrl Pts',(-17.3590292079831,4.93906964482096,
-1166.53235294118));
#158263=CARTESIAN_POINT('Ctrl Pts',(-16.9013570056506,6.54762058645456,
-1168.02647058824));
#158264=CARTESIAN_POINT('Ctrl Pts',(-16.1559070823762,8.04468584505497,
-1169.52058823529));
#158265=CARTESIAN_POINT('Ctrl Pts',(-15.4104571591017,9.54175110365538,
-1171.01470588235));
#158266=CARTESIAN_POINT('Ctrl Pts',(-14.4026149179538,10.8763499173728,
-1172.50882352941));
#158267=CARTESIAN_POINT('Ctrl Pts',(-13.3947726768058,12.2109487310903,
-1174.00294117647));
#158268=CARTESIAN_POINT('Ctrl Pts',(-12.1588589765331,13.3376329379985,
-1175.49705882353));
#158269=CARTESIAN_POINT('Ctrl Pts',(-10.9229452762603,14.4643171449067,
-1176.99117647059));
#158270=CARTESIAN_POINT('Ctrl Pts',(-9.50104767561052,15.3447188656481,
-1178.48529411765));
#158271=CARTESIAN_POINT('Ctrl Pts',(-8.07915007496071,16.2251205863895,
-1179.97941176471));
#158272=CARTESIAN_POINT('Ctrl Pts',(-6.51968959134574,16.8292587962898,
-1181.47352941176));
#158273=CARTESIAN_POINT('Ctrl Pts',(-4.96022910773078,17.4333970061901,
-1182.96764705882));
#158274=CARTESIAN_POINT('Ctrl Pts',(-3.31631129755346,17.7406985030951,
-1184.46176470588));
#158275=CARTESIAN_POINT('Ctrl Pts',(-1.67239348737615,18.048,-1185.95588235294));
#158276=CARTESIAN_POINT('Ctrl Pts',(-2.21024254310115E-15,18.048,-1187.45));
#158277=CARTESIAN_POINT('Ctrl Pts',(1.67239348737616,18.048,-1188.94411764706));
#158278=CARTESIAN_POINT('Ctrl Pts',(3.31631129755346,17.7406985030951,-1190.43823529412));
#158279=CARTESIAN_POINT('Ctrl Pts',(4.96022910773077,17.4333970061901,-1191.93235294118));
#158280=CARTESIAN_POINT('Ctrl Pts',(6.51968959134575,16.8292587962898,-1193.42647058824));
#158281=CARTESIAN_POINT('Ctrl Pts',(8.07915007496071,16.2251205863895,-1194.92058823529));
#158282=CARTESIAN_POINT('Ctrl Pts',(9.50104767561053,15.3447188656481,-1196.41470588235));
#158283=CARTESIAN_POINT('Ctrl Pts',(10.9229452762603,14.4643171449067,-1197.90882352941));
#158284=CARTESIAN_POINT('Ctrl Pts',(12.1588589765331,13.3376329379985,-1199.40294117647));
#158285=CARTESIAN_POINT('Ctrl Pts',(13.3947726768058,12.2109487310903,-1200.89705882353));
#158286=CARTESIAN_POINT('Ctrl Pts',(14.4026149179538,10.8763499173728,-1202.39117647059));
#158287=CARTESIAN_POINT('Ctrl Pts',(15.4104571591017,9.54175110365538,-1203.88529411765));
#158288=CARTESIAN_POINT('Ctrl Pts',(16.1559070823762,8.04468584505496,-1205.37941176471));
#158289=CARTESIAN_POINT('Ctrl Pts',(16.9013570056506,6.54762058645456,-1206.87352941176));
#158290=CARTESIAN_POINT('Ctrl Pts',(17.3590292079831,4.93906964482096,-1208.36764705882));
#158291=CARTESIAN_POINT('Ctrl Pts',(17.8167014103155,3.33051870318735,-1209.86176470588));
#158292=CARTESIAN_POINT('Ctrl Pts',(17.9710104137728,1.66525935159367,-1211.35588235294));
#158293=CARTESIAN_POINT('Ctrl Pts',(18.1253194172301,3.32956716117513E-15,
-1212.85));
#158294=CARTESIAN_POINT('Ctrl Pts',(17.9710104137728,-1.66525935159367,
-1214.34411764706));
#158295=CARTESIAN_POINT('Ctrl Pts',(17.8167014103155,-3.33051870318736,
-1215.83823529412));
#158296=CARTESIAN_POINT('Ctrl Pts',(17.3590292079831,-4.93906964482095,
-1217.33235294118));
#158297=CARTESIAN_POINT('Ctrl Pts',(16.9013570056506,-6.54762058645456,
-1218.82647058824));
#158298=CARTESIAN_POINT('Ctrl Pts',(16.1559070823762,-8.04468584505497,
-1220.32058823529));
#158299=CARTESIAN_POINT('Ctrl Pts',(15.4104571591017,-9.54175110365538,
-1221.81470588235));
#158300=CARTESIAN_POINT('Ctrl Pts',(14.4026149179538,-10.8763499173728,
-1223.30882352941));
#158301=CARTESIAN_POINT('Ctrl Pts',(13.3947726768058,-12.2109487310903,
-1224.80294117647));
#158302=CARTESIAN_POINT('Ctrl Pts',(12.1588589765331,-13.3376329379985,
-1226.29705882353));
#158303=CARTESIAN_POINT('Ctrl Pts',(10.9229452762603,-14.4643171449067,
-1227.79117647059));
#158304=CARTESIAN_POINT('Ctrl Pts',(9.50104767561053,-15.3447188656481,
-1229.28529411765));
#158305=CARTESIAN_POINT('Ctrl Pts',(8.07915007496071,-16.2251205863895,
-1230.77941176471));
#158306=CARTESIAN_POINT('Ctrl Pts',(6.51968959134574,-16.8292587962898,
-1232.27352941176));
#158307=CARTESIAN_POINT('Ctrl Pts',(4.96022910773078,-17.4333970061901,
-1233.76764705882));
#158308=CARTESIAN_POINT('Ctrl Pts',(3.31631129755346,-17.7406985030951,
-1235.26176470588));
#158309=CARTESIAN_POINT('Ctrl Pts',(1.67239348737615,-18.048,-1236.75588235294));
#158310=CARTESIAN_POINT('Ctrl Pts',(0.,-18.048,-1238.25));
#158311=CARTESIAN_POINT('Ctrl Pts',(-1.67239348737615,-18.048,-1239.74411764706));
#158312=CARTESIAN_POINT('Ctrl Pts',(-3.31631129755346,-17.7406985030951,
-1241.23823529412));
#158313=CARTESIAN_POINT('Ctrl Pts',(-4.96022910773077,-17.4333970061901,
-1242.73235294118));
#158314=CARTESIAN_POINT('Ctrl Pts',(-6.51968959134574,-16.8292587962898,
-1244.22647058824));
#158315=CARTESIAN_POINT('Ctrl Pts',(-8.07915007496071,-16.2251205863895,
-1245.72058823529));
#158316=CARTESIAN_POINT('Ctrl Pts',(-9.50104767561052,-15.3447188656481,
-1247.21470588235));
#158317=CARTESIAN_POINT('Ctrl Pts',(-10.9229452762603,-14.4643171449067,
-1248.70882352941));
#158318=CARTESIAN_POINT('Ctrl Pts',(-12.1588589765331,-13.3376329379985,
-1250.20294117647));
#158319=CARTESIAN_POINT('Ctrl Pts',(-13.3947726768058,-12.2109487310903,
-1251.69705882353));
#158320=CARTESIAN_POINT('Ctrl Pts',(-14.4026149179538,-10.8763499173728,
-1253.19117647059));
#158321=CARTESIAN_POINT('Ctrl Pts',(-15.4104571591017,-9.54175110365538,
-1254.68529411765));
#158322=CARTESIAN_POINT('Ctrl Pts',(-16.1559070823762,-8.04468584505497,
-1256.17941176471));
#158323=CARTESIAN_POINT('Ctrl Pts',(-16.9013570056506,-6.54762058645456,
-1257.67352941176));
#158324=CARTESIAN_POINT('Ctrl Pts',(-17.3590292079831,-4.93906964482095,
-1259.16764705882));
#158325=CARTESIAN_POINT('Ctrl Pts',(-17.8167014103155,-3.33051870318735,
-1260.66176470588));
#158326=CARTESIAN_POINT('Ctrl Pts',(-17.9710104137728,-1.66525935159368,
-1262.15588235294));
#158327=CARTESIAN_POINT('Ctrl Pts',(-18.1253194172301,-1.10985572039171E-15,
-1263.65));
#158328=CARTESIAN_POINT('Ctrl Pts',(-17.9710104137728,1.66525935159367,
-1265.14411764706));
#158329=CARTESIAN_POINT('Ctrl Pts',(-17.8167014103155,3.33051870318735,
-1266.63823529412));
#158330=CARTESIAN_POINT('Ctrl Pts',(-17.3590292079831,4.93906964482096,
-1268.13235294118));
#158331=CARTESIAN_POINT('Ctrl Pts',(-16.9013570056506,6.54762058645456,
-1269.62647058824));
#158332=CARTESIAN_POINT('Ctrl Pts',(-16.1559070823762,8.04468584505497,
-1271.12058823529));
#158333=CARTESIAN_POINT('Ctrl Pts',(-15.4104571591017,9.54175110365538,
-1272.61470588235));
#158334=CARTESIAN_POINT('Ctrl Pts',(-14.4026149179538,10.8763499173728,
-1274.10882352941));
#158335=CARTESIAN_POINT('Ctrl Pts',(-13.3947726768058,12.2109487310903,
-1275.60294117647));
#158336=CARTESIAN_POINT('Ctrl Pts',(-12.1588589765331,13.3376329379985,
-1277.09705882353));
#158337=CARTESIAN_POINT('Ctrl Pts',(-10.9229452762603,14.4643171449067,
-1278.59117647059));
#158338=CARTESIAN_POINT('Ctrl Pts',(-9.50104767561052,15.3447188656481,
-1280.08529411765));
#158339=CARTESIAN_POINT('Ctrl Pts',(-8.07915007496071,16.2251205863895,
-1281.57941176471));
#158340=CARTESIAN_POINT('Ctrl Pts',(-6.51968959134574,16.8292587962898,
-1283.07352941176));
#158341=CARTESIAN_POINT('Ctrl Pts',(-4.96022910773078,17.4333970061901,
-1284.56764705882));
#158342=CARTESIAN_POINT('Ctrl Pts',(-3.31631129755346,17.7406985030951,
-1286.06176470588));
#158343=CARTESIAN_POINT('Ctrl Pts',(-1.67239348737615,18.048,-1287.55588235294));
#158344=CARTESIAN_POINT('Ctrl Pts',(-2.21024254310115E-15,18.048,-1289.05));
#158345=CARTESIAN_POINT('Ctrl Pts',(1.67239348737616,18.048,-1290.54411764706));
#158346=CARTESIAN_POINT('Ctrl Pts',(3.31631129755346,17.7406985030951,-1292.03823529412));
#158347=CARTESIAN_POINT('Ctrl Pts',(4.96022910773077,17.4333970061901,-1293.53235294118));
#158348=CARTESIAN_POINT('Ctrl Pts',(6.51968959134575,16.8292587962898,-1295.02647058824));
#158349=CARTESIAN_POINT('Ctrl Pts',(8.07915007496071,16.2251205863895,-1296.52058823529));
#158350=CARTESIAN_POINT('Ctrl Pts',(9.50104767561053,15.3447188656481,-1298.01470588235));
#158351=CARTESIAN_POINT('Ctrl Pts',(10.9229452762603,14.4643171449067,-1299.50882352941));
#158352=CARTESIAN_POINT('Ctrl Pts',(12.1588589765331,13.3376329379985,-1301.00294117647));
#158353=CARTESIAN_POINT('Ctrl Pts',(13.3947726768058,12.2109487310903,-1302.49705882353));
#158354=CARTESIAN_POINT('Ctrl Pts',(14.4026149179538,10.8763499173728,-1303.99117647059));
#158355=CARTESIAN_POINT('Ctrl Pts',(15.4104571591017,9.54175110365538,-1305.48529411765));
#158356=CARTESIAN_POINT('Ctrl Pts',(16.1559070823762,8.04468584505496,-1306.97941176471));
#158357=CARTESIAN_POINT('Ctrl Pts',(16.9013570056506,6.54762058645456,-1308.47352941176));
#158358=CARTESIAN_POINT('Ctrl Pts',(17.3590292079831,4.93906964482096,-1309.96764705882));
#158359=CARTESIAN_POINT('Ctrl Pts',(17.8167014103155,3.33051870318735,-1311.46176470588));
#158360=CARTESIAN_POINT('Ctrl Pts',(17.9710104137728,1.66525935159367,-1312.95588235294));
#158361=CARTESIAN_POINT('Ctrl Pts',(18.1253194172301,3.32956716117513E-15,
-1314.45));
#158362=CARTESIAN_POINT('Ctrl Pts',(17.9710104137728,-1.66525935159367,
-1315.94411764706));
#158363=CARTESIAN_POINT('Ctrl Pts',(17.8167014103155,-3.33051870318736,
-1317.43823529412));
#158364=CARTESIAN_POINT('Ctrl Pts',(17.3590292079831,-4.93906964482095,
-1318.93235294118));
#158365=CARTESIAN_POINT('Ctrl Pts',(16.9013570056506,-6.54762058645456,
-1320.42647058824));
#158366=CARTESIAN_POINT('Ctrl Pts',(16.1559070823762,-8.04468584505497,
-1321.92058823529));
#158367=CARTESIAN_POINT('Ctrl Pts',(15.4104571591017,-9.54175110365538,
-1323.41470588235));
#158368=CARTESIAN_POINT('Ctrl Pts',(14.4026149179538,-10.8763499173728,
-1324.90882352941));
#158369=CARTESIAN_POINT('Ctrl Pts',(13.3947726768058,-12.2109487310903,
-1326.40294117647));
#158370=CARTESIAN_POINT('Ctrl Pts',(12.1588589765331,-13.3376329379985,
-1327.89705882353));
#158371=CARTESIAN_POINT('Ctrl Pts',(10.9229452762603,-14.4643171449067,
-1329.39117647059));
#158372=CARTESIAN_POINT('Ctrl Pts',(9.50104767561053,-15.3447188656481,
-1330.88529411765));
#158373=CARTESIAN_POINT('Ctrl Pts',(8.07915007496071,-16.2251205863895,
-1332.37941176471));
#158374=CARTESIAN_POINT('Ctrl Pts',(6.51968959134574,-16.8292587962898,
-1333.87352941176));
#158375=CARTESIAN_POINT('Ctrl Pts',(4.96022910773078,-17.4333970061901,
-1335.36764705882));
#158376=CARTESIAN_POINT('Ctrl Pts',(3.31631129755346,-17.7406985030951,
-1336.86176470588));
#158377=CARTESIAN_POINT('Ctrl Pts',(1.67239348737615,-18.048,-1338.35588235294));
#158378=CARTESIAN_POINT('Ctrl Pts',(0.,-18.048,-1339.85));
#158379=CARTESIAN_POINT('Ctrl Pts',(-1.67239348737615,-18.048,-1341.34411764706));
#158380=CARTESIAN_POINT('Ctrl Pts',(-3.31631129755346,-17.7406985030951,
-1342.83823529412));
#158381=CARTESIAN_POINT('Ctrl Pts',(-4.96022910773077,-17.4333970061901,
-1344.33235294118));
#158382=CARTESIAN_POINT('Ctrl Pts',(-6.51968959134574,-16.8292587962898,
-1345.82647058824));
#158383=CARTESIAN_POINT('Ctrl Pts',(-8.07915007496071,-16.2251205863895,
-1347.32058823529));
#158384=CARTESIAN_POINT('Ctrl Pts',(-9.50104767561052,-15.3447188656481,
-1348.81470588235));
#158385=CARTESIAN_POINT('Ctrl Pts',(-10.9229452762603,-14.4643171449067,
-1350.30882352941));
#158386=CARTESIAN_POINT('Ctrl Pts',(-12.1588589765331,-13.3376329379985,
-1351.80294117647));
#158387=CARTESIAN_POINT('Ctrl Pts',(-13.3947726768058,-12.2109487310903,
-1353.29705882353));
#158388=CARTESIAN_POINT('Ctrl Pts',(-14.4026149179538,-10.8763499173728,
-1354.79117647059));
#158389=CARTESIAN_POINT('Ctrl Pts',(-15.4104571591017,-9.54175110365538,
-1356.28529411765));
#158390=CARTESIAN_POINT('Ctrl Pts',(-16.1559070823762,-8.04468584505497,
-1357.77941176471));
#158391=CARTESIAN_POINT('Ctrl Pts',(-16.9013570056506,-6.54762058645456,
-1359.27352941176));
#158392=CARTESIAN_POINT('Ctrl Pts',(-17.3590292079831,-4.93906964482095,
-1360.76764705882));
#158393=CARTESIAN_POINT('Ctrl Pts',(-17.8167014103155,-3.33051870318735,
-1362.26176470588));
#158394=CARTESIAN_POINT('Ctrl Pts',(-17.9710104137728,-1.66525935159368,
-1363.75588235294));
#158395=CARTESIAN_POINT('Ctrl Pts',(-18.1253194172301,-1.10985572039171E-15,
-1365.25));
#158396=CARTESIAN_POINT('Ctrl Pts',(-17.9710104137728,1.66525935159367,
-1366.74411764706));
#158397=CARTESIAN_POINT('Ctrl Pts',(-17.8167014103155,3.33051870318735,
-1368.23823529412));
#158398=CARTESIAN_POINT('Ctrl Pts',(-17.3590292079831,4.93906964482096,
-1369.73235294118));
#158399=CARTESIAN_POINT('Ctrl Pts',(-16.9013570056506,6.54762058645456,
-1371.22647058824));
#158400=CARTESIAN_POINT('Ctrl Pts',(-16.1559070823762,8.04468584505497,
-1372.72058823529));
#158401=CARTESIAN_POINT('Ctrl Pts',(-15.4104571591017,9.54175110365538,
-1374.21470588235));
#158402=CARTESIAN_POINT('Ctrl Pts',(-14.4026149179538,10.8763499173728,
-1375.70882352941));
#158403=CARTESIAN_POINT('Ctrl Pts',(-13.3947726768058,12.2109487310903,
-1377.20294117647));
#158404=CARTESIAN_POINT('Ctrl Pts',(-12.1588589765331,13.3376329379985,
-1378.69705882353));
#158405=CARTESIAN_POINT('Ctrl Pts',(-10.9229452762603,14.4643171449067,
-1380.19117647059));
#158406=CARTESIAN_POINT('Ctrl Pts',(-9.50104767561052,15.3447188656481,
-1381.68529411765));
#158407=CARTESIAN_POINT('Ctrl Pts',(-8.07915007496071,16.2251205863895,
-1383.17941176471));
#158408=CARTESIAN_POINT('Ctrl Pts',(-6.51968959134574,16.8292587962898,
-1384.67352941176));
#158409=CARTESIAN_POINT('Ctrl Pts',(-4.96022910773078,17.4333970061901,
-1386.16764705882));
#158410=CARTESIAN_POINT('Ctrl Pts',(-3.31631129755346,17.7406985030951,
-1387.66176470588));
#158411=CARTESIAN_POINT('Ctrl Pts',(-1.67239348737615,18.048,-1389.15588235294));
#158412=CARTESIAN_POINT('Ctrl Pts',(-2.21024254310115E-15,18.048,-1390.65));
#158413=CARTESIAN_POINT('Ctrl Pts',(1.67239348737616,18.048,-1392.14411764706));
#158414=CARTESIAN_POINT('Ctrl Pts',(3.31631129755346,17.7406985030951,-1393.63823529412));
#158415=CARTESIAN_POINT('Ctrl Pts',(4.96022910773077,17.4333970061901,-1395.13235294118));
#158416=CARTESIAN_POINT('Ctrl Pts',(6.51968959134575,16.8292587962898,-1396.62647058824));
#158417=CARTESIAN_POINT('Ctrl Pts',(8.07915007496071,16.2251205863895,-1398.12058823529));
#158418=CARTESIAN_POINT('Ctrl Pts',(9.50104767561053,15.3447188656481,-1399.61470588235));
#158419=CARTESIAN_POINT('Ctrl Pts',(10.9229452762603,14.4643171449067,-1401.10882352941));
#158420=CARTESIAN_POINT('Ctrl Pts',(12.1588589765331,13.3376329379985,-1402.60294117647));
#158421=CARTESIAN_POINT('Ctrl Pts',(13.3947726768058,12.2109487310903,-1404.09705882353));
#158422=CARTESIAN_POINT('Ctrl Pts',(14.4026149179538,10.8763499173728,-1405.59117647059));
#158423=CARTESIAN_POINT('Ctrl Pts',(15.4104571591017,9.54175110365538,-1407.08529411765));
#158424=CARTESIAN_POINT('Ctrl Pts',(16.1559070823762,8.04468584505496,-1408.57941176471));
#158425=CARTESIAN_POINT('Ctrl Pts',(16.9013570056506,6.54762058645456,-1410.07352941176));
#158426=CARTESIAN_POINT('Ctrl Pts',(17.3590292079831,4.93906964482096,-1411.56764705882));
#158427=CARTESIAN_POINT('Ctrl Pts',(17.8167014103155,3.33051870318735,-1413.06176470588));
#158428=CARTESIAN_POINT('Ctrl Pts',(17.9710104137728,1.66525935159367,-1414.55588235294));
#158429=CARTESIAN_POINT('Ctrl Pts',(18.1253194172301,3.32956716117513E-15,
-1416.05));
#158430=CARTESIAN_POINT('Ctrl Pts',(17.9710104137728,-1.66525935159367,
-1417.54411764706));
#158431=CARTESIAN_POINT('Ctrl Pts',(17.8167014103155,-3.33051870318736,
-1419.03823529412));
#158432=CARTESIAN_POINT('Ctrl Pts',(17.3590292079831,-4.93906964482095,
-1420.53235294118));
#158433=CARTESIAN_POINT('Ctrl Pts',(16.9013570056506,-6.54762058645456,
-1422.02647058824));
#158434=CARTESIAN_POINT('Ctrl Pts',(16.1559070823762,-8.04468584505497,
-1423.52058823529));
#158435=CARTESIAN_POINT('Ctrl Pts',(15.4104571591017,-9.54175110365538,
-1425.01470588235));
#158436=CARTESIAN_POINT('Ctrl Pts',(14.4026149179538,-10.8763499173728,
-1426.50882352941));
#158437=CARTESIAN_POINT('Ctrl Pts',(13.3947726768058,-12.2109487310903,
-1428.00294117647));
#158438=CARTESIAN_POINT('Ctrl Pts',(12.1588589765331,-13.3376329379985,
-1429.49705882353));
#158439=CARTESIAN_POINT('Ctrl Pts',(10.9229452762603,-14.4643171449067,
-1430.99117647059));
#158440=CARTESIAN_POINT('Ctrl Pts',(9.50104767561053,-15.3447188656481,
-1432.48529411765));
#158441=CARTESIAN_POINT('Ctrl Pts',(8.07915007496071,-16.2251205863895,
-1433.97941176471));
#158442=CARTESIAN_POINT('Ctrl Pts',(6.51968959134574,-16.8292587962898,
-1435.47352941176));
#158443=CARTESIAN_POINT('Ctrl Pts',(4.96022910773078,-17.4333970061901,
-1436.96764705882));
#158444=CARTESIAN_POINT('Ctrl Pts',(3.31631129755346,-17.7406985030951,
-1438.46176470588));
#158445=CARTESIAN_POINT('Ctrl Pts',(1.67239348737615,-18.048,-1439.95588235294));
#158446=CARTESIAN_POINT('Ctrl Pts',(0.,-18.048,-1441.45));
#158447=CARTESIAN_POINT('Ctrl Pts',(-1.67239348737615,-18.048,-1442.94411764706));
#158448=CARTESIAN_POINT('Ctrl Pts',(-3.31631129755346,-17.7406985030951,
-1444.43823529412));
#158449=CARTESIAN_POINT('Ctrl Pts',(-4.96022910773077,-17.4333970061901,
-1445.93235294118));
#158450=CARTESIAN_POINT('Ctrl Pts',(-6.51968959134574,-16.8292587962898,
-1447.42647058824));
#158451=CARTESIAN_POINT('Ctrl Pts',(-8.07915007496071,-16.2251205863895,
-1448.92058823529));
#158452=CARTESIAN_POINT('Ctrl Pts',(-9.50104767561052,-15.3447188656481,
-1450.41470588235));
#158453=CARTESIAN_POINT('Ctrl Pts',(-10.9229452762603,-14.4643171449067,
-1451.90882352941));
#158454=CARTESIAN_POINT('Ctrl Pts',(-12.1588589765331,-13.3376329379985,
-1453.40294117647));
#158455=CARTESIAN_POINT('Ctrl Pts',(-13.3947726768058,-12.2109487310903,
-1454.89705882353));
#158456=CARTESIAN_POINT('Ctrl Pts',(-14.4026149179538,-10.8763499173728,
-1456.39117647059));
#158457=CARTESIAN_POINT('Ctrl Pts',(-15.4104571591017,-9.54175110365538,
-1457.88529411765));
#158458=CARTESIAN_POINT('Ctrl Pts',(-16.1559070823762,-8.04468584505497,
-1459.37941176471));
#158459=CARTESIAN_POINT('Ctrl Pts',(-16.9013570056506,-6.54762058645456,
-1460.87352941176));
#158460=CARTESIAN_POINT('Ctrl Pts',(-17.3590292079831,-4.93906964482095,
-1462.36764705882));
#158461=CARTESIAN_POINT('Ctrl Pts',(-17.8167014103155,-3.33051870318735,
-1463.86176470588));
#158462=CARTESIAN_POINT('Ctrl Pts',(-17.9710104137728,-1.66525935159368,
-1465.35588235294));
#158463=CARTESIAN_POINT('Ctrl Pts',(-18.1253194172301,-1.10985572039171E-15,
-1466.85));
#158464=CARTESIAN_POINT('Ctrl Pts',(-17.9710104137728,1.66525935159367,
-1468.34411764706));
#158465=CARTESIAN_POINT('Ctrl Pts',(-17.8167014103155,3.33051870318735,
-1469.83823529412));
#158466=CARTESIAN_POINT('Ctrl Pts',(-17.3590292079831,4.93906964482096,
-1471.33235294118));
#158467=CARTESIAN_POINT('Ctrl Pts',(-16.9013570056506,6.54762058645456,
-1472.82647058824));
#158468=CARTESIAN_POINT('Ctrl Pts',(-16.1559070823762,8.04468584505497,
-1474.32058823529));
#158469=CARTESIAN_POINT('Ctrl Pts',(-15.4104571591017,9.54175110365538,
-1475.81470588235));
#158470=CARTESIAN_POINT('Ctrl Pts',(-14.4026149179538,10.8763499173728,
-1477.30882352941));
#158471=CARTESIAN_POINT('Ctrl Pts',(-13.3947726768058,12.2109487310903,
-1478.80294117647));
#158472=CARTESIAN_POINT('Ctrl Pts',(-12.1588589765331,13.3376329379985,
-1480.29705882353));
#158473=CARTESIAN_POINT('Ctrl Pts',(-10.9229452762603,14.4643171449067,
-1481.79117647059));
#158474=CARTESIAN_POINT('Ctrl Pts',(-9.50104767561052,15.3447188656481,
-1483.28529411765));
#158475=CARTESIAN_POINT('Ctrl Pts',(-8.07915007496071,16.2251205863895,
-1484.77941176471));
#158476=CARTESIAN_POINT('Ctrl Pts',(-6.51968959134574,16.8292587962898,
-1486.27352941176));
#158477=CARTESIAN_POINT('Ctrl Pts',(-4.96022910773078,17.4333970061901,
-1487.76764705882));
#158478=CARTESIAN_POINT('Ctrl Pts',(-3.31631129755346,17.7406985030951,
-1489.26176470588));
#158479=CARTESIAN_POINT('Ctrl Pts',(-1.67239348737615,18.048,-1490.75588235294));
#158480=CARTESIAN_POINT('Ctrl Pts',(-2.21024254310115E-15,18.048,-1492.25));
#158481=CARTESIAN_POINT('Ctrl Pts',(1.67239348737616,18.048,-1493.74411764706));
#158482=CARTESIAN_POINT('Ctrl Pts',(3.31631129755346,17.7406985030951,-1495.23823529412));
#158483=CARTESIAN_POINT('Ctrl Pts',(4.96022910773077,17.4333970061901,-1496.73235294118));
#158484=CARTESIAN_POINT('Ctrl Pts',(6.51968959134575,16.8292587962898,-1498.22647058824));
#158485=CARTESIAN_POINT('Ctrl Pts',(7.54125551215708,16.4335020501724,-1499.20523195215));
#158486=CARTESIAN_POINT('Ctrl Pts',(8.50745084181327,15.9170846631577,-1500.18777724595));
#158487=CARTESIAN_POINT('Ctrl Pts',(23.3054395224043,8.00777438919566,-1515.23617759469));
#158488=CARTESIAN_POINT('Ctrl Pts',(38.1034282029954,0.0984641152335814,
-1530.28457794343));
#158489=CARTESIAN_POINT('',(-0.167825465190317,-18.0472196920532,692.));
#158490=CARTESIAN_POINT('',(-0.167825465190317,-18.0472196920532,692.));
#158491=CARTESIAN_POINT('Ctrl Pts',(-2.21024254310115E-15,18.048,742.95));
#158492=CARTESIAN_POINT('Ctrl Pts',(1.67239348737616,18.048,741.455882352941));
#158493=CARTESIAN_POINT('Ctrl Pts',(3.31631129755346,17.7406985030951,739.961764705882));
#158494=CARTESIAN_POINT('Ctrl Pts',(4.96022910773077,17.4333970061901,738.467647058824));
#158495=CARTESIAN_POINT('Ctrl Pts',(6.51968959134575,16.8292587962898,736.973529411765));
#158496=CARTESIAN_POINT('Ctrl Pts',(8.07915007496071,16.2251205863895,735.479411764706));
#158497=CARTESIAN_POINT('Ctrl Pts',(9.50104767561053,15.3447188656481,733.985294117647));
#158498=CARTESIAN_POINT('Ctrl Pts',(10.9229452762603,14.4643171449067,732.491176470588));
#158499=CARTESIAN_POINT('Ctrl Pts',(12.1588589765331,13.3376329379985,730.99705882353));
#158500=CARTESIAN_POINT('Ctrl Pts',(13.3947726768058,12.2109487310903,729.502941176471));
#158501=CARTESIAN_POINT('Ctrl Pts',(14.4026149179538,10.8763499173728,728.008823529412));
#158502=CARTESIAN_POINT('Ctrl Pts',(15.4104571591017,9.54175110365539,726.514705882353));
#158503=CARTESIAN_POINT('Ctrl Pts',(16.1559070823762,8.04468584505496,725.020588235294));
#158504=CARTESIAN_POINT('Ctrl Pts',(16.9013570056506,6.54762058645456,723.526470588235));
#158505=CARTESIAN_POINT('Ctrl Pts',(17.3590292079831,4.93906964482096,722.032352941177));
#158506=CARTESIAN_POINT('Ctrl Pts',(17.8167014103155,3.33051870318735,720.538235294118));
#158507=CARTESIAN_POINT('Ctrl Pts',(17.9710104137728,1.66525935159367,719.044117647059));
#158508=CARTESIAN_POINT('Ctrl Pts',(18.1253194172301,3.32956716117513E-15,
717.55));
#158509=CARTESIAN_POINT('Ctrl Pts',(17.9710104137728,-1.66525935159367,
716.055882352941));
#158510=CARTESIAN_POINT('Ctrl Pts',(17.8167014103155,-3.33051870318736,
714.561764705883));
#158511=CARTESIAN_POINT('Ctrl Pts',(17.3590292079831,-4.93906964482095,
713.067647058824));
#158512=CARTESIAN_POINT('Ctrl Pts',(16.9013570056506,-6.54762058645456,
711.573529411765));
#158513=CARTESIAN_POINT('Ctrl Pts',(16.1559070823762,-8.04468584505497,
710.079411764706));
#158514=CARTESIAN_POINT('Ctrl Pts',(15.4104571591017,-9.54175110365538,
708.585294117647));
#158515=CARTESIAN_POINT('Ctrl Pts',(14.4026149179538,-10.8763499173728,
707.091176470588));
#158516=CARTESIAN_POINT('Ctrl Pts',(13.3947726768058,-12.2109487310903,
705.597058823529));
#158517=CARTESIAN_POINT('Ctrl Pts',(12.1588589765331,-13.3376329379985,
704.102941176471));
#158518=CARTESIAN_POINT('Ctrl Pts',(10.9229452762603,-14.4643171449067,
702.608823529412));
#158519=CARTESIAN_POINT('Ctrl Pts',(9.50104767561053,-15.3447188656481,
701.114705882353));
#158520=CARTESIAN_POINT('Ctrl Pts',(8.07915007496071,-16.2251205863895,
699.620588235294));
#158521=CARTESIAN_POINT('Ctrl Pts',(6.51968959134574,-16.8292587962898,
698.126470588235));
#158522=CARTESIAN_POINT('Ctrl Pts',(4.96022910773078,-17.4333970061901,
696.632352941177));
#158523=CARTESIAN_POINT('Ctrl Pts',(3.31631129755346,-17.7406985030951,
695.138235294118));
#158524=CARTESIAN_POINT('Ctrl Pts',(1.67239348737615,-18.048,693.644117647059));
#158525=CARTESIAN_POINT('Ctrl Pts',(0.,-18.048,692.15));
#158526=CARTESIAN_POINT('Ctrl Pts',(-0.0839145466253093,-18.048,692.075030678543));
#158527=CARTESIAN_POINT('Ctrl Pts',(-0.167825465190317,-18.0472196920532,
692.));
#158528=CARTESIAN_POINT('',(0.,-15.0000000000001,1504.95));
#158529=CARTESIAN_POINT('Ctrl Pts',(0.,-18.048,1500.1875));
#158530=CARTESIAN_POINT('Ctrl Pts',(-1.67239348737615,-18.048,1498.69338235294));
#158531=CARTESIAN_POINT('Ctrl Pts',(-3.31631129755346,-17.7406985030951,
1497.19926470588));
#158532=CARTESIAN_POINT('Ctrl Pts',(-4.96022910773077,-17.4333970061901,
1495.70514705882));
#158533=CARTESIAN_POINT('Ctrl Pts',(-6.51968959134574,-16.8292587962898,
1494.21102941176));
#158534=CARTESIAN_POINT('Ctrl Pts',(-8.07915007496071,-16.2251205863895,
1492.71691176471));
#158535=CARTESIAN_POINT('Ctrl Pts',(-9.50104767561052,-15.3447188656481,
1491.22279411765));
#158536=CARTESIAN_POINT('Ctrl Pts',(-10.9229452762603,-14.4643171449067,
1489.72867647059));
#158537=CARTESIAN_POINT('Ctrl Pts',(-12.1588589765331,-13.3376329379985,
1488.23455882353));
#158538=CARTESIAN_POINT('Ctrl Pts',(-13.3947726768058,-12.2109487310903,
1486.74044117647));
#158539=CARTESIAN_POINT('Ctrl Pts',(-14.4026149179538,-10.8763499173728,
1485.24632352941));
#158540=CARTESIAN_POINT('Ctrl Pts',(-15.4104571591017,-9.54175110365538,
1483.75220588235));
#158541=CARTESIAN_POINT('Ctrl Pts',(-16.1559070823762,-8.04468584505497,
1482.25808823529));
#158542=CARTESIAN_POINT('Ctrl Pts',(-16.9013570056506,-6.54762058645456,
1480.76397058824));
#158543=CARTESIAN_POINT('Ctrl Pts',(-17.3590292079831,-4.93906964482095,
1479.26985294118));
#158544=CARTESIAN_POINT('Ctrl Pts',(-17.8167014103155,-3.33051870318735,
1477.77573529412));
#158545=CARTESIAN_POINT('Ctrl Pts',(-17.9710104137728,-1.66525935159368,
1476.28161764706));
#158546=CARTESIAN_POINT('Ctrl Pts',(-18.1253194172301,-1.10985572039171E-15,
1474.7875));
#158547=CARTESIAN_POINT('Ctrl Pts',(-17.9710104137728,1.66525935159367,
1473.29338235294));
#158548=CARTESIAN_POINT('Ctrl Pts',(-17.8167014103155,3.33051870318735,
1471.79926470588));
#158549=CARTESIAN_POINT('Ctrl Pts',(-17.3590292079831,4.93906964482096,
1470.30514705882));
#158550=CARTESIAN_POINT('Ctrl Pts',(-16.9013570056506,6.54762058645456,
1468.81102941177));
#158551=CARTESIAN_POINT('Ctrl Pts',(-16.1559070823762,8.04468584505497,
1467.31691176471));
#158552=CARTESIAN_POINT('Ctrl Pts',(-15.4104571591017,9.54175110365538,
1465.82279411765));
#158553=CARTESIAN_POINT('Ctrl Pts',(-14.4026149179538,10.8763499173728,
1464.32867647059));
#158554=CARTESIAN_POINT('Ctrl Pts',(-13.3947726768058,12.2109487310903,
1462.83455882353));
#158555=CARTESIAN_POINT('Ctrl Pts',(-12.1588589765331,13.3376329379985,
1461.34044117647));
#158556=CARTESIAN_POINT('Ctrl Pts',(-10.9229452762603,14.4643171449067,
1459.84632352941));
#158557=CARTESIAN_POINT('Ctrl Pts',(-9.50104767561052,15.3447188656481,
1458.35220588235));
#158558=CARTESIAN_POINT('Ctrl Pts',(-8.07915007496071,16.2251205863895,
1456.85808823529));
#158559=CARTESIAN_POINT('Ctrl Pts',(-6.51968959134574,16.8292587962898,
1455.36397058824));
#158560=CARTESIAN_POINT('Ctrl Pts',(-4.96022910773078,17.4333970061901,
1453.86985294118));
#158561=CARTESIAN_POINT('Ctrl Pts',(-3.31631129755346,17.7406985030951,
1452.37573529412));
#158562=CARTESIAN_POINT('Ctrl Pts',(-1.67239348737615,18.048,1450.88161764706));
#158563=CARTESIAN_POINT('Ctrl Pts',(-2.21024254310115E-15,18.048,1449.3875));
#158564=CARTESIAN_POINT('Ctrl Pts',(1.67239348737616,18.048,1447.89338235294));
#158565=CARTESIAN_POINT('Ctrl Pts',(3.31631129755346,17.7406985030951,1446.39926470588));
#158566=CARTESIAN_POINT('Ctrl Pts',(4.96022910773077,17.4333970061901,1444.90514705882));
#158567=CARTESIAN_POINT('Ctrl Pts',(6.51968959134575,16.8292587962898,1443.41102941176));
#158568=CARTESIAN_POINT('Ctrl Pts',(8.07915007496071,16.2251205863895,1441.91691176471));
#158569=CARTESIAN_POINT('Ctrl Pts',(9.50104767561053,15.3447188656481,1440.42279411765));
#158570=CARTESIAN_POINT('Ctrl Pts',(10.9229452762603,14.4643171449067,1438.92867647059));
#158571=CARTESIAN_POINT('Ctrl Pts',(12.1588589765331,13.3376329379985,1437.43455882353));
#158572=CARTESIAN_POINT('Ctrl Pts',(13.3947726768058,12.2109487310903,1435.94044117647));
#158573=CARTESIAN_POINT('Ctrl Pts',(14.4026149179538,10.8763499173728,1434.44632352941));
#158574=CARTESIAN_POINT('Ctrl Pts',(15.4104571591017,9.54175110365538,1432.95220588235));
#158575=CARTESIAN_POINT('Ctrl Pts',(16.1559070823762,8.04468584505496,1431.45808823529));
#158576=CARTESIAN_POINT('Ctrl Pts',(16.9013570056506,6.54762058645456,1429.96397058824));
#158577=CARTESIAN_POINT('Ctrl Pts',(17.3590292079831,4.93906964482096,1428.46985294118));
#158578=CARTESIAN_POINT('Ctrl Pts',(17.8167014103155,3.33051870318735,1426.97573529412));
#158579=CARTESIAN_POINT('Ctrl Pts',(17.9710104137728,1.66525935159367,1425.48161764706));
#158580=CARTESIAN_POINT('Ctrl Pts',(18.1253194172301,3.32956716117513E-15,
1423.9875));
#158581=CARTESIAN_POINT('Ctrl Pts',(17.9710104137728,-1.66525935159367,
1422.49338235294));
#158582=CARTESIAN_POINT('Ctrl Pts',(17.8167014103155,-3.33051870318736,
1420.99926470588));
#158583=CARTESIAN_POINT('Ctrl Pts',(17.3590292079831,-4.93906964482095,
1419.50514705882));
#158584=CARTESIAN_POINT('Ctrl Pts',(16.9013570056506,-6.54762058645456,
1418.01102941176));
#158585=CARTESIAN_POINT('Ctrl Pts',(16.1559070823762,-8.04468584505497,
1416.51691176471));
#158586=CARTESIAN_POINT('Ctrl Pts',(15.4104571591017,-9.54175110365538,
1415.02279411765));
#158587=CARTESIAN_POINT('Ctrl Pts',(14.4026149179538,-10.8763499173728,
1413.52867647059));
#158588=CARTESIAN_POINT('Ctrl Pts',(13.3947726768058,-12.2109487310903,
1412.03455882353));
#158589=CARTESIAN_POINT('Ctrl Pts',(12.1588589765331,-13.3376329379985,
1410.54044117647));
#158590=CARTESIAN_POINT('Ctrl Pts',(10.9229452762603,-14.4643171449067,
1409.04632352941));
#158591=CARTESIAN_POINT('Ctrl Pts',(9.50104767561053,-15.3447188656481,
1407.55220588235));
#158592=CARTESIAN_POINT('Ctrl Pts',(8.07915007496071,-16.2251205863895,
1406.05808823529));
#158593=CARTESIAN_POINT('Ctrl Pts',(6.51968959134574,-16.8292587962898,
1404.56397058824));
#158594=CARTESIAN_POINT('Ctrl Pts',(4.96022910773078,-17.4333970061901,
1403.06985294118));
#158595=CARTESIAN_POINT('Ctrl Pts',(3.31631129755346,-17.7406985030951,
1401.57573529412));
#158596=CARTESIAN_POINT('Ctrl Pts',(1.67239348737615,-18.048,1400.08161764706));
#158597=CARTESIAN_POINT('Ctrl Pts',(0.,-18.048,1398.5875));
#158598=CARTESIAN_POINT('Ctrl Pts',(-1.67239348737615,-18.048,1397.09338235294));
#158599=CARTESIAN_POINT('Ctrl Pts',(-3.31631129755346,-17.7406985030951,
1395.59926470588));
#158600=CARTESIAN_POINT('Ctrl Pts',(-4.96022910773077,-17.4333970061901,
1394.10514705882));
#158601=CARTESIAN_POINT('Ctrl Pts',(-6.51968959134574,-16.8292587962898,
1392.61102941176));
#158602=CARTESIAN_POINT('Ctrl Pts',(-8.07915007496071,-16.2251205863895,
1391.11691176471));
#158603=CARTESIAN_POINT('Ctrl Pts',(-9.50104767561052,-15.3447188656481,
1389.62279411765));
#158604=CARTESIAN_POINT('Ctrl Pts',(-10.9229452762603,-14.4643171449067,
1388.12867647059));
#158605=CARTESIAN_POINT('Ctrl Pts',(-12.1588589765331,-13.3376329379985,
1386.63455882353));
#158606=CARTESIAN_POINT('Ctrl Pts',(-13.3947726768058,-12.2109487310903,
1385.14044117647));
#158607=CARTESIAN_POINT('Ctrl Pts',(-14.4026149179538,-10.8763499173728,
1383.64632352941));
#158608=CARTESIAN_POINT('Ctrl Pts',(-15.4104571591017,-9.54175110365538,
1382.15220588235));
#158609=CARTESIAN_POINT('Ctrl Pts',(-16.1559070823762,-8.04468584505497,
1380.65808823529));
#158610=CARTESIAN_POINT('Ctrl Pts',(-16.9013570056506,-6.54762058645456,
1379.16397058824));
#158611=CARTESIAN_POINT('Ctrl Pts',(-17.3590292079831,-4.93906964482095,
1377.66985294118));
#158612=CARTESIAN_POINT('Ctrl Pts',(-17.8167014103155,-3.33051870318735,
1376.17573529412));
#158613=CARTESIAN_POINT('Ctrl Pts',(-17.9710104137728,-1.66525935159368,
1374.68161764706));
#158614=CARTESIAN_POINT('Ctrl Pts',(-18.1253194172301,-1.10985572039171E-15,
1373.1875));
#158615=CARTESIAN_POINT('Ctrl Pts',(-17.9710104137728,1.66525935159367,
1371.69338235294));
#158616=CARTESIAN_POINT('Ctrl Pts',(-17.8167014103155,3.33051870318735,
1370.19926470588));
#158617=CARTESIAN_POINT('Ctrl Pts',(-17.3590292079831,4.93906964482096,
1368.70514705882));
#158618=CARTESIAN_POINT('Ctrl Pts',(-16.9013570056506,6.54762058645456,
1367.21102941176));
#158619=CARTESIAN_POINT('Ctrl Pts',(-16.1559070823762,8.04468584505497,
1365.71691176471));
#158620=CARTESIAN_POINT('Ctrl Pts',(-15.4104571591017,9.54175110365538,
1364.22279411765));
#158621=CARTESIAN_POINT('Ctrl Pts',(-14.4026149179538,10.8763499173728,
1362.72867647059));
#158622=CARTESIAN_POINT('Ctrl Pts',(-13.3947726768058,12.2109487310903,
1361.23455882353));
#158623=CARTESIAN_POINT('Ctrl Pts',(-12.1588589765331,13.3376329379985,
1359.74044117647));
#158624=CARTESIAN_POINT('Ctrl Pts',(-10.9229452762603,14.4643171449067,
1358.24632352941));
#158625=CARTESIAN_POINT('Ctrl Pts',(-9.50104767561052,15.3447188656481,
1356.75220588235));
#158626=CARTESIAN_POINT('Ctrl Pts',(-8.07915007496071,16.2251205863895,
1355.25808823529));
#158627=CARTESIAN_POINT('Ctrl Pts',(-6.51968959134574,16.8292587962898,
1353.76397058824));
#158628=CARTESIAN_POINT('Ctrl Pts',(-4.96022910773078,17.4333970061901,
1352.26985294118));
#158629=CARTESIAN_POINT('Ctrl Pts',(-3.31631129755346,17.7406985030951,
1350.77573529412));
#158630=CARTESIAN_POINT('Ctrl Pts',(-1.67239348737615,18.048,1349.28161764706));
#158631=CARTESIAN_POINT('Ctrl Pts',(-2.21024254310115E-15,18.048,1347.7875));
#158632=CARTESIAN_POINT('Ctrl Pts',(1.67239348737616,18.048,1346.29338235294));
#158633=CARTESIAN_POINT('Ctrl Pts',(3.31631129755346,17.7406985030951,1344.79926470588));
#158634=CARTESIAN_POINT('Ctrl Pts',(4.96022910773077,17.4333970061901,1343.30514705882));
#158635=CARTESIAN_POINT('Ctrl Pts',(6.51968959134575,16.8292587962898,1341.81102941176));
#158636=CARTESIAN_POINT('Ctrl Pts',(8.07915007496071,16.2251205863895,1340.31691176471));
#158637=CARTESIAN_POINT('Ctrl Pts',(9.50104767561053,15.3447188656481,1338.82279411765));
#158638=CARTESIAN_POINT('Ctrl Pts',(10.9229452762603,14.4643171449067,1337.32867647059));
#158639=CARTESIAN_POINT('Ctrl Pts',(12.1588589765331,13.3376329379985,1335.83455882353));
#158640=CARTESIAN_POINT('Ctrl Pts',(13.3947726768058,12.2109487310903,1334.34044117647));
#158641=CARTESIAN_POINT('Ctrl Pts',(14.4026149179538,10.8763499173728,1332.84632352941));
#158642=CARTESIAN_POINT('Ctrl Pts',(15.4104571591017,9.54175110365538,1331.35220588235));
#158643=CARTESIAN_POINT('Ctrl Pts',(16.1559070823762,8.04468584505496,1329.85808823529));
#158644=CARTESIAN_POINT('Ctrl Pts',(16.9013570056506,6.54762058645456,1328.36397058824));
#158645=CARTESIAN_POINT('Ctrl Pts',(17.3590292079831,4.93906964482096,1326.86985294118));
#158646=CARTESIAN_POINT('Ctrl Pts',(17.8167014103155,3.33051870318735,1325.37573529412));
#158647=CARTESIAN_POINT('Ctrl Pts',(17.9710104137728,1.66525935159367,1323.88161764706));
#158648=CARTESIAN_POINT('Ctrl Pts',(18.1253194172301,3.32956716117513E-15,
1322.3875));
#158649=CARTESIAN_POINT('Ctrl Pts',(17.9710104137728,-1.66525935159367,
1320.89338235294));
#158650=CARTESIAN_POINT('Ctrl Pts',(17.8167014103155,-3.33051870318736,
1319.39926470588));
#158651=CARTESIAN_POINT('Ctrl Pts',(17.3590292079831,-4.93906964482095,
1317.90514705882));
#158652=CARTESIAN_POINT('Ctrl Pts',(16.9013570056506,-6.54762058645456,
1316.41102941176));
#158653=CARTESIAN_POINT('Ctrl Pts',(16.1559070823762,-8.04468584505497,
1314.91691176471));
#158654=CARTESIAN_POINT('Ctrl Pts',(15.4104571591017,-9.54175110365538,
1313.42279411765));
#158655=CARTESIAN_POINT('Ctrl Pts',(14.4026149179538,-10.8763499173728,
1311.92867647059));
#158656=CARTESIAN_POINT('Ctrl Pts',(13.3947726768058,-12.2109487310903,
1310.43455882353));
#158657=CARTESIAN_POINT('Ctrl Pts',(12.1588589765331,-13.3376329379985,
1308.94044117647));
#158658=CARTESIAN_POINT('Ctrl Pts',(10.9229452762603,-14.4643171449067,
1307.44632352941));
#158659=CARTESIAN_POINT('Ctrl Pts',(9.50104767561053,-15.3447188656481,
1305.95220588235));
#158660=CARTESIAN_POINT('Ctrl Pts',(8.07915007496071,-16.2251205863895,
1304.45808823529));
#158661=CARTESIAN_POINT('Ctrl Pts',(6.51968959134574,-16.8292587962898,
1302.96397058824));
#158662=CARTESIAN_POINT('Ctrl Pts',(4.96022910773078,-17.4333970061901,
1301.46985294118));
#158663=CARTESIAN_POINT('Ctrl Pts',(3.31631129755346,-17.7406985030951,
1299.97573529412));
#158664=CARTESIAN_POINT('Ctrl Pts',(1.67239348737615,-18.048,1298.48161764706));
#158665=CARTESIAN_POINT('Ctrl Pts',(0.,-18.048,1296.9875));
#158666=CARTESIAN_POINT('Ctrl Pts',(-1.67239348737615,-18.048,1295.49338235294));
#158667=CARTESIAN_POINT('Ctrl Pts',(-3.31631129755346,-17.7406985030951,
1293.99926470588));
#158668=CARTESIAN_POINT('Ctrl Pts',(-4.96022910773077,-17.4333970061901,
1292.50514705882));
#158669=CARTESIAN_POINT('Ctrl Pts',(-6.51968959134574,-16.8292587962898,
1291.01102941176));
#158670=CARTESIAN_POINT('Ctrl Pts',(-8.07915007496071,-16.2251205863895,
1289.51691176471));
#158671=CARTESIAN_POINT('Ctrl Pts',(-9.50104767561052,-15.3447188656481,
1288.02279411765));
#158672=CARTESIAN_POINT('Ctrl Pts',(-10.9229452762603,-14.4643171449067,
1286.52867647059));
#158673=CARTESIAN_POINT('Ctrl Pts',(-12.1588589765331,-13.3376329379985,
1285.03455882353));
#158674=CARTESIAN_POINT('Ctrl Pts',(-13.3947726768058,-12.2109487310903,
1283.54044117647));
#158675=CARTESIAN_POINT('Ctrl Pts',(-14.4026149179538,-10.8763499173728,
1282.04632352941));
#158676=CARTESIAN_POINT('Ctrl Pts',(-15.4104571591017,-9.54175110365538,
1280.55220588235));
#158677=CARTESIAN_POINT('Ctrl Pts',(-16.1559070823762,-8.04468584505497,
1279.05808823529));
#158678=CARTESIAN_POINT('Ctrl Pts',(-16.9013570056506,-6.54762058645456,
1277.56397058824));
#158679=CARTESIAN_POINT('Ctrl Pts',(-17.3590292079831,-4.93906964482095,
1276.06985294118));
#158680=CARTESIAN_POINT('Ctrl Pts',(-17.8167014103155,-3.33051870318735,
1274.57573529412));
#158681=CARTESIAN_POINT('Ctrl Pts',(-17.9710104137728,-1.66525935159368,
1273.08161764706));
#158682=CARTESIAN_POINT('Ctrl Pts',(-18.1253194172301,-1.10985572039171E-15,
1271.5875));
#158683=CARTESIAN_POINT('Ctrl Pts',(-17.9710104137728,1.66525935159367,
1270.09338235294));
#158684=CARTESIAN_POINT('Ctrl Pts',(-17.8167014103155,3.33051870318735,
1268.59926470588));
#158685=CARTESIAN_POINT('Ctrl Pts',(-17.3590292079831,4.93906964482096,
1267.10514705882));
#158686=CARTESIAN_POINT('Ctrl Pts',(-16.9013570056506,6.54762058645456,
1265.61102941176));
#158687=CARTESIAN_POINT('Ctrl Pts',(-16.1559070823762,8.04468584505497,
1264.11691176471));
#158688=CARTESIAN_POINT('Ctrl Pts',(-15.4104571591017,9.54175110365538,
1262.62279411765));
#158689=CARTESIAN_POINT('Ctrl Pts',(-14.4026149179538,10.8763499173728,
1261.12867647059));
#158690=CARTESIAN_POINT('Ctrl Pts',(-13.3947726768058,12.2109487310903,
1259.63455882353));
#158691=CARTESIAN_POINT('Ctrl Pts',(-12.1588589765331,13.3376329379985,
1258.14044117647));
#158692=CARTESIAN_POINT('Ctrl Pts',(-10.9229452762603,14.4643171449067,
1256.64632352941));
#158693=CARTESIAN_POINT('Ctrl Pts',(-9.50104767561052,15.3447188656481,
1255.15220588235));
#158694=CARTESIAN_POINT('Ctrl Pts',(-8.07915007496071,16.2251205863895,
1253.65808823529));
#158695=CARTESIAN_POINT('Ctrl Pts',(-6.51968959134574,16.8292587962898,
1252.16397058824));
#158696=CARTESIAN_POINT('Ctrl Pts',(-4.96022910773078,17.4333970061901,
1250.66985294118));
#158697=CARTESIAN_POINT('Ctrl Pts',(-3.31631129755346,17.7406985030951,
1249.17573529412));
#158698=CARTESIAN_POINT('Ctrl Pts',(-1.67239348737615,18.048,1247.68161764706));
#158699=CARTESIAN_POINT('Ctrl Pts',(-2.21024254310115E-15,18.048,1246.1875));
#158700=CARTESIAN_POINT('Ctrl Pts',(1.67239348737616,18.048,1244.69338235294));
#158701=CARTESIAN_POINT('Ctrl Pts',(3.31631129755346,17.7406985030951,1243.19926470588));
#158702=CARTESIAN_POINT('Ctrl Pts',(4.96022910773077,17.4333970061901,1241.70514705882));
#158703=CARTESIAN_POINT('Ctrl Pts',(6.51968959134575,16.8292587962898,1240.21102941176));
#158704=CARTESIAN_POINT('Ctrl Pts',(8.07915007496071,16.2251205863895,1238.71691176471));
#158705=CARTESIAN_POINT('Ctrl Pts',(9.50104767561053,15.3447188656481,1237.22279411765));
#158706=CARTESIAN_POINT('Ctrl Pts',(10.9229452762603,14.4643171449067,1235.72867647059));
#158707=CARTESIAN_POINT('Ctrl Pts',(12.1588589765331,13.3376329379985,1234.23455882353));
#158708=CARTESIAN_POINT('Ctrl Pts',(13.3947726768058,12.2109487310903,1232.74044117647));
#158709=CARTESIAN_POINT('Ctrl Pts',(14.4026149179538,10.8763499173728,1231.24632352941));
#158710=CARTESIAN_POINT('Ctrl Pts',(15.4104571591017,9.54175110365538,1229.75220588235));
#158711=CARTESIAN_POINT('Ctrl Pts',(16.1559070823762,8.04468584505496,1228.25808823529));
#158712=CARTESIAN_POINT('Ctrl Pts',(16.9013570056506,6.54762058645456,1226.76397058824));
#158713=CARTESIAN_POINT('Ctrl Pts',(17.3590292079831,4.93906964482096,1225.26985294118));
#158714=CARTESIAN_POINT('Ctrl Pts',(17.8167014103155,3.33051870318735,1223.77573529412));
#158715=CARTESIAN_POINT('Ctrl Pts',(17.9710104137728,1.66525935159367,1222.28161764706));
#158716=CARTESIAN_POINT('Ctrl Pts',(18.1253194172301,3.32956716117513E-15,
1220.7875));
#158717=CARTESIAN_POINT('Ctrl Pts',(17.9710104137728,-1.66525935159367,
1219.29338235294));
#158718=CARTESIAN_POINT('Ctrl Pts',(17.8167014103155,-3.33051870318736,
1217.79926470588));
#158719=CARTESIAN_POINT('Ctrl Pts',(17.3590292079831,-4.93906964482095,
1216.30514705882));
#158720=CARTESIAN_POINT('Ctrl Pts',(16.9013570056506,-6.54762058645456,
1214.81102941176));
#158721=CARTESIAN_POINT('Ctrl Pts',(16.1559070823762,-8.04468584505497,
1213.31691176471));
#158722=CARTESIAN_POINT('Ctrl Pts',(15.4104571591017,-9.54175110365538,
1211.82279411765));
#158723=CARTESIAN_POINT('Ctrl Pts',(14.4026149179538,-10.8763499173728,
1210.32867647059));
#158724=CARTESIAN_POINT('Ctrl Pts',(13.3947726768058,-12.2109487310903,
1208.83455882353));
#158725=CARTESIAN_POINT('Ctrl Pts',(12.1588589765331,-13.3376329379985,
1207.34044117647));
#158726=CARTESIAN_POINT('Ctrl Pts',(10.9229452762603,-14.4643171449067,
1205.84632352941));
#158727=CARTESIAN_POINT('Ctrl Pts',(9.50104767561053,-15.3447188656481,
1204.35220588235));
#158728=CARTESIAN_POINT('Ctrl Pts',(8.07915007496071,-16.2251205863895,
1202.85808823529));
#158729=CARTESIAN_POINT('Ctrl Pts',(6.51968959134574,-16.8292587962898,
1201.36397058824));
#158730=CARTESIAN_POINT('Ctrl Pts',(4.96022910773078,-17.4333970061901,
1199.86985294118));
#158731=CARTESIAN_POINT('Ctrl Pts',(3.31631129755346,-17.7406985030951,
1198.37573529412));
#158732=CARTESIAN_POINT('Ctrl Pts',(1.67239348737615,-18.048,1196.88161764706));
#158733=CARTESIAN_POINT('Ctrl Pts',(0.,-18.048,1195.3875));
#158734=CARTESIAN_POINT('Ctrl Pts',(-1.67239348737615,-18.048,1193.89338235294));
#158735=CARTESIAN_POINT('Ctrl Pts',(-3.31631129755346,-17.7406985030951,
1192.39926470588));
#158736=CARTESIAN_POINT('Ctrl Pts',(-4.96022910773077,-17.4333970061901,
1190.90514705882));
#158737=CARTESIAN_POINT('Ctrl Pts',(-6.51968959134574,-16.8292587962898,
1189.41102941176));
#158738=CARTESIAN_POINT('Ctrl Pts',(-8.07915007496071,-16.2251205863895,
1187.91691176471));
#158739=CARTESIAN_POINT('Ctrl Pts',(-9.50104767561052,-15.3447188656481,
1186.42279411765));
#158740=CARTESIAN_POINT('Ctrl Pts',(-10.9229452762603,-14.4643171449067,
1184.92867647059));
#158741=CARTESIAN_POINT('Ctrl Pts',(-12.1588589765331,-13.3376329379985,
1183.43455882353));
#158742=CARTESIAN_POINT('Ctrl Pts',(-13.3947726768058,-12.2109487310903,
1181.94044117647));
#158743=CARTESIAN_POINT('Ctrl Pts',(-14.4026149179538,-10.8763499173728,
1180.44632352941));
#158744=CARTESIAN_POINT('Ctrl Pts',(-15.4104571591017,-9.54175110365538,
1178.95220588235));
#158745=CARTESIAN_POINT('Ctrl Pts',(-16.1559070823762,-8.04468584505497,
1177.45808823529));
#158746=CARTESIAN_POINT('Ctrl Pts',(-16.9013570056506,-6.54762058645456,
1175.96397058824));
#158747=CARTESIAN_POINT('Ctrl Pts',(-17.3590292079831,-4.93906964482095,
1174.46985294118));
#158748=CARTESIAN_POINT('Ctrl Pts',(-17.8167014103155,-3.33051870318735,
1172.97573529412));
#158749=CARTESIAN_POINT('Ctrl Pts',(-17.9710104137728,-1.66525935159368,
1171.48161764706));
#158750=CARTESIAN_POINT('Ctrl Pts',(-18.1253194172301,-1.10985572039171E-15,
1169.9875));
#158751=CARTESIAN_POINT('Ctrl Pts',(-17.9710104137728,1.66525935159367,
1168.49338235294));
#158752=CARTESIAN_POINT('Ctrl Pts',(-17.8167014103155,3.33051870318735,
1166.99926470588));
#158753=CARTESIAN_POINT('Ctrl Pts',(-17.3590292079831,4.93906964482096,
1165.50514705882));
#158754=CARTESIAN_POINT('Ctrl Pts',(-16.9013570056506,6.54762058645456,
1164.01102941176));
#158755=CARTESIAN_POINT('Ctrl Pts',(-16.1559070823762,8.04468584505497,
1162.51691176471));
#158756=CARTESIAN_POINT('Ctrl Pts',(-15.4104571591017,9.54175110365538,
1161.02279411765));
#158757=CARTESIAN_POINT('Ctrl Pts',(-14.4026149179538,10.8763499173728,
1159.52867647059));
#158758=CARTESIAN_POINT('Ctrl Pts',(-13.3947726768058,12.2109487310903,
1158.03455882353));
#158759=CARTESIAN_POINT('Ctrl Pts',(-12.1588589765331,13.3376329379985,
1156.54044117647));
#158760=CARTESIAN_POINT('Ctrl Pts',(-10.9229452762603,14.4643171449067,
1155.04632352941));
#158761=CARTESIAN_POINT('Ctrl Pts',(-9.50104767561052,15.3447188656481,
1153.55220588235));
#158762=CARTESIAN_POINT('Ctrl Pts',(-8.07915007496071,16.2251205863895,
1152.05808823529));
#158763=CARTESIAN_POINT('Ctrl Pts',(-6.51968959134574,16.8292587962898,
1150.56397058824));
#158764=CARTESIAN_POINT('Ctrl Pts',(-4.96022910773078,17.4333970061901,
1149.06985294118));
#158765=CARTESIAN_POINT('Ctrl Pts',(-3.31631129755346,17.7406985030951,
1147.57573529412));
#158766=CARTESIAN_POINT('Ctrl Pts',(-1.67239348737615,18.048,1146.08161764706));
#158767=CARTESIAN_POINT('Ctrl Pts',(-2.21024254310115E-15,18.048,1144.5875));
#158768=CARTESIAN_POINT('Ctrl Pts',(1.67239348737616,18.048,1143.09338235294));
#158769=CARTESIAN_POINT('Ctrl Pts',(3.31631129755346,17.7406985030951,1141.59926470588));
#158770=CARTESIAN_POINT('Ctrl Pts',(4.96022910773077,17.4333970061901,1140.10514705882));
#158771=CARTESIAN_POINT('Ctrl Pts',(6.51968959134575,16.8292587962898,1138.61102941176));
#158772=CARTESIAN_POINT('Ctrl Pts',(8.07915007496071,16.2251205863895,1137.11691176471));
#158773=CARTESIAN_POINT('Ctrl Pts',(9.50104767561053,15.3447188656481,1135.62279411765));
#158774=CARTESIAN_POINT('Ctrl Pts',(10.9229452762603,14.4643171449067,1134.12867647059));
#158775=CARTESIAN_POINT('Ctrl Pts',(12.1588589765331,13.3376329379985,1132.63455882353));
#158776=CARTESIAN_POINT('Ctrl Pts',(13.3947726768058,12.2109487310903,1131.14044117647));
#158777=CARTESIAN_POINT('Ctrl Pts',(14.4026149179538,10.8763499173728,1129.64632352941));
#158778=CARTESIAN_POINT('Ctrl Pts',(15.4104571591017,9.54175110365538,1128.15220588235));
#158779=CARTESIAN_POINT('Ctrl Pts',(16.1559070823762,8.04468584505496,1126.65808823529));
#158780=CARTESIAN_POINT('Ctrl Pts',(16.9013570056506,6.54762058645456,1125.16397058824));
#158781=CARTESIAN_POINT('Ctrl Pts',(17.3590292079831,4.93906964482096,1123.66985294118));
#158782=CARTESIAN_POINT('Ctrl Pts',(17.8167014103155,3.33051870318735,1122.17573529412));
#158783=CARTESIAN_POINT('Ctrl Pts',(17.9710104137728,1.66525935159367,1120.68161764706));
#158784=CARTESIAN_POINT('Ctrl Pts',(18.1253194172301,3.32956716117513E-15,
1119.1875));
#158785=CARTESIAN_POINT('Ctrl Pts',(17.9710104137728,-1.66525935159367,
1117.69338235294));
#158786=CARTESIAN_POINT('Ctrl Pts',(17.8167014103155,-3.33051870318736,
1116.19926470588));
#158787=CARTESIAN_POINT('Ctrl Pts',(17.3590292079831,-4.93906964482095,
1114.70514705882));
#158788=CARTESIAN_POINT('Ctrl Pts',(16.9013570056506,-6.54762058645456,
1113.21102941176));
#158789=CARTESIAN_POINT('Ctrl Pts',(16.1559070823762,-8.04468584505497,
1111.71691176471));
#158790=CARTESIAN_POINT('Ctrl Pts',(15.4104571591017,-9.54175110365538,
1110.22279411765));
#158791=CARTESIAN_POINT('Ctrl Pts',(14.4026149179538,-10.8763499173728,
1108.72867647059));
#158792=CARTESIAN_POINT('Ctrl Pts',(13.3947726768058,-12.2109487310903,
1107.23455882353));
#158793=CARTESIAN_POINT('Ctrl Pts',(12.1588589765331,-13.3376329379985,
1105.74044117647));
#158794=CARTESIAN_POINT('Ctrl Pts',(10.9229452762603,-14.4643171449067,
1104.24632352941));
#158795=CARTESIAN_POINT('Ctrl Pts',(9.50104767561053,-15.3447188656481,
1102.75220588235));
#158796=CARTESIAN_POINT('Ctrl Pts',(8.07915007496071,-16.2251205863895,
1101.25808823529));
#158797=CARTESIAN_POINT('Ctrl Pts',(6.51968959134574,-16.8292587962898,
1099.76397058824));
#158798=CARTESIAN_POINT('Ctrl Pts',(4.96022910773078,-17.4333970061901,
1098.26985294118));
#158799=CARTESIAN_POINT('Ctrl Pts',(3.31631129755346,-17.7406985030951,
1096.77573529412));
#158800=CARTESIAN_POINT('Ctrl Pts',(1.67239348737615,-18.048,1095.28161764706));
#158801=CARTESIAN_POINT('Ctrl Pts',(0.,-18.048,1093.7875));
#158802=CARTESIAN_POINT('Ctrl Pts',(-1.67239348737615,-18.048,1092.29338235294));
#158803=CARTESIAN_POINT('Ctrl Pts',(-3.31631129755346,-17.7406985030951,
1090.79926470588));
#158804=CARTESIAN_POINT('Ctrl Pts',(-4.96022910773077,-17.4333970061901,
1089.30514705882));
#158805=CARTESIAN_POINT('Ctrl Pts',(-6.51968959134574,-16.8292587962898,
1087.81102941176));
#158806=CARTESIAN_POINT('Ctrl Pts',(-8.07915007496071,-16.2251205863895,
1086.31691176471));
#158807=CARTESIAN_POINT('Ctrl Pts',(-9.50104767561052,-15.3447188656481,
1084.82279411765));
#158808=CARTESIAN_POINT('Ctrl Pts',(-10.9229452762603,-14.4643171449067,
1083.32867647059));
#158809=CARTESIAN_POINT('Ctrl Pts',(-12.1588589765331,-13.3376329379985,
1081.83455882353));
#158810=CARTESIAN_POINT('Ctrl Pts',(-13.3947726768058,-12.2109487310903,
1080.34044117647));
#158811=CARTESIAN_POINT('Ctrl Pts',(-14.4026149179538,-10.8763499173728,
1078.84632352941));
#158812=CARTESIAN_POINT('Ctrl Pts',(-15.4104571591017,-9.54175110365538,
1077.35220588235));
#158813=CARTESIAN_POINT('Ctrl Pts',(-16.1559070823762,-8.04468584505497,
1075.85808823529));
#158814=CARTESIAN_POINT('Ctrl Pts',(-16.9013570056506,-6.54762058645456,
1074.36397058824));
#158815=CARTESIAN_POINT('Ctrl Pts',(-17.3590292079831,-4.93906964482095,
1072.86985294118));
#158816=CARTESIAN_POINT('Ctrl Pts',(-17.8167014103155,-3.33051870318735,
1071.37573529412));
#158817=CARTESIAN_POINT('Ctrl Pts',(-17.9710104137728,-1.66525935159368,
1069.88161764706));
#158818=CARTESIAN_POINT('Ctrl Pts',(-18.1253194172301,-1.10985572039171E-15,
1068.3875));
#158819=CARTESIAN_POINT('Ctrl Pts',(-17.9710104137728,1.66525935159367,
1066.89338235294));
#158820=CARTESIAN_POINT('Ctrl Pts',(-17.8167014103155,3.33051870318735,
1065.39926470588));
#158821=CARTESIAN_POINT('Ctrl Pts',(-17.3590292079831,4.93906964482096,
1063.90514705882));
#158822=CARTESIAN_POINT('Ctrl Pts',(-16.9013570056506,6.54762058645456,
1062.41102941176));
#158823=CARTESIAN_POINT('Ctrl Pts',(-16.1559070823762,8.04468584505497,
1060.91691176471));
#158824=CARTESIAN_POINT('Ctrl Pts',(-15.4104571591017,9.54175110365538,
1059.42279411765));
#158825=CARTESIAN_POINT('Ctrl Pts',(-14.4026149179538,10.8763499173728,
1057.92867647059));
#158826=CARTESIAN_POINT('Ctrl Pts',(-13.3947726768058,12.2109487310903,
1056.43455882353));
#158827=CARTESIAN_POINT('Ctrl Pts',(-12.1588589765331,13.3376329379985,
1054.94044117647));
#158828=CARTESIAN_POINT('Ctrl Pts',(-10.9229452762603,14.4643171449067,
1053.44632352941));
#158829=CARTESIAN_POINT('Ctrl Pts',(-9.50104767561052,15.3447188656481,
1051.95220588235));
#158830=CARTESIAN_POINT('Ctrl Pts',(-8.07915007496071,16.2251205863895,
1050.45808823529));
#158831=CARTESIAN_POINT('Ctrl Pts',(-6.51968959134574,16.8292587962898,
1048.96397058824));
#158832=CARTESIAN_POINT('Ctrl Pts',(-4.96022910773078,17.4333970061901,
1047.46985294118));
#158833=CARTESIAN_POINT('Ctrl Pts',(-3.31631129755346,17.7406985030951,
1045.97573529412));
#158834=CARTESIAN_POINT('Ctrl Pts',(-1.67239348737615,18.048,1044.48161764706));
#158835=CARTESIAN_POINT('Ctrl Pts',(-2.21024254310115E-15,18.048,1042.9875));
#158836=CARTESIAN_POINT('Ctrl Pts',(1.67239348737616,18.048,1041.49338235294));
#158837=CARTESIAN_POINT('Ctrl Pts',(3.31631129755346,17.7406985030951,1039.99926470588));
#158838=CARTESIAN_POINT('Ctrl Pts',(4.96022910773077,17.4333970061901,1038.50514705882));
#158839=CARTESIAN_POINT('Ctrl Pts',(6.51968959134575,16.8292587962898,1037.01102941176));
#158840=CARTESIAN_POINT('Ctrl Pts',(8.07915007496071,16.2251205863895,1035.51691176471));
#158841=CARTESIAN_POINT('Ctrl Pts',(9.50104767561053,15.3447188656481,1034.02279411765));
#158842=CARTESIAN_POINT('Ctrl Pts',(10.9229452762603,14.4643171449067,1032.52867647059));
#158843=CARTESIAN_POINT('Ctrl Pts',(12.1588589765331,13.3376329379985,1031.03455882353));
#158844=CARTESIAN_POINT('Ctrl Pts',(13.3947726768058,12.2109487310903,1029.54044117647));
#158845=CARTESIAN_POINT('Ctrl Pts',(14.4026149179538,10.8763499173728,1028.04632352941));
#158846=CARTESIAN_POINT('Ctrl Pts',(15.4104571591017,9.54175110365538,1026.55220588235));
#158847=CARTESIAN_POINT('Ctrl Pts',(16.1559070823762,8.04468584505496,1025.05808823529));
#158848=CARTESIAN_POINT('Ctrl Pts',(16.9013570056506,6.54762058645456,1023.56397058824));
#158849=CARTESIAN_POINT('Ctrl Pts',(17.3590292079831,4.93906964482096,1022.06985294118));
#158850=CARTESIAN_POINT('Ctrl Pts',(17.8167014103155,3.33051870318735,1020.57573529412));
#158851=CARTESIAN_POINT('Ctrl Pts',(17.9710104137728,1.66525935159367,1019.08161764706));
#158852=CARTESIAN_POINT('Ctrl Pts',(18.1253194172301,3.32956716117513E-15,
1017.5875));
#158853=CARTESIAN_POINT('Ctrl Pts',(17.9710104137728,-1.66525935159367,
1016.09338235294));
#158854=CARTESIAN_POINT('Ctrl Pts',(17.8167014103155,-3.33051870318736,
1014.59926470588));
#158855=CARTESIAN_POINT('Ctrl Pts',(17.3590292079831,-4.93906964482095,
1013.10514705882));
#158856=CARTESIAN_POINT('Ctrl Pts',(16.9013570056506,-6.54762058645456,
1011.61102941176));
#158857=CARTESIAN_POINT('Ctrl Pts',(16.1559070823762,-8.04468584505497,
1010.11691176471));
#158858=CARTESIAN_POINT('Ctrl Pts',(15.4104571591017,-9.54175110365538,
1008.62279411765));
#158859=CARTESIAN_POINT('Ctrl Pts',(14.4026149179538,-10.8763499173728,
1007.12867647059));
#158860=CARTESIAN_POINT('Ctrl Pts',(13.3947726768058,-12.2109487310903,
1005.63455882353));
#158861=CARTESIAN_POINT('Ctrl Pts',(12.1588589765331,-13.3376329379985,
1004.14044117647));
#158862=CARTESIAN_POINT('Ctrl Pts',(10.9229452762603,-14.4643171449067,
1002.64632352941));
#158863=CARTESIAN_POINT('Ctrl Pts',(9.50104767561053,-15.3447188656481,
1001.15220588235));
#158864=CARTESIAN_POINT('Ctrl Pts',(8.07915007496071,-16.2251205863895,
999.658088235294));
#158865=CARTESIAN_POINT('Ctrl Pts',(6.51968959134574,-16.8292587962898,
998.163970588235));
#158866=CARTESIAN_POINT('Ctrl Pts',(4.96022910773078,-17.4333970061901,
996.669852941177));
#158867=CARTESIAN_POINT('Ctrl Pts',(3.31631129755346,-17.7406985030951,
995.175735294118));
#158868=CARTESIAN_POINT('Ctrl Pts',(1.67239348737615,-18.048,993.681617647059));
#158869=CARTESIAN_POINT('Ctrl Pts',(0.,-18.048,992.1875));
#158870=CARTESIAN_POINT('Ctrl Pts',(-1.67239348737615,-18.048,990.693382352941));
#158871=CARTESIAN_POINT('Ctrl Pts',(-3.31631129755346,-17.7406985030951,
989.199264705882));
#158872=CARTESIAN_POINT('Ctrl Pts',(-4.96022910773077,-17.4333970061901,
987.705147058824));
#158873=CARTESIAN_POINT('Ctrl Pts',(-6.51968959134574,-16.8292587962898,
986.211029411765));
#158874=CARTESIAN_POINT('Ctrl Pts',(-8.07915007496071,-16.2251205863895,
984.716911764706));
#158875=CARTESIAN_POINT('Ctrl Pts',(-9.50104767561052,-15.3447188656481,
983.222794117647));
#158876=CARTESIAN_POINT('Ctrl Pts',(-10.9229452762603,-14.4643171449067,
981.728676470589));
#158877=CARTESIAN_POINT('Ctrl Pts',(-12.1588589765331,-13.3376329379985,
980.234558823529));
#158878=CARTESIAN_POINT('Ctrl Pts',(-13.3947726768058,-12.2109487310903,
978.740441176471));
#158879=CARTESIAN_POINT('Ctrl Pts',(-14.4026149179538,-10.8763499173728,
977.246323529412));
#158880=CARTESIAN_POINT('Ctrl Pts',(-15.4104571591017,-9.54175110365538,
975.752205882353));
#158881=CARTESIAN_POINT('Ctrl Pts',(-16.1559070823762,-8.04468584505497,
974.258088235294));
#158882=CARTESIAN_POINT('Ctrl Pts',(-16.9013570056506,-6.54762058645456,
972.763970588235));
#158883=CARTESIAN_POINT('Ctrl Pts',(-17.3590292079831,-4.93906964482095,
971.269852941177));
#158884=CARTESIAN_POINT('Ctrl Pts',(-17.8167014103155,-3.33051870318735,
969.775735294118));
#158885=CARTESIAN_POINT('Ctrl Pts',(-17.9710104137728,-1.66525935159368,
968.281617647059));
#158886=CARTESIAN_POINT('Ctrl Pts',(-18.1253194172301,-1.10985572039171E-15,
966.7875));
#158887=CARTESIAN_POINT('Ctrl Pts',(-17.9710104137728,1.66525935159367,
965.293382352941));
#158888=CARTESIAN_POINT('Ctrl Pts',(-17.8167014103155,3.33051870318735,
963.799264705882));
#158889=CARTESIAN_POINT('Ctrl Pts',(-17.3590292079831,4.93906964482096,
962.305147058824));
#158890=CARTESIAN_POINT('Ctrl Pts',(-16.9013570056506,6.54762058645456,
960.811029411765));
#158891=CARTESIAN_POINT('Ctrl Pts',(-16.1559070823762,8.04468584505497,
959.316911764706));
#158892=CARTESIAN_POINT('Ctrl Pts',(-15.4104571591017,9.54175110365538,
957.822794117647));
#158893=CARTESIAN_POINT('Ctrl Pts',(-14.4026149179538,10.8763499173728,
956.328676470588));
#158894=CARTESIAN_POINT('Ctrl Pts',(-13.3947726768058,12.2109487310903,
954.834558823529));
#158895=CARTESIAN_POINT('Ctrl Pts',(-12.1588589765331,13.3376329379985,
953.340441176471));
#158896=CARTESIAN_POINT('Ctrl Pts',(-10.9229452762603,14.4643171449067,
951.846323529412));
#158897=CARTESIAN_POINT('Ctrl Pts',(-9.50104767561052,15.3447188656481,
950.352205882353));
#158898=CARTESIAN_POINT('Ctrl Pts',(-8.07915007496071,16.2251205863895,
948.858088235294));
#158899=CARTESIAN_POINT('Ctrl Pts',(-6.51968959134574,16.8292587962898,
947.363970588235));
#158900=CARTESIAN_POINT('Ctrl Pts',(-4.96022910773078,17.4333970061901,
945.869852941177));
#158901=CARTESIAN_POINT('Ctrl Pts',(-3.31631129755346,17.7406985030951,
944.375735294118));
#158902=CARTESIAN_POINT('Ctrl Pts',(-1.67239348737615,18.048,942.881617647059));
#158903=CARTESIAN_POINT('Ctrl Pts',(-2.21024254310115E-15,18.048,941.3875));
#158904=CARTESIAN_POINT('Ctrl Pts',(1.67239348737616,18.048,939.893382352941));
#158905=CARTESIAN_POINT('Ctrl Pts',(3.31631129755346,17.7406985030951,938.399264705882));
#158906=CARTESIAN_POINT('Ctrl Pts',(4.96022910773077,17.4333970061901,936.905147058824));
#158907=CARTESIAN_POINT('Ctrl Pts',(6.51968959134575,16.8292587962898,935.411029411765));
#158908=CARTESIAN_POINT('Ctrl Pts',(8.07915007496071,16.2251205863895,933.916911764706));
#158909=CARTESIAN_POINT('Ctrl Pts',(9.50104767561053,15.3447188656481,932.422794117647));
#158910=CARTESIAN_POINT('Ctrl Pts',(10.9229452762603,14.4643171449067,930.928676470588));
#158911=CARTESIAN_POINT('Ctrl Pts',(12.1588589765331,13.3376329379985,929.43455882353));
#158912=CARTESIAN_POINT('Ctrl Pts',(13.3947726768058,12.2109487310903,927.94044117647));
#158913=CARTESIAN_POINT('Ctrl Pts',(14.4026149179538,10.8763499173728,926.446323529412));
#158914=CARTESIAN_POINT('Ctrl Pts',(15.4104571591017,9.54175110365538,924.952205882353));
#158915=CARTESIAN_POINT('Ctrl Pts',(16.1559070823762,8.04468584505496,923.458088235294));
#158916=CARTESIAN_POINT('Ctrl Pts',(16.9013570056506,6.54762058645456,921.963970588235));
#158917=CARTESIAN_POINT('Ctrl Pts',(17.3590292079831,4.93906964482096,920.469852941176));
#158918=CARTESIAN_POINT('Ctrl Pts',(17.8167014103155,3.33051870318735,918.975735294118));
#158919=CARTESIAN_POINT('Ctrl Pts',(17.9710104137728,1.66525935159367,917.481617647059));
#158920=CARTESIAN_POINT('Ctrl Pts',(18.1253194172301,3.32956716117513E-15,
915.9875));
#158921=CARTESIAN_POINT('Ctrl Pts',(17.9710104137728,-1.66525935159367,
914.493382352941));
#158922=CARTESIAN_POINT('Ctrl Pts',(17.8167014103155,-3.33051870318736,
912.999264705882));
#158923=CARTESIAN_POINT('Ctrl Pts',(17.3590292079831,-4.93906964482095,
911.505147058824));
#158924=CARTESIAN_POINT('Ctrl Pts',(16.9013570056506,-6.54762058645456,
910.011029411765));
#158925=CARTESIAN_POINT('Ctrl Pts',(16.1559070823762,-8.04468584505497,
908.516911764706));
#158926=CARTESIAN_POINT('Ctrl Pts',(15.4104571591017,-9.54175110365538,
907.022794117647));
#158927=CARTESIAN_POINT('Ctrl Pts',(14.4026149179538,-10.8763499173728,
905.528676470588));
#158928=CARTESIAN_POINT('Ctrl Pts',(13.3947726768058,-12.2109487310903,
904.034558823529));
#158929=CARTESIAN_POINT('Ctrl Pts',(12.1588589765331,-13.3376329379985,
902.540441176471));
#158930=CARTESIAN_POINT('Ctrl Pts',(10.9229452762603,-14.4643171449067,
901.046323529412));
#158931=CARTESIAN_POINT('Ctrl Pts',(9.50104767561053,-15.3447188656481,
899.552205882353));
#158932=CARTESIAN_POINT('Ctrl Pts',(8.07915007496071,-16.2251205863895,
898.058088235294));
#158933=CARTESIAN_POINT('Ctrl Pts',(6.51968959134574,-16.8292587962898,
896.563970588235));
#158934=CARTESIAN_POINT('Ctrl Pts',(4.96022910773078,-17.4333970061901,
895.069852941177));
#158935=CARTESIAN_POINT('Ctrl Pts',(3.31631129755346,-17.7406985030951,
893.575735294118));
#158936=CARTESIAN_POINT('Ctrl Pts',(1.67239348737615,-18.048,892.081617647059));
#158937=CARTESIAN_POINT('Ctrl Pts',(0.,-18.048,890.5875));
#158938=CARTESIAN_POINT('Ctrl Pts',(-1.67239348737615,-18.048,889.093382352941));
#158939=CARTESIAN_POINT('Ctrl Pts',(-3.31631129755346,-17.7406985030951,
887.599264705882));
#158940=CARTESIAN_POINT('Ctrl Pts',(-4.96022910773077,-17.4333970061901,
886.105147058824));
#158941=CARTESIAN_POINT('Ctrl Pts',(-6.51968959134574,-16.8292587962898,
884.611029411765));
#158942=CARTESIAN_POINT('Ctrl Pts',(-8.07915007496071,-16.2251205863895,
883.116911764706));
#158943=CARTESIAN_POINT('Ctrl Pts',(-9.50104767561052,-15.3447188656481,
881.622794117647));
#158944=CARTESIAN_POINT('Ctrl Pts',(-10.9229452762603,-14.4643171449067,
880.128676470588));
#158945=CARTESIAN_POINT('Ctrl Pts',(-12.1588589765331,-13.3376329379985,
878.634558823529));
#158946=CARTESIAN_POINT('Ctrl Pts',(-13.3947726768058,-12.2109487310903,
877.140441176471));
#158947=CARTESIAN_POINT('Ctrl Pts',(-14.4026149179538,-10.8763499173728,
875.646323529412));
#158948=CARTESIAN_POINT('Ctrl Pts',(-15.4104571591017,-9.54175110365538,
874.152205882353));
#158949=CARTESIAN_POINT('Ctrl Pts',(-16.1559070823762,-8.04468584505497,
872.658088235294));
#158950=CARTESIAN_POINT('Ctrl Pts',(-16.9013570056506,-6.54762058645456,
871.163970588236));
#158951=CARTESIAN_POINT('Ctrl Pts',(-17.3590292079831,-4.93906964482095,
869.669852941176));
#158952=CARTESIAN_POINT('Ctrl Pts',(-17.8167014103155,-3.33051870318735,
868.175735294118));
#158953=CARTESIAN_POINT('Ctrl Pts',(-17.9710104137728,-1.66525935159368,
866.681617647059));
#158954=CARTESIAN_POINT('Ctrl Pts',(-18.1253194172301,-1.10985572039171E-15,
865.1875));
#158955=CARTESIAN_POINT('Ctrl Pts',(-17.9710104137728,1.66525935159367,
863.693382352941));
#158956=CARTESIAN_POINT('Ctrl Pts',(-17.8167014103155,3.33051870318735,
862.199264705883));
#158957=CARTESIAN_POINT('Ctrl Pts',(-17.3590292079831,4.93906964482096,
860.705147058824));
#158958=CARTESIAN_POINT('Ctrl Pts',(-16.9013570056506,6.54762058645456,
859.211029411765));
#158959=CARTESIAN_POINT('Ctrl Pts',(-16.1559070823762,8.04468584505497,
857.716911764706));
#158960=CARTESIAN_POINT('Ctrl Pts',(-15.4104571591017,9.54175110365538,
856.222794117647));
#158961=CARTESIAN_POINT('Ctrl Pts',(-14.4026149179538,10.8763499173728,
854.728676470588));
#158962=CARTESIAN_POINT('Ctrl Pts',(-13.3947726768058,12.2109487310903,
853.234558823529));
#158963=CARTESIAN_POINT('Ctrl Pts',(-12.1588589765331,13.3376329379985,
851.740441176471));
#158964=CARTESIAN_POINT('Ctrl Pts',(-10.9229452762603,14.4643171449067,
850.246323529412));
#158965=CARTESIAN_POINT('Ctrl Pts',(-9.50104767561052,15.3447188656481,
848.752205882353));
#158966=CARTESIAN_POINT('Ctrl Pts',(-8.07915007496071,16.2251205863895,
847.258088235294));
#158967=CARTESIAN_POINT('Ctrl Pts',(-6.51968959134574,16.8292587962898,
845.763970588235));
#158968=CARTESIAN_POINT('Ctrl Pts',(-4.96022910773078,17.4333970061901,
844.269852941177));
#158969=CARTESIAN_POINT('Ctrl Pts',(-3.31631129755346,17.7406985030951,
842.775735294118));
#158970=CARTESIAN_POINT('Ctrl Pts',(-1.67239348737615,18.048,841.281617647059));
#158971=CARTESIAN_POINT('Ctrl Pts',(-2.21024254310115E-15,18.048,839.7875));
#158972=CARTESIAN_POINT('Ctrl Pts',(1.67239348737616,18.048,838.293382352941));
#158973=CARTESIAN_POINT('Ctrl Pts',(3.31631129755346,17.7406985030951,836.799264705882));
#158974=CARTESIAN_POINT('Ctrl Pts',(4.96022910773077,17.4333970061901,835.305147058824));
#158975=CARTESIAN_POINT('Ctrl Pts',(6.51968959134575,16.8292587962898,833.811029411765));
#158976=CARTESIAN_POINT('Ctrl Pts',(8.07915007496071,16.2251205863895,832.316911764706));
#158977=CARTESIAN_POINT('Ctrl Pts',(9.50104767561053,15.3447188656481,830.822794117647));
#158978=CARTESIAN_POINT('Ctrl Pts',(10.9229452762603,14.4643171449067,829.328676470588));
#158979=CARTESIAN_POINT('Ctrl Pts',(12.1588589765331,13.3376329379985,827.834558823529));
#158980=CARTESIAN_POINT('Ctrl Pts',(13.3947726768058,12.2109487310903,826.340441176471));
#158981=CARTESIAN_POINT('Ctrl Pts',(14.4026149179538,10.8763499173728,824.846323529412));
#158982=CARTESIAN_POINT('Ctrl Pts',(15.4104571591017,9.54175110365538,823.352205882353));
#158983=CARTESIAN_POINT('Ctrl Pts',(16.1559070823762,8.04468584505496,821.858088235294));
#158984=CARTESIAN_POINT('Ctrl Pts',(16.9013570056506,6.54762058645456,820.363970588236));
#158985=CARTESIAN_POINT('Ctrl Pts',(17.3590292079831,4.93906964482096,818.869852941177));
#158986=CARTESIAN_POINT('Ctrl Pts',(17.8167014103155,3.33051870318735,817.375735294118));
#158987=CARTESIAN_POINT('Ctrl Pts',(17.9710104137728,1.66525935159367,815.881617647059));
#158988=CARTESIAN_POINT('Ctrl Pts',(18.1253194172301,3.32956716117513E-15,
814.3875));
#158989=CARTESIAN_POINT('Ctrl Pts',(17.9710104137728,-1.66525935159367,
812.893382352941));
#158990=CARTESIAN_POINT('Ctrl Pts',(17.8167014103155,-3.33051870318736,
811.399264705883));
#158991=CARTESIAN_POINT('Ctrl Pts',(17.3590292079831,-4.93906964482095,
809.905147058824));
#158992=CARTESIAN_POINT('Ctrl Pts',(16.9013570056506,-6.54762058645456,
808.411029411765));
#158993=CARTESIAN_POINT('Ctrl Pts',(16.1559070823762,-8.04468584505497,
806.916911764706));
#158994=CARTESIAN_POINT('Ctrl Pts',(15.4104571591017,-9.54175110365538,
805.422794117647));
#158995=CARTESIAN_POINT('Ctrl Pts',(14.4026149179538,-10.8763499173728,
803.928676470588));
#158996=CARTESIAN_POINT('Ctrl Pts',(13.3947726768058,-12.2109487310903,
802.434558823529));
#158997=CARTESIAN_POINT('Ctrl Pts',(12.1588589765331,-13.3376329379985,
800.940441176471));
#158998=CARTESIAN_POINT('Ctrl Pts',(10.9229452762603,-14.4643171449067,
799.446323529412));
#158999=CARTESIAN_POINT('Ctrl Pts',(9.50104767561053,-15.3447188656481,
797.952205882353));
#159000=CARTESIAN_POINT('Ctrl Pts',(8.07915007496071,-16.2251205863895,
796.458088235294));
#159001=CARTESIAN_POINT('Ctrl Pts',(6.51968959134574,-16.8292587962898,
794.963970588235));
#159002=CARTESIAN_POINT('Ctrl Pts',(4.96022910773078,-17.4333970061901,
793.469852941176));
#159003=CARTESIAN_POINT('Ctrl Pts',(3.31631129755346,-17.7406985030951,
791.975735294118));
#159004=CARTESIAN_POINT('Ctrl Pts',(1.67239348737615,-18.048,790.481617647059));
#159005=CARTESIAN_POINT('Ctrl Pts',(0.,-18.048,788.9875));
#159006=CARTESIAN_POINT('Ctrl Pts',(-1.67239348737615,-18.048,787.493382352941));
#159007=CARTESIAN_POINT('Ctrl Pts',(-3.31631129755346,-17.7406985030951,
785.999264705882));
#159008=CARTESIAN_POINT('Ctrl Pts',(-4.96022910773077,-17.4333970061901,
784.505147058824));
#159009=CARTESIAN_POINT('Ctrl Pts',(-6.51968959134574,-16.8292587962898,
783.011029411765));
#159010=CARTESIAN_POINT('Ctrl Pts',(-8.07915007496071,-16.2251205863895,
781.516911764706));
#159011=CARTESIAN_POINT('Ctrl Pts',(-9.50104767561052,-15.3447188656481,
780.022794117647));
#159012=CARTESIAN_POINT('Ctrl Pts',(-10.9229452762603,-14.4643171449067,
778.528676470588));
#159013=CARTESIAN_POINT('Ctrl Pts',(-12.1588589765331,-13.3376329379985,
777.03455882353));
#159014=CARTESIAN_POINT('Ctrl Pts',(-13.3947726768058,-12.2109487310903,
775.540441176471));
#159015=CARTESIAN_POINT('Ctrl Pts',(-14.4026149179538,-10.8763499173728,
774.046323529412));
#159016=CARTESIAN_POINT('Ctrl Pts',(-15.4104571591017,-9.54175110365538,
772.552205882353));
#159017=CARTESIAN_POINT('Ctrl Pts',(-16.1559070823762,-8.04468584505497,
771.058088235294));
#159018=CARTESIAN_POINT('Ctrl Pts',(-16.9013570056506,-6.54762058645456,
769.563970588235));
#159019=CARTESIAN_POINT('Ctrl Pts',(-17.3590292079831,-4.93906964482095,
768.069852941177));
#159020=CARTESIAN_POINT('Ctrl Pts',(-17.8167014103155,-3.33051870318735,
766.575735294118));
#159021=CARTESIAN_POINT('Ctrl Pts',(-17.9710104137728,-1.66525935159368,
765.081617647059));
#159022=CARTESIAN_POINT('Ctrl Pts',(-18.1253194172301,-1.10985572039171E-15,
763.5875));
#159023=CARTESIAN_POINT('Ctrl Pts',(-17.9710104137728,1.66525935159367,
762.093382352941));
#159024=CARTESIAN_POINT('Ctrl Pts',(-17.8167014103155,3.33051870318735,
760.599264705883));
#159025=CARTESIAN_POINT('Ctrl Pts',(-17.3590292079831,4.93906964482096,
759.105147058824));
#159026=CARTESIAN_POINT('Ctrl Pts',(-16.9013570056506,6.54762058645456,
757.611029411765));
#159027=CARTESIAN_POINT('Ctrl Pts',(-16.1559070823762,8.04468584505497,
756.116911764706));
#159028=CARTESIAN_POINT('Ctrl Pts',(-15.4104571591017,9.54175110365538,
754.622794117647));
#159029=CARTESIAN_POINT('Ctrl Pts',(-14.4026149179538,10.8763499173728,
753.128676470588));
#159030=CARTESIAN_POINT('Ctrl Pts',(-13.3947726768058,12.2109487310903,
751.634558823529));
#159031=CARTESIAN_POINT('Ctrl Pts',(-12.1588589765331,13.3376329379985,
750.140441176471));
#159032=CARTESIAN_POINT('Ctrl Pts',(-10.9229452762603,14.4643171449067,
748.646323529412));
#159033=CARTESIAN_POINT('Ctrl Pts',(-9.50104767561052,15.3447188656481,
747.152205882353));
#159034=CARTESIAN_POINT('Ctrl Pts',(-8.07915007496071,16.2251205863895,
745.658088235294));
#159035=CARTESIAN_POINT('Ctrl Pts',(-6.51968959134574,16.8292587962898,
744.163970588235));
#159036=CARTESIAN_POINT('Ctrl Pts',(-4.96022910773078,17.4333970061901,
742.669852941176));
#159037=CARTESIAN_POINT('Ctrl Pts',(-3.31631129755346,17.7406985030951,
741.175735294118));
#159038=CARTESIAN_POINT('Ctrl Pts',(-1.67239348737615,18.048,739.681617647059));
#159039=CARTESIAN_POINT('Ctrl Pts',(-2.21024254310115E-15,18.048,738.1875));
#159040=CARTESIAN_POINT('Ctrl Pts',(1.67239348737616,18.048,736.693382352941));
#159041=CARTESIAN_POINT('Ctrl Pts',(3.31631129755346,17.7406985030951,735.199264705882));
#159042=CARTESIAN_POINT('Ctrl Pts',(4.96022910773077,17.4333970061901,733.705147058824));
#159043=CARTESIAN_POINT('Ctrl Pts',(6.51968959134575,16.8292587962898,732.211029411765));
#159044=CARTESIAN_POINT('Ctrl Pts',(8.07915007496071,16.2251205863895,730.716911764706));
#159045=CARTESIAN_POINT('Ctrl Pts',(9.50104767561053,15.3447188656481,729.222794117647));
#159046=CARTESIAN_POINT('Ctrl Pts',(10.9229452762603,14.4643171449067,727.728676470588));
#159047=CARTESIAN_POINT('Ctrl Pts',(12.1588589765331,13.3376329379985,726.234558823529));
#159048=CARTESIAN_POINT('Ctrl Pts',(13.3947726768058,12.2109487310903,724.740441176471));
#159049=CARTESIAN_POINT('Ctrl Pts',(14.4026149179538,10.8763499173728,723.246323529412));
#159050=CARTESIAN_POINT('Ctrl Pts',(15.4104571591017,9.54175110365538,721.752205882353));
#159051=CARTESIAN_POINT('Ctrl Pts',(16.1559070823762,8.04468584505496,720.258088235294));
#159052=CARTESIAN_POINT('Ctrl Pts',(16.9013570056506,6.54762058645456,718.763970588235));
#159053=CARTESIAN_POINT('Ctrl Pts',(17.3590292079831,4.93906964482096,717.269852941177));
#159054=CARTESIAN_POINT('Ctrl Pts',(17.8167014103155,3.33051870318735,715.775735294118));
#159055=CARTESIAN_POINT('Ctrl Pts',(17.9710104137728,1.66525935159367,714.281617647059));
#159056=CARTESIAN_POINT('Ctrl Pts',(18.1253194172301,3.32956716117513E-15,
712.7875));
#159057=CARTESIAN_POINT('Ctrl Pts',(17.9710104137728,-1.66525935159367,
711.293382352941));
#159058=CARTESIAN_POINT('Ctrl Pts',(17.8167014103155,-3.33051870318736,
709.799264705883));
#159059=CARTESIAN_POINT('Ctrl Pts',(17.3590292079831,-4.93906964482095,
708.305147058824));
#159060=CARTESIAN_POINT('Ctrl Pts',(16.9013570056506,-6.54762058645456,
706.811029411765));
#159061=CARTESIAN_POINT('Ctrl Pts',(16.1559070823762,-8.04468584505497,
705.316911764706));
#159062=CARTESIAN_POINT('Ctrl Pts',(15.4104571591017,-9.54175110365538,
703.822794117647));
#159063=CARTESIAN_POINT('Ctrl Pts',(14.4026149179538,-10.8763499173728,
702.328676470588));
#159064=CARTESIAN_POINT('Ctrl Pts',(13.3947726768058,-12.2109487310903,
700.83455882353));
#159065=CARTESIAN_POINT('Ctrl Pts',(12.1588589765331,-13.3376329379985,
699.340441176471));
#159066=CARTESIAN_POINT('Ctrl Pts',(10.9229452762603,-14.4643171449067,
697.846323529412));
#159067=CARTESIAN_POINT('Ctrl Pts',(9.50104767561053,-15.3447188656481,
696.352205882353));
#159068=CARTESIAN_POINT('Ctrl Pts',(8.07915007496071,-16.2251205863895,
694.858088235294));
#159069=CARTESIAN_POINT('Ctrl Pts',(6.51968959134574,-16.8292587962898,
693.363970588235));
#159070=CARTESIAN_POINT('Ctrl Pts',(4.96022910773078,-17.4333970061901,
691.869852941177));
#159071=CARTESIAN_POINT('Ctrl Pts',(3.31631129755346,-17.7406985030951,
690.375735294118));
#159072=CARTESIAN_POINT('Ctrl Pts',(1.67239348737615,-18.048,688.881617647059));
#159073=CARTESIAN_POINT('Ctrl Pts',(0.,-18.048,687.3875));
#159074=CARTESIAN_POINT('Ctrl Pts',(-1.67239348737615,-18.048,685.893382352941));
#159075=CARTESIAN_POINT('Ctrl Pts',(-3.31631129755346,-17.7406985030951,
684.399264705883));
#159076=CARTESIAN_POINT('Ctrl Pts',(-4.96022910773077,-17.4333970061901,
682.905147058824));
#159077=CARTESIAN_POINT('Ctrl Pts',(-6.51968959134574,-16.8292587962898,
681.411029411765));
#159078=CARTESIAN_POINT('Ctrl Pts',(-8.07915007496071,-16.2251205863895,
679.916911764706));
#159079=CARTESIAN_POINT('Ctrl Pts',(-9.50104767561052,-15.3447188656481,
678.422794117647));
#159080=CARTESIAN_POINT('Ctrl Pts',(-10.9229452762603,-14.4643171449067,
676.928676470588));
#159081=CARTESIAN_POINT('Ctrl Pts',(-12.1588589765331,-13.3376329379985,
675.434558823529));
#159082=CARTESIAN_POINT('Ctrl Pts',(-13.3947726768058,-12.2109487310903,
673.940441176471));
#159083=CARTESIAN_POINT('Ctrl Pts',(-14.4026149179538,-10.8763499173728,
672.446323529412));
#159084=CARTESIAN_POINT('Ctrl Pts',(-15.4104571591017,-9.54175110365538,
670.952205882353));
#159085=CARTESIAN_POINT('Ctrl Pts',(-16.1559070823762,-8.04468584505497,
669.458088235294));
#159086=CARTESIAN_POINT('Ctrl Pts',(-16.9013570056506,-6.54762058645456,
667.963970588235));
#159087=CARTESIAN_POINT('Ctrl Pts',(-17.3590292079831,-4.93906964482095,
666.469852941176));
#159088=CARTESIAN_POINT('Ctrl Pts',(-17.8167014103155,-3.33051870318735,
664.975735294118));
#159089=CARTESIAN_POINT('Ctrl Pts',(-17.9710104137728,-1.66525935159368,
663.481617647059));
#159090=CARTESIAN_POINT('Ctrl Pts',(-18.1253194172301,-1.10985572039171E-15,
661.9875));
#159091=CARTESIAN_POINT('Ctrl Pts',(-17.9710104137728,1.66525935159367,
660.493382352941));
#159092=CARTESIAN_POINT('Ctrl Pts',(-17.8167014103155,3.33051870318735,
658.999264705882));
#159093=CARTESIAN_POINT('Ctrl Pts',(-17.3590292079831,4.93906964482096,
657.505147058824));
#159094=CARTESIAN_POINT('Ctrl Pts',(-16.9013570056506,6.54762058645456,
656.011029411765));
#159095=CARTESIAN_POINT('Ctrl Pts',(-16.1559070823762,8.04468584505497,
654.516911764706));
#159096=CARTESIAN_POINT('Ctrl Pts',(-15.4104571591017,9.54175110365538,
653.022794117647));
#159097=CARTESIAN_POINT('Ctrl Pts',(-14.4026149179538,10.8763499173728,
651.528676470588));
#159098=CARTESIAN_POINT('Ctrl Pts',(-13.3947726768058,12.2109487310903,
650.03455882353));
#159099=CARTESIAN_POINT('Ctrl Pts',(-12.1588589765331,13.3376329379985,
648.540441176471));
#159100=CARTESIAN_POINT('Ctrl Pts',(-10.9229452762603,14.4643171449067,
647.046323529412));
#159101=CARTESIAN_POINT('Ctrl Pts',(-9.50104767561052,15.3447188656481,
645.552205882353));
#159102=CARTESIAN_POINT('Ctrl Pts',(-8.07915007496071,16.2251205863895,
644.058088235294));
#159103=CARTESIAN_POINT('Ctrl Pts',(-6.51968959134574,16.8292587962898,
642.563970588235));
#159104=CARTESIAN_POINT('Ctrl Pts',(-4.96022910773078,17.4333970061901,
641.069852941176));
#159105=CARTESIAN_POINT('Ctrl Pts',(-3.31631129755346,17.7406985030951,
639.575735294118));
#159106=CARTESIAN_POINT('Ctrl Pts',(-1.67239348737615,18.048,638.081617647059));
#159107=CARTESIAN_POINT('Ctrl Pts',(-2.21024254310115E-15,18.048,636.5875));
#159108=CARTESIAN_POINT('Ctrl Pts',(1.67239348737616,18.048,635.093382352941));
#159109=CARTESIAN_POINT('Ctrl Pts',(3.31631129755346,17.7406985030951,633.599264705882));
#159110=CARTESIAN_POINT('Ctrl Pts',(4.96022910773077,17.4333970061901,632.105147058824));
#159111=CARTESIAN_POINT('Ctrl Pts',(6.51968959134575,16.8292587962898,630.611029411765));
#159112=CARTESIAN_POINT('Ctrl Pts',(8.07915007496071,16.2251205863895,629.116911764706));
#159113=CARTESIAN_POINT('Ctrl Pts',(9.50104767561053,15.3447188656481,627.622794117647));
#159114=CARTESIAN_POINT('Ctrl Pts',(10.9229452762603,14.4643171449067,626.128676470588));
#159115=CARTESIAN_POINT('Ctrl Pts',(12.1588589765331,13.3376329379985,624.634558823529));
#159116=CARTESIAN_POINT('Ctrl Pts',(13.3947726768058,12.2109487310903,623.140441176471));
#159117=CARTESIAN_POINT('Ctrl Pts',(14.4026149179538,10.8763499173728,621.646323529412));
#159118=CARTESIAN_POINT('Ctrl Pts',(15.4104571591017,9.54175110365538,620.152205882353));
#159119=CARTESIAN_POINT('Ctrl Pts',(16.1559070823762,8.04468584505496,618.658088235294));
#159120=CARTESIAN_POINT('Ctrl Pts',(16.9013570056506,6.54762058645456,617.163970588235));
#159121=CARTESIAN_POINT('Ctrl Pts',(17.3590292079831,4.93906964482096,615.669852941176));
#159122=CARTESIAN_POINT('Ctrl Pts',(17.8167014103155,3.33051870318735,614.175735294118));
#159123=CARTESIAN_POINT('Ctrl Pts',(17.9710104137728,1.66525935159367,612.681617647059));
#159124=CARTESIAN_POINT('Ctrl Pts',(18.1253194172301,3.32956716117513E-15,
611.1875));
#159125=CARTESIAN_POINT('Ctrl Pts',(17.9710104137728,-1.66525935159367,
609.693382352941));
#159126=CARTESIAN_POINT('Ctrl Pts',(17.8167014103155,-3.33051870318736,
608.199264705882));
#159127=CARTESIAN_POINT('Ctrl Pts',(17.3590292079831,-4.93906964482095,
606.705147058824));
#159128=CARTESIAN_POINT('Ctrl Pts',(16.9013570056506,-6.54762058645456,
605.211029411765));
#159129=CARTESIAN_POINT('Ctrl Pts',(16.1559070823762,-8.04468584505497,
603.716911764706));
#159130=CARTESIAN_POINT('Ctrl Pts',(15.4104571591017,-9.54175110365538,
602.222794117647));
#159131=CARTESIAN_POINT('Ctrl Pts',(14.4026149179538,-10.8763499173728,
600.728676470588));
#159132=CARTESIAN_POINT('Ctrl Pts',(13.3947726768058,-12.2109487310903,
599.23455882353));
#159133=CARTESIAN_POINT('Ctrl Pts',(12.1588589765331,-13.3376329379985,
597.740441176471));
#159134=CARTESIAN_POINT('Ctrl Pts',(10.9229452762603,-14.4643171449067,
596.246323529412));
#159135=CARTESIAN_POINT('Ctrl Pts',(9.50104767561053,-15.3447188656481,
594.752205882353));
#159136=CARTESIAN_POINT('Ctrl Pts',(8.07915007496071,-16.2251205863895,
593.258088235294));
#159137=CARTESIAN_POINT('Ctrl Pts',(6.51968959134574,-16.8292587962898,
591.763970588235));
#159138=CARTESIAN_POINT('Ctrl Pts',(4.96022910773078,-17.4333970061901,
590.269852941177));
#159139=CARTESIAN_POINT('Ctrl Pts',(3.31631129755346,-17.7406985030951,
588.775735294118));
#159140=CARTESIAN_POINT('Ctrl Pts',(1.67239348737615,-18.048,587.281617647059));
#159141=CARTESIAN_POINT('Ctrl Pts',(0.,-18.048,585.7875));
#159142=CARTESIAN_POINT('Ctrl Pts',(-1.67239348737615,-18.048,584.293382352941));
#159143=CARTESIAN_POINT('Ctrl Pts',(-3.31631129755346,-17.7406985030951,
582.799264705882));
#159144=CARTESIAN_POINT('Ctrl Pts',(-4.96022910773077,-17.4333970061901,
581.305147058824));
#159145=CARTESIAN_POINT('Ctrl Pts',(-6.51968959134574,-16.8292587962898,
579.811029411765));
#159146=CARTESIAN_POINT('Ctrl Pts',(-8.07915007496071,-16.2251205863895,
578.316911764706));
#159147=CARTESIAN_POINT('Ctrl Pts',(-9.50104767561052,-15.3447188656481,
576.822794117647));
#159148=CARTESIAN_POINT('Ctrl Pts',(-10.9229452762603,-14.4643171449067,
575.328676470588));
#159149=CARTESIAN_POINT('Ctrl Pts',(-12.1588589765331,-13.3376329379985,
573.834558823529));
#159150=CARTESIAN_POINT('Ctrl Pts',(-13.3947726768058,-12.2109487310903,
572.340441176471));
#159151=CARTESIAN_POINT('Ctrl Pts',(-14.4026149179538,-10.8763499173728,
570.846323529412));
#159152=CARTESIAN_POINT('Ctrl Pts',(-15.4104571591017,-9.54175110365538,
569.352205882353));
#159153=CARTESIAN_POINT('Ctrl Pts',(-16.1559070823762,-8.04468584505497,
567.858088235294));
#159154=CARTESIAN_POINT('Ctrl Pts',(-16.9013570056506,-6.54762058645456,
566.363970588235));
#159155=CARTESIAN_POINT('Ctrl Pts',(-17.3590292079831,-4.93906964482095,
564.869852941177));
#159156=CARTESIAN_POINT('Ctrl Pts',(-17.8167014103155,-3.33051870318735,
563.375735294118));
#159157=CARTESIAN_POINT('Ctrl Pts',(-17.9710104137728,-1.66525935159368,
561.881617647059));
#159158=CARTESIAN_POINT('Ctrl Pts',(-18.1253194172301,-1.10985572039171E-15,
560.3875));
#159159=CARTESIAN_POINT('Ctrl Pts',(-17.9710104137728,1.66525935159367,
558.893382352941));
#159160=CARTESIAN_POINT('Ctrl Pts',(-17.8167014103155,3.33051870318735,
557.399264705882));
#159161=CARTESIAN_POINT('Ctrl Pts',(-17.3590292079831,4.93906964482096,
555.905147058824));
#159162=CARTESIAN_POINT('Ctrl Pts',(-16.9013570056506,6.54762058645456,
554.411029411765));
#159163=CARTESIAN_POINT('Ctrl Pts',(-16.1559070823762,8.04468584505497,
552.916911764706));
#159164=CARTESIAN_POINT('Ctrl Pts',(-15.4104571591017,9.54175110365538,
551.422794117647));
#159165=CARTESIAN_POINT('Ctrl Pts',(-14.4026149179538,10.8763499173728,
549.928676470588));
#159166=CARTESIAN_POINT('Ctrl Pts',(-13.3947726768058,12.2109487310903,
548.43455882353));
#159167=CARTESIAN_POINT('Ctrl Pts',(-12.1588589765331,13.3376329379985,
546.940441176471));
#159168=CARTESIAN_POINT('Ctrl Pts',(-10.9229452762603,14.4643171449067,
545.446323529412));
#159169=CARTESIAN_POINT('Ctrl Pts',(-9.50104767561052,15.3447188656481,
543.952205882353));
#159170=CARTESIAN_POINT('Ctrl Pts',(-8.07915007496071,16.2251205863895,
542.458088235294));
#159171=CARTESIAN_POINT('Ctrl Pts',(-6.51968959134574,16.8292587962898,
540.963970588235));
#159172=CARTESIAN_POINT('Ctrl Pts',(-4.96022910773078,17.4333970061901,
539.469852941177));
#159173=CARTESIAN_POINT('Ctrl Pts',(-3.31631129755346,17.7406985030951,
537.975735294118));
#159174=CARTESIAN_POINT('Ctrl Pts',(-1.67239348737615,18.048,536.481617647059));
#159175=CARTESIAN_POINT('Ctrl Pts',(-2.21024254310115E-15,18.048,534.9875));
#159176=CARTESIAN_POINT('Ctrl Pts',(1.67239348737616,18.048,533.493382352941));
#159177=CARTESIAN_POINT('Ctrl Pts',(3.31631129755346,17.7406985030951,531.999264705882));
#159178=CARTESIAN_POINT('Ctrl Pts',(4.96022910773077,17.4333970061901,530.505147058824));
#159179=CARTESIAN_POINT('Ctrl Pts',(6.51968959134575,16.8292587962898,529.011029411765));
#159180=CARTESIAN_POINT('Ctrl Pts',(8.07915007496071,16.2251205863895,527.516911764706));
#159181=CARTESIAN_POINT('Ctrl Pts',(9.50104767561053,15.3447188656481,526.022794117647));
#159182=CARTESIAN_POINT('Ctrl Pts',(10.9229452762603,14.4643171449067,524.528676470588));
#159183=CARTESIAN_POINT('Ctrl Pts',(12.1588589765331,13.3376329379985,523.03455882353));
#159184=CARTESIAN_POINT('Ctrl Pts',(13.3947726768058,12.2109487310903,521.540441176471));
#159185=CARTESIAN_POINT('Ctrl Pts',(14.4026149179538,10.8763499173728,520.046323529412));
#159186=CARTESIAN_POINT('Ctrl Pts',(15.4104571591017,9.54175110365538,518.552205882353));
#159187=CARTESIAN_POINT('Ctrl Pts',(16.1559070823762,8.04468584505496,517.058088235294));
#159188=CARTESIAN_POINT('Ctrl Pts',(16.9013570056506,6.54762058645456,515.563970588235));
#159189=CARTESIAN_POINT('Ctrl Pts',(17.3590292079831,4.93906964482096,514.069852941176));
#159190=CARTESIAN_POINT('Ctrl Pts',(17.8167014103155,3.33051870318735,512.575735294118));
#159191=CARTESIAN_POINT('Ctrl Pts',(17.9710104137728,1.66525935159367,511.081617647059));
#159192=CARTESIAN_POINT('Ctrl Pts',(18.1253194172301,3.32956716117513E-15,
509.5875));
#159193=CARTESIAN_POINT('Ctrl Pts',(17.9710104137728,-1.66525935159367,
508.093382352941));
#159194=CARTESIAN_POINT('Ctrl Pts',(17.8167014103155,-3.33051870318736,
506.599264705882));
#159195=CARTESIAN_POINT('Ctrl Pts',(17.3590292079831,-4.93906964482095,
505.105147058824));
#159196=CARTESIAN_POINT('Ctrl Pts',(16.9013570056506,-6.54762058645456,
503.611029411765));
#159197=CARTESIAN_POINT('Ctrl Pts',(16.1559070823762,-8.04468584505497,
502.116911764706));
#159198=CARTESIAN_POINT('Ctrl Pts',(15.4104571591017,-9.54175110365538,
500.622794117647));
#159199=CARTESIAN_POINT('Ctrl Pts',(14.4026149179538,-10.8763499173728,
499.128676470588));
#159200=CARTESIAN_POINT('Ctrl Pts',(13.3947726768058,-12.2109487310903,
497.63455882353));
#159201=CARTESIAN_POINT('Ctrl Pts',(12.1588589765331,-13.3376329379985,
496.140441176471));
#159202=CARTESIAN_POINT('Ctrl Pts',(10.9229452762603,-14.4643171449067,
494.646323529412));
#159203=CARTESIAN_POINT('Ctrl Pts',(9.50104767561053,-15.3447188656481,
493.152205882353));
#159204=CARTESIAN_POINT('Ctrl Pts',(8.07915007496071,-16.2251205863895,
491.658088235294));
#159205=CARTESIAN_POINT('Ctrl Pts',(6.51968959134574,-16.8292587962898,
490.163970588235));
#159206=CARTESIAN_POINT('Ctrl Pts',(4.96022910773078,-17.4333970061901,
488.669852941177));
#159207=CARTESIAN_POINT('Ctrl Pts',(3.31631129755346,-17.7406985030951,
487.175735294118));
#159208=CARTESIAN_POINT('Ctrl Pts',(1.67239348737615,-18.048,485.681617647059));
#159209=CARTESIAN_POINT('Ctrl Pts',(0.,-18.048,484.1875));
#159210=CARTESIAN_POINT('Ctrl Pts',(-1.67239348737615,-18.048,482.693382352941));
#159211=CARTESIAN_POINT('Ctrl Pts',(-3.31631129755346,-17.7406985030951,
481.199264705882));
#159212=CARTESIAN_POINT('Ctrl Pts',(-4.96022910773077,-17.4333970061901,
479.705147058824));
#159213=CARTESIAN_POINT('Ctrl Pts',(-6.51968959134574,-16.8292587962898,
478.211029411765));
#159214=CARTESIAN_POINT('Ctrl Pts',(-8.07915007496071,-16.2251205863895,
476.716911764706));
#159215=CARTESIAN_POINT('Ctrl Pts',(-9.50104767561052,-15.3447188656481,
475.222794117647));
#159216=CARTESIAN_POINT('Ctrl Pts',(-10.9229452762603,-14.4643171449067,
473.728676470588));
#159217=CARTESIAN_POINT('Ctrl Pts',(-12.1588589765331,-13.3376329379985,
472.234558823529));
#159218=CARTESIAN_POINT('Ctrl Pts',(-13.3947726768058,-12.2109487310903,
470.740441176471));
#159219=CARTESIAN_POINT('Ctrl Pts',(-14.4026149179538,-10.8763499173728,
469.246323529412));
#159220=CARTESIAN_POINT('Ctrl Pts',(-15.4104571591017,-9.54175110365538,
467.752205882353));
#159221=CARTESIAN_POINT('Ctrl Pts',(-16.1559070823762,-8.04468584505497,
466.258088235294));
#159222=CARTESIAN_POINT('Ctrl Pts',(-16.9013570056506,-6.54762058645456,
464.763970588236));
#159223=CARTESIAN_POINT('Ctrl Pts',(-17.3590292079831,-4.93906964482095,
463.269852941177));
#159224=CARTESIAN_POINT('Ctrl Pts',(-17.8167014103155,-3.33051870318735,
461.775735294118));
#159225=CARTESIAN_POINT('Ctrl Pts',(-17.9710104137728,-1.66525935159368,
460.281617647059));
#159226=CARTESIAN_POINT('Ctrl Pts',(-18.1253194172301,-1.10985572039171E-15,
458.7875));
#159227=CARTESIAN_POINT('Ctrl Pts',(-17.9710104137728,1.66525935159367,
457.293382352941));
#159228=CARTESIAN_POINT('Ctrl Pts',(-17.8167014103155,3.33051870318735,
455.799264705882));
#159229=CARTESIAN_POINT('Ctrl Pts',(-17.3590292079831,4.93906964482096,
454.305147058824));
#159230=CARTESIAN_POINT('Ctrl Pts',(-16.9013570056506,6.54762058645456,
452.811029411765));
#159231=CARTESIAN_POINT('Ctrl Pts',(-16.1559070823762,8.04468584505497,
451.316911764706));
#159232=CARTESIAN_POINT('Ctrl Pts',(-15.4104571591017,9.54175110365538,
449.822794117647));
#159233=CARTESIAN_POINT('Ctrl Pts',(-14.4026149179538,10.8763499173728,
448.328676470588));
#159234=CARTESIAN_POINT('Ctrl Pts',(-13.3947726768058,12.2109487310903,
446.83455882353));
#159235=CARTESIAN_POINT('Ctrl Pts',(-12.1588589765331,13.3376329379985,
445.340441176471));
#159236=CARTESIAN_POINT('Ctrl Pts',(-10.9229452762603,14.4643171449067,
443.846323529412));
#159237=CARTESIAN_POINT('Ctrl Pts',(-9.50104767561052,15.3447188656481,
442.352205882353));
#159238=CARTESIAN_POINT('Ctrl Pts',(-8.07915007496071,16.2251205863895,
440.858088235294));
#159239=CARTESIAN_POINT('Ctrl Pts',(-6.51968959134574,16.8292587962898,
439.363970588235));
#159240=CARTESIAN_POINT('Ctrl Pts',(-4.96022910773078,17.4333970061901,
437.869852941176));
#159241=CARTESIAN_POINT('Ctrl Pts',(-3.31631129755346,17.7406985030951,
436.375735294118));
#159242=CARTESIAN_POINT('Ctrl Pts',(-1.67239348737615,18.048,434.881617647059));
#159243=CARTESIAN_POINT('Ctrl Pts',(-2.21024254310115E-15,18.048,433.3875));
#159244=CARTESIAN_POINT('Ctrl Pts',(1.67239348737616,18.048,431.893382352941));
#159245=CARTESIAN_POINT('Ctrl Pts',(3.31631129755346,17.7406985030951,430.399264705882));
#159246=CARTESIAN_POINT('Ctrl Pts',(4.96022910773077,17.4333970061901,428.905147058824));
#159247=CARTESIAN_POINT('Ctrl Pts',(6.51968959134575,16.8292587962898,427.411029411765));
#159248=CARTESIAN_POINT('Ctrl Pts',(8.07915007496071,16.2251205863895,425.916911764706));
#159249=CARTESIAN_POINT('Ctrl Pts',(9.50104767561053,15.3447188656481,424.422794117647));
#159250=CARTESIAN_POINT('Ctrl Pts',(10.9229452762603,14.4643171449067,422.928676470588));
#159251=CARTESIAN_POINT('Ctrl Pts',(12.1588589765331,13.3376329379985,421.43455882353));
#159252=CARTESIAN_POINT('Ctrl Pts',(13.3947726768058,12.2109487310903,419.940441176471));
#159253=CARTESIAN_POINT('Ctrl Pts',(14.4026149179538,10.8763499173728,418.446323529412));
#159254=CARTESIAN_POINT('Ctrl Pts',(15.4104571591017,9.54175110365538,416.952205882353));
#159255=CARTESIAN_POINT('Ctrl Pts',(16.1559070823762,8.04468584505496,415.458088235294));
#159256=CARTESIAN_POINT('Ctrl Pts',(16.9013570056506,6.54762058645456,413.963970588235));
#159257=CARTESIAN_POINT('Ctrl Pts',(17.3590292079831,4.93906964482096,412.469852941177));
#159258=CARTESIAN_POINT('Ctrl Pts',(17.8167014103155,3.33051870318735,410.975735294118));
#159259=CARTESIAN_POINT('Ctrl Pts',(17.9710104137728,1.66525935159367,409.481617647059));
#159260=CARTESIAN_POINT('Ctrl Pts',(18.1253194172301,3.32956716117513E-15,
407.9875));
#159261=CARTESIAN_POINT('Ctrl Pts',(17.9710104137728,-1.66525935159367,
406.493382352941));
#159262=CARTESIAN_POINT('Ctrl Pts',(17.8167014103155,-3.33051870318736,
404.999264705882));
#159263=CARTESIAN_POINT('Ctrl Pts',(17.3590292079831,-4.93906964482095,
403.505147058824));
#159264=CARTESIAN_POINT('Ctrl Pts',(16.9013570056506,-6.54762058645456,
402.011029411765));
#159265=CARTESIAN_POINT('Ctrl Pts',(16.1559070823762,-8.04468584505497,
400.516911764706));
#159266=CARTESIAN_POINT('Ctrl Pts',(15.4104571591017,-9.54175110365538,
399.022794117647));
#159267=CARTESIAN_POINT('Ctrl Pts',(14.4026149179538,-10.8763499173728,
397.528676470588));
#159268=CARTESIAN_POINT('Ctrl Pts',(13.3947726768058,-12.2109487310903,
396.034558823529));
#159269=CARTESIAN_POINT('Ctrl Pts',(12.1588589765331,-13.3376329379985,
394.540441176471));
#159270=CARTESIAN_POINT('Ctrl Pts',(10.9229452762603,-14.4643171449067,
393.046323529412));
#159271=CARTESIAN_POINT('Ctrl Pts',(9.50104767561053,-15.3447188656481,
391.552205882353));
#159272=CARTESIAN_POINT('Ctrl Pts',(8.07915007496071,-16.2251205863895,
390.058088235294));
#159273=CARTESIAN_POINT('Ctrl Pts',(6.51968959134574,-16.8292587962898,
388.563970588235));
#159274=CARTESIAN_POINT('Ctrl Pts',(4.96022910773078,-17.4333970061901,
387.069852941177));
#159275=CARTESIAN_POINT('Ctrl Pts',(3.31631129755346,-17.7406985030951,
385.575735294118));
#159276=CARTESIAN_POINT('Ctrl Pts',(1.67239348737615,-18.048,384.081617647059));
#159277=CARTESIAN_POINT('Ctrl Pts',(0.,-18.048,382.5875));
#159278=CARTESIAN_POINT('Ctrl Pts',(-1.67239348737615,-18.048,381.093382352941));
#159279=CARTESIAN_POINT('Ctrl Pts',(-3.31631129755346,-17.7406985030951,
379.599264705882));
#159280=CARTESIAN_POINT('Ctrl Pts',(-4.96022910773077,-17.4333970061901,
378.105147058823));
#159281=CARTESIAN_POINT('Ctrl Pts',(-6.51968959134574,-16.8292587962898,
376.611029411765));
#159282=CARTESIAN_POINT('Ctrl Pts',(-8.07915007496071,-16.2251205863895,
375.116911764706));
#159283=CARTESIAN_POINT('Ctrl Pts',(-9.50104767561052,-15.3447188656481,
373.622794117647));
#159284=CARTESIAN_POINT('Ctrl Pts',(-10.9229452762603,-14.4643171449067,
372.128676470588));
#159285=CARTESIAN_POINT('Ctrl Pts',(-12.1588589765331,-13.3376329379985,
370.634558823529));
#159286=CARTESIAN_POINT('Ctrl Pts',(-13.3947726768058,-12.2109487310903,
369.140441176471));
#159287=CARTESIAN_POINT('Ctrl Pts',(-14.4026149179538,-10.8763499173728,
367.646323529412));
#159288=CARTESIAN_POINT('Ctrl Pts',(-15.4104571591017,-9.54175110365538,
366.152205882353));
#159289=CARTESIAN_POINT('Ctrl Pts',(-16.1559070823762,-8.04468584505497,
364.658088235294));
#159290=CARTESIAN_POINT('Ctrl Pts',(-16.9013570056506,-6.54762058645456,
363.163970588235));
#159291=CARTESIAN_POINT('Ctrl Pts',(-17.3590292079831,-4.93906964482095,
361.669852941177));
#159292=CARTESIAN_POINT('Ctrl Pts',(-17.8167014103155,-3.33051870318735,
360.175735294118));
#159293=CARTESIAN_POINT('Ctrl Pts',(-17.9710104137728,-1.66525935159368,
358.681617647059));
#159294=CARTESIAN_POINT('Ctrl Pts',(-18.1253194172301,-1.10985572039171E-15,
357.1875));
#159295=CARTESIAN_POINT('Ctrl Pts',(-17.9710104137728,1.66525935159367,
355.693382352941));
#159296=CARTESIAN_POINT('Ctrl Pts',(-17.8167014103155,3.33051870318735,
354.199264705883));
#159297=CARTESIAN_POINT('Ctrl Pts',(-17.3590292079831,4.93906964482096,
352.705147058824));
#159298=CARTESIAN_POINT('Ctrl Pts',(-16.9013570056506,6.54762058645456,
351.211029411765));
#159299=CARTESIAN_POINT('Ctrl Pts',(-16.1559070823762,8.04468584505497,
349.716911764706));
#159300=CARTESIAN_POINT('Ctrl Pts',(-15.4104571591017,9.54175110365538,
348.222794117647));
#159301=CARTESIAN_POINT('Ctrl Pts',(-14.4026149179538,10.8763499173728,
346.728676470588));
#159302=CARTESIAN_POINT('Ctrl Pts',(-13.3947726768058,12.2109487310903,
345.234558823529));
#159303=CARTESIAN_POINT('Ctrl Pts',(-12.1588589765331,13.3376329379985,
343.740441176471));
#159304=CARTESIAN_POINT('Ctrl Pts',(-10.9229452762603,14.4643171449067,
342.246323529412));
#159305=CARTESIAN_POINT('Ctrl Pts',(-9.50104767561052,15.3447188656481,
340.752205882353));
#159306=CARTESIAN_POINT('Ctrl Pts',(-8.07915007496071,16.2251205863895,
339.258088235294));
#159307=CARTESIAN_POINT('Ctrl Pts',(-6.51968959134574,16.8292587962898,
337.763970588235));
#159308=CARTESIAN_POINT('Ctrl Pts',(-4.96022910773078,17.4333970061901,
336.269852941177));
#159309=CARTESIAN_POINT('Ctrl Pts',(-3.31631129755346,17.7406985030951,
334.775735294118));
#159310=CARTESIAN_POINT('Ctrl Pts',(-1.67239348737615,18.048,333.281617647059));
#159311=CARTESIAN_POINT('Ctrl Pts',(-2.21024254310115E-15,18.048,331.7875));
#159312=CARTESIAN_POINT('Ctrl Pts',(1.67239348737616,18.048,330.293382352941));
#159313=CARTESIAN_POINT('Ctrl Pts',(3.31631129755346,17.7406985030951,328.799264705882));
#159314=CARTESIAN_POINT('Ctrl Pts',(4.96022910773077,17.4333970061901,327.305147058824));
#159315=CARTESIAN_POINT('Ctrl Pts',(6.51968959134575,16.8292587962898,325.811029411765));
#159316=CARTESIAN_POINT('Ctrl Pts',(8.07915007496071,16.2251205863895,324.316911764706));
#159317=CARTESIAN_POINT('Ctrl Pts',(9.50104767561053,15.3447188656481,322.822794117647));
#159318=CARTESIAN_POINT('Ctrl Pts',(10.9229452762603,14.4643171449067,321.328676470588));
#159319=CARTESIAN_POINT('Ctrl Pts',(12.1588589765331,13.3376329379985,319.834558823529));
#159320=CARTESIAN_POINT('Ctrl Pts',(13.3947726768058,12.2109487310903,318.340441176471));
#159321=CARTESIAN_POINT('Ctrl Pts',(14.4026149179538,10.8763499173728,316.846323529412));
#159322=CARTESIAN_POINT('Ctrl Pts',(15.4104571591017,9.54175110365538,315.352205882353));
#159323=CARTESIAN_POINT('Ctrl Pts',(16.1559070823762,8.04468584505496,313.858088235294));
#159324=CARTESIAN_POINT('Ctrl Pts',(16.9013570056506,6.54762058645456,312.363970588235));
#159325=CARTESIAN_POINT('Ctrl Pts',(17.3590292079831,4.93906964482096,310.869852941176));
#159326=CARTESIAN_POINT('Ctrl Pts',(17.8167014103155,3.33051870318735,309.375735294118));
#159327=CARTESIAN_POINT('Ctrl Pts',(17.9710104137728,1.66525935159367,307.881617647059));
#159328=CARTESIAN_POINT('Ctrl Pts',(18.1253194172301,3.32956716117513E-15,
306.3875));
#159329=CARTESIAN_POINT('Ctrl Pts',(17.9710104137728,-1.66525935159367,
304.893382352941));
#159330=CARTESIAN_POINT('Ctrl Pts',(17.8167014103155,-3.33051870318736,
303.399264705882));
#159331=CARTESIAN_POINT('Ctrl Pts',(17.3590292079831,-4.93906964482095,
301.905147058824));
#159332=CARTESIAN_POINT('Ctrl Pts',(16.9013570056506,-6.54762058645456,
300.411029411765));
#159333=CARTESIAN_POINT('Ctrl Pts',(16.1559070823762,-8.04468584505497,
298.916911764706));
#159334=CARTESIAN_POINT('Ctrl Pts',(15.4104571591017,-9.54175110365538,
297.422794117647));
#159335=CARTESIAN_POINT('Ctrl Pts',(14.4026149179538,-10.8763499173728,
295.928676470588));
#159336=CARTESIAN_POINT('Ctrl Pts',(13.3947726768058,-12.2109487310903,
294.43455882353));
#159337=CARTESIAN_POINT('Ctrl Pts',(12.1588589765331,-13.3376329379985,
292.940441176471));
#159338=CARTESIAN_POINT('Ctrl Pts',(10.9229452762603,-14.4643171449067,
291.446323529412));
#159339=CARTESIAN_POINT('Ctrl Pts',(9.50104767561053,-15.3447188656481,
289.952205882353));
#159340=CARTESIAN_POINT('Ctrl Pts',(8.07915007496071,-16.2251205863895,
288.458088235294));
#159341=CARTESIAN_POINT('Ctrl Pts',(6.51968959134574,-16.8292587962898,
286.963970588235));
#159342=CARTESIAN_POINT('Ctrl Pts',(4.96022910773078,-17.4333970061901,
285.469852941177));
#159343=CARTESIAN_POINT('Ctrl Pts',(3.31631129755346,-17.7406985030951,
283.975735294118));
#159344=CARTESIAN_POINT('Ctrl Pts',(1.67239348737615,-18.048,282.481617647059));
#159345=CARTESIAN_POINT('Ctrl Pts',(0.,-18.048,280.9875));
#159346=CARTESIAN_POINT('Ctrl Pts',(-1.67239348737615,-18.048,279.493382352941));
#159347=CARTESIAN_POINT('Ctrl Pts',(-3.31631129755346,-17.7406985030951,
277.999264705882));
#159348=CARTESIAN_POINT('Ctrl Pts',(-4.96022910773077,-17.4333970061901,
276.505147058824));
#159349=CARTESIAN_POINT('Ctrl Pts',(-6.51968959134574,-16.8292587962898,
275.011029411765));
#159350=CARTESIAN_POINT('Ctrl Pts',(-8.07915007496071,-16.2251205863895,
273.516911764706));
#159351=CARTESIAN_POINT('Ctrl Pts',(-9.50104767561052,-15.3447188656481,
272.022794117647));
#159352=CARTESIAN_POINT('Ctrl Pts',(-10.9229452762603,-14.4643171449067,
270.528676470588));
#159353=CARTESIAN_POINT('Ctrl Pts',(-12.1588589765331,-13.3376329379985,
269.034558823529));
#159354=CARTESIAN_POINT('Ctrl Pts',(-13.3947726768058,-12.2109487310903,
267.540441176471));
#159355=CARTESIAN_POINT('Ctrl Pts',(-14.4026149179538,-10.8763499173728,
266.046323529412));
#159356=CARTESIAN_POINT('Ctrl Pts',(-15.4104571591017,-9.54175110365538,
264.552205882353));
#159357=CARTESIAN_POINT('Ctrl Pts',(-16.1559070823762,-8.04468584505497,
263.058088235294));
#159358=CARTESIAN_POINT('Ctrl Pts',(-16.9013570056506,-6.54762058645456,
261.563970588235));
#159359=CARTESIAN_POINT('Ctrl Pts',(-17.3590292079831,-4.93906964482095,
260.069852941176));
#159360=CARTESIAN_POINT('Ctrl Pts',(-17.8167014103155,-3.33051870318735,
258.575735294118));
#159361=CARTESIAN_POINT('Ctrl Pts',(-17.9710104137728,-1.66525935159368,
257.081617647059));
#159362=CARTESIAN_POINT('Ctrl Pts',(-18.1253194172301,-1.10985572039171E-15,
255.5875));
#159363=CARTESIAN_POINT('Ctrl Pts',(-17.9710104137728,1.66525935159367,
254.093382352941));
#159364=CARTESIAN_POINT('Ctrl Pts',(-17.8167014103155,3.33051870318735,
252.599264705882));
#159365=CARTESIAN_POINT('Ctrl Pts',(-17.3590292079831,4.93906964482096,
251.105147058823));
#159366=CARTESIAN_POINT('Ctrl Pts',(-16.9013570056506,6.54762058645456,
249.611029411765));
#159367=CARTESIAN_POINT('Ctrl Pts',(-16.1559070823762,8.04468584505497,
248.116911764706));
#159368=CARTESIAN_POINT('Ctrl Pts',(-15.4104571591017,9.54175110365538,
246.622794117647));
#159369=CARTESIAN_POINT('Ctrl Pts',(-14.4026149179538,10.8763499173728,
245.128676470588));
#159370=CARTESIAN_POINT('Ctrl Pts',(-13.3947726768058,12.2109487310903,
243.634558823529));
#159371=CARTESIAN_POINT('Ctrl Pts',(-12.1588589765331,13.3376329379985,
242.140441176471));
#159372=CARTESIAN_POINT('Ctrl Pts',(-10.9229452762603,14.4643171449067,
240.646323529412));
#159373=CARTESIAN_POINT('Ctrl Pts',(-9.50104767561052,15.3447188656481,
239.152205882353));
#159374=CARTESIAN_POINT('Ctrl Pts',(-8.07915007496071,16.2251205863895,
237.658088235294));
#159375=CARTESIAN_POINT('Ctrl Pts',(-6.51968959134574,16.8292587962898,
236.163970588235));
#159376=CARTESIAN_POINT('Ctrl Pts',(-4.96022910773078,17.4333970061901,
234.669852941177));
#159377=CARTESIAN_POINT('Ctrl Pts',(-3.31631129755346,17.7406985030951,
233.175735294118));
#159378=CARTESIAN_POINT('Ctrl Pts',(-1.67239348737615,18.048,231.681617647059));
#159379=CARTESIAN_POINT('Ctrl Pts',(-2.21024254310115E-15,18.048,230.1875));
#159380=CARTESIAN_POINT('Ctrl Pts',(1.67239348737616,18.048,228.693382352941));
#159381=CARTESIAN_POINT('Ctrl Pts',(3.31631129755346,17.7406985030951,227.199264705882));
#159382=CARTESIAN_POINT('Ctrl Pts',(4.96022910773077,17.4333970061901,225.705147058824));
#159383=CARTESIAN_POINT('Ctrl Pts',(6.51968959134575,16.8292587962898,224.211029411765));
#159384=CARTESIAN_POINT('Ctrl Pts',(8.07915007496071,16.2251205863895,222.716911764706));
#159385=CARTESIAN_POINT('Ctrl Pts',(9.50104767561053,15.3447188656481,221.222794117647));
#159386=CARTESIAN_POINT('Ctrl Pts',(10.9229452762603,14.4643171449067,219.728676470588));
#159387=CARTESIAN_POINT('Ctrl Pts',(12.1588589765331,13.3376329379985,218.234558823529));
#159388=CARTESIAN_POINT('Ctrl Pts',(13.3947726768058,12.2109487310903,216.740441176471));
#159389=CARTESIAN_POINT('Ctrl Pts',(14.4026149179538,10.8763499173728,215.246323529412));
#159390=CARTESIAN_POINT('Ctrl Pts',(15.4104571591017,9.54175110365538,213.752205882353));
#159391=CARTESIAN_POINT('Ctrl Pts',(16.1559070823762,8.04468584505496,212.258088235294));
#159392=CARTESIAN_POINT('Ctrl Pts',(16.9013570056506,6.54762058645456,210.763970588235));
#159393=CARTESIAN_POINT('Ctrl Pts',(17.3590292079831,4.93906964482096,209.269852941177));
#159394=CARTESIAN_POINT('Ctrl Pts',(17.8167014103155,3.33051870318735,207.775735294118));
#159395=CARTESIAN_POINT('Ctrl Pts',(17.9710104137728,1.66525935159367,206.281617647059));
#159396=CARTESIAN_POINT('Ctrl Pts',(18.1253194172301,3.32956716117513E-15,
204.7875));
#159397=CARTESIAN_POINT('Ctrl Pts',(17.9710104137728,-1.66525935159367,
203.293382352941));
#159398=CARTESIAN_POINT('Ctrl Pts',(17.8167014103155,-3.33051870318736,
201.799264705882));
#159399=CARTESIAN_POINT('Ctrl Pts',(17.3590292079831,-4.93906964482095,
200.305147058824));
#159400=CARTESIAN_POINT('Ctrl Pts',(16.9013570056506,-6.54762058645456,
198.811029411765));
#159401=CARTESIAN_POINT('Ctrl Pts',(16.1559070823762,-8.04468584505497,
197.316911764706));
#159402=CARTESIAN_POINT('Ctrl Pts',(15.4104571591017,-9.54175110365538,
195.822794117647));
#159403=CARTESIAN_POINT('Ctrl Pts',(14.4026149179538,-10.8763499173728,
194.328676470588));
#159404=CARTESIAN_POINT('Ctrl Pts',(13.3947726768058,-12.2109487310903,
192.834558823529));
#159405=CARTESIAN_POINT('Ctrl Pts',(12.1588589765331,-13.3376329379985,
191.340441176471));
#159406=CARTESIAN_POINT('Ctrl Pts',(10.9229452762603,-14.4643171449067,
189.846323529412));
#159407=CARTESIAN_POINT('Ctrl Pts',(9.50104767561053,-15.3447188656481,
188.352205882353));
#159408=CARTESIAN_POINT('Ctrl Pts',(8.07915007496071,-16.2251205863895,
186.858088235294));
#159409=CARTESIAN_POINT('Ctrl Pts',(6.51968959134574,-16.8292587962898,
185.363970588235));
#159410=CARTESIAN_POINT('Ctrl Pts',(4.96022910773078,-17.4333970061901,
183.869852941176));
#159411=CARTESIAN_POINT('Ctrl Pts',(3.31631129755346,-17.7406985030951,
182.375735294118));
#159412=CARTESIAN_POINT('Ctrl Pts',(1.67239348737615,-18.048,180.881617647059));
#159413=CARTESIAN_POINT('Ctrl Pts',(0.,-18.048,179.3875));
#159414=CARTESIAN_POINT('Ctrl Pts',(-1.67239348737615,-18.048,177.893382352941));
#159415=CARTESIAN_POINT('Ctrl Pts',(-3.31631129755346,-17.7406985030951,
176.399264705882));
#159416=CARTESIAN_POINT('Ctrl Pts',(-4.96022910773077,-17.4333970061901,
174.905147058824));
#159417=CARTESIAN_POINT('Ctrl Pts',(-6.51968959134574,-16.8292587962898,
173.411029411765));
#159418=CARTESIAN_POINT('Ctrl Pts',(-8.07915007496071,-16.2251205863895,
171.916911764706));
#159419=CARTESIAN_POINT('Ctrl Pts',(-9.50104767561052,-15.3447188656481,
170.422794117647));
#159420=CARTESIAN_POINT('Ctrl Pts',(-10.9229452762603,-14.4643171449067,
168.928676470588));
#159421=CARTESIAN_POINT('Ctrl Pts',(-12.1588589765331,-13.3376329379985,
167.43455882353));
#159422=CARTESIAN_POINT('Ctrl Pts',(-13.3947726768058,-12.2109487310903,
165.940441176471));
#159423=CARTESIAN_POINT('Ctrl Pts',(-14.4026149179538,-10.8763499173728,
164.446323529412));
#159424=CARTESIAN_POINT('Ctrl Pts',(-15.4104571591017,-9.54175110365538,
162.952205882353));
#159425=CARTESIAN_POINT('Ctrl Pts',(-16.1559070823762,-8.04468584505497,
161.458088235294));
#159426=CARTESIAN_POINT('Ctrl Pts',(-16.9013570056506,-6.54762058645456,
159.963970588235));
#159427=CARTESIAN_POINT('Ctrl Pts',(-17.3590292079831,-4.93906964482095,
158.469852941177));
#159428=CARTESIAN_POINT('Ctrl Pts',(-17.8167014103155,-3.33051870318735,
156.975735294118));
#159429=CARTESIAN_POINT('Ctrl Pts',(-17.9710104137728,-1.66525935159368,
155.481617647059));
#159430=CARTESIAN_POINT('Ctrl Pts',(-18.1253194172301,-1.10985572039171E-15,
153.9875));
#159431=CARTESIAN_POINT('Ctrl Pts',(-17.9710104137728,1.66525935159367,
152.493382352941));
#159432=CARTESIAN_POINT('Ctrl Pts',(-17.8167014103155,3.33051870318735,
150.999264705882));
#159433=CARTESIAN_POINT('Ctrl Pts',(-17.3590292079831,4.93906964482096,
149.505147058824));
#159434=CARTESIAN_POINT('Ctrl Pts',(-16.9013570056506,6.54762058645456,
148.011029411765));
#159435=CARTESIAN_POINT('Ctrl Pts',(-16.1559070823762,8.04468584505497,
146.516911764706));
#159436=CARTESIAN_POINT('Ctrl Pts',(-15.4104571591017,9.54175110365538,
145.022794117647));
#159437=CARTESIAN_POINT('Ctrl Pts',(-14.4026149179538,10.8763499173728,
143.528676470588));
#159438=CARTESIAN_POINT('Ctrl Pts',(-13.3947726768058,12.2109487310903,
142.034558823529));
#159439=CARTESIAN_POINT('Ctrl Pts',(-12.1588589765331,13.3376329379985,
140.540441176471));
#159440=CARTESIAN_POINT('Ctrl Pts',(-10.9229452762603,14.4643171449067,
139.046323529412));
#159441=CARTESIAN_POINT('Ctrl Pts',(-9.50104767561052,15.3447188656481,
137.552205882353));
#159442=CARTESIAN_POINT('Ctrl Pts',(-8.07915007496071,16.2251205863895,
136.058088235294));
#159443=CARTESIAN_POINT('Ctrl Pts',(-6.51968959134574,16.8292587962898,
134.563970588235));
#159444=CARTESIAN_POINT('Ctrl Pts',(-4.96022910773078,17.4333970061901,
133.069852941176));
#159445=CARTESIAN_POINT('Ctrl Pts',(-3.31631129755346,17.7406985030951,
131.575735294118));
#159446=CARTESIAN_POINT('Ctrl Pts',(-1.67239348737615,18.048,130.081617647059));
#159447=CARTESIAN_POINT('Ctrl Pts',(-2.21024254310115E-15,18.048,128.5875));
#159448=CARTESIAN_POINT('Ctrl Pts',(1.67239348737616,18.048,127.093382352941));
#159449=CARTESIAN_POINT('Ctrl Pts',(3.31631129755346,17.7406985030951,125.599264705882));
#159450=CARTESIAN_POINT('Ctrl Pts',(4.96022910773077,17.4333970061901,124.105147058824));
#159451=CARTESIAN_POINT('Ctrl Pts',(6.51968959134575,16.8292587962898,122.611029411765));
#159452=CARTESIAN_POINT('Ctrl Pts',(8.07915007496071,16.2251205863895,121.116911764706));
#159453=CARTESIAN_POINT('Ctrl Pts',(9.50104767561053,15.3447188656481,119.622794117647));
#159454=CARTESIAN_POINT('Ctrl Pts',(10.9229452762603,14.4643171449067,118.128676470588));
#159455=CARTESIAN_POINT('Ctrl Pts',(12.1588589765331,13.3376329379985,116.634558823529));
#159456=CARTESIAN_POINT('Ctrl Pts',(13.3947726768058,12.2109487310903,115.140441176471));
#159457=CARTESIAN_POINT('Ctrl Pts',(14.4026149179538,10.8763499173728,113.646323529412));
#159458=CARTESIAN_POINT('Ctrl Pts',(15.4104571591017,9.54175110365538,112.152205882353));
#159459=CARTESIAN_POINT('Ctrl Pts',(16.1559070823762,8.04468584505496,110.658088235294));
#159460=CARTESIAN_POINT('Ctrl Pts',(16.9013570056506,6.54762058645456,109.163970588235));
#159461=CARTESIAN_POINT('Ctrl Pts',(17.3590292079831,4.93906964482096,107.669852941177));
#159462=CARTESIAN_POINT('Ctrl Pts',(17.8167014103155,3.33051870318735,106.175735294118));
#159463=CARTESIAN_POINT('Ctrl Pts',(17.9710104137728,1.66525935159367,104.681617647059));
#159464=CARTESIAN_POINT('Ctrl Pts',(18.1253194172301,3.32956716117513E-15,
103.1875));
#159465=CARTESIAN_POINT('Ctrl Pts',(17.9710104137728,-1.66525935159367,
101.693382352941));
#159466=CARTESIAN_POINT('Ctrl Pts',(17.8167014103155,-3.33051870318736,
100.199264705882));
#159467=CARTESIAN_POINT('Ctrl Pts',(17.3590292079831,-4.93906964482095,
98.7051470588236));
#159468=CARTESIAN_POINT('Ctrl Pts',(16.9013570056506,-6.54762058645456,
97.2110294117647));
#159469=CARTESIAN_POINT('Ctrl Pts',(16.1559070823762,-8.04468584505497,
95.7169117647059));
#159470=CARTESIAN_POINT('Ctrl Pts',(15.4104571591017,-9.54175110365538,
94.222794117647));
#159471=CARTESIAN_POINT('Ctrl Pts',(14.4026149179538,-10.8763499173728,
92.7286764705884));
#159472=CARTESIAN_POINT('Ctrl Pts',(13.3947726768058,-12.2109487310903,
91.2345588235295));
#159473=CARTESIAN_POINT('Ctrl Pts',(12.1588589765331,-13.3376329379985,
89.7404411764706));
#159474=CARTESIAN_POINT('Ctrl Pts',(10.9229452762603,-14.4643171449067,
88.2463235294117));
#159475=CARTESIAN_POINT('Ctrl Pts',(9.50104767561053,-15.3447188656481,
86.7522058823529));
#159476=CARTESIAN_POINT('Ctrl Pts',(8.07915007496071,-16.2251205863895,
85.2580882352942));
#159477=CARTESIAN_POINT('Ctrl Pts',(6.51968959134574,-16.8292587962898,
83.7639705882354));
#159478=CARTESIAN_POINT('Ctrl Pts',(4.96022910773078,-17.4333970061901,
82.2698529411765));
#159479=CARTESIAN_POINT('Ctrl Pts',(3.31631129755346,-17.7406985030951,
80.7757352941176));
#159480=CARTESIAN_POINT('Ctrl Pts',(1.67239348737615,-18.048,79.2816176470588));
#159481=CARTESIAN_POINT('Ctrl Pts',(0.,-18.048,77.7875000000001));
#159482=CARTESIAN_POINT('Ctrl Pts',(-1.67239348737615,-18.048,76.2933823529413));
#159483=CARTESIAN_POINT('Ctrl Pts',(-3.31631129755346,-17.7406985030951,
74.7992647058824));
#159484=CARTESIAN_POINT('Ctrl Pts',(-4.96022910773077,-17.4333970061901,
73.3051470588235));
#159485=CARTESIAN_POINT('Ctrl Pts',(-6.51968959134574,-16.8292587962898,
71.8110294117647));
#159486=CARTESIAN_POINT('Ctrl Pts',(-8.07915007496071,-16.2251205863895,
70.316911764706));
#159487=CARTESIAN_POINT('Ctrl Pts',(-9.50104767561052,-15.3447188656481,
68.8227941176471));
#159488=CARTESIAN_POINT('Ctrl Pts',(-10.9229452762603,-14.4643171449067,
67.3286764705883));
#159489=CARTESIAN_POINT('Ctrl Pts',(-12.1588589765331,-13.3376329379985,
65.8345588235294));
#159490=CARTESIAN_POINT('Ctrl Pts',(-13.3947726768058,-12.2109487310903,
64.3404411764705));
#159491=CARTESIAN_POINT('Ctrl Pts',(-14.4026149179538,-10.8763499173728,
62.8463235294119));
#159492=CARTESIAN_POINT('Ctrl Pts',(-15.4104571591017,-9.54175110365538,
61.352205882353));
#159493=CARTESIAN_POINT('Ctrl Pts',(-16.1559070823762,-8.04468584505497,
59.8580882352941));
#159494=CARTESIAN_POINT('Ctrl Pts',(-16.9013570056506,-6.54762058645456,
58.3639705882353));
#159495=CARTESIAN_POINT('Ctrl Pts',(-17.3590292079831,-4.93906964482095,
56.8698529411764));
#159496=CARTESIAN_POINT('Ctrl Pts',(-17.8167014103155,-3.33051870318735,
55.3757352941178));
#159497=CARTESIAN_POINT('Ctrl Pts',(-17.9710104137728,-1.66525935159368,
53.8816176470589));
#159498=CARTESIAN_POINT('Ctrl Pts',(-18.1253194172301,-1.10985572039171E-15,
52.3875));
#159499=CARTESIAN_POINT('Ctrl Pts',(-17.9710104137728,1.66525935159367,
50.8933823529412));
#159500=CARTESIAN_POINT('Ctrl Pts',(-17.8167014103155,3.33051870318735,
49.3992647058823));
#159501=CARTESIAN_POINT('Ctrl Pts',(-17.3590292079831,4.93906964482096,
47.9051470588237));
#159502=CARTESIAN_POINT('Ctrl Pts',(-16.9013570056506,6.54762058645456,
46.4110294117648));
#159503=CARTESIAN_POINT('Ctrl Pts',(-16.1559070823762,8.04468584505497,
44.9169117647059));
#159504=CARTESIAN_POINT('Ctrl Pts',(-15.4104571591017,9.54175110365538,
43.422794117647));
#159505=CARTESIAN_POINT('Ctrl Pts',(-14.4026149179538,10.8763499173728,
41.9286764705882));
#159506=CARTESIAN_POINT('Ctrl Pts',(-13.3947726768058,12.2109487310903,
40.4345588235295));
#159507=CARTESIAN_POINT('Ctrl Pts',(-12.1588589765331,13.3376329379985,
38.9404411764707));
#159508=CARTESIAN_POINT('Ctrl Pts',(-10.9229452762603,14.4643171449067,
37.4463235294118));
#159509=CARTESIAN_POINT('Ctrl Pts',(-9.50104767561052,15.3447188656481,
35.9522058823529));
#159510=CARTESIAN_POINT('Ctrl Pts',(-8.07915007496071,16.2251205863895,
34.4580882352941));
#159511=CARTESIAN_POINT('Ctrl Pts',(-6.51968959134574,16.8292587962898,
32.9639705882354));
#159512=CARTESIAN_POINT('Ctrl Pts',(-4.96022910773078,17.4333970061901,
31.4698529411765));
#159513=CARTESIAN_POINT('Ctrl Pts',(-3.31631129755346,17.7406985030951,
29.9757352941177));
#159514=CARTESIAN_POINT('Ctrl Pts',(-1.67239348737615,18.048,28.4816176470588));
#159515=CARTESIAN_POINT('Ctrl Pts',(-2.21024254310115E-15,18.048,26.9874999999999));
#159516=CARTESIAN_POINT('Ctrl Pts',(1.67239348737616,18.048,25.4933823529413));
#159517=CARTESIAN_POINT('Ctrl Pts',(3.31631129755346,17.7406985030951,23.9992647058824));
#159518=CARTESIAN_POINT('Ctrl Pts',(4.96022910773077,17.4333970061901,22.5051470588236));
#159519=CARTESIAN_POINT('Ctrl Pts',(6.51968959134575,16.8292587962898,21.0110294117647));
#159520=CARTESIAN_POINT('Ctrl Pts',(8.07915007496071,16.2251205863895,19.5169117647058));
#159521=CARTESIAN_POINT('Ctrl Pts',(9.50104767561053,15.3447188656481,18.0227941176472));
#159522=CARTESIAN_POINT('Ctrl Pts',(10.9229452762603,14.4643171449067,16.5286764705883));
#159523=CARTESIAN_POINT('Ctrl Pts',(12.1588589765331,13.3376329379985,15.0345588235294));
#159524=CARTESIAN_POINT('Ctrl Pts',(13.3947726768058,12.2109487310903,13.5404411764706));
#159525=CARTESIAN_POINT('Ctrl Pts',(14.4026149179538,10.8763499173728,12.0463235294117));
#159526=CARTESIAN_POINT('Ctrl Pts',(15.4104571591017,9.54175110365538,10.5522058823531));
#159527=CARTESIAN_POINT('Ctrl Pts',(16.1559070823762,8.04468584505496,9.05808823529419));
#159528=CARTESIAN_POINT('Ctrl Pts',(16.9013570056506,6.54762058645456,7.56397058823533));
#159529=CARTESIAN_POINT('Ctrl Pts',(17.3590292079831,4.93906964482096,6.06985294117646));
#159530=CARTESIAN_POINT('Ctrl Pts',(17.8167014103155,3.33051870318735,4.57573529411759));
#159531=CARTESIAN_POINT('Ctrl Pts',(17.9710104137728,1.66525935159367,3.08161764705894));
#159532=CARTESIAN_POINT('Ctrl Pts',(18.1253194172301,3.32956716117513E-15,
1.58750000000007));
#159533=CARTESIAN_POINT('Ctrl Pts',(17.9710104137728,-1.66525935159367,
0.093382352941207));
#159534=CARTESIAN_POINT('Ctrl Pts',(17.8167014103155,-3.33051870318736,
-1.40073529411766));
#159535=CARTESIAN_POINT('Ctrl Pts',(17.3590292079831,-4.93906964482095,
-2.89485294117653));
#159536=CARTESIAN_POINT('Ctrl Pts',(16.9013570056506,-6.54762058645456,
-4.38897058823517));
#159537=CARTESIAN_POINT('Ctrl Pts',(16.1559070823762,-8.04468584505497,
-5.88308823529404));
#159538=CARTESIAN_POINT('Ctrl Pts',(15.4104571591017,-9.54175110365538,
-7.37720588235291));
#159539=CARTESIAN_POINT('Ctrl Pts',(14.4026149179538,-10.8763499173728,
-8.87132352941178));
#159540=CARTESIAN_POINT('Ctrl Pts',(13.3947726768058,-12.2109487310903,
-10.3654411764706));
#159541=CARTESIAN_POINT('Ctrl Pts',(12.1588589765331,-13.3376329379985,
-11.8595588235293));
#159542=CARTESIAN_POINT('Ctrl Pts',(10.9229452762603,-14.4643171449067,
-13.3536764705882));
#159543=CARTESIAN_POINT('Ctrl Pts',(9.50104767561053,-15.3447188656481,
-14.847794117647));
#159544=CARTESIAN_POINT('Ctrl Pts',(8.07915007496071,-16.2251205863895,
-16.3419117647059));
#159545=CARTESIAN_POINT('Ctrl Pts',(6.51968959134574,-16.8292587962898,
-17.8360294117648));
#159546=CARTESIAN_POINT('Ctrl Pts',(4.96022910773078,-17.4333970061901,
-19.3301470588234));
#159547=CARTESIAN_POINT('Ctrl Pts',(3.31631129755346,-17.7406985030951,
-20.8242647058823));
#159548=CARTESIAN_POINT('Ctrl Pts',(1.67239348737615,-18.048,-22.3183823529411));
#159549=CARTESIAN_POINT('Ctrl Pts',(0.,-18.048,-23.8125));
#159550=CARTESIAN_POINT('Ctrl Pts',(-1.67239348737615,-18.048,-25.3066176470589));
#159551=CARTESIAN_POINT('Ctrl Pts',(-3.31631129755346,-17.7406985030951,
-26.8007352941175));
#159552=CARTESIAN_POINT('Ctrl Pts',(-4.96022910773077,-17.4333970061901,
-28.2948529411764));
#159553=CARTESIAN_POINT('Ctrl Pts',(-6.51968959134574,-16.8292587962898,
-29.7889705882353));
#159554=CARTESIAN_POINT('Ctrl Pts',(-8.07915007496071,-16.2251205863895,
-31.2830882352941));
#159555=CARTESIAN_POINT('Ctrl Pts',(-9.50104767561052,-15.3447188656481,
-32.777205882353));
#159556=CARTESIAN_POINT('Ctrl Pts',(-10.9229452762603,-14.4643171449067,
-34.2713235294116));
#159557=CARTESIAN_POINT('Ctrl Pts',(-12.1588589765331,-13.3376329379985,
-35.7654411764705));
#159558=CARTESIAN_POINT('Ctrl Pts',(-13.3947726768058,-12.2109487310903,
-37.2595588235294));
#159559=CARTESIAN_POINT('Ctrl Pts',(-14.4026149179538,-10.8763499173728,
-38.7536764705882));
#159560=CARTESIAN_POINT('Ctrl Pts',(-15.4104571591017,-9.54175110365538,
-40.2477941176471));
#159561=CARTESIAN_POINT('Ctrl Pts',(-16.1559070823762,-8.04468584505497,
-41.7419117647058));
#159562=CARTESIAN_POINT('Ctrl Pts',(-16.9013570056506,-6.54762058645456,
-43.2360294117646));
#159563=CARTESIAN_POINT('Ctrl Pts',(-17.3590292079831,-4.93906964482095,
-44.7301470588235));
#159564=CARTESIAN_POINT('Ctrl Pts',(-17.8167014103155,-3.33051870318735,
-46.2242647058824));
#159565=CARTESIAN_POINT('Ctrl Pts',(-17.9710104137728,-1.66525935159368,
-47.7183823529412));
#159566=CARTESIAN_POINT('Ctrl Pts',(-18.1253194172301,-1.10985572039171E-15,
-49.2124999999999));
#159567=CARTESIAN_POINT('Ctrl Pts',(-17.9710104137728,1.66525935159367,
-50.7066176470587));
#159568=CARTESIAN_POINT('Ctrl Pts',(-17.8167014103155,3.33051870318735,
-52.2007352941176));
#159569=CARTESIAN_POINT('Ctrl Pts',(-17.3590292079831,4.93906964482096,
-53.6948529411765));
#159570=CARTESIAN_POINT('Ctrl Pts',(-16.9013570056506,6.54762058645456,
-55.1889705882354));
#159571=CARTESIAN_POINT('Ctrl Pts',(-16.1559070823762,8.04468584505497,
-56.683088235294));
#159572=CARTESIAN_POINT('Ctrl Pts',(-15.4104571591017,9.54175110365538,
-58.1772058823529));
#159573=CARTESIAN_POINT('Ctrl Pts',(-14.4026149179538,10.8763499173728,
-59.6713235294117));
#159574=CARTESIAN_POINT('Ctrl Pts',(-13.3947726768058,12.2109487310903,
-61.1654411764706));
#159575=CARTESIAN_POINT('Ctrl Pts',(-12.1588589765331,13.3376329379985,
-62.6595588235295));
#159576=CARTESIAN_POINT('Ctrl Pts',(-10.9229452762603,14.4643171449067,
-64.1536764705881));
#159577=CARTESIAN_POINT('Ctrl Pts',(-9.50104767561052,15.3447188656481,
-65.647794117647));
#159578=CARTESIAN_POINT('Ctrl Pts',(-8.07915007496071,16.2251205863895,
-67.1419117647059));
#159579=CARTESIAN_POINT('Ctrl Pts',(-6.51968959134574,16.8292587962898,
-68.6360294117647));
#159580=CARTESIAN_POINT('Ctrl Pts',(-4.96022910773078,17.4333970061901,
-70.1301470588236));
#159581=CARTESIAN_POINT('Ctrl Pts',(-3.31631129755346,17.7406985030951,
-71.6242647058822));
#159582=CARTESIAN_POINT('Ctrl Pts',(-1.67239348737615,18.048,-73.1183823529411));
#159583=CARTESIAN_POINT('Ctrl Pts',(-2.21024254310115E-15,18.048,-74.6125));
#159584=CARTESIAN_POINT('Ctrl Pts',(1.67239348737616,18.048,-76.1066176470589));
#159585=CARTESIAN_POINT('Ctrl Pts',(3.31631129755346,17.7406985030951,-77.6007352941177));
#159586=CARTESIAN_POINT('Ctrl Pts',(4.96022910773077,17.4333970061901,-79.0948529411764));
#159587=CARTESIAN_POINT('Ctrl Pts',(6.51968959134575,16.8292587962898,-80.5889705882352));
#159588=CARTESIAN_POINT('Ctrl Pts',(8.07915007496071,16.2251205863895,-82.0830882352941));
#159589=CARTESIAN_POINT('Ctrl Pts',(9.50104767561053,15.3447188656481,-83.577205882353));
#159590=CARTESIAN_POINT('Ctrl Pts',(10.9229452762603,14.4643171449067,-85.0713235294118));
#159591=CARTESIAN_POINT('Ctrl Pts',(12.1588589765331,13.3376329379985,-86.5654411764705));
#159592=CARTESIAN_POINT('Ctrl Pts',(13.3947726768058,12.2109487310903,-88.0595588235294));
#159593=CARTESIAN_POINT('Ctrl Pts',(14.4026149179538,10.8763499173728,-89.5536764705882));
#159594=CARTESIAN_POINT('Ctrl Pts',(15.4104571591017,9.54175110365538,-91.0477941176471));
#159595=CARTESIAN_POINT('Ctrl Pts',(16.1559070823762,8.04468584505496,-92.541911764706));
#159596=CARTESIAN_POINT('Ctrl Pts',(16.9013570056506,6.54762058645456,-94.0360294117646));
#159597=CARTESIAN_POINT('Ctrl Pts',(17.3590292079831,4.93906964482096,-95.5301470588235));
#159598=CARTESIAN_POINT('Ctrl Pts',(17.8167014103155,3.33051870318735,-97.0242647058824));
#159599=CARTESIAN_POINT('Ctrl Pts',(17.9710104137728,1.66525935159367,-98.5183823529412));
#159600=CARTESIAN_POINT('Ctrl Pts',(18.1253194172301,3.32956716117513E-15,
-100.0125));
#159601=CARTESIAN_POINT('Ctrl Pts',(17.9710104137728,-1.66525935159367,
-101.506617647059));
#159602=CARTESIAN_POINT('Ctrl Pts',(17.8167014103155,-3.33051870318736,
-103.000735294118));
#159603=CARTESIAN_POINT('Ctrl Pts',(17.3590292079831,-4.93906964482095,
-104.494852941176));
#159604=CARTESIAN_POINT('Ctrl Pts',(16.9013570056506,-6.54762058645456,
-105.988970588235));
#159605=CARTESIAN_POINT('Ctrl Pts',(16.1559070823762,-8.04468584505497,
-107.483088235294));
#159606=CARTESIAN_POINT('Ctrl Pts',(15.4104571591017,-9.54175110365538,
-108.977205882353));
#159607=CARTESIAN_POINT('Ctrl Pts',(14.4026149179538,-10.8763499173728,
-110.471323529412));
#159608=CARTESIAN_POINT('Ctrl Pts',(13.3947726768058,-12.2109487310903,
-111.965441176471));
#159609=CARTESIAN_POINT('Ctrl Pts',(12.1588589765331,-13.3376329379985,
-113.459558823529));
#159610=CARTESIAN_POINT('Ctrl Pts',(10.9229452762603,-14.4643171449067,
-114.953676470588));
#159611=CARTESIAN_POINT('Ctrl Pts',(9.50104767561053,-15.3447188656481,
-116.447794117647));
#159612=CARTESIAN_POINT('Ctrl Pts',(8.07915007496071,-16.2251205863895,
-117.941911764706));
#159613=CARTESIAN_POINT('Ctrl Pts',(6.51968959134574,-16.8292587962898,
-119.436029411765));
#159614=CARTESIAN_POINT('Ctrl Pts',(4.96022910773078,-17.4333970061901,
-120.930147058824));
#159615=CARTESIAN_POINT('Ctrl Pts',(3.31631129755346,-17.7406985030951,
-122.424264705882));
#159616=CARTESIAN_POINT('Ctrl Pts',(1.67239348737615,-18.048,-123.918382352941));
#159617=CARTESIAN_POINT('Ctrl Pts',(0.,-18.048,-125.4125));
#159618=CARTESIAN_POINT('Ctrl Pts',(-1.67239348737615,-18.048,-126.906617647059));
#159619=CARTESIAN_POINT('Ctrl Pts',(-3.31631129755346,-17.7406985030951,
-128.400735294118));
#159620=CARTESIAN_POINT('Ctrl Pts',(-4.96022910773077,-17.4333970061901,
-129.894852941177));
#159621=CARTESIAN_POINT('Ctrl Pts',(-6.51968959134574,-16.8292587962898,
-131.388970588235));
#159622=CARTESIAN_POINT('Ctrl Pts',(-8.07915007496071,-16.2251205863895,
-132.883088235294));
#159623=CARTESIAN_POINT('Ctrl Pts',(-9.50104767561052,-15.3447188656481,
-134.377205882353));
#159624=CARTESIAN_POINT('Ctrl Pts',(-10.9229452762603,-14.4643171449067,
-135.871323529412));
#159625=CARTESIAN_POINT('Ctrl Pts',(-12.1588589765331,-13.3376329379985,
-137.365441176471));
#159626=CARTESIAN_POINT('Ctrl Pts',(-13.3947726768058,-12.2109487310903,
-138.859558823529));
#159627=CARTESIAN_POINT('Ctrl Pts',(-14.4026149179538,-10.8763499173728,
-140.353676470588));
#159628=CARTESIAN_POINT('Ctrl Pts',(-15.4104571591017,-9.54175110365538,
-141.847794117647));
#159629=CARTESIAN_POINT('Ctrl Pts',(-16.1559070823762,-8.04468584505497,
-143.341911764706));
#159630=CARTESIAN_POINT('Ctrl Pts',(-16.9013570056506,-6.54762058645456,
-144.836029411765));
#159631=CARTESIAN_POINT('Ctrl Pts',(-17.3590292079831,-4.93906964482095,
-146.330147058823));
#159632=CARTESIAN_POINT('Ctrl Pts',(-17.8167014103155,-3.33051870318735,
-147.824264705882));
#159633=CARTESIAN_POINT('Ctrl Pts',(-17.9710104137728,-1.66525935159368,
-149.318382352941));
#159634=CARTESIAN_POINT('Ctrl Pts',(-18.1253194172301,-1.10985572039171E-15,
-150.8125));
#159635=CARTESIAN_POINT('Ctrl Pts',(-17.9710104137728,1.66525935159367,
-152.306617647059));
#159636=CARTESIAN_POINT('Ctrl Pts',(-17.8167014103155,3.33051870318735,
-153.800735294118));
#159637=CARTESIAN_POINT('Ctrl Pts',(-17.3590292079831,4.93906964482096,
-155.294852941176));
#159638=CARTESIAN_POINT('Ctrl Pts',(-16.9013570056506,6.54762058645456,
-156.788970588235));
#159639=CARTESIAN_POINT('Ctrl Pts',(-16.1559070823762,8.04468584505497,
-158.283088235294));
#159640=CARTESIAN_POINT('Ctrl Pts',(-15.4104571591017,9.54175110365538,
-159.777205882353));
#159641=CARTESIAN_POINT('Ctrl Pts',(-14.4026149179538,10.8763499173728,
-161.271323529412));
#159642=CARTESIAN_POINT('Ctrl Pts',(-13.3947726768058,12.2109487310903,
-162.765441176471));
#159643=CARTESIAN_POINT('Ctrl Pts',(-12.1588589765331,13.3376329379985,
-164.259558823529));
#159644=CARTESIAN_POINT('Ctrl Pts',(-10.9229452762603,14.4643171449067,
-165.753676470588));
#159645=CARTESIAN_POINT('Ctrl Pts',(-9.50104767561052,15.3447188656481,
-167.247794117647));
#159646=CARTESIAN_POINT('Ctrl Pts',(-8.07915007496071,16.2251205863895,
-168.741911764706));
#159647=CARTESIAN_POINT('Ctrl Pts',(-6.51968959134574,16.8292587962898,
-170.236029411765));
#159648=CARTESIAN_POINT('Ctrl Pts',(-4.96022910773078,17.4333970061901,
-171.730147058823));
#159649=CARTESIAN_POINT('Ctrl Pts',(-3.31631129755346,17.7406985030951,
-173.224264705882));
#159650=CARTESIAN_POINT('Ctrl Pts',(-1.67239348737615,18.048,-174.718382352941));
#159651=CARTESIAN_POINT('Ctrl Pts',(-2.21024254310115E-15,18.048,-176.2125));
#159652=CARTESIAN_POINT('Ctrl Pts',(1.67239348737616,18.048,-177.706617647059));
#159653=CARTESIAN_POINT('Ctrl Pts',(3.31631129755346,17.7406985030951,-179.200735294118));
#159654=CARTESIAN_POINT('Ctrl Pts',(4.96022910773077,17.4333970061901,-180.694852941176));
#159655=CARTESIAN_POINT('Ctrl Pts',(6.51968959134575,16.8292587962898,-182.188970588235));
#159656=CARTESIAN_POINT('Ctrl Pts',(8.07915007496071,16.2251205863895,-183.683088235294));
#159657=CARTESIAN_POINT('Ctrl Pts',(9.50104767561053,15.3447188656481,-185.177205882353));
#159658=CARTESIAN_POINT('Ctrl Pts',(10.9229452762603,14.4643171449067,-186.671323529412));
#159659=CARTESIAN_POINT('Ctrl Pts',(12.1588589765331,13.3376329379985,-188.165441176471));
#159660=CARTESIAN_POINT('Ctrl Pts',(13.3947726768058,12.2109487310903,-189.659558823529));
#159661=CARTESIAN_POINT('Ctrl Pts',(14.4026149179538,10.8763499173728,-191.153676470588));
#159662=CARTESIAN_POINT('Ctrl Pts',(15.4104571591017,9.54175110365538,-192.647794117647));
#159663=CARTESIAN_POINT('Ctrl Pts',(16.1559070823762,8.04468584505496,-194.141911764706));
#159664=CARTESIAN_POINT('Ctrl Pts',(16.9013570056506,6.54762058645456,-195.636029411765));
#159665=CARTESIAN_POINT('Ctrl Pts',(17.3590292079831,4.93906964482096,-197.130147058824));
#159666=CARTESIAN_POINT('Ctrl Pts',(17.8167014103155,3.33051870318735,-198.624264705882));
#159667=CARTESIAN_POINT('Ctrl Pts',(17.9710104137728,1.66525935159367,-200.118382352941));
#159668=CARTESIAN_POINT('Ctrl Pts',(18.1253194172301,3.32956716117513E-15,
-201.6125));
#159669=CARTESIAN_POINT('Ctrl Pts',(17.9710104137728,-1.66525935159367,
-203.106617647059));
#159670=CARTESIAN_POINT('Ctrl Pts',(17.8167014103155,-3.33051870318736,
-204.600735294118));
#159671=CARTESIAN_POINT('Ctrl Pts',(17.3590292079831,-4.93906964482095,
-206.094852941176));
#159672=CARTESIAN_POINT('Ctrl Pts',(16.9013570056506,-6.54762058645456,
-207.588970588235));
#159673=CARTESIAN_POINT('Ctrl Pts',(16.1559070823762,-8.04468584505497,
-209.083088235294));
#159674=CARTESIAN_POINT('Ctrl Pts',(15.4104571591017,-9.54175110365538,
-210.577205882353));
#159675=CARTESIAN_POINT('Ctrl Pts',(14.4026149179538,-10.8763499173728,
-212.071323529412));
#159676=CARTESIAN_POINT('Ctrl Pts',(13.3947726768058,-12.2109487310903,
-213.56544117647));
#159677=CARTESIAN_POINT('Ctrl Pts',(12.1588589765331,-13.3376329379985,
-215.059558823529));
#159678=CARTESIAN_POINT('Ctrl Pts',(10.9229452762603,-14.4643171449067,
-216.553676470588));
#159679=CARTESIAN_POINT('Ctrl Pts',(9.50104767561053,-15.3447188656481,
-218.047794117647));
#159680=CARTESIAN_POINT('Ctrl Pts',(8.07915007496071,-16.2251205863895,
-219.541911764706));
#159681=CARTESIAN_POINT('Ctrl Pts',(6.51968959134574,-16.8292587962898,
-221.036029411765));
#159682=CARTESIAN_POINT('Ctrl Pts',(4.96022910773078,-17.4333970061901,
-222.530147058823));
#159683=CARTESIAN_POINT('Ctrl Pts',(3.31631129755346,-17.7406985030951,
-224.024264705882));
#159684=CARTESIAN_POINT('Ctrl Pts',(1.67239348737615,-18.048,-225.518382352941));
#159685=CARTESIAN_POINT('Ctrl Pts',(0.,-18.048,-227.0125));
#159686=CARTESIAN_POINT('Ctrl Pts',(-1.67239348737615,-18.048,-228.506617647059));
#159687=CARTESIAN_POINT('Ctrl Pts',(-3.31631129755346,-17.7406985030951,
-230.000735294118));
#159688=CARTESIAN_POINT('Ctrl Pts',(-4.96022910773077,-17.4333970061901,
-231.494852941176));
#159689=CARTESIAN_POINT('Ctrl Pts',(-6.51968959134574,-16.8292587962898,
-232.988970588235));
#159690=CARTESIAN_POINT('Ctrl Pts',(-8.07915007496071,-16.2251205863895,
-234.483088235294));
#159691=CARTESIAN_POINT('Ctrl Pts',(-9.50104767561052,-15.3447188656481,
-235.977205882353));
#159692=CARTESIAN_POINT('Ctrl Pts',(-10.9229452762603,-14.4643171449067,
-237.471323529412));
#159693=CARTESIAN_POINT('Ctrl Pts',(-12.1588589765331,-13.3376329379985,
-238.965441176471));
#159694=CARTESIAN_POINT('Ctrl Pts',(-13.3947726768058,-12.2109487310903,
-240.459558823529));
#159695=CARTESIAN_POINT('Ctrl Pts',(-14.4026149179538,-10.8763499173728,
-241.953676470588));
#159696=CARTESIAN_POINT('Ctrl Pts',(-15.4104571591017,-9.54175110365538,
-243.447794117647));
#159697=CARTESIAN_POINT('Ctrl Pts',(-16.1559070823762,-8.04468584505497,
-244.941911764706));
#159698=CARTESIAN_POINT('Ctrl Pts',(-16.9013570056506,-6.54762058645456,
-246.436029411765));
#159699=CARTESIAN_POINT('Ctrl Pts',(-17.3590292079831,-4.93906964482095,
-247.930147058824));
#159700=CARTESIAN_POINT('Ctrl Pts',(-17.8167014103155,-3.33051870318735,
-249.424264705882));
#159701=CARTESIAN_POINT('Ctrl Pts',(-17.9710104137728,-1.66525935159368,
-250.918382352941));
#159702=CARTESIAN_POINT('Ctrl Pts',(-18.1253194172301,-1.10985572039171E-15,
-252.4125));
#159703=CARTESIAN_POINT('Ctrl Pts',(-17.9710104137728,1.66525935159367,
-253.906617647059));
#159704=CARTESIAN_POINT('Ctrl Pts',(-17.8167014103155,3.33051870318735,
-255.400735294118));
#159705=CARTESIAN_POINT('Ctrl Pts',(-17.3590292079831,4.93906964482096,
-256.894852941177));
#159706=CARTESIAN_POINT('Ctrl Pts',(-16.9013570056506,6.54762058645456,
-258.388970588235));
#159707=CARTESIAN_POINT('Ctrl Pts',(-16.1559070823762,8.04468584505497,
-259.883088235294));
#159708=CARTESIAN_POINT('Ctrl Pts',(-15.4104571591017,9.54175110365538,
-261.377205882353));
#159709=CARTESIAN_POINT('Ctrl Pts',(-14.4026149179538,10.8763499173728,
-262.871323529412));
#159710=CARTESIAN_POINT('Ctrl Pts',(-13.3947726768058,12.2109487310903,
-264.365441176471));
#159711=CARTESIAN_POINT('Ctrl Pts',(-12.1588589765331,13.3376329379985,
-265.859558823529));
#159712=CARTESIAN_POINT('Ctrl Pts',(-10.9229452762603,14.4643171449067,
-267.353676470588));
#159713=CARTESIAN_POINT('Ctrl Pts',(-9.50104767561052,15.3447188656481,
-268.847794117647));
#159714=CARTESIAN_POINT('Ctrl Pts',(-8.07915007496071,16.2251205863895,
-270.341911764706));
#159715=CARTESIAN_POINT('Ctrl Pts',(-6.51968959134574,16.8292587962898,
-271.836029411765));
#159716=CARTESIAN_POINT('Ctrl Pts',(-4.96022910773078,17.4333970061901,
-273.330147058823));
#159717=CARTESIAN_POINT('Ctrl Pts',(-3.31631129755346,17.7406985030951,
-274.824264705882));
#159718=CARTESIAN_POINT('Ctrl Pts',(-1.67239348737615,18.048,-276.318382352941));
#159719=CARTESIAN_POINT('Ctrl Pts',(-2.21024254310115E-15,18.048,-277.8125));
#159720=CARTESIAN_POINT('Ctrl Pts',(1.67239348737616,18.048,-279.306617647059));
#159721=CARTESIAN_POINT('Ctrl Pts',(3.31631129755346,17.7406985030951,-280.800735294118));
#159722=CARTESIAN_POINT('Ctrl Pts',(4.96022910773077,17.4333970061901,-282.294852941176));
#159723=CARTESIAN_POINT('Ctrl Pts',(6.51968959134575,16.8292587962898,-283.788970588235));
#159724=CARTESIAN_POINT('Ctrl Pts',(8.07915007496071,16.2251205863895,-285.283088235294));
#159725=CARTESIAN_POINT('Ctrl Pts',(9.50104767561053,15.3447188656481,-286.777205882353));
#159726=CARTESIAN_POINT('Ctrl Pts',(10.9229452762603,14.4643171449067,-288.271323529412));
#159727=CARTESIAN_POINT('Ctrl Pts',(12.1588589765331,13.3376329379985,-289.765441176471));
#159728=CARTESIAN_POINT('Ctrl Pts',(13.3947726768058,12.2109487310903,-291.259558823529));
#159729=CARTESIAN_POINT('Ctrl Pts',(14.4026149179538,10.8763499173728,-292.753676470588));
#159730=CARTESIAN_POINT('Ctrl Pts',(15.4104571591017,9.54175110365538,-294.247794117647));
#159731=CARTESIAN_POINT('Ctrl Pts',(16.1559070823762,8.04468584505496,-295.741911764706));
#159732=CARTESIAN_POINT('Ctrl Pts',(16.9013570056506,6.54762058645456,-297.236029411765));
#159733=CARTESIAN_POINT('Ctrl Pts',(17.3590292079831,4.93906964482096,-298.730147058823));
#159734=CARTESIAN_POINT('Ctrl Pts',(17.8167014103155,3.33051870318735,-300.224264705882));
#159735=CARTESIAN_POINT('Ctrl Pts',(17.9710104137728,1.66525935159367,-301.718382352941));
#159736=CARTESIAN_POINT('Ctrl Pts',(18.1253194172301,3.32956716117513E-15,
-303.2125));
#159737=CARTESIAN_POINT('Ctrl Pts',(17.9710104137728,-1.66525935159367,
-304.706617647059));
#159738=CARTESIAN_POINT('Ctrl Pts',(17.8167014103155,-3.33051870318736,
-306.200735294118));
#159739=CARTESIAN_POINT('Ctrl Pts',(17.3590292079831,-4.93906964482095,
-307.694852941176));
#159740=CARTESIAN_POINT('Ctrl Pts',(16.9013570056506,-6.54762058645456,
-309.188970588235));
#159741=CARTESIAN_POINT('Ctrl Pts',(16.1559070823762,-8.04468584505497,
-310.683088235294));
#159742=CARTESIAN_POINT('Ctrl Pts',(15.4104571591017,-9.54175110365538,
-312.177205882353));
#159743=CARTESIAN_POINT('Ctrl Pts',(14.4026149179538,-10.8763499173728,
-313.671323529412));
#159744=CARTESIAN_POINT('Ctrl Pts',(13.3947726768058,-12.2109487310903,
-315.165441176471));
#159745=CARTESIAN_POINT('Ctrl Pts',(12.1588589765331,-13.3376329379985,
-316.659558823529));
#159746=CARTESIAN_POINT('Ctrl Pts',(10.9229452762603,-14.4643171449067,
-318.153676470588));
#159747=CARTESIAN_POINT('Ctrl Pts',(9.50104767561053,-15.3447188656481,
-319.647794117647));
#159748=CARTESIAN_POINT('Ctrl Pts',(8.07915007496071,-16.2251205863895,
-321.141911764706));
#159749=CARTESIAN_POINT('Ctrl Pts',(6.51968959134574,-16.8292587962898,
-322.636029411765));
#159750=CARTESIAN_POINT('Ctrl Pts',(4.96022910773078,-17.4333970061901,
-324.130147058824));
#159751=CARTESIAN_POINT('Ctrl Pts',(3.31631129755346,-17.7406985030951,
-325.624264705882));
#159752=CARTESIAN_POINT('Ctrl Pts',(1.67239348737615,-18.048,-327.118382352941));
#159753=CARTESIAN_POINT('Ctrl Pts',(0.,-18.048,-328.6125));
#159754=CARTESIAN_POINT('Ctrl Pts',(-1.67239348737615,-18.048,-330.106617647059));
#159755=CARTESIAN_POINT('Ctrl Pts',(-3.31631129755346,-17.7406985030951,
-331.600735294118));
#159756=CARTESIAN_POINT('Ctrl Pts',(-4.96022910773077,-17.4333970061901,
-333.094852941176));
#159757=CARTESIAN_POINT('Ctrl Pts',(-6.51968959134574,-16.8292587962898,
-334.588970588235));
#159758=CARTESIAN_POINT('Ctrl Pts',(-8.07915007496071,-16.2251205863895,
-336.083088235294));
#159759=CARTESIAN_POINT('Ctrl Pts',(-9.50104767561052,-15.3447188656481,
-337.577205882353));
#159760=CARTESIAN_POINT('Ctrl Pts',(-10.9229452762603,-14.4643171449067,
-339.071323529412));
#159761=CARTESIAN_POINT('Ctrl Pts',(-12.1588589765331,-13.3376329379985,
-340.56544117647));
#159762=CARTESIAN_POINT('Ctrl Pts',(-13.3947726768058,-12.2109487310903,
-342.059558823529));
#159763=CARTESIAN_POINT('Ctrl Pts',(-14.4026149179538,-10.8763499173728,
-343.553676470588));
#159764=CARTESIAN_POINT('Ctrl Pts',(-15.4104571591017,-9.54175110365538,
-345.047794117647));
#159765=CARTESIAN_POINT('Ctrl Pts',(-16.1559070823762,-8.04468584505497,
-346.541911764706));
#159766=CARTESIAN_POINT('Ctrl Pts',(-16.9013570056506,-6.54762058645456,
-348.036029411765));
#159767=CARTESIAN_POINT('Ctrl Pts',(-17.3590292079831,-4.93906964482095,
-349.530147058823));
#159768=CARTESIAN_POINT('Ctrl Pts',(-17.8167014103155,-3.33051870318735,
-351.024264705883));
#159769=CARTESIAN_POINT('Ctrl Pts',(-17.9710104137728,-1.66525935159368,
-352.518382352941));
#159770=CARTESIAN_POINT('Ctrl Pts',(-18.1253194172301,-1.10985572039171E-15,
-354.0125));
#159771=CARTESIAN_POINT('Ctrl Pts',(-17.9710104137728,1.66525935159367,
-355.506617647059));
#159772=CARTESIAN_POINT('Ctrl Pts',(-17.8167014103155,3.33051870318735,
-357.000735294118));
#159773=CARTESIAN_POINT('Ctrl Pts',(-17.3590292079831,4.93906964482096,
-358.494852941176));
#159774=CARTESIAN_POINT('Ctrl Pts',(-16.9013570056506,6.54762058645456,
-359.988970588235));
#159775=CARTESIAN_POINT('Ctrl Pts',(-16.1559070823762,8.04468584505497,
-361.483088235294));
#159776=CARTESIAN_POINT('Ctrl Pts',(-15.4104571591017,9.54175110365538,
-362.977205882353));
#159777=CARTESIAN_POINT('Ctrl Pts',(-14.4026149179538,10.8763499173728,
-364.471323529412));
#159778=CARTESIAN_POINT('Ctrl Pts',(-13.3947726768058,12.2109487310903,
-365.965441176471));
#159779=CARTESIAN_POINT('Ctrl Pts',(-12.1588589765331,13.3376329379985,
-367.459558823529));
#159780=CARTESIAN_POINT('Ctrl Pts',(-10.9229452762603,14.4643171449067,
-368.953676470588));
#159781=CARTESIAN_POINT('Ctrl Pts',(-9.50104767561052,15.3447188656481,
-370.447794117647));
#159782=CARTESIAN_POINT('Ctrl Pts',(-8.07915007496071,16.2251205863895,
-371.941911764706));
#159783=CARTESIAN_POINT('Ctrl Pts',(-6.51968959134574,16.8292587962898,
-373.436029411765));
#159784=CARTESIAN_POINT('Ctrl Pts',(-4.96022910773078,17.4333970061901,
-374.930147058824));
#159785=CARTESIAN_POINT('Ctrl Pts',(-3.31631129755346,17.7406985030951,
-376.424264705882));
#159786=CARTESIAN_POINT('Ctrl Pts',(-1.67239348737615,18.048,-377.918382352941));
#159787=CARTESIAN_POINT('Ctrl Pts',(-2.21024254310115E-15,18.048,-379.4125));
#159788=CARTESIAN_POINT('Ctrl Pts',(1.67239348737616,18.048,-380.906617647059));
#159789=CARTESIAN_POINT('Ctrl Pts',(3.31631129755346,17.7406985030951,-382.400735294118));
#159790=CARTESIAN_POINT('Ctrl Pts',(4.96022910773077,17.4333970061901,-383.894852941177));
#159791=CARTESIAN_POINT('Ctrl Pts',(6.51968959134575,16.8292587962898,-385.388970588235));
#159792=CARTESIAN_POINT('Ctrl Pts',(8.07915007496071,16.2251205863895,-386.883088235294));
#159793=CARTESIAN_POINT('Ctrl Pts',(9.50104767561053,15.3447188656481,-388.377205882353));
#159794=CARTESIAN_POINT('Ctrl Pts',(10.9229452762603,14.4643171449067,-389.871323529412));
#159795=CARTESIAN_POINT('Ctrl Pts',(12.1588589765331,13.3376329379985,-391.365441176471));
#159796=CARTESIAN_POINT('Ctrl Pts',(13.3947726768058,12.2109487310903,-392.859558823529));
#159797=CARTESIAN_POINT('Ctrl Pts',(14.4026149179538,10.8763499173728,-394.353676470588));
#159798=CARTESIAN_POINT('Ctrl Pts',(15.4104571591017,9.54175110365538,-395.847794117647));
#159799=CARTESIAN_POINT('Ctrl Pts',(16.1559070823762,8.04468584505496,-397.341911764706));
#159800=CARTESIAN_POINT('Ctrl Pts',(16.9013570056506,6.54762058645456,-398.836029411765));
#159801=CARTESIAN_POINT('Ctrl Pts',(17.3590292079831,4.93906964482096,-400.330147058823));
#159802=CARTESIAN_POINT('Ctrl Pts',(17.8167014103155,3.33051870318735,-401.824264705882));
#159803=CARTESIAN_POINT('Ctrl Pts',(17.9710104137728,1.66525935159367,-403.318382352941));
#159804=CARTESIAN_POINT('Ctrl Pts',(18.1253194172301,3.32956716117513E-15,
-404.8125));
#159805=CARTESIAN_POINT('Ctrl Pts',(17.9710104137728,-1.66525935159367,
-406.306617647059));
#159806=CARTESIAN_POINT('Ctrl Pts',(17.8167014103155,-3.33051870318736,
-407.800735294118));
#159807=CARTESIAN_POINT('Ctrl Pts',(17.3590292079831,-4.93906964482095,
-409.294852941176));
#159808=CARTESIAN_POINT('Ctrl Pts',(16.9013570056506,-6.54762058645456,
-410.788970588235));
#159809=CARTESIAN_POINT('Ctrl Pts',(16.1559070823762,-8.04468584505497,
-412.283088235294));
#159810=CARTESIAN_POINT('Ctrl Pts',(15.4104571591017,-9.54175110365538,
-413.777205882353));
#159811=CARTESIAN_POINT('Ctrl Pts',(14.4026149179538,-10.8763499173728,
-415.271323529412));
#159812=CARTESIAN_POINT('Ctrl Pts',(13.3947726768058,-12.2109487310903,
-416.765441176471));
#159813=CARTESIAN_POINT('Ctrl Pts',(12.1588589765331,-13.3376329379985,
-418.259558823529));
#159814=CARTESIAN_POINT('Ctrl Pts',(10.9229452762603,-14.4643171449067,
-419.753676470588));
#159815=CARTESIAN_POINT('Ctrl Pts',(9.50104767561053,-15.3447188656481,
-421.247794117647));
#159816=CARTESIAN_POINT('Ctrl Pts',(8.07915007496071,-16.2251205863895,
-422.741911764706));
#159817=CARTESIAN_POINT('Ctrl Pts',(6.51968959134574,-16.8292587962898,
-424.236029411765));
#159818=CARTESIAN_POINT('Ctrl Pts',(4.96022910773078,-17.4333970061901,
-425.730147058824));
#159819=CARTESIAN_POINT('Ctrl Pts',(3.31631129755346,-17.7406985030951,
-427.224264705882));
#159820=CARTESIAN_POINT('Ctrl Pts',(1.67239348737615,-18.048,-428.718382352941));
#159821=CARTESIAN_POINT('Ctrl Pts',(0.,-18.048,-430.2125));
#159822=CARTESIAN_POINT('Ctrl Pts',(-1.67239348737615,-18.048,-431.706617647059));
#159823=CARTESIAN_POINT('Ctrl Pts',(-3.31631129755346,-17.7406985030951,
-433.200735294118));
#159824=CARTESIAN_POINT('Ctrl Pts',(-4.96022910773077,-17.4333970061901,
-434.694852941176));
#159825=CARTESIAN_POINT('Ctrl Pts',(-6.51968959134574,-16.8292587962898,
-436.188970588235));
#159826=CARTESIAN_POINT('Ctrl Pts',(-8.07915007496071,-16.2251205863895,
-437.683088235294));
#159827=CARTESIAN_POINT('Ctrl Pts',(-9.50104767561052,-15.3447188656481,
-439.177205882353));
#159828=CARTESIAN_POINT('Ctrl Pts',(-10.9229452762603,-14.4643171449067,
-440.671323529412));
#159829=CARTESIAN_POINT('Ctrl Pts',(-12.1588589765331,-13.3376329379985,
-442.165441176471));
#159830=CARTESIAN_POINT('Ctrl Pts',(-13.3947726768058,-12.2109487310903,
-443.65955882353));
#159831=CARTESIAN_POINT('Ctrl Pts',(-14.4026149179538,-10.8763499173728,
-445.153676470588));
#159832=CARTESIAN_POINT('Ctrl Pts',(-15.4104571591017,-9.54175110365538,
-446.647794117647));
#159833=CARTESIAN_POINT('Ctrl Pts',(-16.1559070823762,-8.04468584505497,
-448.141911764706));
#159834=CARTESIAN_POINT('Ctrl Pts',(-16.9013570056506,-6.54762058645456,
-449.636029411765));
#159835=CARTESIAN_POINT('Ctrl Pts',(-17.3590292079831,-4.93906964482095,
-451.130147058824));
#159836=CARTESIAN_POINT('Ctrl Pts',(-17.8167014103155,-3.33051870318735,
-452.624264705882));
#159837=CARTESIAN_POINT('Ctrl Pts',(-17.9710104137728,-1.66525935159368,
-454.118382352941));
#159838=CARTESIAN_POINT('Ctrl Pts',(-18.1253194172301,-1.10985572039171E-15,
-455.6125));
#159839=CARTESIAN_POINT('Ctrl Pts',(-17.9710104137728,1.66525935159367,
-457.106617647059));
#159840=CARTESIAN_POINT('Ctrl Pts',(-17.8167014103155,3.33051870318735,
-458.600735294118));
#159841=CARTESIAN_POINT('Ctrl Pts',(-17.3590292079831,4.93906964482096,
-460.094852941176));
#159842=CARTESIAN_POINT('Ctrl Pts',(-16.9013570056506,6.54762058645456,
-461.588970588235));
#159843=CARTESIAN_POINT('Ctrl Pts',(-16.1559070823762,8.04468584505497,
-463.083088235294));
#159844=CARTESIAN_POINT('Ctrl Pts',(-15.4104571591017,9.54175110365538,
-464.577205882353));
#159845=CARTESIAN_POINT('Ctrl Pts',(-14.4026149179538,10.8763499173728,
-466.071323529412));
#159846=CARTESIAN_POINT('Ctrl Pts',(-13.3947726768058,12.2109487310903,
-467.565441176471));
#159847=CARTESIAN_POINT('Ctrl Pts',(-12.1588589765331,13.3376329379985,
-469.059558823529));
#159848=CARTESIAN_POINT('Ctrl Pts',(-10.9229452762603,14.4643171449067,
-470.553676470588));
#159849=CARTESIAN_POINT('Ctrl Pts',(-9.50104767561052,15.3447188656481,
-472.047794117647));
#159850=CARTESIAN_POINT('Ctrl Pts',(-8.07915007496071,16.2251205863895,
-473.541911764706));
#159851=CARTESIAN_POINT('Ctrl Pts',(-6.51968959134574,16.8292587962898,
-475.036029411765));
#159852=CARTESIAN_POINT('Ctrl Pts',(-4.96022910773078,17.4333970061901,
-476.530147058824));
#159853=CARTESIAN_POINT('Ctrl Pts',(-3.31631129755346,17.7406985030951,
-478.024264705882));
#159854=CARTESIAN_POINT('Ctrl Pts',(-1.67239348737615,18.048,-479.518382352941));
#159855=CARTESIAN_POINT('Ctrl Pts',(-2.21024254310115E-15,18.048,-481.0125));
#159856=CARTESIAN_POINT('Ctrl Pts',(1.67239348737616,18.048,-482.506617647059));
#159857=CARTESIAN_POINT('Ctrl Pts',(3.31631129755346,17.7406985030951,-484.000735294118));
#159858=CARTESIAN_POINT('Ctrl Pts',(4.96022910773077,17.4333970061901,-485.494852941177));
#159859=CARTESIAN_POINT('Ctrl Pts',(6.51968959134575,16.8292587962898,-486.988970588235));
#159860=CARTESIAN_POINT('Ctrl Pts',(8.07915007496071,16.2251205863895,-488.483088235294));
#159861=CARTESIAN_POINT('Ctrl Pts',(9.50104767561053,15.3447188656481,-489.977205882353));
#159862=CARTESIAN_POINT('Ctrl Pts',(10.9229452762603,14.4643171449067,-491.471323529412));
#159863=CARTESIAN_POINT('Ctrl Pts',(12.1588589765331,13.3376329379985,-492.965441176471));
#159864=CARTESIAN_POINT('Ctrl Pts',(13.3947726768058,12.2109487310903,-494.45955882353));
#159865=CARTESIAN_POINT('Ctrl Pts',(14.4026149179538,10.8763499173728,-495.953676470588));
#159866=CARTESIAN_POINT('Ctrl Pts',(15.4104571591017,9.54175110365538,-497.447794117647));
#159867=CARTESIAN_POINT('Ctrl Pts',(16.1559070823762,8.04468584505496,-498.941911764706));
#159868=CARTESIAN_POINT('Ctrl Pts',(16.9013570056506,6.54762058645456,-500.436029411765));
#159869=CARTESIAN_POINT('Ctrl Pts',(17.3590292079831,4.93906964482096,-501.930147058824));
#159870=CARTESIAN_POINT('Ctrl Pts',(17.8167014103155,3.33051870318735,-503.424264705883));
#159871=CARTESIAN_POINT('Ctrl Pts',(17.9710104137728,1.66525935159367,-504.918382352941));
#159872=CARTESIAN_POINT('Ctrl Pts',(18.1253194172301,3.32956716117513E-15,
-506.4125));
#159873=CARTESIAN_POINT('Ctrl Pts',(17.9710104137728,-1.66525935159367,
-507.906617647059));
#159874=CARTESIAN_POINT('Ctrl Pts',(17.8167014103155,-3.33051870318736,
-509.400735294117));
#159875=CARTESIAN_POINT('Ctrl Pts',(17.3590292079831,-4.93906964482095,
-510.894852941176));
#159876=CARTESIAN_POINT('Ctrl Pts',(16.9013570056506,-6.54762058645456,
-512.388970588235));
#159877=CARTESIAN_POINT('Ctrl Pts',(16.1559070823762,-8.04468584505497,
-513.883088235294));
#159878=CARTESIAN_POINT('Ctrl Pts',(15.4104571591017,-9.54175110365538,
-515.377205882353));
#159879=CARTESIAN_POINT('Ctrl Pts',(14.4026149179538,-10.8763499173728,
-516.871323529412));
#159880=CARTESIAN_POINT('Ctrl Pts',(13.3947726768058,-12.2109487310903,
-518.365441176471));
#159881=CARTESIAN_POINT('Ctrl Pts',(12.1588589765331,-13.3376329379985,
-519.85955882353));
#159882=CARTESIAN_POINT('Ctrl Pts',(10.9229452762603,-14.4643171449067,
-521.353676470588));
#159883=CARTESIAN_POINT('Ctrl Pts',(9.50104767561053,-15.3447188656481,
-522.847794117647));
#159884=CARTESIAN_POINT('Ctrl Pts',(8.07915007496071,-16.2251205863895,
-524.341911764706));
#159885=CARTESIAN_POINT('Ctrl Pts',(6.51968959134574,-16.8292587962898,
-525.836029411765));
#159886=CARTESIAN_POINT('Ctrl Pts',(4.96022910773078,-17.4333970061901,
-527.330147058823));
#159887=CARTESIAN_POINT('Ctrl Pts',(3.31631129755346,-17.7406985030951,
-528.824264705882));
#159888=CARTESIAN_POINT('Ctrl Pts',(1.67239348737615,-18.048,-530.318382352941));
#159889=CARTESIAN_POINT('Ctrl Pts',(0.,-18.048,-531.8125));
#159890=CARTESIAN_POINT('Ctrl Pts',(-1.67239348737615,-18.048,-533.306617647059));
#159891=CARTESIAN_POINT('Ctrl Pts',(-3.31631129755346,-17.7406985030951,
-534.800735294118));
#159892=CARTESIAN_POINT('Ctrl Pts',(-4.96022910773077,-17.4333970061901,
-536.294852941177));
#159893=CARTESIAN_POINT('Ctrl Pts',(-6.51968959134574,-16.8292587962898,
-537.788970588235));
#159894=CARTESIAN_POINT('Ctrl Pts',(-8.07915007496071,-16.2251205863895,
-539.283088235294));
#159895=CARTESIAN_POINT('Ctrl Pts',(-9.50104767561052,-15.3447188656481,
-540.777205882353));
#159896=CARTESIAN_POINT('Ctrl Pts',(-10.9229452762603,-14.4643171449067,
-542.271323529412));
#159897=CARTESIAN_POINT('Ctrl Pts',(-12.1588589765331,-13.3376329379985,
-543.765441176471));
#159898=CARTESIAN_POINT('Ctrl Pts',(-13.3947726768058,-12.2109487310903,
-545.259558823529));
#159899=CARTESIAN_POINT('Ctrl Pts',(-14.4026149179538,-10.8763499173728,
-546.753676470588));
#159900=CARTESIAN_POINT('Ctrl Pts',(-15.4104571591017,-9.54175110365538,
-548.247794117647));
#159901=CARTESIAN_POINT('Ctrl Pts',(-16.1559070823762,-8.04468584505497,
-549.741911764706));
#159902=CARTESIAN_POINT('Ctrl Pts',(-16.9013570056506,-6.54762058645456,
-551.236029411765));
#159903=CARTESIAN_POINT('Ctrl Pts',(-17.3590292079831,-4.93906964482095,
-552.730147058823));
#159904=CARTESIAN_POINT('Ctrl Pts',(-17.8167014103155,-3.33051870318735,
-554.224264705882));
#159905=CARTESIAN_POINT('Ctrl Pts',(-17.9710104137728,-1.66525935159368,
-555.718382352941));
#159906=CARTESIAN_POINT('Ctrl Pts',(-18.1253194172301,-1.10985572039171E-15,
-557.2125));
#159907=CARTESIAN_POINT('Ctrl Pts',(-17.9710104137728,1.66525935159367,
-558.706617647059));
#159908=CARTESIAN_POINT('Ctrl Pts',(-17.8167014103155,3.33051870318735,
-560.200735294118));
#159909=CARTESIAN_POINT('Ctrl Pts',(-17.3590292079831,4.93906964482096,
-561.694852941176));
#159910=CARTESIAN_POINT('Ctrl Pts',(-16.9013570056506,6.54762058645456,
-563.188970588235));
#159911=CARTESIAN_POINT('Ctrl Pts',(-16.1559070823762,8.04468584505497,
-564.683088235294));
#159912=CARTESIAN_POINT('Ctrl Pts',(-15.4104571591017,9.54175110365538,
-566.177205882353));
#159913=CARTESIAN_POINT('Ctrl Pts',(-14.4026149179538,10.8763499173728,
-567.671323529412));
#159914=CARTESIAN_POINT('Ctrl Pts',(-13.3947726768058,12.2109487310903,
-569.16544117647));
#159915=CARTESIAN_POINT('Ctrl Pts',(-12.1588589765331,13.3376329379985,
-570.659558823529));
#159916=CARTESIAN_POINT('Ctrl Pts',(-10.9229452762603,14.4643171449067,
-572.153676470588));
#159917=CARTESIAN_POINT('Ctrl Pts',(-9.50104767561052,15.3447188656481,
-573.647794117647));
#159918=CARTESIAN_POINT('Ctrl Pts',(-8.07915007496071,16.2251205863895,
-575.141911764706));
#159919=CARTESIAN_POINT('Ctrl Pts',(-6.51968959134574,16.8292587962898,
-576.636029411765));
#159920=CARTESIAN_POINT('Ctrl Pts',(-4.96022910773078,17.4333970061901,
-578.130147058824));
#159921=CARTESIAN_POINT('Ctrl Pts',(-3.31631129755346,17.7406985030951,
-579.624264705882));
#159922=CARTESIAN_POINT('Ctrl Pts',(-1.67239348737615,18.048,-581.118382352941));
#159923=CARTESIAN_POINT('Ctrl Pts',(-2.21024254310115E-15,18.048,-582.6125));
#159924=CARTESIAN_POINT('Ctrl Pts',(1.67239348737616,18.048,-584.106617647059));
#159925=CARTESIAN_POINT('Ctrl Pts',(3.31631129755346,17.7406985030951,-585.600735294117));
#159926=CARTESIAN_POINT('Ctrl Pts',(4.96022910773077,17.4333970061901,-587.094852941176));
#159927=CARTESIAN_POINT('Ctrl Pts',(6.51968959134575,16.8292587962898,-588.588970588235));
#159928=CARTESIAN_POINT('Ctrl Pts',(8.07915007496071,16.2251205863895,-590.083088235294));
#159929=CARTESIAN_POINT('Ctrl Pts',(9.50104767561053,15.3447188656481,-591.577205882353));
#159930=CARTESIAN_POINT('Ctrl Pts',(10.9229452762603,14.4643171449067,-593.071323529412));
#159931=CARTESIAN_POINT('Ctrl Pts',(12.1588589765331,13.3376329379985,-594.565441176471));
#159932=CARTESIAN_POINT('Ctrl Pts',(13.3947726768058,12.2109487310903,-596.05955882353));
#159933=CARTESIAN_POINT('Ctrl Pts',(14.4026149179538,10.8763499173728,-597.553676470588));
#159934=CARTESIAN_POINT('Ctrl Pts',(15.4104571591017,9.54175110365538,-599.047794117647));
#159935=CARTESIAN_POINT('Ctrl Pts',(16.1559070823762,8.04468584505496,-600.541911764706));
#159936=CARTESIAN_POINT('Ctrl Pts',(16.9013570056506,6.54762058645456,-602.036029411765));
#159937=CARTESIAN_POINT('Ctrl Pts',(17.3590292079831,4.93906964482096,-603.530147058823));
#159938=CARTESIAN_POINT('Ctrl Pts',(17.8167014103155,3.33051870318735,-605.024264705882));
#159939=CARTESIAN_POINT('Ctrl Pts',(17.9710104137728,1.66525935159367,-606.518382352941));
#159940=CARTESIAN_POINT('Ctrl Pts',(18.1253194172301,3.32956716117513E-15,
-608.0125));
#159941=CARTESIAN_POINT('Ctrl Pts',(17.9710104137728,-1.66525935159367,
-609.506617647059));
#159942=CARTESIAN_POINT('Ctrl Pts',(17.8167014103155,-3.33051870318736,
-611.000735294118));
#159943=CARTESIAN_POINT('Ctrl Pts',(17.3590292079831,-4.93906964482095,
-612.494852941176));
#159944=CARTESIAN_POINT('Ctrl Pts',(16.9013570056506,-6.54762058645456,
-613.988970588235));
#159945=CARTESIAN_POINT('Ctrl Pts',(16.1559070823762,-8.04468584505497,
-615.483088235294));
#159946=CARTESIAN_POINT('Ctrl Pts',(15.4104571591017,-9.54175110365538,
-616.977205882353));
#159947=CARTESIAN_POINT('Ctrl Pts',(14.4026149179538,-10.8763499173728,
-618.471323529412));
#159948=CARTESIAN_POINT('Ctrl Pts',(13.3947726768058,-12.2109487310903,
-619.96544117647));
#159949=CARTESIAN_POINT('Ctrl Pts',(12.1588589765331,-13.3376329379985,
-621.459558823529));
#159950=CARTESIAN_POINT('Ctrl Pts',(10.9229452762603,-14.4643171449067,
-622.953676470588));
#159951=CARTESIAN_POINT('Ctrl Pts',(9.50104767561053,-15.3447188656481,
-624.447794117647));
#159952=CARTESIAN_POINT('Ctrl Pts',(8.07915007496071,-16.2251205863895,
-625.941911764706));
#159953=CARTESIAN_POINT('Ctrl Pts',(6.51968959134574,-16.8292587962898,
-627.436029411764));
#159954=CARTESIAN_POINT('Ctrl Pts',(4.96022910773078,-17.4333970061901,
-628.930147058823));
#159955=CARTESIAN_POINT('Ctrl Pts',(3.31631129755346,-17.7406985030951,
-630.424264705882));
#159956=CARTESIAN_POINT('Ctrl Pts',(1.67239348737615,-18.048,-631.918382352941));
#159957=CARTESIAN_POINT('Ctrl Pts',(0.,-18.048,-633.4125));
#159958=CARTESIAN_POINT('Ctrl Pts',(-1.67239348737615,-18.048,-634.906617647059));
#159959=CARTESIAN_POINT('Ctrl Pts',(-3.31631129755346,-17.7406985030951,
-636.400735294118));
#159960=CARTESIAN_POINT('Ctrl Pts',(-4.96022910773077,-17.4333970061901,
-637.894852941177));
#159961=CARTESIAN_POINT('Ctrl Pts',(-6.51968959134574,-16.8292587962898,
-639.388970588235));
#159962=CARTESIAN_POINT('Ctrl Pts',(-8.07915007496071,-16.2251205863895,
-640.883088235294));
#159963=CARTESIAN_POINT('Ctrl Pts',(-9.50104767561052,-15.3447188656481,
-642.377205882353));
#159964=CARTESIAN_POINT('Ctrl Pts',(-10.9229452762603,-14.4643171449067,
-643.871323529412));
#159965=CARTESIAN_POINT('Ctrl Pts',(-12.1588589765331,-13.3376329379985,
-645.36544117647));
#159966=CARTESIAN_POINT('Ctrl Pts',(-13.3947726768058,-12.2109487310903,
-646.859558823529));
#159967=CARTESIAN_POINT('Ctrl Pts',(-14.4026149179538,-10.8763499173728,
-648.353676470588));
#159968=CARTESIAN_POINT('Ctrl Pts',(-15.4104571591017,-9.54175110365538,
-649.847794117647));
#159969=CARTESIAN_POINT('Ctrl Pts',(-16.1559070823762,-8.04468584505497,
-651.341911764706));
#159970=CARTESIAN_POINT('Ctrl Pts',(-16.9013570056506,-6.54762058645456,
-652.836029411765));
#159971=CARTESIAN_POINT('Ctrl Pts',(-17.3590292079831,-4.93906964482095,
-654.330147058824));
#159972=CARTESIAN_POINT('Ctrl Pts',(-17.8167014103155,-3.33051870318735,
-655.824264705882));
#159973=CARTESIAN_POINT('Ctrl Pts',(-17.9710104137728,-1.66525935159368,
-657.318382352941));
#159974=CARTESIAN_POINT('Ctrl Pts',(-18.1253194172301,-1.10985572039171E-15,
-658.8125));
#159975=CARTESIAN_POINT('Ctrl Pts',(-17.9710104137728,1.66525935159367,
-660.306617647059));
#159976=CARTESIAN_POINT('Ctrl Pts',(-17.8167014103155,3.33051870318735,
-661.800735294117));
#159977=CARTESIAN_POINT('Ctrl Pts',(-17.3590292079831,4.93906964482096,
-663.294852941176));
#159978=CARTESIAN_POINT('Ctrl Pts',(-16.9013570056506,6.54762058645456,
-664.788970588236));
#159979=CARTESIAN_POINT('Ctrl Pts',(-16.1559070823762,8.04468584505497,
-666.283088235294));
#159980=CARTESIAN_POINT('Ctrl Pts',(-15.4104571591017,9.54175110365538,
-667.777205882353));
#159981=CARTESIAN_POINT('Ctrl Pts',(-14.4026149179538,10.8763499173728,
-669.271323529412));
#159982=CARTESIAN_POINT('Ctrl Pts',(-13.3947726768058,12.2109487310903,
-670.765441176471));
#159983=CARTESIAN_POINT('Ctrl Pts',(-12.1588589765331,13.3376329379985,
-672.259558823529));
#159984=CARTESIAN_POINT('Ctrl Pts',(-10.9229452762603,14.4643171449067,
-673.753676470588));
#159985=CARTESIAN_POINT('Ctrl Pts',(-9.50104767561052,15.3447188656481,
-675.247794117647));
#159986=CARTESIAN_POINT('Ctrl Pts',(-8.07915007496071,16.2251205863895,
-676.741911764706));
#159987=CARTESIAN_POINT('Ctrl Pts',(-6.51968959134574,16.8292587962898,
-678.236029411765));
#159988=CARTESIAN_POINT('Ctrl Pts',(-4.96022910773078,17.4333970061901,
-679.730147058824));
#159989=CARTESIAN_POINT('Ctrl Pts',(-3.31631129755346,17.7406985030951,
-681.224264705883));
#159990=CARTESIAN_POINT('Ctrl Pts',(-1.67239348737615,18.048,-682.718382352941));
#159991=CARTESIAN_POINT('Ctrl Pts',(-2.21024254310115E-15,18.048,-684.2125));
#159992=CARTESIAN_POINT('Ctrl Pts',(1.67239348737616,18.048,-685.706617647059));
#159993=CARTESIAN_POINT('Ctrl Pts',(3.31631129755346,17.7406985030951,-687.200735294118));
#159994=CARTESIAN_POINT('Ctrl Pts',(4.96022910773077,17.4333970061901,-688.694852941176));
#159995=CARTESIAN_POINT('Ctrl Pts',(6.51968959134575,16.8292587962898,-690.188970588235));
#159996=CARTESIAN_POINT('Ctrl Pts',(8.07915007496071,16.2251205863895,-691.683088235294));
#159997=CARTESIAN_POINT('Ctrl Pts',(9.50104767561053,15.3447188656481,-693.177205882353));
#159998=CARTESIAN_POINT('Ctrl Pts',(10.9229452762603,14.4643171449067,-694.671323529412));
#159999=CARTESIAN_POINT('Ctrl Pts',(12.1588589765331,13.3376329379985,-696.165441176471));
#160000=CARTESIAN_POINT('Ctrl Pts',(13.3947726768058,12.2109487310903,-697.659558823529));
#160001=CARTESIAN_POINT('Ctrl Pts',(14.4026149179538,10.8763499173728,-699.153676470588));
#160002=CARTESIAN_POINT('Ctrl Pts',(15.4104571591017,9.54175110365538,-700.647794117647));
#160003=CARTESIAN_POINT('Ctrl Pts',(16.1559070823762,8.04468584505496,-702.141911764706));
#160004=CARTESIAN_POINT('Ctrl Pts',(16.9013570056506,6.54762058645456,-703.636029411765));
#160005=CARTESIAN_POINT('Ctrl Pts',(17.3590292079831,4.93906964482096,-705.130147058823));
#160006=CARTESIAN_POINT('Ctrl Pts',(17.8167014103155,3.33051870318735,-706.624264705882));
#160007=CARTESIAN_POINT('Ctrl Pts',(17.9710104137728,1.66525935159367,-708.118382352941));
#160008=CARTESIAN_POINT('Ctrl Pts',(18.1253194172301,3.32956716117513E-15,
-709.6125));
#160009=CARTESIAN_POINT('Ctrl Pts',(17.9710104137728,-1.66525935159367,
-711.106617647059));
#160010=CARTESIAN_POINT('Ctrl Pts',(17.8167014103155,-3.33051870318736,
-712.600735294118));
#160011=CARTESIAN_POINT('Ctrl Pts',(17.3590292079831,-4.93906964482095,
-714.094852941177));
#160012=CARTESIAN_POINT('Ctrl Pts',(16.9013570056506,-6.54762058645456,
-715.588970588235));
#160013=CARTESIAN_POINT('Ctrl Pts',(16.1559070823762,-8.04468584505497,
-717.083088235294));
#160014=CARTESIAN_POINT('Ctrl Pts',(15.4104571591017,-9.54175110365538,
-718.577205882353));
#160015=CARTESIAN_POINT('Ctrl Pts',(14.4026149179538,-10.8763499173728,
-720.071323529412));
#160016=CARTESIAN_POINT('Ctrl Pts',(13.3947726768058,-12.2109487310903,
-721.56544117647));
#160017=CARTESIAN_POINT('Ctrl Pts',(12.1588589765331,-13.3376329379985,
-723.059558823529));
#160018=CARTESIAN_POINT('Ctrl Pts',(10.9229452762603,-14.4643171449067,
-724.553676470588));
#160019=CARTESIAN_POINT('Ctrl Pts',(9.50104767561053,-15.3447188656481,
-726.047794117647));
#160020=CARTESIAN_POINT('Ctrl Pts',(8.07915007496071,-16.2251205863895,
-727.541911764706));
#160021=CARTESIAN_POINT('Ctrl Pts',(6.51968959134574,-16.8292587962898,
-729.036029411765));
#160022=CARTESIAN_POINT('Ctrl Pts',(4.96022910773078,-17.4333970061901,
-730.530147058824));
#160023=CARTESIAN_POINT('Ctrl Pts',(3.31631129755346,-17.7406985030951,
-732.024264705882));
#160024=CARTESIAN_POINT('Ctrl Pts',(1.67239348737615,-18.048,-733.518382352941));
#160025=CARTESIAN_POINT('Ctrl Pts',(0.,-18.048,-735.0125));
#160026=CARTESIAN_POINT('Ctrl Pts',(-1.67239348737615,-18.048,-736.506617647059));
#160027=CARTESIAN_POINT('Ctrl Pts',(-3.31631129755346,-17.7406985030951,
-738.000735294118));
#160028=CARTESIAN_POINT('Ctrl Pts',(-4.96022910773077,-17.4333970061901,
-739.494852941177));
#160029=CARTESIAN_POINT('Ctrl Pts',(-6.51968959134574,-16.8292587962898,
-740.988970588235));
#160030=CARTESIAN_POINT('Ctrl Pts',(-8.07915007496071,-16.2251205863895,
-742.483088235294));
#160031=CARTESIAN_POINT('Ctrl Pts',(-9.50104767561052,-15.3447188656481,
-743.977205882353));
#160032=CARTESIAN_POINT('Ctrl Pts',(-10.9229452762603,-14.4643171449067,
-745.471323529412));
#160033=CARTESIAN_POINT('Ctrl Pts',(-12.1588589765331,-13.3376329379985,
-746.96544117647));
#160034=CARTESIAN_POINT('Ctrl Pts',(-13.3947726768058,-12.2109487310903,
-748.459558823529));
#160035=CARTESIAN_POINT('Ctrl Pts',(-14.4026149179538,-10.8763499173728,
-749.953676470588));
#160036=CARTESIAN_POINT('Ctrl Pts',(-15.4104571591017,-9.54175110365538,
-751.447794117647));
#160037=CARTESIAN_POINT('Ctrl Pts',(-16.1559070823762,-8.04468584505497,
-752.941911764706));
#160038=CARTESIAN_POINT('Ctrl Pts',(-16.9013570056506,-6.54762058645456,
-754.436029411765));
#160039=CARTESIAN_POINT('Ctrl Pts',(-17.3590292079831,-4.93906964482095,
-755.930147058824));
#160040=CARTESIAN_POINT('Ctrl Pts',(-17.8167014103155,-3.33051870318735,
-757.424264705882));
#160041=CARTESIAN_POINT('Ctrl Pts',(-17.9710104137728,-1.66525935159368,
-758.918382352941));
#160042=CARTESIAN_POINT('Ctrl Pts',(-18.1253194172301,-1.10985572039171E-15,
-760.4125));
#160043=CARTESIAN_POINT('Ctrl Pts',(-17.9710104137728,1.66525935159367,
-761.906617647059));
#160044=CARTESIAN_POINT('Ctrl Pts',(-17.8167014103155,3.33051870318735,
-763.400735294118));
#160045=CARTESIAN_POINT('Ctrl Pts',(-17.3590292079831,4.93906964482096,
-764.894852941176));
#160046=CARTESIAN_POINT('Ctrl Pts',(-16.9013570056506,6.54762058645456,
-766.388970588235));
#160047=CARTESIAN_POINT('Ctrl Pts',(-16.1559070823762,8.04468584505497,
-767.883088235294));
#160048=CARTESIAN_POINT('Ctrl Pts',(-15.4104571591017,9.54175110365538,
-769.377205882353));
#160049=CARTESIAN_POINT('Ctrl Pts',(-14.4026149179538,10.8763499173728,
-770.871323529412));
#160050=CARTESIAN_POINT('Ctrl Pts',(-13.3947726768058,12.2109487310903,
-772.365441176471));
#160051=CARTESIAN_POINT('Ctrl Pts',(-12.1588589765331,13.3376329379985,
-773.85955882353));
#160052=CARTESIAN_POINT('Ctrl Pts',(-10.9229452762603,14.4643171449067,
-775.353676470589));
#160053=CARTESIAN_POINT('Ctrl Pts',(-9.50104767561052,15.3447188656481,
-776.847794117647));
#160054=CARTESIAN_POINT('Ctrl Pts',(-8.07915007496071,16.2251205863895,
-778.341911764706));
#160055=CARTESIAN_POINT('Ctrl Pts',(-6.51968959134574,16.8292587962898,
-779.836029411765));
#160056=CARTESIAN_POINT('Ctrl Pts',(-4.96022910773078,17.4333970061901,
-781.330147058823));
#160057=CARTESIAN_POINT('Ctrl Pts',(-3.31631129755346,17.7406985030951,
-782.824264705882));
#160058=CARTESIAN_POINT('Ctrl Pts',(-1.67239348737615,18.048,-784.318382352941));
#160059=CARTESIAN_POINT('Ctrl Pts',(-2.21024254310115E-15,18.048,-785.8125));
#160060=CARTESIAN_POINT('Ctrl Pts',(1.67239348737616,18.048,-787.306617647059));
#160061=CARTESIAN_POINT('Ctrl Pts',(3.31631129755346,17.7406985030951,-788.800735294118));
#160062=CARTESIAN_POINT('Ctrl Pts',(4.96022910773077,17.4333970061901,-790.294852941177));
#160063=CARTESIAN_POINT('Ctrl Pts',(6.51968959134575,16.8292587962898,-791.788970588235));
#160064=CARTESIAN_POINT('Ctrl Pts',(8.07915007496071,16.2251205863895,-793.283088235294));
#160065=CARTESIAN_POINT('Ctrl Pts',(9.50104767561053,15.3447188656481,-794.777205882353));
#160066=CARTESIAN_POINT('Ctrl Pts',(10.9229452762603,14.4643171449067,-796.271323529412));
#160067=CARTESIAN_POINT('Ctrl Pts',(12.1588589765331,13.3376329379985,-797.765441176471));
#160068=CARTESIAN_POINT('Ctrl Pts',(13.3947726768058,12.2109487310903,-799.259558823529));
#160069=CARTESIAN_POINT('Ctrl Pts',(14.4026149179538,10.8763499173728,-800.753676470588));
#160070=CARTESIAN_POINT('Ctrl Pts',(15.4104571591017,9.54175110365538,-802.247794117647));
#160071=CARTESIAN_POINT('Ctrl Pts',(16.1559070823762,8.04468584505496,-803.741911764706));
#160072=CARTESIAN_POINT('Ctrl Pts',(16.9013570056506,6.54762058645456,-805.236029411765));
#160073=CARTESIAN_POINT('Ctrl Pts',(17.3590292079831,4.93906964482096,-806.730147058823));
#160074=CARTESIAN_POINT('Ctrl Pts',(17.8167014103155,3.33051870318735,-808.224264705882));
#160075=CARTESIAN_POINT('Ctrl Pts',(17.9710104137728,1.66525935159367,-809.718382352941));
#160076=CARTESIAN_POINT('Ctrl Pts',(18.1253194172301,3.32956716117513E-15,
-811.2125));
#160077=CARTESIAN_POINT('Ctrl Pts',(17.9710104137728,-1.66525935159367,
-812.706617647059));
#160078=CARTESIAN_POINT('Ctrl Pts',(17.8167014103155,-3.33051870318736,
-814.200735294118));
#160079=CARTESIAN_POINT('Ctrl Pts',(17.3590292079831,-4.93906964482095,
-815.694852941177));
#160080=CARTESIAN_POINT('Ctrl Pts',(16.9013570056506,-6.54762058645456,
-817.188970588235));
#160081=CARTESIAN_POINT('Ctrl Pts',(16.1559070823762,-8.04468584505497,
-818.683088235294));
#160082=CARTESIAN_POINT('Ctrl Pts',(15.4104571591017,-9.54175110365538,
-820.177205882353));
#160083=CARTESIAN_POINT('Ctrl Pts',(14.4026149179538,-10.8763499173728,
-821.671323529412));
#160084=CARTESIAN_POINT('Ctrl Pts',(13.3947726768058,-12.2109487310903,
-823.16544117647));
#160085=CARTESIAN_POINT('Ctrl Pts',(12.1588589765331,-13.3376329379985,
-824.659558823529));
#160086=CARTESIAN_POINT('Ctrl Pts',(10.9229452762603,-14.4643171449067,
-826.153676470588));
#160087=CARTESIAN_POINT('Ctrl Pts',(9.50104767561053,-15.3447188656481,
-827.647794117647));
#160088=CARTESIAN_POINT('Ctrl Pts',(8.07915007496071,-16.2251205863895,
-829.141911764706));
#160089=CARTESIAN_POINT('Ctrl Pts',(6.51968959134574,-16.8292587962898,
-830.636029411765));
#160090=CARTESIAN_POINT('Ctrl Pts',(4.96022910773078,-17.4333970061901,
-832.130147058824));
#160091=CARTESIAN_POINT('Ctrl Pts',(3.31631129755346,-17.7406985030951,
-833.624264705883));
#160092=CARTESIAN_POINT('Ctrl Pts',(1.67239348737615,-18.048,-835.118382352941));
#160093=CARTESIAN_POINT('Ctrl Pts',(0.,-18.048,-836.6125));
#160094=CARTESIAN_POINT('Ctrl Pts',(-1.67239348737615,-18.048,-838.106617647059));
#160095=CARTESIAN_POINT('Ctrl Pts',(-3.31631129755346,-17.7406985030951,
-839.600735294118));
#160096=CARTESIAN_POINT('Ctrl Pts',(-4.96022910773077,-17.4333970061901,
-841.094852941176));
#160097=CARTESIAN_POINT('Ctrl Pts',(-6.51968959134574,-16.8292587962898,
-842.588970588235));
#160098=CARTESIAN_POINT('Ctrl Pts',(-8.07915007496071,-16.2251205863895,
-844.083088235294));
#160099=CARTESIAN_POINT('Ctrl Pts',(-9.50104767561052,-15.3447188656481,
-845.577205882353));
#160100=CARTESIAN_POINT('Ctrl Pts',(-10.9229452762603,-14.4643171449067,
-847.071323529412));
#160101=CARTESIAN_POINT('Ctrl Pts',(-12.1588589765331,-13.3376329379985,
-848.565441176471));
#160102=CARTESIAN_POINT('Ctrl Pts',(-13.3947726768058,-12.2109487310903,
-850.05955882353));
#160103=CARTESIAN_POINT('Ctrl Pts',(-14.4026149179538,-10.8763499173728,
-851.553676470588));
#160104=CARTESIAN_POINT('Ctrl Pts',(-15.4104571591017,-9.54175110365538,
-853.047794117647));
#160105=CARTESIAN_POINT('Ctrl Pts',(-16.1559070823762,-8.04468584505497,
-854.541911764706));
#160106=CARTESIAN_POINT('Ctrl Pts',(-16.9013570056506,-6.54762058645456,
-856.036029411765));
#160107=CARTESIAN_POINT('Ctrl Pts',(-17.3590292079831,-4.93906964482095,
-857.530147058824));
#160108=CARTESIAN_POINT('Ctrl Pts',(-17.8167014103155,-3.33051870318735,
-859.024264705882));
#160109=CARTESIAN_POINT('Ctrl Pts',(-17.9710104137728,-1.66525935159368,
-860.518382352941));
#160110=CARTESIAN_POINT('Ctrl Pts',(-18.1253194172301,-1.10985572039171E-15,
-862.0125));
#160111=CARTESIAN_POINT('Ctrl Pts',(-17.9710104137728,1.66525935159367,
-863.506617647059));
#160112=CARTESIAN_POINT('Ctrl Pts',(-17.8167014103155,3.33051870318735,
-865.000735294118));
#160113=CARTESIAN_POINT('Ctrl Pts',(-17.3590292079831,4.93906964482096,
-866.494852941176));
#160114=CARTESIAN_POINT('Ctrl Pts',(-16.9013570056506,6.54762058645456,
-867.988970588235));
#160115=CARTESIAN_POINT('Ctrl Pts',(-16.1559070823762,8.04468584505497,
-869.483088235294));
#160116=CARTESIAN_POINT('Ctrl Pts',(-15.4104571591017,9.54175110365538,
-870.977205882353));
#160117=CARTESIAN_POINT('Ctrl Pts',(-14.4026149179538,10.8763499173728,
-872.471323529412));
#160118=CARTESIAN_POINT('Ctrl Pts',(-13.3947726768058,12.2109487310903,
-873.965441176471));
#160119=CARTESIAN_POINT('Ctrl Pts',(-12.1588589765331,13.3376329379985,
-875.459558823529));
#160120=CARTESIAN_POINT('Ctrl Pts',(-10.9229452762603,14.4643171449067,
-876.953676470588));
#160121=CARTESIAN_POINT('Ctrl Pts',(-9.50104767561052,15.3447188656481,
-878.447794117647));
#160122=CARTESIAN_POINT('Ctrl Pts',(-8.07915007496071,16.2251205863895,
-879.941911764706));
#160123=CARTESIAN_POINT('Ctrl Pts',(-6.51968959134574,16.8292587962898,
-881.436029411765));
#160124=CARTESIAN_POINT('Ctrl Pts',(-4.96022910773078,17.4333970061901,
-882.930147058823));
#160125=CARTESIAN_POINT('Ctrl Pts',(-3.31631129755346,17.7406985030951,
-884.424264705882));
#160126=CARTESIAN_POINT('Ctrl Pts',(-1.67239348737615,18.048,-885.918382352941));
#160127=CARTESIAN_POINT('Ctrl Pts',(-2.21024254310115E-15,18.048,-887.4125));
#160128=CARTESIAN_POINT('Ctrl Pts',(1.67239348737616,18.048,-888.906617647059));
#160129=CARTESIAN_POINT('Ctrl Pts',(3.31631129755346,17.7406985030951,-890.400735294118));
#160130=CARTESIAN_POINT('Ctrl Pts',(4.96022910773077,17.4333970061901,-891.894852941177));
#160131=CARTESIAN_POINT('Ctrl Pts',(6.51968959134575,16.8292587962898,-893.388970588235));
#160132=CARTESIAN_POINT('Ctrl Pts',(8.07915007496071,16.2251205863895,-894.883088235295));
#160133=CARTESIAN_POINT('Ctrl Pts',(9.50104767561053,15.3447188656481,-896.377205882353));
#160134=CARTESIAN_POINT('Ctrl Pts',(10.9229452762603,14.4643171449067,-897.871323529412));
#160135=CARTESIAN_POINT('Ctrl Pts',(12.1588589765331,13.3376329379985,-899.36544117647));
#160136=CARTESIAN_POINT('Ctrl Pts',(13.3947726768058,12.2109487310903,-900.859558823529));
#160137=CARTESIAN_POINT('Ctrl Pts',(14.4026149179538,10.8763499173728,-902.353676470588));
#160138=CARTESIAN_POINT('Ctrl Pts',(15.4104571591017,9.54175110365538,-903.847794117647));
#160139=CARTESIAN_POINT('Ctrl Pts',(16.1559070823762,8.04468584505496,-905.341911764706));
#160140=CARTESIAN_POINT('Ctrl Pts',(16.9013570056506,6.54762058645456,-906.836029411765));
#160141=CARTESIAN_POINT('Ctrl Pts',(17.3590292079831,4.93906964482096,-908.330147058824));
#160142=CARTESIAN_POINT('Ctrl Pts',(17.8167014103155,3.33051870318735,-909.824264705883));
#160143=CARTESIAN_POINT('Ctrl Pts',(17.9710104137728,1.66525935159367,-911.318382352941));
#160144=CARTESIAN_POINT('Ctrl Pts',(18.1253194172301,3.32956716117513E-15,
-912.8125));
#160145=CARTESIAN_POINT('Ctrl Pts',(17.9710104137728,-1.66525935159367,
-914.306617647059));
#160146=CARTESIAN_POINT('Ctrl Pts',(17.8167014103155,-3.33051870318736,
-915.800735294118));
#160147=CARTESIAN_POINT('Ctrl Pts',(17.3590292079831,-4.93906964482095,
-917.294852941176));
#160148=CARTESIAN_POINT('Ctrl Pts',(16.9013570056506,-6.54762058645456,
-918.788970588235));
#160149=CARTESIAN_POINT('Ctrl Pts',(16.1559070823762,-8.04468584505497,
-920.283088235294));
#160150=CARTESIAN_POINT('Ctrl Pts',(15.4104571591017,-9.54175110365538,
-921.777205882353));
#160151=CARTESIAN_POINT('Ctrl Pts',(14.4026149179538,-10.8763499173728,
-923.271323529412));
#160152=CARTESIAN_POINT('Ctrl Pts',(13.3947726768058,-12.2109487310903,
-924.765441176471));
#160153=CARTESIAN_POINT('Ctrl Pts',(12.1588589765331,-13.3376329379985,
-926.259558823529));
#160154=CARTESIAN_POINT('Ctrl Pts',(10.9229452762603,-14.4643171449067,
-927.753676470588));
#160155=CARTESIAN_POINT('Ctrl Pts',(9.50104767561053,-15.3447188656481,
-929.247794117647));
#160156=CARTESIAN_POINT('Ctrl Pts',(8.07915007496071,-16.2251205863895,
-930.741911764706));
#160157=CARTESIAN_POINT('Ctrl Pts',(6.51968959134574,-16.8292587962898,
-932.236029411765));
#160158=CARTESIAN_POINT('Ctrl Pts',(4.96022910773078,-17.4333970061901,
-933.730147058824));
#160159=CARTESIAN_POINT('Ctrl Pts',(3.31631129755346,-17.7406985030951,
-935.224264705882));
#160160=CARTESIAN_POINT('Ctrl Pts',(1.67239348737615,-18.048,-936.718382352941));
#160161=CARTESIAN_POINT('Ctrl Pts',(0.,-18.048,-938.2125));
#160162=CARTESIAN_POINT('Ctrl Pts',(-1.67239348737615,-18.048,-939.706617647059));
#160163=CARTESIAN_POINT('Ctrl Pts',(-3.31631129755346,-17.7406985030951,
-941.200735294117));
#160164=CARTESIAN_POINT('Ctrl Pts',(-4.96022910773077,-17.4333970061901,
-942.694852941176));
#160165=CARTESIAN_POINT('Ctrl Pts',(-6.51968959134574,-16.8292587962898,
-944.188970588235));
#160166=CARTESIAN_POINT('Ctrl Pts',(-8.07915007496071,-16.2251205863895,
-945.683088235294));
#160167=CARTESIAN_POINT('Ctrl Pts',(-9.50104767561052,-15.3447188656481,
-947.177205882353));
#160168=CARTESIAN_POINT('Ctrl Pts',(-10.9229452762603,-14.4643171449067,
-948.671323529412));
#160169=CARTESIAN_POINT('Ctrl Pts',(-12.1588589765331,-13.3376329379985,
-950.165441176471));
#160170=CARTESIAN_POINT('Ctrl Pts',(-13.3947726768058,-12.2109487310903,
-951.65955882353));
#160171=CARTESIAN_POINT('Ctrl Pts',(-14.4026149179538,-10.8763499173728,
-953.153676470588));
#160172=CARTESIAN_POINT('Ctrl Pts',(-15.4104571591017,-9.54175110365538,
-954.647794117647));
#160173=CARTESIAN_POINT('Ctrl Pts',(-16.1559070823762,-8.04468584505497,
-956.141911764706));
#160174=CARTESIAN_POINT('Ctrl Pts',(-16.9013570056506,-6.54762058645456,
-957.636029411764));
#160175=CARTESIAN_POINT('Ctrl Pts',(-17.3590292079831,-4.93906964482095,
-959.130147058823));
#160176=CARTESIAN_POINT('Ctrl Pts',(-17.8167014103155,-3.33051870318735,
-960.624264705882));
#160177=CARTESIAN_POINT('Ctrl Pts',(-17.9710104137728,-1.66525935159368,
-962.118382352941));
#160178=CARTESIAN_POINT('Ctrl Pts',(-18.1253194172301,-1.10985572039171E-15,
-963.6125));
#160179=CARTESIAN_POINT('Ctrl Pts',(-17.9710104137728,1.66525935159367,
-965.106617647059));
#160180=CARTESIAN_POINT('Ctrl Pts',(-17.8167014103155,3.33051870318735,
-966.600735294118));
#160181=CARTESIAN_POINT('Ctrl Pts',(-17.3590292079831,4.93906964482096,
-968.094852941177));
#160182=CARTESIAN_POINT('Ctrl Pts',(-16.9013570056506,6.54762058645456,
-969.588970588235));
#160183=CARTESIAN_POINT('Ctrl Pts',(-16.1559070823762,8.04468584505497,
-971.083088235294));
#160184=CARTESIAN_POINT('Ctrl Pts',(-15.4104571591017,9.54175110365538,
-972.577205882353));
#160185=CARTESIAN_POINT('Ctrl Pts',(-14.4026149179538,10.8763499173728,
-974.071323529412));
#160186=CARTESIAN_POINT('Ctrl Pts',(-13.3947726768058,12.2109487310903,
-975.565441176471));
#160187=CARTESIAN_POINT('Ctrl Pts',(-12.1588589765331,13.3376329379985,
-977.059558823529));
#160188=CARTESIAN_POINT('Ctrl Pts',(-10.9229452762603,14.4643171449067,
-978.553676470588));
#160189=CARTESIAN_POINT('Ctrl Pts',(-9.50104767561052,15.3447188656481,
-980.047794117647));
#160190=CARTESIAN_POINT('Ctrl Pts',(-8.07915007496071,16.2251205863895,
-981.541911764706));
#160191=CARTESIAN_POINT('Ctrl Pts',(-6.51968959134574,16.8292587962898,
-983.036029411765));
#160192=CARTESIAN_POINT('Ctrl Pts',(-4.96022910773078,17.4333970061901,
-984.530147058824));
#160193=CARTESIAN_POINT('Ctrl Pts',(-3.31631129755346,17.7406985030951,
-986.024264705882));
#160194=CARTESIAN_POINT('Ctrl Pts',(-1.67239348737615,18.048,-987.518382352941));
#160195=CARTESIAN_POINT('Ctrl Pts',(-2.21024254310115E-15,18.048,-989.0125));
#160196=CARTESIAN_POINT('Ctrl Pts',(1.67239348737616,18.048,-990.506617647059));
#160197=CARTESIAN_POINT('Ctrl Pts',(3.31631129755346,17.7406985030951,-992.000735294118));
#160198=CARTESIAN_POINT('Ctrl Pts',(4.96022910773077,17.4333970061901,-993.494852941176));
#160199=CARTESIAN_POINT('Ctrl Pts',(6.51968959134575,16.8292587962898,-994.988970588235));
#160200=CARTESIAN_POINT('Ctrl Pts',(8.07915007496071,16.2251205863895,-996.483088235294));
#160201=CARTESIAN_POINT('Ctrl Pts',(9.50104767561053,15.3447188656481,-997.977205882353));
#160202=CARTESIAN_POINT('Ctrl Pts',(10.9229452762603,14.4643171449067,-999.471323529412));
#160203=CARTESIAN_POINT('Ctrl Pts',(12.1588589765331,13.3376329379985,-1000.96544117647));
#160204=CARTESIAN_POINT('Ctrl Pts',(13.3947726768058,12.2109487310903,-1002.45955882353));
#160205=CARTESIAN_POINT('Ctrl Pts',(14.4026149179538,10.8763499173728,-1003.95367647059));
#160206=CARTESIAN_POINT('Ctrl Pts',(15.4104571591017,9.54175110365538,-1005.44779411765));
#160207=CARTESIAN_POINT('Ctrl Pts',(16.1559070823762,8.04468584505496,-1006.94191176471));
#160208=CARTESIAN_POINT('Ctrl Pts',(16.9013570056506,6.54762058645456,-1008.43602941176));
#160209=CARTESIAN_POINT('Ctrl Pts',(17.3590292079831,4.93906964482096,-1009.93014705882));
#160210=CARTESIAN_POINT('Ctrl Pts',(17.8167014103155,3.33051870318735,-1011.42426470588));
#160211=CARTESIAN_POINT('Ctrl Pts',(17.9710104137728,1.66525935159367,-1012.91838235294));
#160212=CARTESIAN_POINT('Ctrl Pts',(18.1253194172301,3.32956716117513E-15,
-1014.4125));
#160213=CARTESIAN_POINT('Ctrl Pts',(17.9710104137728,-1.66525935159367,
-1015.90661764706));
#160214=CARTESIAN_POINT('Ctrl Pts',(17.8167014103155,-3.33051870318736,
-1017.40073529412));
#160215=CARTESIAN_POINT('Ctrl Pts',(17.3590292079831,-4.93906964482095,
-1018.89485294118));
#160216=CARTESIAN_POINT('Ctrl Pts',(16.9013570056506,-6.54762058645456,
-1020.38897058824));
#160217=CARTESIAN_POINT('Ctrl Pts',(16.1559070823762,-8.04468584505497,
-1021.88308823529));
#160218=CARTESIAN_POINT('Ctrl Pts',(15.4104571591017,-9.54175110365538,
-1023.37720588235));
#160219=CARTESIAN_POINT('Ctrl Pts',(14.4026149179538,-10.8763499173728,
-1024.87132352941));
#160220=CARTESIAN_POINT('Ctrl Pts',(13.3947726768058,-12.2109487310903,
-1026.36544117647));
#160221=CARTESIAN_POINT('Ctrl Pts',(12.1588589765331,-13.3376329379985,
-1027.85955882353));
#160222=CARTESIAN_POINT('Ctrl Pts',(10.9229452762603,-14.4643171449067,
-1029.35367647059));
#160223=CARTESIAN_POINT('Ctrl Pts',(9.50104767561053,-15.3447188656481,
-1030.84779411765));
#160224=CARTESIAN_POINT('Ctrl Pts',(8.07915007496071,-16.2251205863895,
-1032.34191176471));
#160225=CARTESIAN_POINT('Ctrl Pts',(6.51968959134574,-16.8292587962898,
-1033.83602941176));
#160226=CARTESIAN_POINT('Ctrl Pts',(4.96022910773078,-17.4333970061901,
-1035.33014705882));
#160227=CARTESIAN_POINT('Ctrl Pts',(3.31631129755346,-17.7406985030951,
-1036.82426470588));
#160228=CARTESIAN_POINT('Ctrl Pts',(1.67239348737615,-18.048,-1038.31838235294));
#160229=CARTESIAN_POINT('Ctrl Pts',(0.,-18.048,-1039.8125));
#160230=CARTESIAN_POINT('Ctrl Pts',(-1.67239348737615,-18.048,-1041.30661764706));
#160231=CARTESIAN_POINT('Ctrl Pts',(-3.31631129755346,-17.7406985030951,
-1042.80073529412));
#160232=CARTESIAN_POINT('Ctrl Pts',(-4.96022910773077,-17.4333970061901,
-1044.29485294118));
#160233=CARTESIAN_POINT('Ctrl Pts',(-6.51968959134574,-16.8292587962898,
-1045.78897058824));
#160234=CARTESIAN_POINT('Ctrl Pts',(-8.07915007496071,-16.2251205863895,
-1047.28308823529));
#160235=CARTESIAN_POINT('Ctrl Pts',(-9.50104767561052,-15.3447188656481,
-1048.77720588235));
#160236=CARTESIAN_POINT('Ctrl Pts',(-10.9229452762603,-14.4643171449067,
-1050.27132352941));
#160237=CARTESIAN_POINT('Ctrl Pts',(-12.1588589765331,-13.3376329379985,
-1051.76544117647));
#160238=CARTESIAN_POINT('Ctrl Pts',(-13.3947726768058,-12.2109487310903,
-1053.25955882353));
#160239=CARTESIAN_POINT('Ctrl Pts',(-14.4026149179538,-10.8763499173728,
-1054.75367647059));
#160240=CARTESIAN_POINT('Ctrl Pts',(-15.4104571591017,-9.54175110365538,
-1056.24779411765));
#160241=CARTESIAN_POINT('Ctrl Pts',(-16.1559070823762,-8.04468584505497,
-1057.74191176471));
#160242=CARTESIAN_POINT('Ctrl Pts',(-16.9013570056506,-6.54762058645456,
-1059.23602941177));
#160243=CARTESIAN_POINT('Ctrl Pts',(-17.3590292079831,-4.93906964482095,
-1060.73014705882));
#160244=CARTESIAN_POINT('Ctrl Pts',(-17.8167014103155,-3.33051870318735,
-1062.22426470588));
#160245=CARTESIAN_POINT('Ctrl Pts',(-17.9710104137728,-1.66525935159368,
-1063.71838235294));
#160246=CARTESIAN_POINT('Ctrl Pts',(-18.1253194172301,-1.10985572039171E-15,
-1065.2125));
#160247=CARTESIAN_POINT('Ctrl Pts',(-17.9710104137728,1.66525935159367,
-1066.70661764706));
#160248=CARTESIAN_POINT('Ctrl Pts',(-17.8167014103155,3.33051870318735,
-1068.20073529412));
#160249=CARTESIAN_POINT('Ctrl Pts',(-17.3590292079831,4.93906964482096,
-1069.69485294118));
#160250=CARTESIAN_POINT('Ctrl Pts',(-16.9013570056506,6.54762058645456,
-1071.18897058824));
#160251=CARTESIAN_POINT('Ctrl Pts',(-16.1559070823762,8.04468584505497,
-1072.68308823529));
#160252=CARTESIAN_POINT('Ctrl Pts',(-15.4104571591017,9.54175110365538,
-1074.17720588235));
#160253=CARTESIAN_POINT('Ctrl Pts',(-14.4026149179538,10.8763499173728,
-1075.67132352941));
#160254=CARTESIAN_POINT('Ctrl Pts',(-13.3947726768058,12.2109487310903,
-1077.16544117647));
#160255=CARTESIAN_POINT('Ctrl Pts',(-12.1588589765331,13.3376329379985,
-1078.65955882353));
#160256=CARTESIAN_POINT('Ctrl Pts',(-10.9229452762603,14.4643171449067,
-1080.15367647059));
#160257=CARTESIAN_POINT('Ctrl Pts',(-9.50104767561052,15.3447188656481,
-1081.64779411765));
#160258=CARTESIAN_POINT('Ctrl Pts',(-8.07915007496071,16.2251205863895,
-1083.14191176471));
#160259=CARTESIAN_POINT('Ctrl Pts',(-6.51968959134574,16.8292587962898,
-1084.63602941176));
#160260=CARTESIAN_POINT('Ctrl Pts',(-4.96022910773078,17.4333970061901,
-1086.13014705882));
#160261=CARTESIAN_POINT('Ctrl Pts',(-3.31631129755346,17.7406985030951,
-1087.62426470588));
#160262=CARTESIAN_POINT('Ctrl Pts',(-1.67239348737615,18.048,-1089.11838235294));
#160263=CARTESIAN_POINT('Ctrl Pts',(-2.21024254310115E-15,18.048,-1090.6125));
#160264=CARTESIAN_POINT('Ctrl Pts',(1.67239348737616,18.048,-1092.10661764706));
#160265=CARTESIAN_POINT('Ctrl Pts',(3.31631129755346,17.7406985030951,-1093.60073529412));
#160266=CARTESIAN_POINT('Ctrl Pts',(4.96022910773077,17.4333970061901,-1095.09485294118));
#160267=CARTESIAN_POINT('Ctrl Pts',(6.51968959134575,16.8292587962898,-1096.58897058824));
#160268=CARTESIAN_POINT('Ctrl Pts',(8.07915007496071,16.2251205863895,-1098.08308823529));
#160269=CARTESIAN_POINT('Ctrl Pts',(9.50104767561053,15.3447188656481,-1099.57720588235));
#160270=CARTESIAN_POINT('Ctrl Pts',(10.9229452762603,14.4643171449067,-1101.07132352941));
#160271=CARTESIAN_POINT('Ctrl Pts',(12.1588589765331,13.3376329379985,-1102.56544117647));
#160272=CARTESIAN_POINT('Ctrl Pts',(13.3947726768058,12.2109487310903,-1104.05955882353));
#160273=CARTESIAN_POINT('Ctrl Pts',(14.4026149179538,10.8763499173728,-1105.55367647059));
#160274=CARTESIAN_POINT('Ctrl Pts',(15.4104571591017,9.54175110365538,-1107.04779411765));
#160275=CARTESIAN_POINT('Ctrl Pts',(16.1559070823762,8.04468584505496,-1108.54191176471));
#160276=CARTESIAN_POINT('Ctrl Pts',(16.9013570056506,6.54762058645456,-1110.03602941176));
#160277=CARTESIAN_POINT('Ctrl Pts',(17.3590292079831,4.93906964482096,-1111.53014705882));
#160278=CARTESIAN_POINT('Ctrl Pts',(17.8167014103155,3.33051870318735,-1113.02426470588));
#160279=CARTESIAN_POINT('Ctrl Pts',(17.9710104137728,1.66525935159367,-1114.51838235294));
#160280=CARTESIAN_POINT('Ctrl Pts',(18.1253194172301,3.32956716117513E-15,
-1116.0125));
#160281=CARTESIAN_POINT('Ctrl Pts',(17.9710104137728,-1.66525935159367,
-1117.50661764706));
#160282=CARTESIAN_POINT('Ctrl Pts',(17.8167014103155,-3.33051870318736,
-1119.00073529412));
#160283=CARTESIAN_POINT('Ctrl Pts',(17.3590292079831,-4.93906964482095,
-1120.49485294118));
#160284=CARTESIAN_POINT('Ctrl Pts',(16.9013570056506,-6.54762058645456,
-1121.98897058824));
#160285=CARTESIAN_POINT('Ctrl Pts',(16.1559070823762,-8.04468584505497,
-1123.48308823529));
#160286=CARTESIAN_POINT('Ctrl Pts',(15.4104571591017,-9.54175110365538,
-1124.97720588235));
#160287=CARTESIAN_POINT('Ctrl Pts',(14.4026149179538,-10.8763499173728,
-1126.47132352941));
#160288=CARTESIAN_POINT('Ctrl Pts',(13.3947726768058,-12.2109487310903,
-1127.96544117647));
#160289=CARTESIAN_POINT('Ctrl Pts',(12.1588589765331,-13.3376329379985,
-1129.45955882353));
#160290=CARTESIAN_POINT('Ctrl Pts',(10.9229452762603,-14.4643171449067,
-1130.95367647059));
#160291=CARTESIAN_POINT('Ctrl Pts',(9.50104767561053,-15.3447188656481,
-1132.44779411765));
#160292=CARTESIAN_POINT('Ctrl Pts',(8.07915007496071,-16.2251205863895,
-1133.94191176471));
#160293=CARTESIAN_POINT('Ctrl Pts',(6.51968959134574,-16.8292587962898,
-1135.43602941176));
#160294=CARTESIAN_POINT('Ctrl Pts',(4.96022910773078,-17.4333970061901,
-1136.93014705882));
#160295=CARTESIAN_POINT('Ctrl Pts',(3.31631129755346,-17.7406985030951,
-1138.42426470588));
#160296=CARTESIAN_POINT('Ctrl Pts',(1.67239348737615,-18.048,-1139.91838235294));
#160297=CARTESIAN_POINT('Ctrl Pts',(0.,-18.048,-1141.4125));
#160298=CARTESIAN_POINT('Ctrl Pts',(-1.67239348737615,-18.048,-1142.90661764706));
#160299=CARTESIAN_POINT('Ctrl Pts',(-3.31631129755346,-17.7406985030951,
-1144.40073529412));
#160300=CARTESIAN_POINT('Ctrl Pts',(-4.96022910773077,-17.4333970061901,
-1145.89485294118));
#160301=CARTESIAN_POINT('Ctrl Pts',(-6.51968959134574,-16.8292587962898,
-1147.38897058824));
#160302=CARTESIAN_POINT('Ctrl Pts',(-8.07915007496071,-16.2251205863895,
-1148.88308823529));
#160303=CARTESIAN_POINT('Ctrl Pts',(-9.50104767561052,-15.3447188656481,
-1150.37720588235));
#160304=CARTESIAN_POINT('Ctrl Pts',(-10.9229452762603,-14.4643171449067,
-1151.87132352941));
#160305=CARTESIAN_POINT('Ctrl Pts',(-12.1588589765331,-13.3376329379985,
-1153.36544117647));
#160306=CARTESIAN_POINT('Ctrl Pts',(-13.3947726768058,-12.2109487310903,
-1154.85955882353));
#160307=CARTESIAN_POINT('Ctrl Pts',(-14.4026149179538,-10.8763499173728,
-1156.35367647059));
#160308=CARTESIAN_POINT('Ctrl Pts',(-15.4104571591017,-9.54175110365538,
-1157.84779411765));
#160309=CARTESIAN_POINT('Ctrl Pts',(-16.1559070823762,-8.04468584505497,
-1159.34191176471));
#160310=CARTESIAN_POINT('Ctrl Pts',(-16.9013570056506,-6.54762058645456,
-1160.83602941176));
#160311=CARTESIAN_POINT('Ctrl Pts',(-17.3590292079831,-4.93906964482095,
-1162.33014705882));
#160312=CARTESIAN_POINT('Ctrl Pts',(-17.8167014103155,-3.33051870318735,
-1163.82426470588));
#160313=CARTESIAN_POINT('Ctrl Pts',(-17.9710104137728,-1.66525935159368,
-1165.31838235294));
#160314=CARTESIAN_POINT('Ctrl Pts',(-18.1253194172301,-1.10985572039171E-15,
-1166.8125));
#160315=CARTESIAN_POINT('Ctrl Pts',(-17.9710104137728,1.66525935159367,
-1168.30661764706));
#160316=CARTESIAN_POINT('Ctrl Pts',(-17.8167014103155,3.33051870318735,
-1169.80073529412));
#160317=CARTESIAN_POINT('Ctrl Pts',(-17.3590292079831,4.93906964482096,
-1171.29485294118));
#160318=CARTESIAN_POINT('Ctrl Pts',(-16.9013570056506,6.54762058645456,
-1172.78897058824));
#160319=CARTESIAN_POINT('Ctrl Pts',(-16.1559070823762,8.04468584505497,
-1174.28308823529));
#160320=CARTESIAN_POINT('Ctrl Pts',(-15.4104571591017,9.54175110365538,
-1175.77720588235));
#160321=CARTESIAN_POINT('Ctrl Pts',(-14.4026149179538,10.8763499173728,
-1177.27132352941));
#160322=CARTESIAN_POINT('Ctrl Pts',(-13.3947726768058,12.2109487310903,
-1178.76544117647));
#160323=CARTESIAN_POINT('Ctrl Pts',(-12.1588589765331,13.3376329379985,
-1180.25955882353));
#160324=CARTESIAN_POINT('Ctrl Pts',(-10.9229452762603,14.4643171449067,
-1181.75367647059));
#160325=CARTESIAN_POINT('Ctrl Pts',(-9.50104767561052,15.3447188656481,
-1183.24779411765));
#160326=CARTESIAN_POINT('Ctrl Pts',(-8.07915007496071,16.2251205863895,
-1184.74191176471));
#160327=CARTESIAN_POINT('Ctrl Pts',(-6.51968959134574,16.8292587962898,
-1186.23602941176));
#160328=CARTESIAN_POINT('Ctrl Pts',(-4.96022910773078,17.4333970061901,
-1187.73014705882));
#160329=CARTESIAN_POINT('Ctrl Pts',(-3.31631129755346,17.7406985030951,
-1189.22426470588));
#160330=CARTESIAN_POINT('Ctrl Pts',(-1.67239348737615,18.048,-1190.71838235294));
#160331=CARTESIAN_POINT('Ctrl Pts',(-2.21024254310115E-15,18.048,-1192.2125));
#160332=CARTESIAN_POINT('Ctrl Pts',(1.67239348737616,18.048,-1193.70661764706));
#160333=CARTESIAN_POINT('Ctrl Pts',(3.31631129755346,17.7406985030951,-1195.20073529412));
#160334=CARTESIAN_POINT('Ctrl Pts',(4.96022910773077,17.4333970061901,-1196.69485294118));
#160335=CARTESIAN_POINT('Ctrl Pts',(6.51968959134575,16.8292587962898,-1198.18897058824));
#160336=CARTESIAN_POINT('Ctrl Pts',(8.07915007496071,16.2251205863895,-1199.68308823529));
#160337=CARTESIAN_POINT('Ctrl Pts',(9.50104767561053,15.3447188656481,-1201.17720588235));
#160338=CARTESIAN_POINT('Ctrl Pts',(10.9229452762603,14.4643171449067,-1202.67132352941));
#160339=CARTESIAN_POINT('Ctrl Pts',(12.1588589765331,13.3376329379985,-1204.16544117647));
#160340=CARTESIAN_POINT('Ctrl Pts',(13.3947726768058,12.2109487310903,-1205.65955882353));
#160341=CARTESIAN_POINT('Ctrl Pts',(14.4026149179538,10.8763499173728,-1207.15367647059));
#160342=CARTESIAN_POINT('Ctrl Pts',(15.4104571591017,9.54175110365538,-1208.64779411765));
#160343=CARTESIAN_POINT('Ctrl Pts',(16.1559070823762,8.04468584505496,-1210.14191176471));
#160344=CARTESIAN_POINT('Ctrl Pts',(16.9013570056506,6.54762058645456,-1211.63602941176));
#160345=CARTESIAN_POINT('Ctrl Pts',(17.3590292079831,4.93906964482096,-1213.13014705882));
#160346=CARTESIAN_POINT('Ctrl Pts',(17.8167014103155,3.33051870318735,-1214.62426470588));
#160347=CARTESIAN_POINT('Ctrl Pts',(17.9710104137728,1.66525935159367,-1216.11838235294));
#160348=CARTESIAN_POINT('Ctrl Pts',(18.1253194172301,3.32956716117513E-15,
-1217.6125));
#160349=CARTESIAN_POINT('Ctrl Pts',(17.9710104137728,-1.66525935159367,
-1219.10661764706));
#160350=CARTESIAN_POINT('Ctrl Pts',(17.8167014103155,-3.33051870318736,
-1220.60073529412));
#160351=CARTESIAN_POINT('Ctrl Pts',(17.3590292079831,-4.93906964482095,
-1222.09485294118));
#160352=CARTESIAN_POINT('Ctrl Pts',(16.9013570056506,-6.54762058645456,
-1223.58897058824));
#160353=CARTESIAN_POINT('Ctrl Pts',(16.1559070823762,-8.04468584505497,
-1225.08308823529));
#160354=CARTESIAN_POINT('Ctrl Pts',(15.4104571591017,-9.54175110365538,
-1226.57720588235));
#160355=CARTESIAN_POINT('Ctrl Pts',(14.4026149179538,-10.8763499173728,
-1228.07132352941));
#160356=CARTESIAN_POINT('Ctrl Pts',(13.3947726768058,-12.2109487310903,
-1229.56544117647));
#160357=CARTESIAN_POINT('Ctrl Pts',(12.1588589765331,-13.3376329379985,
-1231.05955882353));
#160358=CARTESIAN_POINT('Ctrl Pts',(10.9229452762603,-14.4643171449067,
-1232.55367647059));
#160359=CARTESIAN_POINT('Ctrl Pts',(9.50104767561053,-15.3447188656481,
-1234.04779411765));
#160360=CARTESIAN_POINT('Ctrl Pts',(8.07915007496071,-16.2251205863895,
-1235.54191176471));
#160361=CARTESIAN_POINT('Ctrl Pts',(6.51968959134574,-16.8292587962898,
-1237.03602941176));
#160362=CARTESIAN_POINT('Ctrl Pts',(4.96022910773078,-17.4333970061901,
-1238.53014705882));
#160363=CARTESIAN_POINT('Ctrl Pts',(3.31631129755346,-17.7406985030951,
-1240.02426470588));
#160364=CARTESIAN_POINT('Ctrl Pts',(1.67239348737615,-18.048,-1241.51838235294));
#160365=CARTESIAN_POINT('Ctrl Pts',(0.,-18.048,-1243.0125));
#160366=CARTESIAN_POINT('Ctrl Pts',(-1.67239348737615,-18.048,-1244.50661764706));
#160367=CARTESIAN_POINT('Ctrl Pts',(-3.31631129755346,-17.7406985030951,
-1246.00073529412));
#160368=CARTESIAN_POINT('Ctrl Pts',(-4.96022910773077,-17.4333970061901,
-1247.49485294118));
#160369=CARTESIAN_POINT('Ctrl Pts',(-6.51968959134574,-16.8292587962898,
-1248.98897058824));
#160370=CARTESIAN_POINT('Ctrl Pts',(-8.07915007496071,-16.2251205863895,
-1250.48308823529));
#160371=CARTESIAN_POINT('Ctrl Pts',(-9.50104767561052,-15.3447188656481,
-1251.97720588235));
#160372=CARTESIAN_POINT('Ctrl Pts',(-10.9229452762603,-14.4643171449067,
-1253.47132352941));
#160373=CARTESIAN_POINT('Ctrl Pts',(-12.1588589765331,-13.3376329379985,
-1254.96544117647));
#160374=CARTESIAN_POINT('Ctrl Pts',(-13.3947726768058,-12.2109487310903,
-1256.45955882353));
#160375=CARTESIAN_POINT('Ctrl Pts',(-14.4026149179538,-10.8763499173728,
-1257.95367647059));
#160376=CARTESIAN_POINT('Ctrl Pts',(-15.4104571591017,-9.54175110365538,
-1259.44779411765));
#160377=CARTESIAN_POINT('Ctrl Pts',(-16.1559070823762,-8.04468584505497,
-1260.94191176471));
#160378=CARTESIAN_POINT('Ctrl Pts',(-16.9013570056506,-6.54762058645456,
-1262.43602941176));
#160379=CARTESIAN_POINT('Ctrl Pts',(-17.3590292079831,-4.93906964482095,
-1263.93014705882));
#160380=CARTESIAN_POINT('Ctrl Pts',(-17.8167014103155,-3.33051870318735,
-1265.42426470588));
#160381=CARTESIAN_POINT('Ctrl Pts',(-17.9710104137728,-1.66525935159368,
-1266.91838235294));
#160382=CARTESIAN_POINT('Ctrl Pts',(-18.1253194172301,-1.10985572039171E-15,
-1268.4125));
#160383=CARTESIAN_POINT('Ctrl Pts',(-17.9710104137728,1.66525935159367,
-1269.90661764706));
#160384=CARTESIAN_POINT('Ctrl Pts',(-17.8167014103155,3.33051870318735,
-1271.40073529412));
#160385=CARTESIAN_POINT('Ctrl Pts',(-17.3590292079831,4.93906964482096,
-1272.89485294118));
#160386=CARTESIAN_POINT('Ctrl Pts',(-16.9013570056506,6.54762058645456,
-1274.38897058824));
#160387=CARTESIAN_POINT('Ctrl Pts',(-16.1559070823762,8.04468584505497,
-1275.88308823529));
#160388=CARTESIAN_POINT('Ctrl Pts',(-15.4104571591017,9.54175110365538,
-1277.37720588235));
#160389=CARTESIAN_POINT('Ctrl Pts',(-14.4026149179538,10.8763499173728,
-1278.87132352941));
#160390=CARTESIAN_POINT('Ctrl Pts',(-13.3947726768058,12.2109487310903,
-1280.36544117647));
#160391=CARTESIAN_POINT('Ctrl Pts',(-12.1588589765331,13.3376329379985,
-1281.85955882353));
#160392=CARTESIAN_POINT('Ctrl Pts',(-10.9229452762603,14.4643171449067,
-1283.35367647059));
#160393=CARTESIAN_POINT('Ctrl Pts',(-9.50104767561052,15.3447188656481,
-1284.84779411765));
#160394=CARTESIAN_POINT('Ctrl Pts',(-8.07915007496071,16.2251205863895,
-1286.34191176471));
#160395=CARTESIAN_POINT('Ctrl Pts',(-6.51968959134574,16.8292587962898,
-1287.83602941176));
#160396=CARTESIAN_POINT('Ctrl Pts',(-4.96022910773078,17.4333970061901,
-1289.33014705882));
#160397=CARTESIAN_POINT('Ctrl Pts',(-3.31631129755346,17.7406985030951,
-1290.82426470588));
#160398=CARTESIAN_POINT('Ctrl Pts',(-1.67239348737615,18.048,-1292.31838235294));
#160399=CARTESIAN_POINT('Ctrl Pts',(-2.21024254310115E-15,18.048,-1293.8125));
#160400=CARTESIAN_POINT('Ctrl Pts',(1.67239348737616,18.048,-1295.30661764706));
#160401=CARTESIAN_POINT('Ctrl Pts',(3.31631129755346,17.7406985030951,-1296.80073529412));
#160402=CARTESIAN_POINT('Ctrl Pts',(4.96022910773077,17.4333970061901,-1298.29485294118));
#160403=CARTESIAN_POINT('Ctrl Pts',(6.51968959134575,16.8292587962898,-1299.78897058824));
#160404=CARTESIAN_POINT('Ctrl Pts',(8.07915007496071,16.2251205863895,-1301.28308823529));
#160405=CARTESIAN_POINT('Ctrl Pts',(9.50104767561053,15.3447188656481,-1302.77720588235));
#160406=CARTESIAN_POINT('Ctrl Pts',(10.9229452762603,14.4643171449067,-1304.27132352941));
#160407=CARTESIAN_POINT('Ctrl Pts',(12.1588589765331,13.3376329379985,-1305.76544117647));
#160408=CARTESIAN_POINT('Ctrl Pts',(13.3947726768058,12.2109487310903,-1307.25955882353));
#160409=CARTESIAN_POINT('Ctrl Pts',(14.4026149179538,10.8763499173728,-1308.75367647059));
#160410=CARTESIAN_POINT('Ctrl Pts',(15.4104571591017,9.54175110365538,-1310.24779411765));
#160411=CARTESIAN_POINT('Ctrl Pts',(16.1559070823762,8.04468584505496,-1311.74191176471));
#160412=CARTESIAN_POINT('Ctrl Pts',(16.9013570056506,6.54762058645456,-1313.23602941176));
#160413=CARTESIAN_POINT('Ctrl Pts',(17.3590292079831,4.93906964482096,-1314.73014705882));
#160414=CARTESIAN_POINT('Ctrl Pts',(17.8167014103155,3.33051870318735,-1316.22426470588));
#160415=CARTESIAN_POINT('Ctrl Pts',(17.9710104137728,1.66525935159367,-1317.71838235294));
#160416=CARTESIAN_POINT('Ctrl Pts',(18.1253194172301,3.32956716117513E-15,
-1319.2125));
#160417=CARTESIAN_POINT('Ctrl Pts',(17.9710104137728,-1.66525935159367,
-1320.70661764706));
#160418=CARTESIAN_POINT('Ctrl Pts',(17.8167014103155,-3.33051870318736,
-1322.20073529412));
#160419=CARTESIAN_POINT('Ctrl Pts',(17.3590292079831,-4.93906964482095,
-1323.69485294118));
#160420=CARTESIAN_POINT('Ctrl Pts',(16.9013570056506,-6.54762058645456,
-1325.18897058824));
#160421=CARTESIAN_POINT('Ctrl Pts',(16.1559070823762,-8.04468584505497,
-1326.68308823529));
#160422=CARTESIAN_POINT('Ctrl Pts',(15.4104571591017,-9.54175110365538,
-1328.17720588235));
#160423=CARTESIAN_POINT('Ctrl Pts',(14.4026149179538,-10.8763499173728,
-1329.67132352941));
#160424=CARTESIAN_POINT('Ctrl Pts',(13.3947726768058,-12.2109487310903,
-1331.16544117647));
#160425=CARTESIAN_POINT('Ctrl Pts',(12.1588589765331,-13.3376329379985,
-1332.65955882353));
#160426=CARTESIAN_POINT('Ctrl Pts',(10.9229452762603,-14.4643171449067,
-1334.15367647059));
#160427=CARTESIAN_POINT('Ctrl Pts',(9.50104767561053,-15.3447188656481,
-1335.64779411765));
#160428=CARTESIAN_POINT('Ctrl Pts',(8.07915007496071,-16.2251205863895,
-1337.14191176471));
#160429=CARTESIAN_POINT('Ctrl Pts',(6.51968959134574,-16.8292587962898,
-1338.63602941176));
#160430=CARTESIAN_POINT('Ctrl Pts',(4.96022910773078,-17.4333970061901,
-1340.13014705882));
#160431=CARTESIAN_POINT('Ctrl Pts',(3.31631129755346,-17.7406985030951,
-1341.62426470588));
#160432=CARTESIAN_POINT('Ctrl Pts',(1.67239348737615,-18.048,-1343.11838235294));
#160433=CARTESIAN_POINT('Ctrl Pts',(0.,-18.048,-1344.6125));
#160434=CARTESIAN_POINT('Ctrl Pts',(-1.67239348737615,-18.048,-1346.10661764706));
#160435=CARTESIAN_POINT('Ctrl Pts',(-3.31631129755346,-17.7406985030951,
-1347.60073529412));
#160436=CARTESIAN_POINT('Ctrl Pts',(-4.96022910773077,-17.4333970061901,
-1349.09485294118));
#160437=CARTESIAN_POINT('Ctrl Pts',(-6.51968959134574,-16.8292587962898,
-1350.58897058824));
#160438=CARTESIAN_POINT('Ctrl Pts',(-8.07915007496071,-16.2251205863895,
-1352.08308823529));
#160439=CARTESIAN_POINT('Ctrl Pts',(-9.50104767561052,-15.3447188656481,
-1353.57720588235));
#160440=CARTESIAN_POINT('Ctrl Pts',(-10.9229452762603,-14.4643171449067,
-1355.07132352941));
#160441=CARTESIAN_POINT('Ctrl Pts',(-12.1588589765331,-13.3376329379985,
-1356.56544117647));
#160442=CARTESIAN_POINT('Ctrl Pts',(-13.3947726768058,-12.2109487310903,
-1358.05955882353));
#160443=CARTESIAN_POINT('Ctrl Pts',(-14.4026149179538,-10.8763499173728,
-1359.55367647059));
#160444=CARTESIAN_POINT('Ctrl Pts',(-15.4104571591017,-9.54175110365538,
-1361.04779411765));
#160445=CARTESIAN_POINT('Ctrl Pts',(-16.1559070823762,-8.04468584505497,
-1362.54191176471));
#160446=CARTESIAN_POINT('Ctrl Pts',(-16.9013570056506,-6.54762058645456,
-1364.03602941176));
#160447=CARTESIAN_POINT('Ctrl Pts',(-17.3590292079831,-4.93906964482095,
-1365.53014705882));
#160448=CARTESIAN_POINT('Ctrl Pts',(-17.8167014103155,-3.33051870318735,
-1367.02426470588));
#160449=CARTESIAN_POINT('Ctrl Pts',(-17.9710104137728,-1.66525935159368,
-1368.51838235294));
#160450=CARTESIAN_POINT('Ctrl Pts',(-18.1253194172301,-1.10985572039171E-15,
-1370.0125));
#160451=CARTESIAN_POINT('Ctrl Pts',(-17.9710104137728,1.66525935159367,
-1371.50661764706));
#160452=CARTESIAN_POINT('Ctrl Pts',(-17.8167014103155,3.33051870318735,
-1373.00073529412));
#160453=CARTESIAN_POINT('Ctrl Pts',(-17.3590292079831,4.93906964482096,
-1374.49485294118));
#160454=CARTESIAN_POINT('Ctrl Pts',(-16.9013570056506,6.54762058645456,
-1375.98897058824));
#160455=CARTESIAN_POINT('Ctrl Pts',(-16.1559070823762,8.04468584505497,
-1377.48308823529));
#160456=CARTESIAN_POINT('Ctrl Pts',(-15.4104571591017,9.54175110365538,
-1378.97720588235));
#160457=CARTESIAN_POINT('Ctrl Pts',(-14.4026149179538,10.8763499173728,
-1380.47132352941));
#160458=CARTESIAN_POINT('Ctrl Pts',(-13.3947726768058,12.2109487310903,
-1381.96544117647));
#160459=CARTESIAN_POINT('Ctrl Pts',(-12.1588589765331,13.3376329379985,
-1383.45955882353));
#160460=CARTESIAN_POINT('Ctrl Pts',(-10.9229452762603,14.4643171449067,
-1384.95367647059));
#160461=CARTESIAN_POINT('Ctrl Pts',(-9.50104767561052,15.3447188656481,
-1386.44779411765));
#160462=CARTESIAN_POINT('Ctrl Pts',(-8.07915007496071,16.2251205863895,
-1387.94191176471));
#160463=CARTESIAN_POINT('Ctrl Pts',(-6.51968959134574,16.8292587962898,
-1389.43602941176));
#160464=CARTESIAN_POINT('Ctrl Pts',(-4.96022910773078,17.4333970061901,
-1390.93014705882));
#160465=CARTESIAN_POINT('Ctrl Pts',(-3.31631129755346,17.7406985030951,
-1392.42426470588));
#160466=CARTESIAN_POINT('Ctrl Pts',(-1.67239348737615,18.048,-1393.91838235294));
#160467=CARTESIAN_POINT('Ctrl Pts',(-2.21024254310115E-15,18.048,-1395.4125));
#160468=CARTESIAN_POINT('Ctrl Pts',(1.67239348737616,18.048,-1396.90661764706));
#160469=CARTESIAN_POINT('Ctrl Pts',(3.31631129755346,17.7406985030951,-1398.40073529412));
#160470=CARTESIAN_POINT('Ctrl Pts',(4.96022910773077,17.4333970061901,-1399.89485294118));
#160471=CARTESIAN_POINT('Ctrl Pts',(6.51968959134575,16.8292587962898,-1401.38897058824));
#160472=CARTESIAN_POINT('Ctrl Pts',(8.07915007496071,16.2251205863895,-1402.88308823529));
#160473=CARTESIAN_POINT('Ctrl Pts',(9.50104767561053,15.3447188656481,-1404.37720588235));
#160474=CARTESIAN_POINT('Ctrl Pts',(10.9229452762603,14.4643171449067,-1405.87132352941));
#160475=CARTESIAN_POINT('Ctrl Pts',(12.1588589765331,13.3376329379985,-1407.36544117647));
#160476=CARTESIAN_POINT('Ctrl Pts',(13.3947726768058,12.2109487310903,-1408.85955882353));
#160477=CARTESIAN_POINT('Ctrl Pts',(14.4026149179538,10.8763499173728,-1410.35367647059));
#160478=CARTESIAN_POINT('Ctrl Pts',(15.4104571591017,9.54175110365538,-1411.84779411765));
#160479=CARTESIAN_POINT('Ctrl Pts',(16.1559070823762,8.04468584505496,-1413.34191176471));
#160480=CARTESIAN_POINT('Ctrl Pts',(16.9013570056506,6.54762058645456,-1414.83602941176));
#160481=CARTESIAN_POINT('Ctrl Pts',(17.3590292079831,4.93906964482096,-1416.33014705882));
#160482=CARTESIAN_POINT('Ctrl Pts',(17.8167014103155,3.33051870318735,-1417.82426470588));
#160483=CARTESIAN_POINT('Ctrl Pts',(17.9710104137728,1.66525935159367,-1419.31838235294));
#160484=CARTESIAN_POINT('Ctrl Pts',(18.1253194172301,3.32956716117513E-15,
-1420.8125));
#160485=CARTESIAN_POINT('Ctrl Pts',(17.9710104137728,-1.66525935159367,
-1422.30661764706));
#160486=CARTESIAN_POINT('Ctrl Pts',(17.8167014103155,-3.33051870318736,
-1423.80073529412));
#160487=CARTESIAN_POINT('Ctrl Pts',(17.3590292079831,-4.93906964482095,
-1425.29485294118));
#160488=CARTESIAN_POINT('Ctrl Pts',(16.9013570056506,-6.54762058645456,
-1426.78897058824));
#160489=CARTESIAN_POINT('Ctrl Pts',(16.1559070823762,-8.04468584505497,
-1428.28308823529));
#160490=CARTESIAN_POINT('Ctrl Pts',(15.4104571591017,-9.54175110365538,
-1429.77720588235));
#160491=CARTESIAN_POINT('Ctrl Pts',(14.4026149179538,-10.8763499173728,
-1431.27132352941));
#160492=CARTESIAN_POINT('Ctrl Pts',(13.3947726768058,-12.2109487310903,
-1432.76544117647));
#160493=CARTESIAN_POINT('Ctrl Pts',(12.1588589765331,-13.3376329379985,
-1434.25955882353));
#160494=CARTESIAN_POINT('Ctrl Pts',(10.9229452762603,-14.4643171449067,
-1435.75367647059));
#160495=CARTESIAN_POINT('Ctrl Pts',(9.50104767561053,-15.3447188656481,
-1437.24779411765));
#160496=CARTESIAN_POINT('Ctrl Pts',(8.07915007496071,-16.2251205863895,
-1438.74191176471));
#160497=CARTESIAN_POINT('Ctrl Pts',(6.51968959134574,-16.8292587962898,
-1440.23602941176));
#160498=CARTESIAN_POINT('Ctrl Pts',(4.96022910773078,-17.4333970061901,
-1441.73014705882));
#160499=CARTESIAN_POINT('Ctrl Pts',(3.31631129755346,-17.7406985030951,
-1443.22426470588));
#160500=CARTESIAN_POINT('Ctrl Pts',(1.67239348737615,-18.048,-1444.71838235294));
#160501=CARTESIAN_POINT('Ctrl Pts',(0.,-18.048,-1446.2125));
#160502=CARTESIAN_POINT('Ctrl Pts',(-1.67239348737615,-18.048,-1447.70661764706));
#160503=CARTESIAN_POINT('Ctrl Pts',(-3.31631129755346,-17.7406985030951,
-1449.20073529412));
#160504=CARTESIAN_POINT('Ctrl Pts',(-4.96022910773077,-17.4333970061901,
-1450.69485294118));
#160505=CARTESIAN_POINT('Ctrl Pts',(-6.51968959134574,-16.8292587962898,
-1452.18897058824));
#160506=CARTESIAN_POINT('Ctrl Pts',(-8.07915007496071,-16.2251205863895,
-1453.68308823529));
#160507=CARTESIAN_POINT('Ctrl Pts',(-9.50104767561052,-15.3447188656481,
-1455.17720588235));
#160508=CARTESIAN_POINT('Ctrl Pts',(-10.9229452762603,-14.4643171449067,
-1456.67132352941));
#160509=CARTESIAN_POINT('Ctrl Pts',(-12.1588589765331,-13.3376329379985,
-1458.16544117647));
#160510=CARTESIAN_POINT('Ctrl Pts',(-13.3947726768058,-12.2109487310903,
-1459.65955882353));
#160511=CARTESIAN_POINT('Ctrl Pts',(-14.4026149179538,-10.8763499173728,
-1461.15367647059));
#160512=CARTESIAN_POINT('Ctrl Pts',(-15.4104571591017,-9.54175110365538,
-1462.64779411765));
#160513=CARTESIAN_POINT('Ctrl Pts',(-16.1559070823762,-8.04468584505497,
-1464.14191176471));
#160514=CARTESIAN_POINT('Ctrl Pts',(-16.9013570056506,-6.54762058645456,
-1465.63602941176));
#160515=CARTESIAN_POINT('Ctrl Pts',(-17.3590292079831,-4.93906964482095,
-1467.13014705882));
#160516=CARTESIAN_POINT('Ctrl Pts',(-17.8167014103155,-3.33051870318735,
-1468.62426470588));
#160517=CARTESIAN_POINT('Ctrl Pts',(-17.9710104137728,-1.66525935159368,
-1470.11838235294));
#160518=CARTESIAN_POINT('Ctrl Pts',(-18.1253194172301,-1.10985572039171E-15,
-1471.6125));
#160519=CARTESIAN_POINT('Ctrl Pts',(-17.9710104137728,1.66525935159367,
-1473.10661764706));
#160520=CARTESIAN_POINT('Ctrl Pts',(-17.8167014103155,3.33051870318735,
-1474.60073529412));
#160521=CARTESIAN_POINT('Ctrl Pts',(-17.3590292079831,4.93906964482096,
-1476.09485294118));
#160522=CARTESIAN_POINT('Ctrl Pts',(-16.9013570056506,6.54762058645456,
-1477.58897058824));
#160523=CARTESIAN_POINT('Ctrl Pts',(-16.1559070823762,8.04468584505497,
-1479.08308823529));
#160524=CARTESIAN_POINT('Ctrl Pts',(-15.4104571591017,9.54175110365538,
-1480.57720588235));
#160525=CARTESIAN_POINT('Ctrl Pts',(-14.4026149179538,10.8763499173728,
-1482.07132352941));
#160526=CARTESIAN_POINT('Ctrl Pts',(-13.3947726768058,12.2109487310903,
-1483.56544117647));
#160527=CARTESIAN_POINT('Ctrl Pts',(-12.1588589765331,13.3376329379985,
-1485.05955882353));
#160528=CARTESIAN_POINT('Ctrl Pts',(-10.9229452762603,14.4643171449067,
-1486.55367647059));
#160529=CARTESIAN_POINT('Ctrl Pts',(-9.50104767561052,15.3447188656481,
-1488.04779411765));
#160530=CARTESIAN_POINT('Ctrl Pts',(-8.07915007496071,16.2251205863895,
-1489.54191176471));
#160531=CARTESIAN_POINT('Ctrl Pts',(-6.51968959134574,16.8292587962898,
-1491.03602941176));
#160532=CARTESIAN_POINT('Ctrl Pts',(-4.96022910773078,17.4333970061901,
-1492.53014705882));
#160533=CARTESIAN_POINT('Ctrl Pts',(-3.31631129755346,17.7406985030951,
-1494.02426470588));
#160534=CARTESIAN_POINT('Ctrl Pts',(-1.67239348737615,18.048,-1495.51838235294));
#160535=CARTESIAN_POINT('Ctrl Pts',(-2.21024254310115E-15,18.048,-1497.0125));
#160536=CARTESIAN_POINT('Ctrl Pts',(1.67239348737616,18.048,-1498.50661764706));
#160537=CARTESIAN_POINT('Ctrl Pts',(3.31631129755346,17.7406985030951,-1500.00073529412));
#160538=CARTESIAN_POINT('Ctrl Pts',(4.96022910773077,17.4333970061901,-1501.49485294118));
#160539=CARTESIAN_POINT('Ctrl Pts',(6.51968959134575,16.8292587962898,-1502.98897058824));
#160540=CARTESIAN_POINT('Ctrl Pts',(7.54128438222262,16.4334908658495,-1503.96775961254));
#160541=CARTESIAN_POINT('Ctrl Pts',(8.50750525179181,15.917055581694,-1504.9503325767));
#160542=CARTESIAN_POINT('Ctrl Pts',(0.,-15.,1500.1875));
#160543=CARTESIAN_POINT('Ctrl Pts',(-1.38995469363045,-15.,1498.69338235294));
#160544=CARTESIAN_POINT('Ctrl Pts',(-2.75624276724856,-14.7445964952585,
1497.19926470588));
#160545=CARTESIAN_POINT('Ctrl Pts',(-4.12253084086666,-14.4891929905171,
1495.70514705882));
#160546=CARTESIAN_POINT('Ctrl Pts',(-5.41862499280729,-13.9870834410653,
1494.21102941176));
#160547=CARTESIAN_POINT('Ctrl Pts',(-6.71471914474793,-13.4849738916136,
1492.71691176471));
#160548=CARTESIAN_POINT('Ctrl Pts',(-7.89648244316034,-12.7532570359442,
1491.22279411765));
#160549=CARTESIAN_POINT('Ctrl Pts',(-9.07824574157275,-12.0215401802748,
1489.72867647059));
#160550=CARTESIAN_POINT('Ctrl Pts',(-10.1054346546984,-11.0851337583099,
1488.23455882353));
#160551=CARTESIAN_POINT('Ctrl Pts',(-11.132623567824,-10.148727336345,1486.74044117647));
#160552=CARTESIAN_POINT('Ctrl Pts',(-11.9702584092036,-9.03951954568885,
1485.24632352941));
#160553=CARTESIAN_POINT('Ctrl Pts',(-12.8078932505832,-7.93031175503273,
1483.75220588235));
#160554=CARTESIAN_POINT('Ctrl Pts',(-13.4274493703259,-6.68607533664808,
1482.25808823529));
#160555=CARTESIAN_POINT('Ctrl Pts',(-14.0470054900687,-5.44183891826343,
1480.76397058824));
#160556=CARTESIAN_POINT('Ctrl Pts',(-14.4273846475923,-4.10494485108124,
1479.26985294118));
#160557=CARTESIAN_POINT('Ctrl Pts',(-14.8077638051159,-2.76805078389906,
1477.77573529412));
#160558=CARTESIAN_POINT('Ctrl Pts',(-14.9360126444255,-1.38402539194953,
1476.28161764706));
#160559=CARTESIAN_POINT('Ctrl Pts',(-15.0642614837351,-9.22419980378748E-16,
1474.7875));
#160560=CARTESIAN_POINT('Ctrl Pts',(-14.9360126444255,1.38402539194953,
1473.29338235294));
#160561=CARTESIAN_POINT('Ctrl Pts',(-14.8077638051159,2.76805078389906,
1471.79926470588));
#160562=CARTESIAN_POINT('Ctrl Pts',(-14.4273846475923,4.10494485108124,
1470.30514705882));
#160563=CARTESIAN_POINT('Ctrl Pts',(-14.0470054900687,5.44183891826343,
1468.81102941177));
#160564=CARTESIAN_POINT('Ctrl Pts',(-13.4274493703259,6.68607533664807,
1467.31691176471));
#160565=CARTESIAN_POINT('Ctrl Pts',(-12.8078932505832,7.93031175503273,
1465.82279411765));
#160566=CARTESIAN_POINT('Ctrl Pts',(-11.9702584092036,9.03951954568884,
1464.32867647059));
#160567=CARTESIAN_POINT('Ctrl Pts',(-11.132623567824,10.148727336345,1462.83455882353));
#160568=CARTESIAN_POINT('Ctrl Pts',(-10.1054346546984,11.0851337583099,
1461.34044117647));
#160569=CARTESIAN_POINT('Ctrl Pts',(-9.07824574157275,12.0215401802748,
1459.84632352941));
#160570=CARTESIAN_POINT('Ctrl Pts',(-7.89648244316034,12.7532570359442,
1458.35220588235));
#160571=CARTESIAN_POINT('Ctrl Pts',(-6.71471914474793,13.4849738916136,
1456.85808823529));
#160572=CARTESIAN_POINT('Ctrl Pts',(-5.41862499280729,13.9870834410653,
1455.36397058824));
#160573=CARTESIAN_POINT('Ctrl Pts',(-4.12253084086667,14.4891929905171,
1453.86985294118));
#160574=CARTESIAN_POINT('Ctrl Pts',(-2.75624276724856,14.7445964952585,
1452.37573529412));
#160575=CARTESIAN_POINT('Ctrl Pts',(-1.38995469363044,15.,1450.88161764706));
#160576=CARTESIAN_POINT('Ctrl Pts',(-1.83697019872103E-15,15.,1449.3875));
#160577=CARTESIAN_POINT('Ctrl Pts',(1.38995469363045,15.,1447.89338235294));
#160578=CARTESIAN_POINT('Ctrl Pts',(2.75624276724855,14.7445964952585,1446.39926470588));
#160579=CARTESIAN_POINT('Ctrl Pts',(4.12253084086666,14.4891929905171,1444.90514705882));
#160580=CARTESIAN_POINT('Ctrl Pts',(5.4186249928073,13.9870834410653,1443.41102941176));
#160581=CARTESIAN_POINT('Ctrl Pts',(6.71471914474792,13.4849738916136,1441.91691176471));
#160582=CARTESIAN_POINT('Ctrl Pts',(7.89648244316034,12.7532570359442,1440.42279411765));
#160583=CARTESIAN_POINT('Ctrl Pts',(9.07824574157275,12.0215401802748,1438.92867647059));
#160584=CARTESIAN_POINT('Ctrl Pts',(10.1054346546984,11.0851337583099,1437.43455882353));
#160585=CARTESIAN_POINT('Ctrl Pts',(11.132623567824,10.148727336345,1435.94044117647));
#160586=CARTESIAN_POINT('Ctrl Pts',(11.9702584092036,9.03951954568885,1434.44632352941));
#160587=CARTESIAN_POINT('Ctrl Pts',(12.8078932505832,7.93031175503273,1432.95220588235));
#160588=CARTESIAN_POINT('Ctrl Pts',(13.4274493703259,6.68607533664807,1431.45808823529));
#160589=CARTESIAN_POINT('Ctrl Pts',(14.0470054900687,5.44183891826343,1429.96397058824));
#160590=CARTESIAN_POINT('Ctrl Pts',(14.4273846475923,4.10494485108125,1428.46985294118));
#160591=CARTESIAN_POINT('Ctrl Pts',(14.8077638051159,2.76805078389905,1426.97573529412));
#160592=CARTESIAN_POINT('Ctrl Pts',(14.9360126444255,1.38402539194953,1425.48161764706));
#160593=CARTESIAN_POINT('Ctrl Pts',(15.0642614837351,2.76725994113625E-15,
1423.9875));
#160594=CARTESIAN_POINT('Ctrl Pts',(14.9360126444255,-1.38402539194952,
1422.49338235294));
#160595=CARTESIAN_POINT('Ctrl Pts',(14.8077638051159,-2.76805078389906,
1420.99926470588));
#160596=CARTESIAN_POINT('Ctrl Pts',(14.4273846475923,-4.10494485108124,
1419.50514705882));
#160597=CARTESIAN_POINT('Ctrl Pts',(14.0470054900687,-5.44183891826342,
1418.01102941176));
#160598=CARTESIAN_POINT('Ctrl Pts',(13.4274493703259,-6.68607533664808,
1416.51691176471));
#160599=CARTESIAN_POINT('Ctrl Pts',(12.8078932505832,-7.93031175503273,
1415.02279411765));
#160600=CARTESIAN_POINT('Ctrl Pts',(11.9702584092036,-9.03951954568884,
1413.52867647059));
#160601=CARTESIAN_POINT('Ctrl Pts',(11.132623567824,-10.148727336345,1412.03455882353));
#160602=CARTESIAN_POINT('Ctrl Pts',(10.1054346546984,-11.0851337583099,
1410.54044117647));
#160603=CARTESIAN_POINT('Ctrl Pts',(9.07824574157275,-12.0215401802748,
1409.04632352941));
#160604=CARTESIAN_POINT('Ctrl Pts',(7.89648244316034,-12.7532570359442,
1407.55220588235));
#160605=CARTESIAN_POINT('Ctrl Pts',(6.71471914474792,-13.4849738916136,
1406.05808823529));
#160606=CARTESIAN_POINT('Ctrl Pts',(5.4186249928073,-13.9870834410653,1404.56397058824));
#160607=CARTESIAN_POINT('Ctrl Pts',(4.12253084086667,-14.4891929905171,
1403.06985294118));
#160608=CARTESIAN_POINT('Ctrl Pts',(2.75624276724855,-14.7445964952585,
1401.57573529412));
#160609=CARTESIAN_POINT('Ctrl Pts',(1.38995469363045,-15.,1400.08161764706));
#160610=CARTESIAN_POINT('Ctrl Pts',(0.,-15.,1398.5875));
#160611=CARTESIAN_POINT('Ctrl Pts',(-1.38995469363045,-15.,1397.09338235294));
#160612=CARTESIAN_POINT('Ctrl Pts',(-2.75624276724856,-14.7445964952585,
1395.59926470588));
#160613=CARTESIAN_POINT('Ctrl Pts',(-4.12253084086666,-14.4891929905171,
1394.10514705882));
#160614=CARTESIAN_POINT('Ctrl Pts',(-5.41862499280729,-13.9870834410653,
1392.61102941176));
#160615=CARTESIAN_POINT('Ctrl Pts',(-6.71471914474793,-13.4849738916136,
1391.11691176471));
#160616=CARTESIAN_POINT('Ctrl Pts',(-7.89648244316034,-12.7532570359442,
1389.62279411765));
#160617=CARTESIAN_POINT('Ctrl Pts',(-9.07824574157275,-12.0215401802748,
1388.12867647059));
#160618=CARTESIAN_POINT('Ctrl Pts',(-10.1054346546984,-11.0851337583099,
1386.63455882353));
#160619=CARTESIAN_POINT('Ctrl Pts',(-11.132623567824,-10.148727336345,1385.14044117647));
#160620=CARTESIAN_POINT('Ctrl Pts',(-11.9702584092036,-9.03951954568885,
1383.64632352941));
#160621=CARTESIAN_POINT('Ctrl Pts',(-12.8078932505832,-7.93031175503273,
1382.15220588235));
#160622=CARTESIAN_POINT('Ctrl Pts',(-13.4274493703259,-6.68607533664808,
1380.65808823529));
#160623=CARTESIAN_POINT('Ctrl Pts',(-14.0470054900687,-5.44183891826343,
1379.16397058824));
#160624=CARTESIAN_POINT('Ctrl Pts',(-14.4273846475923,-4.10494485108124,
1377.66985294118));
#160625=CARTESIAN_POINT('Ctrl Pts',(-14.8077638051159,-2.76805078389906,
1376.17573529412));
#160626=CARTESIAN_POINT('Ctrl Pts',(-14.9360126444255,-1.38402539194953,
1374.68161764706));
#160627=CARTESIAN_POINT('Ctrl Pts',(-15.0642614837351,-9.22419980378748E-16,
1373.1875));
#160628=CARTESIAN_POINT('Ctrl Pts',(-14.9360126444255,1.38402539194953,
1371.69338235294));
#160629=CARTESIAN_POINT('Ctrl Pts',(-14.8077638051159,2.76805078389906,
1370.19926470588));
#160630=CARTESIAN_POINT('Ctrl Pts',(-14.4273846475923,4.10494485108124,
1368.70514705882));
#160631=CARTESIAN_POINT('Ctrl Pts',(-14.0470054900687,5.44183891826343,
1367.21102941176));
#160632=CARTESIAN_POINT('Ctrl Pts',(-13.4274493703259,6.68607533664807,
1365.71691176471));
#160633=CARTESIAN_POINT('Ctrl Pts',(-12.8078932505832,7.93031175503273,
1364.22279411765));
#160634=CARTESIAN_POINT('Ctrl Pts',(-11.9702584092036,9.03951954568884,
1362.72867647059));
#160635=CARTESIAN_POINT('Ctrl Pts',(-11.132623567824,10.148727336345,1361.23455882353));
#160636=CARTESIAN_POINT('Ctrl Pts',(-10.1054346546984,11.0851337583099,
1359.74044117647));
#160637=CARTESIAN_POINT('Ctrl Pts',(-9.07824574157275,12.0215401802748,
1358.24632352941));
#160638=CARTESIAN_POINT('Ctrl Pts',(-7.89648244316034,12.7532570359442,
1356.75220588235));
#160639=CARTESIAN_POINT('Ctrl Pts',(-6.71471914474793,13.4849738916136,
1355.25808823529));
#160640=CARTESIAN_POINT('Ctrl Pts',(-5.41862499280729,13.9870834410653,
1353.76397058824));
#160641=CARTESIAN_POINT('Ctrl Pts',(-4.12253084086667,14.4891929905171,
1352.26985294118));
#160642=CARTESIAN_POINT('Ctrl Pts',(-2.75624276724856,14.7445964952585,
1350.77573529412));
#160643=CARTESIAN_POINT('Ctrl Pts',(-1.38995469363044,15.,1349.28161764706));
#160644=CARTESIAN_POINT('Ctrl Pts',(-1.83697019872103E-15,15.,1347.7875));
#160645=CARTESIAN_POINT('Ctrl Pts',(1.38995469363045,15.,1346.29338235294));
#160646=CARTESIAN_POINT('Ctrl Pts',(2.75624276724855,14.7445964952585,1344.79926470588));
#160647=CARTESIAN_POINT('Ctrl Pts',(4.12253084086666,14.4891929905171,1343.30514705882));
#160648=CARTESIAN_POINT('Ctrl Pts',(5.4186249928073,13.9870834410653,1341.81102941176));
#160649=CARTESIAN_POINT('Ctrl Pts',(6.71471914474792,13.4849738916136,1340.31691176471));
#160650=CARTESIAN_POINT('Ctrl Pts',(7.89648244316034,12.7532570359442,1338.82279411765));
#160651=CARTESIAN_POINT('Ctrl Pts',(9.07824574157275,12.0215401802748,1337.32867647059));
#160652=CARTESIAN_POINT('Ctrl Pts',(10.1054346546984,11.0851337583099,1335.83455882353));
#160653=CARTESIAN_POINT('Ctrl Pts',(11.132623567824,10.148727336345,1334.34044117647));
#160654=CARTESIAN_POINT('Ctrl Pts',(11.9702584092036,9.03951954568885,1332.84632352941));
#160655=CARTESIAN_POINT('Ctrl Pts',(12.8078932505832,7.93031175503273,1331.35220588235));
#160656=CARTESIAN_POINT('Ctrl Pts',(13.4274493703259,6.68607533664807,1329.85808823529));
#160657=CARTESIAN_POINT('Ctrl Pts',(14.0470054900687,5.44183891826343,1328.36397058824));
#160658=CARTESIAN_POINT('Ctrl Pts',(14.4273846475923,4.10494485108125,1326.86985294118));
#160659=CARTESIAN_POINT('Ctrl Pts',(14.8077638051159,2.76805078389905,1325.37573529412));
#160660=CARTESIAN_POINT('Ctrl Pts',(14.9360126444255,1.38402539194953,1323.88161764706));
#160661=CARTESIAN_POINT('Ctrl Pts',(15.0642614837351,2.76725994113625E-15,
1322.3875));
#160662=CARTESIAN_POINT('Ctrl Pts',(14.9360126444255,-1.38402539194952,
1320.89338235294));
#160663=CARTESIAN_POINT('Ctrl Pts',(14.8077638051159,-2.76805078389906,
1319.39926470588));
#160664=CARTESIAN_POINT('Ctrl Pts',(14.4273846475923,-4.10494485108124,
1317.90514705882));
#160665=CARTESIAN_POINT('Ctrl Pts',(14.0470054900687,-5.44183891826342,
1316.41102941176));
#160666=CARTESIAN_POINT('Ctrl Pts',(13.4274493703259,-6.68607533664808,
1314.91691176471));
#160667=CARTESIAN_POINT('Ctrl Pts',(12.8078932505832,-7.93031175503273,
1313.42279411765));
#160668=CARTESIAN_POINT('Ctrl Pts',(11.9702584092036,-9.03951954568884,
1311.92867647059));
#160669=CARTESIAN_POINT('Ctrl Pts',(11.132623567824,-10.148727336345,1310.43455882353));
#160670=CARTESIAN_POINT('Ctrl Pts',(10.1054346546984,-11.0851337583099,
1308.94044117647));
#160671=CARTESIAN_POINT('Ctrl Pts',(9.07824574157275,-12.0215401802748,
1307.44632352941));
#160672=CARTESIAN_POINT('Ctrl Pts',(7.89648244316034,-12.7532570359442,
1305.95220588235));
#160673=CARTESIAN_POINT('Ctrl Pts',(6.71471914474792,-13.4849738916136,
1304.45808823529));
#160674=CARTESIAN_POINT('Ctrl Pts',(5.4186249928073,-13.9870834410653,1302.96397058824));
#160675=CARTESIAN_POINT('Ctrl Pts',(4.12253084086667,-14.4891929905171,
1301.46985294118));
#160676=CARTESIAN_POINT('Ctrl Pts',(2.75624276724855,-14.7445964952585,
1299.97573529412));
#160677=CARTESIAN_POINT('Ctrl Pts',(1.38995469363045,-15.,1298.48161764706));
#160678=CARTESIAN_POINT('Ctrl Pts',(0.,-15.,1296.9875));
#160679=CARTESIAN_POINT('Ctrl Pts',(-1.38995469363045,-15.,1295.49338235294));
#160680=CARTESIAN_POINT('Ctrl Pts',(-2.75624276724856,-14.7445964952585,
1293.99926470588));
#160681=CARTESIAN_POINT('Ctrl Pts',(-4.12253084086666,-14.4891929905171,
1292.50514705882));
#160682=CARTESIAN_POINT('Ctrl Pts',(-5.41862499280729,-13.9870834410653,
1291.01102941176));
#160683=CARTESIAN_POINT('Ctrl Pts',(-6.71471914474793,-13.4849738916136,
1289.51691176471));
#160684=CARTESIAN_POINT('Ctrl Pts',(-7.89648244316034,-12.7532570359442,
1288.02279411765));
#160685=CARTESIAN_POINT('Ctrl Pts',(-9.07824574157275,-12.0215401802748,
1286.52867647059));
#160686=CARTESIAN_POINT('Ctrl Pts',(-10.1054346546984,-11.0851337583099,
1285.03455882353));
#160687=CARTESIAN_POINT('Ctrl Pts',(-11.132623567824,-10.148727336345,1283.54044117647));
#160688=CARTESIAN_POINT('Ctrl Pts',(-11.9702584092036,-9.03951954568885,
1282.04632352941));
#160689=CARTESIAN_POINT('Ctrl Pts',(-12.8078932505832,-7.93031175503273,
1280.55220588235));
#160690=CARTESIAN_POINT('Ctrl Pts',(-13.4274493703259,-6.68607533664808,
1279.05808823529));
#160691=CARTESIAN_POINT('Ctrl Pts',(-14.0470054900687,-5.44183891826343,
1277.56397058824));
#160692=CARTESIAN_POINT('Ctrl Pts',(-14.4273846475923,-4.10494485108124,
1276.06985294118));
#160693=CARTESIAN_POINT('Ctrl Pts',(-14.8077638051159,-2.76805078389906,
1274.57573529412));
#160694=CARTESIAN_POINT('Ctrl Pts',(-14.9360126444255,-1.38402539194953,
1273.08161764706));
#160695=CARTESIAN_POINT('Ctrl Pts',(-15.0642614837351,-9.22419980378748E-16,
1271.5875));
#160696=CARTESIAN_POINT('Ctrl Pts',(-14.9360126444255,1.38402539194953,
1270.09338235294));
#160697=CARTESIAN_POINT('Ctrl Pts',(-14.8077638051159,2.76805078389906,
1268.59926470588));
#160698=CARTESIAN_POINT('Ctrl Pts',(-14.4273846475923,4.10494485108124,
1267.10514705882));
#160699=CARTESIAN_POINT('Ctrl Pts',(-14.0470054900687,5.44183891826343,
1265.61102941176));
#160700=CARTESIAN_POINT('Ctrl Pts',(-13.4274493703259,6.68607533664807,
1264.11691176471));
#160701=CARTESIAN_POINT('Ctrl Pts',(-12.8078932505832,7.93031175503273,
1262.62279411765));
#160702=CARTESIAN_POINT('Ctrl Pts',(-11.9702584092036,9.03951954568884,
1261.12867647059));
#160703=CARTESIAN_POINT('Ctrl Pts',(-11.132623567824,10.148727336345,1259.63455882353));
#160704=CARTESIAN_POINT('Ctrl Pts',(-10.1054346546984,11.0851337583099,
1258.14044117647));
#160705=CARTESIAN_POINT('Ctrl Pts',(-9.07824574157275,12.0215401802748,
1256.64632352941));
#160706=CARTESIAN_POINT('Ctrl Pts',(-7.89648244316034,12.7532570359442,
1255.15220588235));
#160707=CARTESIAN_POINT('Ctrl Pts',(-6.71471914474793,13.4849738916136,
1253.65808823529));
#160708=CARTESIAN_POINT('Ctrl Pts',(-5.41862499280729,13.9870834410653,
1252.16397058824));
#160709=CARTESIAN_POINT('Ctrl Pts',(-4.12253084086667,14.4891929905171,
1250.66985294118));
#160710=CARTESIAN_POINT('Ctrl Pts',(-2.75624276724856,14.7445964952585,
1249.17573529412));
#160711=CARTESIAN_POINT('Ctrl Pts',(-1.38995469363044,15.,1247.68161764706));
#160712=CARTESIAN_POINT('Ctrl Pts',(-1.83697019872103E-15,15.,1246.1875));
#160713=CARTESIAN_POINT('Ctrl Pts',(1.38995469363045,15.,1244.69338235294));
#160714=CARTESIAN_POINT('Ctrl Pts',(2.75624276724855,14.7445964952585,1243.19926470588));
#160715=CARTESIAN_POINT('Ctrl Pts',(4.12253084086666,14.4891929905171,1241.70514705882));
#160716=CARTESIAN_POINT('Ctrl Pts',(5.4186249928073,13.9870834410653,1240.21102941176));
#160717=CARTESIAN_POINT('Ctrl Pts',(6.71471914474792,13.4849738916136,1238.71691176471));
#160718=CARTESIAN_POINT('Ctrl Pts',(7.89648244316034,12.7532570359442,1237.22279411765));
#160719=CARTESIAN_POINT('Ctrl Pts',(9.07824574157275,12.0215401802748,1235.72867647059));
#160720=CARTESIAN_POINT('Ctrl Pts',(10.1054346546984,11.0851337583099,1234.23455882353));
#160721=CARTESIAN_POINT('Ctrl Pts',(11.132623567824,10.148727336345,1232.74044117647));
#160722=CARTESIAN_POINT('Ctrl Pts',(11.9702584092036,9.03951954568885,1231.24632352941));
#160723=CARTESIAN_POINT('Ctrl Pts',(12.8078932505832,7.93031175503273,1229.75220588235));
#160724=CARTESIAN_POINT('Ctrl Pts',(13.4274493703259,6.68607533664807,1228.25808823529));
#160725=CARTESIAN_POINT('Ctrl Pts',(14.0470054900687,5.44183891826343,1226.76397058824));
#160726=CARTESIAN_POINT('Ctrl Pts',(14.4273846475923,4.10494485108125,1225.26985294118));
#160727=CARTESIAN_POINT('Ctrl Pts',(14.8077638051159,2.76805078389905,1223.77573529412));
#160728=CARTESIAN_POINT('Ctrl Pts',(14.9360126444255,1.38402539194953,1222.28161764706));
#160729=CARTESIAN_POINT('Ctrl Pts',(15.0642614837351,2.76725994113625E-15,
1220.7875));
#160730=CARTESIAN_POINT('Ctrl Pts',(14.9360126444255,-1.38402539194952,
1219.29338235294));
#160731=CARTESIAN_POINT('Ctrl Pts',(14.8077638051159,-2.76805078389906,
1217.79926470588));
#160732=CARTESIAN_POINT('Ctrl Pts',(14.4273846475923,-4.10494485108124,
1216.30514705882));
#160733=CARTESIAN_POINT('Ctrl Pts',(14.0470054900687,-5.44183891826342,
1214.81102941176));
#160734=CARTESIAN_POINT('Ctrl Pts',(13.4274493703259,-6.68607533664808,
1213.31691176471));
#160735=CARTESIAN_POINT('Ctrl Pts',(12.8078932505832,-7.93031175503273,
1211.82279411765));
#160736=CARTESIAN_POINT('Ctrl Pts',(11.9702584092036,-9.03951954568884,
1210.32867647059));
#160737=CARTESIAN_POINT('Ctrl Pts',(11.132623567824,-10.148727336345,1208.83455882353));
#160738=CARTESIAN_POINT('Ctrl Pts',(10.1054346546984,-11.0851337583099,
1207.34044117647));
#160739=CARTESIAN_POINT('Ctrl Pts',(9.07824574157275,-12.0215401802748,
1205.84632352941));
#160740=CARTESIAN_POINT('Ctrl Pts',(7.89648244316034,-12.7532570359442,
1204.35220588235));
#160741=CARTESIAN_POINT('Ctrl Pts',(6.71471914474792,-13.4849738916136,
1202.85808823529));
#160742=CARTESIAN_POINT('Ctrl Pts',(5.4186249928073,-13.9870834410653,1201.36397058824));
#160743=CARTESIAN_POINT('Ctrl Pts',(4.12253084086667,-14.4891929905171,
1199.86985294118));
#160744=CARTESIAN_POINT('Ctrl Pts',(2.75624276724855,-14.7445964952585,
1198.37573529412));
#160745=CARTESIAN_POINT('Ctrl Pts',(1.38995469363045,-15.,1196.88161764706));
#160746=CARTESIAN_POINT('Ctrl Pts',(0.,-15.,1195.3875));
#160747=CARTESIAN_POINT('Ctrl Pts',(-1.38995469363045,-15.,1193.89338235294));
#160748=CARTESIAN_POINT('Ctrl Pts',(-2.75624276724856,-14.7445964952585,
1192.39926470588));
#160749=CARTESIAN_POINT('Ctrl Pts',(-4.12253084086666,-14.4891929905171,
1190.90514705882));
#160750=CARTESIAN_POINT('Ctrl Pts',(-5.41862499280729,-13.9870834410653,
1189.41102941176));
#160751=CARTESIAN_POINT('Ctrl Pts',(-6.71471914474793,-13.4849738916136,
1187.91691176471));
#160752=CARTESIAN_POINT('Ctrl Pts',(-7.89648244316034,-12.7532570359442,
1186.42279411765));
#160753=CARTESIAN_POINT('Ctrl Pts',(-9.07824574157275,-12.0215401802748,
1184.92867647059));
#160754=CARTESIAN_POINT('Ctrl Pts',(-10.1054346546984,-11.0851337583099,
1183.43455882353));
#160755=CARTESIAN_POINT('Ctrl Pts',(-11.132623567824,-10.148727336345,1181.94044117647));
#160756=CARTESIAN_POINT('Ctrl Pts',(-11.9702584092036,-9.03951954568885,
1180.44632352941));
#160757=CARTESIAN_POINT('Ctrl Pts',(-12.8078932505832,-7.93031175503273,
1178.95220588235));
#160758=CARTESIAN_POINT('Ctrl Pts',(-13.4274493703259,-6.68607533664808,
1177.45808823529));
#160759=CARTESIAN_POINT('Ctrl Pts',(-14.0470054900687,-5.44183891826343,
1175.96397058824));
#160760=CARTESIAN_POINT('Ctrl Pts',(-14.4273846475923,-4.10494485108124,
1174.46985294118));
#160761=CARTESIAN_POINT('Ctrl Pts',(-14.8077638051159,-2.76805078389906,
1172.97573529412));
#160762=CARTESIAN_POINT('Ctrl Pts',(-14.9360126444255,-1.38402539194953,
1171.48161764706));
#160763=CARTESIAN_POINT('Ctrl Pts',(-15.0642614837351,-9.22419980378748E-16,
1169.9875));
#160764=CARTESIAN_POINT('Ctrl Pts',(-14.9360126444255,1.38402539194953,
1168.49338235294));
#160765=CARTESIAN_POINT('Ctrl Pts',(-14.8077638051159,2.76805078389906,
1166.99926470588));
#160766=CARTESIAN_POINT('Ctrl Pts',(-14.4273846475923,4.10494485108124,
1165.50514705882));
#160767=CARTESIAN_POINT('Ctrl Pts',(-14.0470054900687,5.44183891826343,
1164.01102941176));
#160768=CARTESIAN_POINT('Ctrl Pts',(-13.4274493703259,6.68607533664807,
1162.51691176471));
#160769=CARTESIAN_POINT('Ctrl Pts',(-12.8078932505832,7.93031175503273,
1161.02279411765));
#160770=CARTESIAN_POINT('Ctrl Pts',(-11.9702584092036,9.03951954568884,
1159.52867647059));
#160771=CARTESIAN_POINT('Ctrl Pts',(-11.132623567824,10.148727336345,1158.03455882353));
#160772=CARTESIAN_POINT('Ctrl Pts',(-10.1054346546984,11.0851337583099,
1156.54044117647));
#160773=CARTESIAN_POINT('Ctrl Pts',(-9.07824574157275,12.0215401802748,
1155.04632352941));
#160774=CARTESIAN_POINT('Ctrl Pts',(-7.89648244316034,12.7532570359442,
1153.55220588235));
#160775=CARTESIAN_POINT('Ctrl Pts',(-6.71471914474793,13.4849738916136,
1152.05808823529));
#160776=CARTESIAN_POINT('Ctrl Pts',(-5.41862499280729,13.9870834410653,
1150.56397058824));
#160777=CARTESIAN_POINT('Ctrl Pts',(-4.12253084086667,14.4891929905171,
1149.06985294118));
#160778=CARTESIAN_POINT('Ctrl Pts',(-2.75624276724856,14.7445964952585,
1147.57573529412));
#160779=CARTESIAN_POINT('Ctrl Pts',(-1.38995469363044,15.,1146.08161764706));
#160780=CARTESIAN_POINT('Ctrl Pts',(-1.83697019872103E-15,15.,1144.5875));
#160781=CARTESIAN_POINT('Ctrl Pts',(1.38995469363045,15.,1143.09338235294));
#160782=CARTESIAN_POINT('Ctrl Pts',(2.75624276724855,14.7445964952585,1141.59926470588));
#160783=CARTESIAN_POINT('Ctrl Pts',(4.12253084086666,14.4891929905171,1140.10514705882));
#160784=CARTESIAN_POINT('Ctrl Pts',(5.4186249928073,13.9870834410653,1138.61102941176));
#160785=CARTESIAN_POINT('Ctrl Pts',(6.71471914474792,13.4849738916136,1137.11691176471));
#160786=CARTESIAN_POINT('Ctrl Pts',(7.89648244316034,12.7532570359442,1135.62279411765));
#160787=CARTESIAN_POINT('Ctrl Pts',(9.07824574157275,12.0215401802748,1134.12867647059));
#160788=CARTESIAN_POINT('Ctrl Pts',(10.1054346546984,11.0851337583099,1132.63455882353));
#160789=CARTESIAN_POINT('Ctrl Pts',(11.132623567824,10.148727336345,1131.14044117647));
#160790=CARTESIAN_POINT('Ctrl Pts',(11.9702584092036,9.03951954568885,1129.64632352941));
#160791=CARTESIAN_POINT('Ctrl Pts',(12.8078932505832,7.93031175503273,1128.15220588235));
#160792=CARTESIAN_POINT('Ctrl Pts',(13.4274493703259,6.68607533664807,1126.65808823529));
#160793=CARTESIAN_POINT('Ctrl Pts',(14.0470054900687,5.44183891826343,1125.16397058824));
#160794=CARTESIAN_POINT('Ctrl Pts',(14.4273846475923,4.10494485108125,1123.66985294118));
#160795=CARTESIAN_POINT('Ctrl Pts',(14.8077638051159,2.76805078389905,1122.17573529412));
#160796=CARTESIAN_POINT('Ctrl Pts',(14.9360126444255,1.38402539194953,1120.68161764706));
#160797=CARTESIAN_POINT('Ctrl Pts',(15.0642614837351,2.76725994113625E-15,
1119.1875));
#160798=CARTESIAN_POINT('Ctrl Pts',(14.9360126444255,-1.38402539194952,
1117.69338235294));
#160799=CARTESIAN_POINT('Ctrl Pts',(14.8077638051159,-2.76805078389906,
1116.19926470588));
#160800=CARTESIAN_POINT('Ctrl Pts',(14.4273846475923,-4.10494485108124,
1114.70514705882));
#160801=CARTESIAN_POINT('Ctrl Pts',(14.0470054900687,-5.44183891826342,
1113.21102941176));
#160802=CARTESIAN_POINT('Ctrl Pts',(13.4274493703259,-6.68607533664808,
1111.71691176471));
#160803=CARTESIAN_POINT('Ctrl Pts',(12.8078932505832,-7.93031175503273,
1110.22279411765));
#160804=CARTESIAN_POINT('Ctrl Pts',(11.9702584092036,-9.03951954568884,
1108.72867647059));
#160805=CARTESIAN_POINT('Ctrl Pts',(11.132623567824,-10.148727336345,1107.23455882353));
#160806=CARTESIAN_POINT('Ctrl Pts',(10.1054346546984,-11.0851337583099,
1105.74044117647));
#160807=CARTESIAN_POINT('Ctrl Pts',(9.07824574157275,-12.0215401802748,
1104.24632352941));
#160808=CARTESIAN_POINT('Ctrl Pts',(7.89648244316034,-12.7532570359442,
1102.75220588235));
#160809=CARTESIAN_POINT('Ctrl Pts',(6.71471914474792,-13.4849738916136,
1101.25808823529));
#160810=CARTESIAN_POINT('Ctrl Pts',(5.4186249928073,-13.9870834410653,1099.76397058824));
#160811=CARTESIAN_POINT('Ctrl Pts',(4.12253084086667,-14.4891929905171,
1098.26985294118));
#160812=CARTESIAN_POINT('Ctrl Pts',(2.75624276724855,-14.7445964952585,
1096.77573529412));
#160813=CARTESIAN_POINT('Ctrl Pts',(1.38995469363045,-15.,1095.28161764706));
#160814=CARTESIAN_POINT('Ctrl Pts',(0.,-15.,1093.7875));
#160815=CARTESIAN_POINT('Ctrl Pts',(-1.38995469363045,-15.,1092.29338235294));
#160816=CARTESIAN_POINT('Ctrl Pts',(-2.75624276724856,-14.7445964952585,
1090.79926470588));
#160817=CARTESIAN_POINT('Ctrl Pts',(-4.12253084086666,-14.4891929905171,
1089.30514705882));
#160818=CARTESIAN_POINT('Ctrl Pts',(-5.41862499280729,-13.9870834410653,
1087.81102941176));
#160819=CARTESIAN_POINT('Ctrl Pts',(-6.71471914474793,-13.4849738916136,
1086.31691176471));
#160820=CARTESIAN_POINT('Ctrl Pts',(-7.89648244316034,-12.7532570359442,
1084.82279411765));
#160821=CARTESIAN_POINT('Ctrl Pts',(-9.07824574157275,-12.0215401802748,
1083.32867647059));
#160822=CARTESIAN_POINT('Ctrl Pts',(-10.1054346546984,-11.0851337583099,
1081.83455882353));
#160823=CARTESIAN_POINT('Ctrl Pts',(-11.132623567824,-10.148727336345,1080.34044117647));
#160824=CARTESIAN_POINT('Ctrl Pts',(-11.9702584092036,-9.03951954568885,
1078.84632352941));
#160825=CARTESIAN_POINT('Ctrl Pts',(-12.8078932505832,-7.93031175503273,
1077.35220588235));
#160826=CARTESIAN_POINT('Ctrl Pts',(-13.4274493703259,-6.68607533664808,
1075.85808823529));
#160827=CARTESIAN_POINT('Ctrl Pts',(-14.0470054900687,-5.44183891826343,
1074.36397058824));
#160828=CARTESIAN_POINT('Ctrl Pts',(-14.4273846475923,-4.10494485108124,
1072.86985294118));
#160829=CARTESIAN_POINT('Ctrl Pts',(-14.8077638051159,-2.76805078389906,
1071.37573529412));
#160830=CARTESIAN_POINT('Ctrl Pts',(-14.9360126444255,-1.38402539194953,
1069.88161764706));
#160831=CARTESIAN_POINT('Ctrl Pts',(-15.0642614837351,-9.22419980378748E-16,
1068.3875));
#160832=CARTESIAN_POINT('Ctrl Pts',(-14.9360126444255,1.38402539194953,
1066.89338235294));
#160833=CARTESIAN_POINT('Ctrl Pts',(-14.8077638051159,2.76805078389906,
1065.39926470588));
#160834=CARTESIAN_POINT('Ctrl Pts',(-14.4273846475923,4.10494485108124,
1063.90514705882));
#160835=CARTESIAN_POINT('Ctrl Pts',(-14.0470054900687,5.44183891826343,
1062.41102941176));
#160836=CARTESIAN_POINT('Ctrl Pts',(-13.4274493703259,6.68607533664807,
1060.91691176471));
#160837=CARTESIAN_POINT('Ctrl Pts',(-12.8078932505832,7.93031175503273,
1059.42279411765));
#160838=CARTESIAN_POINT('Ctrl Pts',(-11.9702584092036,9.03951954568884,
1057.92867647059));
#160839=CARTESIAN_POINT('Ctrl Pts',(-11.132623567824,10.148727336345,1056.43455882353));
#160840=CARTESIAN_POINT('Ctrl Pts',(-10.1054346546984,11.0851337583099,
1054.94044117647));
#160841=CARTESIAN_POINT('Ctrl Pts',(-9.07824574157275,12.0215401802748,
1053.44632352941));
#160842=CARTESIAN_POINT('Ctrl Pts',(-7.89648244316034,12.7532570359442,
1051.95220588235));
#160843=CARTESIAN_POINT('Ctrl Pts',(-6.71471914474793,13.4849738916136,
1050.45808823529));
#160844=CARTESIAN_POINT('Ctrl Pts',(-5.41862499280729,13.9870834410653,
1048.96397058824));
#160845=CARTESIAN_POINT('Ctrl Pts',(-4.12253084086667,14.4891929905171,
1047.46985294118));
#160846=CARTESIAN_POINT('Ctrl Pts',(-2.75624276724856,14.7445964952585,
1045.97573529412));
#160847=CARTESIAN_POINT('Ctrl Pts',(-1.38995469363044,15.,1044.48161764706));
#160848=CARTESIAN_POINT('Ctrl Pts',(-1.83697019872103E-15,15.,1042.9875));
#160849=CARTESIAN_POINT('Ctrl Pts',(1.38995469363045,15.,1041.49338235294));
#160850=CARTESIAN_POINT('Ctrl Pts',(2.75624276724855,14.7445964952585,1039.99926470588));
#160851=CARTESIAN_POINT('Ctrl Pts',(4.12253084086666,14.4891929905171,1038.50514705882));
#160852=CARTESIAN_POINT('Ctrl Pts',(5.4186249928073,13.9870834410653,1037.01102941176));
#160853=CARTESIAN_POINT('Ctrl Pts',(6.71471914474792,13.4849738916136,1035.51691176471));
#160854=CARTESIAN_POINT('Ctrl Pts',(7.89648244316034,12.7532570359442,1034.02279411765));
#160855=CARTESIAN_POINT('Ctrl Pts',(9.07824574157275,12.0215401802748,1032.52867647059));
#160856=CARTESIAN_POINT('Ctrl Pts',(10.1054346546984,11.0851337583099,1031.03455882353));
#160857=CARTESIAN_POINT('Ctrl Pts',(11.132623567824,10.148727336345,1029.54044117647));
#160858=CARTESIAN_POINT('Ctrl Pts',(11.9702584092036,9.03951954568885,1028.04632352941));
#160859=CARTESIAN_POINT('Ctrl Pts',(12.8078932505832,7.93031175503273,1026.55220588235));
#160860=CARTESIAN_POINT('Ctrl Pts',(13.4274493703259,6.68607533664807,1025.05808823529));
#160861=CARTESIAN_POINT('Ctrl Pts',(14.0470054900687,5.44183891826343,1023.56397058824));
#160862=CARTESIAN_POINT('Ctrl Pts',(14.4273846475923,4.10494485108125,1022.06985294118));
#160863=CARTESIAN_POINT('Ctrl Pts',(14.8077638051159,2.76805078389905,1020.57573529412));
#160864=CARTESIAN_POINT('Ctrl Pts',(14.9360126444255,1.38402539194953,1019.08161764706));
#160865=CARTESIAN_POINT('Ctrl Pts',(15.0642614837351,2.76725994113625E-15,
1017.5875));
#160866=CARTESIAN_POINT('Ctrl Pts',(14.9360126444255,-1.38402539194952,
1016.09338235294));
#160867=CARTESIAN_POINT('Ctrl Pts',(14.8077638051159,-2.76805078389906,
1014.59926470588));
#160868=CARTESIAN_POINT('Ctrl Pts',(14.4273846475923,-4.10494485108124,
1013.10514705882));
#160869=CARTESIAN_POINT('Ctrl Pts',(14.0470054900687,-5.44183891826342,
1011.61102941176));
#160870=CARTESIAN_POINT('Ctrl Pts',(13.4274493703259,-6.68607533664808,
1010.11691176471));
#160871=CARTESIAN_POINT('Ctrl Pts',(12.8078932505832,-7.93031175503273,
1008.62279411765));
#160872=CARTESIAN_POINT('Ctrl Pts',(11.9702584092036,-9.03951954568884,
1007.12867647059));
#160873=CARTESIAN_POINT('Ctrl Pts',(11.132623567824,-10.148727336345,1005.63455882353));
#160874=CARTESIAN_POINT('Ctrl Pts',(10.1054346546984,-11.0851337583099,
1004.14044117647));
#160875=CARTESIAN_POINT('Ctrl Pts',(9.07824574157275,-12.0215401802748,
1002.64632352941));
#160876=CARTESIAN_POINT('Ctrl Pts',(7.89648244316034,-12.7532570359442,
1001.15220588235));
#160877=CARTESIAN_POINT('Ctrl Pts',(6.71471914474792,-13.4849738916136,
999.658088235294));
#160878=CARTESIAN_POINT('Ctrl Pts',(5.4186249928073,-13.9870834410653,998.163970588235));
#160879=CARTESIAN_POINT('Ctrl Pts',(4.12253084086667,-14.4891929905171,
996.669852941177));
#160880=CARTESIAN_POINT('Ctrl Pts',(2.75624276724855,-14.7445964952585,
995.175735294118));
#160881=CARTESIAN_POINT('Ctrl Pts',(1.38995469363045,-15.,993.681617647059));
#160882=CARTESIAN_POINT('Ctrl Pts',(0.,-15.,992.1875));
#160883=CARTESIAN_POINT('Ctrl Pts',(-1.38995469363045,-15.,990.693382352941));
#160884=CARTESIAN_POINT('Ctrl Pts',(-2.75624276724856,-14.7445964952585,
989.199264705882));
#160885=CARTESIAN_POINT('Ctrl Pts',(-4.12253084086666,-14.4891929905171,
987.705147058824));
#160886=CARTESIAN_POINT('Ctrl Pts',(-5.41862499280729,-13.9870834410653,
986.211029411765));
#160887=CARTESIAN_POINT('Ctrl Pts',(-6.71471914474793,-13.4849738916136,
984.716911764706));
#160888=CARTESIAN_POINT('Ctrl Pts',(-7.89648244316034,-12.7532570359442,
983.222794117647));
#160889=CARTESIAN_POINT('Ctrl Pts',(-9.07824574157275,-12.0215401802748,
981.728676470589));
#160890=CARTESIAN_POINT('Ctrl Pts',(-10.1054346546984,-11.0851337583099,
980.234558823529));
#160891=CARTESIAN_POINT('Ctrl Pts',(-11.132623567824,-10.148727336345,978.740441176471));
#160892=CARTESIAN_POINT('Ctrl Pts',(-11.9702584092036,-9.03951954568885,
977.246323529412));
#160893=CARTESIAN_POINT('Ctrl Pts',(-12.8078932505832,-7.93031175503273,
975.752205882353));
#160894=CARTESIAN_POINT('Ctrl Pts',(-13.4274493703259,-6.68607533664808,
974.258088235294));
#160895=CARTESIAN_POINT('Ctrl Pts',(-14.0470054900687,-5.44183891826343,
972.763970588235));
#160896=CARTESIAN_POINT('Ctrl Pts',(-14.4273846475923,-4.10494485108124,
971.269852941177));
#160897=CARTESIAN_POINT('Ctrl Pts',(-14.8077638051159,-2.76805078389906,
969.775735294118));
#160898=CARTESIAN_POINT('Ctrl Pts',(-14.9360126444255,-1.38402539194953,
968.281617647059));
#160899=CARTESIAN_POINT('Ctrl Pts',(-15.0642614837351,-9.22419980378748E-16,
966.7875));
#160900=CARTESIAN_POINT('Ctrl Pts',(-14.9360126444255,1.38402539194953,
965.293382352941));
#160901=CARTESIAN_POINT('Ctrl Pts',(-14.8077638051159,2.76805078389906,
963.799264705882));
#160902=CARTESIAN_POINT('Ctrl Pts',(-14.4273846475923,4.10494485108124,
962.305147058824));
#160903=CARTESIAN_POINT('Ctrl Pts',(-14.0470054900687,5.44183891826343,
960.811029411765));
#160904=CARTESIAN_POINT('Ctrl Pts',(-13.4274493703259,6.68607533664807,
959.316911764706));
#160905=CARTESIAN_POINT('Ctrl Pts',(-12.8078932505832,7.93031175503273,
957.822794117647));
#160906=CARTESIAN_POINT('Ctrl Pts',(-11.9702584092036,9.03951954568884,
956.328676470588));
#160907=CARTESIAN_POINT('Ctrl Pts',(-11.132623567824,10.148727336345,954.834558823529));
#160908=CARTESIAN_POINT('Ctrl Pts',(-10.1054346546984,11.0851337583099,
953.340441176471));
#160909=CARTESIAN_POINT('Ctrl Pts',(-9.07824574157275,12.0215401802748,
951.846323529412));
#160910=CARTESIAN_POINT('Ctrl Pts',(-7.89648244316034,12.7532570359442,
950.352205882353));
#160911=CARTESIAN_POINT('Ctrl Pts',(-6.71471914474793,13.4849738916136,
948.858088235294));
#160912=CARTESIAN_POINT('Ctrl Pts',(-5.41862499280729,13.9870834410653,
947.363970588235));
#160913=CARTESIAN_POINT('Ctrl Pts',(-4.12253084086667,14.4891929905171,
945.869852941177));
#160914=CARTESIAN_POINT('Ctrl Pts',(-2.75624276724856,14.7445964952585,
944.375735294118));
#160915=CARTESIAN_POINT('Ctrl Pts',(-1.38995469363044,15.,942.881617647059));
#160916=CARTESIAN_POINT('Ctrl Pts',(-1.83697019872103E-15,15.,941.3875));
#160917=CARTESIAN_POINT('Ctrl Pts',(1.38995469363045,15.,939.893382352941));
#160918=CARTESIAN_POINT('Ctrl Pts',(2.75624276724855,14.7445964952585,938.399264705882));
#160919=CARTESIAN_POINT('Ctrl Pts',(4.12253084086666,14.4891929905171,936.905147058824));
#160920=CARTESIAN_POINT('Ctrl Pts',(5.4186249928073,13.9870834410653,935.411029411765));
#160921=CARTESIAN_POINT('Ctrl Pts',(6.71471914474792,13.4849738916136,933.916911764706));
#160922=CARTESIAN_POINT('Ctrl Pts',(7.89648244316034,12.7532570359442,932.422794117647));
#160923=CARTESIAN_POINT('Ctrl Pts',(9.07824574157275,12.0215401802748,930.928676470588));
#160924=CARTESIAN_POINT('Ctrl Pts',(10.1054346546984,11.0851337583099,929.43455882353));
#160925=CARTESIAN_POINT('Ctrl Pts',(11.132623567824,10.148727336345,927.94044117647));
#160926=CARTESIAN_POINT('Ctrl Pts',(11.9702584092036,9.03951954568885,926.446323529412));
#160927=CARTESIAN_POINT('Ctrl Pts',(12.8078932505832,7.93031175503273,924.952205882353));
#160928=CARTESIAN_POINT('Ctrl Pts',(13.4274493703259,6.68607533664807,923.458088235294));
#160929=CARTESIAN_POINT('Ctrl Pts',(14.0470054900687,5.44183891826343,921.963970588235));
#160930=CARTESIAN_POINT('Ctrl Pts',(14.4273846475923,4.10494485108125,920.469852941176));
#160931=CARTESIAN_POINT('Ctrl Pts',(14.8077638051159,2.76805078389905,918.975735294118));
#160932=CARTESIAN_POINT('Ctrl Pts',(14.9360126444255,1.38402539194953,917.481617647059));
#160933=CARTESIAN_POINT('Ctrl Pts',(15.0642614837351,2.76725994113625E-15,
915.9875));
#160934=CARTESIAN_POINT('Ctrl Pts',(14.9360126444255,-1.38402539194952,
914.493382352941));
#160935=CARTESIAN_POINT('Ctrl Pts',(14.8077638051159,-2.76805078389906,
912.999264705882));
#160936=CARTESIAN_POINT('Ctrl Pts',(14.4273846475923,-4.10494485108124,
911.505147058824));
#160937=CARTESIAN_POINT('Ctrl Pts',(14.0470054900687,-5.44183891826342,
910.011029411765));
#160938=CARTESIAN_POINT('Ctrl Pts',(13.4274493703259,-6.68607533664808,
908.516911764706));
#160939=CARTESIAN_POINT('Ctrl Pts',(12.8078932505832,-7.93031175503273,
907.022794117647));
#160940=CARTESIAN_POINT('Ctrl Pts',(11.9702584092036,-9.03951954568884,
905.528676470588));
#160941=CARTESIAN_POINT('Ctrl Pts',(11.132623567824,-10.148727336345,904.034558823529));
#160942=CARTESIAN_POINT('Ctrl Pts',(10.1054346546984,-11.0851337583099,
902.540441176471));
#160943=CARTESIAN_POINT('Ctrl Pts',(9.07824574157275,-12.0215401802748,
901.046323529412));
#160944=CARTESIAN_POINT('Ctrl Pts',(7.89648244316034,-12.7532570359442,
899.552205882353));
#160945=CARTESIAN_POINT('Ctrl Pts',(6.71471914474792,-13.4849738916136,
898.058088235294));
#160946=CARTESIAN_POINT('Ctrl Pts',(5.4186249928073,-13.9870834410653,896.563970588235));
#160947=CARTESIAN_POINT('Ctrl Pts',(4.12253084086667,-14.4891929905171,
895.069852941177));
#160948=CARTESIAN_POINT('Ctrl Pts',(2.75624276724855,-14.7445964952585,
893.575735294118));
#160949=CARTESIAN_POINT('Ctrl Pts',(1.38995469363045,-15.,892.081617647059));
#160950=CARTESIAN_POINT('Ctrl Pts',(0.,-15.,890.5875));
#160951=CARTESIAN_POINT('Ctrl Pts',(-1.38995469363045,-15.,889.093382352941));
#160952=CARTESIAN_POINT('Ctrl Pts',(-2.75624276724856,-14.7445964952585,
887.599264705882));
#160953=CARTESIAN_POINT('Ctrl Pts',(-4.12253084086666,-14.4891929905171,
886.105147058824));
#160954=CARTESIAN_POINT('Ctrl Pts',(-5.41862499280729,-13.9870834410653,
884.611029411765));
#160955=CARTESIAN_POINT('Ctrl Pts',(-6.71471914474793,-13.4849738916136,
883.116911764706));
#160956=CARTESIAN_POINT('Ctrl Pts',(-7.89648244316034,-12.7532570359442,
881.622794117647));
#160957=CARTESIAN_POINT('Ctrl Pts',(-9.07824574157275,-12.0215401802748,
880.128676470588));
#160958=CARTESIAN_POINT('Ctrl Pts',(-10.1054346546984,-11.0851337583099,
878.634558823529));
#160959=CARTESIAN_POINT('Ctrl Pts',(-11.132623567824,-10.148727336345,877.140441176471));
#160960=CARTESIAN_POINT('Ctrl Pts',(-11.9702584092036,-9.03951954568885,
875.646323529412));
#160961=CARTESIAN_POINT('Ctrl Pts',(-12.8078932505832,-7.93031175503273,
874.152205882353));
#160962=CARTESIAN_POINT('Ctrl Pts',(-13.4274493703259,-6.68607533664808,
872.658088235294));
#160963=CARTESIAN_POINT('Ctrl Pts',(-14.0470054900687,-5.44183891826343,
871.163970588236));
#160964=CARTESIAN_POINT('Ctrl Pts',(-14.4273846475923,-4.10494485108124,
869.669852941176));
#160965=CARTESIAN_POINT('Ctrl Pts',(-14.8077638051159,-2.76805078389906,
868.175735294118));
#160966=CARTESIAN_POINT('Ctrl Pts',(-14.9360126444255,-1.38402539194953,
866.681617647059));
#160967=CARTESIAN_POINT('Ctrl Pts',(-15.0642614837351,-9.22419980378748E-16,
865.1875));
#160968=CARTESIAN_POINT('Ctrl Pts',(-14.9360126444255,1.38402539194953,
863.693382352941));
#160969=CARTESIAN_POINT('Ctrl Pts',(-14.8077638051159,2.76805078389906,
862.199264705883));
#160970=CARTESIAN_POINT('Ctrl Pts',(-14.4273846475923,4.10494485108124,
860.705147058824));
#160971=CARTESIAN_POINT('Ctrl Pts',(-14.0470054900687,5.44183891826343,
859.211029411765));
#160972=CARTESIAN_POINT('Ctrl Pts',(-13.4274493703259,6.68607533664807,
857.716911764706));
#160973=CARTESIAN_POINT('Ctrl Pts',(-12.8078932505832,7.93031175503273,
856.222794117647));
#160974=CARTESIAN_POINT('Ctrl Pts',(-11.9702584092036,9.03951954568884,
854.728676470588));
#160975=CARTESIAN_POINT('Ctrl Pts',(-11.132623567824,10.148727336345,853.234558823529));
#160976=CARTESIAN_POINT('Ctrl Pts',(-10.1054346546984,11.0851337583099,
851.740441176471));
#160977=CARTESIAN_POINT('Ctrl Pts',(-9.07824574157275,12.0215401802748,
850.246323529412));
#160978=CARTESIAN_POINT('Ctrl Pts',(-7.89648244316034,12.7532570359442,
848.752205882353));
#160979=CARTESIAN_POINT('Ctrl Pts',(-6.71471914474793,13.4849738916136,
847.258088235294));
#160980=CARTESIAN_POINT('Ctrl Pts',(-5.41862499280729,13.9870834410653,
845.763970588235));
#160981=CARTESIAN_POINT('Ctrl Pts',(-4.12253084086667,14.4891929905171,
844.269852941177));
#160982=CARTESIAN_POINT('Ctrl Pts',(-2.75624276724856,14.7445964952585,
842.775735294118));
#160983=CARTESIAN_POINT('Ctrl Pts',(-1.38995469363044,15.,841.281617647059));
#160984=CARTESIAN_POINT('Ctrl Pts',(-1.83697019872103E-15,15.,839.7875));
#160985=CARTESIAN_POINT('Ctrl Pts',(1.38995469363045,15.,838.293382352941));
#160986=CARTESIAN_POINT('Ctrl Pts',(2.75624276724855,14.7445964952585,836.799264705882));
#160987=CARTESIAN_POINT('Ctrl Pts',(4.12253084086666,14.4891929905171,835.305147058824));
#160988=CARTESIAN_POINT('Ctrl Pts',(5.4186249928073,13.9870834410653,833.811029411765));
#160989=CARTESIAN_POINT('Ctrl Pts',(6.71471914474792,13.4849738916136,832.316911764706));
#160990=CARTESIAN_POINT('Ctrl Pts',(7.89648244316034,12.7532570359442,830.822794117647));
#160991=CARTESIAN_POINT('Ctrl Pts',(9.07824574157275,12.0215401802748,829.328676470588));
#160992=CARTESIAN_POINT('Ctrl Pts',(10.1054346546984,11.0851337583099,827.834558823529));
#160993=CARTESIAN_POINT('Ctrl Pts',(11.132623567824,10.148727336345,826.340441176471));
#160994=CARTESIAN_POINT('Ctrl Pts',(11.9702584092036,9.03951954568885,824.846323529412));
#160995=CARTESIAN_POINT('Ctrl Pts',(12.8078932505832,7.93031175503273,823.352205882353));
#160996=CARTESIAN_POINT('Ctrl Pts',(13.4274493703259,6.68607533664807,821.858088235294));
#160997=CARTESIAN_POINT('Ctrl Pts',(14.0470054900687,5.44183891826343,820.363970588236));
#160998=CARTESIAN_POINT('Ctrl Pts',(14.4273846475923,4.10494485108125,818.869852941177));
#160999=CARTESIAN_POINT('Ctrl Pts',(14.8077638051159,2.76805078389905,817.375735294118));
#161000=CARTESIAN_POINT('Ctrl Pts',(14.9360126444255,1.38402539194953,815.881617647059));
#161001=CARTESIAN_POINT('Ctrl Pts',(15.0642614837351,2.76725994113625E-15,
814.3875));
#161002=CARTESIAN_POINT('Ctrl Pts',(14.9360126444255,-1.38402539194952,
812.893382352941));
#161003=CARTESIAN_POINT('Ctrl Pts',(14.8077638051159,-2.76805078389906,
811.399264705883));
#161004=CARTESIAN_POINT('Ctrl Pts',(14.4273846475923,-4.10494485108124,
809.905147058824));
#161005=CARTESIAN_POINT('Ctrl Pts',(14.0470054900687,-5.44183891826342,
808.411029411765));
#161006=CARTESIAN_POINT('Ctrl Pts',(13.4274493703259,-6.68607533664808,
806.916911764706));
#161007=CARTESIAN_POINT('Ctrl Pts',(12.8078932505832,-7.93031175503273,
805.422794117647));
#161008=CARTESIAN_POINT('Ctrl Pts',(11.9702584092036,-9.03951954568884,
803.928676470588));
#161009=CARTESIAN_POINT('Ctrl Pts',(11.132623567824,-10.148727336345,802.434558823529));
#161010=CARTESIAN_POINT('Ctrl Pts',(10.1054346546984,-11.0851337583099,
800.940441176471));
#161011=CARTESIAN_POINT('Ctrl Pts',(9.07824574157275,-12.0215401802748,
799.446323529412));
#161012=CARTESIAN_POINT('Ctrl Pts',(7.89648244316034,-12.7532570359442,
797.952205882353));
#161013=CARTESIAN_POINT('Ctrl Pts',(6.71471914474792,-13.4849738916136,
796.458088235294));
#161014=CARTESIAN_POINT('Ctrl Pts',(5.4186249928073,-13.9870834410653,794.963970588235));
#161015=CARTESIAN_POINT('Ctrl Pts',(4.12253084086667,-14.4891929905171,
793.469852941176));
#161016=CARTESIAN_POINT('Ctrl Pts',(2.75624276724855,-14.7445964952585,
791.975735294118));
#161017=CARTESIAN_POINT('Ctrl Pts',(1.38995469363045,-15.,790.481617647059));
#161018=CARTESIAN_POINT('Ctrl Pts',(0.,-15.,788.9875));
#161019=CARTESIAN_POINT('Ctrl Pts',(-1.38995469363045,-15.,787.493382352941));
#161020=CARTESIAN_POINT('Ctrl Pts',(-2.75624276724856,-14.7445964952585,
785.999264705882));
#161021=CARTESIAN_POINT('Ctrl Pts',(-4.12253084086666,-14.4891929905171,
784.505147058824));
#161022=CARTESIAN_POINT('Ctrl Pts',(-5.41862499280729,-13.9870834410653,
783.011029411765));
#161023=CARTESIAN_POINT('Ctrl Pts',(-6.71471914474793,-13.4849738916136,
781.516911764706));
#161024=CARTESIAN_POINT('Ctrl Pts',(-7.89648244316034,-12.7532570359442,
780.022794117647));
#161025=CARTESIAN_POINT('Ctrl Pts',(-9.07824574157275,-12.0215401802748,
778.528676470588));
#161026=CARTESIAN_POINT('Ctrl Pts',(-10.1054346546984,-11.0851337583099,
777.03455882353));
#161027=CARTESIAN_POINT('Ctrl Pts',(-11.132623567824,-10.148727336345,775.540441176471));
#161028=CARTESIAN_POINT('Ctrl Pts',(-11.9702584092036,-9.03951954568885,
774.046323529412));
#161029=CARTESIAN_POINT('Ctrl Pts',(-12.8078932505832,-7.93031175503273,
772.552205882353));
#161030=CARTESIAN_POINT('Ctrl Pts',(-13.4274493703259,-6.68607533664808,
771.058088235294));
#161031=CARTESIAN_POINT('Ctrl Pts',(-14.0470054900687,-5.44183891826343,
769.563970588235));
#161032=CARTESIAN_POINT('Ctrl Pts',(-14.4273846475923,-4.10494485108124,
768.069852941177));
#161033=CARTESIAN_POINT('Ctrl Pts',(-14.8077638051159,-2.76805078389906,
766.575735294118));
#161034=CARTESIAN_POINT('Ctrl Pts',(-14.9360126444255,-1.38402539194953,
765.081617647059));
#161035=CARTESIAN_POINT('Ctrl Pts',(-15.0642614837351,-9.22419980378748E-16,
763.5875));
#161036=CARTESIAN_POINT('Ctrl Pts',(-14.9360126444255,1.38402539194953,
762.093382352941));
#161037=CARTESIAN_POINT('Ctrl Pts',(-14.8077638051159,2.76805078389906,
760.599264705883));
#161038=CARTESIAN_POINT('Ctrl Pts',(-14.4273846475923,4.10494485108124,
759.105147058824));
#161039=CARTESIAN_POINT('Ctrl Pts',(-14.0470054900687,5.44183891826343,
757.611029411765));
#161040=CARTESIAN_POINT('Ctrl Pts',(-13.4274493703259,6.68607533664807,
756.116911764706));
#161041=CARTESIAN_POINT('Ctrl Pts',(-12.8078932505832,7.93031175503273,
754.622794117647));
#161042=CARTESIAN_POINT('Ctrl Pts',(-11.9702584092036,9.03951954568884,
753.128676470588));
#161043=CARTESIAN_POINT('Ctrl Pts',(-11.132623567824,10.148727336345,751.634558823529));
#161044=CARTESIAN_POINT('Ctrl Pts',(-10.1054346546984,11.0851337583099,
750.140441176471));
#161045=CARTESIAN_POINT('Ctrl Pts',(-9.07824574157275,12.0215401802748,
748.646323529412));
#161046=CARTESIAN_POINT('Ctrl Pts',(-7.89648244316034,12.7532570359442,
747.152205882353));
#161047=CARTESIAN_POINT('Ctrl Pts',(-6.71471914474793,13.4849738916136,
745.658088235294));
#161048=CARTESIAN_POINT('Ctrl Pts',(-5.41862499280729,13.9870834410653,
744.163970588235));
#161049=CARTESIAN_POINT('Ctrl Pts',(-4.12253084086667,14.4891929905171,
742.669852941176));
#161050=CARTESIAN_POINT('Ctrl Pts',(-2.75624276724856,14.7445964952585,
741.175735294118));
#161051=CARTESIAN_POINT('Ctrl Pts',(-1.38995469363044,15.,739.681617647059));
#161052=CARTESIAN_POINT('Ctrl Pts',(-1.83697019872103E-15,15.,738.1875));
#161053=CARTESIAN_POINT('Ctrl Pts',(1.38995469363045,15.,736.693382352941));
#161054=CARTESIAN_POINT('Ctrl Pts',(2.75624276724855,14.7445964952585,735.199264705882));
#161055=CARTESIAN_POINT('Ctrl Pts',(4.12253084086666,14.4891929905171,733.705147058824));
#161056=CARTESIAN_POINT('Ctrl Pts',(5.4186249928073,13.9870834410653,732.211029411765));
#161057=CARTESIAN_POINT('Ctrl Pts',(6.71471914474792,13.4849738916136,730.716911764706));
#161058=CARTESIAN_POINT('Ctrl Pts',(7.89648244316034,12.7532570359442,729.222794117647));
#161059=CARTESIAN_POINT('Ctrl Pts',(9.07824574157275,12.0215401802748,727.728676470588));
#161060=CARTESIAN_POINT('Ctrl Pts',(10.1054346546984,11.0851337583099,726.234558823529));
#161061=CARTESIAN_POINT('Ctrl Pts',(11.132623567824,10.148727336345,724.740441176471));
#161062=CARTESIAN_POINT('Ctrl Pts',(11.9702584092036,9.03951954568885,723.246323529412));
#161063=CARTESIAN_POINT('Ctrl Pts',(12.8078932505832,7.93031175503273,721.752205882353));
#161064=CARTESIAN_POINT('Ctrl Pts',(13.4274493703259,6.68607533664807,720.258088235294));
#161065=CARTESIAN_POINT('Ctrl Pts',(14.0470054900687,5.44183891826343,718.763970588235));
#161066=CARTESIAN_POINT('Ctrl Pts',(14.4273846475923,4.10494485108125,717.269852941177));
#161067=CARTESIAN_POINT('Ctrl Pts',(14.8077638051159,2.76805078389905,715.775735294118));
#161068=CARTESIAN_POINT('Ctrl Pts',(14.9360126444255,1.38402539194953,714.281617647059));
#161069=CARTESIAN_POINT('Ctrl Pts',(15.0642614837351,2.76725994113625E-15,
712.7875));
#161070=CARTESIAN_POINT('Ctrl Pts',(14.9360126444255,-1.38402539194952,
711.293382352941));
#161071=CARTESIAN_POINT('Ctrl Pts',(14.8077638051159,-2.76805078389906,
709.799264705883));
#161072=CARTESIAN_POINT('Ctrl Pts',(14.4273846475923,-4.10494485108124,
708.305147058824));
#161073=CARTESIAN_POINT('Ctrl Pts',(14.0470054900687,-5.44183891826342,
706.811029411765));
#161074=CARTESIAN_POINT('Ctrl Pts',(13.4274493703259,-6.68607533664808,
705.316911764706));
#161075=CARTESIAN_POINT('Ctrl Pts',(12.8078932505832,-7.93031175503273,
703.822794117647));
#161076=CARTESIAN_POINT('Ctrl Pts',(11.9702584092036,-9.03951954568884,
702.328676470588));
#161077=CARTESIAN_POINT('Ctrl Pts',(11.132623567824,-10.148727336345,700.83455882353));
#161078=CARTESIAN_POINT('Ctrl Pts',(10.1054346546984,-11.0851337583099,
699.340441176471));
#161079=CARTESIAN_POINT('Ctrl Pts',(9.07824574157275,-12.0215401802748,
697.846323529412));
#161080=CARTESIAN_POINT('Ctrl Pts',(7.89648244316034,-12.7532570359442,
696.352205882353));
#161081=CARTESIAN_POINT('Ctrl Pts',(6.71471914474792,-13.4849738916136,
694.858088235294));
#161082=CARTESIAN_POINT('Ctrl Pts',(5.4186249928073,-13.9870834410653,693.363970588235));
#161083=CARTESIAN_POINT('Ctrl Pts',(4.12253084086667,-14.4891929905171,
691.869852941177));
#161084=CARTESIAN_POINT('Ctrl Pts',(2.75624276724855,-14.7445964952585,
690.375735294118));
#161085=CARTESIAN_POINT('Ctrl Pts',(1.38995469363045,-15.,688.881617647059));
#161086=CARTESIAN_POINT('Ctrl Pts',(0.,-15.,687.3875));
#161087=CARTESIAN_POINT('Ctrl Pts',(-1.38995469363045,-15.,685.893382352941));
#161088=CARTESIAN_POINT('Ctrl Pts',(-2.75624276724856,-14.7445964952585,
684.399264705883));
#161089=CARTESIAN_POINT('Ctrl Pts',(-4.12253084086666,-14.4891929905171,
682.905147058824));
#161090=CARTESIAN_POINT('Ctrl Pts',(-5.41862499280729,-13.9870834410653,
681.411029411765));
#161091=CARTESIAN_POINT('Ctrl Pts',(-6.71471914474793,-13.4849738916136,
679.916911764706));
#161092=CARTESIAN_POINT('Ctrl Pts',(-7.89648244316034,-12.7532570359442,
678.422794117647));
#161093=CARTESIAN_POINT('Ctrl Pts',(-9.07824574157275,-12.0215401802748,
676.928676470588));
#161094=CARTESIAN_POINT('Ctrl Pts',(-10.1054346546984,-11.0851337583099,
675.434558823529));
#161095=CARTESIAN_POINT('Ctrl Pts',(-11.132623567824,-10.148727336345,673.940441176471));
#161096=CARTESIAN_POINT('Ctrl Pts',(-11.9702584092036,-9.03951954568885,
672.446323529412));
#161097=CARTESIAN_POINT('Ctrl Pts',(-12.8078932505832,-7.93031175503273,
670.952205882353));
#161098=CARTESIAN_POINT('Ctrl Pts',(-13.4274493703259,-6.68607533664808,
669.458088235294));
#161099=CARTESIAN_POINT('Ctrl Pts',(-14.0470054900687,-5.44183891826343,
667.963970588235));
#161100=CARTESIAN_POINT('Ctrl Pts',(-14.4273846475923,-4.10494485108124,
666.469852941176));
#161101=CARTESIAN_POINT('Ctrl Pts',(-14.8077638051159,-2.76805078389906,
664.975735294118));
#161102=CARTESIAN_POINT('Ctrl Pts',(-14.9360126444255,-1.38402539194953,
663.481617647059));
#161103=CARTESIAN_POINT('Ctrl Pts',(-15.0642614837351,-9.22419980378748E-16,
661.9875));
#161104=CARTESIAN_POINT('Ctrl Pts',(-14.9360126444255,1.38402539194953,
660.493382352941));
#161105=CARTESIAN_POINT('Ctrl Pts',(-14.8077638051159,2.76805078389906,
658.999264705882));
#161106=CARTESIAN_POINT('Ctrl Pts',(-14.4273846475923,4.10494485108124,
657.505147058824));
#161107=CARTESIAN_POINT('Ctrl Pts',(-14.0470054900687,5.44183891826343,
656.011029411765));
#161108=CARTESIAN_POINT('Ctrl Pts',(-13.4274493703259,6.68607533664807,
654.516911764706));
#161109=CARTESIAN_POINT('Ctrl Pts',(-12.8078932505832,7.93031175503273,
653.022794117647));
#161110=CARTESIAN_POINT('Ctrl Pts',(-11.9702584092036,9.03951954568884,
651.528676470588));
#161111=CARTESIAN_POINT('Ctrl Pts',(-11.132623567824,10.148727336345,650.03455882353));
#161112=CARTESIAN_POINT('Ctrl Pts',(-10.1054346546984,11.0851337583099,
648.540441176471));
#161113=CARTESIAN_POINT('Ctrl Pts',(-9.07824574157275,12.0215401802748,
647.046323529412));
#161114=CARTESIAN_POINT('Ctrl Pts',(-7.89648244316034,12.7532570359442,
645.552205882353));
#161115=CARTESIAN_POINT('Ctrl Pts',(-6.71471914474793,13.4849738916136,
644.058088235294));
#161116=CARTESIAN_POINT('Ctrl Pts',(-5.41862499280729,13.9870834410653,
642.563970588235));
#161117=CARTESIAN_POINT('Ctrl Pts',(-4.12253084086667,14.4891929905171,
641.069852941176));
#161118=CARTESIAN_POINT('Ctrl Pts',(-2.75624276724856,14.7445964952585,
639.575735294118));
#161119=CARTESIAN_POINT('Ctrl Pts',(-1.38995469363044,15.,638.081617647059));
#161120=CARTESIAN_POINT('Ctrl Pts',(-1.83697019872103E-15,15.,636.5875));
#161121=CARTESIAN_POINT('Ctrl Pts',(1.38995469363045,15.,635.093382352941));
#161122=CARTESIAN_POINT('Ctrl Pts',(2.75624276724855,14.7445964952585,633.599264705882));
#161123=CARTESIAN_POINT('Ctrl Pts',(4.12253084086666,14.4891929905171,632.105147058824));
#161124=CARTESIAN_POINT('Ctrl Pts',(5.4186249928073,13.9870834410653,630.611029411765));
#161125=CARTESIAN_POINT('Ctrl Pts',(6.71471914474792,13.4849738916136,629.116911764706));
#161126=CARTESIAN_POINT('Ctrl Pts',(7.89648244316034,12.7532570359442,627.622794117647));
#161127=CARTESIAN_POINT('Ctrl Pts',(9.07824574157275,12.0215401802748,626.128676470588));
#161128=CARTESIAN_POINT('Ctrl Pts',(10.1054346546984,11.0851337583099,624.634558823529));
#161129=CARTESIAN_POINT('Ctrl Pts',(11.132623567824,10.148727336345,623.140441176471));
#161130=CARTESIAN_POINT('Ctrl Pts',(11.9702584092036,9.03951954568885,621.646323529412));
#161131=CARTESIAN_POINT('Ctrl Pts',(12.8078932505832,7.93031175503273,620.152205882353));
#161132=CARTESIAN_POINT('Ctrl Pts',(13.4274493703259,6.68607533664807,618.658088235294));
#161133=CARTESIAN_POINT('Ctrl Pts',(14.0470054900687,5.44183891826343,617.163970588235));
#161134=CARTESIAN_POINT('Ctrl Pts',(14.4273846475923,4.10494485108125,615.669852941176));
#161135=CARTESIAN_POINT('Ctrl Pts',(14.8077638051159,2.76805078389905,614.175735294118));
#161136=CARTESIAN_POINT('Ctrl Pts',(14.9360126444255,1.38402539194953,612.681617647059));
#161137=CARTESIAN_POINT('Ctrl Pts',(15.0642614837351,2.76725994113625E-15,
611.1875));
#161138=CARTESIAN_POINT('Ctrl Pts',(14.9360126444255,-1.38402539194952,
609.693382352941));
#161139=CARTESIAN_POINT('Ctrl Pts',(14.8077638051159,-2.76805078389906,
608.199264705882));
#161140=CARTESIAN_POINT('Ctrl Pts',(14.4273846475923,-4.10494485108124,
606.705147058824));
#161141=CARTESIAN_POINT('Ctrl Pts',(14.0470054900687,-5.44183891826342,
605.211029411765));
#161142=CARTESIAN_POINT('Ctrl Pts',(13.4274493703259,-6.68607533664808,
603.716911764706));
#161143=CARTESIAN_POINT('Ctrl Pts',(12.8078932505832,-7.93031175503273,
602.222794117647));
#161144=CARTESIAN_POINT('Ctrl Pts',(11.9702584092036,-9.03951954568884,
600.728676470588));
#161145=CARTESIAN_POINT('Ctrl Pts',(11.132623567824,-10.148727336345,599.23455882353));
#161146=CARTESIAN_POINT('Ctrl Pts',(10.1054346546984,-11.0851337583099,
597.740441176471));
#161147=CARTESIAN_POINT('Ctrl Pts',(9.07824574157275,-12.0215401802748,
596.246323529412));
#161148=CARTESIAN_POINT('Ctrl Pts',(7.89648244316034,-12.7532570359442,
594.752205882353));
#161149=CARTESIAN_POINT('Ctrl Pts',(6.71471914474792,-13.4849738916136,
593.258088235294));
#161150=CARTESIAN_POINT('Ctrl Pts',(5.4186249928073,-13.9870834410653,591.763970588235));
#161151=CARTESIAN_POINT('Ctrl Pts',(4.12253084086667,-14.4891929905171,
590.269852941177));
#161152=CARTESIAN_POINT('Ctrl Pts',(2.75624276724855,-14.7445964952585,
588.775735294118));
#161153=CARTESIAN_POINT('Ctrl Pts',(1.38995469363045,-15.,587.281617647059));
#161154=CARTESIAN_POINT('Ctrl Pts',(0.,-15.,585.7875));
#161155=CARTESIAN_POINT('Ctrl Pts',(-1.38995469363045,-15.,584.293382352941));
#161156=CARTESIAN_POINT('Ctrl Pts',(-2.75624276724856,-14.7445964952585,
582.799264705882));
#161157=CARTESIAN_POINT('Ctrl Pts',(-4.12253084086666,-14.4891929905171,
581.305147058824));
#161158=CARTESIAN_POINT('Ctrl Pts',(-5.41862499280729,-13.9870834410653,
579.811029411765));
#161159=CARTESIAN_POINT('Ctrl Pts',(-6.71471914474793,-13.4849738916136,
578.316911764706));
#161160=CARTESIAN_POINT('Ctrl Pts',(-7.89648244316034,-12.7532570359442,
576.822794117647));
#161161=CARTESIAN_POINT('Ctrl Pts',(-9.07824574157275,-12.0215401802748,
575.328676470588));
#161162=CARTESIAN_POINT('Ctrl Pts',(-10.1054346546984,-11.0851337583099,
573.834558823529));
#161163=CARTESIAN_POINT('Ctrl Pts',(-11.132623567824,-10.148727336345,572.340441176471));
#161164=CARTESIAN_POINT('Ctrl Pts',(-11.9702584092036,-9.03951954568885,
570.846323529412));
#161165=CARTESIAN_POINT('Ctrl Pts',(-12.8078932505832,-7.93031175503273,
569.352205882353));
#161166=CARTESIAN_POINT('Ctrl Pts',(-13.4274493703259,-6.68607533664808,
567.858088235294));
#161167=CARTESIAN_POINT('Ctrl Pts',(-14.0470054900687,-5.44183891826343,
566.363970588235));
#161168=CARTESIAN_POINT('Ctrl Pts',(-14.4273846475923,-4.10494485108124,
564.869852941177));
#161169=CARTESIAN_POINT('Ctrl Pts',(-14.8077638051159,-2.76805078389906,
563.375735294118));
#161170=CARTESIAN_POINT('Ctrl Pts',(-14.9360126444255,-1.38402539194953,
561.881617647059));
#161171=CARTESIAN_POINT('Ctrl Pts',(-15.0642614837351,-9.22419980378748E-16,
560.3875));
#161172=CARTESIAN_POINT('Ctrl Pts',(-14.9360126444255,1.38402539194953,
558.893382352941));
#161173=CARTESIAN_POINT('Ctrl Pts',(-14.8077638051159,2.76805078389906,
557.399264705882));
#161174=CARTESIAN_POINT('Ctrl Pts',(-14.4273846475923,4.10494485108124,
555.905147058824));
#161175=CARTESIAN_POINT('Ctrl Pts',(-14.0470054900687,5.44183891826343,
554.411029411765));
#161176=CARTESIAN_POINT('Ctrl Pts',(-13.4274493703259,6.68607533664807,
552.916911764706));
#161177=CARTESIAN_POINT('Ctrl Pts',(-12.8078932505832,7.93031175503273,
551.422794117647));
#161178=CARTESIAN_POINT('Ctrl Pts',(-11.9702584092036,9.03951954568884,
549.928676470588));
#161179=CARTESIAN_POINT('Ctrl Pts',(-11.132623567824,10.148727336345,548.43455882353));
#161180=CARTESIAN_POINT('Ctrl Pts',(-10.1054346546984,11.0851337583099,
546.940441176471));
#161181=CARTESIAN_POINT('Ctrl Pts',(-9.07824574157275,12.0215401802748,
545.446323529412));
#161182=CARTESIAN_POINT('Ctrl Pts',(-7.89648244316034,12.7532570359442,
543.952205882353));
#161183=CARTESIAN_POINT('Ctrl Pts',(-6.71471914474793,13.4849738916136,
542.458088235294));
#161184=CARTESIAN_POINT('Ctrl Pts',(-5.41862499280729,13.9870834410653,
540.963970588235));
#161185=CARTESIAN_POINT('Ctrl Pts',(-4.12253084086667,14.4891929905171,
539.469852941177));
#161186=CARTESIAN_POINT('Ctrl Pts',(-2.75624276724856,14.7445964952585,
537.975735294118));
#161187=CARTESIAN_POINT('Ctrl Pts',(-1.38995469363044,15.,536.481617647059));
#161188=CARTESIAN_POINT('Ctrl Pts',(-1.83697019872103E-15,15.,534.9875));
#161189=CARTESIAN_POINT('Ctrl Pts',(1.38995469363045,15.,533.493382352941));
#161190=CARTESIAN_POINT('Ctrl Pts',(2.75624276724855,14.7445964952585,531.999264705882));
#161191=CARTESIAN_POINT('Ctrl Pts',(4.12253084086666,14.4891929905171,530.505147058824));
#161192=CARTESIAN_POINT('Ctrl Pts',(5.4186249928073,13.9870834410653,529.011029411765));
#161193=CARTESIAN_POINT('Ctrl Pts',(6.71471914474792,13.4849738916136,527.516911764706));
#161194=CARTESIAN_POINT('Ctrl Pts',(7.89648244316034,12.7532570359442,526.022794117647));
#161195=CARTESIAN_POINT('Ctrl Pts',(9.07824574157275,12.0215401802748,524.528676470588));
#161196=CARTESIAN_POINT('Ctrl Pts',(10.1054346546984,11.0851337583099,523.03455882353));
#161197=CARTESIAN_POINT('Ctrl Pts',(11.132623567824,10.148727336345,521.540441176471));
#161198=CARTESIAN_POINT('Ctrl Pts',(11.9702584092036,9.03951954568885,520.046323529412));
#161199=CARTESIAN_POINT('Ctrl Pts',(12.8078932505832,7.93031175503273,518.552205882353));
#161200=CARTESIAN_POINT('Ctrl Pts',(13.4274493703259,6.68607533664807,517.058088235294));
#161201=CARTESIAN_POINT('Ctrl Pts',(14.0470054900687,5.44183891826343,515.563970588235));
#161202=CARTESIAN_POINT('Ctrl Pts',(14.4273846475923,4.10494485108125,514.069852941176));
#161203=CARTESIAN_POINT('Ctrl Pts',(14.8077638051159,2.76805078389905,512.575735294118));
#161204=CARTESIAN_POINT('Ctrl Pts',(14.9360126444255,1.38402539194953,511.081617647059));
#161205=CARTESIAN_POINT('Ctrl Pts',(15.0642614837351,2.76725994113625E-15,
509.5875));
#161206=CARTESIAN_POINT('Ctrl Pts',(14.9360126444255,-1.38402539194952,
508.093382352941));
#161207=CARTESIAN_POINT('Ctrl Pts',(14.8077638051159,-2.76805078389906,
506.599264705882));
#161208=CARTESIAN_POINT('Ctrl Pts',(14.4273846475923,-4.10494485108124,
505.105147058824));
#161209=CARTESIAN_POINT('Ctrl Pts',(14.0470054900687,-5.44183891826342,
503.611029411765));
#161210=CARTESIAN_POINT('Ctrl Pts',(13.4274493703259,-6.68607533664808,
502.116911764706));
#161211=CARTESIAN_POINT('Ctrl Pts',(12.8078932505832,-7.93031175503273,
500.622794117647));
#161212=CARTESIAN_POINT('Ctrl Pts',(11.9702584092036,-9.03951954568884,
499.128676470588));
#161213=CARTESIAN_POINT('Ctrl Pts',(11.132623567824,-10.148727336345,497.63455882353));
#161214=CARTESIAN_POINT('Ctrl Pts',(10.1054346546984,-11.0851337583099,
496.140441176471));
#161215=CARTESIAN_POINT('Ctrl Pts',(9.07824574157275,-12.0215401802748,
494.646323529412));
#161216=CARTESIAN_POINT('Ctrl Pts',(7.89648244316034,-12.7532570359442,
493.152205882353));
#161217=CARTESIAN_POINT('Ctrl Pts',(6.71471914474792,-13.4849738916136,
491.658088235294));
#161218=CARTESIAN_POINT('Ctrl Pts',(5.4186249928073,-13.9870834410653,490.163970588235));
#161219=CARTESIAN_POINT('Ctrl Pts',(4.12253084086667,-14.4891929905171,
488.669852941177));
#161220=CARTESIAN_POINT('Ctrl Pts',(2.75624276724855,-14.7445964952585,
487.175735294118));
#161221=CARTESIAN_POINT('Ctrl Pts',(1.38995469363045,-15.,485.681617647059));
#161222=CARTESIAN_POINT('Ctrl Pts',(0.,-15.,484.1875));
#161223=CARTESIAN_POINT('Ctrl Pts',(-1.38995469363045,-15.,482.693382352941));
#161224=CARTESIAN_POINT('Ctrl Pts',(-2.75624276724856,-14.7445964952585,
481.199264705882));
#161225=CARTESIAN_POINT('Ctrl Pts',(-4.12253084086666,-14.4891929905171,
479.705147058824));
#161226=CARTESIAN_POINT('Ctrl Pts',(-5.41862499280729,-13.9870834410653,
478.211029411765));
#161227=CARTESIAN_POINT('Ctrl Pts',(-6.71471914474793,-13.4849738916136,
476.716911764706));
#161228=CARTESIAN_POINT('Ctrl Pts',(-7.89648244316034,-12.7532570359442,
475.222794117647));
#161229=CARTESIAN_POINT('Ctrl Pts',(-9.07824574157275,-12.0215401802748,
473.728676470588));
#161230=CARTESIAN_POINT('Ctrl Pts',(-10.1054346546984,-11.0851337583099,
472.234558823529));
#161231=CARTESIAN_POINT('Ctrl Pts',(-11.132623567824,-10.148727336345,470.740441176471));
#161232=CARTESIAN_POINT('Ctrl Pts',(-11.9702584092036,-9.03951954568885,
469.246323529412));
#161233=CARTESIAN_POINT('Ctrl Pts',(-12.8078932505832,-7.93031175503273,
467.752205882353));
#161234=CARTESIAN_POINT('Ctrl Pts',(-13.4274493703259,-6.68607533664808,
466.258088235294));
#161235=CARTESIAN_POINT('Ctrl Pts',(-14.0470054900687,-5.44183891826343,
464.763970588236));
#161236=CARTESIAN_POINT('Ctrl Pts',(-14.4273846475923,-4.10494485108124,
463.269852941177));
#161237=CARTESIAN_POINT('Ctrl Pts',(-14.8077638051159,-2.76805078389906,
461.775735294118));
#161238=CARTESIAN_POINT('Ctrl Pts',(-14.9360126444255,-1.38402539194953,
460.281617647059));
#161239=CARTESIAN_POINT('Ctrl Pts',(-15.0642614837351,-9.22419980378748E-16,
458.7875));
#161240=CARTESIAN_POINT('Ctrl Pts',(-14.9360126444255,1.38402539194953,
457.293382352941));
#161241=CARTESIAN_POINT('Ctrl Pts',(-14.8077638051159,2.76805078389906,
455.799264705882));
#161242=CARTESIAN_POINT('Ctrl Pts',(-14.4273846475923,4.10494485108124,
454.305147058824));
#161243=CARTESIAN_POINT('Ctrl Pts',(-14.0470054900687,5.44183891826343,
452.811029411765));
#161244=CARTESIAN_POINT('Ctrl Pts',(-13.4274493703259,6.68607533664807,
451.316911764706));
#161245=CARTESIAN_POINT('Ctrl Pts',(-12.8078932505832,7.93031175503273,
449.822794117647));
#161246=CARTESIAN_POINT('Ctrl Pts',(-11.9702584092036,9.03951954568884,
448.328676470588));
#161247=CARTESIAN_POINT('Ctrl Pts',(-11.132623567824,10.148727336345,446.83455882353));
#161248=CARTESIAN_POINT('Ctrl Pts',(-10.1054346546984,11.0851337583099,
445.340441176471));
#161249=CARTESIAN_POINT('Ctrl Pts',(-9.07824574157275,12.0215401802748,
443.846323529412));
#161250=CARTESIAN_POINT('Ctrl Pts',(-7.89648244316034,12.7532570359442,
442.352205882353));
#161251=CARTESIAN_POINT('Ctrl Pts',(-6.71471914474793,13.4849738916136,
440.858088235294));
#161252=CARTESIAN_POINT('Ctrl Pts',(-5.41862499280729,13.9870834410653,
439.363970588235));
#161253=CARTESIAN_POINT('Ctrl Pts',(-4.12253084086667,14.4891929905171,
437.869852941176));
#161254=CARTESIAN_POINT('Ctrl Pts',(-2.75624276724856,14.7445964952585,
436.375735294118));
#161255=CARTESIAN_POINT('Ctrl Pts',(-1.38995469363044,15.,434.881617647059));
#161256=CARTESIAN_POINT('Ctrl Pts',(-1.83697019872103E-15,15.,433.3875));
#161257=CARTESIAN_POINT('Ctrl Pts',(1.38995469363045,15.,431.893382352941));
#161258=CARTESIAN_POINT('Ctrl Pts',(2.75624276724855,14.7445964952585,430.399264705882));
#161259=CARTESIAN_POINT('Ctrl Pts',(4.12253084086666,14.4891929905171,428.905147058824));
#161260=CARTESIAN_POINT('Ctrl Pts',(5.4186249928073,13.9870834410653,427.411029411765));
#161261=CARTESIAN_POINT('Ctrl Pts',(6.71471914474792,13.4849738916136,425.916911764706));
#161262=CARTESIAN_POINT('Ctrl Pts',(7.89648244316034,12.7532570359442,424.422794117647));
#161263=CARTESIAN_POINT('Ctrl Pts',(9.07824574157275,12.0215401802748,422.928676470588));
#161264=CARTESIAN_POINT('Ctrl Pts',(10.1054346546984,11.0851337583099,421.43455882353));
#161265=CARTESIAN_POINT('Ctrl Pts',(11.132623567824,10.148727336345,419.940441176471));
#161266=CARTESIAN_POINT('Ctrl Pts',(11.9702584092036,9.03951954568885,418.446323529412));
#161267=CARTESIAN_POINT('Ctrl Pts',(12.8078932505832,7.93031175503273,416.952205882353));
#161268=CARTESIAN_POINT('Ctrl Pts',(13.4274493703259,6.68607533664807,415.458088235294));
#161269=CARTESIAN_POINT('Ctrl Pts',(14.0470054900687,5.44183891826343,413.963970588235));
#161270=CARTESIAN_POINT('Ctrl Pts',(14.4273846475923,4.10494485108125,412.469852941177));
#161271=CARTESIAN_POINT('Ctrl Pts',(14.8077638051159,2.76805078389905,410.975735294118));
#161272=CARTESIAN_POINT('Ctrl Pts',(14.9360126444255,1.38402539194953,409.481617647059));
#161273=CARTESIAN_POINT('Ctrl Pts',(15.0642614837351,2.76725994113625E-15,
407.9875));
#161274=CARTESIAN_POINT('Ctrl Pts',(14.9360126444255,-1.38402539194952,
406.493382352941));
#161275=CARTESIAN_POINT('Ctrl Pts',(14.8077638051159,-2.76805078389906,
404.999264705882));
#161276=CARTESIAN_POINT('Ctrl Pts',(14.4273846475923,-4.10494485108124,
403.505147058824));
#161277=CARTESIAN_POINT('Ctrl Pts',(14.0470054900687,-5.44183891826342,
402.011029411765));
#161278=CARTESIAN_POINT('Ctrl Pts',(13.4274493703259,-6.68607533664808,
400.516911764706));
#161279=CARTESIAN_POINT('Ctrl Pts',(12.8078932505832,-7.93031175503273,
399.022794117647));
#161280=CARTESIAN_POINT('Ctrl Pts',(11.9702584092036,-9.03951954568884,
397.528676470588));
#161281=CARTESIAN_POINT('Ctrl Pts',(11.132623567824,-10.148727336345,396.034558823529));
#161282=CARTESIAN_POINT('Ctrl Pts',(10.1054346546984,-11.0851337583099,
394.540441176471));
#161283=CARTESIAN_POINT('Ctrl Pts',(9.07824574157275,-12.0215401802748,
393.046323529412));
#161284=CARTESIAN_POINT('Ctrl Pts',(7.89648244316034,-12.7532570359442,
391.552205882353));
#161285=CARTESIAN_POINT('Ctrl Pts',(6.71471914474792,-13.4849738916136,
390.058088235294));
#161286=CARTESIAN_POINT('Ctrl Pts',(5.4186249928073,-13.9870834410653,388.563970588235));
#161287=CARTESIAN_POINT('Ctrl Pts',(4.12253084086667,-14.4891929905171,
387.069852941177));
#161288=CARTESIAN_POINT('Ctrl Pts',(2.75624276724855,-14.7445964952585,
385.575735294118));
#161289=CARTESIAN_POINT('Ctrl Pts',(1.38995469363045,-15.,384.081617647059));
#161290=CARTESIAN_POINT('Ctrl Pts',(0.,-15.,382.5875));
#161291=CARTESIAN_POINT('Ctrl Pts',(-1.38995469363045,-15.,381.093382352941));
#161292=CARTESIAN_POINT('Ctrl Pts',(-2.75624276724856,-14.7445964952585,
379.599264705882));
#161293=CARTESIAN_POINT('Ctrl Pts',(-4.12253084086666,-14.4891929905171,
378.105147058823));
#161294=CARTESIAN_POINT('Ctrl Pts',(-5.41862499280729,-13.9870834410653,
376.611029411765));
#161295=CARTESIAN_POINT('Ctrl Pts',(-6.71471914474793,-13.4849738916136,
375.116911764706));
#161296=CARTESIAN_POINT('Ctrl Pts',(-7.89648244316034,-12.7532570359442,
373.622794117647));
#161297=CARTESIAN_POINT('Ctrl Pts',(-9.07824574157275,-12.0215401802748,
372.128676470588));
#161298=CARTESIAN_POINT('Ctrl Pts',(-10.1054346546984,-11.0851337583099,
370.634558823529));
#161299=CARTESIAN_POINT('Ctrl Pts',(-11.132623567824,-10.148727336345,369.140441176471));
#161300=CARTESIAN_POINT('Ctrl Pts',(-11.9702584092036,-9.03951954568885,
367.646323529412));
#161301=CARTESIAN_POINT('Ctrl Pts',(-12.8078932505832,-7.93031175503273,
366.152205882353));
#161302=CARTESIAN_POINT('Ctrl Pts',(-13.4274493703259,-6.68607533664808,
364.658088235294));
#161303=CARTESIAN_POINT('Ctrl Pts',(-14.0470054900687,-5.44183891826343,
363.163970588235));
#161304=CARTESIAN_POINT('Ctrl Pts',(-14.4273846475923,-4.10494485108124,
361.669852941177));
#161305=CARTESIAN_POINT('Ctrl Pts',(-14.8077638051159,-2.76805078389906,
360.175735294118));
#161306=CARTESIAN_POINT('Ctrl Pts',(-14.9360126444255,-1.38402539194953,
358.681617647059));
#161307=CARTESIAN_POINT('Ctrl Pts',(-15.0642614837351,-9.22419980378748E-16,
357.1875));
#161308=CARTESIAN_POINT('Ctrl Pts',(-14.9360126444255,1.38402539194953,
355.693382352941));
#161309=CARTESIAN_POINT('Ctrl Pts',(-14.8077638051159,2.76805078389906,
354.199264705883));
#161310=CARTESIAN_POINT('Ctrl Pts',(-14.4273846475923,4.10494485108124,
352.705147058824));
#161311=CARTESIAN_POINT('Ctrl Pts',(-14.0470054900687,5.44183891826343,
351.211029411765));
#161312=CARTESIAN_POINT('Ctrl Pts',(-13.4274493703259,6.68607533664807,
349.716911764706));
#161313=CARTESIAN_POINT('Ctrl Pts',(-12.8078932505832,7.93031175503273,
348.222794117647));
#161314=CARTESIAN_POINT('Ctrl Pts',(-11.9702584092036,9.03951954568884,
346.728676470588));
#161315=CARTESIAN_POINT('Ctrl Pts',(-11.132623567824,10.148727336345,345.234558823529));
#161316=CARTESIAN_POINT('Ctrl Pts',(-10.1054346546984,11.0851337583099,
343.740441176471));
#161317=CARTESIAN_POINT('Ctrl Pts',(-9.07824574157275,12.0215401802748,
342.246323529412));
#161318=CARTESIAN_POINT('Ctrl Pts',(-7.89648244316034,12.7532570359442,
340.752205882353));
#161319=CARTESIAN_POINT('Ctrl Pts',(-6.71471914474793,13.4849738916136,
339.258088235294));
#161320=CARTESIAN_POINT('Ctrl Pts',(-5.41862499280729,13.9870834410653,
337.763970588235));
#161321=CARTESIAN_POINT('Ctrl Pts',(-4.12253084086667,14.4891929905171,
336.269852941177));
#161322=CARTESIAN_POINT('Ctrl Pts',(-2.75624276724856,14.7445964952585,
334.775735294118));
#161323=CARTESIAN_POINT('Ctrl Pts',(-1.38995469363044,15.,333.281617647059));
#161324=CARTESIAN_POINT('Ctrl Pts',(-1.83697019872103E-15,15.,331.7875));
#161325=CARTESIAN_POINT('Ctrl Pts',(1.38995469363045,15.,330.293382352941));
#161326=CARTESIAN_POINT('Ctrl Pts',(2.75624276724855,14.7445964952585,328.799264705882));
#161327=CARTESIAN_POINT('Ctrl Pts',(4.12253084086666,14.4891929905171,327.305147058824));
#161328=CARTESIAN_POINT('Ctrl Pts',(5.4186249928073,13.9870834410653,325.811029411765));
#161329=CARTESIAN_POINT('Ctrl Pts',(6.71471914474792,13.4849738916136,324.316911764706));
#161330=CARTESIAN_POINT('Ctrl Pts',(7.89648244316034,12.7532570359442,322.822794117647));
#161331=CARTESIAN_POINT('Ctrl Pts',(9.07824574157275,12.0215401802748,321.328676470588));
#161332=CARTESIAN_POINT('Ctrl Pts',(10.1054346546984,11.0851337583099,319.834558823529));
#161333=CARTESIAN_POINT('Ctrl Pts',(11.132623567824,10.148727336345,318.340441176471));
#161334=CARTESIAN_POINT('Ctrl Pts',(11.9702584092036,9.03951954568885,316.846323529412));
#161335=CARTESIAN_POINT('Ctrl Pts',(12.8078932505832,7.93031175503273,315.352205882353));
#161336=CARTESIAN_POINT('Ctrl Pts',(13.4274493703259,6.68607533664807,313.858088235294));
#161337=CARTESIAN_POINT('Ctrl Pts',(14.0470054900687,5.44183891826343,312.363970588235));
#161338=CARTESIAN_POINT('Ctrl Pts',(14.4273846475923,4.10494485108125,310.869852941176));
#161339=CARTESIAN_POINT('Ctrl Pts',(14.8077638051159,2.76805078389905,309.375735294118));
#161340=CARTESIAN_POINT('Ctrl Pts',(14.9360126444255,1.38402539194953,307.881617647059));
#161341=CARTESIAN_POINT('Ctrl Pts',(15.0642614837351,2.76725994113625E-15,
306.3875));
#161342=CARTESIAN_POINT('Ctrl Pts',(14.9360126444255,-1.38402539194952,
304.893382352941));
#161343=CARTESIAN_POINT('Ctrl Pts',(14.8077638051159,-2.76805078389906,
303.399264705882));
#161344=CARTESIAN_POINT('Ctrl Pts',(14.4273846475923,-4.10494485108124,
301.905147058824));
#161345=CARTESIAN_POINT('Ctrl Pts',(14.0470054900687,-5.44183891826342,
300.411029411765));
#161346=CARTESIAN_POINT('Ctrl Pts',(13.4274493703259,-6.68607533664808,
298.916911764706));
#161347=CARTESIAN_POINT('Ctrl Pts',(12.8078932505832,-7.93031175503273,
297.422794117647));
#161348=CARTESIAN_POINT('Ctrl Pts',(11.9702584092036,-9.03951954568884,
295.928676470588));
#161349=CARTESIAN_POINT('Ctrl Pts',(11.132623567824,-10.148727336345,294.43455882353));
#161350=CARTESIAN_POINT('Ctrl Pts',(10.1054346546984,-11.0851337583099,
292.940441176471));
#161351=CARTESIAN_POINT('Ctrl Pts',(9.07824574157275,-12.0215401802748,
291.446323529412));
#161352=CARTESIAN_POINT('Ctrl Pts',(7.89648244316034,-12.7532570359442,
289.952205882353));
#161353=CARTESIAN_POINT('Ctrl Pts',(6.71471914474792,-13.4849738916136,
288.458088235294));
#161354=CARTESIAN_POINT('Ctrl Pts',(5.4186249928073,-13.9870834410653,286.963970588235));
#161355=CARTESIAN_POINT('Ctrl Pts',(4.12253084086667,-14.4891929905171,
285.469852941177));
#161356=CARTESIAN_POINT('Ctrl Pts',(2.75624276724855,-14.7445964952585,
283.975735294118));
#161357=CARTESIAN_POINT('Ctrl Pts',(1.38995469363045,-15.,282.481617647059));
#161358=CARTESIAN_POINT('Ctrl Pts',(0.,-15.,280.9875));
#161359=CARTESIAN_POINT('Ctrl Pts',(-1.38995469363045,-15.,279.493382352941));
#161360=CARTESIAN_POINT('Ctrl Pts',(-2.75624276724856,-14.7445964952585,
277.999264705882));
#161361=CARTESIAN_POINT('Ctrl Pts',(-4.12253084086666,-14.4891929905171,
276.505147058824));
#161362=CARTESIAN_POINT('Ctrl Pts',(-5.41862499280729,-13.9870834410653,
275.011029411765));
#161363=CARTESIAN_POINT('Ctrl Pts',(-6.71471914474793,-13.4849738916136,
273.516911764706));
#161364=CARTESIAN_POINT('Ctrl Pts',(-7.89648244316034,-12.7532570359442,
272.022794117647));
#161365=CARTESIAN_POINT('Ctrl Pts',(-9.07824574157275,-12.0215401802748,
270.528676470588));
#161366=CARTESIAN_POINT('Ctrl Pts',(-10.1054346546984,-11.0851337583099,
269.034558823529));
#161367=CARTESIAN_POINT('Ctrl Pts',(-11.132623567824,-10.148727336345,267.540441176471));
#161368=CARTESIAN_POINT('Ctrl Pts',(-11.9702584092036,-9.03951954568885,
266.046323529412));
#161369=CARTESIAN_POINT('Ctrl Pts',(-12.8078932505832,-7.93031175503273,
264.552205882353));
#161370=CARTESIAN_POINT('Ctrl Pts',(-13.4274493703259,-6.68607533664808,
263.058088235294));
#161371=CARTESIAN_POINT('Ctrl Pts',(-14.0470054900687,-5.44183891826343,
261.563970588235));
#161372=CARTESIAN_POINT('Ctrl Pts',(-14.4273846475923,-4.10494485108124,
260.069852941176));
#161373=CARTESIAN_POINT('Ctrl Pts',(-14.8077638051159,-2.76805078389906,
258.575735294118));
#161374=CARTESIAN_POINT('Ctrl Pts',(-14.9360126444255,-1.38402539194953,
257.081617647059));
#161375=CARTESIAN_POINT('Ctrl Pts',(-15.0642614837351,-9.22419980378748E-16,
255.5875));
#161376=CARTESIAN_POINT('Ctrl Pts',(-14.9360126444255,1.38402539194953,
254.093382352941));
#161377=CARTESIAN_POINT('Ctrl Pts',(-14.8077638051159,2.76805078389906,
252.599264705882));
#161378=CARTESIAN_POINT('Ctrl Pts',(-14.4273846475923,4.10494485108124,
251.105147058823));
#161379=CARTESIAN_POINT('Ctrl Pts',(-14.0470054900687,5.44183891826343,
249.611029411765));
#161380=CARTESIAN_POINT('Ctrl Pts',(-13.4274493703259,6.68607533664807,
248.116911764706));
#161381=CARTESIAN_POINT('Ctrl Pts',(-12.8078932505832,7.93031175503273,
246.622794117647));
#161382=CARTESIAN_POINT('Ctrl Pts',(-11.9702584092036,9.03951954568884,
245.128676470588));
#161383=CARTESIAN_POINT('Ctrl Pts',(-11.132623567824,10.148727336345,243.634558823529));
#161384=CARTESIAN_POINT('Ctrl Pts',(-10.1054346546984,11.0851337583099,
242.140441176471));
#161385=CARTESIAN_POINT('Ctrl Pts',(-9.07824574157275,12.0215401802748,
240.646323529412));
#161386=CARTESIAN_POINT('Ctrl Pts',(-7.89648244316034,12.7532570359442,
239.152205882353));
#161387=CARTESIAN_POINT('Ctrl Pts',(-6.71471914474793,13.4849738916136,
237.658088235294));
#161388=CARTESIAN_POINT('Ctrl Pts',(-5.41862499280729,13.9870834410653,
236.163970588235));
#161389=CARTESIAN_POINT('Ctrl Pts',(-4.12253084086667,14.4891929905171,
234.669852941177));
#161390=CARTESIAN_POINT('Ctrl Pts',(-2.75624276724856,14.7445964952585,
233.175735294118));
#161391=CARTESIAN_POINT('Ctrl Pts',(-1.38995469363044,15.,231.681617647059));
#161392=CARTESIAN_POINT('Ctrl Pts',(-1.83697019872103E-15,15.,230.1875));
#161393=CARTESIAN_POINT('Ctrl Pts',(1.38995469363045,15.,228.693382352941));
#161394=CARTESIAN_POINT('Ctrl Pts',(2.75624276724855,14.7445964952585,227.199264705882));
#161395=CARTESIAN_POINT('Ctrl Pts',(4.12253084086666,14.4891929905171,225.705147058824));
#161396=CARTESIAN_POINT('Ctrl Pts',(5.4186249928073,13.9870834410653,224.211029411765));
#161397=CARTESIAN_POINT('Ctrl Pts',(6.71471914474792,13.4849738916136,222.716911764706));
#161398=CARTESIAN_POINT('Ctrl Pts',(7.89648244316034,12.7532570359442,221.222794117647));
#161399=CARTESIAN_POINT('Ctrl Pts',(9.07824574157275,12.0215401802748,219.728676470588));
#161400=CARTESIAN_POINT('Ctrl Pts',(10.1054346546984,11.0851337583099,218.234558823529));
#161401=CARTESIAN_POINT('Ctrl Pts',(11.132623567824,10.148727336345,216.740441176471));
#161402=CARTESIAN_POINT('Ctrl Pts',(11.9702584092036,9.03951954568885,215.246323529412));
#161403=CARTESIAN_POINT('Ctrl Pts',(12.8078932505832,7.93031175503273,213.752205882353));
#161404=CARTESIAN_POINT('Ctrl Pts',(13.4274493703259,6.68607533664807,212.258088235294));
#161405=CARTESIAN_POINT('Ctrl Pts',(14.0470054900687,5.44183891826343,210.763970588235));
#161406=CARTESIAN_POINT('Ctrl Pts',(14.4273846475923,4.10494485108125,209.269852941177));
#161407=CARTESIAN_POINT('Ctrl Pts',(14.8077638051159,2.76805078389905,207.775735294118));
#161408=CARTESIAN_POINT('Ctrl Pts',(14.9360126444255,1.38402539194953,206.281617647059));
#161409=CARTESIAN_POINT('Ctrl Pts',(15.0642614837351,2.76725994113625E-15,
204.7875));
#161410=CARTESIAN_POINT('Ctrl Pts',(14.9360126444255,-1.38402539194952,
203.293382352941));
#161411=CARTESIAN_POINT('Ctrl Pts',(14.8077638051159,-2.76805078389906,
201.799264705882));
#161412=CARTESIAN_POINT('Ctrl Pts',(14.4273846475923,-4.10494485108124,
200.305147058824));
#161413=CARTESIAN_POINT('Ctrl Pts',(14.0470054900687,-5.44183891826342,
198.811029411765));
#161414=CARTESIAN_POINT('Ctrl Pts',(13.4274493703259,-6.68607533664808,
197.316911764706));
#161415=CARTESIAN_POINT('Ctrl Pts',(12.8078932505832,-7.93031175503273,
195.822794117647));
#161416=CARTESIAN_POINT('Ctrl Pts',(11.9702584092036,-9.03951954568884,
194.328676470588));
#161417=CARTESIAN_POINT('Ctrl Pts',(11.132623567824,-10.148727336345,192.834558823529));
#161418=CARTESIAN_POINT('Ctrl Pts',(10.1054346546984,-11.0851337583099,
191.340441176471));
#161419=CARTESIAN_POINT('Ctrl Pts',(9.07824574157275,-12.0215401802748,
189.846323529412));
#161420=CARTESIAN_POINT('Ctrl Pts',(7.89648244316034,-12.7532570359442,
188.352205882353));
#161421=CARTESIAN_POINT('Ctrl Pts',(6.71471914474792,-13.4849738916136,
186.858088235294));
#161422=CARTESIAN_POINT('Ctrl Pts',(5.4186249928073,-13.9870834410653,185.363970588235));
#161423=CARTESIAN_POINT('Ctrl Pts',(4.12253084086667,-14.4891929905171,
183.869852941176));
#161424=CARTESIAN_POINT('Ctrl Pts',(2.75624276724855,-14.7445964952585,
182.375735294118));
#161425=CARTESIAN_POINT('Ctrl Pts',(1.38995469363045,-15.,180.881617647059));
#161426=CARTESIAN_POINT('Ctrl Pts',(0.,-15.,179.3875));
#161427=CARTESIAN_POINT('Ctrl Pts',(-1.38995469363045,-15.,177.893382352941));
#161428=CARTESIAN_POINT('Ctrl Pts',(-2.75624276724856,-14.7445964952585,
176.399264705882));
#161429=CARTESIAN_POINT('Ctrl Pts',(-4.12253084086666,-14.4891929905171,
174.905147058824));
#161430=CARTESIAN_POINT('Ctrl Pts',(-5.41862499280729,-13.9870834410653,
173.411029411765));
#161431=CARTESIAN_POINT('Ctrl Pts',(-6.71471914474793,-13.4849738916136,
171.916911764706));
#161432=CARTESIAN_POINT('Ctrl Pts',(-7.89648244316034,-12.7532570359442,
170.422794117647));
#161433=CARTESIAN_POINT('Ctrl Pts',(-9.07824574157275,-12.0215401802748,
168.928676470588));
#161434=CARTESIAN_POINT('Ctrl Pts',(-10.1054346546984,-11.0851337583099,
167.43455882353));
#161435=CARTESIAN_POINT('Ctrl Pts',(-11.132623567824,-10.148727336345,165.940441176471));
#161436=CARTESIAN_POINT('Ctrl Pts',(-11.9702584092036,-9.03951954568885,
164.446323529412));
#161437=CARTESIAN_POINT('Ctrl Pts',(-12.8078932505832,-7.93031175503273,
162.952205882353));
#161438=CARTESIAN_POINT('Ctrl Pts',(-13.4274493703259,-6.68607533664808,
161.458088235294));
#161439=CARTESIAN_POINT('Ctrl Pts',(-14.0470054900687,-5.44183891826343,
159.963970588235));
#161440=CARTESIAN_POINT('Ctrl Pts',(-14.4273846475923,-4.10494485108124,
158.469852941177));
#161441=CARTESIAN_POINT('Ctrl Pts',(-14.8077638051159,-2.76805078389906,
156.975735294118));
#161442=CARTESIAN_POINT('Ctrl Pts',(-14.9360126444255,-1.38402539194953,
155.481617647059));
#161443=CARTESIAN_POINT('Ctrl Pts',(-15.0642614837351,-9.22419980378748E-16,
153.9875));
#161444=CARTESIAN_POINT('Ctrl Pts',(-14.9360126444255,1.38402539194953,
152.493382352941));
#161445=CARTESIAN_POINT('Ctrl Pts',(-14.8077638051159,2.76805078389906,
150.999264705882));
#161446=CARTESIAN_POINT('Ctrl Pts',(-14.4273846475923,4.10494485108124,
149.505147058824));
#161447=CARTESIAN_POINT('Ctrl Pts',(-14.0470054900687,5.44183891826343,
148.011029411765));
#161448=CARTESIAN_POINT('Ctrl Pts',(-13.4274493703259,6.68607533664807,
146.516911764706));
#161449=CARTESIAN_POINT('Ctrl Pts',(-12.8078932505832,7.93031175503273,
145.022794117647));
#161450=CARTESIAN_POINT('Ctrl Pts',(-11.9702584092036,9.03951954568884,
143.528676470588));
#161451=CARTESIAN_POINT('Ctrl Pts',(-11.132623567824,10.148727336345,142.034558823529));
#161452=CARTESIAN_POINT('Ctrl Pts',(-10.1054346546984,11.0851337583099,
140.540441176471));
#161453=CARTESIAN_POINT('Ctrl Pts',(-9.07824574157275,12.0215401802748,
139.046323529412));
#161454=CARTESIAN_POINT('Ctrl Pts',(-7.89648244316034,12.7532570359442,
137.552205882353));
#161455=CARTESIAN_POINT('Ctrl Pts',(-6.71471914474793,13.4849738916136,
136.058088235294));
#161456=CARTESIAN_POINT('Ctrl Pts',(-5.41862499280729,13.9870834410653,
134.563970588235));
#161457=CARTESIAN_POINT('Ctrl Pts',(-4.12253084086667,14.4891929905171,
133.069852941176));
#161458=CARTESIAN_POINT('Ctrl Pts',(-2.75624276724856,14.7445964952585,
131.575735294118));
#161459=CARTESIAN_POINT('Ctrl Pts',(-1.38995469363044,15.,130.081617647059));
#161460=CARTESIAN_POINT('Ctrl Pts',(-1.83697019872103E-15,15.,128.5875));
#161461=CARTESIAN_POINT('Ctrl Pts',(1.38995469363045,15.,127.093382352941));
#161462=CARTESIAN_POINT('Ctrl Pts',(2.75624276724855,14.7445964952585,125.599264705882));
#161463=CARTESIAN_POINT('Ctrl Pts',(4.12253084086666,14.4891929905171,124.105147058824));
#161464=CARTESIAN_POINT('Ctrl Pts',(5.4186249928073,13.9870834410653,122.611029411765));
#161465=CARTESIAN_POINT('Ctrl Pts',(6.71471914474792,13.4849738916136,121.116911764706));
#161466=CARTESIAN_POINT('Ctrl Pts',(7.89648244316034,12.7532570359442,119.622794117647));
#161467=CARTESIAN_POINT('Ctrl Pts',(9.07824574157275,12.0215401802748,118.128676470588));
#161468=CARTESIAN_POINT('Ctrl Pts',(10.1054346546984,11.0851337583099,116.634558823529));
#161469=CARTESIAN_POINT('Ctrl Pts',(11.132623567824,10.148727336345,115.140441176471));
#161470=CARTESIAN_POINT('Ctrl Pts',(11.9702584092036,9.03951954568885,113.646323529412));
#161471=CARTESIAN_POINT('Ctrl Pts',(12.8078932505832,7.93031175503273,112.152205882353));
#161472=CARTESIAN_POINT('Ctrl Pts',(13.4274493703259,6.68607533664807,110.658088235294));
#161473=CARTESIAN_POINT('Ctrl Pts',(14.0470054900687,5.44183891826343,109.163970588235));
#161474=CARTESIAN_POINT('Ctrl Pts',(14.4273846475923,4.10494485108125,107.669852941177));
#161475=CARTESIAN_POINT('Ctrl Pts',(14.8077638051159,2.76805078389905,106.175735294118));
#161476=CARTESIAN_POINT('Ctrl Pts',(14.9360126444255,1.38402539194953,104.681617647059));
#161477=CARTESIAN_POINT('Ctrl Pts',(15.0642614837351,2.76725994113625E-15,
103.1875));
#161478=CARTESIAN_POINT('Ctrl Pts',(14.9360126444255,-1.38402539194952,
101.693382352941));
#161479=CARTESIAN_POINT('Ctrl Pts',(14.8077638051159,-2.76805078389906,
100.199264705882));
#161480=CARTESIAN_POINT('Ctrl Pts',(14.4273846475923,-4.10494485108124,
98.7051470588236));
#161481=CARTESIAN_POINT('Ctrl Pts',(14.0470054900687,-5.44183891826342,
97.2110294117647));
#161482=CARTESIAN_POINT('Ctrl Pts',(13.4274493703259,-6.68607533664808,
95.7169117647059));
#161483=CARTESIAN_POINT('Ctrl Pts',(12.8078932505832,-7.93031175503273,
94.222794117647));
#161484=CARTESIAN_POINT('Ctrl Pts',(11.9702584092036,-9.03951954568884,
92.7286764705884));
#161485=CARTESIAN_POINT('Ctrl Pts',(11.132623567824,-10.148727336345,91.2345588235295));
#161486=CARTESIAN_POINT('Ctrl Pts',(10.1054346546984,-11.0851337583099,
89.7404411764706));
#161487=CARTESIAN_POINT('Ctrl Pts',(9.07824574157275,-12.0215401802748,
88.2463235294117));
#161488=CARTESIAN_POINT('Ctrl Pts',(7.89648244316034,-12.7532570359442,
86.7522058823529));
#161489=CARTESIAN_POINT('Ctrl Pts',(6.71471914474792,-13.4849738916136,
85.2580882352942));
#161490=CARTESIAN_POINT('Ctrl Pts',(5.4186249928073,-13.9870834410653,83.7639705882354));
#161491=CARTESIAN_POINT('Ctrl Pts',(4.12253084086667,-14.4891929905171,
82.2698529411765));
#161492=CARTESIAN_POINT('Ctrl Pts',(2.75624276724855,-14.7445964952585,
80.7757352941176));
#161493=CARTESIAN_POINT('Ctrl Pts',(1.38995469363045,-15.,79.2816176470588));
#161494=CARTESIAN_POINT('Ctrl Pts',(0.,-15.,77.7875000000001));
#161495=CARTESIAN_POINT('Ctrl Pts',(-1.38995469363045,-15.,76.2933823529413));
#161496=CARTESIAN_POINT('Ctrl Pts',(-2.75624276724856,-14.7445964952585,
74.7992647058824));
#161497=CARTESIAN_POINT('Ctrl Pts',(-4.12253084086666,-14.4891929905171,
73.3051470588235));
#161498=CARTESIAN_POINT('Ctrl Pts',(-5.41862499280729,-13.9870834410653,
71.8110294117647));
#161499=CARTESIAN_POINT('Ctrl Pts',(-6.71471914474793,-13.4849738916136,
70.316911764706));
#161500=CARTESIAN_POINT('Ctrl Pts',(-7.89648244316034,-12.7532570359442,
68.8227941176471));
#161501=CARTESIAN_POINT('Ctrl Pts',(-9.07824574157275,-12.0215401802748,
67.3286764705883));
#161502=CARTESIAN_POINT('Ctrl Pts',(-10.1054346546984,-11.0851337583099,
65.8345588235294));
#161503=CARTESIAN_POINT('Ctrl Pts',(-11.132623567824,-10.148727336345,64.3404411764705));
#161504=CARTESIAN_POINT('Ctrl Pts',(-11.9702584092036,-9.03951954568885,
62.8463235294119));
#161505=CARTESIAN_POINT('Ctrl Pts',(-12.8078932505832,-7.93031175503273,
61.352205882353));
#161506=CARTESIAN_POINT('Ctrl Pts',(-13.4274493703259,-6.68607533664808,
59.8580882352941));
#161507=CARTESIAN_POINT('Ctrl Pts',(-14.0470054900687,-5.44183891826343,
58.3639705882353));
#161508=CARTESIAN_POINT('Ctrl Pts',(-14.4273846475923,-4.10494485108124,
56.8698529411764));
#161509=CARTESIAN_POINT('Ctrl Pts',(-14.8077638051159,-2.76805078389906,
55.3757352941178));
#161510=CARTESIAN_POINT('Ctrl Pts',(-14.9360126444255,-1.38402539194953,
53.8816176470589));
#161511=CARTESIAN_POINT('Ctrl Pts',(-15.0642614837351,-9.22419980378748E-16,
52.3875));
#161512=CARTESIAN_POINT('Ctrl Pts',(-14.9360126444255,1.38402539194953,
50.8933823529412));
#161513=CARTESIAN_POINT('Ctrl Pts',(-14.8077638051159,2.76805078389906,
49.3992647058823));
#161514=CARTESIAN_POINT('Ctrl Pts',(-14.4273846475923,4.10494485108124,
47.9051470588237));
#161515=CARTESIAN_POINT('Ctrl Pts',(-14.0470054900687,5.44183891826343,
46.4110294117648));
#161516=CARTESIAN_POINT('Ctrl Pts',(-13.4274493703259,6.68607533664807,
44.9169117647059));
#161517=CARTESIAN_POINT('Ctrl Pts',(-12.8078932505832,7.93031175503273,
43.422794117647));
#161518=CARTESIAN_POINT('Ctrl Pts',(-11.9702584092036,9.03951954568884,
41.9286764705882));
#161519=CARTESIAN_POINT('Ctrl Pts',(-11.132623567824,10.148727336345,40.4345588235295));
#161520=CARTESIAN_POINT('Ctrl Pts',(-10.1054346546984,11.0851337583099,
38.9404411764707));
#161521=CARTESIAN_POINT('Ctrl Pts',(-9.07824574157275,12.0215401802748,
37.4463235294118));
#161522=CARTESIAN_POINT('Ctrl Pts',(-7.89648244316034,12.7532570359442,
35.9522058823529));
#161523=CARTESIAN_POINT('Ctrl Pts',(-6.71471914474793,13.4849738916136,
34.4580882352941));
#161524=CARTESIAN_POINT('Ctrl Pts',(-5.41862499280729,13.9870834410653,
32.9639705882354));
#161525=CARTESIAN_POINT('Ctrl Pts',(-4.12253084086667,14.4891929905171,
31.4698529411765));
#161526=CARTESIAN_POINT('Ctrl Pts',(-2.75624276724856,14.7445964952585,
29.9757352941177));
#161527=CARTESIAN_POINT('Ctrl Pts',(-1.38995469363044,15.,28.4816176470588));
#161528=CARTESIAN_POINT('Ctrl Pts',(-1.83697019872103E-15,15.,26.9874999999999));
#161529=CARTESIAN_POINT('Ctrl Pts',(1.38995469363045,15.,25.4933823529413));
#161530=CARTESIAN_POINT('Ctrl Pts',(2.75624276724855,14.7445964952585,23.9992647058824));
#161531=CARTESIAN_POINT('Ctrl Pts',(4.12253084086666,14.4891929905171,22.5051470588236));
#161532=CARTESIAN_POINT('Ctrl Pts',(5.4186249928073,13.9870834410653,21.0110294117647));
#161533=CARTESIAN_POINT('Ctrl Pts',(6.71471914474792,13.4849738916136,19.5169117647058));
#161534=CARTESIAN_POINT('Ctrl Pts',(7.89648244316034,12.7532570359442,18.0227941176472));
#161535=CARTESIAN_POINT('Ctrl Pts',(9.07824574157275,12.0215401802748,16.5286764705883));
#161536=CARTESIAN_POINT('Ctrl Pts',(10.1054346546984,11.0851337583099,15.0345588235294));
#161537=CARTESIAN_POINT('Ctrl Pts',(11.132623567824,10.148727336345,13.5404411764706));
#161538=CARTESIAN_POINT('Ctrl Pts',(11.9702584092036,9.03951954568885,12.0463235294117));
#161539=CARTESIAN_POINT('Ctrl Pts',(12.8078932505832,7.93031175503273,10.5522058823531));
#161540=CARTESIAN_POINT('Ctrl Pts',(13.4274493703259,6.68607533664807,9.05808823529419));
#161541=CARTESIAN_POINT('Ctrl Pts',(14.0470054900687,5.44183891826343,7.56397058823533));
#161542=CARTESIAN_POINT('Ctrl Pts',(14.4273846475923,4.10494485108125,6.06985294117646));
#161543=CARTESIAN_POINT('Ctrl Pts',(14.8077638051159,2.76805078389905,4.57573529411759));
#161544=CARTESIAN_POINT('Ctrl Pts',(14.9360126444255,1.38402539194953,3.08161764705894));
#161545=CARTESIAN_POINT('Ctrl Pts',(15.0642614837351,2.76725994113625E-15,
1.58750000000007));
#161546=CARTESIAN_POINT('Ctrl Pts',(14.9360126444255,-1.38402539194952,
0.093382352941207));
#161547=CARTESIAN_POINT('Ctrl Pts',(14.8077638051159,-2.76805078389906,
-1.40073529411766));
#161548=CARTESIAN_POINT('Ctrl Pts',(14.4273846475923,-4.10494485108124,
-2.89485294117653));
#161549=CARTESIAN_POINT('Ctrl Pts',(14.0470054900687,-5.44183891826342,
-4.38897058823517));
#161550=CARTESIAN_POINT('Ctrl Pts',(13.4274493703259,-6.68607533664808,
-5.88308823529404));
#161551=CARTESIAN_POINT('Ctrl Pts',(12.8078932505832,-7.93031175503273,
-7.37720588235291));
#161552=CARTESIAN_POINT('Ctrl Pts',(11.9702584092036,-9.03951954568884,
-8.87132352941178));
#161553=CARTESIAN_POINT('Ctrl Pts',(11.132623567824,-10.148727336345,-10.3654411764706));
#161554=CARTESIAN_POINT('Ctrl Pts',(10.1054346546984,-11.0851337583099,
-11.8595588235293));
#161555=CARTESIAN_POINT('Ctrl Pts',(9.07824574157275,-12.0215401802748,
-13.3536764705882));
#161556=CARTESIAN_POINT('Ctrl Pts',(7.89648244316034,-12.7532570359442,
-14.847794117647));
#161557=CARTESIAN_POINT('Ctrl Pts',(6.71471914474792,-13.4849738916136,
-16.3419117647059));
#161558=CARTESIAN_POINT('Ctrl Pts',(5.4186249928073,-13.9870834410653,-17.8360294117648));
#161559=CARTESIAN_POINT('Ctrl Pts',(4.12253084086667,-14.4891929905171,
-19.3301470588234));
#161560=CARTESIAN_POINT('Ctrl Pts',(2.75624276724855,-14.7445964952585,
-20.8242647058823));
#161561=CARTESIAN_POINT('Ctrl Pts',(1.38995469363045,-15.,-22.3183823529411));
#161562=CARTESIAN_POINT('Ctrl Pts',(0.,-15.,-23.8125));
#161563=CARTESIAN_POINT('Ctrl Pts',(-1.38995469363045,-15.,-25.3066176470589));
#161564=CARTESIAN_POINT('Ctrl Pts',(-2.75624276724856,-14.7445964952585,
-26.8007352941175));
#161565=CARTESIAN_POINT('Ctrl Pts',(-4.12253084086666,-14.4891929905171,
-28.2948529411764));
#161566=CARTESIAN_POINT('Ctrl Pts',(-5.41862499280729,-13.9870834410653,
-29.7889705882353));
#161567=CARTESIAN_POINT('Ctrl Pts',(-6.71471914474793,-13.4849738916136,
-31.2830882352941));
#161568=CARTESIAN_POINT('Ctrl Pts',(-7.89648244316034,-12.7532570359442,
-32.777205882353));
#161569=CARTESIAN_POINT('Ctrl Pts',(-9.07824574157275,-12.0215401802748,
-34.2713235294116));
#161570=CARTESIAN_POINT('Ctrl Pts',(-10.1054346546984,-11.0851337583099,
-35.7654411764705));
#161571=CARTESIAN_POINT('Ctrl Pts',(-11.132623567824,-10.148727336345,-37.2595588235294));
#161572=CARTESIAN_POINT('Ctrl Pts',(-11.9702584092036,-9.03951954568885,
-38.7536764705882));
#161573=CARTESIAN_POINT('Ctrl Pts',(-12.8078932505832,-7.93031175503273,
-40.2477941176471));
#161574=CARTESIAN_POINT('Ctrl Pts',(-13.4274493703259,-6.68607533664808,
-41.7419117647058));
#161575=CARTESIAN_POINT('Ctrl Pts',(-14.0470054900687,-5.44183891826343,
-43.2360294117646));
#161576=CARTESIAN_POINT('Ctrl Pts',(-14.4273846475923,-4.10494485108124,
-44.7301470588235));
#161577=CARTESIAN_POINT('Ctrl Pts',(-14.8077638051159,-2.76805078389906,
-46.2242647058824));
#161578=CARTESIAN_POINT('Ctrl Pts',(-14.9360126444255,-1.38402539194953,
-47.7183823529412));
#161579=CARTESIAN_POINT('Ctrl Pts',(-15.0642614837351,-9.22419980378748E-16,
-49.2124999999999));
#161580=CARTESIAN_POINT('Ctrl Pts',(-14.9360126444255,1.38402539194953,
-50.7066176470587));
#161581=CARTESIAN_POINT('Ctrl Pts',(-14.8077638051159,2.76805078389906,
-52.2007352941176));
#161582=CARTESIAN_POINT('Ctrl Pts',(-14.4273846475923,4.10494485108124,
-53.6948529411765));
#161583=CARTESIAN_POINT('Ctrl Pts',(-14.0470054900687,5.44183891826343,
-55.1889705882354));
#161584=CARTESIAN_POINT('Ctrl Pts',(-13.4274493703259,6.68607533664807,
-56.683088235294));
#161585=CARTESIAN_POINT('Ctrl Pts',(-12.8078932505832,7.93031175503273,
-58.1772058823529));
#161586=CARTESIAN_POINT('Ctrl Pts',(-11.9702584092036,9.03951954568884,
-59.6713235294117));
#161587=CARTESIAN_POINT('Ctrl Pts',(-11.132623567824,10.148727336345,-61.1654411764706));
#161588=CARTESIAN_POINT('Ctrl Pts',(-10.1054346546984,11.0851337583099,
-62.6595588235295));
#161589=CARTESIAN_POINT('Ctrl Pts',(-9.07824574157275,12.0215401802748,
-64.1536764705881));
#161590=CARTESIAN_POINT('Ctrl Pts',(-7.89648244316034,12.7532570359442,
-65.647794117647));
#161591=CARTESIAN_POINT('Ctrl Pts',(-6.71471914474793,13.4849738916136,
-67.1419117647059));
#161592=CARTESIAN_POINT('Ctrl Pts',(-5.41862499280729,13.9870834410653,
-68.6360294117647));
#161593=CARTESIAN_POINT('Ctrl Pts',(-4.12253084086667,14.4891929905171,
-70.1301470588236));
#161594=CARTESIAN_POINT('Ctrl Pts',(-2.75624276724856,14.7445964952585,
-71.6242647058822));
#161595=CARTESIAN_POINT('Ctrl Pts',(-1.38995469363044,15.,-73.1183823529411));
#161596=CARTESIAN_POINT('Ctrl Pts',(-1.83697019872103E-15,15.,-74.6125));
#161597=CARTESIAN_POINT('Ctrl Pts',(1.38995469363045,15.,-76.1066176470589));
#161598=CARTESIAN_POINT('Ctrl Pts',(2.75624276724855,14.7445964952585,-77.6007352941177));
#161599=CARTESIAN_POINT('Ctrl Pts',(4.12253084086666,14.4891929905171,-79.0948529411764));
#161600=CARTESIAN_POINT('Ctrl Pts',(5.4186249928073,13.9870834410653,-80.5889705882352));
#161601=CARTESIAN_POINT('Ctrl Pts',(6.71471914474792,13.4849738916136,-82.0830882352941));
#161602=CARTESIAN_POINT('Ctrl Pts',(7.89648244316034,12.7532570359442,-83.577205882353));
#161603=CARTESIAN_POINT('Ctrl Pts',(9.07824574157275,12.0215401802748,-85.0713235294118));
#161604=CARTESIAN_POINT('Ctrl Pts',(10.1054346546984,11.0851337583099,-86.5654411764705));
#161605=CARTESIAN_POINT('Ctrl Pts',(11.132623567824,10.148727336345,-88.0595588235294));
#161606=CARTESIAN_POINT('Ctrl Pts',(11.9702584092036,9.03951954568885,-89.5536764705882));
#161607=CARTESIAN_POINT('Ctrl Pts',(12.8078932505832,7.93031175503273,-91.0477941176471));
#161608=CARTESIAN_POINT('Ctrl Pts',(13.4274493703259,6.68607533664807,-92.541911764706));
#161609=CARTESIAN_POINT('Ctrl Pts',(14.0470054900687,5.44183891826343,-94.0360294117646));
#161610=CARTESIAN_POINT('Ctrl Pts',(14.4273846475923,4.10494485108125,-95.5301470588235));
#161611=CARTESIAN_POINT('Ctrl Pts',(14.8077638051159,2.76805078389905,-97.0242647058824));
#161612=CARTESIAN_POINT('Ctrl Pts',(14.9360126444255,1.38402539194953,-98.5183823529412));
#161613=CARTESIAN_POINT('Ctrl Pts',(15.0642614837351,2.76725994113625E-15,
-100.0125));
#161614=CARTESIAN_POINT('Ctrl Pts',(14.9360126444255,-1.38402539194952,
-101.506617647059));
#161615=CARTESIAN_POINT('Ctrl Pts',(14.8077638051159,-2.76805078389906,
-103.000735294118));
#161616=CARTESIAN_POINT('Ctrl Pts',(14.4273846475923,-4.10494485108124,
-104.494852941176));
#161617=CARTESIAN_POINT('Ctrl Pts',(14.0470054900687,-5.44183891826342,
-105.988970588235));
#161618=CARTESIAN_POINT('Ctrl Pts',(13.4274493703259,-6.68607533664808,
-107.483088235294));
#161619=CARTESIAN_POINT('Ctrl Pts',(12.8078932505832,-7.93031175503273,
-108.977205882353));
#161620=CARTESIAN_POINT('Ctrl Pts',(11.9702584092036,-9.03951954568884,
-110.471323529412));
#161621=CARTESIAN_POINT('Ctrl Pts',(11.132623567824,-10.148727336345,-111.965441176471));
#161622=CARTESIAN_POINT('Ctrl Pts',(10.1054346546984,-11.0851337583099,
-113.459558823529));
#161623=CARTESIAN_POINT('Ctrl Pts',(9.07824574157275,-12.0215401802748,
-114.953676470588));
#161624=CARTESIAN_POINT('Ctrl Pts',(7.89648244316034,-12.7532570359442,
-116.447794117647));
#161625=CARTESIAN_POINT('Ctrl Pts',(6.71471914474792,-13.4849738916136,
-117.941911764706));
#161626=CARTESIAN_POINT('Ctrl Pts',(5.4186249928073,-13.9870834410653,-119.436029411765));
#161627=CARTESIAN_POINT('Ctrl Pts',(4.12253084086667,-14.4891929905171,
-120.930147058824));
#161628=CARTESIAN_POINT('Ctrl Pts',(2.75624276724855,-14.7445964952585,
-122.424264705882));
#161629=CARTESIAN_POINT('Ctrl Pts',(1.38995469363045,-15.,-123.918382352941));
#161630=CARTESIAN_POINT('Ctrl Pts',(0.,-15.,-125.4125));
#161631=CARTESIAN_POINT('Ctrl Pts',(-1.38995469363045,-15.,-126.906617647059));
#161632=CARTESIAN_POINT('Ctrl Pts',(-2.75624276724856,-14.7445964952585,
-128.400735294118));
#161633=CARTESIAN_POINT('Ctrl Pts',(-4.12253084086666,-14.4891929905171,
-129.894852941177));
#161634=CARTESIAN_POINT('Ctrl Pts',(-5.41862499280729,-13.9870834410653,
-131.388970588235));
#161635=CARTESIAN_POINT('Ctrl Pts',(-6.71471914474793,-13.4849738916136,
-132.883088235294));
#161636=CARTESIAN_POINT('Ctrl Pts',(-7.89648244316034,-12.7532570359442,
-134.377205882353));
#161637=CARTESIAN_POINT('Ctrl Pts',(-9.07824574157275,-12.0215401802748,
-135.871323529412));
#161638=CARTESIAN_POINT('Ctrl Pts',(-10.1054346546984,-11.0851337583099,
-137.365441176471));
#161639=CARTESIAN_POINT('Ctrl Pts',(-11.132623567824,-10.148727336345,-138.859558823529));
#161640=CARTESIAN_POINT('Ctrl Pts',(-11.9702584092036,-9.03951954568885,
-140.353676470588));
#161641=CARTESIAN_POINT('Ctrl Pts',(-12.8078932505832,-7.93031175503273,
-141.847794117647));
#161642=CARTESIAN_POINT('Ctrl Pts',(-13.4274493703259,-6.68607533664808,
-143.341911764706));
#161643=CARTESIAN_POINT('Ctrl Pts',(-14.0470054900687,-5.44183891826343,
-144.836029411765));
#161644=CARTESIAN_POINT('Ctrl Pts',(-14.4273846475923,-4.10494485108124,
-146.330147058823));
#161645=CARTESIAN_POINT('Ctrl Pts',(-14.8077638051159,-2.76805078389906,
-147.824264705882));
#161646=CARTESIAN_POINT('Ctrl Pts',(-14.9360126444255,-1.38402539194953,
-149.318382352941));
#161647=CARTESIAN_POINT('Ctrl Pts',(-15.0642614837351,-9.22419980378748E-16,
-150.8125));
#161648=CARTESIAN_POINT('Ctrl Pts',(-14.9360126444255,1.38402539194953,
-152.306617647059));
#161649=CARTESIAN_POINT('Ctrl Pts',(-14.8077638051159,2.76805078389906,
-153.800735294118));
#161650=CARTESIAN_POINT('Ctrl Pts',(-14.4273846475923,4.10494485108124,
-155.294852941176));
#161651=CARTESIAN_POINT('Ctrl Pts',(-14.0470054900687,5.44183891826343,
-156.788970588235));
#161652=CARTESIAN_POINT('Ctrl Pts',(-13.4274493703259,6.68607533664807,
-158.283088235294));
#161653=CARTESIAN_POINT('Ctrl Pts',(-12.8078932505832,7.93031175503273,
-159.777205882353));
#161654=CARTESIAN_POINT('Ctrl Pts',(-11.9702584092036,9.03951954568884,
-161.271323529412));
#161655=CARTESIAN_POINT('Ctrl Pts',(-11.132623567824,10.148727336345,-162.765441176471));
#161656=CARTESIAN_POINT('Ctrl Pts',(-10.1054346546984,11.0851337583099,
-164.259558823529));
#161657=CARTESIAN_POINT('Ctrl Pts',(-9.07824574157275,12.0215401802748,
-165.753676470588));
#161658=CARTESIAN_POINT('Ctrl Pts',(-7.89648244316034,12.7532570359442,
-167.247794117647));
#161659=CARTESIAN_POINT('Ctrl Pts',(-6.71471914474793,13.4849738916136,
-168.741911764706));
#161660=CARTESIAN_POINT('Ctrl Pts',(-5.41862499280729,13.9870834410653,
-170.236029411765));
#161661=CARTESIAN_POINT('Ctrl Pts',(-4.12253084086667,14.4891929905171,
-171.730147058823));
#161662=CARTESIAN_POINT('Ctrl Pts',(-2.75624276724856,14.7445964952585,
-173.224264705882));
#161663=CARTESIAN_POINT('Ctrl Pts',(-1.38995469363044,15.,-174.718382352941));
#161664=CARTESIAN_POINT('Ctrl Pts',(-1.83697019872103E-15,15.,-176.2125));
#161665=CARTESIAN_POINT('Ctrl Pts',(1.38995469363045,15.,-177.706617647059));
#161666=CARTESIAN_POINT('Ctrl Pts',(2.75624276724855,14.7445964952585,-179.200735294118));
#161667=CARTESIAN_POINT('Ctrl Pts',(4.12253084086666,14.4891929905171,-180.694852941176));
#161668=CARTESIAN_POINT('Ctrl Pts',(5.4186249928073,13.9870834410653,-182.188970588235));
#161669=CARTESIAN_POINT('Ctrl Pts',(6.71471914474792,13.4849738916136,-183.683088235294));
#161670=CARTESIAN_POINT('Ctrl Pts',(7.89648244316034,12.7532570359442,-185.177205882353));
#161671=CARTESIAN_POINT('Ctrl Pts',(9.07824574157275,12.0215401802748,-186.671323529412));
#161672=CARTESIAN_POINT('Ctrl Pts',(10.1054346546984,11.0851337583099,-188.165441176471));
#161673=CARTESIAN_POINT('Ctrl Pts',(11.132623567824,10.148727336345,-189.659558823529));
#161674=CARTESIAN_POINT('Ctrl Pts',(11.9702584092036,9.03951954568885,-191.153676470588));
#161675=CARTESIAN_POINT('Ctrl Pts',(12.8078932505832,7.93031175503273,-192.647794117647));
#161676=CARTESIAN_POINT('Ctrl Pts',(13.4274493703259,6.68607533664807,-194.141911764706));
#161677=CARTESIAN_POINT('Ctrl Pts',(14.0470054900687,5.44183891826343,-195.636029411765));
#161678=CARTESIAN_POINT('Ctrl Pts',(14.4273846475923,4.10494485108125,-197.130147058824));
#161679=CARTESIAN_POINT('Ctrl Pts',(14.8077638051159,2.76805078389905,-198.624264705882));
#161680=CARTESIAN_POINT('Ctrl Pts',(14.9360126444255,1.38402539194953,-200.118382352941));
#161681=CARTESIAN_POINT('Ctrl Pts',(15.0642614837351,2.76725994113625E-15,
-201.6125));
#161682=CARTESIAN_POINT('Ctrl Pts',(14.9360126444255,-1.38402539194952,
-203.106617647059));
#161683=CARTESIAN_POINT('Ctrl Pts',(14.8077638051159,-2.76805078389906,
-204.600735294118));
#161684=CARTESIAN_POINT('Ctrl Pts',(14.4273846475923,-4.10494485108124,
-206.094852941176));
#161685=CARTESIAN_POINT('Ctrl Pts',(14.0470054900687,-5.44183891826342,
-207.588970588235));
#161686=CARTESIAN_POINT('Ctrl Pts',(13.4274493703259,-6.68607533664808,
-209.083088235294));
#161687=CARTESIAN_POINT('Ctrl Pts',(12.8078932505832,-7.93031175503273,
-210.577205882353));
#161688=CARTESIAN_POINT('Ctrl Pts',(11.9702584092036,-9.03951954568884,
-212.071323529412));
#161689=CARTESIAN_POINT('Ctrl Pts',(11.132623567824,-10.148727336345,-213.56544117647));
#161690=CARTESIAN_POINT('Ctrl Pts',(10.1054346546984,-11.0851337583099,
-215.059558823529));
#161691=CARTESIAN_POINT('Ctrl Pts',(9.07824574157275,-12.0215401802748,
-216.553676470588));
#161692=CARTESIAN_POINT('Ctrl Pts',(7.89648244316034,-12.7532570359442,
-218.047794117647));
#161693=CARTESIAN_POINT('Ctrl Pts',(6.71471914474792,-13.4849738916136,
-219.541911764706));
#161694=CARTESIAN_POINT('Ctrl Pts',(5.4186249928073,-13.9870834410653,-221.036029411765));
#161695=CARTESIAN_POINT('Ctrl Pts',(4.12253084086667,-14.4891929905171,
-222.530147058823));
#161696=CARTESIAN_POINT('Ctrl Pts',(2.75624276724855,-14.7445964952585,
-224.024264705882));
#161697=CARTESIAN_POINT('Ctrl Pts',(1.38995469363045,-15.,-225.518382352941));
#161698=CARTESIAN_POINT('Ctrl Pts',(0.,-15.,-227.0125));
#161699=CARTESIAN_POINT('Ctrl Pts',(-1.38995469363045,-15.,-228.506617647059));
#161700=CARTESIAN_POINT('Ctrl Pts',(-2.75624276724856,-14.7445964952585,
-230.000735294118));
#161701=CARTESIAN_POINT('Ctrl Pts',(-4.12253084086666,-14.4891929905171,
-231.494852941176));
#161702=CARTESIAN_POINT('Ctrl Pts',(-5.41862499280729,-13.9870834410653,
-232.988970588235));
#161703=CARTESIAN_POINT('Ctrl Pts',(-6.71471914474793,-13.4849738916136,
-234.483088235294));
#161704=CARTESIAN_POINT('Ctrl Pts',(-7.89648244316034,-12.7532570359442,
-235.977205882353));
#161705=CARTESIAN_POINT('Ctrl Pts',(-9.07824574157275,-12.0215401802748,
-237.471323529412));
#161706=CARTESIAN_POINT('Ctrl Pts',(-10.1054346546984,-11.0851337583099,
-238.965441176471));
#161707=CARTESIAN_POINT('Ctrl Pts',(-11.132623567824,-10.148727336345,-240.459558823529));
#161708=CARTESIAN_POINT('Ctrl Pts',(-11.9702584092036,-9.03951954568885,
-241.953676470588));
#161709=CARTESIAN_POINT('Ctrl Pts',(-12.8078932505832,-7.93031175503273,
-243.447794117647));
#161710=CARTESIAN_POINT('Ctrl Pts',(-13.4274493703259,-6.68607533664808,
-244.941911764706));
#161711=CARTESIAN_POINT('Ctrl Pts',(-14.0470054900687,-5.44183891826343,
-246.436029411765));
#161712=CARTESIAN_POINT('Ctrl Pts',(-14.4273846475923,-4.10494485108124,
-247.930147058824));
#161713=CARTESIAN_POINT('Ctrl Pts',(-14.8077638051159,-2.76805078389906,
-249.424264705882));
#161714=CARTESIAN_POINT('Ctrl Pts',(-14.9360126444255,-1.38402539194953,
-250.918382352941));
#161715=CARTESIAN_POINT('Ctrl Pts',(-15.0642614837351,-9.22419980378748E-16,
-252.4125));
#161716=CARTESIAN_POINT('Ctrl Pts',(-14.9360126444255,1.38402539194953,
-253.906617647059));
#161717=CARTESIAN_POINT('Ctrl Pts',(-14.8077638051159,2.76805078389906,
-255.400735294118));
#161718=CARTESIAN_POINT('Ctrl Pts',(-14.4273846475923,4.10494485108124,
-256.894852941177));
#161719=CARTESIAN_POINT('Ctrl Pts',(-14.0470054900687,5.44183891826343,
-258.388970588235));
#161720=CARTESIAN_POINT('Ctrl Pts',(-13.4274493703259,6.68607533664807,
-259.883088235294));
#161721=CARTESIAN_POINT('Ctrl Pts',(-12.8078932505832,7.93031175503273,
-261.377205882353));
#161722=CARTESIAN_POINT('Ctrl Pts',(-11.9702584092036,9.03951954568884,
-262.871323529412));
#161723=CARTESIAN_POINT('Ctrl Pts',(-11.132623567824,10.148727336345,-264.365441176471));
#161724=CARTESIAN_POINT('Ctrl Pts',(-10.1054346546984,11.0851337583099,
-265.859558823529));
#161725=CARTESIAN_POINT('Ctrl Pts',(-9.07824574157275,12.0215401802748,
-267.353676470588));
#161726=CARTESIAN_POINT('Ctrl Pts',(-7.89648244316034,12.7532570359442,
-268.847794117647));
#161727=CARTESIAN_POINT('Ctrl Pts',(-6.71471914474793,13.4849738916136,
-270.341911764706));
#161728=CARTESIAN_POINT('Ctrl Pts',(-5.41862499280729,13.9870834410653,
-271.836029411765));
#161729=CARTESIAN_POINT('Ctrl Pts',(-4.12253084086667,14.4891929905171,
-273.330147058823));
#161730=CARTESIAN_POINT('Ctrl Pts',(-2.75624276724856,14.7445964952585,
-274.824264705882));
#161731=CARTESIAN_POINT('Ctrl Pts',(-1.38995469363044,15.,-276.318382352941));
#161732=CARTESIAN_POINT('Ctrl Pts',(-1.83697019872103E-15,15.,-277.8125));
#161733=CARTESIAN_POINT('Ctrl Pts',(1.38995469363045,15.,-279.306617647059));
#161734=CARTESIAN_POINT('Ctrl Pts',(2.75624276724855,14.7445964952585,-280.800735294118));
#161735=CARTESIAN_POINT('Ctrl Pts',(4.12253084086666,14.4891929905171,-282.294852941176));
#161736=CARTESIAN_POINT('Ctrl Pts',(5.4186249928073,13.9870834410653,-283.788970588235));
#161737=CARTESIAN_POINT('Ctrl Pts',(6.71471914474792,13.4849738916136,-285.283088235294));
#161738=CARTESIAN_POINT('Ctrl Pts',(7.89648244316034,12.7532570359442,-286.777205882353));
#161739=CARTESIAN_POINT('Ctrl Pts',(9.07824574157275,12.0215401802748,-288.271323529412));
#161740=CARTESIAN_POINT('Ctrl Pts',(10.1054346546984,11.0851337583099,-289.765441176471));
#161741=CARTESIAN_POINT('Ctrl Pts',(11.132623567824,10.148727336345,-291.259558823529));
#161742=CARTESIAN_POINT('Ctrl Pts',(11.9702584092036,9.03951954568885,-292.753676470588));
#161743=CARTESIAN_POINT('Ctrl Pts',(12.8078932505832,7.93031175503273,-294.247794117647));
#161744=CARTESIAN_POINT('Ctrl Pts',(13.4274493703259,6.68607533664807,-295.741911764706));
#161745=CARTESIAN_POINT('Ctrl Pts',(14.0470054900687,5.44183891826343,-297.236029411765));
#161746=CARTESIAN_POINT('Ctrl Pts',(14.4273846475923,4.10494485108125,-298.730147058823));
#161747=CARTESIAN_POINT('Ctrl Pts',(14.8077638051159,2.76805078389905,-300.224264705882));
#161748=CARTESIAN_POINT('Ctrl Pts',(14.9360126444255,1.38402539194953,-301.718382352941));
#161749=CARTESIAN_POINT('Ctrl Pts',(15.0642614837351,2.76725994113625E-15,
-303.2125));
#161750=CARTESIAN_POINT('Ctrl Pts',(14.9360126444255,-1.38402539194952,
-304.706617647059));
#161751=CARTESIAN_POINT('Ctrl Pts',(14.8077638051159,-2.76805078389906,
-306.200735294118));
#161752=CARTESIAN_POINT('Ctrl Pts',(14.4273846475923,-4.10494485108124,
-307.694852941176));
#161753=CARTESIAN_POINT('Ctrl Pts',(14.0470054900687,-5.44183891826342,
-309.188970588235));
#161754=CARTESIAN_POINT('Ctrl Pts',(13.4274493703259,-6.68607533664808,
-310.683088235294));
#161755=CARTESIAN_POINT('Ctrl Pts',(12.8078932505832,-7.93031175503273,
-312.177205882353));
#161756=CARTESIAN_POINT('Ctrl Pts',(11.9702584092036,-9.03951954568884,
-313.671323529412));
#161757=CARTESIAN_POINT('Ctrl Pts',(11.132623567824,-10.148727336345,-315.165441176471));
#161758=CARTESIAN_POINT('Ctrl Pts',(10.1054346546984,-11.0851337583099,
-316.659558823529));
#161759=CARTESIAN_POINT('Ctrl Pts',(9.07824574157275,-12.0215401802748,
-318.153676470588));
#161760=CARTESIAN_POINT('Ctrl Pts',(7.89648244316034,-12.7532570359442,
-319.647794117647));
#161761=CARTESIAN_POINT('Ctrl Pts',(6.71471914474792,-13.4849738916136,
-321.141911764706));
#161762=CARTESIAN_POINT('Ctrl Pts',(5.4186249928073,-13.9870834410653,-322.636029411765));
#161763=CARTESIAN_POINT('Ctrl Pts',(4.12253084086667,-14.4891929905171,
-324.130147058824));
#161764=CARTESIAN_POINT('Ctrl Pts',(2.75624276724855,-14.7445964952585,
-325.624264705882));
#161765=CARTESIAN_POINT('Ctrl Pts',(1.38995469363045,-15.,-327.118382352941));
#161766=CARTESIAN_POINT('Ctrl Pts',(0.,-15.,-328.6125));
#161767=CARTESIAN_POINT('Ctrl Pts',(-1.38995469363045,-15.,-330.106617647059));
#161768=CARTESIAN_POINT('Ctrl Pts',(-2.75624276724856,-14.7445964952585,
-331.600735294118));
#161769=CARTESIAN_POINT('Ctrl Pts',(-4.12253084086666,-14.4891929905171,
-333.094852941176));
#161770=CARTESIAN_POINT('Ctrl Pts',(-5.41862499280729,-13.9870834410653,
-334.588970588235));
#161771=CARTESIAN_POINT('Ctrl Pts',(-6.71471914474793,-13.4849738916136,
-336.083088235294));
#161772=CARTESIAN_POINT('Ctrl Pts',(-7.89648244316034,-12.7532570359442,
-337.577205882353));
#161773=CARTESIAN_POINT('Ctrl Pts',(-9.07824574157275,-12.0215401802748,
-339.071323529412));
#161774=CARTESIAN_POINT('Ctrl Pts',(-10.1054346546984,-11.0851337583099,
-340.56544117647));
#161775=CARTESIAN_POINT('Ctrl Pts',(-11.132623567824,-10.148727336345,-342.059558823529));
#161776=CARTESIAN_POINT('Ctrl Pts',(-11.9702584092036,-9.03951954568885,
-343.553676470588));
#161777=CARTESIAN_POINT('Ctrl Pts',(-12.8078932505832,-7.93031175503273,
-345.047794117647));
#161778=CARTESIAN_POINT('Ctrl Pts',(-13.4274493703259,-6.68607533664808,
-346.541911764706));
#161779=CARTESIAN_POINT('Ctrl Pts',(-14.0470054900687,-5.44183891826343,
-348.036029411765));
#161780=CARTESIAN_POINT('Ctrl Pts',(-14.4273846475923,-4.10494485108124,
-349.530147058823));
#161781=CARTESIAN_POINT('Ctrl Pts',(-14.8077638051159,-2.76805078389906,
-351.024264705883));
#161782=CARTESIAN_POINT('Ctrl Pts',(-14.9360126444255,-1.38402539194953,
-352.518382352941));
#161783=CARTESIAN_POINT('Ctrl Pts',(-15.0642614837351,-9.22419980378748E-16,
-354.0125));
#161784=CARTESIAN_POINT('Ctrl Pts',(-14.9360126444255,1.38402539194953,
-355.506617647059));
#161785=CARTESIAN_POINT('Ctrl Pts',(-14.8077638051159,2.76805078389906,
-357.000735294118));
#161786=CARTESIAN_POINT('Ctrl Pts',(-14.4273846475923,4.10494485108124,
-358.494852941176));
#161787=CARTESIAN_POINT('Ctrl Pts',(-14.0470054900687,5.44183891826343,
-359.988970588235));
#161788=CARTESIAN_POINT('Ctrl Pts',(-13.4274493703259,6.68607533664807,
-361.483088235294));
#161789=CARTESIAN_POINT('Ctrl Pts',(-12.8078932505832,7.93031175503273,
-362.977205882353));
#161790=CARTESIAN_POINT('Ctrl Pts',(-11.9702584092036,9.03951954568884,
-364.471323529412));
#161791=CARTESIAN_POINT('Ctrl Pts',(-11.132623567824,10.148727336345,-365.965441176471));
#161792=CARTESIAN_POINT('Ctrl Pts',(-10.1054346546984,11.0851337583099,
-367.459558823529));
#161793=CARTESIAN_POINT('Ctrl Pts',(-9.07824574157275,12.0215401802748,
-368.953676470588));
#161794=CARTESIAN_POINT('Ctrl Pts',(-7.89648244316034,12.7532570359442,
-370.447794117647));
#161795=CARTESIAN_POINT('Ctrl Pts',(-6.71471914474793,13.4849738916136,
-371.941911764706));
#161796=CARTESIAN_POINT('Ctrl Pts',(-5.41862499280729,13.9870834410653,
-373.436029411765));
#161797=CARTESIAN_POINT('Ctrl Pts',(-4.12253084086667,14.4891929905171,
-374.930147058824));
#161798=CARTESIAN_POINT('Ctrl Pts',(-2.75624276724856,14.7445964952585,
-376.424264705882));
#161799=CARTESIAN_POINT('Ctrl Pts',(-1.38995469363044,15.,-377.918382352941));
#161800=CARTESIAN_POINT('Ctrl Pts',(-1.83697019872103E-15,15.,-379.4125));
#161801=CARTESIAN_POINT('Ctrl Pts',(1.38995469363045,15.,-380.906617647059));
#161802=CARTESIAN_POINT('Ctrl Pts',(2.75624276724855,14.7445964952585,-382.400735294118));
#161803=CARTESIAN_POINT('Ctrl Pts',(4.12253084086666,14.4891929905171,-383.894852941177));
#161804=CARTESIAN_POINT('Ctrl Pts',(5.4186249928073,13.9870834410653,-385.388970588235));
#161805=CARTESIAN_POINT('Ctrl Pts',(6.71471914474792,13.4849738916136,-386.883088235294));
#161806=CARTESIAN_POINT('Ctrl Pts',(7.89648244316034,12.7532570359442,-388.377205882353));
#161807=CARTESIAN_POINT('Ctrl Pts',(9.07824574157275,12.0215401802748,-389.871323529412));
#161808=CARTESIAN_POINT('Ctrl Pts',(10.1054346546984,11.0851337583099,-391.365441176471));
#161809=CARTESIAN_POINT('Ctrl Pts',(11.132623567824,10.148727336345,-392.859558823529));
#161810=CARTESIAN_POINT('Ctrl Pts',(11.9702584092036,9.03951954568885,-394.353676470588));
#161811=CARTESIAN_POINT('Ctrl Pts',(12.8078932505832,7.93031175503273,-395.847794117647));
#161812=CARTESIAN_POINT('Ctrl Pts',(13.4274493703259,6.68607533664807,-397.341911764706));
#161813=CARTESIAN_POINT('Ctrl Pts',(14.0470054900687,5.44183891826343,-398.836029411765));
#161814=CARTESIAN_POINT('Ctrl Pts',(14.4273846475923,4.10494485108125,-400.330147058823));
#161815=CARTESIAN_POINT('Ctrl Pts',(14.8077638051159,2.76805078389905,-401.824264705882));
#161816=CARTESIAN_POINT('Ctrl Pts',(14.9360126444255,1.38402539194953,-403.318382352941));
#161817=CARTESIAN_POINT('Ctrl Pts',(15.0642614837351,2.76725994113625E-15,
-404.8125));
#161818=CARTESIAN_POINT('Ctrl Pts',(14.9360126444255,-1.38402539194952,
-406.306617647059));
#161819=CARTESIAN_POINT('Ctrl Pts',(14.8077638051159,-2.76805078389906,
-407.800735294118));
#161820=CARTESIAN_POINT('Ctrl Pts',(14.4273846475923,-4.10494485108124,
-409.294852941176));
#161821=CARTESIAN_POINT('Ctrl Pts',(14.0470054900687,-5.44183891826342,
-410.788970588235));
#161822=CARTESIAN_POINT('Ctrl Pts',(13.4274493703259,-6.68607533664808,
-412.283088235294));
#161823=CARTESIAN_POINT('Ctrl Pts',(12.8078932505832,-7.93031175503273,
-413.777205882353));
#161824=CARTESIAN_POINT('Ctrl Pts',(11.9702584092036,-9.03951954568884,
-415.271323529412));
#161825=CARTESIAN_POINT('Ctrl Pts',(11.132623567824,-10.148727336345,-416.765441176471));
#161826=CARTESIAN_POINT('Ctrl Pts',(10.1054346546984,-11.0851337583099,
-418.259558823529));
#161827=CARTESIAN_POINT('Ctrl Pts',(9.07824574157275,-12.0215401802748,
-419.753676470588));
#161828=CARTESIAN_POINT('Ctrl Pts',(7.89648244316034,-12.7532570359442,
-421.247794117647));
#161829=CARTESIAN_POINT('Ctrl Pts',(6.71471914474792,-13.4849738916136,
-422.741911764706));
#161830=CARTESIAN_POINT('Ctrl Pts',(5.4186249928073,-13.9870834410653,-424.236029411765));
#161831=CARTESIAN_POINT('Ctrl Pts',(4.12253084086667,-14.4891929905171,
-425.730147058824));
#161832=CARTESIAN_POINT('Ctrl Pts',(2.75624276724855,-14.7445964952585,
-427.224264705882));
#161833=CARTESIAN_POINT('Ctrl Pts',(1.38995469363045,-15.,-428.718382352941));
#161834=CARTESIAN_POINT('Ctrl Pts',(0.,-15.,-430.2125));
#161835=CARTESIAN_POINT('Ctrl Pts',(-1.38995469363045,-15.,-431.706617647059));
#161836=CARTESIAN_POINT('Ctrl Pts',(-2.75624276724856,-14.7445964952585,
-433.200735294118));
#161837=CARTESIAN_POINT('Ctrl Pts',(-4.12253084086666,-14.4891929905171,
-434.694852941176));
#161838=CARTESIAN_POINT('Ctrl Pts',(-5.41862499280729,-13.9870834410653,
-436.188970588235));
#161839=CARTESIAN_POINT('Ctrl Pts',(-6.71471914474793,-13.4849738916136,
-437.683088235294));
#161840=CARTESIAN_POINT('Ctrl Pts',(-7.89648244316034,-12.7532570359442,
-439.177205882353));
#161841=CARTESIAN_POINT('Ctrl Pts',(-9.07824574157275,-12.0215401802748,
-440.671323529412));
#161842=CARTESIAN_POINT('Ctrl Pts',(-10.1054346546984,-11.0851337583099,
-442.165441176471));
#161843=CARTESIAN_POINT('Ctrl Pts',(-11.132623567824,-10.148727336345,-443.65955882353));
#161844=CARTESIAN_POINT('Ctrl Pts',(-11.9702584092036,-9.03951954568885,
-445.153676470588));
#161845=CARTESIAN_POINT('Ctrl Pts',(-12.8078932505832,-7.93031175503273,
-446.647794117647));
#161846=CARTESIAN_POINT('Ctrl Pts',(-13.4274493703259,-6.68607533664808,
-448.141911764706));
#161847=CARTESIAN_POINT('Ctrl Pts',(-14.0470054900687,-5.44183891826343,
-449.636029411765));
#161848=CARTESIAN_POINT('Ctrl Pts',(-14.4273846475923,-4.10494485108124,
-451.130147058824));
#161849=CARTESIAN_POINT('Ctrl Pts',(-14.8077638051159,-2.76805078389906,
-452.624264705882));
#161850=CARTESIAN_POINT('Ctrl Pts',(-14.9360126444255,-1.38402539194953,
-454.118382352941));
#161851=CARTESIAN_POINT('Ctrl Pts',(-15.0642614837351,-9.22419980378748E-16,
-455.6125));
#161852=CARTESIAN_POINT('Ctrl Pts',(-14.9360126444255,1.38402539194953,
-457.106617647059));
#161853=CARTESIAN_POINT('Ctrl Pts',(-14.8077638051159,2.76805078389906,
-458.600735294118));
#161854=CARTESIAN_POINT('Ctrl Pts',(-14.4273846475923,4.10494485108124,
-460.094852941176));
#161855=CARTESIAN_POINT('Ctrl Pts',(-14.0470054900687,5.44183891826343,
-461.588970588235));
#161856=CARTESIAN_POINT('Ctrl Pts',(-13.4274493703259,6.68607533664807,
-463.083088235294));
#161857=CARTESIAN_POINT('Ctrl Pts',(-12.8078932505832,7.93031175503273,
-464.577205882353));
#161858=CARTESIAN_POINT('Ctrl Pts',(-11.9702584092036,9.03951954568884,
-466.071323529412));
#161859=CARTESIAN_POINT('Ctrl Pts',(-11.132623567824,10.148727336345,-467.565441176471));
#161860=CARTESIAN_POINT('Ctrl Pts',(-10.1054346546984,11.0851337583099,
-469.059558823529));
#161861=CARTESIAN_POINT('Ctrl Pts',(-9.07824574157275,12.0215401802748,
-470.553676470588));
#161862=CARTESIAN_POINT('Ctrl Pts',(-7.89648244316034,12.7532570359442,
-472.047794117647));
#161863=CARTESIAN_POINT('Ctrl Pts',(-6.71471914474793,13.4849738916136,
-473.541911764706));
#161864=CARTESIAN_POINT('Ctrl Pts',(-5.41862499280729,13.9870834410653,
-475.036029411765));
#161865=CARTESIAN_POINT('Ctrl Pts',(-4.12253084086667,14.4891929905171,
-476.530147058824));
#161866=CARTESIAN_POINT('Ctrl Pts',(-2.75624276724856,14.7445964952585,
-478.024264705882));
#161867=CARTESIAN_POINT('Ctrl Pts',(-1.38995469363044,15.,-479.518382352941));
#161868=CARTESIAN_POINT('Ctrl Pts',(-1.83697019872103E-15,15.,-481.0125));
#161869=CARTESIAN_POINT('Ctrl Pts',(1.38995469363045,15.,-482.506617647059));
#161870=CARTESIAN_POINT('Ctrl Pts',(2.75624276724855,14.7445964952585,-484.000735294118));
#161871=CARTESIAN_POINT('Ctrl Pts',(4.12253084086666,14.4891929905171,-485.494852941177));
#161872=CARTESIAN_POINT('Ctrl Pts',(5.4186249928073,13.9870834410653,-486.988970588235));
#161873=CARTESIAN_POINT('Ctrl Pts',(6.71471914474792,13.4849738916136,-488.483088235294));
#161874=CARTESIAN_POINT('Ctrl Pts',(7.89648244316034,12.7532570359442,-489.977205882353));
#161875=CARTESIAN_POINT('Ctrl Pts',(9.07824574157275,12.0215401802748,-491.471323529412));
#161876=CARTESIAN_POINT('Ctrl Pts',(10.1054346546984,11.0851337583099,-492.965441176471));
#161877=CARTESIAN_POINT('Ctrl Pts',(11.132623567824,10.148727336345,-494.45955882353));
#161878=CARTESIAN_POINT('Ctrl Pts',(11.9702584092036,9.03951954568885,-495.953676470588));
#161879=CARTESIAN_POINT('Ctrl Pts',(12.8078932505832,7.93031175503273,-497.447794117647));
#161880=CARTESIAN_POINT('Ctrl Pts',(13.4274493703259,6.68607533664807,-498.941911764706));
#161881=CARTESIAN_POINT('Ctrl Pts',(14.0470054900687,5.44183891826343,-500.436029411765));
#161882=CARTESIAN_POINT('Ctrl Pts',(14.4273846475923,4.10494485108125,-501.930147058824));
#161883=CARTESIAN_POINT('Ctrl Pts',(14.8077638051159,2.76805078389905,-503.424264705883));
#161884=CARTESIAN_POINT('Ctrl Pts',(14.9360126444255,1.38402539194953,-504.918382352941));
#161885=CARTESIAN_POINT('Ctrl Pts',(15.0642614837351,2.76725994113625E-15,
-506.4125));
#161886=CARTESIAN_POINT('Ctrl Pts',(14.9360126444255,-1.38402539194952,
-507.906617647059));
#161887=CARTESIAN_POINT('Ctrl Pts',(14.8077638051159,-2.76805078389906,
-509.400735294117));
#161888=CARTESIAN_POINT('Ctrl Pts',(14.4273846475923,-4.10494485108124,
-510.894852941176));
#161889=CARTESIAN_POINT('Ctrl Pts',(14.0470054900687,-5.44183891826342,
-512.388970588235));
#161890=CARTESIAN_POINT('Ctrl Pts',(13.4274493703259,-6.68607533664808,
-513.883088235294));
#161891=CARTESIAN_POINT('Ctrl Pts',(12.8078932505832,-7.93031175503273,
-515.377205882353));
#161892=CARTESIAN_POINT('Ctrl Pts',(11.9702584092036,-9.03951954568884,
-516.871323529412));
#161893=CARTESIAN_POINT('Ctrl Pts',(11.132623567824,-10.148727336345,-518.365441176471));
#161894=CARTESIAN_POINT('Ctrl Pts',(10.1054346546984,-11.0851337583099,
-519.85955882353));
#161895=CARTESIAN_POINT('Ctrl Pts',(9.07824574157275,-12.0215401802748,
-521.353676470588));
#161896=CARTESIAN_POINT('Ctrl Pts',(7.89648244316034,-12.7532570359442,
-522.847794117647));
#161897=CARTESIAN_POINT('Ctrl Pts',(6.71471914474792,-13.4849738916136,
-524.341911764706));
#161898=CARTESIAN_POINT('Ctrl Pts',(5.4186249928073,-13.9870834410653,-525.836029411765));
#161899=CARTESIAN_POINT('Ctrl Pts',(4.12253084086667,-14.4891929905171,
-527.330147058823));
#161900=CARTESIAN_POINT('Ctrl Pts',(2.75624276724855,-14.7445964952585,
-528.824264705882));
#161901=CARTESIAN_POINT('Ctrl Pts',(1.38995469363045,-15.,-530.318382352941));
#161902=CARTESIAN_POINT('Ctrl Pts',(0.,-15.,-531.8125));
#161903=CARTESIAN_POINT('Ctrl Pts',(-1.38995469363045,-15.,-533.306617647059));
#161904=CARTESIAN_POINT('Ctrl Pts',(-2.75624276724856,-14.7445964952585,
-534.800735294118));
#161905=CARTESIAN_POINT('Ctrl Pts',(-4.12253084086666,-14.4891929905171,
-536.294852941177));
#161906=CARTESIAN_POINT('Ctrl Pts',(-5.41862499280729,-13.9870834410653,
-537.788970588235));
#161907=CARTESIAN_POINT('Ctrl Pts',(-6.71471914474793,-13.4849738916136,
-539.283088235294));
#161908=CARTESIAN_POINT('Ctrl Pts',(-7.89648244316034,-12.7532570359442,
-540.777205882353));
#161909=CARTESIAN_POINT('Ctrl Pts',(-9.07824574157275,-12.0215401802748,
-542.271323529412));
#161910=CARTESIAN_POINT('Ctrl Pts',(-10.1054346546984,-11.0851337583099,
-543.765441176471));
#161911=CARTESIAN_POINT('Ctrl Pts',(-11.132623567824,-10.148727336345,-545.259558823529));
#161912=CARTESIAN_POINT('Ctrl Pts',(-11.9702584092036,-9.03951954568885,
-546.753676470588));
#161913=CARTESIAN_POINT('Ctrl Pts',(-12.8078932505832,-7.93031175503273,
-548.247794117647));
#161914=CARTESIAN_POINT('Ctrl Pts',(-13.4274493703259,-6.68607533664808,
-549.741911764706));
#161915=CARTESIAN_POINT('Ctrl Pts',(-14.0470054900687,-5.44183891826343,
-551.236029411765));
#161916=CARTESIAN_POINT('Ctrl Pts',(-14.4273846475923,-4.10494485108124,
-552.730147058823));
#161917=CARTESIAN_POINT('Ctrl Pts',(-14.8077638051159,-2.76805078389906,
-554.224264705882));
#161918=CARTESIAN_POINT('Ctrl Pts',(-14.9360126444255,-1.38402539194953,
-555.718382352941));
#161919=CARTESIAN_POINT('Ctrl Pts',(-15.0642614837351,-9.22419980378748E-16,
-557.2125));
#161920=CARTESIAN_POINT('Ctrl Pts',(-14.9360126444255,1.38402539194953,
-558.706617647059));
#161921=CARTESIAN_POINT('Ctrl Pts',(-14.8077638051159,2.76805078389906,
-560.200735294118));
#161922=CARTESIAN_POINT('Ctrl Pts',(-14.4273846475923,4.10494485108124,
-561.694852941176));
#161923=CARTESIAN_POINT('Ctrl Pts',(-14.0470054900687,5.44183891826343,
-563.188970588235));
#161924=CARTESIAN_POINT('Ctrl Pts',(-13.4274493703259,6.68607533664807,
-564.683088235294));
#161925=CARTESIAN_POINT('Ctrl Pts',(-12.8078932505832,7.93031175503273,
-566.177205882353));
#161926=CARTESIAN_POINT('Ctrl Pts',(-11.9702584092036,9.03951954568884,
-567.671323529412));
#161927=CARTESIAN_POINT('Ctrl Pts',(-11.132623567824,10.148727336345,-569.16544117647));
#161928=CARTESIAN_POINT('Ctrl Pts',(-10.1054346546984,11.0851337583099,
-570.659558823529));
#161929=CARTESIAN_POINT('Ctrl Pts',(-9.07824574157275,12.0215401802748,
-572.153676470588));
#161930=CARTESIAN_POINT('Ctrl Pts',(-7.89648244316034,12.7532570359442,
-573.647794117647));
#161931=CARTESIAN_POINT('Ctrl Pts',(-6.71471914474793,13.4849738916136,
-575.141911764706));
#161932=CARTESIAN_POINT('Ctrl Pts',(-5.41862499280729,13.9870834410653,
-576.636029411765));
#161933=CARTESIAN_POINT('Ctrl Pts',(-4.12253084086667,14.4891929905171,
-578.130147058824));
#161934=CARTESIAN_POINT('Ctrl Pts',(-2.75624276724856,14.7445964952585,
-579.624264705882));
#161935=CARTESIAN_POINT('Ctrl Pts',(-1.38995469363044,15.,-581.118382352941));
#161936=CARTESIAN_POINT('Ctrl Pts',(-1.83697019872103E-15,15.,-582.6125));
#161937=CARTESIAN_POINT('Ctrl Pts',(1.38995469363045,15.,-584.106617647059));
#161938=CARTESIAN_POINT('Ctrl Pts',(2.75624276724855,14.7445964952585,-585.600735294117));
#161939=CARTESIAN_POINT('Ctrl Pts',(4.12253084086666,14.4891929905171,-587.094852941176));
#161940=CARTESIAN_POINT('Ctrl Pts',(5.4186249928073,13.9870834410653,-588.588970588235));
#161941=CARTESIAN_POINT('Ctrl Pts',(6.71471914474792,13.4849738916136,-590.083088235294));
#161942=CARTESIAN_POINT('Ctrl Pts',(7.89648244316034,12.7532570359442,-591.577205882353));
#161943=CARTESIAN_POINT('Ctrl Pts',(9.07824574157275,12.0215401802748,-593.071323529412));
#161944=CARTESIAN_POINT('Ctrl Pts',(10.1054346546984,11.0851337583099,-594.565441176471));
#161945=CARTESIAN_POINT('Ctrl Pts',(11.132623567824,10.148727336345,-596.05955882353));
#161946=CARTESIAN_POINT('Ctrl Pts',(11.9702584092036,9.03951954568885,-597.553676470588));
#161947=CARTESIAN_POINT('Ctrl Pts',(12.8078932505832,7.93031175503273,-599.047794117647));
#161948=CARTESIAN_POINT('Ctrl Pts',(13.4274493703259,6.68607533664807,-600.541911764706));
#161949=CARTESIAN_POINT('Ctrl Pts',(14.0470054900687,5.44183891826343,-602.036029411765));
#161950=CARTESIAN_POINT('Ctrl Pts',(14.4273846475923,4.10494485108125,-603.530147058823));
#161951=CARTESIAN_POINT('Ctrl Pts',(14.8077638051159,2.76805078389905,-605.024264705882));
#161952=CARTESIAN_POINT('Ctrl Pts',(14.9360126444255,1.38402539194953,-606.518382352941));
#161953=CARTESIAN_POINT('Ctrl Pts',(15.0642614837351,2.76725994113625E-15,
-608.0125));
#161954=CARTESIAN_POINT('Ctrl Pts',(14.9360126444255,-1.38402539194952,
-609.506617647059));
#161955=CARTESIAN_POINT('Ctrl Pts',(14.8077638051159,-2.76805078389906,
-611.000735294118));
#161956=CARTESIAN_POINT('Ctrl Pts',(14.4273846475923,-4.10494485108124,
-612.494852941176));
#161957=CARTESIAN_POINT('Ctrl Pts',(14.0470054900687,-5.44183891826342,
-613.988970588235));
#161958=CARTESIAN_POINT('Ctrl Pts',(13.4274493703259,-6.68607533664808,
-615.483088235294));
#161959=CARTESIAN_POINT('Ctrl Pts',(12.8078932505832,-7.93031175503273,
-616.977205882353));
#161960=CARTESIAN_POINT('Ctrl Pts',(11.9702584092036,-9.03951954568884,
-618.471323529412));
#161961=CARTESIAN_POINT('Ctrl Pts',(11.132623567824,-10.148727336345,-619.96544117647));
#161962=CARTESIAN_POINT('Ctrl Pts',(10.1054346546984,-11.0851337583099,
-621.459558823529));
#161963=CARTESIAN_POINT('Ctrl Pts',(9.07824574157275,-12.0215401802748,
-622.953676470588));
#161964=CARTESIAN_POINT('Ctrl Pts',(7.89648244316034,-12.7532570359442,
-624.447794117647));
#161965=CARTESIAN_POINT('Ctrl Pts',(6.71471914474792,-13.4849738916136,
-625.941911764706));
#161966=CARTESIAN_POINT('Ctrl Pts',(5.4186249928073,-13.9870834410653,-627.436029411764));
#161967=CARTESIAN_POINT('Ctrl Pts',(4.12253084086667,-14.4891929905171,
-628.930147058823));
#161968=CARTESIAN_POINT('Ctrl Pts',(2.75624276724855,-14.7445964952585,
-630.424264705882));
#161969=CARTESIAN_POINT('Ctrl Pts',(1.38995469363045,-15.,-631.918382352941));
#161970=CARTESIAN_POINT('Ctrl Pts',(0.,-15.,-633.4125));
#161971=CARTESIAN_POINT('Ctrl Pts',(-1.38995469363045,-15.,-634.906617647059));
#161972=CARTESIAN_POINT('Ctrl Pts',(-2.75624276724856,-14.7445964952585,
-636.400735294118));
#161973=CARTESIAN_POINT('Ctrl Pts',(-4.12253084086666,-14.4891929905171,
-637.894852941177));
#161974=CARTESIAN_POINT('Ctrl Pts',(-5.41862499280729,-13.9870834410653,
-639.388970588235));
#161975=CARTESIAN_POINT('Ctrl Pts',(-6.71471914474793,-13.4849738916136,
-640.883088235294));
#161976=CARTESIAN_POINT('Ctrl Pts',(-7.89648244316034,-12.7532570359442,
-642.377205882353));
#161977=CARTESIAN_POINT('Ctrl Pts',(-9.07824574157275,-12.0215401802748,
-643.871323529412));
#161978=CARTESIAN_POINT('Ctrl Pts',(-10.1054346546984,-11.0851337583099,
-645.36544117647));
#161979=CARTESIAN_POINT('Ctrl Pts',(-11.132623567824,-10.148727336345,-646.859558823529));
#161980=CARTESIAN_POINT('Ctrl Pts',(-11.9702584092036,-9.03951954568885,
-648.353676470588));
#161981=CARTESIAN_POINT('Ctrl Pts',(-12.8078932505832,-7.93031175503273,
-649.847794117647));
#161982=CARTESIAN_POINT('Ctrl Pts',(-13.4274493703259,-6.68607533664808,
-651.341911764706));
#161983=CARTESIAN_POINT('Ctrl Pts',(-14.0470054900687,-5.44183891826343,
-652.836029411765));
#161984=CARTESIAN_POINT('Ctrl Pts',(-14.4273846475923,-4.10494485108124,
-654.330147058824));
#161985=CARTESIAN_POINT('Ctrl Pts',(-14.8077638051159,-2.76805078389906,
-655.824264705882));
#161986=CARTESIAN_POINT('Ctrl Pts',(-14.9360126444255,-1.38402539194953,
-657.318382352941));
#161987=CARTESIAN_POINT('Ctrl Pts',(-15.0642614837351,-9.22419980378748E-16,
-658.8125));
#161988=CARTESIAN_POINT('Ctrl Pts',(-14.9360126444255,1.38402539194953,
-660.306617647059));
#161989=CARTESIAN_POINT('Ctrl Pts',(-14.8077638051159,2.76805078389906,
-661.800735294117));
#161990=CARTESIAN_POINT('Ctrl Pts',(-14.4273846475923,4.10494485108124,
-663.294852941176));
#161991=CARTESIAN_POINT('Ctrl Pts',(-14.0470054900687,5.44183891826343,
-664.788970588236));
#161992=CARTESIAN_POINT('Ctrl Pts',(-13.4274493703259,6.68607533664807,
-666.283088235294));
#161993=CARTESIAN_POINT('Ctrl Pts',(-12.8078932505832,7.93031175503273,
-667.777205882353));
#161994=CARTESIAN_POINT('Ctrl Pts',(-11.9702584092036,9.03951954568884,
-669.271323529412));
#161995=CARTESIAN_POINT('Ctrl Pts',(-11.132623567824,10.148727336345,-670.765441176471));
#161996=CARTESIAN_POINT('Ctrl Pts',(-10.1054346546984,11.0851337583099,
-672.259558823529));
#161997=CARTESIAN_POINT('Ctrl Pts',(-9.07824574157275,12.0215401802748,
-673.753676470588));
#161998=CARTESIAN_POINT('Ctrl Pts',(-7.89648244316034,12.7532570359442,
-675.247794117647));
#161999=CARTESIAN_POINT('Ctrl Pts',(-6.71471914474793,13.4849738916136,
-676.741911764706));
#162000=CARTESIAN_POINT('Ctrl Pts',(-5.41862499280729,13.9870834410653,
-678.236029411765));
#162001=CARTESIAN_POINT('Ctrl Pts',(-4.12253084086667,14.4891929905171,
-679.730147058824));
#162002=CARTESIAN_POINT('Ctrl Pts',(-2.75624276724856,14.7445964952585,
-681.224264705883));
#162003=CARTESIAN_POINT('Ctrl Pts',(-1.38995469363044,15.,-682.718382352941));
#162004=CARTESIAN_POINT('Ctrl Pts',(-1.83697019872103E-15,15.,-684.2125));
#162005=CARTESIAN_POINT('Ctrl Pts',(1.38995469363045,15.,-685.706617647059));
#162006=CARTESIAN_POINT('Ctrl Pts',(2.75624276724855,14.7445964952585,-687.200735294118));
#162007=CARTESIAN_POINT('Ctrl Pts',(4.12253084086666,14.4891929905171,-688.694852941176));
#162008=CARTESIAN_POINT('Ctrl Pts',(5.4186249928073,13.9870834410653,-690.188970588235));
#162009=CARTESIAN_POINT('Ctrl Pts',(6.71471914474792,13.4849738916136,-691.683088235294));
#162010=CARTESIAN_POINT('Ctrl Pts',(7.89648244316034,12.7532570359442,-693.177205882353));
#162011=CARTESIAN_POINT('Ctrl Pts',(9.07824574157275,12.0215401802748,-694.671323529412));
#162012=CARTESIAN_POINT('Ctrl Pts',(10.1054346546984,11.0851337583099,-696.165441176471));
#162013=CARTESIAN_POINT('Ctrl Pts',(11.132623567824,10.148727336345,-697.659558823529));
#162014=CARTESIAN_POINT('Ctrl Pts',(11.9702584092036,9.03951954568885,-699.153676470588));
#162015=CARTESIAN_POINT('Ctrl Pts',(12.8078932505832,7.93031175503273,-700.647794117647));
#162016=CARTESIAN_POINT('Ctrl Pts',(13.4274493703259,6.68607533664807,-702.141911764706));
#162017=CARTESIAN_POINT('Ctrl Pts',(14.0470054900687,5.44183891826343,-703.636029411765));
#162018=CARTESIAN_POINT('Ctrl Pts',(14.4273846475923,4.10494485108125,-705.130147058823));
#162019=CARTESIAN_POINT('Ctrl Pts',(14.8077638051159,2.76805078389905,-706.624264705882));
#162020=CARTESIAN_POINT('Ctrl Pts',(14.9360126444255,1.38402539194953,-708.118382352941));
#162021=CARTESIAN_POINT('Ctrl Pts',(15.0642614837351,2.76725994113625E-15,
-709.6125));
#162022=CARTESIAN_POINT('Ctrl Pts',(14.9360126444255,-1.38402539194952,
-711.106617647059));
#162023=CARTESIAN_POINT('Ctrl Pts',(14.8077638051159,-2.76805078389906,
-712.600735294118));
#162024=CARTESIAN_POINT('Ctrl Pts',(14.4273846475923,-4.10494485108124,
-714.094852941177));
#162025=CARTESIAN_POINT('Ctrl Pts',(14.0470054900687,-5.44183891826342,
-715.588970588235));
#162026=CARTESIAN_POINT('Ctrl Pts',(13.4274493703259,-6.68607533664808,
-717.083088235294));
#162027=CARTESIAN_POINT('Ctrl Pts',(12.8078932505832,-7.93031175503273,
-718.577205882353));
#162028=CARTESIAN_POINT('Ctrl Pts',(11.9702584092036,-9.03951954568884,
-720.071323529412));
#162029=CARTESIAN_POINT('Ctrl Pts',(11.132623567824,-10.148727336345,-721.56544117647));
#162030=CARTESIAN_POINT('Ctrl Pts',(10.1054346546984,-11.0851337583099,
-723.059558823529));
#162031=CARTESIAN_POINT('Ctrl Pts',(9.07824574157275,-12.0215401802748,
-724.553676470588));
#162032=CARTESIAN_POINT('Ctrl Pts',(7.89648244316034,-12.7532570359442,
-726.047794117647));
#162033=CARTESIAN_POINT('Ctrl Pts',(6.71471914474792,-13.4849738916136,
-727.541911764706));
#162034=CARTESIAN_POINT('Ctrl Pts',(5.4186249928073,-13.9870834410653,-729.036029411765));
#162035=CARTESIAN_POINT('Ctrl Pts',(4.12253084086667,-14.4891929905171,
-730.530147058824));
#162036=CARTESIAN_POINT('Ctrl Pts',(2.75624276724855,-14.7445964952585,
-732.024264705882));
#162037=CARTESIAN_POINT('Ctrl Pts',(1.38995469363045,-15.,-733.518382352941));
#162038=CARTESIAN_POINT('Ctrl Pts',(0.,-15.,-735.0125));
#162039=CARTESIAN_POINT('Ctrl Pts',(-1.38995469363045,-15.,-736.506617647059));
#162040=CARTESIAN_POINT('Ctrl Pts',(-2.75624276724856,-14.7445964952585,
-738.000735294118));
#162041=CARTESIAN_POINT('Ctrl Pts',(-4.12253084086666,-14.4891929905171,
-739.494852941177));
#162042=CARTESIAN_POINT('Ctrl Pts',(-5.41862499280729,-13.9870834410653,
-740.988970588235));
#162043=CARTESIAN_POINT('Ctrl Pts',(-6.71471914474793,-13.4849738916136,
-742.483088235294));
#162044=CARTESIAN_POINT('Ctrl Pts',(-7.89648244316034,-12.7532570359442,
-743.977205882353));
#162045=CARTESIAN_POINT('Ctrl Pts',(-9.07824574157275,-12.0215401802748,
-745.471323529412));
#162046=CARTESIAN_POINT('Ctrl Pts',(-10.1054346546984,-11.0851337583099,
-746.96544117647));
#162047=CARTESIAN_POINT('Ctrl Pts',(-11.132623567824,-10.148727336345,-748.459558823529));
#162048=CARTESIAN_POINT('Ctrl Pts',(-11.9702584092036,-9.03951954568885,
-749.953676470588));
#162049=CARTESIAN_POINT('Ctrl Pts',(-12.8078932505832,-7.93031175503273,
-751.447794117647));
#162050=CARTESIAN_POINT('Ctrl Pts',(-13.4274493703259,-6.68607533664808,
-752.941911764706));
#162051=CARTESIAN_POINT('Ctrl Pts',(-14.0470054900687,-5.44183891826343,
-754.436029411765));
#162052=CARTESIAN_POINT('Ctrl Pts',(-14.4273846475923,-4.10494485108124,
-755.930147058824));
#162053=CARTESIAN_POINT('Ctrl Pts',(-14.8077638051159,-2.76805078389906,
-757.424264705882));
#162054=CARTESIAN_POINT('Ctrl Pts',(-14.9360126444255,-1.38402539194953,
-758.918382352941));
#162055=CARTESIAN_POINT('Ctrl Pts',(-15.0642614837351,-9.22419980378748E-16,
-760.4125));
#162056=CARTESIAN_POINT('Ctrl Pts',(-14.9360126444255,1.38402539194953,
-761.906617647059));
#162057=CARTESIAN_POINT('Ctrl Pts',(-14.8077638051159,2.76805078389906,
-763.400735294118));
#162058=CARTESIAN_POINT('Ctrl Pts',(-14.4273846475923,4.10494485108124,
-764.894852941176));
#162059=CARTESIAN_POINT('Ctrl Pts',(-14.0470054900687,5.44183891826343,
-766.388970588235));
#162060=CARTESIAN_POINT('Ctrl Pts',(-13.4274493703259,6.68607533664807,
-767.883088235294));
#162061=CARTESIAN_POINT('Ctrl Pts',(-12.8078932505832,7.93031175503273,
-769.377205882353));
#162062=CARTESIAN_POINT('Ctrl Pts',(-11.9702584092036,9.03951954568884,
-770.871323529412));
#162063=CARTESIAN_POINT('Ctrl Pts',(-11.132623567824,10.148727336345,-772.365441176471));
#162064=CARTESIAN_POINT('Ctrl Pts',(-10.1054346546984,11.0851337583099,
-773.85955882353));
#162065=CARTESIAN_POINT('Ctrl Pts',(-9.07824574157275,12.0215401802748,
-775.353676470589));
#162066=CARTESIAN_POINT('Ctrl Pts',(-7.89648244316034,12.7532570359442,
-776.847794117647));
#162067=CARTESIAN_POINT('Ctrl Pts',(-6.71471914474793,13.4849738916136,
-778.341911764706));
#162068=CARTESIAN_POINT('Ctrl Pts',(-5.41862499280729,13.9870834410653,
-779.836029411765));
#162069=CARTESIAN_POINT('Ctrl Pts',(-4.12253084086667,14.4891929905171,
-781.330147058823));
#162070=CARTESIAN_POINT('Ctrl Pts',(-2.75624276724856,14.7445964952585,
-782.824264705882));
#162071=CARTESIAN_POINT('Ctrl Pts',(-1.38995469363044,15.,-784.318382352941));
#162072=CARTESIAN_POINT('Ctrl Pts',(-1.83697019872103E-15,15.,-785.8125));
#162073=CARTESIAN_POINT('Ctrl Pts',(1.38995469363045,15.,-787.306617647059));
#162074=CARTESIAN_POINT('Ctrl Pts',(2.75624276724855,14.7445964952585,-788.800735294118));
#162075=CARTESIAN_POINT('Ctrl Pts',(4.12253084086666,14.4891929905171,-790.294852941177));
#162076=CARTESIAN_POINT('Ctrl Pts',(5.4186249928073,13.9870834410653,-791.788970588235));
#162077=CARTESIAN_POINT('Ctrl Pts',(6.71471914474792,13.4849738916136,-793.283088235294));
#162078=CARTESIAN_POINT('Ctrl Pts',(7.89648244316034,12.7532570359442,-794.777205882353));
#162079=CARTESIAN_POINT('Ctrl Pts',(9.07824574157275,12.0215401802748,-796.271323529412));
#162080=CARTESIAN_POINT('Ctrl Pts',(10.1054346546984,11.0851337583099,-797.765441176471));
#162081=CARTESIAN_POINT('Ctrl Pts',(11.132623567824,10.148727336345,-799.259558823529));
#162082=CARTESIAN_POINT('Ctrl Pts',(11.9702584092036,9.03951954568885,-800.753676470588));
#162083=CARTESIAN_POINT('Ctrl Pts',(12.8078932505832,7.93031175503273,-802.247794117647));
#162084=CARTESIAN_POINT('Ctrl Pts',(13.4274493703259,6.68607533664807,-803.741911764706));
#162085=CARTESIAN_POINT('Ctrl Pts',(14.0470054900687,5.44183891826343,-805.236029411765));
#162086=CARTESIAN_POINT('Ctrl Pts',(14.4273846475923,4.10494485108125,-806.730147058823));
#162087=CARTESIAN_POINT('Ctrl Pts',(14.8077638051159,2.76805078389905,-808.224264705882));
#162088=CARTESIAN_POINT('Ctrl Pts',(14.9360126444255,1.38402539194953,-809.718382352941));
#162089=CARTESIAN_POINT('Ctrl Pts',(15.0642614837351,2.76725994113625E-15,
-811.2125));
#162090=CARTESIAN_POINT('Ctrl Pts',(14.9360126444255,-1.38402539194952,
-812.706617647059));
#162091=CARTESIAN_POINT('Ctrl Pts',(14.8077638051159,-2.76805078389906,
-814.200735294118));
#162092=CARTESIAN_POINT('Ctrl Pts',(14.4273846475923,-4.10494485108124,
-815.694852941177));
#162093=CARTESIAN_POINT('Ctrl Pts',(14.0470054900687,-5.44183891826342,
-817.188970588235));
#162094=CARTESIAN_POINT('Ctrl Pts',(13.4274493703259,-6.68607533664808,
-818.683088235294));
#162095=CARTESIAN_POINT('Ctrl Pts',(12.8078932505832,-7.93031175503273,
-820.177205882353));
#162096=CARTESIAN_POINT('Ctrl Pts',(11.9702584092036,-9.03951954568884,
-821.671323529412));
#162097=CARTESIAN_POINT('Ctrl Pts',(11.132623567824,-10.148727336345,-823.16544117647));
#162098=CARTESIAN_POINT('Ctrl Pts',(10.1054346546984,-11.0851337583099,
-824.659558823529));
#162099=CARTESIAN_POINT('Ctrl Pts',(9.07824574157275,-12.0215401802748,
-826.153676470588));
#162100=CARTESIAN_POINT('Ctrl Pts',(7.89648244316034,-12.7532570359442,
-827.647794117647));
#162101=CARTESIAN_POINT('Ctrl Pts',(6.71471914474792,-13.4849738916136,
-829.141911764706));
#162102=CARTESIAN_POINT('Ctrl Pts',(5.4186249928073,-13.9870834410653,-830.636029411765));
#162103=CARTESIAN_POINT('Ctrl Pts',(4.12253084086667,-14.4891929905171,
-832.130147058824));
#162104=CARTESIAN_POINT('Ctrl Pts',(2.75624276724855,-14.7445964952585,
-833.624264705883));
#162105=CARTESIAN_POINT('Ctrl Pts',(1.38995469363045,-15.,-835.118382352941));
#162106=CARTESIAN_POINT('Ctrl Pts',(0.,-15.,-836.6125));
#162107=CARTESIAN_POINT('Ctrl Pts',(-1.38995469363045,-15.,-838.106617647059));
#162108=CARTESIAN_POINT('Ctrl Pts',(-2.75624276724856,-14.7445964952585,
-839.600735294118));
#162109=CARTESIAN_POINT('Ctrl Pts',(-4.12253084086666,-14.4891929905171,
-841.094852941176));
#162110=CARTESIAN_POINT('Ctrl Pts',(-5.41862499280729,-13.9870834410653,
-842.588970588235));
#162111=CARTESIAN_POINT('Ctrl Pts',(-6.71471914474793,-13.4849738916136,
-844.083088235294));
#162112=CARTESIAN_POINT('Ctrl Pts',(-7.89648244316034,-12.7532570359442,
-845.577205882353));
#162113=CARTESIAN_POINT('Ctrl Pts',(-9.07824574157275,-12.0215401802748,
-847.071323529412));
#162114=CARTESIAN_POINT('Ctrl Pts',(-10.1054346546984,-11.0851337583099,
-848.565441176471));
#162115=CARTESIAN_POINT('Ctrl Pts',(-11.132623567824,-10.148727336345,-850.05955882353));
#162116=CARTESIAN_POINT('Ctrl Pts',(-11.9702584092036,-9.03951954568885,
-851.553676470588));
#162117=CARTESIAN_POINT('Ctrl Pts',(-12.8078932505832,-7.93031175503273,
-853.047794117647));
#162118=CARTESIAN_POINT('Ctrl Pts',(-13.4274493703259,-6.68607533664808,
-854.541911764706));
#162119=CARTESIAN_POINT('Ctrl Pts',(-14.0470054900687,-5.44183891826343,
-856.036029411765));
#162120=CARTESIAN_POINT('Ctrl Pts',(-14.4273846475923,-4.10494485108124,
-857.530147058824));
#162121=CARTESIAN_POINT('Ctrl Pts',(-14.8077638051159,-2.76805078389906,
-859.024264705882));
#162122=CARTESIAN_POINT('Ctrl Pts',(-14.9360126444255,-1.38402539194953,
-860.518382352941));
#162123=CARTESIAN_POINT('Ctrl Pts',(-15.0642614837351,-9.22419980378748E-16,
-862.0125));
#162124=CARTESIAN_POINT('Ctrl Pts',(-14.9360126444255,1.38402539194953,
-863.506617647059));
#162125=CARTESIAN_POINT('Ctrl Pts',(-14.8077638051159,2.76805078389906,
-865.000735294118));
#162126=CARTESIAN_POINT('Ctrl Pts',(-14.4273846475923,4.10494485108124,
-866.494852941176));
#162127=CARTESIAN_POINT('Ctrl Pts',(-14.0470054900687,5.44183891826343,
-867.988970588235));
#162128=CARTESIAN_POINT('Ctrl Pts',(-13.4274493703259,6.68607533664807,
-869.483088235294));
#162129=CARTESIAN_POINT('Ctrl Pts',(-12.8078932505832,7.93031175503273,
-870.977205882353));
#162130=CARTESIAN_POINT('Ctrl Pts',(-11.9702584092036,9.03951954568884,
-872.471323529412));
#162131=CARTESIAN_POINT('Ctrl Pts',(-11.132623567824,10.148727336345,-873.965441176471));
#162132=CARTESIAN_POINT('Ctrl Pts',(-10.1054346546984,11.0851337583099,
-875.459558823529));
#162133=CARTESIAN_POINT('Ctrl Pts',(-9.07824574157275,12.0215401802748,
-876.953676470588));
#162134=CARTESIAN_POINT('Ctrl Pts',(-7.89648244316034,12.7532570359442,
-878.447794117647));
#162135=CARTESIAN_POINT('Ctrl Pts',(-6.71471914474793,13.4849738916136,
-879.941911764706));
#162136=CARTESIAN_POINT('Ctrl Pts',(-5.41862499280729,13.9870834410653,
-881.436029411765));
#162137=CARTESIAN_POINT('Ctrl Pts',(-4.12253084086667,14.4891929905171,
-882.930147058823));
#162138=CARTESIAN_POINT('Ctrl Pts',(-2.75624276724856,14.7445964952585,
-884.424264705882));
#162139=CARTESIAN_POINT('Ctrl Pts',(-1.38995469363044,15.,-885.918382352941));
#162140=CARTESIAN_POINT('Ctrl Pts',(-1.83697019872103E-15,15.,-887.4125));
#162141=CARTESIAN_POINT('Ctrl Pts',(1.38995469363045,15.,-888.906617647059));
#162142=CARTESIAN_POINT('Ctrl Pts',(2.75624276724855,14.7445964952585,-890.400735294118));
#162143=CARTESIAN_POINT('Ctrl Pts',(4.12253084086666,14.4891929905171,-891.894852941177));
#162144=CARTESIAN_POINT('Ctrl Pts',(5.4186249928073,13.9870834410653,-893.388970588235));
#162145=CARTESIAN_POINT('Ctrl Pts',(6.71471914474792,13.4849738916136,-894.883088235295));
#162146=CARTESIAN_POINT('Ctrl Pts',(7.89648244316034,12.7532570359442,-896.377205882353));
#162147=CARTESIAN_POINT('Ctrl Pts',(9.07824574157275,12.0215401802748,-897.871323529412));
#162148=CARTESIAN_POINT('Ctrl Pts',(10.1054346546984,11.0851337583099,-899.36544117647));
#162149=CARTESIAN_POINT('Ctrl Pts',(11.132623567824,10.148727336345,-900.859558823529));
#162150=CARTESIAN_POINT('Ctrl Pts',(11.9702584092036,9.03951954568885,-902.353676470588));
#162151=CARTESIAN_POINT('Ctrl Pts',(12.8078932505832,7.93031175503273,-903.847794117647));
#162152=CARTESIAN_POINT('Ctrl Pts',(13.4274493703259,6.68607533664807,-905.341911764706));
#162153=CARTESIAN_POINT('Ctrl Pts',(14.0470054900687,5.44183891826343,-906.836029411765));
#162154=CARTESIAN_POINT('Ctrl Pts',(14.4273846475923,4.10494485108125,-908.330147058824));
#162155=CARTESIAN_POINT('Ctrl Pts',(14.8077638051159,2.76805078389905,-909.824264705883));
#162156=CARTESIAN_POINT('Ctrl Pts',(14.9360126444255,1.38402539194953,-911.318382352941));
#162157=CARTESIAN_POINT('Ctrl Pts',(15.0642614837351,2.76725994113625E-15,
-912.8125));
#162158=CARTESIAN_POINT('Ctrl Pts',(14.9360126444255,-1.38402539194952,
-914.306617647059));
#162159=CARTESIAN_POINT('Ctrl Pts',(14.8077638051159,-2.76805078389906,
-915.800735294118));
#162160=CARTESIAN_POINT('Ctrl Pts',(14.4273846475923,-4.10494485108124,
-917.294852941176));
#162161=CARTESIAN_POINT('Ctrl Pts',(14.0470054900687,-5.44183891826342,
-918.788970588235));
#162162=CARTESIAN_POINT('Ctrl Pts',(13.4274493703259,-6.68607533664808,
-920.283088235294));
#162163=CARTESIAN_POINT('Ctrl Pts',(12.8078932505832,-7.93031175503273,
-921.777205882353));
#162164=CARTESIAN_POINT('Ctrl Pts',(11.9702584092036,-9.03951954568884,
-923.271323529412));
#162165=CARTESIAN_POINT('Ctrl Pts',(11.132623567824,-10.148727336345,-924.765441176471));
#162166=CARTESIAN_POINT('Ctrl Pts',(10.1054346546984,-11.0851337583099,
-926.259558823529));
#162167=CARTESIAN_POINT('Ctrl Pts',(9.07824574157275,-12.0215401802748,
-927.753676470588));
#162168=CARTESIAN_POINT('Ctrl Pts',(7.89648244316034,-12.7532570359442,
-929.247794117647));
#162169=CARTESIAN_POINT('Ctrl Pts',(6.71471914474792,-13.4849738916136,
-930.741911764706));
#162170=CARTESIAN_POINT('Ctrl Pts',(5.4186249928073,-13.9870834410653,-932.236029411765));
#162171=CARTESIAN_POINT('Ctrl Pts',(4.12253084086667,-14.4891929905171,
-933.730147058824));
#162172=CARTESIAN_POINT('Ctrl Pts',(2.75624276724855,-14.7445964952585,
-935.224264705882));
#162173=CARTESIAN_POINT('Ctrl Pts',(1.38995469363045,-15.,-936.718382352941));
#162174=CARTESIAN_POINT('Ctrl Pts',(0.,-15.,-938.2125));
#162175=CARTESIAN_POINT('Ctrl Pts',(-1.38995469363045,-15.,-939.706617647059));
#162176=CARTESIAN_POINT('Ctrl Pts',(-2.75624276724856,-14.7445964952585,
-941.200735294117));
#162177=CARTESIAN_POINT('Ctrl Pts',(-4.12253084086666,-14.4891929905171,
-942.694852941176));
#162178=CARTESIAN_POINT('Ctrl Pts',(-5.41862499280729,-13.9870834410653,
-944.188970588235));
#162179=CARTESIAN_POINT('Ctrl Pts',(-6.71471914474793,-13.4849738916136,
-945.683088235294));
#162180=CARTESIAN_POINT('Ctrl Pts',(-7.89648244316034,-12.7532570359442,
-947.177205882353));
#162181=CARTESIAN_POINT('Ctrl Pts',(-9.07824574157275,-12.0215401802748,
-948.671323529412));
#162182=CARTESIAN_POINT('Ctrl Pts',(-10.1054346546984,-11.0851337583099,
-950.165441176471));
#162183=CARTESIAN_POINT('Ctrl Pts',(-11.132623567824,-10.148727336345,-951.65955882353));
#162184=CARTESIAN_POINT('Ctrl Pts',(-11.9702584092036,-9.03951954568885,
-953.153676470588));
#162185=CARTESIAN_POINT('Ctrl Pts',(-12.8078932505832,-7.93031175503273,
-954.647794117647));
#162186=CARTESIAN_POINT('Ctrl Pts',(-13.4274493703259,-6.68607533664808,
-956.141911764706));
#162187=CARTESIAN_POINT('Ctrl Pts',(-14.0470054900687,-5.44183891826343,
-957.636029411764));
#162188=CARTESIAN_POINT('Ctrl Pts',(-14.4273846475923,-4.10494485108124,
-959.130147058823));
#162189=CARTESIAN_POINT('Ctrl Pts',(-14.8077638051159,-2.76805078389906,
-960.624264705882));
#162190=CARTESIAN_POINT('Ctrl Pts',(-14.9360126444255,-1.38402539194953,
-962.118382352941));
#162191=CARTESIAN_POINT('Ctrl Pts',(-15.0642614837351,-9.22419980378748E-16,
-963.6125));
#162192=CARTESIAN_POINT('Ctrl Pts',(-14.9360126444255,1.38402539194953,
-965.106617647059));
#162193=CARTESIAN_POINT('Ctrl Pts',(-14.8077638051159,2.76805078389906,
-966.600735294118));
#162194=CARTESIAN_POINT('Ctrl Pts',(-14.4273846475923,4.10494485108124,
-968.094852941177));
#162195=CARTESIAN_POINT('Ctrl Pts',(-14.0470054900687,5.44183891826343,
-969.588970588235));
#162196=CARTESIAN_POINT('Ctrl Pts',(-13.4274493703259,6.68607533664807,
-971.083088235294));
#162197=CARTESIAN_POINT('Ctrl Pts',(-12.8078932505832,7.93031175503273,
-972.577205882353));
#162198=CARTESIAN_POINT('Ctrl Pts',(-11.9702584092036,9.03951954568884,
-974.071323529412));
#162199=CARTESIAN_POINT('Ctrl Pts',(-11.132623567824,10.148727336345,-975.565441176471));
#162200=CARTESIAN_POINT('Ctrl Pts',(-10.1054346546984,11.0851337583099,
-977.059558823529));
#162201=CARTESIAN_POINT('Ctrl Pts',(-9.07824574157275,12.0215401802748,
-978.553676470588));
#162202=CARTESIAN_POINT('Ctrl Pts',(-7.89648244316034,12.7532570359442,
-980.047794117647));
#162203=CARTESIAN_POINT('Ctrl Pts',(-6.71471914474793,13.4849738916136,
-981.541911764706));
#162204=CARTESIAN_POINT('Ctrl Pts',(-5.41862499280729,13.9870834410653,
-983.036029411765));
#162205=CARTESIAN_POINT('Ctrl Pts',(-4.12253084086667,14.4891929905171,
-984.530147058824));
#162206=CARTESIAN_POINT('Ctrl Pts',(-2.75624276724856,14.7445964952585,
-986.024264705882));
#162207=CARTESIAN_POINT('Ctrl Pts',(-1.38995469363044,15.,-987.518382352941));
#162208=CARTESIAN_POINT('Ctrl Pts',(-1.83697019872103E-15,15.,-989.0125));
#162209=CARTESIAN_POINT('Ctrl Pts',(1.38995469363045,15.,-990.506617647059));
#162210=CARTESIAN_POINT('Ctrl Pts',(2.75624276724855,14.7445964952585,-992.000735294118));
#162211=CARTESIAN_POINT('Ctrl Pts',(4.12253084086666,14.4891929905171,-993.494852941176));
#162212=CARTESIAN_POINT('Ctrl Pts',(5.4186249928073,13.9870834410653,-994.988970588235));
#162213=CARTESIAN_POINT('Ctrl Pts',(6.71471914474792,13.4849738916136,-996.483088235294));
#162214=CARTESIAN_POINT('Ctrl Pts',(7.89648244316034,12.7532570359442,-997.977205882353));
#162215=CARTESIAN_POINT('Ctrl Pts',(9.07824574157275,12.0215401802748,-999.471323529412));
#162216=CARTESIAN_POINT('Ctrl Pts',(10.1054346546984,11.0851337583099,-1000.96544117647));
#162217=CARTESIAN_POINT('Ctrl Pts',(11.132623567824,10.148727336345,-1002.45955882353));
#162218=CARTESIAN_POINT('Ctrl Pts',(11.9702584092036,9.03951954568885,-1003.95367647059));
#162219=CARTESIAN_POINT('Ctrl Pts',(12.8078932505832,7.93031175503273,-1005.44779411765));
#162220=CARTESIAN_POINT('Ctrl Pts',(13.4274493703259,6.68607533664807,-1006.94191176471));
#162221=CARTESIAN_POINT('Ctrl Pts',(14.0470054900687,5.44183891826343,-1008.43602941176));
#162222=CARTESIAN_POINT('Ctrl Pts',(14.4273846475923,4.10494485108125,-1009.93014705882));
#162223=CARTESIAN_POINT('Ctrl Pts',(14.8077638051159,2.76805078389905,-1011.42426470588));
#162224=CARTESIAN_POINT('Ctrl Pts',(14.9360126444255,1.38402539194953,-1012.91838235294));
#162225=CARTESIAN_POINT('Ctrl Pts',(15.0642614837351,2.76725994113625E-15,
-1014.4125));
#162226=CARTESIAN_POINT('Ctrl Pts',(14.9360126444255,-1.38402539194952,
-1015.90661764706));
#162227=CARTESIAN_POINT('Ctrl Pts',(14.8077638051159,-2.76805078389906,
-1017.40073529412));
#162228=CARTESIAN_POINT('Ctrl Pts',(14.4273846475923,-4.10494485108124,
-1018.89485294118));
#162229=CARTESIAN_POINT('Ctrl Pts',(14.0470054900687,-5.44183891826342,
-1020.38897058824));
#162230=CARTESIAN_POINT('Ctrl Pts',(13.4274493703259,-6.68607533664808,
-1021.88308823529));
#162231=CARTESIAN_POINT('Ctrl Pts',(12.8078932505832,-7.93031175503273,
-1023.37720588235));
#162232=CARTESIAN_POINT('Ctrl Pts',(11.9702584092036,-9.03951954568884,
-1024.87132352941));
#162233=CARTESIAN_POINT('Ctrl Pts',(11.132623567824,-10.148727336345,-1026.36544117647));
#162234=CARTESIAN_POINT('Ctrl Pts',(10.1054346546984,-11.0851337583099,
-1027.85955882353));
#162235=CARTESIAN_POINT('Ctrl Pts',(9.07824574157275,-12.0215401802748,
-1029.35367647059));
#162236=CARTESIAN_POINT('Ctrl Pts',(7.89648244316034,-12.7532570359442,
-1030.84779411765));
#162237=CARTESIAN_POINT('Ctrl Pts',(6.71471914474792,-13.4849738916136,
-1032.34191176471));
#162238=CARTESIAN_POINT('Ctrl Pts',(5.4186249928073,-13.9870834410653,-1033.83602941176));
#162239=CARTESIAN_POINT('Ctrl Pts',(4.12253084086667,-14.4891929905171,
-1035.33014705882));
#162240=CARTESIAN_POINT('Ctrl Pts',(2.75624276724855,-14.7445964952585,
-1036.82426470588));
#162241=CARTESIAN_POINT('Ctrl Pts',(1.38995469363045,-15.,-1038.31838235294));
#162242=CARTESIAN_POINT('Ctrl Pts',(0.,-15.,-1039.8125));
#162243=CARTESIAN_POINT('Ctrl Pts',(-1.38995469363045,-15.,-1041.30661764706));
#162244=CARTESIAN_POINT('Ctrl Pts',(-2.75624276724856,-14.7445964952585,
-1042.80073529412));
#162245=CARTESIAN_POINT('Ctrl Pts',(-4.12253084086666,-14.4891929905171,
-1044.29485294118));
#162246=CARTESIAN_POINT('Ctrl Pts',(-5.41862499280729,-13.9870834410653,
-1045.78897058824));
#162247=CARTESIAN_POINT('Ctrl Pts',(-6.71471914474793,-13.4849738916136,
-1047.28308823529));
#162248=CARTESIAN_POINT('Ctrl Pts',(-7.89648244316034,-12.7532570359442,
-1048.77720588235));
#162249=CARTESIAN_POINT('Ctrl Pts',(-9.07824574157275,-12.0215401802748,
-1050.27132352941));
#162250=CARTESIAN_POINT('Ctrl Pts',(-10.1054346546984,-11.0851337583099,
-1051.76544117647));
#162251=CARTESIAN_POINT('Ctrl Pts',(-11.132623567824,-10.148727336345,-1053.25955882353));
#162252=CARTESIAN_POINT('Ctrl Pts',(-11.9702584092036,-9.03951954568885,
-1054.75367647059));
#162253=CARTESIAN_POINT('Ctrl Pts',(-12.8078932505832,-7.93031175503273,
-1056.24779411765));
#162254=CARTESIAN_POINT('Ctrl Pts',(-13.4274493703259,-6.68607533664808,
-1057.74191176471));
#162255=CARTESIAN_POINT('Ctrl Pts',(-14.0470054900687,-5.44183891826343,
-1059.23602941177));
#162256=CARTESIAN_POINT('Ctrl Pts',(-14.4273846475923,-4.10494485108124,
-1060.73014705882));
#162257=CARTESIAN_POINT('Ctrl Pts',(-14.8077638051159,-2.76805078389906,
-1062.22426470588));
#162258=CARTESIAN_POINT('Ctrl Pts',(-14.9360126444255,-1.38402539194953,
-1063.71838235294));
#162259=CARTESIAN_POINT('Ctrl Pts',(-15.0642614837351,-9.22419980378748E-16,
-1065.2125));
#162260=CARTESIAN_POINT('Ctrl Pts',(-14.9360126444255,1.38402539194953,
-1066.70661764706));
#162261=CARTESIAN_POINT('Ctrl Pts',(-14.8077638051159,2.76805078389906,
-1068.20073529412));
#162262=CARTESIAN_POINT('Ctrl Pts',(-14.4273846475923,4.10494485108124,
-1069.69485294118));
#162263=CARTESIAN_POINT('Ctrl Pts',(-14.0470054900687,5.44183891826343,
-1071.18897058824));
#162264=CARTESIAN_POINT('Ctrl Pts',(-13.4274493703259,6.68607533664807,
-1072.68308823529));
#162265=CARTESIAN_POINT('Ctrl Pts',(-12.8078932505832,7.93031175503273,
-1074.17720588235));
#162266=CARTESIAN_POINT('Ctrl Pts',(-11.9702584092036,9.03951954568884,
-1075.67132352941));
#162267=CARTESIAN_POINT('Ctrl Pts',(-11.132623567824,10.148727336345,-1077.16544117647));
#162268=CARTESIAN_POINT('Ctrl Pts',(-10.1054346546984,11.0851337583099,
-1078.65955882353));
#162269=CARTESIAN_POINT('Ctrl Pts',(-9.07824574157275,12.0215401802748,
-1080.15367647059));
#162270=CARTESIAN_POINT('Ctrl Pts',(-7.89648244316034,12.7532570359442,
-1081.64779411765));
#162271=CARTESIAN_POINT('Ctrl Pts',(-6.71471914474793,13.4849738916136,
-1083.14191176471));
#162272=CARTESIAN_POINT('Ctrl Pts',(-5.41862499280729,13.9870834410653,
-1084.63602941176));
#162273=CARTESIAN_POINT('Ctrl Pts',(-4.12253084086667,14.4891929905171,
-1086.13014705882));
#162274=CARTESIAN_POINT('Ctrl Pts',(-2.75624276724856,14.7445964952585,
-1087.62426470588));
#162275=CARTESIAN_POINT('Ctrl Pts',(-1.38995469363044,15.,-1089.11838235294));
#162276=CARTESIAN_POINT('Ctrl Pts',(-1.83697019872103E-15,15.,-1090.6125));
#162277=CARTESIAN_POINT('Ctrl Pts',(1.38995469363045,15.,-1092.10661764706));
#162278=CARTESIAN_POINT('Ctrl Pts',(2.75624276724855,14.7445964952585,-1093.60073529412));
#162279=CARTESIAN_POINT('Ctrl Pts',(4.12253084086666,14.4891929905171,-1095.09485294118));
#162280=CARTESIAN_POINT('Ctrl Pts',(5.4186249928073,13.9870834410653,-1096.58897058824));
#162281=CARTESIAN_POINT('Ctrl Pts',(6.71471914474792,13.4849738916136,-1098.08308823529));
#162282=CARTESIAN_POINT('Ctrl Pts',(7.89648244316034,12.7532570359442,-1099.57720588235));
#162283=CARTESIAN_POINT('Ctrl Pts',(9.07824574157275,12.0215401802748,-1101.07132352941));
#162284=CARTESIAN_POINT('Ctrl Pts',(10.1054346546984,11.0851337583099,-1102.56544117647));
#162285=CARTESIAN_POINT('Ctrl Pts',(11.132623567824,10.148727336345,-1104.05955882353));
#162286=CARTESIAN_POINT('Ctrl Pts',(11.9702584092036,9.03951954568885,-1105.55367647059));
#162287=CARTESIAN_POINT('Ctrl Pts',(12.8078932505832,7.93031175503273,-1107.04779411765));
#162288=CARTESIAN_POINT('Ctrl Pts',(13.4274493703259,6.68607533664807,-1108.54191176471));
#162289=CARTESIAN_POINT('Ctrl Pts',(14.0470054900687,5.44183891826343,-1110.03602941176));
#162290=CARTESIAN_POINT('Ctrl Pts',(14.4273846475923,4.10494485108125,-1111.53014705882));
#162291=CARTESIAN_POINT('Ctrl Pts',(14.8077638051159,2.76805078389905,-1113.02426470588));
#162292=CARTESIAN_POINT('Ctrl Pts',(14.9360126444255,1.38402539194953,-1114.51838235294));
#162293=CARTESIAN_POINT('Ctrl Pts',(15.0642614837351,2.76725994113625E-15,
-1116.0125));
#162294=CARTESIAN_POINT('Ctrl Pts',(14.9360126444255,-1.38402539194952,
-1117.50661764706));
#162295=CARTESIAN_POINT('Ctrl Pts',(14.8077638051159,-2.76805078389906,
-1119.00073529412));
#162296=CARTESIAN_POINT('Ctrl Pts',(14.4273846475923,-4.10494485108124,
-1120.49485294118));
#162297=CARTESIAN_POINT('Ctrl Pts',(14.0470054900687,-5.44183891826342,
-1121.98897058824));
#162298=CARTESIAN_POINT('Ctrl Pts',(13.4274493703259,-6.68607533664808,
-1123.48308823529));
#162299=CARTESIAN_POINT('Ctrl Pts',(12.8078932505832,-7.93031175503273,
-1124.97720588235));
#162300=CARTESIAN_POINT('Ctrl Pts',(11.9702584092036,-9.03951954568884,
-1126.47132352941));
#162301=CARTESIAN_POINT('Ctrl Pts',(11.132623567824,-10.148727336345,-1127.96544117647));
#162302=CARTESIAN_POINT('Ctrl Pts',(10.1054346546984,-11.0851337583099,
-1129.45955882353));
#162303=CARTESIAN_POINT('Ctrl Pts',(9.07824574157275,-12.0215401802748,
-1130.95367647059));
#162304=CARTESIAN_POINT('Ctrl Pts',(7.89648244316034,-12.7532570359442,
-1132.44779411765));
#162305=CARTESIAN_POINT('Ctrl Pts',(6.71471914474792,-13.4849738916136,
-1133.94191176471));
#162306=CARTESIAN_POINT('Ctrl Pts',(5.4186249928073,-13.9870834410653,-1135.43602941176));
#162307=CARTESIAN_POINT('Ctrl Pts',(4.12253084086667,-14.4891929905171,
-1136.93014705882));
#162308=CARTESIAN_POINT('Ctrl Pts',(2.75624276724855,-14.7445964952585,
-1138.42426470588));
#162309=CARTESIAN_POINT('Ctrl Pts',(1.38995469363045,-15.,-1139.91838235294));
#162310=CARTESIAN_POINT('Ctrl Pts',(0.,-15.,-1141.4125));
#162311=CARTESIAN_POINT('Ctrl Pts',(-1.38995469363045,-15.,-1142.90661764706));
#162312=CARTESIAN_POINT('Ctrl Pts',(-2.75624276724856,-14.7445964952585,
-1144.40073529412));
#162313=CARTESIAN_POINT('Ctrl Pts',(-4.12253084086666,-14.4891929905171,
-1145.89485294118));
#162314=CARTESIAN_POINT('Ctrl Pts',(-5.41862499280729,-13.9870834410653,
-1147.38897058824));
#162315=CARTESIAN_POINT('Ctrl Pts',(-6.71471914474793,-13.4849738916136,
-1148.88308823529));
#162316=CARTESIAN_POINT('Ctrl Pts',(-7.89648244316034,-12.7532570359442,
-1150.37720588235));
#162317=CARTESIAN_POINT('Ctrl Pts',(-9.07824574157275,-12.0215401802748,
-1151.87132352941));
#162318=CARTESIAN_POINT('Ctrl Pts',(-10.1054346546984,-11.0851337583099,
-1153.36544117647));
#162319=CARTESIAN_POINT('Ctrl Pts',(-11.132623567824,-10.148727336345,-1154.85955882353));
#162320=CARTESIAN_POINT('Ctrl Pts',(-11.9702584092036,-9.03951954568885,
-1156.35367647059));
#162321=CARTESIAN_POINT('Ctrl Pts',(-12.8078932505832,-7.93031175503273,
-1157.84779411765));
#162322=CARTESIAN_POINT('Ctrl Pts',(-13.4274493703259,-6.68607533664808,
-1159.34191176471));
#162323=CARTESIAN_POINT('Ctrl Pts',(-14.0470054900687,-5.44183891826343,
-1160.83602941176));
#162324=CARTESIAN_POINT('Ctrl Pts',(-14.4273846475923,-4.10494485108124,
-1162.33014705882));
#162325=CARTESIAN_POINT('Ctrl Pts',(-14.8077638051159,-2.76805078389906,
-1163.82426470588));
#162326=CARTESIAN_POINT('Ctrl Pts',(-14.9360126444255,-1.38402539194953,
-1165.31838235294));
#162327=CARTESIAN_POINT('Ctrl Pts',(-15.0642614837351,-9.22419980378748E-16,
-1166.8125));
#162328=CARTESIAN_POINT('Ctrl Pts',(-14.9360126444255,1.38402539194953,
-1168.30661764706));
#162329=CARTESIAN_POINT('Ctrl Pts',(-14.8077638051159,2.76805078389906,
-1169.80073529412));
#162330=CARTESIAN_POINT('Ctrl Pts',(-14.4273846475923,4.10494485108124,
-1171.29485294118));
#162331=CARTESIAN_POINT('Ctrl Pts',(-14.0470054900687,5.44183891826343,
-1172.78897058824));
#162332=CARTESIAN_POINT('Ctrl Pts',(-13.4274493703259,6.68607533664807,
-1174.28308823529));
#162333=CARTESIAN_POINT('Ctrl Pts',(-12.8078932505832,7.93031175503273,
-1175.77720588235));
#162334=CARTESIAN_POINT('Ctrl Pts',(-11.9702584092036,9.03951954568884,
-1177.27132352941));
#162335=CARTESIAN_POINT('Ctrl Pts',(-11.132623567824,10.148727336345,-1178.76544117647));
#162336=CARTESIAN_POINT('Ctrl Pts',(-10.1054346546984,11.0851337583099,
-1180.25955882353));
#162337=CARTESIAN_POINT('Ctrl Pts',(-9.07824574157275,12.0215401802748,
-1181.75367647059));
#162338=CARTESIAN_POINT('Ctrl Pts',(-7.89648244316034,12.7532570359442,
-1183.24779411765));
#162339=CARTESIAN_POINT('Ctrl Pts',(-6.71471914474793,13.4849738916136,
-1184.74191176471));
#162340=CARTESIAN_POINT('Ctrl Pts',(-5.41862499280729,13.9870834410653,
-1186.23602941176));
#162341=CARTESIAN_POINT('Ctrl Pts',(-4.12253084086667,14.4891929905171,
-1187.73014705882));
#162342=CARTESIAN_POINT('Ctrl Pts',(-2.75624276724856,14.7445964952585,
-1189.22426470588));
#162343=CARTESIAN_POINT('Ctrl Pts',(-1.38995469363044,15.,-1190.71838235294));
#162344=CARTESIAN_POINT('Ctrl Pts',(-1.83697019872103E-15,15.,-1192.2125));
#162345=CARTESIAN_POINT('Ctrl Pts',(1.38995469363045,15.,-1193.70661764706));
#162346=CARTESIAN_POINT('Ctrl Pts',(2.75624276724855,14.7445964952585,-1195.20073529412));
#162347=CARTESIAN_POINT('Ctrl Pts',(4.12253084086666,14.4891929905171,-1196.69485294118));
#162348=CARTESIAN_POINT('Ctrl Pts',(5.4186249928073,13.9870834410653,-1198.18897058824));
#162349=CARTESIAN_POINT('Ctrl Pts',(6.71471914474792,13.4849738916136,-1199.68308823529));
#162350=CARTESIAN_POINT('Ctrl Pts',(7.89648244316034,12.7532570359442,-1201.17720588235));
#162351=CARTESIAN_POINT('Ctrl Pts',(9.07824574157275,12.0215401802748,-1202.67132352941));
#162352=CARTESIAN_POINT('Ctrl Pts',(10.1054346546984,11.0851337583099,-1204.16544117647));
#162353=CARTESIAN_POINT('Ctrl Pts',(11.132623567824,10.148727336345,-1205.65955882353));
#162354=CARTESIAN_POINT('Ctrl Pts',(11.9702584092036,9.03951954568885,-1207.15367647059));
#162355=CARTESIAN_POINT('Ctrl Pts',(12.8078932505832,7.93031175503273,-1208.64779411765));
#162356=CARTESIAN_POINT('Ctrl Pts',(13.4274493703259,6.68607533664807,-1210.14191176471));
#162357=CARTESIAN_POINT('Ctrl Pts',(14.0470054900687,5.44183891826343,-1211.63602941176));
#162358=CARTESIAN_POINT('Ctrl Pts',(14.4273846475923,4.10494485108125,-1213.13014705882));
#162359=CARTESIAN_POINT('Ctrl Pts',(14.8077638051159,2.76805078389905,-1214.62426470588));
#162360=CARTESIAN_POINT('Ctrl Pts',(14.9360126444255,1.38402539194953,-1216.11838235294));
#162361=CARTESIAN_POINT('Ctrl Pts',(15.0642614837351,2.76725994113625E-15,
-1217.6125));
#162362=CARTESIAN_POINT('Ctrl Pts',(14.9360126444255,-1.38402539194952,
-1219.10661764706));
#162363=CARTESIAN_POINT('Ctrl Pts',(14.8077638051159,-2.76805078389906,
-1220.60073529412));
#162364=CARTESIAN_POINT('Ctrl Pts',(14.4273846475923,-4.10494485108124,
-1222.09485294118));
#162365=CARTESIAN_POINT('Ctrl Pts',(14.0470054900687,-5.44183891826342,
-1223.58897058824));
#162366=CARTESIAN_POINT('Ctrl Pts',(13.4274493703259,-6.68607533664808,
-1225.08308823529));
#162367=CARTESIAN_POINT('Ctrl Pts',(12.8078932505832,-7.93031175503273,
-1226.57720588235));
#162368=CARTESIAN_POINT('Ctrl Pts',(11.9702584092036,-9.03951954568884,
-1228.07132352941));
#162369=CARTESIAN_POINT('Ctrl Pts',(11.132623567824,-10.148727336345,-1229.56544117647));
#162370=CARTESIAN_POINT('Ctrl Pts',(10.1054346546984,-11.0851337583099,
-1231.05955882353));
#162371=CARTESIAN_POINT('Ctrl Pts',(9.07824574157275,-12.0215401802748,
-1232.55367647059));
#162372=CARTESIAN_POINT('Ctrl Pts',(7.89648244316034,-12.7532570359442,
-1234.04779411765));
#162373=CARTESIAN_POINT('Ctrl Pts',(6.71471914474792,-13.4849738916136,
-1235.54191176471));
#162374=CARTESIAN_POINT('Ctrl Pts',(5.4186249928073,-13.9870834410653,-1237.03602941176));
#162375=CARTESIAN_POINT('Ctrl Pts',(4.12253084086667,-14.4891929905171,
-1238.53014705882));
#162376=CARTESIAN_POINT('Ctrl Pts',(2.75624276724855,-14.7445964952585,
-1240.02426470588));
#162377=CARTESIAN_POINT('Ctrl Pts',(1.38995469363045,-15.,-1241.51838235294));
#162378=CARTESIAN_POINT('Ctrl Pts',(0.,-15.,-1243.0125));
#162379=CARTESIAN_POINT('Ctrl Pts',(-1.38995469363045,-15.,-1244.50661764706));
#162380=CARTESIAN_POINT('Ctrl Pts',(-2.75624276724856,-14.7445964952585,
-1246.00073529412));
#162381=CARTESIAN_POINT('Ctrl Pts',(-4.12253084086666,-14.4891929905171,
-1247.49485294118));
#162382=CARTESIAN_POINT('Ctrl Pts',(-5.41862499280729,-13.9870834410653,
-1248.98897058824));
#162383=CARTESIAN_POINT('Ctrl Pts',(-6.71471914474793,-13.4849738916136,
-1250.48308823529));
#162384=CARTESIAN_POINT('Ctrl Pts',(-7.89648244316034,-12.7532570359442,
-1251.97720588235));
#162385=CARTESIAN_POINT('Ctrl Pts',(-9.07824574157275,-12.0215401802748,
-1253.47132352941));
#162386=CARTESIAN_POINT('Ctrl Pts',(-10.1054346546984,-11.0851337583099,
-1254.96544117647));
#162387=CARTESIAN_POINT('Ctrl Pts',(-11.132623567824,-10.148727336345,-1256.45955882353));
#162388=CARTESIAN_POINT('Ctrl Pts',(-11.9702584092036,-9.03951954568885,
-1257.95367647059));
#162389=CARTESIAN_POINT('Ctrl Pts',(-12.8078932505832,-7.93031175503273,
-1259.44779411765));
#162390=CARTESIAN_POINT('Ctrl Pts',(-13.4274493703259,-6.68607533664808,
-1260.94191176471));
#162391=CARTESIAN_POINT('Ctrl Pts',(-14.0470054900687,-5.44183891826343,
-1262.43602941176));
#162392=CARTESIAN_POINT('Ctrl Pts',(-14.4273846475923,-4.10494485108124,
-1263.93014705882));
#162393=CARTESIAN_POINT('Ctrl Pts',(-14.8077638051159,-2.76805078389906,
-1265.42426470588));
#162394=CARTESIAN_POINT('Ctrl Pts',(-14.9360126444255,-1.38402539194953,
-1266.91838235294));
#162395=CARTESIAN_POINT('Ctrl Pts',(-15.0642614837351,-9.22419980378748E-16,
-1268.4125));
#162396=CARTESIAN_POINT('Ctrl Pts',(-14.9360126444255,1.38402539194953,
-1269.90661764706));
#162397=CARTESIAN_POINT('Ctrl Pts',(-14.8077638051159,2.76805078389906,
-1271.40073529412));
#162398=CARTESIAN_POINT('Ctrl Pts',(-14.4273846475923,4.10494485108124,
-1272.89485294118));
#162399=CARTESIAN_POINT('Ctrl Pts',(-14.0470054900687,5.44183891826343,
-1274.38897058824));
#162400=CARTESIAN_POINT('Ctrl Pts',(-13.4274493703259,6.68607533664807,
-1275.88308823529));
#162401=CARTESIAN_POINT('Ctrl Pts',(-12.8078932505832,7.93031175503273,
-1277.37720588235));
#162402=CARTESIAN_POINT('Ctrl Pts',(-11.9702584092036,9.03951954568884,
-1278.87132352941));
#162403=CARTESIAN_POINT('Ctrl Pts',(-11.132623567824,10.148727336345,-1280.36544117647));
#162404=CARTESIAN_POINT('Ctrl Pts',(-10.1054346546984,11.0851337583099,
-1281.85955882353));
#162405=CARTESIAN_POINT('Ctrl Pts',(-9.07824574157275,12.0215401802748,
-1283.35367647059));
#162406=CARTESIAN_POINT('Ctrl Pts',(-7.89648244316034,12.7532570359442,
-1284.84779411765));
#162407=CARTESIAN_POINT('Ctrl Pts',(-6.71471914474793,13.4849738916136,
-1286.34191176471));
#162408=CARTESIAN_POINT('Ctrl Pts',(-5.41862499280729,13.9870834410653,
-1287.83602941176));
#162409=CARTESIAN_POINT('Ctrl Pts',(-4.12253084086667,14.4891929905171,
-1289.33014705882));
#162410=CARTESIAN_POINT('Ctrl Pts',(-2.75624276724856,14.7445964952585,
-1290.82426470588));
#162411=CARTESIAN_POINT('Ctrl Pts',(-1.38995469363044,15.,-1292.31838235294));
#162412=CARTESIAN_POINT('Ctrl Pts',(-1.83697019872103E-15,15.,-1293.8125));
#162413=CARTESIAN_POINT('Ctrl Pts',(1.38995469363045,15.,-1295.30661764706));
#162414=CARTESIAN_POINT('Ctrl Pts',(2.75624276724855,14.7445964952585,-1296.80073529412));
#162415=CARTESIAN_POINT('Ctrl Pts',(4.12253084086666,14.4891929905171,-1298.29485294118));
#162416=CARTESIAN_POINT('Ctrl Pts',(5.4186249928073,13.9870834410653,-1299.78897058824));
#162417=CARTESIAN_POINT('Ctrl Pts',(6.71471914474792,13.4849738916136,-1301.28308823529));
#162418=CARTESIAN_POINT('Ctrl Pts',(7.89648244316034,12.7532570359442,-1302.77720588235));
#162419=CARTESIAN_POINT('Ctrl Pts',(9.07824574157275,12.0215401802748,-1304.27132352941));
#162420=CARTESIAN_POINT('Ctrl Pts',(10.1054346546984,11.0851337583099,-1305.76544117647));
#162421=CARTESIAN_POINT('Ctrl Pts',(11.132623567824,10.148727336345,-1307.25955882353));
#162422=CARTESIAN_POINT('Ctrl Pts',(11.9702584092036,9.03951954568885,-1308.75367647059));
#162423=CARTESIAN_POINT('Ctrl Pts',(12.8078932505832,7.93031175503273,-1310.24779411765));
#162424=CARTESIAN_POINT('Ctrl Pts',(13.4274493703259,6.68607533664807,-1311.74191176471));
#162425=CARTESIAN_POINT('Ctrl Pts',(14.0470054900687,5.44183891826343,-1313.23602941176));
#162426=CARTESIAN_POINT('Ctrl Pts',(14.4273846475923,4.10494485108125,-1314.73014705882));
#162427=CARTESIAN_POINT('Ctrl Pts',(14.8077638051159,2.76805078389905,-1316.22426470588));
#162428=CARTESIAN_POINT('Ctrl Pts',(14.9360126444255,1.38402539194953,-1317.71838235294));
#162429=CARTESIAN_POINT('Ctrl Pts',(15.0642614837351,2.76725994113625E-15,
-1319.2125));
#162430=CARTESIAN_POINT('Ctrl Pts',(14.9360126444255,-1.38402539194952,
-1320.70661764706));
#162431=CARTESIAN_POINT('Ctrl Pts',(14.8077638051159,-2.76805078389906,
-1322.20073529412));
#162432=CARTESIAN_POINT('Ctrl Pts',(14.4273846475923,-4.10494485108124,
-1323.69485294118));
#162433=CARTESIAN_POINT('Ctrl Pts',(14.0470054900687,-5.44183891826342,
-1325.18897058824));
#162434=CARTESIAN_POINT('Ctrl Pts',(13.4274493703259,-6.68607533664808,
-1326.68308823529));
#162435=CARTESIAN_POINT('Ctrl Pts',(12.8078932505832,-7.93031175503273,
-1328.17720588235));
#162436=CARTESIAN_POINT('Ctrl Pts',(11.9702584092036,-9.03951954568884,
-1329.67132352941));
#162437=CARTESIAN_POINT('Ctrl Pts',(11.132623567824,-10.148727336345,-1331.16544117647));
#162438=CARTESIAN_POINT('Ctrl Pts',(10.1054346546984,-11.0851337583099,
-1332.65955882353));
#162439=CARTESIAN_POINT('Ctrl Pts',(9.07824574157275,-12.0215401802748,
-1334.15367647059));
#162440=CARTESIAN_POINT('Ctrl Pts',(7.89648244316034,-12.7532570359442,
-1335.64779411765));
#162441=CARTESIAN_POINT('Ctrl Pts',(6.71471914474792,-13.4849738916136,
-1337.14191176471));
#162442=CARTESIAN_POINT('Ctrl Pts',(5.4186249928073,-13.9870834410653,-1338.63602941176));
#162443=CARTESIAN_POINT('Ctrl Pts',(4.12253084086667,-14.4891929905171,
-1340.13014705882));
#162444=CARTESIAN_POINT('Ctrl Pts',(2.75624276724855,-14.7445964952585,
-1341.62426470588));
#162445=CARTESIAN_POINT('Ctrl Pts',(1.38995469363045,-15.,-1343.11838235294));
#162446=CARTESIAN_POINT('Ctrl Pts',(0.,-15.,-1344.6125));
#162447=CARTESIAN_POINT('Ctrl Pts',(-1.38995469363045,-15.,-1346.10661764706));
#162448=CARTESIAN_POINT('Ctrl Pts',(-2.75624276724856,-14.7445964952585,
-1347.60073529412));
#162449=CARTESIAN_POINT('Ctrl Pts',(-4.12253084086666,-14.4891929905171,
-1349.09485294118));
#162450=CARTESIAN_POINT('Ctrl Pts',(-5.41862499280729,-13.9870834410653,
-1350.58897058824));
#162451=CARTESIAN_POINT('Ctrl Pts',(-6.71471914474793,-13.4849738916136,
-1352.08308823529));
#162452=CARTESIAN_POINT('Ctrl Pts',(-7.89648244316034,-12.7532570359442,
-1353.57720588235));
#162453=CARTESIAN_POINT('Ctrl Pts',(-9.07824574157275,-12.0215401802748,
-1355.07132352941));
#162454=CARTESIAN_POINT('Ctrl Pts',(-10.1054346546984,-11.0851337583099,
-1356.56544117647));
#162455=CARTESIAN_POINT('Ctrl Pts',(-11.132623567824,-10.148727336345,-1358.05955882353));
#162456=CARTESIAN_POINT('Ctrl Pts',(-11.9702584092036,-9.03951954568885,
-1359.55367647059));
#162457=CARTESIAN_POINT('Ctrl Pts',(-12.8078932505832,-7.93031175503273,
-1361.04779411765));
#162458=CARTESIAN_POINT('Ctrl Pts',(-13.4274493703259,-6.68607533664808,
-1362.54191176471));
#162459=CARTESIAN_POINT('Ctrl Pts',(-14.0470054900687,-5.44183891826343,
-1364.03602941176));
#162460=CARTESIAN_POINT('Ctrl Pts',(-14.4273846475923,-4.10494485108124,
-1365.53014705882));
#162461=CARTESIAN_POINT('Ctrl Pts',(-14.8077638051159,-2.76805078389906,
-1367.02426470588));
#162462=CARTESIAN_POINT('Ctrl Pts',(-14.9360126444255,-1.38402539194953,
-1368.51838235294));
#162463=CARTESIAN_POINT('Ctrl Pts',(-15.0642614837351,-9.22419980378748E-16,
-1370.0125));
#162464=CARTESIAN_POINT('Ctrl Pts',(-14.9360126444255,1.38402539194953,
-1371.50661764706));
#162465=CARTESIAN_POINT('Ctrl Pts',(-14.8077638051159,2.76805078389906,
-1373.00073529412));
#162466=CARTESIAN_POINT('Ctrl Pts',(-14.4273846475923,4.10494485108124,
-1374.49485294118));
#162467=CARTESIAN_POINT('Ctrl Pts',(-14.0470054900687,5.44183891826343,
-1375.98897058824));
#162468=CARTESIAN_POINT('Ctrl Pts',(-13.4274493703259,6.68607533664807,
-1377.48308823529));
#162469=CARTESIAN_POINT('Ctrl Pts',(-12.8078932505832,7.93031175503273,
-1378.97720588235));
#162470=CARTESIAN_POINT('Ctrl Pts',(-11.9702584092036,9.03951954568884,
-1380.47132352941));
#162471=CARTESIAN_POINT('Ctrl Pts',(-11.132623567824,10.148727336345,-1381.96544117647));
#162472=CARTESIAN_POINT('Ctrl Pts',(-10.1054346546984,11.0851337583099,
-1383.45955882353));
#162473=CARTESIAN_POINT('Ctrl Pts',(-9.07824574157275,12.0215401802748,
-1384.95367647059));
#162474=CARTESIAN_POINT('Ctrl Pts',(-7.89648244316034,12.7532570359442,
-1386.44779411765));
#162475=CARTESIAN_POINT('Ctrl Pts',(-6.71471914474793,13.4849738916136,
-1387.94191176471));
#162476=CARTESIAN_POINT('Ctrl Pts',(-5.41862499280729,13.9870834410653,
-1389.43602941176));
#162477=CARTESIAN_POINT('Ctrl Pts',(-4.12253084086667,14.4891929905171,
-1390.93014705882));
#162478=CARTESIAN_POINT('Ctrl Pts',(-2.75624276724856,14.7445964952585,
-1392.42426470588));
#162479=CARTESIAN_POINT('Ctrl Pts',(-1.38995469363044,15.,-1393.91838235294));
#162480=CARTESIAN_POINT('Ctrl Pts',(-1.83697019872103E-15,15.,-1395.4125));
#162481=CARTESIAN_POINT('Ctrl Pts',(1.38995469363045,15.,-1396.90661764706));
#162482=CARTESIAN_POINT('Ctrl Pts',(2.75624276724855,14.7445964952585,-1398.40073529412));
#162483=CARTESIAN_POINT('Ctrl Pts',(4.12253084086666,14.4891929905171,-1399.89485294118));
#162484=CARTESIAN_POINT('Ctrl Pts',(5.4186249928073,13.9870834410653,-1401.38897058824));
#162485=CARTESIAN_POINT('Ctrl Pts',(6.71471914474792,13.4849738916136,-1402.88308823529));
#162486=CARTESIAN_POINT('Ctrl Pts',(7.89648244316034,12.7532570359442,-1404.37720588235));
#162487=CARTESIAN_POINT('Ctrl Pts',(9.07824574157275,12.0215401802748,-1405.87132352941));
#162488=CARTESIAN_POINT('Ctrl Pts',(10.1054346546984,11.0851337583099,-1407.36544117647));
#162489=CARTESIAN_POINT('Ctrl Pts',(11.132623567824,10.148727336345,-1408.85955882353));
#162490=CARTESIAN_POINT('Ctrl Pts',(11.9702584092036,9.03951954568885,-1410.35367647059));
#162491=CARTESIAN_POINT('Ctrl Pts',(12.8078932505832,7.93031175503273,-1411.84779411765));
#162492=CARTESIAN_POINT('Ctrl Pts',(13.4274493703259,6.68607533664807,-1413.34191176471));
#162493=CARTESIAN_POINT('Ctrl Pts',(14.0470054900687,5.44183891826343,-1414.83602941176));
#162494=CARTESIAN_POINT('Ctrl Pts',(14.4273846475923,4.10494485108125,-1416.33014705882));
#162495=CARTESIAN_POINT('Ctrl Pts',(14.8077638051159,2.76805078389905,-1417.82426470588));
#162496=CARTESIAN_POINT('Ctrl Pts',(14.9360126444255,1.38402539194953,-1419.31838235294));
#162497=CARTESIAN_POINT('Ctrl Pts',(15.0642614837351,2.76725994113625E-15,
-1420.8125));
#162498=CARTESIAN_POINT('Ctrl Pts',(14.9360126444255,-1.38402539194952,
-1422.30661764706));
#162499=CARTESIAN_POINT('Ctrl Pts',(14.8077638051159,-2.76805078389906,
-1423.80073529412));
#162500=CARTESIAN_POINT('Ctrl Pts',(14.4273846475923,-4.10494485108124,
-1425.29485294118));
#162501=CARTESIAN_POINT('Ctrl Pts',(14.0470054900687,-5.44183891826342,
-1426.78897058824));
#162502=CARTESIAN_POINT('Ctrl Pts',(13.4274493703259,-6.68607533664808,
-1428.28308823529));
#162503=CARTESIAN_POINT('Ctrl Pts',(12.8078932505832,-7.93031175503273,
-1429.77720588235));
#162504=CARTESIAN_POINT('Ctrl Pts',(11.9702584092036,-9.03951954568884,
-1431.27132352941));
#162505=CARTESIAN_POINT('Ctrl Pts',(11.132623567824,-10.148727336345,-1432.76544117647));
#162506=CARTESIAN_POINT('Ctrl Pts',(10.1054346546984,-11.0851337583099,
-1434.25955882353));
#162507=CARTESIAN_POINT('Ctrl Pts',(9.07824574157275,-12.0215401802748,
-1435.75367647059));
#162508=CARTESIAN_POINT('Ctrl Pts',(7.89648244316034,-12.7532570359442,
-1437.24779411765));
#162509=CARTESIAN_POINT('Ctrl Pts',(6.71471914474792,-13.4849738916136,
-1438.74191176471));
#162510=CARTESIAN_POINT('Ctrl Pts',(5.4186249928073,-13.9870834410653,-1440.23602941176));
#162511=CARTESIAN_POINT('Ctrl Pts',(4.12253084086667,-14.4891929905171,
-1441.73014705882));
#162512=CARTESIAN_POINT('Ctrl Pts',(2.75624276724855,-14.7445964952585,
-1443.22426470588));
#162513=CARTESIAN_POINT('Ctrl Pts',(1.38995469363045,-15.,-1444.71838235294));
#162514=CARTESIAN_POINT('Ctrl Pts',(0.,-15.,-1446.2125));
#162515=CARTESIAN_POINT('Ctrl Pts',(-1.38995469363045,-15.,-1447.70661764706));
#162516=CARTESIAN_POINT('Ctrl Pts',(-2.75624276724856,-14.7445964952585,
-1449.20073529412));
#162517=CARTESIAN_POINT('Ctrl Pts',(-4.12253084086666,-14.4891929905171,
-1450.69485294118));
#162518=CARTESIAN_POINT('Ctrl Pts',(-5.41862499280729,-13.9870834410653,
-1452.18897058824));
#162519=CARTESIAN_POINT('Ctrl Pts',(-6.71471914474793,-13.4849738916136,
-1453.68308823529));
#162520=CARTESIAN_POINT('Ctrl Pts',(-7.89648244316034,-12.7532570359442,
-1455.17720588235));
#162521=CARTESIAN_POINT('Ctrl Pts',(-9.07824574157275,-12.0215401802748,
-1456.67132352941));
#162522=CARTESIAN_POINT('Ctrl Pts',(-10.1054346546984,-11.0851337583099,
-1458.16544117647));
#162523=CARTESIAN_POINT('Ctrl Pts',(-11.132623567824,-10.148727336345,-1459.65955882353));
#162524=CARTESIAN_POINT('Ctrl Pts',(-11.9702584092036,-9.03951954568885,
-1461.15367647059));
#162525=CARTESIAN_POINT('Ctrl Pts',(-12.8078932505832,-7.93031175503273,
-1462.64779411765));
#162526=CARTESIAN_POINT('Ctrl Pts',(-13.4274493703259,-6.68607533664808,
-1464.14191176471));
#162527=CARTESIAN_POINT('Ctrl Pts',(-14.0470054900687,-5.44183891826343,
-1465.63602941176));
#162528=CARTESIAN_POINT('Ctrl Pts',(-14.4273846475923,-4.10494485108124,
-1467.13014705882));
#162529=CARTESIAN_POINT('Ctrl Pts',(-14.8077638051159,-2.76805078389906,
-1468.62426470588));
#162530=CARTESIAN_POINT('Ctrl Pts',(-14.9360126444255,-1.38402539194953,
-1470.11838235294));
#162531=CARTESIAN_POINT('Ctrl Pts',(-15.0642614837351,-9.22419980378748E-16,
-1471.6125));
#162532=CARTESIAN_POINT('Ctrl Pts',(-14.9360126444255,1.38402539194953,
-1473.10661764706));
#162533=CARTESIAN_POINT('Ctrl Pts',(-14.8077638051159,2.76805078389906,
-1474.60073529412));
#162534=CARTESIAN_POINT('Ctrl Pts',(-14.4273846475923,4.10494485108124,
-1476.09485294118));
#162535=CARTESIAN_POINT('Ctrl Pts',(-14.0470054900687,5.44183891826343,
-1477.58897058824));
#162536=CARTESIAN_POINT('Ctrl Pts',(-13.4274493703259,6.68607533664807,
-1479.08308823529));
#162537=CARTESIAN_POINT('Ctrl Pts',(-12.8078932505832,7.93031175503273,
-1480.57720588235));
#162538=CARTESIAN_POINT('Ctrl Pts',(-11.9702584092036,9.03951954568884,
-1482.07132352941));
#162539=CARTESIAN_POINT('Ctrl Pts',(-11.132623567824,10.148727336345,-1483.56544117647));
#162540=CARTESIAN_POINT('Ctrl Pts',(-10.1054346546984,11.0851337583099,
-1485.05955882353));
#162541=CARTESIAN_POINT('Ctrl Pts',(-9.07824574157275,12.0215401802748,
-1486.55367647059));
#162542=CARTESIAN_POINT('Ctrl Pts',(-7.89648244316034,12.7532570359442,
-1488.04779411765));
#162543=CARTESIAN_POINT('Ctrl Pts',(-6.71471914474793,13.4849738916136,
-1489.54191176471));
#162544=CARTESIAN_POINT('Ctrl Pts',(-5.41862499280729,13.9870834410653,
-1491.03602941176));
#162545=CARTESIAN_POINT('Ctrl Pts',(-4.12253084086667,14.4891929905171,
-1492.53014705882));
#162546=CARTESIAN_POINT('Ctrl Pts',(-2.75624276724856,14.7445964952585,
-1494.02426470588));
#162547=CARTESIAN_POINT('Ctrl Pts',(-1.38995469363044,15.,-1495.51838235294));
#162548=CARTESIAN_POINT('Ctrl Pts',(-1.83697019872103E-15,15.,-1497.0125));
#162549=CARTESIAN_POINT('Ctrl Pts',(1.38995469363045,15.,-1498.50661764706));
#162550=CARTESIAN_POINT('Ctrl Pts',(2.75624276724855,14.7445964952585,-1500.00073529412));
#162551=CARTESIAN_POINT('Ctrl Pts',(4.12253084086666,14.4891929905171,-1501.49485294118));
#162552=CARTESIAN_POINT('Ctrl Pts',(5.4186249928073,13.9870834410653,-1502.98897058824));
#162553=CARTESIAN_POINT('Ctrl Pts',(6.26768981235257,13.6581539776009,-1503.96775961254));
#162554=CARTESIAN_POINT('Ctrl Pts',(7.0707324233642,13.2289358225515,-1504.9503325767));
#162555=CARTESIAN_POINT('',(5.07842733458062,-17.3187724682607,692.));
#162556=CARTESIAN_POINT('Ctrl Pts',(4.22076739908463,-14.3939265859884,
691.999999999999));
#162557=CARTESIAN_POINT('Ctrl Pts',(4.36371072147063,-14.881400899031,691.999999999999));
#162558=CARTESIAN_POINT('Ctrl Pts',(4.50665404385759,-15.3688752120733,
692.));
#162559=CARTESIAN_POINT('Ctrl Pts',(4.79254068902232,-16.3438238394976,
692.));
#162560=CARTESIAN_POINT('Ctrl Pts',(4.9354840118019,-16.831298153879,692.000000000001));
#162561=CARTESIAN_POINT('Ctrl Pts',(5.07842733458062,-17.3187724682607,
692.000000000001));
#162562=CARTESIAN_POINT('',(0.,-18.048,1500.1875));
#162563=CARTESIAN_POINT('',(0.,-18.048,1500.1875));
#162564=CARTESIAN_POINT('Ctrl Pts',(0.,-18.048,1500.1875));
#162565=CARTESIAN_POINT('Ctrl Pts',(-1.67239348737614,-18.048,1498.69338235294));
#162566=CARTESIAN_POINT('Ctrl Pts',(-3.31631129755346,-17.7406985030951,
1497.19926470588));
#162567=CARTESIAN_POINT('Ctrl Pts',(-4.96022910773077,-17.4333970061901,
1495.70514705882));
#162568=CARTESIAN_POINT('Ctrl Pts',(-6.51968959134574,-16.8292587962898,
1494.21102941176));
#162569=CARTESIAN_POINT('Ctrl Pts',(-8.07915007496071,-16.2251205863895,
1492.71691176471));
#162570=CARTESIAN_POINT('Ctrl Pts',(-9.50104767561052,-15.3447188656481,
1491.22279411765));
#162571=CARTESIAN_POINT('Ctrl Pts',(-10.9229452762603,-14.4643171449067,
1489.72867647059));
#162572=CARTESIAN_POINT('Ctrl Pts',(-12.1588589765331,-13.3376329379985,
1488.23455882353));
#162573=CARTESIAN_POINT('Ctrl Pts',(-13.3947726768058,-12.2109487310903,
1486.74044117647));
#162574=CARTESIAN_POINT('Ctrl Pts',(-14.4026149179538,-10.8763499173728,
1485.24632352941));
#162575=CARTESIAN_POINT('Ctrl Pts',(-15.4104571591017,-9.54175110365538,
1483.75220588235));
#162576=CARTESIAN_POINT('Ctrl Pts',(-16.1559070823762,-8.04468584505497,
1482.25808823529));
#162577=CARTESIAN_POINT('Ctrl Pts',(-16.9013570056506,-6.54762058645456,
1480.76397058824));
#162578=CARTESIAN_POINT('Ctrl Pts',(-17.3590292079831,-4.93906964482095,
1479.26985294118));
#162579=CARTESIAN_POINT('Ctrl Pts',(-17.8167014103155,-3.33051870318735,
1477.77573529412));
#162580=CARTESIAN_POINT('Ctrl Pts',(-17.9710104137728,-1.66525935159368,
1476.28161764706));
#162581=CARTESIAN_POINT('Ctrl Pts',(-18.1253194172301,-1.10985572039171E-15,
1474.7875));
#162582=CARTESIAN_POINT('Ctrl Pts',(-17.9710104137728,1.66525935159367,
1473.29338235294));
#162583=CARTESIAN_POINT('Ctrl Pts',(-17.8167014103155,3.33051870318735,
1471.79926470588));
#162584=CARTESIAN_POINT('Ctrl Pts',(-17.3590292079831,4.93906964482096,
1470.30514705882));
#162585=CARTESIAN_POINT('Ctrl Pts',(-16.9013570056506,6.54762058645456,
1468.81102941176));
#162586=CARTESIAN_POINT('Ctrl Pts',(-16.1559070823762,8.04468584505497,
1467.31691176471));
#162587=CARTESIAN_POINT('Ctrl Pts',(-15.4104571591017,9.54175110365538,
1465.82279411765));
#162588=CARTESIAN_POINT('Ctrl Pts',(-14.4026149179538,10.8763499173728,
1464.32867647059));
#162589=CARTESIAN_POINT('Ctrl Pts',(-13.3947726768058,12.2109487310903,
1462.83455882353));
#162590=CARTESIAN_POINT('Ctrl Pts',(-12.1588589765331,13.3376329379985,
1461.34044117647));
#162591=CARTESIAN_POINT('Ctrl Pts',(-10.9229452762603,14.4643171449067,
1459.84632352941));
#162592=CARTESIAN_POINT('Ctrl Pts',(-9.50104767561052,15.3447188656481,
1458.35220588235));
#162593=CARTESIAN_POINT('Ctrl Pts',(-8.07915007496071,16.2251205863895,
1456.85808823529));
#162594=CARTESIAN_POINT('Ctrl Pts',(-6.51968959134574,16.8292587962898,
1455.36397058824));
#162595=CARTESIAN_POINT('Ctrl Pts',(-4.96022910773078,17.4333970061901,
1453.86985294118));
#162596=CARTESIAN_POINT('Ctrl Pts',(-3.31631129755346,17.7406985030951,
1452.37573529412));
#162597=CARTESIAN_POINT('Ctrl Pts',(-1.67239348737615,18.048,1450.88161764706));
#162598=CARTESIAN_POINT('Ctrl Pts',(-2.21024254310115E-15,18.048,1449.3875));
#162599=CARTESIAN_POINT('Ctrl Pts',(1.67239348737616,18.048,1447.89338235294));
#162600=CARTESIAN_POINT('Ctrl Pts',(3.31631129755346,17.7406985030951,1446.39926470588));
#162601=CARTESIAN_POINT('Ctrl Pts',(4.96022910773077,17.4333970061901,1444.90514705882));
#162602=CARTESIAN_POINT('Ctrl Pts',(6.51968959134575,16.8292587962898,1443.41102941176));
#162603=CARTESIAN_POINT('Ctrl Pts',(8.07915007496071,16.2251205863895,1441.91691176471));
#162604=CARTESIAN_POINT('Ctrl Pts',(9.50104767561053,15.3447188656481,1440.42279411765));
#162605=CARTESIAN_POINT('Ctrl Pts',(10.9229452762603,14.4643171449067,1438.92867647059));
#162606=CARTESIAN_POINT('Ctrl Pts',(12.1588589765331,13.3376329379985,1437.43455882353));
#162607=CARTESIAN_POINT('Ctrl Pts',(13.3947726768058,12.2109487310903,1435.94044117647));
#162608=CARTESIAN_POINT('Ctrl Pts',(14.4026149179538,10.8763499173728,1434.44632352941));
#162609=CARTESIAN_POINT('Ctrl Pts',(15.4104571591017,9.54175110365539,1432.95220588235));
#162610=CARTESIAN_POINT('Ctrl Pts',(16.1559070823762,8.04468584505496,1431.45808823529));
#162611=CARTESIAN_POINT('Ctrl Pts',(16.9013570056506,6.54762058645456,1429.96397058824));
#162612=CARTESIAN_POINT('Ctrl Pts',(17.3590292079831,4.93906964482096,1428.46985294118));
#162613=CARTESIAN_POINT('Ctrl Pts',(17.8167014103155,3.33051870318735,1426.97573529412));
#162614=CARTESIAN_POINT('Ctrl Pts',(17.9710104137728,1.66525935159367,1425.48161764706));
#162615=CARTESIAN_POINT('Ctrl Pts',(18.1253194172301,3.32956716117513E-15,
1423.9875));
#162616=CARTESIAN_POINT('Ctrl Pts',(17.9710104137728,-1.66525935159367,
1422.49338235294));
#162617=CARTESIAN_POINT('Ctrl Pts',(17.8167014103155,-3.33051870318736,
1420.99926470588));
#162618=CARTESIAN_POINT('Ctrl Pts',(17.3590292079831,-4.93906964482095,
1419.50514705882));
#162619=CARTESIAN_POINT('Ctrl Pts',(16.9013570056506,-6.54762058645456,
1418.01102941176));
#162620=CARTESIAN_POINT('Ctrl Pts',(16.1559070823762,-8.04468584505497,
1416.51691176471));
#162621=CARTESIAN_POINT('Ctrl Pts',(15.4104571591017,-9.54175110365538,
1415.02279411765));
#162622=CARTESIAN_POINT('Ctrl Pts',(14.4026149179538,-10.8763499173728,
1413.52867647059));
#162623=CARTESIAN_POINT('Ctrl Pts',(13.3947726768058,-12.2109487310903,
1412.03455882353));
#162624=CARTESIAN_POINT('Ctrl Pts',(12.1588589765331,-13.3376329379985,
1410.54044117647));
#162625=CARTESIAN_POINT('Ctrl Pts',(10.9229452762603,-14.4643171449067,
1409.04632352941));
#162626=CARTESIAN_POINT('Ctrl Pts',(9.50104767561053,-15.3447188656481,
1407.55220588235));
#162627=CARTESIAN_POINT('Ctrl Pts',(8.07915007496071,-16.2251205863895,
1406.05808823529));
#162628=CARTESIAN_POINT('Ctrl Pts',(6.51968959134574,-16.8292587962898,
1404.56397058824));
#162629=CARTESIAN_POINT('Ctrl Pts',(4.96022910773078,-17.4333970061901,
1403.06985294118));
#162630=CARTESIAN_POINT('Ctrl Pts',(3.31631129755346,-17.7406985030951,
1401.57573529412));
#162631=CARTESIAN_POINT('Ctrl Pts',(1.67239348737615,-18.048,1400.08161764706));
#162632=CARTESIAN_POINT('Ctrl Pts',(0.,-18.048,1398.5875));
#162633=CARTESIAN_POINT('Ctrl Pts',(-1.67239348737615,-18.048,1397.09338235294));
#162634=CARTESIAN_POINT('Ctrl Pts',(-3.31631129755346,-17.7406985030951,
1395.59926470588));
#162635=CARTESIAN_POINT('Ctrl Pts',(-4.96022910773077,-17.4333970061901,
1394.10514705882));
#162636=CARTESIAN_POINT('Ctrl Pts',(-6.51968959134574,-16.8292587962898,
1392.61102941176));
#162637=CARTESIAN_POINT('Ctrl Pts',(-8.07915007496071,-16.2251205863895,
1391.11691176471));
#162638=CARTESIAN_POINT('Ctrl Pts',(-9.50104767561052,-15.3447188656481,
1389.62279411765));
#162639=CARTESIAN_POINT('Ctrl Pts',(-10.9229452762603,-14.4643171449067,
1388.12867647059));
#162640=CARTESIAN_POINT('Ctrl Pts',(-12.1588589765331,-13.3376329379985,
1386.63455882353));
#162641=CARTESIAN_POINT('Ctrl Pts',(-13.3947726768058,-12.2109487310903,
1385.14044117647));
#162642=CARTESIAN_POINT('Ctrl Pts',(-14.4026149179538,-10.8763499173728,
1383.64632352941));
#162643=CARTESIAN_POINT('Ctrl Pts',(-15.4104571591017,-9.54175110365538,
1382.15220588235));
#162644=CARTESIAN_POINT('Ctrl Pts',(-16.1559070823762,-8.04468584505497,
1380.65808823529));
#162645=CARTESIAN_POINT('Ctrl Pts',(-16.9013570056506,-6.54762058645456,
1379.16397058824));
#162646=CARTESIAN_POINT('Ctrl Pts',(-17.3590292079831,-4.93906964482095,
1377.66985294118));
#162647=CARTESIAN_POINT('Ctrl Pts',(-17.8167014103155,-3.33051870318735,
1376.17573529412));
#162648=CARTESIAN_POINT('Ctrl Pts',(-17.9710104137728,-1.66525935159368,
1374.68161764706));
#162649=CARTESIAN_POINT('Ctrl Pts',(-18.1253194172301,-1.10985572039171E-15,
1373.1875));
#162650=CARTESIAN_POINT('Ctrl Pts',(-17.9710104137728,1.66525935159367,
1371.69338235294));
#162651=CARTESIAN_POINT('Ctrl Pts',(-17.8167014103155,3.33051870318735,
1370.19926470588));
#162652=CARTESIAN_POINT('Ctrl Pts',(-17.3590292079831,4.93906964482096,
1368.70514705882));
#162653=CARTESIAN_POINT('Ctrl Pts',(-16.9013570056506,6.54762058645456,
1367.21102941176));
#162654=CARTESIAN_POINT('Ctrl Pts',(-16.1559070823762,8.04468584505497,
1365.71691176471));
#162655=CARTESIAN_POINT('Ctrl Pts',(-15.4104571591017,9.54175110365538,
1364.22279411765));
#162656=CARTESIAN_POINT('Ctrl Pts',(-14.4026149179538,10.8763499173728,
1362.72867647059));
#162657=CARTESIAN_POINT('Ctrl Pts',(-13.3947726768058,12.2109487310903,
1361.23455882353));
#162658=CARTESIAN_POINT('Ctrl Pts',(-12.1588589765331,13.3376329379985,
1359.74044117647));
#162659=CARTESIAN_POINT('Ctrl Pts',(-10.9229452762603,14.4643171449067,
1358.24632352941));
#162660=CARTESIAN_POINT('Ctrl Pts',(-9.50104767561052,15.3447188656481,
1356.75220588235));
#162661=CARTESIAN_POINT('Ctrl Pts',(-8.07915007496071,16.2251205863895,
1355.25808823529));
#162662=CARTESIAN_POINT('Ctrl Pts',(-6.51968959134574,16.8292587962898,
1353.76397058824));
#162663=CARTESIAN_POINT('Ctrl Pts',(-4.96022910773078,17.4333970061901,
1352.26985294118));
#162664=CARTESIAN_POINT('Ctrl Pts',(-3.31631129755346,17.7406985030951,
1350.77573529412));
#162665=CARTESIAN_POINT('Ctrl Pts',(-1.67239348737615,18.048,1349.28161764706));
#162666=CARTESIAN_POINT('Ctrl Pts',(-2.21024254310115E-15,18.048,1347.7875));
#162667=CARTESIAN_POINT('Ctrl Pts',(1.67239348737616,18.048,1346.29338235294));
#162668=CARTESIAN_POINT('Ctrl Pts',(3.31631129755346,17.7406985030951,1344.79926470588));
#162669=CARTESIAN_POINT('Ctrl Pts',(4.96022910773077,17.4333970061901,1343.30514705882));
#162670=CARTESIAN_POINT('Ctrl Pts',(6.51968959134575,16.8292587962898,1341.81102941176));
#162671=CARTESIAN_POINT('Ctrl Pts',(8.07915007496071,16.2251205863895,1340.31691176471));
#162672=CARTESIAN_POINT('Ctrl Pts',(9.50104767561053,15.3447188656481,1338.82279411765));
#162673=CARTESIAN_POINT('Ctrl Pts',(10.9229452762603,14.4643171449067,1337.32867647059));
#162674=CARTESIAN_POINT('Ctrl Pts',(12.1588589765331,13.3376329379985,1335.83455882353));
#162675=CARTESIAN_POINT('Ctrl Pts',(13.3947726768058,12.2109487310903,1334.34044117647));
#162676=CARTESIAN_POINT('Ctrl Pts',(14.4026149179538,10.8763499173728,1332.84632352941));
#162677=CARTESIAN_POINT('Ctrl Pts',(15.4104571591017,9.54175110365539,1331.35220588235));
#162678=CARTESIAN_POINT('Ctrl Pts',(16.1559070823762,8.04468584505496,1329.85808823529));
#162679=CARTESIAN_POINT('Ctrl Pts',(16.9013570056506,6.54762058645456,1328.36397058824));
#162680=CARTESIAN_POINT('Ctrl Pts',(17.3590292079831,4.93906964482096,1326.86985294118));
#162681=CARTESIAN_POINT('Ctrl Pts',(17.8167014103155,3.33051870318735,1325.37573529412));
#162682=CARTESIAN_POINT('Ctrl Pts',(17.9710104137728,1.66525935159367,1323.88161764706));
#162683=CARTESIAN_POINT('Ctrl Pts',(18.1253194172301,3.32956716117513E-15,
1322.3875));
#162684=CARTESIAN_POINT('Ctrl Pts',(17.9710104137728,-1.66525935159367,
1320.89338235294));
#162685=CARTESIAN_POINT('Ctrl Pts',(17.8167014103155,-3.33051870318736,
1319.39926470588));
#162686=CARTESIAN_POINT('Ctrl Pts',(17.3590292079831,-4.93906964482095,
1317.90514705882));
#162687=CARTESIAN_POINT('Ctrl Pts',(16.9013570056506,-6.54762058645456,
1316.41102941176));
#162688=CARTESIAN_POINT('Ctrl Pts',(16.1559070823762,-8.04468584505497,
1314.91691176471));
#162689=CARTESIAN_POINT('Ctrl Pts',(15.4104571591017,-9.54175110365538,
1313.42279411765));
#162690=CARTESIAN_POINT('Ctrl Pts',(14.4026149179538,-10.8763499173728,
1311.92867647059));
#162691=CARTESIAN_POINT('Ctrl Pts',(13.3947726768058,-12.2109487310903,
1310.43455882353));
#162692=CARTESIAN_POINT('Ctrl Pts',(12.1588589765331,-13.3376329379985,
1308.94044117647));
#162693=CARTESIAN_POINT('Ctrl Pts',(10.9229452762603,-14.4643171449067,
1307.44632352941));
#162694=CARTESIAN_POINT('Ctrl Pts',(9.50104767561053,-15.3447188656481,
1305.95220588235));
#162695=CARTESIAN_POINT('Ctrl Pts',(8.07915007496071,-16.2251205863895,
1304.45808823529));
#162696=CARTESIAN_POINT('Ctrl Pts',(6.51968959134574,-16.8292587962898,
1302.96397058824));
#162697=CARTESIAN_POINT('Ctrl Pts',(4.96022910773078,-17.4333970061901,
1301.46985294118));
#162698=CARTESIAN_POINT('Ctrl Pts',(3.31631129755346,-17.7406985030951,
1299.97573529412));
#162699=CARTESIAN_POINT('Ctrl Pts',(1.67239348737615,-18.048,1298.48161764706));
#162700=CARTESIAN_POINT('Ctrl Pts',(0.,-18.048,1296.9875));
#162701=CARTESIAN_POINT('Ctrl Pts',(-1.67239348737615,-18.048,1295.49338235294));
#162702=CARTESIAN_POINT('Ctrl Pts',(-3.31631129755346,-17.7406985030951,
1293.99926470588));
#162703=CARTESIAN_POINT('Ctrl Pts',(-4.96022910773077,-17.4333970061901,
1292.50514705882));
#162704=CARTESIAN_POINT('Ctrl Pts',(-6.51968959134574,-16.8292587962898,
1291.01102941176));
#162705=CARTESIAN_POINT('Ctrl Pts',(-8.07915007496071,-16.2251205863895,
1289.51691176471));
#162706=CARTESIAN_POINT('Ctrl Pts',(-9.50104767561052,-15.3447188656481,
1288.02279411765));
#162707=CARTESIAN_POINT('Ctrl Pts',(-10.9229452762603,-14.4643171449067,
1286.52867647059));
#162708=CARTESIAN_POINT('Ctrl Pts',(-12.1588589765331,-13.3376329379985,
1285.03455882353));
#162709=CARTESIAN_POINT('Ctrl Pts',(-13.3947726768058,-12.2109487310903,
1283.54044117647));
#162710=CARTESIAN_POINT('Ctrl Pts',(-14.4026149179538,-10.8763499173728,
1282.04632352941));
#162711=CARTESIAN_POINT('Ctrl Pts',(-15.4104571591017,-9.54175110365538,
1280.55220588235));
#162712=CARTESIAN_POINT('Ctrl Pts',(-16.1559070823762,-8.04468584505497,
1279.05808823529));
#162713=CARTESIAN_POINT('Ctrl Pts',(-16.9013570056506,-6.54762058645456,
1277.56397058824));
#162714=CARTESIAN_POINT('Ctrl Pts',(-17.3590292079831,-4.93906964482095,
1276.06985294118));
#162715=CARTESIAN_POINT('Ctrl Pts',(-17.8167014103155,-3.33051870318735,
1274.57573529412));
#162716=CARTESIAN_POINT('Ctrl Pts',(-17.9710104137728,-1.66525935159368,
1273.08161764706));
#162717=CARTESIAN_POINT('Ctrl Pts',(-18.1253194172301,-1.10985572039171E-15,
1271.5875));
#162718=CARTESIAN_POINT('Ctrl Pts',(-17.9710104137728,1.66525935159367,
1270.09338235294));
#162719=CARTESIAN_POINT('Ctrl Pts',(-17.8167014103155,3.33051870318735,
1268.59926470588));
#162720=CARTESIAN_POINT('Ctrl Pts',(-17.3590292079831,4.93906964482096,
1267.10514705882));
#162721=CARTESIAN_POINT('Ctrl Pts',(-16.9013570056506,6.54762058645456,
1265.61102941176));
#162722=CARTESIAN_POINT('Ctrl Pts',(-16.1559070823762,8.04468584505497,
1264.11691176471));
#162723=CARTESIAN_POINT('Ctrl Pts',(-15.4104571591017,9.54175110365538,
1262.62279411765));
#162724=CARTESIAN_POINT('Ctrl Pts',(-14.4026149179538,10.8763499173728,
1261.12867647059));
#162725=CARTESIAN_POINT('Ctrl Pts',(-13.3947726768058,12.2109487310903,
1259.63455882353));
#162726=CARTESIAN_POINT('Ctrl Pts',(-12.1588589765331,13.3376329379985,
1258.14044117647));
#162727=CARTESIAN_POINT('Ctrl Pts',(-10.9229452762603,14.4643171449067,
1256.64632352941));
#162728=CARTESIAN_POINT('Ctrl Pts',(-9.50104767561052,15.3447188656481,
1255.15220588235));
#162729=CARTESIAN_POINT('Ctrl Pts',(-8.07915007496071,16.2251205863895,
1253.65808823529));
#162730=CARTESIAN_POINT('Ctrl Pts',(-6.51968959134574,16.8292587962898,
1252.16397058824));
#162731=CARTESIAN_POINT('Ctrl Pts',(-4.96022910773078,17.4333970061901,
1250.66985294118));
#162732=CARTESIAN_POINT('Ctrl Pts',(-3.31631129755346,17.7406985030951,
1249.17573529412));
#162733=CARTESIAN_POINT('Ctrl Pts',(-1.67239348737615,18.048,1247.68161764706));
#162734=CARTESIAN_POINT('Ctrl Pts',(-2.21024254310115E-15,18.048,1246.1875));
#162735=CARTESIAN_POINT('Ctrl Pts',(1.67239348737616,18.048,1244.69338235294));
#162736=CARTESIAN_POINT('Ctrl Pts',(3.31631129755346,17.7406985030951,1243.19926470588));
#162737=CARTESIAN_POINT('Ctrl Pts',(4.96022910773077,17.4333970061901,1241.70514705882));
#162738=CARTESIAN_POINT('Ctrl Pts',(6.51968959134575,16.8292587962898,1240.21102941176));
#162739=CARTESIAN_POINT('Ctrl Pts',(8.07915007496071,16.2251205863895,1238.71691176471));
#162740=CARTESIAN_POINT('Ctrl Pts',(9.50104767561053,15.3447188656481,1237.22279411765));
#162741=CARTESIAN_POINT('Ctrl Pts',(10.9229452762603,14.4643171449067,1235.72867647059));
#162742=CARTESIAN_POINT('Ctrl Pts',(12.1588589765331,13.3376329379985,1234.23455882353));
#162743=CARTESIAN_POINT('Ctrl Pts',(13.3947726768058,12.2109487310903,1232.74044117647));
#162744=CARTESIAN_POINT('Ctrl Pts',(14.4026149179538,10.8763499173728,1231.24632352941));
#162745=CARTESIAN_POINT('Ctrl Pts',(15.4104571591017,9.54175110365539,1229.75220588235));
#162746=CARTESIAN_POINT('Ctrl Pts',(16.1559070823762,8.04468584505496,1228.25808823529));
#162747=CARTESIAN_POINT('Ctrl Pts',(16.9013570056506,6.54762058645456,1226.76397058824));
#162748=CARTESIAN_POINT('Ctrl Pts',(17.3590292079831,4.93906964482096,1225.26985294118));
#162749=CARTESIAN_POINT('Ctrl Pts',(17.8167014103155,3.33051870318735,1223.77573529412));
#162750=CARTESIAN_POINT('Ctrl Pts',(17.9710104137728,1.66525935159367,1222.28161764706));
#162751=CARTESIAN_POINT('Ctrl Pts',(18.1253194172301,3.32956716117513E-15,
1220.7875));
#162752=CARTESIAN_POINT('Ctrl Pts',(17.9710104137728,-1.66525935159367,
1219.29338235294));
#162753=CARTESIAN_POINT('Ctrl Pts',(17.8167014103155,-3.33051870318736,
1217.79926470588));
#162754=CARTESIAN_POINT('Ctrl Pts',(17.3590292079831,-4.93906964482095,
1216.30514705882));
#162755=CARTESIAN_POINT('Ctrl Pts',(16.9013570056506,-6.54762058645456,
1214.81102941176));
#162756=CARTESIAN_POINT('Ctrl Pts',(16.1559070823762,-8.04468584505497,
1213.31691176471));
#162757=CARTESIAN_POINT('Ctrl Pts',(15.4104571591017,-9.54175110365538,
1211.82279411765));
#162758=CARTESIAN_POINT('Ctrl Pts',(14.4026149179538,-10.8763499173728,
1210.32867647059));
#162759=CARTESIAN_POINT('Ctrl Pts',(13.3947726768058,-12.2109487310903,
1208.83455882353));
#162760=CARTESIAN_POINT('Ctrl Pts',(12.1588589765331,-13.3376329379985,
1207.34044117647));
#162761=CARTESIAN_POINT('Ctrl Pts',(10.9229452762603,-14.4643171449067,
1205.84632352941));
#162762=CARTESIAN_POINT('Ctrl Pts',(9.50104767561053,-15.3447188656481,
1204.35220588235));
#162763=CARTESIAN_POINT('Ctrl Pts',(8.07915007496071,-16.2251205863895,
1202.85808823529));
#162764=CARTESIAN_POINT('Ctrl Pts',(6.51968959134574,-16.8292587962898,
1201.36397058824));
#162765=CARTESIAN_POINT('Ctrl Pts',(4.96022910773078,-17.4333970061901,
1199.86985294118));
#162766=CARTESIAN_POINT('Ctrl Pts',(3.31631129755346,-17.7406985030951,
1198.37573529412));
#162767=CARTESIAN_POINT('Ctrl Pts',(1.67239348737615,-18.048,1196.88161764706));
#162768=CARTESIAN_POINT('Ctrl Pts',(0.,-18.048,1195.3875));
#162769=CARTESIAN_POINT('Ctrl Pts',(-1.67239348737615,-18.048,1193.89338235294));
#162770=CARTESIAN_POINT('Ctrl Pts',(-3.31631129755346,-17.7406985030951,
1192.39926470588));
#162771=CARTESIAN_POINT('Ctrl Pts',(-4.96022910773077,-17.4333970061901,
1190.90514705882));
#162772=CARTESIAN_POINT('Ctrl Pts',(-6.51968959134574,-16.8292587962898,
1189.41102941176));
#162773=CARTESIAN_POINT('Ctrl Pts',(-8.07915007496071,-16.2251205863895,
1187.91691176471));
#162774=CARTESIAN_POINT('Ctrl Pts',(-9.50104767561052,-15.3447188656481,
1186.42279411765));
#162775=CARTESIAN_POINT('Ctrl Pts',(-10.9229452762603,-14.4643171449067,
1184.92867647059));
#162776=CARTESIAN_POINT('Ctrl Pts',(-12.1588589765331,-13.3376329379985,
1183.43455882353));
#162777=CARTESIAN_POINT('Ctrl Pts',(-13.3947726768058,-12.2109487310903,
1181.94044117647));
#162778=CARTESIAN_POINT('Ctrl Pts',(-14.4026149179538,-10.8763499173728,
1180.44632352941));
#162779=CARTESIAN_POINT('Ctrl Pts',(-15.4104571591017,-9.54175110365538,
1178.95220588235));
#162780=CARTESIAN_POINT('Ctrl Pts',(-16.1559070823762,-8.04468584505497,
1177.45808823529));
#162781=CARTESIAN_POINT('Ctrl Pts',(-16.9013570056506,-6.54762058645456,
1175.96397058824));
#162782=CARTESIAN_POINT('Ctrl Pts',(-17.3590292079831,-4.93906964482095,
1174.46985294118));
#162783=CARTESIAN_POINT('Ctrl Pts',(-17.8167014103155,-3.33051870318735,
1172.97573529412));
#162784=CARTESIAN_POINT('Ctrl Pts',(-17.9710104137728,-1.66525935159368,
1171.48161764706));
#162785=CARTESIAN_POINT('Ctrl Pts',(-18.1253194172301,-1.10985572039171E-15,
1169.9875));
#162786=CARTESIAN_POINT('Ctrl Pts',(-17.9710104137728,1.66525935159367,
1168.49338235294));
#162787=CARTESIAN_POINT('Ctrl Pts',(-17.8167014103155,3.33051870318735,
1166.99926470588));
#162788=CARTESIAN_POINT('Ctrl Pts',(-17.3590292079831,4.93906964482096,
1165.50514705882));
#162789=CARTESIAN_POINT('Ctrl Pts',(-16.9013570056506,6.54762058645456,
1164.01102941176));
#162790=CARTESIAN_POINT('Ctrl Pts',(-16.1559070823762,8.04468584505497,
1162.51691176471));
#162791=CARTESIAN_POINT('Ctrl Pts',(-15.4104571591017,9.54175110365538,
1161.02279411765));
#162792=CARTESIAN_POINT('Ctrl Pts',(-14.4026149179538,10.8763499173728,
1159.52867647059));
#162793=CARTESIAN_POINT('Ctrl Pts',(-13.3947726768058,12.2109487310903,
1158.03455882353));
#162794=CARTESIAN_POINT('Ctrl Pts',(-12.1588589765331,13.3376329379985,
1156.54044117647));
#162795=CARTESIAN_POINT('Ctrl Pts',(-10.9229452762603,14.4643171449067,
1155.04632352941));
#162796=CARTESIAN_POINT('Ctrl Pts',(-9.50104767561052,15.3447188656481,
1153.55220588235));
#162797=CARTESIAN_POINT('Ctrl Pts',(-8.07915007496071,16.2251205863895,
1152.05808823529));
#162798=CARTESIAN_POINT('Ctrl Pts',(-6.51968959134574,16.8292587962898,
1150.56397058824));
#162799=CARTESIAN_POINT('Ctrl Pts',(-4.96022910773078,17.4333970061901,
1149.06985294118));
#162800=CARTESIAN_POINT('Ctrl Pts',(-3.31631129755346,17.7406985030951,
1147.57573529412));
#162801=CARTESIAN_POINT('Ctrl Pts',(-1.67239348737615,18.048,1146.08161764706));
#162802=CARTESIAN_POINT('Ctrl Pts',(-2.21024254310115E-15,18.048,1144.5875));
#162803=CARTESIAN_POINT('Ctrl Pts',(1.67239348737616,18.048,1143.09338235294));
#162804=CARTESIAN_POINT('Ctrl Pts',(3.31631129755346,17.7406985030951,1141.59926470588));
#162805=CARTESIAN_POINT('Ctrl Pts',(4.96022910773077,17.4333970061901,1140.10514705882));
#162806=CARTESIAN_POINT('Ctrl Pts',(6.51968959134575,16.8292587962898,1138.61102941176));
#162807=CARTESIAN_POINT('Ctrl Pts',(8.07915007496071,16.2251205863895,1137.11691176471));
#162808=CARTESIAN_POINT('Ctrl Pts',(9.50104767561053,15.3447188656481,1135.62279411765));
#162809=CARTESIAN_POINT('Ctrl Pts',(10.9229452762603,14.4643171449067,1134.12867647059));
#162810=CARTESIAN_POINT('Ctrl Pts',(12.1588589765331,13.3376329379985,1132.63455882353));
#162811=CARTESIAN_POINT('Ctrl Pts',(13.3947726768058,12.2109487310903,1131.14044117647));
#162812=CARTESIAN_POINT('Ctrl Pts',(14.4026149179538,10.8763499173728,1129.64632352941));
#162813=CARTESIAN_POINT('Ctrl Pts',(15.4104571591017,9.54175110365539,1128.15220588235));
#162814=CARTESIAN_POINT('Ctrl Pts',(16.1559070823762,8.04468584505496,1126.65808823529));
#162815=CARTESIAN_POINT('Ctrl Pts',(16.9013570056506,6.54762058645456,1125.16397058824));
#162816=CARTESIAN_POINT('Ctrl Pts',(17.3590292079831,4.93906964482096,1123.66985294118));
#162817=CARTESIAN_POINT('Ctrl Pts',(17.8167014103155,3.33051870318735,1122.17573529412));
#162818=CARTESIAN_POINT('Ctrl Pts',(17.9710104137728,1.66525935159367,1120.68161764706));
#162819=CARTESIAN_POINT('Ctrl Pts',(18.1253194172301,3.32956716117513E-15,
1119.1875));
#162820=CARTESIAN_POINT('Ctrl Pts',(17.9710104137728,-1.66525935159367,
1117.69338235294));
#162821=CARTESIAN_POINT('Ctrl Pts',(17.8167014103155,-3.33051870318736,
1116.19926470588));
#162822=CARTESIAN_POINT('Ctrl Pts',(17.3590292079831,-4.93906964482095,
1114.70514705882));
#162823=CARTESIAN_POINT('Ctrl Pts',(16.9013570056506,-6.54762058645456,
1113.21102941176));
#162824=CARTESIAN_POINT('Ctrl Pts',(16.1559070823762,-8.04468584505497,
1111.71691176471));
#162825=CARTESIAN_POINT('Ctrl Pts',(15.4104571591017,-9.54175110365538,
1110.22279411765));
#162826=CARTESIAN_POINT('Ctrl Pts',(14.4026149179538,-10.8763499173728,
1108.72867647059));
#162827=CARTESIAN_POINT('Ctrl Pts',(13.3947726768058,-12.2109487310903,
1107.23455882353));
#162828=CARTESIAN_POINT('Ctrl Pts',(12.1588589765331,-13.3376329379985,
1105.74044117647));
#162829=CARTESIAN_POINT('Ctrl Pts',(10.9229452762603,-14.4643171449067,
1104.24632352941));
#162830=CARTESIAN_POINT('Ctrl Pts',(9.50104767561053,-15.3447188656481,
1102.75220588235));
#162831=CARTESIAN_POINT('Ctrl Pts',(8.07915007496071,-16.2251205863895,
1101.25808823529));
#162832=CARTESIAN_POINT('Ctrl Pts',(6.51968959134574,-16.8292587962898,
1099.76397058824));
#162833=CARTESIAN_POINT('Ctrl Pts',(4.96022910773078,-17.4333970061901,
1098.26985294118));
#162834=CARTESIAN_POINT('Ctrl Pts',(3.31631129755346,-17.7406985030951,
1096.77573529412));
#162835=CARTESIAN_POINT('Ctrl Pts',(1.67239348737615,-18.048,1095.28161764706));
#162836=CARTESIAN_POINT('Ctrl Pts',(0.,-18.048,1093.7875));
#162837=CARTESIAN_POINT('Ctrl Pts',(-1.67239348737615,-18.048,1092.29338235294));
#162838=CARTESIAN_POINT('Ctrl Pts',(-3.31631129755346,-17.7406985030951,
1090.79926470588));
#162839=CARTESIAN_POINT('Ctrl Pts',(-4.96022910773077,-17.4333970061901,
1089.30514705882));
#162840=CARTESIAN_POINT('Ctrl Pts',(-6.51968959134574,-16.8292587962898,
1087.81102941176));
#162841=CARTESIAN_POINT('Ctrl Pts',(-8.07915007496071,-16.2251205863895,
1086.31691176471));
#162842=CARTESIAN_POINT('Ctrl Pts',(-9.50104767561052,-15.3447188656481,
1084.82279411765));
#162843=CARTESIAN_POINT('Ctrl Pts',(-10.9229452762603,-14.4643171449067,
1083.32867647059));
#162844=CARTESIAN_POINT('Ctrl Pts',(-12.1588589765331,-13.3376329379985,
1081.83455882353));
#162845=CARTESIAN_POINT('Ctrl Pts',(-13.3947726768058,-12.2109487310903,
1080.34044117647));
#162846=CARTESIAN_POINT('Ctrl Pts',(-14.4026149179538,-10.8763499173728,
1078.84632352941));
#162847=CARTESIAN_POINT('Ctrl Pts',(-15.4104571591017,-9.54175110365538,
1077.35220588235));
#162848=CARTESIAN_POINT('Ctrl Pts',(-16.1559070823762,-8.04468584505497,
1075.85808823529));
#162849=CARTESIAN_POINT('Ctrl Pts',(-16.9013570056506,-6.54762058645456,
1074.36397058824));
#162850=CARTESIAN_POINT('Ctrl Pts',(-17.3590292079831,-4.93906964482095,
1072.86985294118));
#162851=CARTESIAN_POINT('Ctrl Pts',(-17.8167014103155,-3.33051870318735,
1071.37573529412));
#162852=CARTESIAN_POINT('Ctrl Pts',(-17.9710104137728,-1.66525935159368,
1069.88161764706));
#162853=CARTESIAN_POINT('Ctrl Pts',(-18.1253194172301,-1.10985572039171E-15,
1068.3875));
#162854=CARTESIAN_POINT('Ctrl Pts',(-17.9710104137728,1.66525935159367,
1066.89338235294));
#162855=CARTESIAN_POINT('Ctrl Pts',(-17.8167014103155,3.33051870318735,
1065.39926470588));
#162856=CARTESIAN_POINT('Ctrl Pts',(-17.3590292079831,4.93906964482096,
1063.90514705882));
#162857=CARTESIAN_POINT('Ctrl Pts',(-16.9013570056506,6.54762058645456,
1062.41102941176));
#162858=CARTESIAN_POINT('Ctrl Pts',(-16.1559070823762,8.04468584505497,
1060.91691176471));
#162859=CARTESIAN_POINT('Ctrl Pts',(-15.4104571591017,9.54175110365538,
1059.42279411765));
#162860=CARTESIAN_POINT('Ctrl Pts',(-14.4026149179538,10.8763499173728,
1057.92867647059));
#162861=CARTESIAN_POINT('Ctrl Pts',(-13.3947726768058,12.2109487310903,
1056.43455882353));
#162862=CARTESIAN_POINT('Ctrl Pts',(-12.1588589765331,13.3376329379985,
1054.94044117647));
#162863=CARTESIAN_POINT('Ctrl Pts',(-10.9229452762603,14.4643171449067,
1053.44632352941));
#162864=CARTESIAN_POINT('Ctrl Pts',(-9.50104767561052,15.3447188656481,
1051.95220588235));
#162865=CARTESIAN_POINT('Ctrl Pts',(-8.07915007496071,16.2251205863895,
1050.45808823529));
#162866=CARTESIAN_POINT('Ctrl Pts',(-6.51968959134574,16.8292587962898,
1048.96397058824));
#162867=CARTESIAN_POINT('Ctrl Pts',(-4.96022910773078,17.4333970061901,
1047.46985294118));
#162868=CARTESIAN_POINT('Ctrl Pts',(-3.31631129755346,17.7406985030951,
1045.97573529412));
#162869=CARTESIAN_POINT('Ctrl Pts',(-1.67239348737615,18.048,1044.48161764706));
#162870=CARTESIAN_POINT('Ctrl Pts',(-2.21024254310115E-15,18.048,1042.9875));
#162871=CARTESIAN_POINT('Ctrl Pts',(1.67239348737616,18.048,1041.49338235294));
#162872=CARTESIAN_POINT('Ctrl Pts',(3.31631129755346,17.7406985030951,1039.99926470588));
#162873=CARTESIAN_POINT('Ctrl Pts',(4.96022910773077,17.4333970061901,1038.50514705882));
#162874=CARTESIAN_POINT('Ctrl Pts',(6.51968959134575,16.8292587962898,1037.01102941176));
#162875=CARTESIAN_POINT('Ctrl Pts',(8.07915007496071,16.2251205863895,1035.51691176471));
#162876=CARTESIAN_POINT('Ctrl Pts',(9.50104767561053,15.3447188656481,1034.02279411765));
#162877=CARTESIAN_POINT('Ctrl Pts',(10.9229452762603,14.4643171449067,1032.52867647059));
#162878=CARTESIAN_POINT('Ctrl Pts',(12.1588589765331,13.3376329379985,1031.03455882353));
#162879=CARTESIAN_POINT('Ctrl Pts',(13.3947726768058,12.2109487310903,1029.54044117647));
#162880=CARTESIAN_POINT('Ctrl Pts',(14.4026149179538,10.8763499173728,1028.04632352941));
#162881=CARTESIAN_POINT('Ctrl Pts',(15.4104571591017,9.54175110365539,1026.55220588235));
#162882=CARTESIAN_POINT('Ctrl Pts',(16.1559070823762,8.04468584505496,1025.05808823529));
#162883=CARTESIAN_POINT('Ctrl Pts',(16.9013570056506,6.54762058645456,1023.56397058824));
#162884=CARTESIAN_POINT('Ctrl Pts',(17.3590292079831,4.93906964482096,1022.06985294118));
#162885=CARTESIAN_POINT('Ctrl Pts',(17.8167014103155,3.33051870318735,1020.57573529412));
#162886=CARTESIAN_POINT('Ctrl Pts',(17.9710104137728,1.66525935159367,1019.08161764706));
#162887=CARTESIAN_POINT('Ctrl Pts',(18.1253194172301,3.32956716117513E-15,
1017.5875));
#162888=CARTESIAN_POINT('Ctrl Pts',(17.9710104137728,-1.66525935159367,
1016.09338235294));
#162889=CARTESIAN_POINT('Ctrl Pts',(17.8167014103155,-3.33051870318736,
1014.59926470588));
#162890=CARTESIAN_POINT('Ctrl Pts',(17.3590292079831,-4.93906964482095,
1013.10514705882));
#162891=CARTESIAN_POINT('Ctrl Pts',(16.9013570056506,-6.54762058645456,
1011.61102941177));
#162892=CARTESIAN_POINT('Ctrl Pts',(16.1559070823762,-8.04468584505497,
1010.11691176471));
#162893=CARTESIAN_POINT('Ctrl Pts',(15.4104571591017,-9.54175110365538,
1008.62279411765));
#162894=CARTESIAN_POINT('Ctrl Pts',(14.4026149179538,-10.8763499173728,
1007.12867647059));
#162895=CARTESIAN_POINT('Ctrl Pts',(13.3947726768058,-12.2109487310903,
1005.63455882353));
#162896=CARTESIAN_POINT('Ctrl Pts',(12.1588589765331,-13.3376329379985,
1004.14044117647));
#162897=CARTESIAN_POINT('Ctrl Pts',(10.9229452762603,-14.4643171449067,
1002.64632352941));
#162898=CARTESIAN_POINT('Ctrl Pts',(9.50104767561053,-15.3447188656481,
1001.15220588235));
#162899=CARTESIAN_POINT('Ctrl Pts',(8.07915007496071,-16.2251205863895,
999.658088235294));
#162900=CARTESIAN_POINT('Ctrl Pts',(6.51968959134574,-16.8292587962898,
998.163970588235));
#162901=CARTESIAN_POINT('Ctrl Pts',(4.96022910773078,-17.4333970061901,
996.669852941177));
#162902=CARTESIAN_POINT('Ctrl Pts',(3.31631129755346,-17.7406985030951,
995.175735294118));
#162903=CARTESIAN_POINT('Ctrl Pts',(1.67239348737615,-18.048,993.681617647059));
#162904=CARTESIAN_POINT('Ctrl Pts',(0.,-18.048,992.1875));
#162905=CARTESIAN_POINT('Ctrl Pts',(-1.67239348737615,-18.048,990.693382352941));
#162906=CARTESIAN_POINT('Ctrl Pts',(-3.31631129755346,-17.7406985030951,
989.199264705882));
#162907=CARTESIAN_POINT('Ctrl Pts',(-4.96022910773077,-17.4333970061901,
987.705147058824));
#162908=CARTESIAN_POINT('Ctrl Pts',(-6.51968959134574,-16.8292587962898,
986.211029411765));
#162909=CARTESIAN_POINT('Ctrl Pts',(-8.07915007496071,-16.2251205863895,
984.716911764706));
#162910=CARTESIAN_POINT('Ctrl Pts',(-9.50104767561052,-15.3447188656481,
983.222794117647));
#162911=CARTESIAN_POINT('Ctrl Pts',(-10.9229452762603,-14.4643171449067,
981.728676470589));
#162912=CARTESIAN_POINT('Ctrl Pts',(-12.1588589765331,-13.3376329379985,
980.234558823529));
#162913=CARTESIAN_POINT('Ctrl Pts',(-13.3947726768058,-12.2109487310903,
978.740441176471));
#162914=CARTESIAN_POINT('Ctrl Pts',(-14.4026149179538,-10.8763499173728,
977.246323529412));
#162915=CARTESIAN_POINT('Ctrl Pts',(-15.4104571591017,-9.54175110365538,
975.752205882353));
#162916=CARTESIAN_POINT('Ctrl Pts',(-16.1559070823762,-8.04468584505497,
974.258088235294));
#162917=CARTESIAN_POINT('Ctrl Pts',(-16.9013570056506,-6.54762058645456,
972.763970588235));
#162918=CARTESIAN_POINT('Ctrl Pts',(-17.3590292079831,-4.93906964482095,
971.269852941177));
#162919=CARTESIAN_POINT('Ctrl Pts',(-17.8167014103155,-3.33051870318735,
969.775735294118));
#162920=CARTESIAN_POINT('Ctrl Pts',(-17.9710104137728,-1.66525935159368,
968.281617647059));
#162921=CARTESIAN_POINT('Ctrl Pts',(-18.1253194172301,-1.10985572039171E-15,
966.7875));
#162922=CARTESIAN_POINT('Ctrl Pts',(-17.9710104137728,1.66525935159367,
965.293382352941));
#162923=CARTESIAN_POINT('Ctrl Pts',(-17.8167014103155,3.33051870318735,
963.799264705882));
#162924=CARTESIAN_POINT('Ctrl Pts',(-17.3590292079831,4.93906964482096,
962.305147058824));
#162925=CARTESIAN_POINT('Ctrl Pts',(-16.9013570056506,6.54762058645456,
960.811029411765));
#162926=CARTESIAN_POINT('Ctrl Pts',(-16.1559070823762,8.04468584505497,
959.316911764706));
#162927=CARTESIAN_POINT('Ctrl Pts',(-15.4104571591017,9.54175110365538,
957.822794117647));
#162928=CARTESIAN_POINT('Ctrl Pts',(-14.4026149179538,10.8763499173728,
956.328676470588));
#162929=CARTESIAN_POINT('Ctrl Pts',(-13.3947726768058,12.2109487310903,
954.834558823529));
#162930=CARTESIAN_POINT('Ctrl Pts',(-12.1588589765331,13.3376329379985,
953.340441176471));
#162931=CARTESIAN_POINT('Ctrl Pts',(-10.9229452762603,14.4643171449067,
951.846323529412));
#162932=CARTESIAN_POINT('Ctrl Pts',(-9.50104767561052,15.3447188656481,
950.352205882353));
#162933=CARTESIAN_POINT('Ctrl Pts',(-8.07915007496071,16.2251205863895,
948.858088235294));
#162934=CARTESIAN_POINT('Ctrl Pts',(-6.51968959134574,16.8292587962898,
947.363970588235));
#162935=CARTESIAN_POINT('Ctrl Pts',(-4.96022910773078,17.4333970061901,
945.869852941177));
#162936=CARTESIAN_POINT('Ctrl Pts',(-3.31631129755346,17.7406985030951,
944.375735294118));
#162937=CARTESIAN_POINT('Ctrl Pts',(-1.67239348737615,18.048,942.881617647059));
#162938=CARTESIAN_POINT('Ctrl Pts',(-2.21024254310115E-15,18.048,941.3875));
#162939=CARTESIAN_POINT('Ctrl Pts',(1.67239348737616,18.048,939.893382352941));
#162940=CARTESIAN_POINT('Ctrl Pts',(3.31631129755346,17.7406985030951,938.399264705882));
#162941=CARTESIAN_POINT('Ctrl Pts',(4.96022910773077,17.4333970061901,936.905147058824));
#162942=CARTESIAN_POINT('Ctrl Pts',(6.51968959134575,16.8292587962898,935.411029411765));
#162943=CARTESIAN_POINT('Ctrl Pts',(8.07915007496071,16.2251205863895,933.916911764706));
#162944=CARTESIAN_POINT('Ctrl Pts',(9.50104767561053,15.3447188656481,932.422794117647));
#162945=CARTESIAN_POINT('Ctrl Pts',(10.9229452762603,14.4643171449067,930.928676470588));
#162946=CARTESIAN_POINT('Ctrl Pts',(12.1588589765331,13.3376329379985,929.43455882353));
#162947=CARTESIAN_POINT('Ctrl Pts',(13.3947726768058,12.2109487310903,927.940441176471));
#162948=CARTESIAN_POINT('Ctrl Pts',(14.4026149179538,10.8763499173728,926.446323529412));
#162949=CARTESIAN_POINT('Ctrl Pts',(15.4104571591017,9.54175110365539,924.952205882353));
#162950=CARTESIAN_POINT('Ctrl Pts',(16.1559070823762,8.04468584505496,923.458088235294));
#162951=CARTESIAN_POINT('Ctrl Pts',(16.9013570056506,6.54762058645456,921.963970588235));
#162952=CARTESIAN_POINT('Ctrl Pts',(17.3590292079831,4.93906964482096,920.469852941176));
#162953=CARTESIAN_POINT('Ctrl Pts',(17.8167014103155,3.33051870318735,918.975735294118));
#162954=CARTESIAN_POINT('Ctrl Pts',(17.9710104137728,1.66525935159367,917.481617647059));
#162955=CARTESIAN_POINT('Ctrl Pts',(18.1253194172301,3.32956716117513E-15,
915.9875));
#162956=CARTESIAN_POINT('Ctrl Pts',(17.9710104137728,-1.66525935159367,
914.493382352941));
#162957=CARTESIAN_POINT('Ctrl Pts',(17.8167014103155,-3.33051870318736,
912.999264705882));
#162958=CARTESIAN_POINT('Ctrl Pts',(17.3590292079831,-4.93906964482095,
911.505147058824));
#162959=CARTESIAN_POINT('Ctrl Pts',(16.9013570056506,-6.54762058645456,
910.011029411765));
#162960=CARTESIAN_POINT('Ctrl Pts',(16.1559070823762,-8.04468584505497,
908.516911764706));
#162961=CARTESIAN_POINT('Ctrl Pts',(15.4104571591017,-9.54175110365538,
907.022794117647));
#162962=CARTESIAN_POINT('Ctrl Pts',(14.4026149179538,-10.8763499173728,
905.528676470588));
#162963=CARTESIAN_POINT('Ctrl Pts',(13.3947726768058,-12.2109487310903,
904.034558823529));
#162964=CARTESIAN_POINT('Ctrl Pts',(12.1588589765331,-13.3376329379985,
902.540441176471));
#162965=CARTESIAN_POINT('Ctrl Pts',(10.9229452762603,-14.4643171449067,
901.046323529412));
#162966=CARTESIAN_POINT('Ctrl Pts',(9.50104767561053,-15.3447188656481,
899.552205882353));
#162967=CARTESIAN_POINT('Ctrl Pts',(8.07915007496071,-16.2251205863895,
898.058088235294));
#162968=CARTESIAN_POINT('Ctrl Pts',(6.51968959134574,-16.8292587962898,
896.563970588235));
#162969=CARTESIAN_POINT('Ctrl Pts',(4.96022910773078,-17.4333970061901,
895.069852941177));
#162970=CARTESIAN_POINT('Ctrl Pts',(3.31631129755346,-17.7406985030951,
893.575735294118));
#162971=CARTESIAN_POINT('Ctrl Pts',(1.67239348737615,-18.048,892.081617647059));
#162972=CARTESIAN_POINT('Ctrl Pts',(0.,-18.048,890.5875));
#162973=CARTESIAN_POINT('Ctrl Pts',(-1.67239348737615,-18.048,889.093382352941));
#162974=CARTESIAN_POINT('Ctrl Pts',(-3.31631129755346,-17.7406985030951,
887.599264705882));
#162975=CARTESIAN_POINT('Ctrl Pts',(-4.96022910773077,-17.4333970061901,
886.105147058824));
#162976=CARTESIAN_POINT('Ctrl Pts',(-6.51968959134574,-16.8292587962898,
884.611029411765));
#162977=CARTESIAN_POINT('Ctrl Pts',(-8.07915007496071,-16.2251205863895,
883.116911764706));
#162978=CARTESIAN_POINT('Ctrl Pts',(-9.50104767561052,-15.3447188656481,
881.622794117647));
#162979=CARTESIAN_POINT('Ctrl Pts',(-10.9229452762603,-14.4643171449067,
880.128676470588));
#162980=CARTESIAN_POINT('Ctrl Pts',(-12.1588589765331,-13.3376329379985,
878.634558823529));
#162981=CARTESIAN_POINT('Ctrl Pts',(-13.3947726768058,-12.2109487310903,
877.140441176471));
#162982=CARTESIAN_POINT('Ctrl Pts',(-14.4026149179538,-10.8763499173728,
875.646323529412));
#162983=CARTESIAN_POINT('Ctrl Pts',(-15.4104571591017,-9.54175110365538,
874.152205882353));
#162984=CARTESIAN_POINT('Ctrl Pts',(-16.1559070823762,-8.04468584505497,
872.658088235294));
#162985=CARTESIAN_POINT('Ctrl Pts',(-16.9013570056506,-6.54762058645456,
871.163970588236));
#162986=CARTESIAN_POINT('Ctrl Pts',(-17.3590292079831,-4.93906964482095,
869.669852941176));
#162987=CARTESIAN_POINT('Ctrl Pts',(-17.8167014103155,-3.33051870318735,
868.175735294118));
#162988=CARTESIAN_POINT('Ctrl Pts',(-17.9710104137728,-1.66525935159368,
866.681617647059));
#162989=CARTESIAN_POINT('Ctrl Pts',(-18.1253194172301,-1.10985572039171E-15,
865.1875));
#162990=CARTESIAN_POINT('Ctrl Pts',(-17.9710104137728,1.66525935159367,
863.693382352941));
#162991=CARTESIAN_POINT('Ctrl Pts',(-17.8167014103155,3.33051870318735,
862.199264705882));
#162992=CARTESIAN_POINT('Ctrl Pts',(-17.3590292079831,4.93906964482096,
860.705147058824));
#162993=CARTESIAN_POINT('Ctrl Pts',(-16.9013570056506,6.54762058645456,
859.211029411765));
#162994=CARTESIAN_POINT('Ctrl Pts',(-16.1559070823762,8.04468584505497,
857.716911764706));
#162995=CARTESIAN_POINT('Ctrl Pts',(-15.4104571591017,9.54175110365538,
856.222794117647));
#162996=CARTESIAN_POINT('Ctrl Pts',(-14.4026149179538,10.8763499173728,
854.728676470588));
#162997=CARTESIAN_POINT('Ctrl Pts',(-13.3947726768058,12.2109487310903,
853.234558823529));
#162998=CARTESIAN_POINT('Ctrl Pts',(-12.1588589765331,13.3376329379985,
851.740441176471));
#162999=CARTESIAN_POINT('Ctrl Pts',(-10.9229452762603,14.4643171449067,
850.246323529412));
#163000=CARTESIAN_POINT('Ctrl Pts',(-9.50104767561052,15.3447188656481,
848.752205882353));
#163001=CARTESIAN_POINT('Ctrl Pts',(-8.07915007496071,16.2251205863895,
847.258088235294));
#163002=CARTESIAN_POINT('Ctrl Pts',(-6.51968959134574,16.8292587962898,
845.763970588235));
#163003=CARTESIAN_POINT('Ctrl Pts',(-4.96022910773078,17.4333970061901,
844.269852941177));
#163004=CARTESIAN_POINT('Ctrl Pts',(-3.31631129755346,17.7406985030951,
842.775735294118));
#163005=CARTESIAN_POINT('Ctrl Pts',(-1.67239348737615,18.048,841.281617647059));
#163006=CARTESIAN_POINT('Ctrl Pts',(-2.21024254310115E-15,18.048,839.7875));
#163007=CARTESIAN_POINT('Ctrl Pts',(1.67239348737616,18.048,838.293382352941));
#163008=CARTESIAN_POINT('Ctrl Pts',(3.31631129755346,17.7406985030951,836.799264705882));
#163009=CARTESIAN_POINT('Ctrl Pts',(4.96022910773077,17.4333970061901,835.305147058824));
#163010=CARTESIAN_POINT('Ctrl Pts',(6.51968959134575,16.8292587962898,833.811029411765));
#163011=CARTESIAN_POINT('Ctrl Pts',(8.07915007496071,16.2251205863895,832.316911764706));
#163012=CARTESIAN_POINT('Ctrl Pts',(9.50104767561053,15.3447188656481,830.822794117647));
#163013=CARTESIAN_POINT('Ctrl Pts',(10.9229452762603,14.4643171449067,829.328676470588));
#163014=CARTESIAN_POINT('Ctrl Pts',(12.1588589765331,13.3376329379985,827.834558823529));
#163015=CARTESIAN_POINT('Ctrl Pts',(13.3947726768058,12.2109487310903,826.340441176471));
#163016=CARTESIAN_POINT('Ctrl Pts',(14.4026149179538,10.8763499173728,824.846323529412));
#163017=CARTESIAN_POINT('Ctrl Pts',(15.4104571591017,9.54175110365539,823.352205882353));
#163018=CARTESIAN_POINT('Ctrl Pts',(16.1559070823762,8.04468584505496,821.858088235294));
#163019=CARTESIAN_POINT('Ctrl Pts',(16.9013570056506,6.54762058645456,820.363970588235));
#163020=CARTESIAN_POINT('Ctrl Pts',(17.3590292079831,4.93906964482096,818.869852941177));
#163021=CARTESIAN_POINT('Ctrl Pts',(17.8167014103155,3.33051870318735,817.375735294118));
#163022=CARTESIAN_POINT('Ctrl Pts',(17.9710104137728,1.66525935159367,815.881617647059));
#163023=CARTESIAN_POINT('Ctrl Pts',(18.1253194172301,3.32956716117513E-15,
814.3875));
#163024=CARTESIAN_POINT('Ctrl Pts',(17.9710104137728,-1.66525935159367,
812.893382352941));
#163025=CARTESIAN_POINT('Ctrl Pts',(17.8167014103155,-3.33051870318736,
811.399264705883));
#163026=CARTESIAN_POINT('Ctrl Pts',(17.3590292079831,-4.93906964482095,
809.905147058824));
#163027=CARTESIAN_POINT('Ctrl Pts',(16.9013570056506,-6.54762058645456,
808.411029411765));
#163028=CARTESIAN_POINT('Ctrl Pts',(16.1559070823762,-8.04468584505497,
806.916911764706));
#163029=CARTESIAN_POINT('Ctrl Pts',(15.4104571591017,-9.54175110365538,
805.422794117647));
#163030=CARTESIAN_POINT('Ctrl Pts',(14.4026149179538,-10.8763499173728,
803.928676470588));
#163031=CARTESIAN_POINT('Ctrl Pts',(13.3947726768058,-12.2109487310903,
802.434558823529));
#163032=CARTESIAN_POINT('Ctrl Pts',(12.1588589765331,-13.3376329379985,
800.940441176471));
#163033=CARTESIAN_POINT('Ctrl Pts',(10.9229452762603,-14.4643171449067,
799.446323529412));
#163034=CARTESIAN_POINT('Ctrl Pts',(9.50104767561053,-15.3447188656481,
797.952205882353));
#163035=CARTESIAN_POINT('Ctrl Pts',(8.07915007496071,-16.2251205863895,
796.458088235294));
#163036=CARTESIAN_POINT('Ctrl Pts',(6.51968959134574,-16.8292587962898,
794.963970588235));
#163037=CARTESIAN_POINT('Ctrl Pts',(4.96022910773078,-17.4333970061901,
793.469852941176));
#163038=CARTESIAN_POINT('Ctrl Pts',(3.31631129755346,-17.7406985030951,
791.975735294118));
#163039=CARTESIAN_POINT('Ctrl Pts',(1.67239348737615,-18.048,790.481617647059));
#163040=CARTESIAN_POINT('Ctrl Pts',(0.,-18.048,788.9875));
#163041=CARTESIAN_POINT('Ctrl Pts',(-1.67239348737615,-18.048,787.493382352941));
#163042=CARTESIAN_POINT('Ctrl Pts',(-3.31631129755346,-17.7406985030951,
785.999264705882));
#163043=CARTESIAN_POINT('Ctrl Pts',(-4.96022910773077,-17.4333970061901,
784.505147058824));
#163044=CARTESIAN_POINT('Ctrl Pts',(-6.51968959134574,-16.8292587962898,
783.011029411765));
#163045=CARTESIAN_POINT('Ctrl Pts',(-8.07915007496071,-16.2251205863895,
781.516911764706));
#163046=CARTESIAN_POINT('Ctrl Pts',(-9.50104767561052,-15.3447188656481,
780.022794117647));
#163047=CARTESIAN_POINT('Ctrl Pts',(-10.9229452762603,-14.4643171449067,
778.528676470588));
#163048=CARTESIAN_POINT('Ctrl Pts',(-12.1588589765331,-13.3376329379985,
777.03455882353));
#163049=CARTESIAN_POINT('Ctrl Pts',(-13.3947726768058,-12.2109487310903,
775.540441176471));
#163050=CARTESIAN_POINT('Ctrl Pts',(-14.4026149179538,-10.8763499173728,
774.046323529412));
#163051=CARTESIAN_POINT('Ctrl Pts',(-15.4104571591017,-9.54175110365538,
772.552205882353));
#163052=CARTESIAN_POINT('Ctrl Pts',(-16.1559070823762,-8.04468584505497,
771.058088235294));
#163053=CARTESIAN_POINT('Ctrl Pts',(-16.9013570056506,-6.54762058645456,
769.563970588235));
#163054=CARTESIAN_POINT('Ctrl Pts',(-17.3590292079831,-4.93906964482095,
768.069852941177));
#163055=CARTESIAN_POINT('Ctrl Pts',(-17.8167014103155,-3.33051870318735,
766.575735294118));
#163056=CARTESIAN_POINT('Ctrl Pts',(-17.9710104137728,-1.66525935159368,
765.081617647059));
#163057=CARTESIAN_POINT('Ctrl Pts',(-18.1253194172301,-1.10985572039171E-15,
763.5875));
#163058=CARTESIAN_POINT('Ctrl Pts',(-17.9710104137728,1.66525935159367,
762.093382352941));
#163059=CARTESIAN_POINT('Ctrl Pts',(-17.8167014103155,3.33051870318735,
760.599264705883));
#163060=CARTESIAN_POINT('Ctrl Pts',(-17.3590292079831,4.93906964482096,
759.105147058824));
#163061=CARTESIAN_POINT('Ctrl Pts',(-16.9013570056506,6.54762058645456,
757.611029411765));
#163062=CARTESIAN_POINT('Ctrl Pts',(-16.1559070823762,8.04468584505497,
756.116911764706));
#163063=CARTESIAN_POINT('Ctrl Pts',(-15.4104571591017,9.54175110365538,
754.622794117647));
#163064=CARTESIAN_POINT('Ctrl Pts',(-14.4026149179538,10.8763499173728,
753.128676470588));
#163065=CARTESIAN_POINT('Ctrl Pts',(-13.3947726768058,12.2109487310903,
751.634558823529));
#163066=CARTESIAN_POINT('Ctrl Pts',(-12.1588589765331,13.3376329379985,
750.140441176471));
#163067=CARTESIAN_POINT('Ctrl Pts',(-10.9229452762603,14.4643171449067,
748.646323529412));
#163068=CARTESIAN_POINT('Ctrl Pts',(-9.50104767561052,15.3447188656481,
747.152205882353));
#163069=CARTESIAN_POINT('Ctrl Pts',(-8.07915007496071,16.2251205863895,
745.658088235294));
#163070=CARTESIAN_POINT('Ctrl Pts',(-6.51968959134574,16.8292587962898,
744.163970588235));
#163071=CARTESIAN_POINT('Ctrl Pts',(-4.96022910773078,17.4333970061901,
742.669852941176));
#163072=CARTESIAN_POINT('Ctrl Pts',(-3.31631129755346,17.7406985030951,
741.175735294118));
#163073=CARTESIAN_POINT('Ctrl Pts',(-1.67239348737615,18.048,739.681617647059));
#163074=CARTESIAN_POINT('Ctrl Pts',(-2.21024254310115E-15,18.048,738.1875));
#163075=CARTESIAN_POINT('Ctrl Pts',(1.67239348737616,18.048,736.693382352941));
#163076=CARTESIAN_POINT('Ctrl Pts',(3.31631129755346,17.7406985030951,735.199264705882));
#163077=CARTESIAN_POINT('Ctrl Pts',(4.96022910773077,17.4333970061901,733.705147058824));
#163078=CARTESIAN_POINT('Ctrl Pts',(6.51968959134575,16.8292587962898,732.211029411765));
#163079=CARTESIAN_POINT('Ctrl Pts',(8.07915007496071,16.2251205863895,730.716911764706));
#163080=CARTESIAN_POINT('Ctrl Pts',(9.50104767561053,15.3447188656481,729.222794117647));
#163081=CARTESIAN_POINT('Ctrl Pts',(10.9229452762603,14.4643171449067,727.728676470588));
#163082=CARTESIAN_POINT('Ctrl Pts',(12.1588589765331,13.3376329379985,726.234558823529));
#163083=CARTESIAN_POINT('Ctrl Pts',(13.3947726768058,12.2109487310903,724.740441176471));
#163084=CARTESIAN_POINT('Ctrl Pts',(14.4026149179538,10.8763499173728,723.246323529412));
#163085=CARTESIAN_POINT('Ctrl Pts',(15.4104571591017,9.54175110365539,721.752205882353));
#163086=CARTESIAN_POINT('Ctrl Pts',(16.1559070823762,8.04468584505496,720.258088235294));
#163087=CARTESIAN_POINT('Ctrl Pts',(16.9013570056506,6.54762058645456,718.763970588235));
#163088=CARTESIAN_POINT('Ctrl Pts',(17.3590292079831,4.93906964482096,717.269852941177));
#163089=CARTESIAN_POINT('Ctrl Pts',(17.8167014103155,3.33051870318735,715.775735294118));
#163090=CARTESIAN_POINT('Ctrl Pts',(17.9710104137728,1.66525935159367,714.281617647059));
#163091=CARTESIAN_POINT('Ctrl Pts',(18.1253194172301,3.32956716117513E-15,
712.7875));
#163092=CARTESIAN_POINT('Ctrl Pts',(17.9710104137728,-1.66525935159367,
711.293382352941));
#163093=CARTESIAN_POINT('Ctrl Pts',(17.8167014103155,-3.33051870318736,
709.799264705882));
#163094=CARTESIAN_POINT('Ctrl Pts',(17.3590292079831,-4.93906964482095,
708.305147058824));
#163095=CARTESIAN_POINT('Ctrl Pts',(16.9013570056506,-6.54762058645456,
706.811029411765));
#163096=CARTESIAN_POINT('Ctrl Pts',(16.1559070823762,-8.04468584505497,
705.316911764706));
#163097=CARTESIAN_POINT('Ctrl Pts',(15.4104571591017,-9.54175110365538,
703.822794117647));
#163098=CARTESIAN_POINT('Ctrl Pts',(14.4026149179538,-10.8763499173728,
702.328676470588));
#163099=CARTESIAN_POINT('Ctrl Pts',(13.3947726768058,-12.2109487310903,
700.83455882353));
#163100=CARTESIAN_POINT('Ctrl Pts',(12.1588589765331,-13.3376329379985,
699.340441176471));
#163101=CARTESIAN_POINT('Ctrl Pts',(10.9229452762603,-14.4643171449067,
697.846323529412));
#163102=CARTESIAN_POINT('Ctrl Pts',(9.50104767561053,-15.3447188656481,
696.352205882353));
#163103=CARTESIAN_POINT('Ctrl Pts',(8.07915007496071,-16.2251205863895,
694.858088235294));
#163104=CARTESIAN_POINT('Ctrl Pts',(6.51968959134574,-16.8292587962898,
693.363970588235));
#163105=CARTESIAN_POINT('Ctrl Pts',(5.80938874487777,-17.1044308101911,
692.683432004168));
#163106=CARTESIAN_POINT('Ctrl Pts',(5.07842733458062,-17.3187724682607,
692.));
#163107=CARTESIAN_POINT('Ctrl Pts',(0.,-18.048,1500.28886941341));
#163108=CARTESIAN_POINT('Ctrl Pts',(-1.67239348737615,-18.048,1498.79475176635));
#163109=CARTESIAN_POINT('Ctrl Pts',(-3.31631129755346,-17.7406985030951,
1497.30063411929));
#163110=CARTESIAN_POINT('Ctrl Pts',(-4.96022910773077,-17.4333970061901,
1495.80651647223));
#163111=CARTESIAN_POINT('Ctrl Pts',(-6.51968959134574,-16.8292587962898,
1494.31239882517));
#163112=CARTESIAN_POINT('Ctrl Pts',(-8.07915007496071,-16.2251205863895,
1492.81828117811));
#163113=CARTESIAN_POINT('Ctrl Pts',(-9.50104767561052,-15.3447188656481,
1491.32416353106));
#163114=CARTESIAN_POINT('Ctrl Pts',(-10.9229452762603,-14.4643171449067,
1489.830045884));
#163115=CARTESIAN_POINT('Ctrl Pts',(-12.1588589765331,-13.3376329379985,
1488.33592823694));
#163116=CARTESIAN_POINT('Ctrl Pts',(-13.3947726768058,-12.2109487310903,
1486.84181058988));
#163117=CARTESIAN_POINT('Ctrl Pts',(-14.4026149179538,-10.8763499173728,
1485.34769294282));
#163118=CARTESIAN_POINT('Ctrl Pts',(-15.4104571591017,-9.54175110365538,
1483.85357529576));
#163119=CARTESIAN_POINT('Ctrl Pts',(-16.1559070823762,-8.04468584505497,
1482.3594576487));
#163120=CARTESIAN_POINT('Ctrl Pts',(-16.9013570056506,-6.54762058645456,
1480.86534000164));
#163121=CARTESIAN_POINT('Ctrl Pts',(-17.3590292079831,-4.93906964482095,
1479.37122235458));
#163122=CARTESIAN_POINT('Ctrl Pts',(-17.8167014103155,-3.33051870318735,
1477.87710470753));
#163123=CARTESIAN_POINT('Ctrl Pts',(-17.9710104137728,-1.66525935159368,
1476.38298706047));
#163124=CARTESIAN_POINT('Ctrl Pts',(-18.1253194172301,-1.10985572039171E-15,
1474.88886941341));
#163125=CARTESIAN_POINT('Ctrl Pts',(-17.9710104137728,1.66525935159367,
1473.39475176635));
#163126=CARTESIAN_POINT('Ctrl Pts',(-17.8167014103155,3.33051870318735,
1471.90063411929));
#163127=CARTESIAN_POINT('Ctrl Pts',(-17.3590292079831,4.93906964482096,
1470.40651647223));
#163128=CARTESIAN_POINT('Ctrl Pts',(-16.9013570056506,6.54762058645456,
1468.91239882517));
#163129=CARTESIAN_POINT('Ctrl Pts',(-16.1559070823762,8.04468584505497,
1467.41828117811));
#163130=CARTESIAN_POINT('Ctrl Pts',(-15.4104571591017,9.54175110365538,
1465.92416353106));
#163131=CARTESIAN_POINT('Ctrl Pts',(-14.4026149179538,10.8763499173728,
1464.430045884));
#163132=CARTESIAN_POINT('Ctrl Pts',(-13.3947726768058,12.2109487310903,
1462.93592823694));
#163133=CARTESIAN_POINT('Ctrl Pts',(-12.1588589765331,13.3376329379985,
1461.44181058988));
#163134=CARTESIAN_POINT('Ctrl Pts',(-10.9229452762603,14.4643171449067,
1459.94769294282));
#163135=CARTESIAN_POINT('Ctrl Pts',(-9.50104767561052,15.3447188656481,
1458.45357529576));
#163136=CARTESIAN_POINT('Ctrl Pts',(-8.07915007496071,16.2251205863895,
1456.9594576487));
#163137=CARTESIAN_POINT('Ctrl Pts',(-6.51968959134574,16.8292587962898,
1455.46534000164));
#163138=CARTESIAN_POINT('Ctrl Pts',(-4.96022910773078,17.4333970061901,
1453.97122235458));
#163139=CARTESIAN_POINT('Ctrl Pts',(-3.31631129755346,17.7406985030951,
1452.47710470753));
#163140=CARTESIAN_POINT('Ctrl Pts',(-1.67239348737615,18.048,1450.98298706047));
#163141=CARTESIAN_POINT('Ctrl Pts',(-2.21024254310115E-15,18.048,1449.48886941341));
#163142=CARTESIAN_POINT('Ctrl Pts',(1.67239348737616,18.048,1447.99475176635));
#163143=CARTESIAN_POINT('Ctrl Pts',(3.31631129755346,17.7406985030951,1446.50063411929));
#163144=CARTESIAN_POINT('Ctrl Pts',(4.96022910773077,17.4333970061901,1445.00651647223));
#163145=CARTESIAN_POINT('Ctrl Pts',(6.51968959134575,16.8292587962898,1443.51239882517));
#163146=CARTESIAN_POINT('Ctrl Pts',(8.07915007496071,16.2251205863895,1442.01828117811));
#163147=CARTESIAN_POINT('Ctrl Pts',(9.50104767561053,15.3447188656481,1440.52416353105));
#163148=CARTESIAN_POINT('Ctrl Pts',(10.9229452762603,14.4643171449067,1439.030045884));
#163149=CARTESIAN_POINT('Ctrl Pts',(12.1588589765331,13.3376329379985,1437.53592823694));
#163150=CARTESIAN_POINT('Ctrl Pts',(13.3947726768058,12.2109487310903,1436.04181058988));
#163151=CARTESIAN_POINT('Ctrl Pts',(14.4026149179538,10.8763499173728,1434.54769294282));
#163152=CARTESIAN_POINT('Ctrl Pts',(15.4104571591017,9.54175110365538,1433.05357529576));
#163153=CARTESIAN_POINT('Ctrl Pts',(16.1559070823762,8.04468584505496,1431.5594576487));
#163154=CARTESIAN_POINT('Ctrl Pts',(16.9013570056506,6.54762058645456,1430.06534000164));
#163155=CARTESIAN_POINT('Ctrl Pts',(17.3590292079831,4.93906964482096,1428.57122235458));
#163156=CARTESIAN_POINT('Ctrl Pts',(17.8167014103155,3.33051870318735,1427.07710470753));
#163157=CARTESIAN_POINT('Ctrl Pts',(17.9710104137728,1.66525935159367,1425.58298706047));
#163158=CARTESIAN_POINT('Ctrl Pts',(18.1253194172301,3.32956716117513E-15,
1424.08886941341));
#163159=CARTESIAN_POINT('Ctrl Pts',(17.9710104137728,-1.66525935159367,
1422.59475176635));
#163160=CARTESIAN_POINT('Ctrl Pts',(17.8167014103155,-3.33051870318736,
1421.10063411929));
#163161=CARTESIAN_POINT('Ctrl Pts',(17.3590292079831,-4.93906964482095,
1419.60651647223));
#163162=CARTESIAN_POINT('Ctrl Pts',(16.9013570056506,-6.54762058645456,
1418.11239882517));
#163163=CARTESIAN_POINT('Ctrl Pts',(16.1559070823762,-8.04468584505497,
1416.61828117811));
#163164=CARTESIAN_POINT('Ctrl Pts',(15.4104571591017,-9.54175110365538,
1415.12416353105));
#163165=CARTESIAN_POINT('Ctrl Pts',(14.4026149179538,-10.8763499173728,
1413.630045884));
#163166=CARTESIAN_POINT('Ctrl Pts',(13.3947726768058,-12.2109487310903,
1412.13592823694));
#163167=CARTESIAN_POINT('Ctrl Pts',(12.1588589765331,-13.3376329379985,
1410.64181058988));
#163168=CARTESIAN_POINT('Ctrl Pts',(10.9229452762603,-14.4643171449067,
1409.14769294282));
#163169=CARTESIAN_POINT('Ctrl Pts',(9.50104767561053,-15.3447188656481,
1407.65357529576));
#163170=CARTESIAN_POINT('Ctrl Pts',(8.07915007496071,-16.2251205863895,
1406.1594576487));
#163171=CARTESIAN_POINT('Ctrl Pts',(6.51968959134574,-16.8292587962898,
1404.66534000164));
#163172=CARTESIAN_POINT('Ctrl Pts',(4.96022910773078,-17.4333970061901,
1403.17122235458));
#163173=CARTESIAN_POINT('Ctrl Pts',(3.31631129755346,-17.7406985030951,
1401.67710470753));
#163174=CARTESIAN_POINT('Ctrl Pts',(1.67239348737615,-18.048,1400.18298706047));
#163175=CARTESIAN_POINT('Ctrl Pts',(0.,-18.048,1398.68886941341));
#163176=CARTESIAN_POINT('Ctrl Pts',(-1.67239348737615,-18.048,1397.19475176635));
#163177=CARTESIAN_POINT('Ctrl Pts',(-3.31631129755346,-17.7406985030951,
1395.70063411929));
#163178=CARTESIAN_POINT('Ctrl Pts',(-4.96022910773077,-17.4333970061901,
1394.20651647223));
#163179=CARTESIAN_POINT('Ctrl Pts',(-6.51968959134574,-16.8292587962898,
1392.71239882517));
#163180=CARTESIAN_POINT('Ctrl Pts',(-8.07915007496071,-16.2251205863895,
1391.21828117811));
#163181=CARTESIAN_POINT('Ctrl Pts',(-9.50104767561052,-15.3447188656481,
1389.72416353105));
#163182=CARTESIAN_POINT('Ctrl Pts',(-10.9229452762603,-14.4643171449067,
1388.230045884));
#163183=CARTESIAN_POINT('Ctrl Pts',(-12.1588589765331,-13.3376329379985,
1386.73592823694));
#163184=CARTESIAN_POINT('Ctrl Pts',(-13.3947726768058,-12.2109487310903,
1385.24181058988));
#163185=CARTESIAN_POINT('Ctrl Pts',(-14.4026149179538,-10.8763499173728,
1383.74769294282));
#163186=CARTESIAN_POINT('Ctrl Pts',(-15.4104571591017,-9.54175110365538,
1382.25357529576));
#163187=CARTESIAN_POINT('Ctrl Pts',(-16.1559070823762,-8.04468584505497,
1380.7594576487));
#163188=CARTESIAN_POINT('Ctrl Pts',(-16.9013570056506,-6.54762058645456,
1379.26534000164));
#163189=CARTESIAN_POINT('Ctrl Pts',(-17.3590292079831,-4.93906964482095,
1377.77122235458));
#163190=CARTESIAN_POINT('Ctrl Pts',(-17.8167014103155,-3.33051870318735,
1376.27710470753));
#163191=CARTESIAN_POINT('Ctrl Pts',(-17.9710104137728,-1.66525935159368,
1374.78298706047));
#163192=CARTESIAN_POINT('Ctrl Pts',(-18.1253194172301,-1.10985572039171E-15,
1373.28886941341));
#163193=CARTESIAN_POINT('Ctrl Pts',(-17.9710104137728,1.66525935159367,
1371.79475176635));
#163194=CARTESIAN_POINT('Ctrl Pts',(-17.8167014103155,3.33051870318735,
1370.30063411929));
#163195=CARTESIAN_POINT('Ctrl Pts',(-17.3590292079831,4.93906964482096,
1368.80651647223));
#163196=CARTESIAN_POINT('Ctrl Pts',(-16.9013570056506,6.54762058645456,
1367.31239882517));
#163197=CARTESIAN_POINT('Ctrl Pts',(-16.1559070823762,8.04468584505497,
1365.81828117811));
#163198=CARTESIAN_POINT('Ctrl Pts',(-15.4104571591017,9.54175110365538,
1364.32416353105));
#163199=CARTESIAN_POINT('Ctrl Pts',(-14.4026149179538,10.8763499173728,
1362.830045884));
#163200=CARTESIAN_POINT('Ctrl Pts',(-13.3947726768058,12.2109487310903,
1361.33592823694));
#163201=CARTESIAN_POINT('Ctrl Pts',(-12.1588589765331,13.3376329379985,
1359.84181058988));
#163202=CARTESIAN_POINT('Ctrl Pts',(-10.9229452762603,14.4643171449067,
1358.34769294282));
#163203=CARTESIAN_POINT('Ctrl Pts',(-9.50104767561052,15.3447188656481,
1356.85357529576));
#163204=CARTESIAN_POINT('Ctrl Pts',(-8.07915007496071,16.2251205863895,
1355.3594576487));
#163205=CARTESIAN_POINT('Ctrl Pts',(-6.51968959134574,16.8292587962898,
1353.86534000164));
#163206=CARTESIAN_POINT('Ctrl Pts',(-4.96022910773078,17.4333970061901,
1352.37122235458));
#163207=CARTESIAN_POINT('Ctrl Pts',(-3.31631129755346,17.7406985030951,
1350.87710470753));
#163208=CARTESIAN_POINT('Ctrl Pts',(-1.67239348737615,18.048,1349.38298706047));
#163209=CARTESIAN_POINT('Ctrl Pts',(-2.21024254310115E-15,18.048,1347.88886941341));
#163210=CARTESIAN_POINT('Ctrl Pts',(1.67239348737616,18.048,1346.39475176635));
#163211=CARTESIAN_POINT('Ctrl Pts',(3.31631129755346,17.7406985030951,1344.90063411929));
#163212=CARTESIAN_POINT('Ctrl Pts',(4.96022910773077,17.4333970061901,1343.40651647223));
#163213=CARTESIAN_POINT('Ctrl Pts',(6.51968959134575,16.8292587962898,1341.91239882517));
#163214=CARTESIAN_POINT('Ctrl Pts',(8.07915007496071,16.2251205863895,1340.41828117811));
#163215=CARTESIAN_POINT('Ctrl Pts',(9.50104767561053,15.3447188656481,1338.92416353106));
#163216=CARTESIAN_POINT('Ctrl Pts',(10.9229452762603,14.4643171449067,1337.430045884));
#163217=CARTESIAN_POINT('Ctrl Pts',(12.1588589765331,13.3376329379985,1335.93592823694));
#163218=CARTESIAN_POINT('Ctrl Pts',(13.3947726768058,12.2109487310903,1334.44181058988));
#163219=CARTESIAN_POINT('Ctrl Pts',(14.4026149179538,10.8763499173728,1332.94769294282));
#163220=CARTESIAN_POINT('Ctrl Pts',(15.4104571591017,9.54175110365538,1331.45357529576));
#163221=CARTESIAN_POINT('Ctrl Pts',(16.1559070823762,8.04468584505496,1329.9594576487));
#163222=CARTESIAN_POINT('Ctrl Pts',(16.9013570056506,6.54762058645456,1328.46534000164));
#163223=CARTESIAN_POINT('Ctrl Pts',(17.3590292079831,4.93906964482096,1326.97122235458));
#163224=CARTESIAN_POINT('Ctrl Pts',(17.8167014103155,3.33051870318735,1325.47710470753));
#163225=CARTESIAN_POINT('Ctrl Pts',(17.9710104137728,1.66525935159367,1323.98298706047));
#163226=CARTESIAN_POINT('Ctrl Pts',(18.1253194172301,3.32956716117513E-15,
1322.48886941341));
#163227=CARTESIAN_POINT('Ctrl Pts',(17.9710104137728,-1.66525935159367,
1320.99475176635));
#163228=CARTESIAN_POINT('Ctrl Pts',(17.8167014103155,-3.33051870318736,
1319.50063411929));
#163229=CARTESIAN_POINT('Ctrl Pts',(17.3590292079831,-4.93906964482095,
1318.00651647223));
#163230=CARTESIAN_POINT('Ctrl Pts',(16.9013570056506,-6.54762058645456,
1316.51239882517));
#163231=CARTESIAN_POINT('Ctrl Pts',(16.1559070823762,-8.04468584505497,
1315.01828117811));
#163232=CARTESIAN_POINT('Ctrl Pts',(15.4104571591017,-9.54175110365538,
1313.52416353105));
#163233=CARTESIAN_POINT('Ctrl Pts',(14.4026149179538,-10.8763499173728,
1312.030045884));
#163234=CARTESIAN_POINT('Ctrl Pts',(13.3947726768058,-12.2109487310903,
1310.53592823694));
#163235=CARTESIAN_POINT('Ctrl Pts',(12.1588589765331,-13.3376329379985,
1309.04181058988));
#163236=CARTESIAN_POINT('Ctrl Pts',(10.9229452762603,-14.4643171449067,
1307.54769294282));
#163237=CARTESIAN_POINT('Ctrl Pts',(9.50104767561053,-15.3447188656481,
1306.05357529576));
#163238=CARTESIAN_POINT('Ctrl Pts',(8.07915007496071,-16.2251205863895,
1304.5594576487));
#163239=CARTESIAN_POINT('Ctrl Pts',(6.51968959134574,-16.8292587962898,
1303.06534000164));
#163240=CARTESIAN_POINT('Ctrl Pts',(4.96022910773078,-17.4333970061901,
1301.57122235458));
#163241=CARTESIAN_POINT('Ctrl Pts',(3.31631129755346,-17.7406985030951,
1300.07710470753));
#163242=CARTESIAN_POINT('Ctrl Pts',(1.67239348737615,-18.048,1298.58298706047));
#163243=CARTESIAN_POINT('Ctrl Pts',(0.,-18.048,1297.08886941341));
#163244=CARTESIAN_POINT('Ctrl Pts',(-1.67239348737615,-18.048,1295.59475176635));
#163245=CARTESIAN_POINT('Ctrl Pts',(-3.31631129755346,-17.7406985030951,
1294.10063411929));
#163246=CARTESIAN_POINT('Ctrl Pts',(-4.96022910773077,-17.4333970061901,
1292.60651647223));
#163247=CARTESIAN_POINT('Ctrl Pts',(-6.51968959134574,-16.8292587962898,
1291.11239882517));
#163248=CARTESIAN_POINT('Ctrl Pts',(-8.07915007496071,-16.2251205863895,
1289.61828117811));
#163249=CARTESIAN_POINT('Ctrl Pts',(-9.50104767561052,-15.3447188656481,
1288.12416353105));
#163250=CARTESIAN_POINT('Ctrl Pts',(-10.9229452762603,-14.4643171449067,
1286.630045884));
#163251=CARTESIAN_POINT('Ctrl Pts',(-12.1588589765331,-13.3376329379985,
1285.13592823694));
#163252=CARTESIAN_POINT('Ctrl Pts',(-13.3947726768058,-12.2109487310903,
1283.64181058988));
#163253=CARTESIAN_POINT('Ctrl Pts',(-14.4026149179538,-10.8763499173728,
1282.14769294282));
#163254=CARTESIAN_POINT('Ctrl Pts',(-15.4104571591017,-9.54175110365538,
1280.65357529576));
#163255=CARTESIAN_POINT('Ctrl Pts',(-16.1559070823762,-8.04468584505497,
1279.1594576487));
#163256=CARTESIAN_POINT('Ctrl Pts',(-16.9013570056506,-6.54762058645456,
1277.66534000164));
#163257=CARTESIAN_POINT('Ctrl Pts',(-17.3590292079831,-4.93906964482095,
1276.17122235458));
#163258=CARTESIAN_POINT('Ctrl Pts',(-17.8167014103155,-3.33051870318735,
1274.67710470753));
#163259=CARTESIAN_POINT('Ctrl Pts',(-17.9710104137728,-1.66525935159368,
1273.18298706047));
#163260=CARTESIAN_POINT('Ctrl Pts',(-18.1253194172301,-1.10985572039171E-15,
1271.68886941341));
#163261=CARTESIAN_POINT('Ctrl Pts',(-17.9710104137728,1.66525935159367,
1270.19475176635));
#163262=CARTESIAN_POINT('Ctrl Pts',(-17.8167014103155,3.33051870318735,
1268.70063411929));
#163263=CARTESIAN_POINT('Ctrl Pts',(-17.3590292079831,4.93906964482096,
1267.20651647223));
#163264=CARTESIAN_POINT('Ctrl Pts',(-16.9013570056506,6.54762058645456,
1265.71239882517));
#163265=CARTESIAN_POINT('Ctrl Pts',(-16.1559070823762,8.04468584505497,
1264.21828117811));
#163266=CARTESIAN_POINT('Ctrl Pts',(-15.4104571591017,9.54175110365538,
1262.72416353105));
#163267=CARTESIAN_POINT('Ctrl Pts',(-14.4026149179538,10.8763499173728,
1261.230045884));
#163268=CARTESIAN_POINT('Ctrl Pts',(-13.3947726768058,12.2109487310903,
1259.73592823694));
#163269=CARTESIAN_POINT('Ctrl Pts',(-12.1588589765331,13.3376329379985,
1258.24181058988));
#163270=CARTESIAN_POINT('Ctrl Pts',(-10.9229452762603,14.4643171449067,
1256.74769294282));
#163271=CARTESIAN_POINT('Ctrl Pts',(-9.50104767561052,15.3447188656481,
1255.25357529576));
#163272=CARTESIAN_POINT('Ctrl Pts',(-8.07915007496071,16.2251205863895,
1253.7594576487));
#163273=CARTESIAN_POINT('Ctrl Pts',(-6.51968959134574,16.8292587962898,
1252.26534000164));
#163274=CARTESIAN_POINT('Ctrl Pts',(-4.96022910773078,17.4333970061901,
1250.77122235458));
#163275=CARTESIAN_POINT('Ctrl Pts',(-3.31631129755346,17.7406985030951,
1249.27710470753));
#163276=CARTESIAN_POINT('Ctrl Pts',(-1.67239348737615,18.048,1247.78298706047));
#163277=CARTESIAN_POINT('Ctrl Pts',(-2.21024254310115E-15,18.048,1246.28886941341));
#163278=CARTESIAN_POINT('Ctrl Pts',(1.67239348737616,18.048,1244.79475176635));
#163279=CARTESIAN_POINT('Ctrl Pts',(3.31631129755346,17.7406985030951,1243.30063411929));
#163280=CARTESIAN_POINT('Ctrl Pts',(4.96022910773077,17.4333970061901,1241.80651647223));
#163281=CARTESIAN_POINT('Ctrl Pts',(6.51968959134575,16.8292587962898,1240.31239882517));
#163282=CARTESIAN_POINT('Ctrl Pts',(8.07915007496071,16.2251205863895,1238.81828117811));
#163283=CARTESIAN_POINT('Ctrl Pts',(9.50104767561053,15.3447188656481,1237.32416353105));
#163284=CARTESIAN_POINT('Ctrl Pts',(10.9229452762603,14.4643171449067,1235.830045884));
#163285=CARTESIAN_POINT('Ctrl Pts',(12.1588589765331,13.3376329379985,1234.33592823694));
#163286=CARTESIAN_POINT('Ctrl Pts',(13.3947726768058,12.2109487310903,1232.84181058988));
#163287=CARTESIAN_POINT('Ctrl Pts',(14.4026149179538,10.8763499173728,1231.34769294282));
#163288=CARTESIAN_POINT('Ctrl Pts',(15.4104571591017,9.54175110365538,1229.85357529576));
#163289=CARTESIAN_POINT('Ctrl Pts',(16.1559070823762,8.04468584505496,1228.3594576487));
#163290=CARTESIAN_POINT('Ctrl Pts',(16.9013570056506,6.54762058645456,1226.86534000164));
#163291=CARTESIAN_POINT('Ctrl Pts',(17.3590292079831,4.93906964482096,1225.37122235458));
#163292=CARTESIAN_POINT('Ctrl Pts',(17.8167014103155,3.33051870318735,1223.87710470753));
#163293=CARTESIAN_POINT('Ctrl Pts',(17.9710104137728,1.66525935159367,1222.38298706047));
#163294=CARTESIAN_POINT('Ctrl Pts',(18.1253194172301,3.32956716117513E-15,
1220.88886941341));
#163295=CARTESIAN_POINT('Ctrl Pts',(17.9710104137728,-1.66525935159367,
1219.39475176635));
#163296=CARTESIAN_POINT('Ctrl Pts',(17.8167014103155,-3.33051870318736,
1217.90063411929));
#163297=CARTESIAN_POINT('Ctrl Pts',(17.3590292079831,-4.93906964482095,
1216.40651647223));
#163298=CARTESIAN_POINT('Ctrl Pts',(16.9013570056506,-6.54762058645456,
1214.91239882517));
#163299=CARTESIAN_POINT('Ctrl Pts',(16.1559070823762,-8.04468584505497,
1213.41828117811));
#163300=CARTESIAN_POINT('Ctrl Pts',(15.4104571591017,-9.54175110365538,
1211.92416353105));
#163301=CARTESIAN_POINT('Ctrl Pts',(14.4026149179538,-10.8763499173728,
1210.430045884));
#163302=CARTESIAN_POINT('Ctrl Pts',(13.3947726768058,-12.2109487310903,
1208.93592823694));
#163303=CARTESIAN_POINT('Ctrl Pts',(12.1588589765331,-13.3376329379985,
1207.44181058988));
#163304=CARTESIAN_POINT('Ctrl Pts',(10.9229452762603,-14.4643171449067,
1205.94769294282));
#163305=CARTESIAN_POINT('Ctrl Pts',(9.50104767561053,-15.3447188656481,
1204.45357529576));
#163306=CARTESIAN_POINT('Ctrl Pts',(8.07915007496071,-16.2251205863895,
1202.9594576487));
#163307=CARTESIAN_POINT('Ctrl Pts',(6.51968959134574,-16.8292587962898,
1201.46534000164));
#163308=CARTESIAN_POINT('Ctrl Pts',(4.96022910773078,-17.4333970061901,
1199.97122235458));
#163309=CARTESIAN_POINT('Ctrl Pts',(3.31631129755346,-17.7406985030951,
1198.47710470753));
#163310=CARTESIAN_POINT('Ctrl Pts',(1.67239348737615,-18.048,1196.98298706047));
#163311=CARTESIAN_POINT('Ctrl Pts',(0.,-18.048,1195.48886941341));
#163312=CARTESIAN_POINT('Ctrl Pts',(-1.67239348737615,-18.048,1193.99475176635));
#163313=CARTESIAN_POINT('Ctrl Pts',(-3.31631129755346,-17.7406985030951,
1192.50063411929));
#163314=CARTESIAN_POINT('Ctrl Pts',(-4.96022910773077,-17.4333970061901,
1191.00651647223));
#163315=CARTESIAN_POINT('Ctrl Pts',(-6.51968959134574,-16.8292587962898,
1189.51239882517));
#163316=CARTESIAN_POINT('Ctrl Pts',(-8.07915007496071,-16.2251205863895,
1188.01828117811));
#163317=CARTESIAN_POINT('Ctrl Pts',(-9.50104767561052,-15.3447188656481,
1186.52416353105));
#163318=CARTESIAN_POINT('Ctrl Pts',(-10.9229452762603,-14.4643171449067,
1185.030045884));
#163319=CARTESIAN_POINT('Ctrl Pts',(-12.1588589765331,-13.3376329379985,
1183.53592823694));
#163320=CARTESIAN_POINT('Ctrl Pts',(-13.3947726768058,-12.2109487310903,
1182.04181058988));
#163321=CARTESIAN_POINT('Ctrl Pts',(-14.4026149179538,-10.8763499173728,
1180.54769294282));
#163322=CARTESIAN_POINT('Ctrl Pts',(-15.4104571591017,-9.54175110365538,
1179.05357529576));
#163323=CARTESIAN_POINT('Ctrl Pts',(-16.1559070823762,-8.04468584505497,
1177.5594576487));
#163324=CARTESIAN_POINT('Ctrl Pts',(-16.9013570056506,-6.54762058645456,
1176.06534000164));
#163325=CARTESIAN_POINT('Ctrl Pts',(-17.3590292079831,-4.93906964482095,
1174.57122235458));
#163326=CARTESIAN_POINT('Ctrl Pts',(-17.8167014103155,-3.33051870318735,
1173.07710470753));
#163327=CARTESIAN_POINT('Ctrl Pts',(-17.9710104137728,-1.66525935159368,
1171.58298706047));
#163328=CARTESIAN_POINT('Ctrl Pts',(-18.1253194172301,-1.10985572039171E-15,
1170.08886941341));
#163329=CARTESIAN_POINT('Ctrl Pts',(-17.9710104137728,1.66525935159367,
1168.59475176635));
#163330=CARTESIAN_POINT('Ctrl Pts',(-17.8167014103155,3.33051870318735,
1167.10063411929));
#163331=CARTESIAN_POINT('Ctrl Pts',(-17.3590292079831,4.93906964482096,
1165.60651647223));
#163332=CARTESIAN_POINT('Ctrl Pts',(-16.9013570056506,6.54762058645456,
1164.11239882517));
#163333=CARTESIAN_POINT('Ctrl Pts',(-16.1559070823762,8.04468584505497,
1162.61828117811));
#163334=CARTESIAN_POINT('Ctrl Pts',(-15.4104571591017,9.54175110365538,
1161.12416353106));
#163335=CARTESIAN_POINT('Ctrl Pts',(-14.4026149179538,10.8763499173728,
1159.630045884));
#163336=CARTESIAN_POINT('Ctrl Pts',(-13.3947726768058,12.2109487310903,
1158.13592823694));
#163337=CARTESIAN_POINT('Ctrl Pts',(-12.1588589765331,13.3376329379985,
1156.64181058988));
#163338=CARTESIAN_POINT('Ctrl Pts',(-10.9229452762603,14.4643171449067,
1155.14769294282));
#163339=CARTESIAN_POINT('Ctrl Pts',(-9.50104767561052,15.3447188656481,
1153.65357529576));
#163340=CARTESIAN_POINT('Ctrl Pts',(-8.07915007496071,16.2251205863895,
1152.1594576487));
#163341=CARTESIAN_POINT('Ctrl Pts',(-6.51968959134574,16.8292587962898,
1150.66534000164));
#163342=CARTESIAN_POINT('Ctrl Pts',(-4.96022910773078,17.4333970061901,
1149.17122235458));
#163343=CARTESIAN_POINT('Ctrl Pts',(-3.31631129755346,17.7406985030951,
1147.67710470753));
#163344=CARTESIAN_POINT('Ctrl Pts',(-1.67239348737615,18.048,1146.18298706047));
#163345=CARTESIAN_POINT('Ctrl Pts',(-2.21024254310115E-15,18.048,1144.68886941341));
#163346=CARTESIAN_POINT('Ctrl Pts',(1.67239348737616,18.048,1143.19475176635));
#163347=CARTESIAN_POINT('Ctrl Pts',(3.31631129755346,17.7406985030951,1141.70063411929));
#163348=CARTESIAN_POINT('Ctrl Pts',(4.96022910773077,17.4333970061901,1140.20651647223));
#163349=CARTESIAN_POINT('Ctrl Pts',(6.51968959134575,16.8292587962898,1138.71239882517));
#163350=CARTESIAN_POINT('Ctrl Pts',(8.07915007496071,16.2251205863895,1137.21828117811));
#163351=CARTESIAN_POINT('Ctrl Pts',(9.50104767561053,15.3447188656481,1135.72416353105));
#163352=CARTESIAN_POINT('Ctrl Pts',(10.9229452762603,14.4643171449067,1134.230045884));
#163353=CARTESIAN_POINT('Ctrl Pts',(12.1588589765331,13.3376329379985,1132.73592823694));
#163354=CARTESIAN_POINT('Ctrl Pts',(13.3947726768058,12.2109487310903,1131.24181058988));
#163355=CARTESIAN_POINT('Ctrl Pts',(14.4026149179538,10.8763499173728,1129.74769294282));
#163356=CARTESIAN_POINT('Ctrl Pts',(15.4104571591017,9.54175110365538,1128.25357529576));
#163357=CARTESIAN_POINT('Ctrl Pts',(16.1559070823762,8.04468584505496,1126.7594576487));
#163358=CARTESIAN_POINT('Ctrl Pts',(16.9013570056506,6.54762058645456,1125.26534000164));
#163359=CARTESIAN_POINT('Ctrl Pts',(17.3590292079831,4.93906964482096,1123.77122235458));
#163360=CARTESIAN_POINT('Ctrl Pts',(17.8167014103155,3.33051870318735,1122.27710470753));
#163361=CARTESIAN_POINT('Ctrl Pts',(17.9710104137728,1.66525935159367,1120.78298706047));
#163362=CARTESIAN_POINT('Ctrl Pts',(18.1253194172301,3.32956716117513E-15,
1119.28886941341));
#163363=CARTESIAN_POINT('Ctrl Pts',(17.9710104137728,-1.66525935159367,
1117.79475176635));
#163364=CARTESIAN_POINT('Ctrl Pts',(17.8167014103155,-3.33051870318736,
1116.30063411929));
#163365=CARTESIAN_POINT('Ctrl Pts',(17.3590292079831,-4.93906964482095,
1114.80651647223));
#163366=CARTESIAN_POINT('Ctrl Pts',(16.9013570056506,-6.54762058645456,
1113.31239882517));
#163367=CARTESIAN_POINT('Ctrl Pts',(16.1559070823762,-8.04468584505497,
1111.81828117811));
#163368=CARTESIAN_POINT('Ctrl Pts',(15.4104571591017,-9.54175110365538,
1110.32416353105));
#163369=CARTESIAN_POINT('Ctrl Pts',(14.4026149179538,-10.8763499173728,
1108.830045884));
#163370=CARTESIAN_POINT('Ctrl Pts',(13.3947726768058,-12.2109487310903,
1107.33592823694));
#163371=CARTESIAN_POINT('Ctrl Pts',(12.1588589765331,-13.3376329379985,
1105.84181058988));
#163372=CARTESIAN_POINT('Ctrl Pts',(10.9229452762603,-14.4643171449067,
1104.34769294282));
#163373=CARTESIAN_POINT('Ctrl Pts',(9.50104767561053,-15.3447188656481,
1102.85357529576));
#163374=CARTESIAN_POINT('Ctrl Pts',(8.07915007496071,-16.2251205863895,
1101.3594576487));
#163375=CARTESIAN_POINT('Ctrl Pts',(6.51968959134574,-16.8292587962898,
1099.86534000164));
#163376=CARTESIAN_POINT('Ctrl Pts',(4.96022910773078,-17.4333970061901,
1098.37122235458));
#163377=CARTESIAN_POINT('Ctrl Pts',(3.31631129755346,-17.7406985030951,
1096.87710470753));
#163378=CARTESIAN_POINT('Ctrl Pts',(1.67239348737615,-18.048,1095.38298706047));
#163379=CARTESIAN_POINT('Ctrl Pts',(0.,-18.048,1093.88886941341));
#163380=CARTESIAN_POINT('Ctrl Pts',(-1.67239348737615,-18.048,1092.39475176635));
#163381=CARTESIAN_POINT('Ctrl Pts',(-3.31631129755346,-17.7406985030951,
1090.90063411929));
#163382=CARTESIAN_POINT('Ctrl Pts',(-4.96022910773077,-17.4333970061901,
1089.40651647223));
#163383=CARTESIAN_POINT('Ctrl Pts',(-6.51968959134574,-16.8292587962898,
1087.91239882517));
#163384=CARTESIAN_POINT('Ctrl Pts',(-8.07915007496071,-16.2251205863895,
1086.41828117811));
#163385=CARTESIAN_POINT('Ctrl Pts',(-9.50104767561052,-15.3447188656481,
1084.92416353106));
#163386=CARTESIAN_POINT('Ctrl Pts',(-10.9229452762603,-14.4643171449067,
1083.430045884));
#163387=CARTESIAN_POINT('Ctrl Pts',(-12.1588589765331,-13.3376329379985,
1081.93592823694));
#163388=CARTESIAN_POINT('Ctrl Pts',(-13.3947726768058,-12.2109487310903,
1080.44181058988));
#163389=CARTESIAN_POINT('Ctrl Pts',(-14.4026149179538,-10.8763499173728,
1078.94769294282));
#163390=CARTESIAN_POINT('Ctrl Pts',(-15.4104571591017,-9.54175110365538,
1077.45357529576));
#163391=CARTESIAN_POINT('Ctrl Pts',(-16.1559070823762,-8.04468584505497,
1075.9594576487));
#163392=CARTESIAN_POINT('Ctrl Pts',(-16.9013570056506,-6.54762058645456,
1074.46534000164));
#163393=CARTESIAN_POINT('Ctrl Pts',(-17.3590292079831,-4.93906964482095,
1072.97122235458));
#163394=CARTESIAN_POINT('Ctrl Pts',(-17.8167014103155,-3.33051870318735,
1071.47710470753));
#163395=CARTESIAN_POINT('Ctrl Pts',(-17.9710104137728,-1.66525935159368,
1069.98298706047));
#163396=CARTESIAN_POINT('Ctrl Pts',(-18.1253194172301,-1.10985572039171E-15,
1068.48886941341));
#163397=CARTESIAN_POINT('Ctrl Pts',(-17.9710104137728,1.66525935159367,
1066.99475176635));
#163398=CARTESIAN_POINT('Ctrl Pts',(-17.8167014103155,3.33051870318735,
1065.50063411929));
#163399=CARTESIAN_POINT('Ctrl Pts',(-17.3590292079831,4.93906964482096,
1064.00651647223));
#163400=CARTESIAN_POINT('Ctrl Pts',(-16.9013570056506,6.54762058645456,
1062.51239882517));
#163401=CARTESIAN_POINT('Ctrl Pts',(-16.1559070823762,8.04468584505497,
1061.01828117811));
#163402=CARTESIAN_POINT('Ctrl Pts',(-15.4104571591017,9.54175110365538,
1059.52416353105));
#163403=CARTESIAN_POINT('Ctrl Pts',(-14.4026149179538,10.8763499173728,
1058.030045884));
#163404=CARTESIAN_POINT('Ctrl Pts',(-13.3947726768058,12.2109487310903,
1056.53592823694));
#163405=CARTESIAN_POINT('Ctrl Pts',(-12.1588589765331,13.3376329379985,
1055.04181058988));
#163406=CARTESIAN_POINT('Ctrl Pts',(-10.9229452762603,14.4643171449067,
1053.54769294282));
#163407=CARTESIAN_POINT('Ctrl Pts',(-9.50104767561052,15.3447188656481,
1052.05357529576));
#163408=CARTESIAN_POINT('Ctrl Pts',(-8.07915007496071,16.2251205863895,
1050.5594576487));
#163409=CARTESIAN_POINT('Ctrl Pts',(-6.51968959134574,16.8292587962898,
1049.06534000164));
#163410=CARTESIAN_POINT('Ctrl Pts',(-4.96022910773078,17.4333970061901,
1047.57122235458));
#163411=CARTESIAN_POINT('Ctrl Pts',(-3.31631129755346,17.7406985030951,
1046.07710470753));
#163412=CARTESIAN_POINT('Ctrl Pts',(-1.67239348737615,18.048,1044.58298706047));
#163413=CARTESIAN_POINT('Ctrl Pts',(-2.21024254310115E-15,18.048,1043.08886941341));
#163414=CARTESIAN_POINT('Ctrl Pts',(1.67239348737616,18.048,1041.59475176635));
#163415=CARTESIAN_POINT('Ctrl Pts',(3.31631129755346,17.7406985030951,1040.10063411929));
#163416=CARTESIAN_POINT('Ctrl Pts',(4.96022910773077,17.4333970061901,1038.60651647223));
#163417=CARTESIAN_POINT('Ctrl Pts',(6.51968959134575,16.8292587962898,1037.11239882517));
#163418=CARTESIAN_POINT('Ctrl Pts',(8.07915007496071,16.2251205863895,1035.61828117811));
#163419=CARTESIAN_POINT('Ctrl Pts',(9.50104767561053,15.3447188656481,1034.12416353105));
#163420=CARTESIAN_POINT('Ctrl Pts',(10.9229452762603,14.4643171449067,1032.630045884));
#163421=CARTESIAN_POINT('Ctrl Pts',(12.1588589765331,13.3376329379985,1031.13592823694));
#163422=CARTESIAN_POINT('Ctrl Pts',(13.3947726768058,12.2109487310903,1029.64181058988));
#163423=CARTESIAN_POINT('Ctrl Pts',(14.4026149179538,10.8763499173728,1028.14769294282));
#163424=CARTESIAN_POINT('Ctrl Pts',(15.4104571591017,9.54175110365538,1026.65357529576));
#163425=CARTESIAN_POINT('Ctrl Pts',(16.1559070823762,8.04468584505496,1025.1594576487));
#163426=CARTESIAN_POINT('Ctrl Pts',(16.9013570056506,6.54762058645456,1023.66534000164));
#163427=CARTESIAN_POINT('Ctrl Pts',(17.3590292079831,4.93906964482096,1022.17122235458));
#163428=CARTESIAN_POINT('Ctrl Pts',(17.8167014103155,3.33051870318735,1020.67710470753));
#163429=CARTESIAN_POINT('Ctrl Pts',(17.9710104137728,1.66525935159367,1019.18298706047));
#163430=CARTESIAN_POINT('Ctrl Pts',(18.1253194172301,3.32956716117513E-15,
1017.68886941341));
#163431=CARTESIAN_POINT('Ctrl Pts',(17.9710104137728,-1.66525935159367,
1016.19475176635));
#163432=CARTESIAN_POINT('Ctrl Pts',(17.8167014103155,-3.33051870318736,
1014.70063411929));
#163433=CARTESIAN_POINT('Ctrl Pts',(17.3590292079831,-4.93906964482095,
1013.20651647223));
#163434=CARTESIAN_POINT('Ctrl Pts',(16.9013570056506,-6.54762058645456,
1011.71239882517));
#163435=CARTESIAN_POINT('Ctrl Pts',(16.1559070823762,-8.04468584505497,
1010.21828117811));
#163436=CARTESIAN_POINT('Ctrl Pts',(15.4104571591017,-9.54175110365538,
1008.72416353105));
#163437=CARTESIAN_POINT('Ctrl Pts',(14.4026149179538,-10.8763499173728,
1007.230045884));
#163438=CARTESIAN_POINT('Ctrl Pts',(13.3947726768058,-12.2109487310903,
1005.73592823694));
#163439=CARTESIAN_POINT('Ctrl Pts',(12.1588589765331,-13.3376329379985,
1004.24181058988));
#163440=CARTESIAN_POINT('Ctrl Pts',(10.9229452762603,-14.4643171449067,
1002.74769294282));
#163441=CARTESIAN_POINT('Ctrl Pts',(9.50104767561053,-15.3447188656481,
1001.25357529576));
#163442=CARTESIAN_POINT('Ctrl Pts',(8.07915007496071,-16.2251205863895,
999.759457648702));
#163443=CARTESIAN_POINT('Ctrl Pts',(6.51968959134574,-16.8292587962898,
998.265340001643));
#163444=CARTESIAN_POINT('Ctrl Pts',(4.96022910773078,-17.4333970061901,
996.771222354585));
#163445=CARTESIAN_POINT('Ctrl Pts',(3.31631129755346,-17.7406985030951,
995.277104707525));
#163446=CARTESIAN_POINT('Ctrl Pts',(1.67239348737615,-18.048,993.782987060467));
#163447=CARTESIAN_POINT('Ctrl Pts',(0.,-18.048,992.288869413408));
#163448=CARTESIAN_POINT('Ctrl Pts',(-1.67239348737615,-18.048,990.794751766349));
#163449=CARTESIAN_POINT('Ctrl Pts',(-3.31631129755346,-17.7406985030951,
989.30063411929));
#163450=CARTESIAN_POINT('Ctrl Pts',(-4.96022910773077,-17.4333970061901,
987.806516472232));
#163451=CARTESIAN_POINT('Ctrl Pts',(-6.51968959134574,-16.8292587962898,
986.312398825173));
#163452=CARTESIAN_POINT('Ctrl Pts',(-8.07915007496071,-16.2251205863895,
984.818281178114));
#163453=CARTESIAN_POINT('Ctrl Pts',(-9.50104767561052,-15.3447188656481,
983.324163531055));
#163454=CARTESIAN_POINT('Ctrl Pts',(-10.9229452762603,-14.4643171449067,
981.830045883996));
#163455=CARTESIAN_POINT('Ctrl Pts',(-12.1588589765331,-13.3376329379985,
980.335928236937));
#163456=CARTESIAN_POINT('Ctrl Pts',(-13.3947726768058,-12.2109487310903,
978.841810589878));
#163457=CARTESIAN_POINT('Ctrl Pts',(-14.4026149179538,-10.8763499173728,
977.34769294282));
#163458=CARTESIAN_POINT('Ctrl Pts',(-15.4104571591017,-9.54175110365538,
975.853575295761));
#163459=CARTESIAN_POINT('Ctrl Pts',(-16.1559070823762,-8.04468584505497,
974.359457648702));
#163460=CARTESIAN_POINT('Ctrl Pts',(-16.9013570056506,-6.54762058645456,
972.865340001643));
#163461=CARTESIAN_POINT('Ctrl Pts',(-17.3590292079831,-4.93906964482095,
971.371222354584));
#163462=CARTESIAN_POINT('Ctrl Pts',(-17.8167014103155,-3.33051870318735,
969.877104707525));
#163463=CARTESIAN_POINT('Ctrl Pts',(-17.9710104137728,-1.66525935159368,
968.382987060467));
#163464=CARTESIAN_POINT('Ctrl Pts',(-18.1253194172301,-1.10985572039171E-15,
966.888869413408));
#163465=CARTESIAN_POINT('Ctrl Pts',(-17.9710104137728,1.66525935159367,
965.394751766349));
#163466=CARTESIAN_POINT('Ctrl Pts',(-17.8167014103155,3.33051870318735,
963.90063411929));
#163467=CARTESIAN_POINT('Ctrl Pts',(-17.3590292079831,4.93906964482096,
962.406516472231));
#163468=CARTESIAN_POINT('Ctrl Pts',(-16.9013570056506,6.54762058645456,
960.912398825173));
#163469=CARTESIAN_POINT('Ctrl Pts',(-16.1559070823762,8.04468584505497,
959.418281178114));
#163470=CARTESIAN_POINT('Ctrl Pts',(-15.4104571591017,9.54175110365538,
957.924163531055));
#163471=CARTESIAN_POINT('Ctrl Pts',(-14.4026149179538,10.8763499173728,
956.430045883996));
#163472=CARTESIAN_POINT('Ctrl Pts',(-13.3947726768058,12.2109487310903,
954.935928236937));
#163473=CARTESIAN_POINT('Ctrl Pts',(-12.1588589765331,13.3376329379985,
953.441810589878));
#163474=CARTESIAN_POINT('Ctrl Pts',(-10.9229452762603,14.4643171449067,
951.94769294282));
#163475=CARTESIAN_POINT('Ctrl Pts',(-9.50104767561052,15.3447188656481,
950.453575295761));
#163476=CARTESIAN_POINT('Ctrl Pts',(-8.07915007496071,16.2251205863895,
948.959457648702));
#163477=CARTESIAN_POINT('Ctrl Pts',(-6.51968959134574,16.8292587962898,
947.465340001643));
#163478=CARTESIAN_POINT('Ctrl Pts',(-4.96022910773078,17.4333970061901,
945.971222354585));
#163479=CARTESIAN_POINT('Ctrl Pts',(-3.31631129755346,17.7406985030951,
944.477104707526));
#163480=CARTESIAN_POINT('Ctrl Pts',(-1.67239348737615,18.048,942.982987060467));
#163481=CARTESIAN_POINT('Ctrl Pts',(-2.21024254310115E-15,18.048,941.488869413408));
#163482=CARTESIAN_POINT('Ctrl Pts',(1.67239348737616,18.048,939.994751766349));
#163483=CARTESIAN_POINT('Ctrl Pts',(3.31631129755346,17.7406985030951,938.50063411929));
#163484=CARTESIAN_POINT('Ctrl Pts',(4.96022910773077,17.4333970061901,937.006516472232));
#163485=CARTESIAN_POINT('Ctrl Pts',(6.51968959134575,16.8292587962898,935.512398825173));
#163486=CARTESIAN_POINT('Ctrl Pts',(8.07915007496071,16.2251205863895,934.018281178114));
#163487=CARTESIAN_POINT('Ctrl Pts',(9.50104767561053,15.3447188656481,932.524163531055));
#163488=CARTESIAN_POINT('Ctrl Pts',(10.9229452762603,14.4643171449067,931.030045883996));
#163489=CARTESIAN_POINT('Ctrl Pts',(12.1588589765331,13.3376329379985,929.535928236937));
#163490=CARTESIAN_POINT('Ctrl Pts',(13.3947726768058,12.2109487310903,928.041810589879));
#163491=CARTESIAN_POINT('Ctrl Pts',(14.4026149179538,10.8763499173728,926.54769294282));
#163492=CARTESIAN_POINT('Ctrl Pts',(15.4104571591017,9.54175110365538,925.053575295761));
#163493=CARTESIAN_POINT('Ctrl Pts',(16.1559070823762,8.04468584505496,923.559457648702));
#163494=CARTESIAN_POINT('Ctrl Pts',(16.9013570056506,6.54762058645456,922.065340001643));
#163495=CARTESIAN_POINT('Ctrl Pts',(17.3590292079831,4.93906964482096,920.571222354584));
#163496=CARTESIAN_POINT('Ctrl Pts',(17.8167014103155,3.33051870318735,919.077104707525));
#163497=CARTESIAN_POINT('Ctrl Pts',(17.9710104137728,1.66525935159367,917.582987060467));
#163498=CARTESIAN_POINT('Ctrl Pts',(18.1253194172301,3.32956716117513E-15,
916.088869413408));
#163499=CARTESIAN_POINT('Ctrl Pts',(17.9710104137728,-1.66525935159367,
914.594751766349));
#163500=CARTESIAN_POINT('Ctrl Pts',(17.8167014103155,-3.33051870318736,
913.10063411929));
#163501=CARTESIAN_POINT('Ctrl Pts',(17.3590292079831,-4.93906964482095,
911.606516472231));
#163502=CARTESIAN_POINT('Ctrl Pts',(16.9013570056506,-6.54762058645456,
910.112398825173));
#163503=CARTESIAN_POINT('Ctrl Pts',(16.1559070823762,-8.04468584505497,
908.618281178114));
#163504=CARTESIAN_POINT('Ctrl Pts',(15.4104571591017,-9.54175110365538,
907.124163531055));
#163505=CARTESIAN_POINT('Ctrl Pts',(14.4026149179538,-10.8763499173728,
905.630045883996));
#163506=CARTESIAN_POINT('Ctrl Pts',(13.3947726768058,-12.2109487310903,
904.135928236937));
#163507=CARTESIAN_POINT('Ctrl Pts',(12.1588589765331,-13.3376329379985,
902.641810589878));
#163508=CARTESIAN_POINT('Ctrl Pts',(10.9229452762603,-14.4643171449067,
901.14769294282));
#163509=CARTESIAN_POINT('Ctrl Pts',(9.50104767561053,-15.3447188656481,
899.653575295761));
#163510=CARTESIAN_POINT('Ctrl Pts',(8.07915007496071,-16.2251205863895,
898.159457648702));
#163511=CARTESIAN_POINT('Ctrl Pts',(6.51968959134574,-16.8292587962898,
896.665340001643));
#163512=CARTESIAN_POINT('Ctrl Pts',(4.96022910773078,-17.4333970061901,
895.171222354584));
#163513=CARTESIAN_POINT('Ctrl Pts',(3.31631129755346,-17.7406985030951,
893.677104707526));
#163514=CARTESIAN_POINT('Ctrl Pts',(1.67239348737615,-18.048,892.182987060467));
#163515=CARTESIAN_POINT('Ctrl Pts',(0.,-18.048,890.688869413408));
#163516=CARTESIAN_POINT('Ctrl Pts',(-1.67239348737615,-18.048,889.194751766349));
#163517=CARTESIAN_POINT('Ctrl Pts',(-3.31631129755346,-17.7406985030951,
887.70063411929));
#163518=CARTESIAN_POINT('Ctrl Pts',(-4.96022910773077,-17.4333970061901,
886.206516472232));
#163519=CARTESIAN_POINT('Ctrl Pts',(-6.51968959134574,-16.8292587962898,
884.712398825172));
#163520=CARTESIAN_POINT('Ctrl Pts',(-8.07915007496071,-16.2251205863895,
883.218281178114));
#163521=CARTESIAN_POINT('Ctrl Pts',(-9.50104767561052,-15.3447188656481,
881.724163531055));
#163522=CARTESIAN_POINT('Ctrl Pts',(-10.9229452762603,-14.4643171449067,
880.230045883996));
#163523=CARTESIAN_POINT('Ctrl Pts',(-12.1588589765331,-13.3376329379985,
878.735928236937));
#163524=CARTESIAN_POINT('Ctrl Pts',(-13.3947726768058,-12.2109487310903,
877.241810589879));
#163525=CARTESIAN_POINT('Ctrl Pts',(-14.4026149179538,-10.8763499173728,
875.74769294282));
#163526=CARTESIAN_POINT('Ctrl Pts',(-15.4104571591017,-9.54175110365538,
874.253575295761));
#163527=CARTESIAN_POINT('Ctrl Pts',(-16.1559070823762,-8.04468584505497,
872.759457648702));
#163528=CARTESIAN_POINT('Ctrl Pts',(-16.9013570056506,-6.54762058645456,
871.265340001643));
#163529=CARTESIAN_POINT('Ctrl Pts',(-17.3590292079831,-4.93906964482095,
869.771222354584));
#163530=CARTESIAN_POINT('Ctrl Pts',(-17.8167014103155,-3.33051870318735,
868.277104707525));
#163531=CARTESIAN_POINT('Ctrl Pts',(-17.9710104137728,-1.66525935159368,
866.782987060467));
#163532=CARTESIAN_POINT('Ctrl Pts',(-18.1253194172301,-1.10985572039171E-15,
865.288869413408));
#163533=CARTESIAN_POINT('Ctrl Pts',(-17.9710104137728,1.66525935159367,
863.794751766349));
#163534=CARTESIAN_POINT('Ctrl Pts',(-17.8167014103155,3.33051870318735,
862.30063411929));
#163535=CARTESIAN_POINT('Ctrl Pts',(-17.3590292079831,4.93906964482096,
860.806516472231));
#163536=CARTESIAN_POINT('Ctrl Pts',(-16.9013570056506,6.54762058645456,
859.312398825173));
#163537=CARTESIAN_POINT('Ctrl Pts',(-16.1559070823762,8.04468584505497,
857.818281178114));
#163538=CARTESIAN_POINT('Ctrl Pts',(-15.4104571591017,9.54175110365538,
856.324163531055));
#163539=CARTESIAN_POINT('Ctrl Pts',(-14.4026149179538,10.8763499173728,
854.830045883996));
#163540=CARTESIAN_POINT('Ctrl Pts',(-13.3947726768058,12.2109487310903,
853.335928236937));
#163541=CARTESIAN_POINT('Ctrl Pts',(-12.1588589765331,13.3376329379985,
851.841810589878));
#163542=CARTESIAN_POINT('Ctrl Pts',(-10.9229452762603,14.4643171449067,
850.34769294282));
#163543=CARTESIAN_POINT('Ctrl Pts',(-9.50104767561052,15.3447188656481,
848.853575295761));
#163544=CARTESIAN_POINT('Ctrl Pts',(-8.07915007496071,16.2251205863895,
847.359457648702));
#163545=CARTESIAN_POINT('Ctrl Pts',(-6.51968959134574,16.8292587962898,
845.865340001643));
#163546=CARTESIAN_POINT('Ctrl Pts',(-4.96022910773078,17.4333970061901,
844.371222354584));
#163547=CARTESIAN_POINT('Ctrl Pts',(-3.31631129755346,17.7406985030951,
842.877104707525));
#163548=CARTESIAN_POINT('Ctrl Pts',(-1.67239348737615,18.048,841.382987060467));
#163549=CARTESIAN_POINT('Ctrl Pts',(-2.21024254310115E-15,18.048,839.888869413408));
#163550=CARTESIAN_POINT('Ctrl Pts',(1.67239348737616,18.048,838.394751766349));
#163551=CARTESIAN_POINT('Ctrl Pts',(3.31631129755346,17.7406985030951,836.90063411929));
#163552=CARTESIAN_POINT('Ctrl Pts',(4.96022910773077,17.4333970061901,835.406516472232));
#163553=CARTESIAN_POINT('Ctrl Pts',(6.51968959134575,16.8292587962898,833.912398825173));
#163554=CARTESIAN_POINT('Ctrl Pts',(8.07915007496071,16.2251205863895,832.418281178114));
#163555=CARTESIAN_POINT('Ctrl Pts',(9.50104767561053,15.3447188656481,830.924163531055));
#163556=CARTESIAN_POINT('Ctrl Pts',(10.9229452762603,14.4643171449067,829.430045883996));
#163557=CARTESIAN_POINT('Ctrl Pts',(12.1588589765331,13.3376329379985,827.935928236937));
#163558=CARTESIAN_POINT('Ctrl Pts',(13.3947726768058,12.2109487310903,826.441810589879));
#163559=CARTESIAN_POINT('Ctrl Pts',(14.4026149179538,10.8763499173728,824.94769294282));
#163560=CARTESIAN_POINT('Ctrl Pts',(15.4104571591017,9.54175110365538,823.453575295761));
#163561=CARTESIAN_POINT('Ctrl Pts',(16.1559070823762,8.04468584505496,821.959457648702));
#163562=CARTESIAN_POINT('Ctrl Pts',(16.9013570056506,6.54762058645456,820.465340001643));
#163563=CARTESIAN_POINT('Ctrl Pts',(17.3590292079831,4.93906964482096,818.971222354584));
#163564=CARTESIAN_POINT('Ctrl Pts',(17.8167014103155,3.33051870318735,817.477104707526));
#163565=CARTESIAN_POINT('Ctrl Pts',(17.9710104137728,1.66525935159367,815.982987060467));
#163566=CARTESIAN_POINT('Ctrl Pts',(18.1253194172301,3.32956716117513E-15,
814.488869413408));
#163567=CARTESIAN_POINT('Ctrl Pts',(17.9710104137728,-1.66525935159367,
812.994751766349));
#163568=CARTESIAN_POINT('Ctrl Pts',(17.8167014103155,-3.33051870318736,
811.50063411929));
#163569=CARTESIAN_POINT('Ctrl Pts',(17.3590292079831,-4.93906964482095,
810.006516472231));
#163570=CARTESIAN_POINT('Ctrl Pts',(16.9013570056506,-6.54762058645456,
808.512398825172));
#163571=CARTESIAN_POINT('Ctrl Pts',(16.1559070823762,-8.04468584505497,
807.018281178114));
#163572=CARTESIAN_POINT('Ctrl Pts',(15.4104571591017,-9.54175110365538,
805.524163531055));
#163573=CARTESIAN_POINT('Ctrl Pts',(14.4026149179538,-10.8763499173728,
804.030045883996));
#163574=CARTESIAN_POINT('Ctrl Pts',(13.3947726768058,-12.2109487310903,
802.535928236937));
#163575=CARTESIAN_POINT('Ctrl Pts',(12.1588589765331,-13.3376329379985,
801.041810589878));
#163576=CARTESIAN_POINT('Ctrl Pts',(10.9229452762603,-14.4643171449067,
799.54769294282));
#163577=CARTESIAN_POINT('Ctrl Pts',(9.50104767561053,-15.3447188656481,
798.053575295761));
#163578=CARTESIAN_POINT('Ctrl Pts',(8.07915007496071,-16.2251205863895,
796.559457648702));
#163579=CARTESIAN_POINT('Ctrl Pts',(6.51968959134574,-16.8292587962898,
795.065340001643));
#163580=CARTESIAN_POINT('Ctrl Pts',(4.96022910773078,-17.4333970061901,
793.571222354584));
#163581=CARTESIAN_POINT('Ctrl Pts',(3.31631129755346,-17.7406985030951,
792.077104707525));
#163582=CARTESIAN_POINT('Ctrl Pts',(1.67239348737615,-18.048,790.582987060467));
#163583=CARTESIAN_POINT('Ctrl Pts',(0.,-18.048,789.088869413408));
#163584=CARTESIAN_POINT('Ctrl Pts',(-1.67239348737615,-18.048,787.594751766349));
#163585=CARTESIAN_POINT('Ctrl Pts',(-3.31631129755346,-17.7406985030951,
786.10063411929));
#163586=CARTESIAN_POINT('Ctrl Pts',(-4.96022910773077,-17.4333970061901,
784.606516472231));
#163587=CARTESIAN_POINT('Ctrl Pts',(-6.51968959134574,-16.8292587962898,
783.112398825173));
#163588=CARTESIAN_POINT('Ctrl Pts',(-8.07915007496071,-16.2251205863895,
781.618281178114));
#163589=CARTESIAN_POINT('Ctrl Pts',(-9.50104767561052,-15.3447188656481,
780.124163531055));
#163590=CARTESIAN_POINT('Ctrl Pts',(-10.9229452762603,-14.4643171449067,
778.630045883996));
#163591=CARTESIAN_POINT('Ctrl Pts',(-12.1588589765331,-13.3376329379985,
777.135928236937));
#163592=CARTESIAN_POINT('Ctrl Pts',(-13.3947726768058,-12.2109487310903,
775.641810589879));
#163593=CARTESIAN_POINT('Ctrl Pts',(-14.4026149179538,-10.8763499173728,
774.14769294282));
#163594=CARTESIAN_POINT('Ctrl Pts',(-15.4104571591017,-9.54175110365538,
772.653575295761));
#163595=CARTESIAN_POINT('Ctrl Pts',(-16.1559070823762,-8.04468584505497,
771.159457648702));
#163596=CARTESIAN_POINT('Ctrl Pts',(-16.9013570056506,-6.54762058645456,
769.665340001643));
#163597=CARTESIAN_POINT('Ctrl Pts',(-17.3590292079831,-4.93906964482095,
768.171222354584));
#163598=CARTESIAN_POINT('Ctrl Pts',(-17.8167014103155,-3.33051870318735,
766.677104707526));
#163599=CARTESIAN_POINT('Ctrl Pts',(-17.9710104137728,-1.66525935159368,
765.182987060467));
#163600=CARTESIAN_POINT('Ctrl Pts',(-18.1253194172301,-1.10985572039171E-15,
763.688869413408));
#163601=CARTESIAN_POINT('Ctrl Pts',(-17.9710104137728,1.66525935159367,
762.194751766349));
#163602=CARTESIAN_POINT('Ctrl Pts',(-17.8167014103155,3.33051870318735,
760.70063411929));
#163603=CARTESIAN_POINT('Ctrl Pts',(-17.3590292079831,4.93906964482096,
759.206516472231));
#163604=CARTESIAN_POINT('Ctrl Pts',(-16.9013570056506,6.54762058645456,
757.712398825172));
#163605=CARTESIAN_POINT('Ctrl Pts',(-16.1559070823762,8.04468584505497,
756.218281178114));
#163606=CARTESIAN_POINT('Ctrl Pts',(-15.4104571591017,9.54175110365538,
754.724163531055));
#163607=CARTESIAN_POINT('Ctrl Pts',(-14.4026149179538,10.8763499173728,
753.230045883996));
#163608=CARTESIAN_POINT('Ctrl Pts',(-13.3947726768058,12.2109487310903,
751.735928236937));
#163609=CARTESIAN_POINT('Ctrl Pts',(-12.1588589765331,13.3376329379985,
750.241810589878));
#163610=CARTESIAN_POINT('Ctrl Pts',(-10.9229452762603,14.4643171449067,
748.74769294282));
#163611=CARTESIAN_POINT('Ctrl Pts',(-9.50104767561052,15.3447188656481,
747.253575295761));
#163612=CARTESIAN_POINT('Ctrl Pts',(-8.07915007496071,16.2251205863895,
745.759457648702));
#163613=CARTESIAN_POINT('Ctrl Pts',(-6.51968959134574,16.8292587962898,
744.265340001643));
#163614=CARTESIAN_POINT('Ctrl Pts',(-4.96022910773078,17.4333970061901,
742.771222354584));
#163615=CARTESIAN_POINT('Ctrl Pts',(-3.31631129755346,17.7406985030951,
741.277104707525));
#163616=CARTESIAN_POINT('Ctrl Pts',(-1.67239348737615,18.048,739.782987060467));
#163617=CARTESIAN_POINT('Ctrl Pts',(-2.21024254310115E-15,18.048,738.288869413408));
#163618=CARTESIAN_POINT('Ctrl Pts',(1.67239348737616,18.048,736.794751766349));
#163619=CARTESIAN_POINT('Ctrl Pts',(3.31631129755346,17.7406985030951,735.30063411929));
#163620=CARTESIAN_POINT('Ctrl Pts',(4.96022910773077,17.4333970061901,733.806516472231));
#163621=CARTESIAN_POINT('Ctrl Pts',(6.51968959134575,16.8292587962898,732.312398825173));
#163622=CARTESIAN_POINT('Ctrl Pts',(8.07915007496071,16.2251205863895,730.818281178114));
#163623=CARTESIAN_POINT('Ctrl Pts',(9.50104767561053,15.3447188656481,729.324163531055));
#163624=CARTESIAN_POINT('Ctrl Pts',(10.9229452762603,14.4643171449067,727.830045883996));
#163625=CARTESIAN_POINT('Ctrl Pts',(12.1588589765331,13.3376329379985,726.335928236937));
#163626=CARTESIAN_POINT('Ctrl Pts',(13.3947726768058,12.2109487310903,724.841810589879));
#163627=CARTESIAN_POINT('Ctrl Pts',(14.4026149179538,10.8763499173728,723.34769294282));
#163628=CARTESIAN_POINT('Ctrl Pts',(15.4104571591017,9.54175110365538,721.853575295761));
#163629=CARTESIAN_POINT('Ctrl Pts',(16.1559070823762,8.04468584505496,720.359457648702));
#163630=CARTESIAN_POINT('Ctrl Pts',(16.9013570056506,6.54762058645456,718.865340001643));
#163631=CARTESIAN_POINT('Ctrl Pts',(17.3590292079831,4.93906964482096,717.371222354584));
#163632=CARTESIAN_POINT('Ctrl Pts',(17.8167014103155,3.33051870318735,715.877104707526));
#163633=CARTESIAN_POINT('Ctrl Pts',(17.9710104137728,1.66525935159367,714.382987060467));
#163634=CARTESIAN_POINT('Ctrl Pts',(18.1253194172301,3.32956716117513E-15,
712.888869413408));
#163635=CARTESIAN_POINT('Ctrl Pts',(17.9710104137728,-1.66525935159367,
711.394751766349));
#163636=CARTESIAN_POINT('Ctrl Pts',(17.8167014103155,-3.33051870318736,
709.90063411929));
#163637=CARTESIAN_POINT('Ctrl Pts',(17.3590292079831,-4.93906964482095,
708.406516472231));
#163638=CARTESIAN_POINT('Ctrl Pts',(16.9013570056506,-6.54762058645456,
706.912398825173));
#163639=CARTESIAN_POINT('Ctrl Pts',(16.1559070823762,-8.04468584505497,
705.418281178114));
#163640=CARTESIAN_POINT('Ctrl Pts',(15.4104571591017,-9.54175110365538,
703.924163531055));
#163641=CARTESIAN_POINT('Ctrl Pts',(14.4026149179538,-10.8763499173728,
702.430045883996));
#163642=CARTESIAN_POINT('Ctrl Pts',(13.3947726768058,-12.2109487310903,
700.935928236937));
#163643=CARTESIAN_POINT('Ctrl Pts',(12.1588589765331,-13.3376329379985,
699.441810589878));
#163644=CARTESIAN_POINT('Ctrl Pts',(10.9229452762603,-14.4643171449067,
697.94769294282));
#163645=CARTESIAN_POINT('Ctrl Pts',(9.50104767561053,-15.3447188656481,
696.453575295761));
#163646=CARTESIAN_POINT('Ctrl Pts',(8.07915007496071,-16.2251205863895,
694.959457648702));
#163647=CARTESIAN_POINT('Ctrl Pts',(6.51968959134574,-16.8292587962898,
693.465340001643));
#163648=CARTESIAN_POINT('Ctrl Pts',(4.96022910773078,-17.4333970061901,
691.971222354584));
#163649=CARTESIAN_POINT('Ctrl Pts',(3.31631129755346,-17.7406985030951,
690.477104707526));
#163650=CARTESIAN_POINT('Ctrl Pts',(1.67239348737615,-18.048,688.982987060467));
#163651=CARTESIAN_POINT('Ctrl Pts',(0.,-18.048,687.488869413408));
#163652=CARTESIAN_POINT('Ctrl Pts',(-1.67239348737615,-18.048,685.994751766349));
#163653=CARTESIAN_POINT('Ctrl Pts',(-3.31631129755346,-17.7406985030951,
684.50063411929));
#163654=CARTESIAN_POINT('Ctrl Pts',(-4.96022910773077,-17.4333970061901,
683.006516472232));
#163655=CARTESIAN_POINT('Ctrl Pts',(-6.51968959134574,-16.8292587962898,
681.512398825172));
#163656=CARTESIAN_POINT('Ctrl Pts',(-8.07915007496071,-16.2251205863895,
680.018281178114));
#163657=CARTESIAN_POINT('Ctrl Pts',(-9.50104767561052,-15.3447188656481,
678.524163531055));
#163658=CARTESIAN_POINT('Ctrl Pts',(-10.9229452762603,-14.4643171449067,
677.030045883996));
#163659=CARTESIAN_POINT('Ctrl Pts',(-12.1588589765331,-13.3376329379985,
675.535928236937));
#163660=CARTESIAN_POINT('Ctrl Pts',(-13.3947726768058,-12.2109487310903,
674.041810589878));
#163661=CARTESIAN_POINT('Ctrl Pts',(-14.4026149179538,-10.8763499173728,
672.54769294282));
#163662=CARTESIAN_POINT('Ctrl Pts',(-15.4104571591017,-9.54175110365538,
671.053575295761));
#163663=CARTESIAN_POINT('Ctrl Pts',(-16.1559070823762,-8.04468584505497,
669.559457648702));
#163664=CARTESIAN_POINT('Ctrl Pts',(-16.9013570056506,-6.54762058645456,
668.065340001643));
#163665=CARTESIAN_POINT('Ctrl Pts',(-17.3590292079831,-4.93906964482095,
666.571222354584));
#163666=CARTESIAN_POINT('Ctrl Pts',(-17.8167014103155,-3.33051870318735,
665.077104707526));
#163667=CARTESIAN_POINT('Ctrl Pts',(-17.9710104137728,-1.66525935159368,
663.582987060467));
#163668=CARTESIAN_POINT('Ctrl Pts',(-18.1253194172301,-1.10985572039171E-15,
662.088869413408));
#163669=CARTESIAN_POINT('Ctrl Pts',(-17.9710104137728,1.66525935159367,
660.594751766349));
#163670=CARTESIAN_POINT('Ctrl Pts',(-17.8167014103155,3.33051870318735,
659.10063411929));
#163671=CARTESIAN_POINT('Ctrl Pts',(-17.3590292079831,4.93906964482096,
657.606516472231));
#163672=CARTESIAN_POINT('Ctrl Pts',(-16.9013570056506,6.54762058645456,
656.112398825172));
#163673=CARTESIAN_POINT('Ctrl Pts',(-16.1559070823762,8.04468584505497,
654.618281178114));
#163674=CARTESIAN_POINT('Ctrl Pts',(-15.4104571591017,9.54175110365538,
653.124163531055));
#163675=CARTESIAN_POINT('Ctrl Pts',(-14.4026149179538,10.8763499173728,
651.630045883996));
#163676=CARTESIAN_POINT('Ctrl Pts',(-13.3947726768058,12.2109487310903,
650.135928236937));
#163677=CARTESIAN_POINT('Ctrl Pts',(-12.1588589765331,13.3376329379985,
648.641810589878));
#163678=CARTESIAN_POINT('Ctrl Pts',(-10.9229452762603,14.4643171449067,
647.14769294282));
#163679=CARTESIAN_POINT('Ctrl Pts',(-9.50104767561052,15.3447188656481,
645.653575295761));
#163680=CARTESIAN_POINT('Ctrl Pts',(-8.07915007496071,16.2251205863895,
644.159457648702));
#163681=CARTESIAN_POINT('Ctrl Pts',(-6.51968959134574,16.8292587962898,
642.665340001643));
#163682=CARTESIAN_POINT('Ctrl Pts',(-4.96022910773078,17.4333970061901,
641.171222354584));
#163683=CARTESIAN_POINT('Ctrl Pts',(-3.31631129755346,17.7406985030951,
639.677104707525));
#163684=CARTESIAN_POINT('Ctrl Pts',(-1.67239348737615,18.048,638.182987060467));
#163685=CARTESIAN_POINT('Ctrl Pts',(-2.21024254310115E-15,18.048,636.688869413408));
#163686=CARTESIAN_POINT('Ctrl Pts',(1.67239348737616,18.048,635.194751766349));
#163687=CARTESIAN_POINT('Ctrl Pts',(3.31631129755346,17.7406985030951,633.70063411929));
#163688=CARTESIAN_POINT('Ctrl Pts',(4.96022910773077,17.4333970061901,632.206516472231));
#163689=CARTESIAN_POINT('Ctrl Pts',(6.51968959134575,16.8292587962898,630.712398825172));
#163690=CARTESIAN_POINT('Ctrl Pts',(8.07915007496071,16.2251205863895,629.218281178114));
#163691=CARTESIAN_POINT('Ctrl Pts',(9.50104767561053,15.3447188656481,627.724163531055));
#163692=CARTESIAN_POINT('Ctrl Pts',(10.9229452762603,14.4643171449067,626.230045883996));
#163693=CARTESIAN_POINT('Ctrl Pts',(12.1588589765331,13.3376329379985,624.735928236937));
#163694=CARTESIAN_POINT('Ctrl Pts',(13.3947726768058,12.2109487310903,623.241810589878));
#163695=CARTESIAN_POINT('Ctrl Pts',(14.4026149179538,10.8763499173728,621.74769294282));
#163696=CARTESIAN_POINT('Ctrl Pts',(15.4104571591017,9.54175110365538,620.253575295761));
#163697=CARTESIAN_POINT('Ctrl Pts',(16.1559070823762,8.04468584505496,618.759457648702));
#163698=CARTESIAN_POINT('Ctrl Pts',(16.9013570056506,6.54762058645456,617.265340001643));
#163699=CARTESIAN_POINT('Ctrl Pts',(17.3590292079831,4.93906964482096,615.771222354584));
#163700=CARTESIAN_POINT('Ctrl Pts',(17.8167014103155,3.33051870318735,614.277104707526));
#163701=CARTESIAN_POINT('Ctrl Pts',(17.9710104137728,1.66525935159367,612.782987060467));
#163702=CARTESIAN_POINT('Ctrl Pts',(18.1253194172301,3.32956716117513E-15,
611.288869413408));
#163703=CARTESIAN_POINT('Ctrl Pts',(17.9710104137728,-1.66525935159367,
609.794751766349));
#163704=CARTESIAN_POINT('Ctrl Pts',(17.8167014103155,-3.33051870318736,
608.30063411929));
#163705=CARTESIAN_POINT('Ctrl Pts',(17.3590292079831,-4.93906964482095,
606.806516472231));
#163706=CARTESIAN_POINT('Ctrl Pts',(16.9013570056506,-6.54762058645456,
605.312398825173));
#163707=CARTESIAN_POINT('Ctrl Pts',(16.1559070823762,-8.04468584505497,
603.818281178114));
#163708=CARTESIAN_POINT('Ctrl Pts',(15.4104571591017,-9.54175110365538,
602.324163531055));
#163709=CARTESIAN_POINT('Ctrl Pts',(14.4026149179538,-10.8763499173728,
600.830045883996));
#163710=CARTESIAN_POINT('Ctrl Pts',(13.3947726768058,-12.2109487310903,
599.335928236937));
#163711=CARTESIAN_POINT('Ctrl Pts',(12.1588589765331,-13.3376329379985,
597.841810589878));
#163712=CARTESIAN_POINT('Ctrl Pts',(10.9229452762603,-14.4643171449067,
596.34769294282));
#163713=CARTESIAN_POINT('Ctrl Pts',(9.50104767561053,-15.3447188656481,
594.853575295761));
#163714=CARTESIAN_POINT('Ctrl Pts',(8.07915007496071,-16.2251205863895,
593.359457648702));
#163715=CARTESIAN_POINT('Ctrl Pts',(6.51968959134574,-16.8292587962898,
591.865340001643));
#163716=CARTESIAN_POINT('Ctrl Pts',(4.96022910773078,-17.4333970061901,
590.371222354584));
#163717=CARTESIAN_POINT('Ctrl Pts',(3.31631129755346,-17.7406985030951,
588.877104707525));
#163718=CARTESIAN_POINT('Ctrl Pts',(1.67239348737615,-18.048,587.382987060467));
#163719=CARTESIAN_POINT('Ctrl Pts',(0.,-18.048,585.888869413408));
#163720=CARTESIAN_POINT('Ctrl Pts',(-1.67239348737615,-18.048,584.394751766349));
#163721=CARTESIAN_POINT('Ctrl Pts',(-3.31631129755346,-17.7406985030951,
582.90063411929));
#163722=CARTESIAN_POINT('Ctrl Pts',(-4.96022910773077,-17.4333970061901,
581.406516472231));
#163723=CARTESIAN_POINT('Ctrl Pts',(-6.51968959134574,-16.8292587962898,
579.912398825173));
#163724=CARTESIAN_POINT('Ctrl Pts',(-8.07915007496071,-16.2251205863895,
578.418281178114));
#163725=CARTESIAN_POINT('Ctrl Pts',(-9.50104767561052,-15.3447188656481,
576.924163531055));
#163726=CARTESIAN_POINT('Ctrl Pts',(-10.9229452762603,-14.4643171449067,
575.430045883996));
#163727=CARTESIAN_POINT('Ctrl Pts',(-12.1588589765331,-13.3376329379985,
573.935928236937));
#163728=CARTESIAN_POINT('Ctrl Pts',(-13.3947726768058,-12.2109487310903,
572.441810589879));
#163729=CARTESIAN_POINT('Ctrl Pts',(-14.4026149179538,-10.8763499173728,
570.94769294282));
#163730=CARTESIAN_POINT('Ctrl Pts',(-15.4104571591017,-9.54175110365538,
569.453575295761));
#163731=CARTESIAN_POINT('Ctrl Pts',(-16.1559070823762,-8.04468584505497,
567.959457648702));
#163732=CARTESIAN_POINT('Ctrl Pts',(-16.9013570056506,-6.54762058645456,
566.465340001643));
#163733=CARTESIAN_POINT('Ctrl Pts',(-17.3590292079831,-4.93906964482095,
564.971222354584));
#163734=CARTESIAN_POINT('Ctrl Pts',(-17.8167014103155,-3.33051870318735,
563.477104707526));
#163735=CARTESIAN_POINT('Ctrl Pts',(-17.9710104137728,-1.66525935159368,
561.982987060467));
#163736=CARTESIAN_POINT('Ctrl Pts',(-18.1253194172301,-1.10985572039171E-15,
560.488869413408));
#163737=CARTESIAN_POINT('Ctrl Pts',(-17.9710104137728,1.66525935159367,
558.994751766349));
#163738=CARTESIAN_POINT('Ctrl Pts',(-17.8167014103155,3.33051870318735,
557.50063411929));
#163739=CARTESIAN_POINT('Ctrl Pts',(-17.3590292079831,4.93906964482096,
556.006516472231));
#163740=CARTESIAN_POINT('Ctrl Pts',(-16.9013570056506,6.54762058645456,
554.512398825173));
#163741=CARTESIAN_POINT('Ctrl Pts',(-16.1559070823762,8.04468584505497,
553.018281178114));
#163742=CARTESIAN_POINT('Ctrl Pts',(-15.4104571591017,9.54175110365538,
551.524163531055));
#163743=CARTESIAN_POINT('Ctrl Pts',(-14.4026149179538,10.8763499173728,
550.030045883996));
#163744=CARTESIAN_POINT('Ctrl Pts',(-13.3947726768058,12.2109487310903,
548.535928236937));
#163745=CARTESIAN_POINT('Ctrl Pts',(-12.1588589765331,13.3376329379985,
547.041810589878));
#163746=CARTESIAN_POINT('Ctrl Pts',(-10.9229452762603,14.4643171449067,
545.54769294282));
#163747=CARTESIAN_POINT('Ctrl Pts',(-9.50104767561052,15.3447188656481,
544.053575295761));
#163748=CARTESIAN_POINT('Ctrl Pts',(-8.07915007496071,16.2251205863895,
542.559457648702));
#163749=CARTESIAN_POINT('Ctrl Pts',(-6.51968959134574,16.8292587962898,
541.065340001643));
#163750=CARTESIAN_POINT('Ctrl Pts',(-4.96022910773078,17.4333970061901,
539.571222354584));
#163751=CARTESIAN_POINT('Ctrl Pts',(-3.31631129755346,17.7406985030951,
538.077104707525));
#163752=CARTESIAN_POINT('Ctrl Pts',(-1.67239348737615,18.048,536.582987060467));
#163753=CARTESIAN_POINT('Ctrl Pts',(-2.21024254310115E-15,18.048,535.088869413408));
#163754=CARTESIAN_POINT('Ctrl Pts',(1.67239348737616,18.048,533.594751766349));
#163755=CARTESIAN_POINT('Ctrl Pts',(3.31631129755346,17.7406985030951,532.10063411929));
#163756=CARTESIAN_POINT('Ctrl Pts',(4.96022910773077,17.4333970061901,530.606516472231));
#163757=CARTESIAN_POINT('Ctrl Pts',(6.51968959134575,16.8292587962898,529.112398825172));
#163758=CARTESIAN_POINT('Ctrl Pts',(8.07915007496071,16.2251205863895,527.618281178114));
#163759=CARTESIAN_POINT('Ctrl Pts',(9.50104767561053,15.3447188656481,526.124163531055));
#163760=CARTESIAN_POINT('Ctrl Pts',(10.9229452762603,14.4643171449067,524.630045883996));
#163761=CARTESIAN_POINT('Ctrl Pts',(12.1588589765331,13.3376329379985,523.135928236937));
#163762=CARTESIAN_POINT('Ctrl Pts',(13.3947726768058,12.2109487310903,521.641810589878));
#163763=CARTESIAN_POINT('Ctrl Pts',(14.4026149179538,10.8763499173728,520.14769294282));
#163764=CARTESIAN_POINT('Ctrl Pts',(15.4104571591017,9.54175110365538,518.653575295761));
#163765=CARTESIAN_POINT('Ctrl Pts',(16.1559070823762,8.04468584505496,517.159457648702));
#163766=CARTESIAN_POINT('Ctrl Pts',(16.9013570056506,6.54762058645456,515.665340001643));
#163767=CARTESIAN_POINT('Ctrl Pts',(17.3590292079831,4.93906964482096,514.171222354584));
#163768=CARTESIAN_POINT('Ctrl Pts',(17.8167014103155,3.33051870318735,512.677104707525));
#163769=CARTESIAN_POINT('Ctrl Pts',(17.9710104137728,1.66525935159367,511.182987060467));
#163770=CARTESIAN_POINT('Ctrl Pts',(18.1253194172301,3.32956716117513E-15,
509.688869413408));
#163771=CARTESIAN_POINT('Ctrl Pts',(17.9710104137728,-1.66525935159367,
508.194751766349));
#163772=CARTESIAN_POINT('Ctrl Pts',(17.8167014103155,-3.33051870318736,
506.70063411929));
#163773=CARTESIAN_POINT('Ctrl Pts',(17.3590292079831,-4.93906964482095,
505.206516472231));
#163774=CARTESIAN_POINT('Ctrl Pts',(16.9013570056506,-6.54762058645456,
503.712398825173));
#163775=CARTESIAN_POINT('Ctrl Pts',(16.1559070823762,-8.04468584505497,
502.218281178114));
#163776=CARTESIAN_POINT('Ctrl Pts',(15.4104571591017,-9.54175110365538,
500.724163531055));
#163777=CARTESIAN_POINT('Ctrl Pts',(14.4026149179538,-10.8763499173728,
499.230045883996));
#163778=CARTESIAN_POINT('Ctrl Pts',(13.3947726768058,-12.2109487310903,
497.735928236937));
#163779=CARTESIAN_POINT('Ctrl Pts',(12.1588589765331,-13.3376329379985,
496.241810589879));
#163780=CARTESIAN_POINT('Ctrl Pts',(10.9229452762603,-14.4643171449067,
494.74769294282));
#163781=CARTESIAN_POINT('Ctrl Pts',(9.50104767561053,-15.3447188656481,
493.253575295761));
#163782=CARTESIAN_POINT('Ctrl Pts',(8.07915007496071,-16.2251205863895,
491.759457648702));
#163783=CARTESIAN_POINT('Ctrl Pts',(6.51968959134574,-16.8292587962898,
490.265340001643));
#163784=CARTESIAN_POINT('Ctrl Pts',(4.96022910773078,-17.4333970061901,
488.771222354584));
#163785=CARTESIAN_POINT('Ctrl Pts',(3.31631129755346,-17.7406985030951,
487.277104707526));
#163786=CARTESIAN_POINT('Ctrl Pts',(1.67239348737615,-18.048,485.782987060467));
#163787=CARTESIAN_POINT('Ctrl Pts',(0.,-18.048,484.288869413408));
#163788=CARTESIAN_POINT('Ctrl Pts',(-1.67239348737615,-18.048,482.794751766349));
#163789=CARTESIAN_POINT('Ctrl Pts',(-3.31631129755346,-17.7406985030951,
481.30063411929));
#163790=CARTESIAN_POINT('Ctrl Pts',(-4.96022910773077,-17.4333970061901,
479.806516472231));
#163791=CARTESIAN_POINT('Ctrl Pts',(-6.51968959134574,-16.8292587962898,
478.312398825173));
#163792=CARTESIAN_POINT('Ctrl Pts',(-8.07915007496071,-16.2251205863895,
476.818281178114));
#163793=CARTESIAN_POINT('Ctrl Pts',(-9.50104767561052,-15.3447188656481,
475.324163531055));
#163794=CARTESIAN_POINT('Ctrl Pts',(-10.9229452762603,-14.4643171449067,
473.830045883996));
#163795=CARTESIAN_POINT('Ctrl Pts',(-12.1588589765331,-13.3376329379985,
472.335928236937));
#163796=CARTESIAN_POINT('Ctrl Pts',(-13.3947726768058,-12.2109487310903,
470.841810589878));
#163797=CARTESIAN_POINT('Ctrl Pts',(-14.4026149179538,-10.8763499173728,
469.34769294282));
#163798=CARTESIAN_POINT('Ctrl Pts',(-15.4104571591017,-9.54175110365538,
467.853575295761));
#163799=CARTESIAN_POINT('Ctrl Pts',(-16.1559070823762,-8.04468584505497,
466.359457648702));
#163800=CARTESIAN_POINT('Ctrl Pts',(-16.9013570056506,-6.54762058645456,
464.865340001643));
#163801=CARTESIAN_POINT('Ctrl Pts',(-17.3590292079831,-4.93906964482095,
463.371222354584));
#163802=CARTESIAN_POINT('Ctrl Pts',(-17.8167014103155,-3.33051870318735,
461.877104707525));
#163803=CARTESIAN_POINT('Ctrl Pts',(-17.9710104137728,-1.66525935159368,
460.382987060467));
#163804=CARTESIAN_POINT('Ctrl Pts',(-18.1253194172301,-1.10985572039171E-15,
458.888869413408));
#163805=CARTESIAN_POINT('Ctrl Pts',(-17.9710104137728,1.66525935159367,
457.394751766349));
#163806=CARTESIAN_POINT('Ctrl Pts',(-17.8167014103155,3.33051870318735,
455.90063411929));
#163807=CARTESIAN_POINT('Ctrl Pts',(-17.3590292079831,4.93906964482096,
454.406516472231));
#163808=CARTESIAN_POINT('Ctrl Pts',(-16.9013570056506,6.54762058645456,
452.912398825173));
#163809=CARTESIAN_POINT('Ctrl Pts',(-16.1559070823762,8.04468584505497,
451.418281178114));
#163810=CARTESIAN_POINT('Ctrl Pts',(-15.4104571591017,9.54175110365538,
449.924163531055));
#163811=CARTESIAN_POINT('Ctrl Pts',(-14.4026149179538,10.8763499173728,
448.430045883996));
#163812=CARTESIAN_POINT('Ctrl Pts',(-13.3947726768058,12.2109487310903,
446.935928236937));
#163813=CARTESIAN_POINT('Ctrl Pts',(-12.1588589765331,13.3376329379985,
445.441810589878));
#163814=CARTESIAN_POINT('Ctrl Pts',(-10.9229452762603,14.4643171449067,
443.94769294282));
#163815=CARTESIAN_POINT('Ctrl Pts',(-9.50104767561052,15.3447188656481,
442.453575295761));
#163816=CARTESIAN_POINT('Ctrl Pts',(-8.07915007496071,16.2251205863895,
440.959457648702));
#163817=CARTESIAN_POINT('Ctrl Pts',(-6.51968959134574,16.8292587962898,
439.465340001643));
#163818=CARTESIAN_POINT('Ctrl Pts',(-4.96022910773078,17.4333970061901,
437.971222354584));
#163819=CARTESIAN_POINT('Ctrl Pts',(-3.31631129755346,17.7406985030951,
436.477104707526));
#163820=CARTESIAN_POINT('Ctrl Pts',(-1.67239348737615,18.048,434.982987060467));
#163821=CARTESIAN_POINT('Ctrl Pts',(-2.21024254310115E-15,18.048,433.488869413408));
#163822=CARTESIAN_POINT('Ctrl Pts',(1.67239348737616,18.048,431.994751766349));
#163823=CARTESIAN_POINT('Ctrl Pts',(3.31631129755346,17.7406985030951,430.50063411929));
#163824=CARTESIAN_POINT('Ctrl Pts',(4.96022910773077,17.4333970061901,429.006516472231));
#163825=CARTESIAN_POINT('Ctrl Pts',(6.51968959134575,16.8292587962898,427.512398825173));
#163826=CARTESIAN_POINT('Ctrl Pts',(8.07915007496071,16.2251205863895,426.018281178114));
#163827=CARTESIAN_POINT('Ctrl Pts',(9.50104767561053,15.3447188656481,424.524163531055));
#163828=CARTESIAN_POINT('Ctrl Pts',(10.9229452762603,14.4643171449067,423.030045883996));
#163829=CARTESIAN_POINT('Ctrl Pts',(12.1588589765331,13.3376329379985,421.535928236937));
#163830=CARTESIAN_POINT('Ctrl Pts',(13.3947726768058,12.2109487310903,420.041810589879));
#163831=CARTESIAN_POINT('Ctrl Pts',(14.4026149179538,10.8763499173728,418.54769294282));
#163832=CARTESIAN_POINT('Ctrl Pts',(15.4104571591017,9.54175110365538,417.053575295761));
#163833=CARTESIAN_POINT('Ctrl Pts',(16.1559070823762,8.04468584505496,415.559457648702));
#163834=CARTESIAN_POINT('Ctrl Pts',(16.9013570056506,6.54762058645456,414.065340001643));
#163835=CARTESIAN_POINT('Ctrl Pts',(17.3590292079831,4.93906964482096,412.571222354584));
#163836=CARTESIAN_POINT('Ctrl Pts',(17.8167014103155,3.33051870318735,411.077104707526));
#163837=CARTESIAN_POINT('Ctrl Pts',(17.9710104137728,1.66525935159367,409.582987060467));
#163838=CARTESIAN_POINT('Ctrl Pts',(18.1253194172301,3.32956716117513E-15,
408.088869413408));
#163839=CARTESIAN_POINT('Ctrl Pts',(17.9710104137728,-1.66525935159367,
406.594751766349));
#163840=CARTESIAN_POINT('Ctrl Pts',(17.8167014103155,-3.33051870318736,
405.10063411929));
#163841=CARTESIAN_POINT('Ctrl Pts',(17.3590292079831,-4.93906964482095,
403.606516472231));
#163842=CARTESIAN_POINT('Ctrl Pts',(16.9013570056506,-6.54762058645456,
402.112398825173));
#163843=CARTESIAN_POINT('Ctrl Pts',(16.1559070823762,-8.04468584505497,
400.618281178114));
#163844=CARTESIAN_POINT('Ctrl Pts',(15.4104571591017,-9.54175110365538,
399.124163531055));
#163845=CARTESIAN_POINT('Ctrl Pts',(14.4026149179538,-10.8763499173728,
397.630045883996));
#163846=CARTESIAN_POINT('Ctrl Pts',(13.3947726768058,-12.2109487310903,
396.135928236937));
#163847=CARTESIAN_POINT('Ctrl Pts',(12.1588589765331,-13.3376329379985,
394.641810589878));
#163848=CARTESIAN_POINT('Ctrl Pts',(10.9229452762603,-14.4643171449067,
393.147692942819));
#163849=CARTESIAN_POINT('Ctrl Pts',(9.50104767561053,-15.3447188656481,
391.653575295761));
#163850=CARTESIAN_POINT('Ctrl Pts',(8.07915007496071,-16.2251205863895,
390.159457648702));
#163851=CARTESIAN_POINT('Ctrl Pts',(6.51968959134574,-16.8292587962898,
388.665340001643));
#163852=CARTESIAN_POINT('Ctrl Pts',(4.96022910773078,-17.4333970061901,
387.171222354584));
#163853=CARTESIAN_POINT('Ctrl Pts',(3.31631129755346,-17.7406985030951,
385.677104707525));
#163854=CARTESIAN_POINT('Ctrl Pts',(1.67239348737615,-18.048,384.182987060467));
#163855=CARTESIAN_POINT('Ctrl Pts',(0.,-18.048,382.688869413408));
#163856=CARTESIAN_POINT('Ctrl Pts',(-1.67239348737615,-18.048,381.194751766349));
#163857=CARTESIAN_POINT('Ctrl Pts',(-3.31631129755346,-17.7406985030951,
379.70063411929));
#163858=CARTESIAN_POINT('Ctrl Pts',(-4.96022910773077,-17.4333970061901,
378.206516472231));
#163859=CARTESIAN_POINT('Ctrl Pts',(-6.51968959134574,-16.8292587962898,
376.712398825173));
#163860=CARTESIAN_POINT('Ctrl Pts',(-8.07915007496071,-16.2251205863895,
375.218281178114));
#163861=CARTESIAN_POINT('Ctrl Pts',(-9.50104767561052,-15.3447188656481,
373.724163531055));
#163862=CARTESIAN_POINT('Ctrl Pts',(-10.9229452762603,-14.4643171449067,
372.230045883996));
#163863=CARTESIAN_POINT('Ctrl Pts',(-12.1588589765331,-13.3376329379985,
370.735928236937));
#163864=CARTESIAN_POINT('Ctrl Pts',(-13.3947726768058,-12.2109487310903,
369.241810589879));
#163865=CARTESIAN_POINT('Ctrl Pts',(-14.4026149179538,-10.8763499173728,
367.74769294282));
#163866=CARTESIAN_POINT('Ctrl Pts',(-15.4104571591017,-9.54175110365538,
366.253575295761));
#163867=CARTESIAN_POINT('Ctrl Pts',(-16.1559070823762,-8.04468584505497,
364.759457648702));
#163868=CARTESIAN_POINT('Ctrl Pts',(-16.9013570056506,-6.54762058645456,
363.265340001643));
#163869=CARTESIAN_POINT('Ctrl Pts',(-17.3590292079831,-4.93906964482095,
361.771222354584));
#163870=CARTESIAN_POINT('Ctrl Pts',(-17.8167014103155,-3.33051870318735,
360.277104707525));
#163871=CARTESIAN_POINT('Ctrl Pts',(-17.9710104137728,-1.66525935159368,
358.782987060467));
#163872=CARTESIAN_POINT('Ctrl Pts',(-18.1253194172301,-1.10985572039171E-15,
357.288869413408));
#163873=CARTESIAN_POINT('Ctrl Pts',(-17.9710104137728,1.66525935159367,
355.794751766349));
#163874=CARTESIAN_POINT('Ctrl Pts',(-17.8167014103155,3.33051870318735,
354.30063411929));
#163875=CARTESIAN_POINT('Ctrl Pts',(-17.3590292079831,4.93906964482096,
352.806516472231));
#163876=CARTESIAN_POINT('Ctrl Pts',(-16.9013570056506,6.54762058645456,
351.312398825173));
#163877=CARTESIAN_POINT('Ctrl Pts',(-16.1559070823762,8.04468584505497,
349.818281178114));
#163878=CARTESIAN_POINT('Ctrl Pts',(-15.4104571591017,9.54175110365538,
348.324163531055));
#163879=CARTESIAN_POINT('Ctrl Pts',(-14.4026149179538,10.8763499173728,
346.830045883996));
#163880=CARTESIAN_POINT('Ctrl Pts',(-13.3947726768058,12.2109487310903,
345.335928236937));
#163881=CARTESIAN_POINT('Ctrl Pts',(-12.1588589765331,13.3376329379985,
343.841810589878));
#163882=CARTESIAN_POINT('Ctrl Pts',(-10.9229452762603,14.4643171449067,
342.34769294282));
#163883=CARTESIAN_POINT('Ctrl Pts',(-9.50104767561052,15.3447188656481,
340.853575295761));
#163884=CARTESIAN_POINT('Ctrl Pts',(-8.07915007496071,16.2251205863895,
339.359457648702));
#163885=CARTESIAN_POINT('Ctrl Pts',(-6.51968959134574,16.8292587962898,
337.865340001643));
#163886=CARTESIAN_POINT('Ctrl Pts',(-4.96022910773078,17.4333970061901,
336.371222354584));
#163887=CARTESIAN_POINT('Ctrl Pts',(-3.31631129755346,17.7406985030951,
334.877104707525));
#163888=CARTESIAN_POINT('Ctrl Pts',(-1.67239348737615,18.048,333.382987060467));
#163889=CARTESIAN_POINT('Ctrl Pts',(-2.21024254310115E-15,18.048,331.888869413408));
#163890=CARTESIAN_POINT('Ctrl Pts',(1.67239348737616,18.048,330.394751766349));
#163891=CARTESIAN_POINT('Ctrl Pts',(3.31631129755346,17.7406985030951,328.90063411929));
#163892=CARTESIAN_POINT('Ctrl Pts',(4.96022910773077,17.4333970061901,327.406516472231));
#163893=CARTESIAN_POINT('Ctrl Pts',(6.51968959134575,16.8292587962898,325.912398825172));
#163894=CARTESIAN_POINT('Ctrl Pts',(8.07915007496071,16.2251205863895,324.418281178114));
#163895=CARTESIAN_POINT('Ctrl Pts',(9.50104767561053,15.3447188656481,322.924163531055));
#163896=CARTESIAN_POINT('Ctrl Pts',(10.9229452762603,14.4643171449067,321.430045883996));
#163897=CARTESIAN_POINT('Ctrl Pts',(12.1588589765331,13.3376329379985,319.935928236937));
#163898=CARTESIAN_POINT('Ctrl Pts',(13.3947726768058,12.2109487310903,318.441810589878));
#163899=CARTESIAN_POINT('Ctrl Pts',(14.4026149179538,10.8763499173728,316.94769294282));
#163900=CARTESIAN_POINT('Ctrl Pts',(15.4104571591017,9.54175110365538,315.453575295761));
#163901=CARTESIAN_POINT('Ctrl Pts',(16.1559070823762,8.04468584505496,313.959457648702));
#163902=CARTESIAN_POINT('Ctrl Pts',(16.9013570056506,6.54762058645456,312.465340001643));
#163903=CARTESIAN_POINT('Ctrl Pts',(17.3590292079831,4.93906964482096,310.971222354584));
#163904=CARTESIAN_POINT('Ctrl Pts',(17.8167014103155,3.33051870318735,309.477104707526));
#163905=CARTESIAN_POINT('Ctrl Pts',(17.9710104137728,1.66525935159367,307.982987060467));
#163906=CARTESIAN_POINT('Ctrl Pts',(18.1253194172301,3.32956716117513E-15,
306.488869413408));
#163907=CARTESIAN_POINT('Ctrl Pts',(17.9710104137728,-1.66525935159367,
304.994751766349));
#163908=CARTESIAN_POINT('Ctrl Pts',(17.8167014103155,-3.33051870318736,
303.50063411929));
#163909=CARTESIAN_POINT('Ctrl Pts',(17.3590292079831,-4.93906964482095,
302.006516472231));
#163910=CARTESIAN_POINT('Ctrl Pts',(16.9013570056506,-6.54762058645456,
300.512398825173));
#163911=CARTESIAN_POINT('Ctrl Pts',(16.1559070823762,-8.04468584505497,
299.018281178114));
#163912=CARTESIAN_POINT('Ctrl Pts',(15.4104571591017,-9.54175110365538,
297.524163531055));
#163913=CARTESIAN_POINT('Ctrl Pts',(14.4026149179538,-10.8763499173728,
296.030045883996));
#163914=CARTESIAN_POINT('Ctrl Pts',(13.3947726768058,-12.2109487310903,
294.535928236937));
#163915=CARTESIAN_POINT('Ctrl Pts',(12.1588589765331,-13.3376329379985,
293.041810589878));
#163916=CARTESIAN_POINT('Ctrl Pts',(10.9229452762603,-14.4643171449067,
291.54769294282));
#163917=CARTESIAN_POINT('Ctrl Pts',(9.50104767561053,-15.3447188656481,
290.053575295761));
#163918=CARTESIAN_POINT('Ctrl Pts',(8.07915007496071,-16.2251205863895,
288.559457648702));
#163919=CARTESIAN_POINT('Ctrl Pts',(6.51968959134574,-16.8292587962898,
287.065340001643));
#163920=CARTESIAN_POINT('Ctrl Pts',(4.96022910773078,-17.4333970061901,
285.571222354584));
#163921=CARTESIAN_POINT('Ctrl Pts',(3.31631129755346,-17.7406985030951,
284.077104707525));
#163922=CARTESIAN_POINT('Ctrl Pts',(1.67239348737615,-18.048,282.582987060467));
#163923=CARTESIAN_POINT('Ctrl Pts',(0.,-18.048,281.088869413408));
#163924=CARTESIAN_POINT('Ctrl Pts',(-1.67239348737615,-18.048,279.594751766349));
#163925=CARTESIAN_POINT('Ctrl Pts',(-3.31631129755346,-17.7406985030951,
278.10063411929));
#163926=CARTESIAN_POINT('Ctrl Pts',(-4.96022910773077,-17.4333970061901,
276.606516472231));
#163927=CARTESIAN_POINT('Ctrl Pts',(-6.51968959134574,-16.8292587962898,
275.112398825172));
#163928=CARTESIAN_POINT('Ctrl Pts',(-8.07915007496071,-16.2251205863895,
273.618281178114));
#163929=CARTESIAN_POINT('Ctrl Pts',(-9.50104767561052,-15.3447188656481,
272.124163531055));
#163930=CARTESIAN_POINT('Ctrl Pts',(-10.9229452762603,-14.4643171449067,
270.630045883996));
#163931=CARTESIAN_POINT('Ctrl Pts',(-12.1588589765331,-13.3376329379985,
269.135928236937));
#163932=CARTESIAN_POINT('Ctrl Pts',(-13.3947726768058,-12.2109487310903,
267.641810589878));
#163933=CARTESIAN_POINT('Ctrl Pts',(-14.4026149179538,-10.8763499173728,
266.14769294282));
#163934=CARTESIAN_POINT('Ctrl Pts',(-15.4104571591017,-9.54175110365538,
264.653575295761));
#163935=CARTESIAN_POINT('Ctrl Pts',(-16.1559070823762,-8.04468584505497,
263.159457648702));
#163936=CARTESIAN_POINT('Ctrl Pts',(-16.9013570056506,-6.54762058645456,
261.665340001643));
#163937=CARTESIAN_POINT('Ctrl Pts',(-17.3590292079831,-4.93906964482095,
260.171222354584));
#163938=CARTESIAN_POINT('Ctrl Pts',(-17.8167014103155,-3.33051870318735,
258.677104707525));
#163939=CARTESIAN_POINT('Ctrl Pts',(-17.9710104137728,-1.66525935159368,
257.182987060467));
#163940=CARTESIAN_POINT('Ctrl Pts',(-18.1253194172301,-1.10985572039171E-15,
255.688869413408));
#163941=CARTESIAN_POINT('Ctrl Pts',(-17.9710104137728,1.66525935159367,
254.194751766349));
#163942=CARTESIAN_POINT('Ctrl Pts',(-17.8167014103155,3.33051870318735,
252.70063411929));
#163943=CARTESIAN_POINT('Ctrl Pts',(-17.3590292079831,4.93906964482096,
251.206516472231));
#163944=CARTESIAN_POINT('Ctrl Pts',(-16.9013570056506,6.54762058645456,
249.712398825173));
#163945=CARTESIAN_POINT('Ctrl Pts',(-16.1559070823762,8.04468584505497,
248.218281178114));
#163946=CARTESIAN_POINT('Ctrl Pts',(-15.4104571591017,9.54175110365538,
246.724163531055));
#163947=CARTESIAN_POINT('Ctrl Pts',(-14.4026149179538,10.8763499173728,
245.230045883996));
#163948=CARTESIAN_POINT('Ctrl Pts',(-13.3947726768058,12.2109487310903,
243.735928236937));
#163949=CARTESIAN_POINT('Ctrl Pts',(-12.1588589765331,13.3376329379985,
242.241810589878));
#163950=CARTESIAN_POINT('Ctrl Pts',(-10.9229452762603,14.4643171449067,
240.74769294282));
#163951=CARTESIAN_POINT('Ctrl Pts',(-9.50104767561052,15.3447188656481,
239.253575295761));
#163952=CARTESIAN_POINT('Ctrl Pts',(-8.07915007496071,16.2251205863895,
237.759457648702));
#163953=CARTESIAN_POINT('Ctrl Pts',(-6.51968959134574,16.8292587962898,
236.265340001643));
#163954=CARTESIAN_POINT('Ctrl Pts',(-4.96022910773078,17.4333970061901,
234.771222354584));
#163955=CARTESIAN_POINT('Ctrl Pts',(-3.31631129755346,17.7406985030951,
233.277104707525));
#163956=CARTESIAN_POINT('Ctrl Pts',(-1.67239348737615,18.048,231.782987060467));
#163957=CARTESIAN_POINT('Ctrl Pts',(-2.21024254310115E-15,18.048,230.288869413408));
#163958=CARTESIAN_POINT('Ctrl Pts',(1.67239348737616,18.048,228.794751766349));
#163959=CARTESIAN_POINT('Ctrl Pts',(3.31631129755346,17.7406985030951,227.30063411929));
#163960=CARTESIAN_POINT('Ctrl Pts',(4.96022910773077,17.4333970061901,225.806516472231));
#163961=CARTESIAN_POINT('Ctrl Pts',(6.51968959134575,16.8292587962898,224.312398825173));
#163962=CARTESIAN_POINT('Ctrl Pts',(8.07915007496071,16.2251205863895,222.818281178114));
#163963=CARTESIAN_POINT('Ctrl Pts',(9.50104767561053,15.3447188656481,221.324163531055));
#163964=CARTESIAN_POINT('Ctrl Pts',(10.9229452762603,14.4643171449067,219.830045883996));
#163965=CARTESIAN_POINT('Ctrl Pts',(12.1588589765331,13.3376329379985,218.335928236937));
#163966=CARTESIAN_POINT('Ctrl Pts',(13.3947726768058,12.2109487310903,216.841810589878));
#163967=CARTESIAN_POINT('Ctrl Pts',(14.4026149179538,10.8763499173728,215.34769294282));
#163968=CARTESIAN_POINT('Ctrl Pts',(15.4104571591017,9.54175110365538,213.853575295761));
#163969=CARTESIAN_POINT('Ctrl Pts',(16.1559070823762,8.04468584505496,212.359457648702));
#163970=CARTESIAN_POINT('Ctrl Pts',(16.9013570056506,6.54762058645456,210.865340001643));
#163971=CARTESIAN_POINT('Ctrl Pts',(17.3590292079831,4.93906964482096,209.371222354584));
#163972=CARTESIAN_POINT('Ctrl Pts',(17.8167014103155,3.33051870318735,207.877104707525));
#163973=CARTESIAN_POINT('Ctrl Pts',(17.9710104137728,1.66525935159367,206.382987060467));
#163974=CARTESIAN_POINT('Ctrl Pts',(18.1253194172301,3.32956716117513E-15,
204.888869413408));
#163975=CARTESIAN_POINT('Ctrl Pts',(17.9710104137728,-1.66525935159367,
203.394751766349));
#163976=CARTESIAN_POINT('Ctrl Pts',(17.8167014103155,-3.33051870318736,
201.90063411929));
#163977=CARTESIAN_POINT('Ctrl Pts',(17.3590292079831,-4.93906964482095,
200.406516472231));
#163978=CARTESIAN_POINT('Ctrl Pts',(16.9013570056506,-6.54762058645456,
198.912398825172));
#163979=CARTESIAN_POINT('Ctrl Pts',(16.1559070823762,-8.04468584505497,
197.418281178114));
#163980=CARTESIAN_POINT('Ctrl Pts',(15.4104571591017,-9.54175110365538,
195.924163531055));
#163981=CARTESIAN_POINT('Ctrl Pts',(14.4026149179538,-10.8763499173728,
194.430045883996));
#163982=CARTESIAN_POINT('Ctrl Pts',(13.3947726768058,-12.2109487310903,
192.935928236937));
#163983=CARTESIAN_POINT('Ctrl Pts',(12.1588589765331,-13.3376329379985,
191.441810589878));
#163984=CARTESIAN_POINT('Ctrl Pts',(10.9229452762603,-14.4643171449067,
189.94769294282));
#163985=CARTESIAN_POINT('Ctrl Pts',(9.50104767561053,-15.3447188656481,
188.453575295761));
#163986=CARTESIAN_POINT('Ctrl Pts',(8.07915007496071,-16.2251205863895,
186.959457648702));
#163987=CARTESIAN_POINT('Ctrl Pts',(6.51968959134574,-16.8292587962898,
185.465340001643));
#163988=CARTESIAN_POINT('Ctrl Pts',(4.96022910773078,-17.4333970061901,
183.971222354584));
#163989=CARTESIAN_POINT('Ctrl Pts',(3.31631129755346,-17.7406985030951,
182.477104707526));
#163990=CARTESIAN_POINT('Ctrl Pts',(1.67239348737615,-18.048,180.982987060467));
#163991=CARTESIAN_POINT('Ctrl Pts',(0.,-18.048,179.488869413408));
#163992=CARTESIAN_POINT('Ctrl Pts',(-1.67239348737615,-18.048,177.994751766349));
#163993=CARTESIAN_POINT('Ctrl Pts',(-3.31631129755346,-17.7406985030951,
176.50063411929));
#163994=CARTESIAN_POINT('Ctrl Pts',(-4.96022910773077,-17.4333970061901,
175.006516472231));
#163995=CARTESIAN_POINT('Ctrl Pts',(-6.51968959134574,-16.8292587962898,
173.512398825173));
#163996=CARTESIAN_POINT('Ctrl Pts',(-8.07915007496071,-16.2251205863895,
172.018281178114));
#163997=CARTESIAN_POINT('Ctrl Pts',(-9.50104767561052,-15.3447188656481,
170.524163531055));
#163998=CARTESIAN_POINT('Ctrl Pts',(-10.9229452762603,-14.4643171449067,
169.030045883996));
#163999=CARTESIAN_POINT('Ctrl Pts',(-12.1588589765331,-13.3376329379985,
167.535928236937));
#164000=CARTESIAN_POINT('Ctrl Pts',(-13.3947726768058,-12.2109487310903,
166.041810589878));
#164001=CARTESIAN_POINT('Ctrl Pts',(-14.4026149179538,-10.8763499173728,
164.54769294282));
#164002=CARTESIAN_POINT('Ctrl Pts',(-15.4104571591017,-9.54175110365538,
163.053575295761));
#164003=CARTESIAN_POINT('Ctrl Pts',(-16.1559070823762,-8.04468584505497,
161.559457648702));
#164004=CARTESIAN_POINT('Ctrl Pts',(-16.9013570056506,-6.54762058645456,
160.065340001643));
#164005=CARTESIAN_POINT('Ctrl Pts',(-17.3590292079831,-4.93906964482095,
158.571222354584));
#164006=CARTESIAN_POINT('Ctrl Pts',(-17.8167014103155,-3.33051870318735,
157.077104707525));
#164007=CARTESIAN_POINT('Ctrl Pts',(-17.9710104137728,-1.66525935159368,
155.582987060467));
#164008=CARTESIAN_POINT('Ctrl Pts',(-18.1253194172301,-1.10985572039171E-15,
154.088869413408));
#164009=CARTESIAN_POINT('Ctrl Pts',(-17.9710104137728,1.66525935159367,
152.594751766349));
#164010=CARTESIAN_POINT('Ctrl Pts',(-17.8167014103155,3.33051870318735,
151.10063411929));
#164011=CARTESIAN_POINT('Ctrl Pts',(-17.3590292079831,4.93906964482096,
149.606516472231));
#164012=CARTESIAN_POINT('Ctrl Pts',(-16.9013570056506,6.54762058645456,
148.112398825172));
#164013=CARTESIAN_POINT('Ctrl Pts',(-16.1559070823762,8.04468584505497,
146.618281178114));
#164014=CARTESIAN_POINT('Ctrl Pts',(-15.4104571591017,9.54175110365538,
145.124163531055));
#164015=CARTESIAN_POINT('Ctrl Pts',(-14.4026149179538,10.8763499173728,
143.630045883996));
#164016=CARTESIAN_POINT('Ctrl Pts',(-13.3947726768058,12.2109487310903,
142.135928236937));
#164017=CARTESIAN_POINT('Ctrl Pts',(-12.1588589765331,13.3376329379985,
140.641810589878));
#164018=CARTESIAN_POINT('Ctrl Pts',(-10.9229452762603,14.4643171449067,
139.147692942819));
#164019=CARTESIAN_POINT('Ctrl Pts',(-9.50104767561052,15.3447188656481,
137.653575295761));
#164020=CARTESIAN_POINT('Ctrl Pts',(-8.07915007496071,16.2251205863895,
136.159457648702));
#164021=CARTESIAN_POINT('Ctrl Pts',(-6.51968959134574,16.8292587962898,
134.665340001643));
#164022=CARTESIAN_POINT('Ctrl Pts',(-4.96022910773078,17.4333970061901,
133.171222354584));
#164023=CARTESIAN_POINT('Ctrl Pts',(-3.31631129755346,17.7406985030951,
131.677104707525));
#164024=CARTESIAN_POINT('Ctrl Pts',(-1.67239348737615,18.048,130.182987060467));
#164025=CARTESIAN_POINT('Ctrl Pts',(-2.21024254310115E-15,18.048,128.688869413408));
#164026=CARTESIAN_POINT('Ctrl Pts',(1.67239348737616,18.048,127.194751766349));
#164027=CARTESIAN_POINT('Ctrl Pts',(3.31631129755346,17.7406985030951,125.70063411929));
#164028=CARTESIAN_POINT('Ctrl Pts',(4.96022910773077,17.4333970061901,124.206516472231));
#164029=CARTESIAN_POINT('Ctrl Pts',(6.51968959134575,16.8292587962898,122.712398825173));
#164030=CARTESIAN_POINT('Ctrl Pts',(8.07915007496071,16.2251205863895,121.218281178114));
#164031=CARTESIAN_POINT('Ctrl Pts',(9.50104767561053,15.3447188656481,119.724163531055));
#164032=CARTESIAN_POINT('Ctrl Pts',(10.9229452762603,14.4643171449067,118.230045883996));
#164033=CARTESIAN_POINT('Ctrl Pts',(12.1588589765331,13.3376329379985,116.735928236937));
#164034=CARTESIAN_POINT('Ctrl Pts',(13.3947726768058,12.2109487310903,115.241810589878));
#164035=CARTESIAN_POINT('Ctrl Pts',(14.4026149179538,10.8763499173728,113.74769294282));
#164036=CARTESIAN_POINT('Ctrl Pts',(15.4104571591017,9.54175110365538,112.253575295761));
#164037=CARTESIAN_POINT('Ctrl Pts',(16.1559070823762,8.04468584505496,110.759457648702));
#164038=CARTESIAN_POINT('Ctrl Pts',(16.9013570056506,6.54762058645456,109.265340001643));
#164039=CARTESIAN_POINT('Ctrl Pts',(17.3590292079831,4.93906964482096,107.771222354584));
#164040=CARTESIAN_POINT('Ctrl Pts',(17.8167014103155,3.33051870318735,106.277104707526));
#164041=CARTESIAN_POINT('Ctrl Pts',(17.9710104137728,1.66525935159367,104.782987060467));
#164042=CARTESIAN_POINT('Ctrl Pts',(18.1253194172301,3.32956716117513E-15,
103.288869413408));
#164043=CARTESIAN_POINT('Ctrl Pts',(17.9710104137728,-1.66525935159367,
101.794751766349));
#164044=CARTESIAN_POINT('Ctrl Pts',(17.8167014103155,-3.33051870318736,
100.30063411929));
#164045=CARTESIAN_POINT('Ctrl Pts',(17.3590292079831,-4.93906964482095,
98.8065164722314));
#164046=CARTESIAN_POINT('Ctrl Pts',(16.9013570056506,-6.54762058645456,
97.3123988251725));
#164047=CARTESIAN_POINT('Ctrl Pts',(16.1559070823762,-8.04468584505497,
95.8182811781136));
#164048=CARTESIAN_POINT('Ctrl Pts',(15.4104571591017,-9.54175110365538,
94.3241635310548));
#164049=CARTESIAN_POINT('Ctrl Pts',(14.4026149179538,-10.8763499173728,
92.8300458839961));
#164050=CARTESIAN_POINT('Ctrl Pts',(13.3947726768058,-12.2109487310903,
91.3359282369372));
#164051=CARTESIAN_POINT('Ctrl Pts',(12.1588589765331,-13.3376329379985,
89.8418105898784));
#164052=CARTESIAN_POINT('Ctrl Pts',(10.9229452762603,-14.4643171449067,
88.3476929428195));
#164053=CARTESIAN_POINT('Ctrl Pts',(9.50104767561053,-15.3447188656481,
86.8535752957606));
#164054=CARTESIAN_POINT('Ctrl Pts',(8.07915007496071,-16.2251205863895,
85.359457648702));
#164055=CARTESIAN_POINT('Ctrl Pts',(6.51968959134574,-16.8292587962898,
83.8653400016432));
#164056=CARTESIAN_POINT('Ctrl Pts',(4.96022910773078,-17.4333970061901,
82.3712223545843));
#164057=CARTESIAN_POINT('Ctrl Pts',(3.31631129755346,-17.7406985030951,
80.8771047075254));
#164058=CARTESIAN_POINT('Ctrl Pts',(1.67239348737615,-18.048,79.3829870604665));
#164059=CARTESIAN_POINT('Ctrl Pts',(0.,-18.048,77.8888694134079));
#164060=CARTESIAN_POINT('Ctrl Pts',(-1.67239348737615,-18.048,76.394751766349));
#164061=CARTESIAN_POINT('Ctrl Pts',(-3.31631129755346,-17.7406985030951,
74.9006341192902));
#164062=CARTESIAN_POINT('Ctrl Pts',(-4.96022910773077,-17.4333970061901,
73.4065164722313));
#164063=CARTESIAN_POINT('Ctrl Pts',(-6.51968959134574,-16.8292587962898,
71.9123988251724));
#164064=CARTESIAN_POINT('Ctrl Pts',(-8.07915007496071,-16.2251205863895,
70.4182811781138));
#164065=CARTESIAN_POINT('Ctrl Pts',(-9.50104767561052,-15.3447188656481,
68.9241635310549));
#164066=CARTESIAN_POINT('Ctrl Pts',(-10.9229452762603,-14.4643171449067,
67.430045883996));
#164067=CARTESIAN_POINT('Ctrl Pts',(-12.1588589765331,-13.3376329379985,
65.9359282369372));
#164068=CARTESIAN_POINT('Ctrl Pts',(-13.3947726768058,-12.2109487310903,
64.4418105898783));
#164069=CARTESIAN_POINT('Ctrl Pts',(-14.4026149179538,-10.8763499173728,
62.9476929428197));
#164070=CARTESIAN_POINT('Ctrl Pts',(-15.4104571591017,-9.54175110365538,
61.4535752957608));
#164071=CARTESIAN_POINT('Ctrl Pts',(-16.1559070823762,-8.04468584505497,
59.9594576487019));
#164072=CARTESIAN_POINT('Ctrl Pts',(-16.9013570056506,-6.54762058645456,
58.4653400016431));
#164073=CARTESIAN_POINT('Ctrl Pts',(-17.3590292079831,-4.93906964482095,
56.9712223545842));
#164074=CARTESIAN_POINT('Ctrl Pts',(-17.8167014103155,-3.33051870318735,
55.4771047075255));
#164075=CARTESIAN_POINT('Ctrl Pts',(-17.9710104137728,-1.66525935159368,
53.9829870604667));
#164076=CARTESIAN_POINT('Ctrl Pts',(-18.1253194172301,-1.10985572039171E-15,
52.4888694134078));
#164077=CARTESIAN_POINT('Ctrl Pts',(-17.9710104137728,1.66525935159367,
50.9947517663489));
#164078=CARTESIAN_POINT('Ctrl Pts',(-17.8167014103155,3.33051870318735,
49.5006341192901));
#164079=CARTESIAN_POINT('Ctrl Pts',(-17.3590292079831,4.93906964482096,
48.0065164722314));
#164080=CARTESIAN_POINT('Ctrl Pts',(-16.9013570056506,6.54762058645456,
46.5123988251726));
#164081=CARTESIAN_POINT('Ctrl Pts',(-16.1559070823762,8.04468584505497,
45.0182811781137));
#164082=CARTESIAN_POINT('Ctrl Pts',(-15.4104571591017,9.54175110365538,
43.5241635310548));
#164083=CARTESIAN_POINT('Ctrl Pts',(-14.4026149179538,10.8763499173728,
42.0300458839959));
#164084=CARTESIAN_POINT('Ctrl Pts',(-13.3947726768058,12.2109487310903,
40.5359282369373));
#164085=CARTESIAN_POINT('Ctrl Pts',(-12.1588589765331,13.3376329379985,
39.0418105898784));
#164086=CARTESIAN_POINT('Ctrl Pts',(-10.9229452762603,14.4643171449067,
37.5476929428196));
#164087=CARTESIAN_POINT('Ctrl Pts',(-9.50104767561052,15.3447188656481,
36.0535752957607));
#164088=CARTESIAN_POINT('Ctrl Pts',(-8.07915007496071,16.2251205863895,
34.5594576487018));
#164089=CARTESIAN_POINT('Ctrl Pts',(-6.51968959134574,16.8292587962898,
33.0653400016432));
#164090=CARTESIAN_POINT('Ctrl Pts',(-4.96022910773078,17.4333970061901,
31.5712223545843));
#164091=CARTESIAN_POINT('Ctrl Pts',(-3.31631129755346,17.7406985030951,
30.0771047075255));
#164092=CARTESIAN_POINT('Ctrl Pts',(-1.67239348737615,18.048,28.5829870604666));
#164093=CARTESIAN_POINT('Ctrl Pts',(-2.21024254310115E-15,18.048,27.0888694134077));
#164094=CARTESIAN_POINT('Ctrl Pts',(1.67239348737616,18.048,25.5947517663491));
#164095=CARTESIAN_POINT('Ctrl Pts',(3.31631129755346,17.7406985030951,24.1006341192902));
#164096=CARTESIAN_POINT('Ctrl Pts',(4.96022910773077,17.4333970061901,22.6065164722313));
#164097=CARTESIAN_POINT('Ctrl Pts',(6.51968959134575,16.8292587962898,21.1123988251725));
#164098=CARTESIAN_POINT('Ctrl Pts',(8.07915007496071,16.2251205863895,19.6182811781136));
#164099=CARTESIAN_POINT('Ctrl Pts',(9.50104767561053,15.3447188656481,18.1241635310549));
#164100=CARTESIAN_POINT('Ctrl Pts',(10.9229452762603,14.4643171449067,16.6300458839961));
#164101=CARTESIAN_POINT('Ctrl Pts',(12.1588589765331,13.3376329379985,15.1359282369372));
#164102=CARTESIAN_POINT('Ctrl Pts',(13.3947726768058,12.2109487310903,13.6418105898783));
#164103=CARTESIAN_POINT('Ctrl Pts',(14.4026149179538,10.8763499173728,12.1476929428195));
#164104=CARTESIAN_POINT('Ctrl Pts',(15.4104571591017,9.54175110365538,10.6535752957608));
#164105=CARTESIAN_POINT('Ctrl Pts',(16.1559070823762,8.04468584505496,9.15945764870196));
#164106=CARTESIAN_POINT('Ctrl Pts',(16.9013570056506,6.54762058645456,7.6653400016431));
#164107=CARTESIAN_POINT('Ctrl Pts',(17.3590292079831,4.93906964482096,6.17122235458423));
#164108=CARTESIAN_POINT('Ctrl Pts',(17.8167014103155,3.33051870318735,4.67710470752536));
#164109=CARTESIAN_POINT('Ctrl Pts',(17.9710104137728,1.66525935159367,3.18298706046671));
#164110=CARTESIAN_POINT('Ctrl Pts',(18.1253194172301,3.32956716117513E-15,
1.68886941340785));
#164111=CARTESIAN_POINT('Ctrl Pts',(17.9710104137728,-1.66525935159367,
0.194751766348977));
#164112=CARTESIAN_POINT('Ctrl Pts',(17.8167014103155,-3.33051870318736,
-1.29936588070989));
#164113=CARTESIAN_POINT('Ctrl Pts',(17.3590292079831,-4.93906964482095,
-2.79348352776876));
#164114=CARTESIAN_POINT('Ctrl Pts',(16.9013570056506,-6.54762058645456,
-4.2876011748274));
#164115=CARTESIAN_POINT('Ctrl Pts',(16.1559070823762,-8.04468584505497,
-5.78171882188627));
#164116=CARTESIAN_POINT('Ctrl Pts',(15.4104571591017,-9.54175110365538,
-7.27583646894514));
#164117=CARTESIAN_POINT('Ctrl Pts',(14.4026149179538,-10.8763499173728,
-8.76995411600401));
#164118=CARTESIAN_POINT('Ctrl Pts',(13.3947726768058,-12.2109487310903,
-10.2640717630629));
#164119=CARTESIAN_POINT('Ctrl Pts',(12.1588589765331,-13.3376329379985,
-11.7581894101215));
#164120=CARTESIAN_POINT('Ctrl Pts',(10.9229452762603,-14.4643171449067,
-13.2523070571804));
#164121=CARTESIAN_POINT('Ctrl Pts',(9.50104767561053,-15.3447188656481,
-14.7464247042393));
#164122=CARTESIAN_POINT('Ctrl Pts',(8.07915007496071,-16.2251205863895,
-16.2405423512981));
#164123=CARTESIAN_POINT('Ctrl Pts',(6.51968959134574,-16.8292587962898,
-17.734659998357));
#164124=CARTESIAN_POINT('Ctrl Pts',(4.96022910773078,-17.4333970061901,
-19.2287776454156));
#164125=CARTESIAN_POINT('Ctrl Pts',(3.31631129755346,-17.7406985030951,
-20.7228952924745));
#164126=CARTESIAN_POINT('Ctrl Pts',(1.67239348737615,-18.048,-22.2170129395334));
#164127=CARTESIAN_POINT('Ctrl Pts',(0.,-18.048,-23.7111305865922));
#164128=CARTESIAN_POINT('Ctrl Pts',(-1.67239348737615,-18.048,-25.2052482336511));
#164129=CARTESIAN_POINT('Ctrl Pts',(-3.31631129755346,-17.7406985030951,
-26.6993658807098));
#164130=CARTESIAN_POINT('Ctrl Pts',(-4.96022910773077,-17.4333970061901,
-28.1934835277686));
#164131=CARTESIAN_POINT('Ctrl Pts',(-6.51968959134574,-16.8292587962898,
-29.6876011748275));
#164132=CARTESIAN_POINT('Ctrl Pts',(-8.07915007496071,-16.2251205863895,
-31.1817188218864));
#164133=CARTESIAN_POINT('Ctrl Pts',(-9.50104767561052,-15.3447188656481,
-32.6758364689452));
#164134=CARTESIAN_POINT('Ctrl Pts',(-10.9229452762603,-14.4643171449067,
-34.1699541160039));
#164135=CARTESIAN_POINT('Ctrl Pts',(-12.1588589765331,-13.3376329379985,
-35.6640717630627));
#164136=CARTESIAN_POINT('Ctrl Pts',(-13.3947726768058,-12.2109487310903,
-37.1581894101216));
#164137=CARTESIAN_POINT('Ctrl Pts',(-14.4026149179538,-10.8763499173728,
-38.6523070571805));
#164138=CARTESIAN_POINT('Ctrl Pts',(-15.4104571591017,-9.54175110365538,
-40.1464247042394));
#164139=CARTESIAN_POINT('Ctrl Pts',(-16.1559070823762,-8.04468584505497,
-41.640542351298));
#164140=CARTESIAN_POINT('Ctrl Pts',(-16.9013570056506,-6.54762058645456,
-43.1346599983569));
#164141=CARTESIAN_POINT('Ctrl Pts',(-17.3590292079831,-4.93906964482095,
-44.6287776454157));
#164142=CARTESIAN_POINT('Ctrl Pts',(-17.8167014103155,-3.33051870318735,
-46.1228952924746));
#164143=CARTESIAN_POINT('Ctrl Pts',(-17.9710104137728,-1.66525935159368,
-47.6170129395335));
#164144=CARTESIAN_POINT('Ctrl Pts',(-18.1253194172301,-1.10985572039171E-15,
-49.1111305865921));
#164145=CARTESIAN_POINT('Ctrl Pts',(-17.9710104137728,1.66525935159367,
-50.605248233651));
#164146=CARTESIAN_POINT('Ctrl Pts',(-17.8167014103155,3.33051870318735,
-52.0993658807098));
#164147=CARTESIAN_POINT('Ctrl Pts',(-17.3590292079831,4.93906964482096,
-53.5934835277687));
#164148=CARTESIAN_POINT('Ctrl Pts',(-16.9013570056506,6.54762058645456,
-55.0876011748276));
#164149=CARTESIAN_POINT('Ctrl Pts',(-16.1559070823762,8.04468584505497,
-56.5817188218862));
#164150=CARTESIAN_POINT('Ctrl Pts',(-15.4104571591017,9.54175110365538,
-58.0758364689451));
#164151=CARTESIAN_POINT('Ctrl Pts',(-14.4026149179538,10.8763499173728,
-59.569954116004));
#164152=CARTESIAN_POINT('Ctrl Pts',(-13.3947726768058,12.2109487310903,
-61.0640717630628));
#164153=CARTESIAN_POINT('Ctrl Pts',(-12.1588589765331,13.3376329379985,
-62.5581894101217));
#164154=CARTESIAN_POINT('Ctrl Pts',(-10.9229452762603,14.4643171449067,
-64.0523070571803));
#164155=CARTESIAN_POINT('Ctrl Pts',(-9.50104767561052,15.3447188656481,
-65.5464247042392));
#164156=CARTESIAN_POINT('Ctrl Pts',(-8.07915007496071,16.2251205863895,
-67.0405423512981));
#164157=CARTESIAN_POINT('Ctrl Pts',(-6.51968959134574,16.8292587962898,
-68.5346599983569));
#164158=CARTESIAN_POINT('Ctrl Pts',(-4.96022910773078,17.4333970061901,
-70.0287776454158));
#164159=CARTESIAN_POINT('Ctrl Pts',(-3.31631129755346,17.7406985030951,
-71.5228952924745));
#164160=CARTESIAN_POINT('Ctrl Pts',(-1.67239348737615,18.048,-73.0170129395333));
#164161=CARTESIAN_POINT('Ctrl Pts',(-2.21024254310115E-15,18.048,-74.5111305865922));
#164162=CARTESIAN_POINT('Ctrl Pts',(1.67239348737616,18.048,-76.0052482336511));
#164163=CARTESIAN_POINT('Ctrl Pts',(3.31631129755346,17.7406985030951,-77.4993658807099));
#164164=CARTESIAN_POINT('Ctrl Pts',(4.96022910773077,17.4333970061901,-78.9934835277686));
#164165=CARTESIAN_POINT('Ctrl Pts',(6.51968959134575,16.8292587962898,-80.4876011748274));
#164166=CARTESIAN_POINT('Ctrl Pts',(8.07915007496071,16.2251205863895,-81.9817188218863));
#164167=CARTESIAN_POINT('Ctrl Pts',(9.50104767561053,15.3447188656481,-83.4758364689452));
#164168=CARTESIAN_POINT('Ctrl Pts',(10.9229452762603,14.4643171449067,-84.9699541160041));
#164169=CARTESIAN_POINT('Ctrl Pts',(12.1588589765331,13.3376329379985,-86.4640717630627));
#164170=CARTESIAN_POINT('Ctrl Pts',(13.3947726768058,12.2109487310903,-87.9581894101216));
#164171=CARTESIAN_POINT('Ctrl Pts',(14.4026149179538,10.8763499173728,-89.4523070571804));
#164172=CARTESIAN_POINT('Ctrl Pts',(15.4104571591017,9.54175110365538,-90.9464247042393));
#164173=CARTESIAN_POINT('Ctrl Pts',(16.1559070823762,8.04468584505496,-92.4405423512982));
#164174=CARTESIAN_POINT('Ctrl Pts',(16.9013570056506,6.54762058645456,-93.9346599983568));
#164175=CARTESIAN_POINT('Ctrl Pts',(17.3590292079831,4.93906964482096,-95.4287776454157));
#164176=CARTESIAN_POINT('Ctrl Pts',(17.8167014103155,3.33051870318735,-96.9228952924745));
#164177=CARTESIAN_POINT('Ctrl Pts',(17.9710104137728,1.66525935159367,-98.4170129395334));
#164178=CARTESIAN_POINT('Ctrl Pts',(18.1253194172301,3.32956716117513E-15,
-99.9111305865923));
#164179=CARTESIAN_POINT('Ctrl Pts',(17.9710104137728,-1.66525935159367,
-101.405248233651));
#164180=CARTESIAN_POINT('Ctrl Pts',(17.8167014103155,-3.33051870318736,
-102.89936588071));
#164181=CARTESIAN_POINT('Ctrl Pts',(17.3590292079831,-4.93906964482095,
-104.393483527769));
#164182=CARTESIAN_POINT('Ctrl Pts',(16.9013570056506,-6.54762058645456,
-105.887601174828));
#164183=CARTESIAN_POINT('Ctrl Pts',(16.1559070823762,-8.04468584505497,
-107.381718821886));
#164184=CARTESIAN_POINT('Ctrl Pts',(15.4104571591017,-9.54175110365538,
-108.875836468945));
#164185=CARTESIAN_POINT('Ctrl Pts',(14.4026149179538,-10.8763499173728,
-110.369954116004));
#164186=CARTESIAN_POINT('Ctrl Pts',(13.3947726768058,-12.2109487310903,
-111.864071763063));
#164187=CARTESIAN_POINT('Ctrl Pts',(12.1588589765331,-13.3376329379985,
-113.358189410122));
#164188=CARTESIAN_POINT('Ctrl Pts',(10.9229452762603,-14.4643171449067,
-114.852307057181));
#164189=CARTESIAN_POINT('Ctrl Pts',(9.50104767561053,-15.3447188656481,
-116.346424704239));
#164190=CARTESIAN_POINT('Ctrl Pts',(8.07915007496071,-16.2251205863895,
-117.840542351298));
#164191=CARTESIAN_POINT('Ctrl Pts',(6.51968959134574,-16.8292587962898,
-119.334659998357));
#164192=CARTESIAN_POINT('Ctrl Pts',(4.96022910773078,-17.4333970061901,
-120.828777645416));
#164193=CARTESIAN_POINT('Ctrl Pts',(3.31631129755346,-17.7406985030951,
-122.322895292475));
#164194=CARTESIAN_POINT('Ctrl Pts',(1.67239348737615,-18.048,-123.817012939533));
#164195=CARTESIAN_POINT('Ctrl Pts',(0.,-18.048,-125.311130586592));
#164196=CARTESIAN_POINT('Ctrl Pts',(-1.67239348737615,-18.048,-126.805248233651));
#164197=CARTESIAN_POINT('Ctrl Pts',(-3.31631129755346,-17.7406985030951,
-128.29936588071));
#164198=CARTESIAN_POINT('Ctrl Pts',(-4.96022910773077,-17.4333970061901,
-129.793483527769));
#164199=CARTESIAN_POINT('Ctrl Pts',(-6.51968959134574,-16.8292587962898,
-131.287601174827));
#164200=CARTESIAN_POINT('Ctrl Pts',(-8.07915007496071,-16.2251205863895,
-132.781718821886));
#164201=CARTESIAN_POINT('Ctrl Pts',(-9.50104767561052,-15.3447188656481,
-134.275836468945));
#164202=CARTESIAN_POINT('Ctrl Pts',(-10.9229452762603,-14.4643171449067,
-135.769954116004));
#164203=CARTESIAN_POINT('Ctrl Pts',(-12.1588589765331,-13.3376329379985,
-137.264071763063));
#164204=CARTESIAN_POINT('Ctrl Pts',(-13.3947726768058,-12.2109487310903,
-138.758189410122));
#164205=CARTESIAN_POINT('Ctrl Pts',(-14.4026149179538,-10.8763499173728,
-140.25230705718));
#164206=CARTESIAN_POINT('Ctrl Pts',(-15.4104571591017,-9.54175110365538,
-141.746424704239));
#164207=CARTESIAN_POINT('Ctrl Pts',(-16.1559070823762,-8.04468584505497,
-143.240542351298));
#164208=CARTESIAN_POINT('Ctrl Pts',(-16.9013570056506,-6.54762058645456,
-144.734659998357));
#164209=CARTESIAN_POINT('Ctrl Pts',(-17.3590292079831,-4.93906964482095,
-146.228777645416));
#164210=CARTESIAN_POINT('Ctrl Pts',(-17.8167014103155,-3.33051870318735,
-147.722895292475));
#164211=CARTESIAN_POINT('Ctrl Pts',(-17.9710104137728,-1.66525935159368,
-149.217012939533));
#164212=CARTESIAN_POINT('Ctrl Pts',(-18.1253194172301,-1.10985572039171E-15,
-150.711130586592));
#164213=CARTESIAN_POINT('Ctrl Pts',(-17.9710104137728,1.66525935159367,
-152.205248233651));
#164214=CARTESIAN_POINT('Ctrl Pts',(-17.8167014103155,3.33051870318735,
-153.69936588071));
#164215=CARTESIAN_POINT('Ctrl Pts',(-17.3590292079831,4.93906964482096,
-155.193483527769));
#164216=CARTESIAN_POINT('Ctrl Pts',(-16.9013570056506,6.54762058645456,
-156.687601174828));
#164217=CARTESIAN_POINT('Ctrl Pts',(-16.1559070823762,8.04468584505497,
-158.181718821886));
#164218=CARTESIAN_POINT('Ctrl Pts',(-15.4104571591017,9.54175110365538,
-159.675836468945));
#164219=CARTESIAN_POINT('Ctrl Pts',(-14.4026149179538,10.8763499173728,
-161.169954116004));
#164220=CARTESIAN_POINT('Ctrl Pts',(-13.3947726768058,12.2109487310903,
-162.664071763063));
#164221=CARTESIAN_POINT('Ctrl Pts',(-12.1588589765331,13.3376329379985,
-164.158189410122));
#164222=CARTESIAN_POINT('Ctrl Pts',(-10.9229452762603,14.4643171449067,
-165.65230705718));
#164223=CARTESIAN_POINT('Ctrl Pts',(-9.50104767561052,15.3447188656481,
-167.146424704239));
#164224=CARTESIAN_POINT('Ctrl Pts',(-8.07915007496071,16.2251205863895,
-168.640542351298));
#164225=CARTESIAN_POINT('Ctrl Pts',(-6.51968959134574,16.8292587962898,
-170.134659998357));
#164226=CARTESIAN_POINT('Ctrl Pts',(-4.96022910773078,17.4333970061901,
-171.628777645416));
#164227=CARTESIAN_POINT('Ctrl Pts',(-3.31631129755346,17.7406985030951,
-173.122895292475));
#164228=CARTESIAN_POINT('Ctrl Pts',(-1.67239348737615,18.048,-174.617012939534));
#164229=CARTESIAN_POINT('Ctrl Pts',(-2.21024254310115E-15,18.048,-176.111130586592));
#164230=CARTESIAN_POINT('Ctrl Pts',(1.67239348737616,18.048,-177.605248233651));
#164231=CARTESIAN_POINT('Ctrl Pts',(3.31631129755346,17.7406985030951,-179.09936588071));
#164232=CARTESIAN_POINT('Ctrl Pts',(4.96022910773077,17.4333970061901,-180.593483527769));
#164233=CARTESIAN_POINT('Ctrl Pts',(6.51968959134575,16.8292587962898,-182.087601174828));
#164234=CARTESIAN_POINT('Ctrl Pts',(8.07915007496071,16.2251205863895,-183.581718821886));
#164235=CARTESIAN_POINT('Ctrl Pts',(9.50104767561053,15.3447188656481,-185.075836468945));
#164236=CARTESIAN_POINT('Ctrl Pts',(10.9229452762603,14.4643171449067,-186.569954116004));
#164237=CARTESIAN_POINT('Ctrl Pts',(12.1588589765331,13.3376329379985,-188.064071763063));
#164238=CARTESIAN_POINT('Ctrl Pts',(13.3947726768058,12.2109487310903,-189.558189410122));
#164239=CARTESIAN_POINT('Ctrl Pts',(14.4026149179538,10.8763499173728,-191.05230705718));
#164240=CARTESIAN_POINT('Ctrl Pts',(15.4104571591017,9.54175110365538,-192.546424704239));
#164241=CARTESIAN_POINT('Ctrl Pts',(16.1559070823762,8.04468584505496,-194.040542351298));
#164242=CARTESIAN_POINT('Ctrl Pts',(16.9013570056506,6.54762058645456,-195.534659998357));
#164243=CARTESIAN_POINT('Ctrl Pts',(17.3590292079831,4.93906964482096,-197.028777645416));
#164244=CARTESIAN_POINT('Ctrl Pts',(17.8167014103155,3.33051870318735,-198.522895292475));
#164245=CARTESIAN_POINT('Ctrl Pts',(17.9710104137728,1.66525935159367,-200.017012939533));
#164246=CARTESIAN_POINT('Ctrl Pts',(18.1253194172301,3.32956716117513E-15,
-201.511130586592));
#164247=CARTESIAN_POINT('Ctrl Pts',(17.9710104137728,-1.66525935159367,
-203.005248233651));
#164248=CARTESIAN_POINT('Ctrl Pts',(17.8167014103155,-3.33051870318736,
-204.49936588071));
#164249=CARTESIAN_POINT('Ctrl Pts',(17.3590292079831,-4.93906964482095,
-205.993483527769));
#164250=CARTESIAN_POINT('Ctrl Pts',(16.9013570056506,-6.54762058645456,
-207.487601174827));
#164251=CARTESIAN_POINT('Ctrl Pts',(16.1559070823762,-8.04468584505497,
-208.981718821886));
#164252=CARTESIAN_POINT('Ctrl Pts',(15.4104571591017,-9.54175110365538,
-210.475836468945));
#164253=CARTESIAN_POINT('Ctrl Pts',(14.4026149179538,-10.8763499173728,
-211.969954116004));
#164254=CARTESIAN_POINT('Ctrl Pts',(13.3947726768058,-12.2109487310903,
-213.464071763063));
#164255=CARTESIAN_POINT('Ctrl Pts',(12.1588589765331,-13.3376329379985,
-214.958189410122));
#164256=CARTESIAN_POINT('Ctrl Pts',(10.9229452762603,-14.4643171449067,
-216.45230705718));
#164257=CARTESIAN_POINT('Ctrl Pts',(9.50104767561053,-15.3447188656481,
-217.946424704239));
#164258=CARTESIAN_POINT('Ctrl Pts',(8.07915007496071,-16.2251205863895,
-219.440542351298));
#164259=CARTESIAN_POINT('Ctrl Pts',(6.51968959134574,-16.8292587962898,
-220.934659998357));
#164260=CARTESIAN_POINT('Ctrl Pts',(4.96022910773078,-17.4333970061901,
-222.428777645416));
#164261=CARTESIAN_POINT('Ctrl Pts',(3.31631129755346,-17.7406985030951,
-223.922895292475));
#164262=CARTESIAN_POINT('Ctrl Pts',(1.67239348737615,-18.048,-225.417012939533));
#164263=CARTESIAN_POINT('Ctrl Pts',(0.,-18.048,-226.911130586592));
#164264=CARTESIAN_POINT('Ctrl Pts',(-1.67239348737615,-18.048,-228.405248233651));
#164265=CARTESIAN_POINT('Ctrl Pts',(-3.31631129755346,-17.7406985030951,
-229.89936588071));
#164266=CARTESIAN_POINT('Ctrl Pts',(-4.96022910773077,-17.4333970061901,
-231.393483527769));
#164267=CARTESIAN_POINT('Ctrl Pts',(-6.51968959134574,-16.8292587962898,
-232.887601174828));
#164268=CARTESIAN_POINT('Ctrl Pts',(-8.07915007496071,-16.2251205863895,
-234.381718821886));
#164269=CARTESIAN_POINT('Ctrl Pts',(-9.50104767561052,-15.3447188656481,
-235.875836468945));
#164270=CARTESIAN_POINT('Ctrl Pts',(-10.9229452762603,-14.4643171449067,
-237.369954116004));
#164271=CARTESIAN_POINT('Ctrl Pts',(-12.1588589765331,-13.3376329379985,
-238.864071763063));
#164272=CARTESIAN_POINT('Ctrl Pts',(-13.3947726768058,-12.2109487310903,
-240.358189410122));
#164273=CARTESIAN_POINT('Ctrl Pts',(-14.4026149179538,-10.8763499173728,
-241.852307057181));
#164274=CARTESIAN_POINT('Ctrl Pts',(-15.4104571591017,-9.54175110365538,
-243.346424704239));
#164275=CARTESIAN_POINT('Ctrl Pts',(-16.1559070823762,-8.04468584505497,
-244.840542351298));
#164276=CARTESIAN_POINT('Ctrl Pts',(-16.9013570056506,-6.54762058645456,
-246.334659998357));
#164277=CARTESIAN_POINT('Ctrl Pts',(-17.3590292079831,-4.93906964482095,
-247.828777645416));
#164278=CARTESIAN_POINT('Ctrl Pts',(-17.8167014103155,-3.33051870318735,
-249.322895292475));
#164279=CARTESIAN_POINT('Ctrl Pts',(-17.9710104137728,-1.66525935159368,
-250.817012939533));
#164280=CARTESIAN_POINT('Ctrl Pts',(-18.1253194172301,-1.10985572039171E-15,
-252.311130586592));
#164281=CARTESIAN_POINT('Ctrl Pts',(-17.9710104137728,1.66525935159367,
-253.805248233651));
#164282=CARTESIAN_POINT('Ctrl Pts',(-17.8167014103155,3.33051870318735,
-255.29936588071));
#164283=CARTESIAN_POINT('Ctrl Pts',(-17.3590292079831,4.93906964482096,
-256.793483527769));
#164284=CARTESIAN_POINT('Ctrl Pts',(-16.9013570056506,6.54762058645456,
-258.287601174827));
#164285=CARTESIAN_POINT('Ctrl Pts',(-16.1559070823762,8.04468584505497,
-259.781718821886));
#164286=CARTESIAN_POINT('Ctrl Pts',(-15.4104571591017,9.54175110365538,
-261.275836468945));
#164287=CARTESIAN_POINT('Ctrl Pts',(-14.4026149179538,10.8763499173728,
-262.769954116004));
#164288=CARTESIAN_POINT('Ctrl Pts',(-13.3947726768058,12.2109487310903,
-264.264071763063));
#164289=CARTESIAN_POINT('Ctrl Pts',(-12.1588589765331,13.3376329379985,
-265.758189410122));
#164290=CARTESIAN_POINT('Ctrl Pts',(-10.9229452762603,14.4643171449067,
-267.25230705718));
#164291=CARTESIAN_POINT('Ctrl Pts',(-9.50104767561052,15.3447188656481,
-268.746424704239));
#164292=CARTESIAN_POINT('Ctrl Pts',(-8.07915007496071,16.2251205863895,
-270.240542351298));
#164293=CARTESIAN_POINT('Ctrl Pts',(-6.51968959134574,16.8292587962898,
-271.734659998357));
#164294=CARTESIAN_POINT('Ctrl Pts',(-4.96022910773078,17.4333970061901,
-273.228777645416));
#164295=CARTESIAN_POINT('Ctrl Pts',(-3.31631129755346,17.7406985030951,
-274.722895292475));
#164296=CARTESIAN_POINT('Ctrl Pts',(-1.67239348737615,18.048,-276.217012939533));
#164297=CARTESIAN_POINT('Ctrl Pts',(-2.21024254310115E-15,18.048,-277.711130586592));
#164298=CARTESIAN_POINT('Ctrl Pts',(1.67239348737616,18.048,-279.205248233651));
#164299=CARTESIAN_POINT('Ctrl Pts',(3.31631129755346,17.7406985030951,-280.69936588071));
#164300=CARTESIAN_POINT('Ctrl Pts',(4.96022910773077,17.4333970061901,-282.193483527769));
#164301=CARTESIAN_POINT('Ctrl Pts',(6.51968959134575,16.8292587962898,-283.687601174827));
#164302=CARTESIAN_POINT('Ctrl Pts',(8.07915007496071,16.2251205863895,-285.181718821886));
#164303=CARTESIAN_POINT('Ctrl Pts',(9.50104767561053,15.3447188656481,-286.675836468945));
#164304=CARTESIAN_POINT('Ctrl Pts',(10.9229452762603,14.4643171449067,-288.169954116004));
#164305=CARTESIAN_POINT('Ctrl Pts',(12.1588589765331,13.3376329379985,-289.664071763063));
#164306=CARTESIAN_POINT('Ctrl Pts',(13.3947726768058,12.2109487310903,-291.158189410122));
#164307=CARTESIAN_POINT('Ctrl Pts',(14.4026149179538,10.8763499173728,-292.652307057181));
#164308=CARTESIAN_POINT('Ctrl Pts',(15.4104571591017,9.54175110365538,-294.146424704239));
#164309=CARTESIAN_POINT('Ctrl Pts',(16.1559070823762,8.04468584505496,-295.640542351298));
#164310=CARTESIAN_POINT('Ctrl Pts',(16.9013570056506,6.54762058645456,-297.134659998357));
#164311=CARTESIAN_POINT('Ctrl Pts',(17.3590292079831,4.93906964482096,-298.628777645416));
#164312=CARTESIAN_POINT('Ctrl Pts',(17.8167014103155,3.33051870318735,-300.122895292475));
#164313=CARTESIAN_POINT('Ctrl Pts',(17.9710104137728,1.66525935159367,-301.617012939533));
#164314=CARTESIAN_POINT('Ctrl Pts',(18.1253194172301,3.32956716117513E-15,
-303.111130586592));
#164315=CARTESIAN_POINT('Ctrl Pts',(17.9710104137728,-1.66525935159367,
-304.605248233651));
#164316=CARTESIAN_POINT('Ctrl Pts',(17.8167014103155,-3.33051870318736,
-306.09936588071));
#164317=CARTESIAN_POINT('Ctrl Pts',(17.3590292079831,-4.93906964482095,
-307.593483527769));
#164318=CARTESIAN_POINT('Ctrl Pts',(16.9013570056506,-6.54762058645456,
-309.087601174828));
#164319=CARTESIAN_POINT('Ctrl Pts',(16.1559070823762,-8.04468584505497,
-310.581718821886));
#164320=CARTESIAN_POINT('Ctrl Pts',(15.4104571591017,-9.54175110365538,
-312.075836468945));
#164321=CARTESIAN_POINT('Ctrl Pts',(14.4026149179538,-10.8763499173728,
-313.569954116004));
#164322=CARTESIAN_POINT('Ctrl Pts',(13.3947726768058,-12.2109487310903,
-315.064071763063));
#164323=CARTESIAN_POINT('Ctrl Pts',(12.1588589765331,-13.3376329379985,
-316.558189410122));
#164324=CARTESIAN_POINT('Ctrl Pts',(10.9229452762603,-14.4643171449067,
-318.05230705718));
#164325=CARTESIAN_POINT('Ctrl Pts',(9.50104767561053,-15.3447188656481,
-319.546424704239));
#164326=CARTESIAN_POINT('Ctrl Pts',(8.07915007496071,-16.2251205863895,
-321.040542351298));
#164327=CARTESIAN_POINT('Ctrl Pts',(6.51968959134574,-16.8292587962898,
-322.534659998357));
#164328=CARTESIAN_POINT('Ctrl Pts',(4.96022910773078,-17.4333970061901,
-324.028777645416));
#164329=CARTESIAN_POINT('Ctrl Pts',(3.31631129755346,-17.7406985030951,
-325.522895292474));
#164330=CARTESIAN_POINT('Ctrl Pts',(1.67239348737615,-18.048,-327.017012939533));
#164331=CARTESIAN_POINT('Ctrl Pts',(0.,-18.048,-328.511130586592));
#164332=CARTESIAN_POINT('Ctrl Pts',(-1.67239348737615,-18.048,-330.005248233651));
#164333=CARTESIAN_POINT('Ctrl Pts',(-3.31631129755346,-17.7406985030951,
-331.49936588071));
#164334=CARTESIAN_POINT('Ctrl Pts',(-4.96022910773077,-17.4333970061901,
-332.993483527769));
#164335=CARTESIAN_POINT('Ctrl Pts',(-6.51968959134574,-16.8292587962898,
-334.487601174827));
#164336=CARTESIAN_POINT('Ctrl Pts',(-8.07915007496071,-16.2251205863895,
-335.981718821886));
#164337=CARTESIAN_POINT('Ctrl Pts',(-9.50104767561052,-15.3447188656481,
-337.475836468945));
#164338=CARTESIAN_POINT('Ctrl Pts',(-10.9229452762603,-14.4643171449067,
-338.969954116004));
#164339=CARTESIAN_POINT('Ctrl Pts',(-12.1588589765331,-13.3376329379985,
-340.464071763063));
#164340=CARTESIAN_POINT('Ctrl Pts',(-13.3947726768058,-12.2109487310903,
-341.958189410122));
#164341=CARTESIAN_POINT('Ctrl Pts',(-14.4026149179538,-10.8763499173728,
-343.45230705718));
#164342=CARTESIAN_POINT('Ctrl Pts',(-15.4104571591017,-9.54175110365538,
-344.946424704239));
#164343=CARTESIAN_POINT('Ctrl Pts',(-16.1559070823762,-8.04468584505497,
-346.440542351298));
#164344=CARTESIAN_POINT('Ctrl Pts',(-16.9013570056506,-6.54762058645456,
-347.934659998357));
#164345=CARTESIAN_POINT('Ctrl Pts',(-17.3590292079831,-4.93906964482095,
-349.428777645416));
#164346=CARTESIAN_POINT('Ctrl Pts',(-17.8167014103155,-3.33051870318735,
-350.922895292475));
#164347=CARTESIAN_POINT('Ctrl Pts',(-17.9710104137728,-1.66525935159368,
-352.417012939533));
#164348=CARTESIAN_POINT('Ctrl Pts',(-18.1253194172301,-1.10985572039171E-15,
-353.911130586592));
#164349=CARTESIAN_POINT('Ctrl Pts',(-17.9710104137728,1.66525935159367,
-355.405248233651));
#164350=CARTESIAN_POINT('Ctrl Pts',(-17.8167014103155,3.33051870318735,
-356.89936588071));
#164351=CARTESIAN_POINT('Ctrl Pts',(-17.3590292079831,4.93906964482096,
-358.393483527769));
#164352=CARTESIAN_POINT('Ctrl Pts',(-16.9013570056506,6.54762058645456,
-359.887601174828));
#164353=CARTESIAN_POINT('Ctrl Pts',(-16.1559070823762,8.04468584505497,
-361.381718821886));
#164354=CARTESIAN_POINT('Ctrl Pts',(-15.4104571591017,9.54175110365538,
-362.875836468945));
#164355=CARTESIAN_POINT('Ctrl Pts',(-14.4026149179538,10.8763499173728,
-364.369954116004));
#164356=CARTESIAN_POINT('Ctrl Pts',(-13.3947726768058,12.2109487310903,
-365.864071763063));
#164357=CARTESIAN_POINT('Ctrl Pts',(-12.1588589765331,13.3376329379985,
-367.358189410122));
#164358=CARTESIAN_POINT('Ctrl Pts',(-10.9229452762603,14.4643171449067,
-368.85230705718));
#164359=CARTESIAN_POINT('Ctrl Pts',(-9.50104767561052,15.3447188656481,
-370.346424704239));
#164360=CARTESIAN_POINT('Ctrl Pts',(-8.07915007496071,16.2251205863895,
-371.840542351298));
#164361=CARTESIAN_POINT('Ctrl Pts',(-6.51968959134574,16.8292587962898,
-373.334659998357));
#164362=CARTESIAN_POINT('Ctrl Pts',(-4.96022910773078,17.4333970061901,
-374.828777645416));
#164363=CARTESIAN_POINT('Ctrl Pts',(-3.31631129755346,17.7406985030951,
-376.322895292475));
#164364=CARTESIAN_POINT('Ctrl Pts',(-1.67239348737615,18.048,-377.817012939533));
#164365=CARTESIAN_POINT('Ctrl Pts',(-2.21024254310115E-15,18.048,-379.311130586592));
#164366=CARTESIAN_POINT('Ctrl Pts',(1.67239348737616,18.048,-380.805248233651));
#164367=CARTESIAN_POINT('Ctrl Pts',(3.31631129755346,17.7406985030951,-382.29936588071));
#164368=CARTESIAN_POINT('Ctrl Pts',(4.96022910773077,17.4333970061901,-383.793483527769));
#164369=CARTESIAN_POINT('Ctrl Pts',(6.51968959134575,16.8292587962898,-385.287601174827));
#164370=CARTESIAN_POINT('Ctrl Pts',(8.07915007496071,16.2251205863895,-386.781718821886));
#164371=CARTESIAN_POINT('Ctrl Pts',(9.50104767561053,15.3447188656481,-388.275836468945));
#164372=CARTESIAN_POINT('Ctrl Pts',(10.9229452762603,14.4643171449067,-389.769954116004));
#164373=CARTESIAN_POINT('Ctrl Pts',(12.1588589765331,13.3376329379985,-391.264071763063));
#164374=CARTESIAN_POINT('Ctrl Pts',(13.3947726768058,12.2109487310903,-392.758189410122));
#164375=CARTESIAN_POINT('Ctrl Pts',(14.4026149179538,10.8763499173728,-394.25230705718));
#164376=CARTESIAN_POINT('Ctrl Pts',(15.4104571591017,9.54175110365538,-395.746424704239));
#164377=CARTESIAN_POINT('Ctrl Pts',(16.1559070823762,8.04468584505496,-397.240542351298));
#164378=CARTESIAN_POINT('Ctrl Pts',(16.9013570056506,6.54762058645456,-398.734659998357));
#164379=CARTESIAN_POINT('Ctrl Pts',(17.3590292079831,4.93906964482096,-400.228777645416));
#164380=CARTESIAN_POINT('Ctrl Pts',(17.8167014103155,3.33051870318735,-401.722895292475));
#164381=CARTESIAN_POINT('Ctrl Pts',(17.9710104137728,1.66525935159367,-403.217012939533));
#164382=CARTESIAN_POINT('Ctrl Pts',(18.1253194172301,3.32956716117513E-15,
-404.711130586592));
#164383=CARTESIAN_POINT('Ctrl Pts',(17.9710104137728,-1.66525935159367,
-406.205248233651));
#164384=CARTESIAN_POINT('Ctrl Pts',(17.8167014103155,-3.33051870318736,
-407.69936588071));
#164385=CARTESIAN_POINT('Ctrl Pts',(17.3590292079831,-4.93906964482095,
-409.193483527769));
#164386=CARTESIAN_POINT('Ctrl Pts',(16.9013570056506,-6.54762058645456,
-410.687601174828));
#164387=CARTESIAN_POINT('Ctrl Pts',(16.1559070823762,-8.04468584505497,
-412.181718821886));
#164388=CARTESIAN_POINT('Ctrl Pts',(15.4104571591017,-9.54175110365538,
-413.675836468945));
#164389=CARTESIAN_POINT('Ctrl Pts',(14.4026149179538,-10.8763499173728,
-415.169954116004));
#164390=CARTESIAN_POINT('Ctrl Pts',(13.3947726768058,-12.2109487310903,
-416.664071763063));
#164391=CARTESIAN_POINT('Ctrl Pts',(12.1588589765331,-13.3376329379985,
-418.158189410122));
#164392=CARTESIAN_POINT('Ctrl Pts',(10.9229452762603,-14.4643171449067,
-419.652307057181));
#164393=CARTESIAN_POINT('Ctrl Pts',(9.50104767561053,-15.3447188656481,
-421.146424704239));
#164394=CARTESIAN_POINT('Ctrl Pts',(8.07915007496071,-16.2251205863895,
-422.640542351298));
#164395=CARTESIAN_POINT('Ctrl Pts',(6.51968959134574,-16.8292587962898,
-424.134659998357));
#164396=CARTESIAN_POINT('Ctrl Pts',(4.96022910773078,-17.4333970061901,
-425.628777645416));
#164397=CARTESIAN_POINT('Ctrl Pts',(3.31631129755346,-17.7406985030951,
-427.122895292475));
#164398=CARTESIAN_POINT('Ctrl Pts',(1.67239348737615,-18.048,-428.617012939534));
#164399=CARTESIAN_POINT('Ctrl Pts',(0.,-18.048,-430.111130586592));
#164400=CARTESIAN_POINT('Ctrl Pts',(-1.67239348737615,-18.048,-431.605248233651));
#164401=CARTESIAN_POINT('Ctrl Pts',(-3.31631129755346,-17.7406985030951,
-433.09936588071));
#164402=CARTESIAN_POINT('Ctrl Pts',(-4.96022910773077,-17.4333970061901,
-434.593483527769));
#164403=CARTESIAN_POINT('Ctrl Pts',(-6.51968959134574,-16.8292587962898,
-436.087601174828));
#164404=CARTESIAN_POINT('Ctrl Pts',(-8.07915007496071,-16.2251205863895,
-437.581718821886));
#164405=CARTESIAN_POINT('Ctrl Pts',(-9.50104767561052,-15.3447188656481,
-439.075836468945));
#164406=CARTESIAN_POINT('Ctrl Pts',(-10.9229452762603,-14.4643171449067,
-440.569954116004));
#164407=CARTESIAN_POINT('Ctrl Pts',(-12.1588589765331,-13.3376329379985,
-442.064071763063));
#164408=CARTESIAN_POINT('Ctrl Pts',(-13.3947726768058,-12.2109487310903,
-443.558189410122));
#164409=CARTESIAN_POINT('Ctrl Pts',(-14.4026149179538,-10.8763499173728,
-445.05230705718));
#164410=CARTESIAN_POINT('Ctrl Pts',(-15.4104571591017,-9.54175110365538,
-446.546424704239));
#164411=CARTESIAN_POINT('Ctrl Pts',(-16.1559070823762,-8.04468584505497,
-448.040542351298));
#164412=CARTESIAN_POINT('Ctrl Pts',(-16.9013570056506,-6.54762058645456,
-449.534659998357));
#164413=CARTESIAN_POINT('Ctrl Pts',(-17.3590292079831,-4.93906964482095,
-451.028777645416));
#164414=CARTESIAN_POINT('Ctrl Pts',(-17.8167014103155,-3.33051870318735,
-452.522895292475));
#164415=CARTESIAN_POINT('Ctrl Pts',(-17.9710104137728,-1.66525935159368,
-454.017012939533));
#164416=CARTESIAN_POINT('Ctrl Pts',(-18.1253194172301,-1.10985572039171E-15,
-455.511130586592));
#164417=CARTESIAN_POINT('Ctrl Pts',(-17.9710104137728,1.66525935159367,
-457.005248233651));
#164418=CARTESIAN_POINT('Ctrl Pts',(-17.8167014103155,3.33051870318735,
-458.49936588071));
#164419=CARTESIAN_POINT('Ctrl Pts',(-17.3590292079831,4.93906964482096,
-459.993483527769));
#164420=CARTESIAN_POINT('Ctrl Pts',(-16.9013570056506,6.54762058645456,
-461.487601174828));
#164421=CARTESIAN_POINT('Ctrl Pts',(-16.1559070823762,8.04468584505497,
-462.981718821886));
#164422=CARTESIAN_POINT('Ctrl Pts',(-15.4104571591017,9.54175110365538,
-464.475836468945));
#164423=CARTESIAN_POINT('Ctrl Pts',(-14.4026149179538,10.8763499173728,
-465.969954116004));
#164424=CARTESIAN_POINT('Ctrl Pts',(-13.3947726768058,12.2109487310903,
-467.464071763063));
#164425=CARTESIAN_POINT('Ctrl Pts',(-12.1588589765331,13.3376329379985,
-468.958189410122));
#164426=CARTESIAN_POINT('Ctrl Pts',(-10.9229452762603,14.4643171449067,
-470.45230705718));
#164427=CARTESIAN_POINT('Ctrl Pts',(-9.50104767561052,15.3447188656481,
-471.946424704239));
#164428=CARTESIAN_POINT('Ctrl Pts',(-8.07915007496071,16.2251205863895,
-473.440542351298));
#164429=CARTESIAN_POINT('Ctrl Pts',(-6.51968959134574,16.8292587962898,
-474.934659998357));
#164430=CARTESIAN_POINT('Ctrl Pts',(-4.96022910773078,17.4333970061901,
-476.428777645416));
#164431=CARTESIAN_POINT('Ctrl Pts',(-3.31631129755346,17.7406985030951,
-477.922895292475));
#164432=CARTESIAN_POINT('Ctrl Pts',(-1.67239348737615,18.048,-479.417012939533));
#164433=CARTESIAN_POINT('Ctrl Pts',(-2.21024254310115E-15,18.048,-480.911130586592));
#164434=CARTESIAN_POINT('Ctrl Pts',(1.67239348737616,18.048,-482.405248233651));
#164435=CARTESIAN_POINT('Ctrl Pts',(3.31631129755346,17.7406985030951,-483.89936588071));
#164436=CARTESIAN_POINT('Ctrl Pts',(4.96022910773077,17.4333970061901,-485.393483527769));
#164437=CARTESIAN_POINT('Ctrl Pts',(6.51968959134575,16.8292587962898,-486.887601174828));
#164438=CARTESIAN_POINT('Ctrl Pts',(8.07915007496071,16.2251205863895,-488.381718821887));
#164439=CARTESIAN_POINT('Ctrl Pts',(9.50104767561053,15.3447188656481,-489.875836468945));
#164440=CARTESIAN_POINT('Ctrl Pts',(10.9229452762603,14.4643171449067,-491.369954116004));
#164441=CARTESIAN_POINT('Ctrl Pts',(12.1588589765331,13.3376329379985,-492.864071763063));
#164442=CARTESIAN_POINT('Ctrl Pts',(13.3947726768058,12.2109487310903,-494.358189410122));
#164443=CARTESIAN_POINT('Ctrl Pts',(14.4026149179538,10.8763499173728,-495.852307057181));
#164444=CARTESIAN_POINT('Ctrl Pts',(15.4104571591017,9.54175110365538,-497.346424704239));
#164445=CARTESIAN_POINT('Ctrl Pts',(16.1559070823762,8.04468584505496,-498.840542351298));
#164446=CARTESIAN_POINT('Ctrl Pts',(16.9013570056506,6.54762058645456,-500.334659998357));
#164447=CARTESIAN_POINT('Ctrl Pts',(17.3590292079831,4.93906964482096,-501.828777645416));
#164448=CARTESIAN_POINT('Ctrl Pts',(17.8167014103155,3.33051870318735,-503.322895292475));
#164449=CARTESIAN_POINT('Ctrl Pts',(17.9710104137728,1.66525935159367,-504.817012939534));
#164450=CARTESIAN_POINT('Ctrl Pts',(18.1253194172301,3.32956716117513E-15,
-506.311130586592));
#164451=CARTESIAN_POINT('Ctrl Pts',(17.9710104137728,-1.66525935159367,
-507.805248233651));
#164452=CARTESIAN_POINT('Ctrl Pts',(17.8167014103155,-3.33051870318736,
-509.29936588071));
#164453=CARTESIAN_POINT('Ctrl Pts',(17.3590292079831,-4.93906964482095,
-510.793483527769));
#164454=CARTESIAN_POINT('Ctrl Pts',(16.9013570056506,-6.54762058645456,
-512.287601174828));
#164455=CARTESIAN_POINT('Ctrl Pts',(16.1559070823762,-8.04468584505497,
-513.781718821886));
#164456=CARTESIAN_POINT('Ctrl Pts',(15.4104571591017,-9.54175110365538,
-515.275836468945));
#164457=CARTESIAN_POINT('Ctrl Pts',(14.4026149179538,-10.8763499173728,
-516.769954116004));
#164458=CARTESIAN_POINT('Ctrl Pts',(13.3947726768058,-12.2109487310903,
-518.264071763063));
#164459=CARTESIAN_POINT('Ctrl Pts',(12.1588589765331,-13.3376329379985,
-519.758189410122));
#164460=CARTESIAN_POINT('Ctrl Pts',(10.9229452762603,-14.4643171449067,
-521.252307057181));
#164461=CARTESIAN_POINT('Ctrl Pts',(9.50104767561053,-15.3447188656481,
-522.746424704239));
#164462=CARTESIAN_POINT('Ctrl Pts',(8.07915007496071,-16.2251205863895,
-524.240542351298));
#164463=CARTESIAN_POINT('Ctrl Pts',(6.51968959134574,-16.8292587962898,
-525.734659998357));
#164464=CARTESIAN_POINT('Ctrl Pts',(4.96022910773078,-17.4333970061901,
-527.228777645416));
#164465=CARTESIAN_POINT('Ctrl Pts',(3.31631129755346,-17.7406985030951,
-528.722895292475));
#164466=CARTESIAN_POINT('Ctrl Pts',(1.67239348737615,-18.048,-530.217012939533));
#164467=CARTESIAN_POINT('Ctrl Pts',(0.,-18.048,-531.711130586592));
#164468=CARTESIAN_POINT('Ctrl Pts',(-1.67239348737615,-18.048,-533.205248233651));
#164469=CARTESIAN_POINT('Ctrl Pts',(-3.31631129755346,-17.7406985030951,
-534.69936588071));
#164470=CARTESIAN_POINT('Ctrl Pts',(-4.96022910773077,-17.4333970061901,
-536.193483527769));
#164471=CARTESIAN_POINT('Ctrl Pts',(-6.51968959134574,-16.8292587962898,
-537.687601174827));
#164472=CARTESIAN_POINT('Ctrl Pts',(-8.07915007496071,-16.2251205863895,
-539.181718821886));
#164473=CARTESIAN_POINT('Ctrl Pts',(-9.50104767561052,-15.3447188656481,
-540.675836468945));
#164474=CARTESIAN_POINT('Ctrl Pts',(-10.9229452762603,-14.4643171449067,
-542.169954116004));
#164475=CARTESIAN_POINT('Ctrl Pts',(-12.1588589765331,-13.3376329379985,
-543.664071763063));
#164476=CARTESIAN_POINT('Ctrl Pts',(-13.3947726768058,-12.2109487310903,
-545.158189410122));
#164477=CARTESIAN_POINT('Ctrl Pts',(-14.4026149179538,-10.8763499173728,
-546.65230705718));
#164478=CARTESIAN_POINT('Ctrl Pts',(-15.4104571591017,-9.54175110365538,
-548.14642470424));
#164479=CARTESIAN_POINT('Ctrl Pts',(-16.1559070823762,-8.04468584505497,
-549.640542351298));
#164480=CARTESIAN_POINT('Ctrl Pts',(-16.9013570056506,-6.54762058645456,
-551.134659998357));
#164481=CARTESIAN_POINT('Ctrl Pts',(-17.3590292079831,-4.93906964482095,
-552.628777645416));
#164482=CARTESIAN_POINT('Ctrl Pts',(-17.8167014103155,-3.33051870318735,
-554.122895292474));
#164483=CARTESIAN_POINT('Ctrl Pts',(-17.9710104137728,-1.66525935159368,
-555.617012939533));
#164484=CARTESIAN_POINT('Ctrl Pts',(-18.1253194172301,-1.10985572039171E-15,
-557.111130586592));
#164485=CARTESIAN_POINT('Ctrl Pts',(-17.9710104137728,1.66525935159367,
-558.605248233651));
#164486=CARTESIAN_POINT('Ctrl Pts',(-17.8167014103155,3.33051870318735,
-560.09936588071));
#164487=CARTESIAN_POINT('Ctrl Pts',(-17.3590292079831,4.93906964482096,
-561.593483527769));
#164488=CARTESIAN_POINT('Ctrl Pts',(-16.9013570056506,6.54762058645456,
-563.087601174828));
#164489=CARTESIAN_POINT('Ctrl Pts',(-16.1559070823762,8.04468584505497,
-564.581718821887));
#164490=CARTESIAN_POINT('Ctrl Pts',(-15.4104571591017,9.54175110365538,
-566.075836468945));
#164491=CARTESIAN_POINT('Ctrl Pts',(-14.4026149179538,10.8763499173728,
-567.569954116004));
#164492=CARTESIAN_POINT('Ctrl Pts',(-13.3947726768058,12.2109487310903,
-569.064071763063));
#164493=CARTESIAN_POINT('Ctrl Pts',(-12.1588589765331,13.3376329379985,
-570.558189410121));
#164494=CARTESIAN_POINT('Ctrl Pts',(-10.9229452762603,14.4643171449067,
-572.05230705718));
#164495=CARTESIAN_POINT('Ctrl Pts',(-9.50104767561052,15.3447188656481,
-573.546424704239));
#164496=CARTESIAN_POINT('Ctrl Pts',(-8.07915007496071,16.2251205863895,
-575.040542351298));
#164497=CARTESIAN_POINT('Ctrl Pts',(-6.51968959134574,16.8292587962898,
-576.534659998357));
#164498=CARTESIAN_POINT('Ctrl Pts',(-4.96022910773078,17.4333970061901,
-578.028777645416));
#164499=CARTESIAN_POINT('Ctrl Pts',(-3.31631129755346,17.7406985030951,
-579.522895292475));
#164500=CARTESIAN_POINT('Ctrl Pts',(-1.67239348737615,18.048,-581.017012939534));
#164501=CARTESIAN_POINT('Ctrl Pts',(-2.21024254310115E-15,18.048,-582.511130586592));
#164502=CARTESIAN_POINT('Ctrl Pts',(1.67239348737616,18.048,-584.005248233651));
#164503=CARTESIAN_POINT('Ctrl Pts',(3.31631129755346,17.7406985030951,-585.49936588071));
#164504=CARTESIAN_POINT('Ctrl Pts',(4.96022910773077,17.4333970061901,-586.993483527769));
#164505=CARTESIAN_POINT('Ctrl Pts',(6.51968959134575,16.8292587962898,-588.487601174827));
#164506=CARTESIAN_POINT('Ctrl Pts',(8.07915007496071,16.2251205863895,-589.981718821886));
#164507=CARTESIAN_POINT('Ctrl Pts',(9.50104767561053,15.3447188656481,-591.475836468945));
#164508=CARTESIAN_POINT('Ctrl Pts',(10.9229452762603,14.4643171449067,-592.969954116004));
#164509=CARTESIAN_POINT('Ctrl Pts',(12.1588589765331,13.3376329379985,-594.464071763063));
#164510=CARTESIAN_POINT('Ctrl Pts',(13.3947726768058,12.2109487310903,-595.958189410122));
#164511=CARTESIAN_POINT('Ctrl Pts',(14.4026149179538,10.8763499173728,-597.45230705718));
#164512=CARTESIAN_POINT('Ctrl Pts',(15.4104571591017,9.54175110365538,-598.946424704239));
#164513=CARTESIAN_POINT('Ctrl Pts',(16.1559070823762,8.04468584505496,-600.440542351298));
#164514=CARTESIAN_POINT('Ctrl Pts',(16.9013570056506,6.54762058645456,-601.934659998357));
#164515=CARTESIAN_POINT('Ctrl Pts',(17.3590292079831,4.93906964482096,-603.428777645416));
#164516=CARTESIAN_POINT('Ctrl Pts',(17.8167014103155,3.33051870318735,-604.922895292475));
#164517=CARTESIAN_POINT('Ctrl Pts',(17.9710104137728,1.66525935159367,-606.417012939533));
#164518=CARTESIAN_POINT('Ctrl Pts',(18.1253194172301,3.32956716117513E-15,
-607.911130586592));
#164519=CARTESIAN_POINT('Ctrl Pts',(17.9710104137728,-1.66525935159367,
-609.405248233651));
#164520=CARTESIAN_POINT('Ctrl Pts',(17.8167014103155,-3.33051870318736,
-610.89936588071));
#164521=CARTESIAN_POINT('Ctrl Pts',(17.3590292079831,-4.93906964482095,
-612.393483527768));
#164522=CARTESIAN_POINT('Ctrl Pts',(16.9013570056506,-6.54762058645456,
-613.887601174828));
#164523=CARTESIAN_POINT('Ctrl Pts',(16.1559070823762,-8.04468584505497,
-615.381718821886));
#164524=CARTESIAN_POINT('Ctrl Pts',(15.4104571591017,-9.54175110365538,
-616.875836468945));
#164525=CARTESIAN_POINT('Ctrl Pts',(14.4026149179538,-10.8763499173728,
-618.369954116004));
#164526=CARTESIAN_POINT('Ctrl Pts',(13.3947726768058,-12.2109487310903,
-619.864071763063));
#164527=CARTESIAN_POINT('Ctrl Pts',(12.1588589765331,-13.3376329379985,
-621.358189410122));
#164528=CARTESIAN_POINT('Ctrl Pts',(10.9229452762603,-14.4643171449067,
-622.852307057181));
#164529=CARTESIAN_POINT('Ctrl Pts',(9.50104767561053,-15.3447188656481,
-624.346424704239));
#164530=CARTESIAN_POINT('Ctrl Pts',(8.07915007496071,-16.2251205863895,
-625.840542351298));
#164531=CARTESIAN_POINT('Ctrl Pts',(6.51968959134574,-16.8292587962898,
-627.334659998357));
#164532=CARTESIAN_POINT('Ctrl Pts',(4.96022910773078,-17.4333970061901,
-628.828777645416));
#164533=CARTESIAN_POINT('Ctrl Pts',(3.31631129755346,-17.7406985030951,
-630.322895292474));
#164534=CARTESIAN_POINT('Ctrl Pts',(1.67239348737615,-18.048,-631.817012939533));
#164535=CARTESIAN_POINT('Ctrl Pts',(0.,-18.048,-633.311130586592));
#164536=CARTESIAN_POINT('Ctrl Pts',(-1.67239348737615,-18.048,-634.805248233651));
#164537=CARTESIAN_POINT('Ctrl Pts',(-3.31631129755346,-17.7406985030951,
-636.29936588071));
#164538=CARTESIAN_POINT('Ctrl Pts',(-4.96022910773077,-17.4333970061901,
-637.793483527769));
#164539=CARTESIAN_POINT('Ctrl Pts',(-6.51968959134574,-16.8292587962898,
-639.287601174828));
#164540=CARTESIAN_POINT('Ctrl Pts',(-8.07915007496071,-16.2251205863895,
-640.781718821886));
#164541=CARTESIAN_POINT('Ctrl Pts',(-9.50104767561052,-15.3447188656481,
-642.275836468945));
#164542=CARTESIAN_POINT('Ctrl Pts',(-10.9229452762603,-14.4643171449067,
-643.769954116004));
#164543=CARTESIAN_POINT('Ctrl Pts',(-12.1588589765331,-13.3376329379985,
-645.264071763063));
#164544=CARTESIAN_POINT('Ctrl Pts',(-13.3947726768058,-12.2109487310903,
-646.758189410122));
#164545=CARTESIAN_POINT('Ctrl Pts',(-14.4026149179538,-10.8763499173728,
-648.25230705718));
#164546=CARTESIAN_POINT('Ctrl Pts',(-15.4104571591017,-9.54175110365538,
-649.746424704239));
#164547=CARTESIAN_POINT('Ctrl Pts',(-16.1559070823762,-8.04468584505497,
-651.240542351298));
#164548=CARTESIAN_POINT('Ctrl Pts',(-16.9013570056506,-6.54762058645456,
-652.734659998357));
#164549=CARTESIAN_POINT('Ctrl Pts',(-17.3590292079831,-4.93906964482095,
-654.228777645416));
#164550=CARTESIAN_POINT('Ctrl Pts',(-17.8167014103155,-3.33051870318735,
-655.722895292475));
#164551=CARTESIAN_POINT('Ctrl Pts',(-17.9710104137728,-1.66525935159368,
-657.217012939533));
#164552=CARTESIAN_POINT('Ctrl Pts',(-18.1253194172301,-1.10985572039171E-15,
-658.711130586592));
#164553=CARTESIAN_POINT('Ctrl Pts',(-17.9710104137728,1.66525935159367,
-660.205248233651));
#164554=CARTESIAN_POINT('Ctrl Pts',(-17.8167014103155,3.33051870318735,
-661.69936588071));
#164555=CARTESIAN_POINT('Ctrl Pts',(-17.3590292079831,4.93906964482096,
-663.193483527769));
#164556=CARTESIAN_POINT('Ctrl Pts',(-16.9013570056506,6.54762058645456,
-664.687601174827));
#164557=CARTESIAN_POINT('Ctrl Pts',(-16.1559070823762,8.04468584505497,
-666.181718821887));
#164558=CARTESIAN_POINT('Ctrl Pts',(-15.4104571591017,9.54175110365538,
-667.675836468945));
#164559=CARTESIAN_POINT('Ctrl Pts',(-14.4026149179538,10.8763499173728,
-669.169954116004));
#164560=CARTESIAN_POINT('Ctrl Pts',(-13.3947726768058,12.2109487310903,
-670.664071763063));
#164561=CARTESIAN_POINT('Ctrl Pts',(-12.1588589765331,13.3376329379985,
-672.158189410121));
#164562=CARTESIAN_POINT('Ctrl Pts',(-10.9229452762603,14.4643171449067,
-673.65230705718));
#164563=CARTESIAN_POINT('Ctrl Pts',(-9.50104767561052,15.3447188656481,
-675.146424704239));
#164564=CARTESIAN_POINT('Ctrl Pts',(-8.07915007496071,16.2251205863895,
-676.640542351298));
#164565=CARTESIAN_POINT('Ctrl Pts',(-6.51968959134574,16.8292587962898,
-678.134659998357));
#164566=CARTESIAN_POINT('Ctrl Pts',(-4.96022910773078,17.4333970061901,
-679.628777645416));
#164567=CARTESIAN_POINT('Ctrl Pts',(-3.31631129755346,17.7406985030951,
-681.122895292475));
#164568=CARTESIAN_POINT('Ctrl Pts',(-1.67239348737615,18.048,-682.617012939534));
#164569=CARTESIAN_POINT('Ctrl Pts',(-2.21024254310115E-15,18.048,-684.111130586592));
#164570=CARTESIAN_POINT('Ctrl Pts',(1.67239348737616,18.048,-685.605248233651));
#164571=CARTESIAN_POINT('Ctrl Pts',(3.31631129755346,17.7406985030951,-687.09936588071));
#164572=CARTESIAN_POINT('Ctrl Pts',(4.96022910773077,17.4333970061901,-688.593483527769));
#164573=CARTESIAN_POINT('Ctrl Pts',(6.51968959134575,16.8292587962898,-690.087601174827));
#164574=CARTESIAN_POINT('Ctrl Pts',(8.07915007496071,16.2251205863895,-691.581718821886));
#164575=CARTESIAN_POINT('Ctrl Pts',(9.50104767561053,15.3447188656481,-693.075836468945));
#164576=CARTESIAN_POINT('Ctrl Pts',(10.9229452762603,14.4643171449067,-694.569954116004));
#164577=CARTESIAN_POINT('Ctrl Pts',(12.1588589765331,13.3376329379985,-696.064071763063));
#164578=CARTESIAN_POINT('Ctrl Pts',(13.3947726768058,12.2109487310903,-697.558189410122));
#164579=CARTESIAN_POINT('Ctrl Pts',(14.4026149179538,10.8763499173728,-699.052307057181));
#164580=CARTESIAN_POINT('Ctrl Pts',(15.4104571591017,9.54175110365538,-700.546424704239));
#164581=CARTESIAN_POINT('Ctrl Pts',(16.1559070823762,8.04468584505496,-702.040542351298));
#164582=CARTESIAN_POINT('Ctrl Pts',(16.9013570056506,6.54762058645456,-703.534659998357));
#164583=CARTESIAN_POINT('Ctrl Pts',(17.3590292079831,4.93906964482096,-705.028777645416));
#164584=CARTESIAN_POINT('Ctrl Pts',(17.8167014103155,3.33051870318735,-706.522895292475));
#164585=CARTESIAN_POINT('Ctrl Pts',(17.9710104137728,1.66525935159367,-708.017012939533));
#164586=CARTESIAN_POINT('Ctrl Pts',(18.1253194172301,3.32956716117513E-15,
-709.511130586592));
#164587=CARTESIAN_POINT('Ctrl Pts',(17.9710104137728,-1.66525935159367,
-711.005248233651));
#164588=CARTESIAN_POINT('Ctrl Pts',(17.8167014103155,-3.33051870318736,
-712.49936588071));
#164589=CARTESIAN_POINT('Ctrl Pts',(17.3590292079831,-4.93906964482095,
-713.993483527769));
#164590=CARTESIAN_POINT('Ctrl Pts',(16.9013570056506,-6.54762058645456,
-715.487601174828));
#164591=CARTESIAN_POINT('Ctrl Pts',(16.1559070823762,-8.04468584505497,
-716.981718821886));
#164592=CARTESIAN_POINT('Ctrl Pts',(15.4104571591017,-9.54175110365538,
-718.475836468945));
#164593=CARTESIAN_POINT('Ctrl Pts',(14.4026149179538,-10.8763499173728,
-719.969954116004));
#164594=CARTESIAN_POINT('Ctrl Pts',(13.3947726768058,-12.2109487310903,
-721.464071763063));
#164595=CARTESIAN_POINT('Ctrl Pts',(12.1588589765331,-13.3376329379985,
-722.958189410122));
#164596=CARTESIAN_POINT('Ctrl Pts',(10.9229452762603,-14.4643171449067,
-724.452307057181));
#164597=CARTESIAN_POINT('Ctrl Pts',(9.50104767561053,-15.3447188656481,
-725.946424704239));
#164598=CARTESIAN_POINT('Ctrl Pts',(8.07915007496071,-16.2251205863895,
-727.440542351298));
#164599=CARTESIAN_POINT('Ctrl Pts',(6.51968959134574,-16.8292587962898,
-728.934659998357));
#164600=CARTESIAN_POINT('Ctrl Pts',(4.96022910773078,-17.4333970061901,
-730.428777645416));
#164601=CARTESIAN_POINT('Ctrl Pts',(3.31631129755346,-17.7406985030951,
-731.922895292474));
#164602=CARTESIAN_POINT('Ctrl Pts',(1.67239348737615,-18.048,-733.417012939533));
#164603=CARTESIAN_POINT('Ctrl Pts',(0.,-18.048,-734.911130586592));
#164604=CARTESIAN_POINT('Ctrl Pts',(-1.67239348737615,-18.048,-736.405248233651));
#164605=CARTESIAN_POINT('Ctrl Pts',(-3.31631129755346,-17.7406985030951,
-737.89936588071));
#164606=CARTESIAN_POINT('Ctrl Pts',(-4.96022910773077,-17.4333970061901,
-739.393483527769));
#164607=CARTESIAN_POINT('Ctrl Pts',(-6.51968959134574,-16.8292587962898,
-740.887601174828));
#164608=CARTESIAN_POINT('Ctrl Pts',(-8.07915007496071,-16.2251205863895,
-742.381718821887));
#164609=CARTESIAN_POINT('Ctrl Pts',(-9.50104767561052,-15.3447188656481,
-743.875836468945));
#164610=CARTESIAN_POINT('Ctrl Pts',(-10.9229452762603,-14.4643171449067,
-745.369954116004));
#164611=CARTESIAN_POINT('Ctrl Pts',(-12.1588589765331,-13.3376329379985,
-746.864071763063));
#164612=CARTESIAN_POINT('Ctrl Pts',(-13.3947726768058,-12.2109487310903,
-748.358189410122));
#164613=CARTESIAN_POINT('Ctrl Pts',(-14.4026149179538,-10.8763499173728,
-749.85230705718));
#164614=CARTESIAN_POINT('Ctrl Pts',(-15.4104571591017,-9.54175110365538,
-751.346424704239));
#164615=CARTESIAN_POINT('Ctrl Pts',(-16.1559070823762,-8.04468584505497,
-752.840542351298));
#164616=CARTESIAN_POINT('Ctrl Pts',(-16.9013570056506,-6.54762058645456,
-754.334659998357));
#164617=CARTESIAN_POINT('Ctrl Pts',(-17.3590292079831,-4.93906964482095,
-755.828777645416));
#164618=CARTESIAN_POINT('Ctrl Pts',(-17.8167014103155,-3.33051870318735,
-757.322895292475));
#164619=CARTESIAN_POINT('Ctrl Pts',(-17.9710104137728,-1.66525935159368,
-758.817012939534));
#164620=CARTESIAN_POINT('Ctrl Pts',(-18.1253194172301,-1.10985572039171E-15,
-760.311130586593));
#164621=CARTESIAN_POINT('Ctrl Pts',(-17.9710104137728,1.66525935159367,
-761.805248233651));
#164622=CARTESIAN_POINT('Ctrl Pts',(-17.8167014103155,3.33051870318735,
-763.29936588071));
#164623=CARTESIAN_POINT('Ctrl Pts',(-17.3590292079831,4.93906964482096,
-764.793483527769));
#164624=CARTESIAN_POINT('Ctrl Pts',(-16.9013570056506,6.54762058645456,
-766.287601174827));
#164625=CARTESIAN_POINT('Ctrl Pts',(-16.1559070823762,8.04468584505497,
-767.781718821886));
#164626=CARTESIAN_POINT('Ctrl Pts',(-15.4104571591017,9.54175110365538,
-769.275836468945));
#164627=CARTESIAN_POINT('Ctrl Pts',(-14.4026149179538,10.8763499173728,
-770.769954116004));
#164628=CARTESIAN_POINT('Ctrl Pts',(-13.3947726768058,12.2109487310903,
-772.264071763063));
#164629=CARTESIAN_POINT('Ctrl Pts',(-12.1588589765331,13.3376329379985,
-773.758189410122));
#164630=CARTESIAN_POINT('Ctrl Pts',(-10.9229452762603,14.4643171449067,
-775.252307057181));
#164631=CARTESIAN_POINT('Ctrl Pts',(-9.50104767561052,15.3447188656481,
-776.746424704239));
#164632=CARTESIAN_POINT('Ctrl Pts',(-8.07915007496071,16.2251205863895,
-778.240542351298));
#164633=CARTESIAN_POINT('Ctrl Pts',(-6.51968959134574,16.8292587962898,
-779.734659998357));
#164634=CARTESIAN_POINT('Ctrl Pts',(-4.96022910773078,17.4333970061901,
-781.228777645416));
#164635=CARTESIAN_POINT('Ctrl Pts',(-3.31631129755346,17.7406985030951,
-782.722895292475));
#164636=CARTESIAN_POINT('Ctrl Pts',(-1.67239348737615,18.048,-784.217012939534));
#164637=CARTESIAN_POINT('Ctrl Pts',(-2.21024254310115E-15,18.048,-785.711130586592));
#164638=CARTESIAN_POINT('Ctrl Pts',(1.67239348737616,18.048,-787.205248233651));
#164639=CARTESIAN_POINT('Ctrl Pts',(3.31631129755346,17.7406985030951,-788.69936588071));
#164640=CARTESIAN_POINT('Ctrl Pts',(4.96022910773077,17.4333970061901,-790.193483527769));
#164641=CARTESIAN_POINT('Ctrl Pts',(6.51968959134575,16.8292587962898,-791.687601174827));
#164642=CARTESIAN_POINT('Ctrl Pts',(8.07915007496071,16.2251205863895,-793.181718821886));
#164643=CARTESIAN_POINT('Ctrl Pts',(9.50104767561053,15.3447188656481,-794.675836468945));
#164644=CARTESIAN_POINT('Ctrl Pts',(10.9229452762603,14.4643171449067,-796.169954116004));
#164645=CARTESIAN_POINT('Ctrl Pts',(12.1588589765331,13.3376329379985,-797.664071763063));
#164646=CARTESIAN_POINT('Ctrl Pts',(13.3947726768058,12.2109487310903,-799.158189410122));
#164647=CARTESIAN_POINT('Ctrl Pts',(14.4026149179538,10.8763499173728,-800.65230705718));
#164648=CARTESIAN_POINT('Ctrl Pts',(15.4104571591017,9.54175110365538,-802.146424704239));
#164649=CARTESIAN_POINT('Ctrl Pts',(16.1559070823762,8.04468584505496,-803.640542351298));
#164650=CARTESIAN_POINT('Ctrl Pts',(16.9013570056506,6.54762058645456,-805.134659998357));
#164651=CARTESIAN_POINT('Ctrl Pts',(17.3590292079831,4.93906964482096,-806.628777645416));
#164652=CARTESIAN_POINT('Ctrl Pts',(17.8167014103155,3.33051870318735,-808.122895292474));
#164653=CARTESIAN_POINT('Ctrl Pts',(17.9710104137728,1.66525935159367,-809.617012939533));
#164654=CARTESIAN_POINT('Ctrl Pts',(18.1253194172301,3.32956716117513E-15,
-811.111130586592));
#164655=CARTESIAN_POINT('Ctrl Pts',(17.9710104137728,-1.66525935159367,
-812.605248233651));
#164656=CARTESIAN_POINT('Ctrl Pts',(17.8167014103155,-3.33051870318736,
-814.09936588071));
#164657=CARTESIAN_POINT('Ctrl Pts',(17.3590292079831,-4.93906964482095,
-815.593483527769));
#164658=CARTESIAN_POINT('Ctrl Pts',(16.9013570056506,-6.54762058645456,
-817.087601174828));
#164659=CARTESIAN_POINT('Ctrl Pts',(16.1559070823762,-8.04468584505497,
-818.581718821887));
#164660=CARTESIAN_POINT('Ctrl Pts',(15.4104571591017,-9.54175110365538,
-820.075836468945));
#164661=CARTESIAN_POINT('Ctrl Pts',(14.4026149179538,-10.8763499173728,
-821.569954116004));
#164662=CARTESIAN_POINT('Ctrl Pts',(13.3947726768058,-12.2109487310903,
-823.064071763063));
#164663=CARTESIAN_POINT('Ctrl Pts',(12.1588589765331,-13.3376329379985,
-824.558189410121));
#164664=CARTESIAN_POINT('Ctrl Pts',(10.9229452762603,-14.4643171449067,
-826.05230705718));
#164665=CARTESIAN_POINT('Ctrl Pts',(9.50104767561053,-15.3447188656481,
-827.546424704239));
#164666=CARTESIAN_POINT('Ctrl Pts',(8.07915007496071,-16.2251205863895,
-829.040542351298));
#164667=CARTESIAN_POINT('Ctrl Pts',(6.51968959134574,-16.8292587962898,
-830.534659998357));
#164668=CARTESIAN_POINT('Ctrl Pts',(4.96022910773078,-17.4333970061901,
-832.028777645416));
#164669=CARTESIAN_POINT('Ctrl Pts',(3.31631129755346,-17.7406985030951,
-833.522895292475));
#164670=CARTESIAN_POINT('Ctrl Pts',(1.67239348737615,-18.048,-835.017012939534));
#164671=CARTESIAN_POINT('Ctrl Pts',(0.,-18.048,-836.511130586592));
#164672=CARTESIAN_POINT('Ctrl Pts',(-1.67239348737615,-18.048,-838.005248233651));
#164673=CARTESIAN_POINT('Ctrl Pts',(-3.31631129755346,-17.7406985030951,
-839.49936588071));
#164674=CARTESIAN_POINT('Ctrl Pts',(-4.96022910773077,-17.4333970061901,
-840.993483527769));
#164675=CARTESIAN_POINT('Ctrl Pts',(-6.51968959134574,-16.8292587962898,
-842.487601174827));
#164676=CARTESIAN_POINT('Ctrl Pts',(-8.07915007496071,-16.2251205863895,
-843.981718821886));
#164677=CARTESIAN_POINT('Ctrl Pts',(-9.50104767561052,-15.3447188656481,
-845.475836468945));
#164678=CARTESIAN_POINT('Ctrl Pts',(-10.9229452762603,-14.4643171449067,
-846.969954116004));
#164679=CARTESIAN_POINT('Ctrl Pts',(-12.1588589765331,-13.3376329379985,
-848.464071763063));
#164680=CARTESIAN_POINT('Ctrl Pts',(-13.3947726768058,-12.2109487310903,
-849.958189410122));
#164681=CARTESIAN_POINT('Ctrl Pts',(-14.4026149179538,-10.8763499173728,
-851.45230705718));
#164682=CARTESIAN_POINT('Ctrl Pts',(-15.4104571591017,-9.54175110365538,
-852.946424704239));
#164683=CARTESIAN_POINT('Ctrl Pts',(-16.1559070823762,-8.04468584505497,
-854.440542351298));
#164684=CARTESIAN_POINT('Ctrl Pts',(-16.9013570056506,-6.54762058645456,
-855.934659998357));
#164685=CARTESIAN_POINT('Ctrl Pts',(-17.3590292079831,-4.93906964482095,
-857.428777645416));
#164686=CARTESIAN_POINT('Ctrl Pts',(-17.8167014103155,-3.33051870318735,
-858.922895292475));
#164687=CARTESIAN_POINT('Ctrl Pts',(-17.9710104137728,-1.66525935159368,
-860.417012939533));
#164688=CARTESIAN_POINT('Ctrl Pts',(-18.1253194172301,-1.10985572039171E-15,
-861.911130586592));
#164689=CARTESIAN_POINT('Ctrl Pts',(-17.9710104137728,1.66525935159367,
-863.405248233651));
#164690=CARTESIAN_POINT('Ctrl Pts',(-17.8167014103155,3.33051870318735,
-864.89936588071));
#164691=CARTESIAN_POINT('Ctrl Pts',(-17.3590292079831,4.93906964482096,
-866.393483527768));
#164692=CARTESIAN_POINT('Ctrl Pts',(-16.9013570056506,6.54762058645456,
-867.887601174827));
#164693=CARTESIAN_POINT('Ctrl Pts',(-16.1559070823762,8.04468584505497,
-869.381718821886));
#164694=CARTESIAN_POINT('Ctrl Pts',(-15.4104571591017,9.54175110365538,
-870.875836468945));
#164695=CARTESIAN_POINT('Ctrl Pts',(-14.4026149179538,10.8763499173728,
-872.369954116004));
#164696=CARTESIAN_POINT('Ctrl Pts',(-13.3947726768058,12.2109487310903,
-873.864071763063));
#164697=CARTESIAN_POINT('Ctrl Pts',(-12.1588589765331,13.3376329379985,
-875.358189410122));
#164698=CARTESIAN_POINT('Ctrl Pts',(-10.9229452762603,14.4643171449067,
-876.85230705718));
#164699=CARTESIAN_POINT('Ctrl Pts',(-9.50104767561052,15.3447188656481,
-878.346424704239));
#164700=CARTESIAN_POINT('Ctrl Pts',(-8.07915007496071,16.2251205863895,
-879.840542351298));
#164701=CARTESIAN_POINT('Ctrl Pts',(-6.51968959134574,16.8292587962898,
-881.334659998357));
#164702=CARTESIAN_POINT('Ctrl Pts',(-4.96022910773078,17.4333970061901,
-882.828777645416));
#164703=CARTESIAN_POINT('Ctrl Pts',(-3.31631129755346,17.7406985030951,
-884.322895292474));
#164704=CARTESIAN_POINT('Ctrl Pts',(-1.67239348737615,18.048,-885.817012939534));
#164705=CARTESIAN_POINT('Ctrl Pts',(-2.21024254310115E-15,18.048,-887.311130586592));
#164706=CARTESIAN_POINT('Ctrl Pts',(1.67239348737616,18.048,-888.805248233651));
#164707=CARTESIAN_POINT('Ctrl Pts',(3.31631129755346,17.7406985030951,-890.29936588071));
#164708=CARTESIAN_POINT('Ctrl Pts',(4.96022910773077,17.4333970061901,-891.793483527769));
#164709=CARTESIAN_POINT('Ctrl Pts',(6.51968959134575,16.8292587962898,-893.287601174828));
#164710=CARTESIAN_POINT('Ctrl Pts',(8.07915007496071,16.2251205863895,-894.781718821887));
#164711=CARTESIAN_POINT('Ctrl Pts',(9.50104767561053,15.3447188656481,-896.275836468945));
#164712=CARTESIAN_POINT('Ctrl Pts',(10.9229452762603,14.4643171449067,-897.769954116004));
#164713=CARTESIAN_POINT('Ctrl Pts',(12.1588589765331,13.3376329379985,-899.264071763063));
#164714=CARTESIAN_POINT('Ctrl Pts',(13.3947726768058,12.2109487310903,-900.758189410122));
#164715=CARTESIAN_POINT('Ctrl Pts',(14.4026149179538,10.8763499173728,-902.25230705718));
#164716=CARTESIAN_POINT('Ctrl Pts',(15.4104571591017,9.54175110365538,-903.746424704239));
#164717=CARTESIAN_POINT('Ctrl Pts',(16.1559070823762,8.04468584505496,-905.240542351298));
#164718=CARTESIAN_POINT('Ctrl Pts',(16.9013570056506,6.54762058645456,-906.734659998357));
#164719=CARTESIAN_POINT('Ctrl Pts',(17.3590292079831,4.93906964482096,-908.228777645416));
#164720=CARTESIAN_POINT('Ctrl Pts',(17.8167014103155,3.33051870318735,-909.722895292475));
#164721=CARTESIAN_POINT('Ctrl Pts',(17.9710104137728,1.66525935159367,-911.217012939533));
#164722=CARTESIAN_POINT('Ctrl Pts',(18.1253194172301,3.32956716117513E-15,
-912.711130586592));
#164723=CARTESIAN_POINT('Ctrl Pts',(17.9710104137728,-1.66525935159367,
-914.205248233651));
#164724=CARTESIAN_POINT('Ctrl Pts',(17.8167014103155,-3.33051870318736,
-915.69936588071));
#164725=CARTESIAN_POINT('Ctrl Pts',(17.3590292079831,-4.93906964482095,
-917.193483527769));
#164726=CARTESIAN_POINT('Ctrl Pts',(16.9013570056506,-6.54762058645456,
-918.687601174827));
#164727=CARTESIAN_POINT('Ctrl Pts',(16.1559070823762,-8.04468584505497,
-920.181718821887));
#164728=CARTESIAN_POINT('Ctrl Pts',(15.4104571591017,-9.54175110365538,
-921.675836468945));
#164729=CARTESIAN_POINT('Ctrl Pts',(14.4026149179538,-10.8763499173728,
-923.169954116004));
#164730=CARTESIAN_POINT('Ctrl Pts',(13.3947726768058,-12.2109487310903,
-924.664071763063));
#164731=CARTESIAN_POINT('Ctrl Pts',(12.1588589765331,-13.3376329379985,
-926.158189410122));
#164732=CARTESIAN_POINT('Ctrl Pts',(10.9229452762603,-14.4643171449067,
-927.65230705718));
#164733=CARTESIAN_POINT('Ctrl Pts',(9.50104767561053,-15.3447188656481,
-929.146424704239));
#164734=CARTESIAN_POINT('Ctrl Pts',(8.07915007496071,-16.2251205863895,
-930.640542351298));
#164735=CARTESIAN_POINT('Ctrl Pts',(6.51968959134574,-16.8292587962898,
-932.134659998357));
#164736=CARTESIAN_POINT('Ctrl Pts',(4.96022910773078,-17.4333970061901,
-933.628777645416));
#164737=CARTESIAN_POINT('Ctrl Pts',(3.31631129755346,-17.7406985030951,
-935.122895292475));
#164738=CARTESIAN_POINT('Ctrl Pts',(1.67239348737615,-18.048,-936.617012939534));
#164739=CARTESIAN_POINT('Ctrl Pts',(0.,-18.048,-938.111130586592));
#164740=CARTESIAN_POINT('Ctrl Pts',(-1.67239348737615,-18.048,-939.605248233651));
#164741=CARTESIAN_POINT('Ctrl Pts',(-3.31631129755346,-17.7406985030951,
-941.09936588071));
#164742=CARTESIAN_POINT('Ctrl Pts',(-4.96022910773077,-17.4333970061901,
-942.593483527769));
#164743=CARTESIAN_POINT('Ctrl Pts',(-6.51968959134574,-16.8292587962898,
-944.087601174827));
#164744=CARTESIAN_POINT('Ctrl Pts',(-8.07915007496071,-16.2251205863895,
-945.581718821886));
#164745=CARTESIAN_POINT('Ctrl Pts',(-9.50104767561052,-15.3447188656481,
-947.075836468945));
#164746=CARTESIAN_POINT('Ctrl Pts',(-10.9229452762603,-14.4643171449067,
-948.569954116004));
#164747=CARTESIAN_POINT('Ctrl Pts',(-12.1588589765331,-13.3376329379985,
-950.064071763063));
#164748=CARTESIAN_POINT('Ctrl Pts',(-13.3947726768058,-12.2109487310903,
-951.558189410122));
#164749=CARTESIAN_POINT('Ctrl Pts',(-14.4026149179538,-10.8763499173728,
-953.052307057181));
#164750=CARTESIAN_POINT('Ctrl Pts',(-15.4104571591017,-9.54175110365538,
-954.54642470424));
#164751=CARTESIAN_POINT('Ctrl Pts',(-16.1559070823762,-8.04468584505497,
-956.040542351298));
#164752=CARTESIAN_POINT('Ctrl Pts',(-16.9013570056506,-6.54762058645456,
-957.534659998357));
#164753=CARTESIAN_POINT('Ctrl Pts',(-17.3590292079831,-4.93906964482095,
-959.028777645416));
#164754=CARTESIAN_POINT('Ctrl Pts',(-17.8167014103155,-3.33051870318735,
-960.522895292475));
#164755=CARTESIAN_POINT('Ctrl Pts',(-17.9710104137728,-1.66525935159368,
-962.017012939533));
#164756=CARTESIAN_POINT('Ctrl Pts',(-18.1253194172301,-1.10985572039171E-15,
-963.511130586592));
#164757=CARTESIAN_POINT('Ctrl Pts',(-17.9710104137728,1.66525935159367,
-965.005248233651));
#164758=CARTESIAN_POINT('Ctrl Pts',(-17.8167014103155,3.33051870318735,
-966.49936588071));
#164759=CARTESIAN_POINT('Ctrl Pts',(-17.3590292079831,4.93906964482096,
-967.993483527769));
#164760=CARTESIAN_POINT('Ctrl Pts',(-16.9013570056506,6.54762058645456,
-969.487601174828));
#164761=CARTESIAN_POINT('Ctrl Pts',(-16.1559070823762,8.04468584505497,
-970.981718821886));
#164762=CARTESIAN_POINT('Ctrl Pts',(-15.4104571591017,9.54175110365538,
-972.475836468945));
#164763=CARTESIAN_POINT('Ctrl Pts',(-14.4026149179538,10.8763499173728,
-973.969954116004));
#164764=CARTESIAN_POINT('Ctrl Pts',(-13.3947726768058,12.2109487310903,
-975.464071763063));
#164765=CARTESIAN_POINT('Ctrl Pts',(-12.1588589765331,13.3376329379985,
-976.958189410122));
#164766=CARTESIAN_POINT('Ctrl Pts',(-10.9229452762603,14.4643171449067,
-978.452307057181));
#164767=CARTESIAN_POINT('Ctrl Pts',(-9.50104767561052,15.3447188656481,
-979.946424704239));
#164768=CARTESIAN_POINT('Ctrl Pts',(-8.07915007496071,16.2251205863895,
-981.440542351298));
#164769=CARTESIAN_POINT('Ctrl Pts',(-6.51968959134574,16.8292587962898,
-982.934659998357));
#164770=CARTESIAN_POINT('Ctrl Pts',(-4.96022910773078,17.4333970061901,
-984.428777645416));
#164771=CARTESIAN_POINT('Ctrl Pts',(-3.31631129755346,17.7406985030951,
-985.922895292474));
#164772=CARTESIAN_POINT('Ctrl Pts',(-1.67239348737615,18.048,-987.417012939533));
#164773=CARTESIAN_POINT('Ctrl Pts',(-2.21024254310115E-15,18.048,-988.911130586592));
#164774=CARTESIAN_POINT('Ctrl Pts',(1.67239348737616,18.048,-990.405248233651));
#164775=CARTESIAN_POINT('Ctrl Pts',(3.31631129755346,17.7406985030951,-991.89936588071));
#164776=CARTESIAN_POINT('Ctrl Pts',(4.96022910773077,17.4333970061901,-993.393483527769));
#164777=CARTESIAN_POINT('Ctrl Pts',(6.51968959134575,16.8292587962898,-994.887601174828));
#164778=CARTESIAN_POINT('Ctrl Pts',(8.07915007496071,16.2251205863895,-996.381718821887));
#164779=CARTESIAN_POINT('Ctrl Pts',(9.50104767561053,15.3447188656481,-997.875836468945));
#164780=CARTESIAN_POINT('Ctrl Pts',(10.9229452762603,14.4643171449067,-999.369954116004));
#164781=CARTESIAN_POINT('Ctrl Pts',(12.1588589765331,13.3376329379985,-1000.86407176306));
#164782=CARTESIAN_POINT('Ctrl Pts',(13.3947726768058,12.2109487310903,-1002.35818941012));
#164783=CARTESIAN_POINT('Ctrl Pts',(14.4026149179538,10.8763499173728,-1003.85230705718));
#164784=CARTESIAN_POINT('Ctrl Pts',(15.4104571591017,9.54175110365538,-1005.34642470424));
#164785=CARTESIAN_POINT('Ctrl Pts',(16.1559070823762,8.04468584505496,-1006.8405423513));
#164786=CARTESIAN_POINT('Ctrl Pts',(16.9013570056506,6.54762058645456,-1008.33465999836));
#164787=CARTESIAN_POINT('Ctrl Pts',(17.3590292079831,4.93906964482096,-1009.82877764542));
#164788=CARTESIAN_POINT('Ctrl Pts',(17.8167014103155,3.33051870318735,-1011.32289529247));
#164789=CARTESIAN_POINT('Ctrl Pts',(17.9710104137728,1.66525935159367,-1012.81701293953));
#164790=CARTESIAN_POINT('Ctrl Pts',(18.1253194172301,3.32956716117513E-15,
-1014.31113058659));
#164791=CARTESIAN_POINT('Ctrl Pts',(17.9710104137728,-1.66525935159367,
-1015.80524823365));
#164792=CARTESIAN_POINT('Ctrl Pts',(17.8167014103155,-3.33051870318736,
-1017.29936588071));
#164793=CARTESIAN_POINT('Ctrl Pts',(17.3590292079831,-4.93906964482095,
-1018.79348352777));
#164794=CARTESIAN_POINT('Ctrl Pts',(16.9013570056506,-6.54762058645456,
-1020.28760117483));
#164795=CARTESIAN_POINT('Ctrl Pts',(16.1559070823762,-8.04468584505497,
-1021.78171882189));
#164796=CARTESIAN_POINT('Ctrl Pts',(15.4104571591017,-9.54175110365538,
-1023.27583646895));
#164797=CARTESIAN_POINT('Ctrl Pts',(14.4026149179538,-10.8763499173728,
-1024.769954116));
#164798=CARTESIAN_POINT('Ctrl Pts',(13.3947726768058,-12.2109487310903,
-1026.26407176306));
#164799=CARTESIAN_POINT('Ctrl Pts',(12.1588589765331,-13.3376329379985,
-1027.75818941012));
#164800=CARTESIAN_POINT('Ctrl Pts',(10.9229452762603,-14.4643171449067,
-1029.25230705718));
#164801=CARTESIAN_POINT('Ctrl Pts',(9.50104767561053,-15.3447188656481,
-1030.74642470424));
#164802=CARTESIAN_POINT('Ctrl Pts',(8.07915007496071,-16.2251205863895,
-1032.2405423513));
#164803=CARTESIAN_POINT('Ctrl Pts',(6.51968959134574,-16.8292587962898,
-1033.73465999836));
#164804=CARTESIAN_POINT('Ctrl Pts',(4.96022910773078,-17.4333970061901,
-1035.22877764542));
#164805=CARTESIAN_POINT('Ctrl Pts',(3.31631129755346,-17.7406985030951,
-1036.72289529247));
#164806=CARTESIAN_POINT('Ctrl Pts',(1.67239348737615,-18.048,-1038.21701293953));
#164807=CARTESIAN_POINT('Ctrl Pts',(0.,-18.048,-1039.71113058659));
#164808=CARTESIAN_POINT('Ctrl Pts',(-1.67239348737615,-18.048,-1041.20524823365));
#164809=CARTESIAN_POINT('Ctrl Pts',(-3.31631129755346,-17.7406985030951,
-1042.69936588071));
#164810=CARTESIAN_POINT('Ctrl Pts',(-4.96022910773077,-17.4333970061901,
-1044.19348352777));
#164811=CARTESIAN_POINT('Ctrl Pts',(-6.51968959134574,-16.8292587962898,
-1045.68760117483));
#164812=CARTESIAN_POINT('Ctrl Pts',(-8.07915007496071,-16.2251205863895,
-1047.18171882189));
#164813=CARTESIAN_POINT('Ctrl Pts',(-9.50104767561052,-15.3447188656481,
-1048.67583646894));
#164814=CARTESIAN_POINT('Ctrl Pts',(-10.9229452762603,-14.4643171449067,
-1050.169954116));
#164815=CARTESIAN_POINT('Ctrl Pts',(-12.1588589765331,-13.3376329379985,
-1051.66407176306));
#164816=CARTESIAN_POINT('Ctrl Pts',(-13.3947726768058,-12.2109487310903,
-1053.15818941012));
#164817=CARTESIAN_POINT('Ctrl Pts',(-14.4026149179538,-10.8763499173728,
-1054.65230705718));
#164818=CARTESIAN_POINT('Ctrl Pts',(-15.4104571591017,-9.54175110365538,
-1056.14642470424));
#164819=CARTESIAN_POINT('Ctrl Pts',(-16.1559070823762,-8.04468584505497,
-1057.6405423513));
#164820=CARTESIAN_POINT('Ctrl Pts',(-16.9013570056506,-6.54762058645456,
-1059.13465999836));
#164821=CARTESIAN_POINT('Ctrl Pts',(-17.3590292079831,-4.93906964482095,
-1060.62877764542));
#164822=CARTESIAN_POINT('Ctrl Pts',(-17.8167014103155,-3.33051870318735,
-1062.12289529247));
#164823=CARTESIAN_POINT('Ctrl Pts',(-17.9710104137728,-1.66525935159368,
-1063.61701293953));
#164824=CARTESIAN_POINT('Ctrl Pts',(-18.1253194172301,-1.10985572039171E-15,
-1065.11113058659));
#164825=CARTESIAN_POINT('Ctrl Pts',(-17.9710104137728,1.66525935159367,
-1066.60524823365));
#164826=CARTESIAN_POINT('Ctrl Pts',(-17.8167014103155,3.33051870318735,
-1068.09936588071));
#164827=CARTESIAN_POINT('Ctrl Pts',(-17.3590292079831,4.93906964482096,
-1069.59348352777));
#164828=CARTESIAN_POINT('Ctrl Pts',(-16.9013570056506,6.54762058645456,
-1071.08760117483));
#164829=CARTESIAN_POINT('Ctrl Pts',(-16.1559070823762,8.04468584505497,
-1072.58171882189));
#164830=CARTESIAN_POINT('Ctrl Pts',(-15.4104571591017,9.54175110365538,
-1074.07583646895));
#164831=CARTESIAN_POINT('Ctrl Pts',(-14.4026149179538,10.8763499173728,
-1075.569954116));
#164832=CARTESIAN_POINT('Ctrl Pts',(-13.3947726768058,12.2109487310903,
-1077.06407176306));
#164833=CARTESIAN_POINT('Ctrl Pts',(-12.1588589765331,13.3376329379985,
-1078.55818941012));
#164834=CARTESIAN_POINT('Ctrl Pts',(-10.9229452762603,14.4643171449067,
-1080.05230705718));
#164835=CARTESIAN_POINT('Ctrl Pts',(-9.50104767561052,15.3447188656481,
-1081.54642470424));
#164836=CARTESIAN_POINT('Ctrl Pts',(-8.07915007496071,16.2251205863895,
-1083.0405423513));
#164837=CARTESIAN_POINT('Ctrl Pts',(-6.51968959134574,16.8292587962898,
-1084.53465999836));
#164838=CARTESIAN_POINT('Ctrl Pts',(-4.96022910773078,17.4333970061901,
-1086.02877764542));
#164839=CARTESIAN_POINT('Ctrl Pts',(-3.31631129755346,17.7406985030951,
-1087.52289529247));
#164840=CARTESIAN_POINT('Ctrl Pts',(-1.67239348737615,18.048,-1089.01701293953));
#164841=CARTESIAN_POINT('Ctrl Pts',(-2.21024254310115E-15,18.048,-1090.51113058659));
#164842=CARTESIAN_POINT('Ctrl Pts',(1.67239348737616,18.048,-1092.00524823365));
#164843=CARTESIAN_POINT('Ctrl Pts',(3.31631129755346,17.7406985030951,-1093.49936588071));
#164844=CARTESIAN_POINT('Ctrl Pts',(4.96022910773077,17.4333970061901,-1094.99348352777));
#164845=CARTESIAN_POINT('Ctrl Pts',(6.51968959134575,16.8292587962898,-1096.48760117483));
#164846=CARTESIAN_POINT('Ctrl Pts',(8.07915007496071,16.2251205863895,-1097.98171882189));
#164847=CARTESIAN_POINT('Ctrl Pts',(9.50104767561053,15.3447188656481,-1099.47583646895));
#164848=CARTESIAN_POINT('Ctrl Pts',(10.9229452762603,14.4643171449067,-1100.969954116));
#164849=CARTESIAN_POINT('Ctrl Pts',(12.1588589765331,13.3376329379985,-1102.46407176306));
#164850=CARTESIAN_POINT('Ctrl Pts',(13.3947726768058,12.2109487310903,-1103.95818941012));
#164851=CARTESIAN_POINT('Ctrl Pts',(14.4026149179538,10.8763499173728,-1105.45230705718));
#164852=CARTESIAN_POINT('Ctrl Pts',(15.4104571591017,9.54175110365538,-1106.94642470424));
#164853=CARTESIAN_POINT('Ctrl Pts',(16.1559070823762,8.04468584505496,-1108.4405423513));
#164854=CARTESIAN_POINT('Ctrl Pts',(16.9013570056506,6.54762058645456,-1109.93465999836));
#164855=CARTESIAN_POINT('Ctrl Pts',(17.3590292079831,4.93906964482096,-1111.42877764542));
#164856=CARTESIAN_POINT('Ctrl Pts',(17.8167014103155,3.33051870318735,-1112.92289529247));
#164857=CARTESIAN_POINT('Ctrl Pts',(17.9710104137728,1.66525935159367,-1114.41701293953));
#164858=CARTESIAN_POINT('Ctrl Pts',(18.1253194172301,3.32956716117513E-15,
-1115.91113058659));
#164859=CARTESIAN_POINT('Ctrl Pts',(17.9710104137728,-1.66525935159367,
-1117.40524823365));
#164860=CARTESIAN_POINT('Ctrl Pts',(17.8167014103155,-3.33051870318736,
-1118.89936588071));
#164861=CARTESIAN_POINT('Ctrl Pts',(17.3590292079831,-4.93906964482095,
-1120.39348352777));
#164862=CARTESIAN_POINT('Ctrl Pts',(16.9013570056506,-6.54762058645456,
-1121.88760117483));
#164863=CARTESIAN_POINT('Ctrl Pts',(16.1559070823762,-8.04468584505497,
-1123.38171882189));
#164864=CARTESIAN_POINT('Ctrl Pts',(15.4104571591017,-9.54175110365538,
-1124.87583646895));
#164865=CARTESIAN_POINT('Ctrl Pts',(14.4026149179538,-10.8763499173728,
-1126.369954116));
#164866=CARTESIAN_POINT('Ctrl Pts',(13.3947726768058,-12.2109487310903,
-1127.86407176306));
#164867=CARTESIAN_POINT('Ctrl Pts',(12.1588589765331,-13.3376329379985,
-1129.35818941012));
#164868=CARTESIAN_POINT('Ctrl Pts',(10.9229452762603,-14.4643171449067,
-1130.85230705718));
#164869=CARTESIAN_POINT('Ctrl Pts',(9.50104767561053,-15.3447188656481,
-1132.34642470424));
#164870=CARTESIAN_POINT('Ctrl Pts',(8.07915007496071,-16.2251205863895,
-1133.8405423513));
#164871=CARTESIAN_POINT('Ctrl Pts',(6.51968959134574,-16.8292587962898,
-1135.33465999836));
#164872=CARTESIAN_POINT('Ctrl Pts',(4.96022910773078,-17.4333970061901,
-1136.82877764542));
#164873=CARTESIAN_POINT('Ctrl Pts',(3.31631129755346,-17.7406985030951,
-1138.32289529247));
#164874=CARTESIAN_POINT('Ctrl Pts',(1.67239348737615,-18.048,-1139.81701293953));
#164875=CARTESIAN_POINT('Ctrl Pts',(0.,-18.048,-1141.31113058659));
#164876=CARTESIAN_POINT('Ctrl Pts',(-1.67239348737615,-18.048,-1142.80524823365));
#164877=CARTESIAN_POINT('Ctrl Pts',(-3.31631129755346,-17.7406985030951,
-1144.29936588071));
#164878=CARTESIAN_POINT('Ctrl Pts',(-4.96022910773077,-17.4333970061901,
-1145.79348352777));
#164879=CARTESIAN_POINT('Ctrl Pts',(-6.51968959134574,-16.8292587962898,
-1147.28760117483));
#164880=CARTESIAN_POINT('Ctrl Pts',(-8.07915007496071,-16.2251205863895,
-1148.78171882189));
#164881=CARTESIAN_POINT('Ctrl Pts',(-9.50104767561052,-15.3447188656481,
-1150.27583646895));
#164882=CARTESIAN_POINT('Ctrl Pts',(-10.9229452762603,-14.4643171449067,
-1151.769954116));
#164883=CARTESIAN_POINT('Ctrl Pts',(-12.1588589765331,-13.3376329379985,
-1153.26407176306));
#164884=CARTESIAN_POINT('Ctrl Pts',(-13.3947726768058,-12.2109487310903,
-1154.75818941012));
#164885=CARTESIAN_POINT('Ctrl Pts',(-14.4026149179538,-10.8763499173728,
-1156.25230705718));
#164886=CARTESIAN_POINT('Ctrl Pts',(-15.4104571591017,-9.54175110365538,
-1157.74642470424));
#164887=CARTESIAN_POINT('Ctrl Pts',(-16.1559070823762,-8.04468584505497,
-1159.2405423513));
#164888=CARTESIAN_POINT('Ctrl Pts',(-16.9013570056506,-6.54762058645456,
-1160.73465999836));
#164889=CARTESIAN_POINT('Ctrl Pts',(-17.3590292079831,-4.93906964482095,
-1162.22877764542));
#164890=CARTESIAN_POINT('Ctrl Pts',(-17.8167014103155,-3.33051870318735,
-1163.72289529247));
#164891=CARTESIAN_POINT('Ctrl Pts',(-17.9710104137728,-1.66525935159368,
-1165.21701293953));
#164892=CARTESIAN_POINT('Ctrl Pts',(-18.1253194172301,-1.10985572039171E-15,
-1166.71113058659));
#164893=CARTESIAN_POINT('Ctrl Pts',(-17.9710104137728,1.66525935159367,
-1168.20524823365));
#164894=CARTESIAN_POINT('Ctrl Pts',(-17.8167014103155,3.33051870318735,
-1169.69936588071));
#164895=CARTESIAN_POINT('Ctrl Pts',(-17.3590292079831,4.93906964482096,
-1171.19348352777));
#164896=CARTESIAN_POINT('Ctrl Pts',(-16.9013570056506,6.54762058645456,
-1172.68760117483));
#164897=CARTESIAN_POINT('Ctrl Pts',(-16.1559070823762,8.04468584505497,
-1174.18171882189));
#164898=CARTESIAN_POINT('Ctrl Pts',(-15.4104571591017,9.54175110365538,
-1175.67583646895));
#164899=CARTESIAN_POINT('Ctrl Pts',(-14.4026149179538,10.8763499173728,
-1177.169954116));
#164900=CARTESIAN_POINT('Ctrl Pts',(-13.3947726768058,12.2109487310903,
-1178.66407176306));
#164901=CARTESIAN_POINT('Ctrl Pts',(-12.1588589765331,13.3376329379985,
-1180.15818941012));
#164902=CARTESIAN_POINT('Ctrl Pts',(-10.9229452762603,14.4643171449067,
-1181.65230705718));
#164903=CARTESIAN_POINT('Ctrl Pts',(-9.50104767561052,15.3447188656481,
-1183.14642470424));
#164904=CARTESIAN_POINT('Ctrl Pts',(-8.07915007496071,16.2251205863895,
-1184.6405423513));
#164905=CARTESIAN_POINT('Ctrl Pts',(-6.51968959134574,16.8292587962898,
-1186.13465999836));
#164906=CARTESIAN_POINT('Ctrl Pts',(-4.96022910773078,17.4333970061901,
-1187.62877764542));
#164907=CARTESIAN_POINT('Ctrl Pts',(-3.31631129755346,17.7406985030951,
-1189.12289529247));
#164908=CARTESIAN_POINT('Ctrl Pts',(-1.67239348737615,18.048,-1190.61701293953));
#164909=CARTESIAN_POINT('Ctrl Pts',(-2.21024254310115E-15,18.048,-1192.11113058659));
#164910=CARTESIAN_POINT('Ctrl Pts',(1.67239348737616,18.048,-1193.60524823365));
#164911=CARTESIAN_POINT('Ctrl Pts',(3.31631129755346,17.7406985030951,-1195.09936588071));
#164912=CARTESIAN_POINT('Ctrl Pts',(4.96022910773077,17.4333970061901,-1196.59348352777));
#164913=CARTESIAN_POINT('Ctrl Pts',(6.51968959134575,16.8292587962898,-1198.08760117483));
#164914=CARTESIAN_POINT('Ctrl Pts',(8.07915007496071,16.2251205863895,-1199.58171882189));
#164915=CARTESIAN_POINT('Ctrl Pts',(9.50104767561053,15.3447188656481,-1201.07583646894));
#164916=CARTESIAN_POINT('Ctrl Pts',(10.9229452762603,14.4643171449067,-1202.569954116));
#164917=CARTESIAN_POINT('Ctrl Pts',(12.1588589765331,13.3376329379985,-1204.06407176306));
#164918=CARTESIAN_POINT('Ctrl Pts',(13.3947726768058,12.2109487310903,-1205.55818941012));
#164919=CARTESIAN_POINT('Ctrl Pts',(14.4026149179538,10.8763499173728,-1207.05230705718));
#164920=CARTESIAN_POINT('Ctrl Pts',(15.4104571591017,9.54175110365538,-1208.54642470424));
#164921=CARTESIAN_POINT('Ctrl Pts',(16.1559070823762,8.04468584505496,-1210.0405423513));
#164922=CARTESIAN_POINT('Ctrl Pts',(16.9013570056506,6.54762058645456,-1211.53465999836));
#164923=CARTESIAN_POINT('Ctrl Pts',(17.3590292079831,4.93906964482096,-1213.02877764542));
#164924=CARTESIAN_POINT('Ctrl Pts',(17.8167014103155,3.33051870318735,-1214.52289529247));
#164925=CARTESIAN_POINT('Ctrl Pts',(17.9710104137728,1.66525935159367,-1216.01701293953));
#164926=CARTESIAN_POINT('Ctrl Pts',(18.1253194172301,3.32956716117513E-15,
-1217.51113058659));
#164927=CARTESIAN_POINT('Ctrl Pts',(17.9710104137728,-1.66525935159367,
-1219.00524823365));
#164928=CARTESIAN_POINT('Ctrl Pts',(17.8167014103155,-3.33051870318736,
-1220.49936588071));
#164929=CARTESIAN_POINT('Ctrl Pts',(17.3590292079831,-4.93906964482095,
-1221.99348352777));
#164930=CARTESIAN_POINT('Ctrl Pts',(16.9013570056506,-6.54762058645456,
-1223.48760117483));
#164931=CARTESIAN_POINT('Ctrl Pts',(16.1559070823762,-8.04468584505497,
-1224.98171882189));
#164932=CARTESIAN_POINT('Ctrl Pts',(15.4104571591017,-9.54175110365538,
-1226.47583646895));
#164933=CARTESIAN_POINT('Ctrl Pts',(14.4026149179538,-10.8763499173728,
-1227.969954116));
#164934=CARTESIAN_POINT('Ctrl Pts',(13.3947726768058,-12.2109487310903,
-1229.46407176306));
#164935=CARTESIAN_POINT('Ctrl Pts',(12.1588589765331,-13.3376329379985,
-1230.95818941012));
#164936=CARTESIAN_POINT('Ctrl Pts',(10.9229452762603,-14.4643171449067,
-1232.45230705718));
#164937=CARTESIAN_POINT('Ctrl Pts',(9.50104767561053,-15.3447188656481,
-1233.94642470424));
#164938=CARTESIAN_POINT('Ctrl Pts',(8.07915007496071,-16.2251205863895,
-1235.4405423513));
#164939=CARTESIAN_POINT('Ctrl Pts',(6.51968959134574,-16.8292587962898,
-1236.93465999836));
#164940=CARTESIAN_POINT('Ctrl Pts',(4.96022910773078,-17.4333970061901,
-1238.42877764542));
#164941=CARTESIAN_POINT('Ctrl Pts',(3.31631129755346,-17.7406985030951,
-1239.92289529247));
#164942=CARTESIAN_POINT('Ctrl Pts',(1.67239348737615,-18.048,-1241.41701293953));
#164943=CARTESIAN_POINT('Ctrl Pts',(0.,-18.048,-1242.91113058659));
#164944=CARTESIAN_POINT('Ctrl Pts',(-1.67239348737615,-18.048,-1244.40524823365));
#164945=CARTESIAN_POINT('Ctrl Pts',(-3.31631129755346,-17.7406985030951,
-1245.89936588071));
#164946=CARTESIAN_POINT('Ctrl Pts',(-4.96022910773077,-17.4333970061901,
-1247.39348352777));
#164947=CARTESIAN_POINT('Ctrl Pts',(-6.51968959134574,-16.8292587962898,
-1248.88760117483));
#164948=CARTESIAN_POINT('Ctrl Pts',(-8.07915007496071,-16.2251205863895,
-1250.38171882189));
#164949=CARTESIAN_POINT('Ctrl Pts',(-9.50104767561052,-15.3447188656481,
-1251.87583646895));
#164950=CARTESIAN_POINT('Ctrl Pts',(-10.9229452762603,-14.4643171449067,
-1253.369954116));
#164951=CARTESIAN_POINT('Ctrl Pts',(-12.1588589765331,-13.3376329379985,
-1254.86407176306));
#164952=CARTESIAN_POINT('Ctrl Pts',(-13.3947726768058,-12.2109487310903,
-1256.35818941012));
#164953=CARTESIAN_POINT('Ctrl Pts',(-14.4026149179538,-10.8763499173728,
-1257.85230705718));
#164954=CARTESIAN_POINT('Ctrl Pts',(-15.4104571591017,-9.54175110365538,
-1259.34642470424));
#164955=CARTESIAN_POINT('Ctrl Pts',(-16.1559070823762,-8.04468584505497,
-1260.8405423513));
#164956=CARTESIAN_POINT('Ctrl Pts',(-16.9013570056506,-6.54762058645456,
-1262.33465999836));
#164957=CARTESIAN_POINT('Ctrl Pts',(-17.3590292079831,-4.93906964482095,
-1263.82877764542));
#164958=CARTESIAN_POINT('Ctrl Pts',(-17.8167014103155,-3.33051870318735,
-1265.32289529247));
#164959=CARTESIAN_POINT('Ctrl Pts',(-17.9710104137728,-1.66525935159368,
-1266.81701293953));
#164960=CARTESIAN_POINT('Ctrl Pts',(-18.1253194172301,-1.10985572039171E-15,
-1268.31113058659));
#164961=CARTESIAN_POINT('Ctrl Pts',(-17.9710104137728,1.66525935159367,
-1269.80524823365));
#164962=CARTESIAN_POINT('Ctrl Pts',(-17.8167014103155,3.33051870318735,
-1271.29936588071));
#164963=CARTESIAN_POINT('Ctrl Pts',(-17.3590292079831,4.93906964482096,
-1272.79348352777));
#164964=CARTESIAN_POINT('Ctrl Pts',(-16.9013570056506,6.54762058645456,
-1274.28760117483));
#164965=CARTESIAN_POINT('Ctrl Pts',(-16.1559070823762,8.04468584505497,
-1275.78171882189));
#164966=CARTESIAN_POINT('Ctrl Pts',(-15.4104571591017,9.54175110365538,
-1277.27583646895));
#164967=CARTESIAN_POINT('Ctrl Pts',(-14.4026149179538,10.8763499173728,
-1278.769954116));
#164968=CARTESIAN_POINT('Ctrl Pts',(-13.3947726768058,12.2109487310903,
-1280.26407176306));
#164969=CARTESIAN_POINT('Ctrl Pts',(-12.1588589765331,13.3376329379985,
-1281.75818941012));
#164970=CARTESIAN_POINT('Ctrl Pts',(-10.9229452762603,14.4643171449067,
-1283.25230705718));
#164971=CARTESIAN_POINT('Ctrl Pts',(-9.50104767561052,15.3447188656481,
-1284.74642470424));
#164972=CARTESIAN_POINT('Ctrl Pts',(-8.07915007496071,16.2251205863895,
-1286.2405423513));
#164973=CARTESIAN_POINT('Ctrl Pts',(-6.51968959134574,16.8292587962898,
-1287.73465999836));
#164974=CARTESIAN_POINT('Ctrl Pts',(-4.96022910773078,17.4333970061901,
-1289.22877764542));
#164975=CARTESIAN_POINT('Ctrl Pts',(-3.31631129755346,17.7406985030951,
-1290.72289529247));
#164976=CARTESIAN_POINT('Ctrl Pts',(-1.67239348737615,18.048,-1292.21701293953));
#164977=CARTESIAN_POINT('Ctrl Pts',(-2.21024254310115E-15,18.048,-1293.71113058659));
#164978=CARTESIAN_POINT('Ctrl Pts',(1.67239348737616,18.048,-1295.20524823365));
#164979=CARTESIAN_POINT('Ctrl Pts',(3.31631129755346,17.7406985030951,-1296.69936588071));
#164980=CARTESIAN_POINT('Ctrl Pts',(4.96022910773077,17.4333970061901,-1298.19348352777));
#164981=CARTESIAN_POINT('Ctrl Pts',(6.51968959134575,16.8292587962898,-1299.68760117483));
#164982=CARTESIAN_POINT('Ctrl Pts',(8.07915007496071,16.2251205863895,-1301.18171882189));
#164983=CARTESIAN_POINT('Ctrl Pts',(9.50104767561053,15.3447188656481,-1302.67583646895));
#164984=CARTESIAN_POINT('Ctrl Pts',(10.9229452762603,14.4643171449067,-1304.169954116));
#164985=CARTESIAN_POINT('Ctrl Pts',(12.1588589765331,13.3376329379985,-1305.66407176306));
#164986=CARTESIAN_POINT('Ctrl Pts',(13.3947726768058,12.2109487310903,-1307.15818941012));
#164987=CARTESIAN_POINT('Ctrl Pts',(14.4026149179538,10.8763499173728,-1308.65230705718));
#164988=CARTESIAN_POINT('Ctrl Pts',(15.4104571591017,9.54175110365538,-1310.14642470424));
#164989=CARTESIAN_POINT('Ctrl Pts',(16.1559070823762,8.04468584505496,-1311.6405423513));
#164990=CARTESIAN_POINT('Ctrl Pts',(16.9013570056506,6.54762058645456,-1313.13465999836));
#164991=CARTESIAN_POINT('Ctrl Pts',(17.3590292079831,4.93906964482096,-1314.62877764542));
#164992=CARTESIAN_POINT('Ctrl Pts',(17.8167014103155,3.33051870318735,-1316.12289529247));
#164993=CARTESIAN_POINT('Ctrl Pts',(17.9710104137728,1.66525935159367,-1317.61701293953));
#164994=CARTESIAN_POINT('Ctrl Pts',(18.1253194172301,3.32956716117513E-15,
-1319.11113058659));
#164995=CARTESIAN_POINT('Ctrl Pts',(17.9710104137728,-1.66525935159367,
-1320.60524823365));
#164996=CARTESIAN_POINT('Ctrl Pts',(17.8167014103155,-3.33051870318736,
-1322.09936588071));
#164997=CARTESIAN_POINT('Ctrl Pts',(17.3590292079831,-4.93906964482095,
-1323.59348352777));
#164998=CARTESIAN_POINT('Ctrl Pts',(16.9013570056506,-6.54762058645456,
-1325.08760117483));
#164999=CARTESIAN_POINT('Ctrl Pts',(16.1559070823762,-8.04468584505497,
-1326.58171882189));
#165000=CARTESIAN_POINT('Ctrl Pts',(15.4104571591017,-9.54175110365538,
-1328.07583646895));
#165001=CARTESIAN_POINT('Ctrl Pts',(14.4026149179538,-10.8763499173728,
-1329.569954116));
#165002=CARTESIAN_POINT('Ctrl Pts',(13.3947726768058,-12.2109487310903,
-1331.06407176306));
#165003=CARTESIAN_POINT('Ctrl Pts',(12.1588589765331,-13.3376329379985,
-1332.55818941012));
#165004=CARTESIAN_POINT('Ctrl Pts',(10.9229452762603,-14.4643171449067,
-1334.05230705718));
#165005=CARTESIAN_POINT('Ctrl Pts',(9.50104767561053,-15.3447188656481,
-1335.54642470424));
#165006=CARTESIAN_POINT('Ctrl Pts',(8.07915007496071,-16.2251205863895,
-1337.0405423513));
#165007=CARTESIAN_POINT('Ctrl Pts',(6.51968959134574,-16.8292587962898,
-1338.53465999836));
#165008=CARTESIAN_POINT('Ctrl Pts',(4.96022910773078,-17.4333970061901,
-1340.02877764542));
#165009=CARTESIAN_POINT('Ctrl Pts',(3.31631129755346,-17.7406985030951,
-1341.52289529247));
#165010=CARTESIAN_POINT('Ctrl Pts',(1.67239348737615,-18.048,-1343.01701293953));
#165011=CARTESIAN_POINT('Ctrl Pts',(0.,-18.048,-1344.51113058659));
#165012=CARTESIAN_POINT('Ctrl Pts',(-1.67239348737615,-18.048,-1346.00524823365));
#165013=CARTESIAN_POINT('Ctrl Pts',(-3.31631129755346,-17.7406985030951,
-1347.49936588071));
#165014=CARTESIAN_POINT('Ctrl Pts',(-4.96022910773077,-17.4333970061901,
-1348.99348352777));
#165015=CARTESIAN_POINT('Ctrl Pts',(-6.51968959134574,-16.8292587962898,
-1350.48760117483));
#165016=CARTESIAN_POINT('Ctrl Pts',(-8.07915007496071,-16.2251205863895,
-1351.98171882189));
#165017=CARTESIAN_POINT('Ctrl Pts',(-9.50104767561052,-15.3447188656481,
-1353.47583646895));
#165018=CARTESIAN_POINT('Ctrl Pts',(-10.9229452762603,-14.4643171449067,
-1354.969954116));
#165019=CARTESIAN_POINT('Ctrl Pts',(-12.1588589765331,-13.3376329379985,
-1356.46407176306));
#165020=CARTESIAN_POINT('Ctrl Pts',(-13.3947726768058,-12.2109487310903,
-1357.95818941012));
#165021=CARTESIAN_POINT('Ctrl Pts',(-14.4026149179538,-10.8763499173728,
-1359.45230705718));
#165022=CARTESIAN_POINT('Ctrl Pts',(-15.4104571591017,-9.54175110365538,
-1360.94642470424));
#165023=CARTESIAN_POINT('Ctrl Pts',(-16.1559070823762,-8.04468584505497,
-1362.4405423513));
#165024=CARTESIAN_POINT('Ctrl Pts',(-16.9013570056506,-6.54762058645456,
-1363.93465999836));
#165025=CARTESIAN_POINT('Ctrl Pts',(-17.3590292079831,-4.93906964482095,
-1365.42877764542));
#165026=CARTESIAN_POINT('Ctrl Pts',(-17.8167014103155,-3.33051870318735,
-1366.92289529248));
#165027=CARTESIAN_POINT('Ctrl Pts',(-17.9710104137728,-1.66525935159368,
-1368.41701293953));
#165028=CARTESIAN_POINT('Ctrl Pts',(-18.1253194172301,-1.10985572039171E-15,
-1369.91113058659));
#165029=CARTESIAN_POINT('Ctrl Pts',(-17.9710104137728,1.66525935159367,
-1371.40524823365));
#165030=CARTESIAN_POINT('Ctrl Pts',(-17.8167014103155,3.33051870318735,
-1372.89936588071));
#165031=CARTESIAN_POINT('Ctrl Pts',(-17.3590292079831,4.93906964482096,
-1374.39348352777));
#165032=CARTESIAN_POINT('Ctrl Pts',(-16.9013570056506,6.54762058645456,
-1375.88760117483));
#165033=CARTESIAN_POINT('Ctrl Pts',(-16.1559070823762,8.04468584505497,
-1377.38171882189));
#165034=CARTESIAN_POINT('Ctrl Pts',(-15.4104571591017,9.54175110365538,
-1378.87583646895));
#165035=CARTESIAN_POINT('Ctrl Pts',(-14.4026149179538,10.8763499173728,
-1380.369954116));
#165036=CARTESIAN_POINT('Ctrl Pts',(-13.3947726768058,12.2109487310903,
-1381.86407176306));
#165037=CARTESIAN_POINT('Ctrl Pts',(-12.1588589765331,13.3376329379985,
-1383.35818941012));
#165038=CARTESIAN_POINT('Ctrl Pts',(-10.9229452762603,14.4643171449067,
-1384.85230705718));
#165039=CARTESIAN_POINT('Ctrl Pts',(-9.50104767561052,15.3447188656481,
-1386.34642470424));
#165040=CARTESIAN_POINT('Ctrl Pts',(-8.07915007496071,16.2251205863895,
-1387.8405423513));
#165041=CARTESIAN_POINT('Ctrl Pts',(-6.51968959134574,16.8292587962898,
-1389.33465999836));
#165042=CARTESIAN_POINT('Ctrl Pts',(-4.96022910773078,17.4333970061901,
-1390.82877764542));
#165043=CARTESIAN_POINT('Ctrl Pts',(-3.31631129755346,17.7406985030951,
-1392.32289529247));
#165044=CARTESIAN_POINT('Ctrl Pts',(-1.67239348737615,18.048,-1393.81701293953));
#165045=CARTESIAN_POINT('Ctrl Pts',(-2.21024254310115E-15,18.048,-1395.31113058659));
#165046=CARTESIAN_POINT('Ctrl Pts',(1.67239348737616,18.048,-1396.80524823365));
#165047=CARTESIAN_POINT('Ctrl Pts',(3.31631129755346,17.7406985030951,-1398.29936588071));
#165048=CARTESIAN_POINT('Ctrl Pts',(4.96022910773077,17.4333970061901,-1399.79348352777));
#165049=CARTESIAN_POINT('Ctrl Pts',(6.51968959134575,16.8292587962898,-1401.28760117483));
#165050=CARTESIAN_POINT('Ctrl Pts',(8.07915007496071,16.2251205863895,-1402.78171882189));
#165051=CARTESIAN_POINT('Ctrl Pts',(9.50104767561053,15.3447188656481,-1404.27583646895));
#165052=CARTESIAN_POINT('Ctrl Pts',(10.9229452762603,14.4643171449067,-1405.769954116));
#165053=CARTESIAN_POINT('Ctrl Pts',(12.1588589765331,13.3376329379985,-1407.26407176306));
#165054=CARTESIAN_POINT('Ctrl Pts',(13.3947726768058,12.2109487310903,-1408.75818941012));
#165055=CARTESIAN_POINT('Ctrl Pts',(14.4026149179538,10.8763499173728,-1410.25230705718));
#165056=CARTESIAN_POINT('Ctrl Pts',(15.4104571591017,9.54175110365538,-1411.74642470424));
#165057=CARTESIAN_POINT('Ctrl Pts',(16.1559070823762,8.04468584505496,-1413.2405423513));
#165058=CARTESIAN_POINT('Ctrl Pts',(16.9013570056506,6.54762058645456,-1414.73465999836));
#165059=CARTESIAN_POINT('Ctrl Pts',(17.3590292079831,4.93906964482096,-1416.22877764542));
#165060=CARTESIAN_POINT('Ctrl Pts',(17.8167014103155,3.33051870318735,-1417.72289529247));
#165061=CARTESIAN_POINT('Ctrl Pts',(17.9710104137728,1.66525935159367,-1419.21701293953));
#165062=CARTESIAN_POINT('Ctrl Pts',(18.1253194172301,3.32956716117513E-15,
-1420.71113058659));
#165063=CARTESIAN_POINT('Ctrl Pts',(17.9710104137728,-1.66525935159367,
-1422.20524823365));
#165064=CARTESIAN_POINT('Ctrl Pts',(17.8167014103155,-3.33051870318736,
-1423.69936588071));
#165065=CARTESIAN_POINT('Ctrl Pts',(17.3590292079831,-4.93906964482095,
-1425.19348352777));
#165066=CARTESIAN_POINT('Ctrl Pts',(16.9013570056506,-6.54762058645456,
-1426.68760117483));
#165067=CARTESIAN_POINT('Ctrl Pts',(16.1559070823762,-8.04468584505497,
-1428.18171882189));
#165068=CARTESIAN_POINT('Ctrl Pts',(15.4104571591017,-9.54175110365538,
-1429.67583646895));
#165069=CARTESIAN_POINT('Ctrl Pts',(14.4026149179538,-10.8763499173728,
-1431.169954116));
#165070=CARTESIAN_POINT('Ctrl Pts',(13.3947726768058,-12.2109487310903,
-1432.66407176306));
#165071=CARTESIAN_POINT('Ctrl Pts',(12.1588589765331,-13.3376329379985,
-1434.15818941012));
#165072=CARTESIAN_POINT('Ctrl Pts',(10.9229452762603,-14.4643171449067,
-1435.65230705718));
#165073=CARTESIAN_POINT('Ctrl Pts',(9.50104767561053,-15.3447188656481,
-1437.14642470424));
#165074=CARTESIAN_POINT('Ctrl Pts',(8.07915007496071,-16.2251205863895,
-1438.6405423513));
#165075=CARTESIAN_POINT('Ctrl Pts',(6.51968959134574,-16.8292587962898,
-1440.13465999836));
#165076=CARTESIAN_POINT('Ctrl Pts',(4.96022910773078,-17.4333970061901,
-1441.62877764542));
#165077=CARTESIAN_POINT('Ctrl Pts',(3.31631129755346,-17.7406985030951,
-1443.12289529247));
#165078=CARTESIAN_POINT('Ctrl Pts',(1.67239348737615,-18.048,-1444.61701293953));
#165079=CARTESIAN_POINT('Ctrl Pts',(0.,-18.048,-1446.11113058659));
#165080=CARTESIAN_POINT('Ctrl Pts',(-1.67239348737615,-18.048,-1447.60524823365));
#165081=CARTESIAN_POINT('Ctrl Pts',(-3.31631129755346,-17.7406985030951,
-1449.09936588071));
#165082=CARTESIAN_POINT('Ctrl Pts',(-4.96022910773077,-17.4333970061901,
-1450.59348352777));
#165083=CARTESIAN_POINT('Ctrl Pts',(-6.51968959134574,-16.8292587962898,
-1452.08760117483));
#165084=CARTESIAN_POINT('Ctrl Pts',(-8.07915007496071,-16.2251205863895,
-1453.58171882189));
#165085=CARTESIAN_POINT('Ctrl Pts',(-9.50104767561052,-15.3447188656481,
-1455.07583646895));
#165086=CARTESIAN_POINT('Ctrl Pts',(-10.9229452762603,-14.4643171449067,
-1456.569954116));
#165087=CARTESIAN_POINT('Ctrl Pts',(-12.1588589765331,-13.3376329379985,
-1458.06407176306));
#165088=CARTESIAN_POINT('Ctrl Pts',(-13.3947726768058,-12.2109487310903,
-1459.55818941012));
#165089=CARTESIAN_POINT('Ctrl Pts',(-14.4026149179538,-10.8763499173728,
-1461.05230705718));
#165090=CARTESIAN_POINT('Ctrl Pts',(-15.4104571591017,-9.54175110365538,
-1462.54642470424));
#165091=CARTESIAN_POINT('Ctrl Pts',(-16.1559070823762,-8.04468584505497,
-1464.0405423513));
#165092=CARTESIAN_POINT('Ctrl Pts',(-16.9013570056506,-6.54762058645456,
-1465.53465999836));
#165093=CARTESIAN_POINT('Ctrl Pts',(-17.3590292079831,-4.93906964482095,
-1467.02877764542));
#165094=CARTESIAN_POINT('Ctrl Pts',(-17.8167014103155,-3.33051870318735,
-1468.52289529247));
#165095=CARTESIAN_POINT('Ctrl Pts',(-17.9710104137728,-1.66525935159368,
-1470.01701293953));
#165096=CARTESIAN_POINT('Ctrl Pts',(-18.1253194172301,-1.10985572039171E-15,
-1471.51113058659));
#165097=CARTESIAN_POINT('Ctrl Pts',(-17.9710104137728,1.66525935159367,
-1473.00524823365));
#165098=CARTESIAN_POINT('Ctrl Pts',(-17.8167014103155,3.33051870318735,
-1474.49936588071));
#165099=CARTESIAN_POINT('Ctrl Pts',(-17.3590292079831,4.93906964482096,
-1475.99348352777));
#165100=CARTESIAN_POINT('Ctrl Pts',(-16.9013570056506,6.54762058645456,
-1477.48760117483));
#165101=CARTESIAN_POINT('Ctrl Pts',(-16.1559070823762,8.04468584505497,
-1478.98171882189));
#165102=CARTESIAN_POINT('Ctrl Pts',(-15.4104571591017,9.54175110365538,
-1480.47583646895));
#165103=CARTESIAN_POINT('Ctrl Pts',(-14.4026149179538,10.8763499173728,
-1481.969954116));
#165104=CARTESIAN_POINT('Ctrl Pts',(-13.3947726768058,12.2109487310903,
-1483.46407176306));
#165105=CARTESIAN_POINT('Ctrl Pts',(-12.1588589765331,13.3376329379985,
-1484.95818941012));
#165106=CARTESIAN_POINT('Ctrl Pts',(-10.9229452762603,14.4643171449067,
-1486.45230705718));
#165107=CARTESIAN_POINT('Ctrl Pts',(-9.50104767561052,15.3447188656481,
-1487.94642470424));
#165108=CARTESIAN_POINT('Ctrl Pts',(-8.07915007496071,16.2251205863895,
-1489.4405423513));
#165109=CARTESIAN_POINT('Ctrl Pts',(-6.51968959134574,16.8292587962898,
-1490.93465999836));
#165110=CARTESIAN_POINT('Ctrl Pts',(-4.96022910773078,17.4333970061901,
-1492.42877764542));
#165111=CARTESIAN_POINT('Ctrl Pts',(-3.31631129755346,17.7406985030951,
-1493.92289529247));
#165112=CARTESIAN_POINT('Ctrl Pts',(-1.67239348737615,18.048,-1495.41701293953));
#165113=CARTESIAN_POINT('Ctrl Pts',(-2.21024254310115E-15,18.048,-1496.91113058659));
#165114=CARTESIAN_POINT('Ctrl Pts',(1.67239348737616,18.048,-1498.40524823365));
#165115=CARTESIAN_POINT('Ctrl Pts',(3.31631129755346,17.7406985030951,-1499.89936588071));
#165116=CARTESIAN_POINT('Ctrl Pts',(4.96022910773077,17.4333970061901,-1501.39348352777));
#165117=CARTESIAN_POINT('Ctrl Pts',(6.51968959134575,16.8292587962898,-1502.88760117483));
#165118=CARTESIAN_POINT('Ctrl Pts',(7.54128438222173,16.4334908658498,-1503.86639019913));
#165119=CARTESIAN_POINT('Ctrl Pts',(8.50750525179015,15.9170555816949,-1504.84896316329));
#165120=CARTESIAN_POINT('Ctrl Pts',(23.3054664377218,8.00769496792138,-1519.89736156162));
#165121=CARTESIAN_POINT('Ctrl Pts',(38.1034276236535,0.0983343541478931,
-1534.94575995995));
#165122=CARTESIAN_POINT('Ctrl Pts',(0.,-18.048,1500.1875));
#165123=CARTESIAN_POINT('Ctrl Pts',(-1.67239348737615,-18.048,1498.69338235294));
#165124=CARTESIAN_POINT('Ctrl Pts',(-3.31631129755346,-17.7406985030951,
1497.19926470588));
#165125=CARTESIAN_POINT('Ctrl Pts',(-4.96022910773077,-17.4333970061901,
1495.70514705882));
#165126=CARTESIAN_POINT('Ctrl Pts',(-6.51968959134574,-16.8292587962898,
1494.21102941176));
#165127=CARTESIAN_POINT('Ctrl Pts',(-8.07915007496071,-16.2251205863895,
1492.71691176471));
#165128=CARTESIAN_POINT('Ctrl Pts',(-9.50104767561052,-15.3447188656481,
1491.22279411765));
#165129=CARTESIAN_POINT('Ctrl Pts',(-10.9229452762603,-14.4643171449067,
1489.72867647059));
#165130=CARTESIAN_POINT('Ctrl Pts',(-12.1588589765331,-13.3376329379985,
1488.23455882353));
#165131=CARTESIAN_POINT('Ctrl Pts',(-13.3947726768058,-12.2109487310903,
1486.74044117647));
#165132=CARTESIAN_POINT('Ctrl Pts',(-14.4026149179538,-10.8763499173728,
1485.24632352941));
#165133=CARTESIAN_POINT('Ctrl Pts',(-15.4104571591017,-9.54175110365538,
1483.75220588235));
#165134=CARTESIAN_POINT('Ctrl Pts',(-16.1559070823762,-8.04468584505497,
1482.25808823529));
#165135=CARTESIAN_POINT('Ctrl Pts',(-16.9013570056506,-6.54762058645456,
1480.76397058824));
#165136=CARTESIAN_POINT('Ctrl Pts',(-17.3590292079831,-4.93906964482095,
1479.26985294118));
#165137=CARTESIAN_POINT('Ctrl Pts',(-17.8167014103155,-3.33051870318735,
1477.77573529412));
#165138=CARTESIAN_POINT('Ctrl Pts',(-17.9710104137728,-1.66525935159368,
1476.28161764706));
#165139=CARTESIAN_POINT('Ctrl Pts',(-18.1253194172301,-1.10985572039171E-15,
1474.7875));
#165140=CARTESIAN_POINT('Ctrl Pts',(-17.9710104137728,1.66525935159367,
1473.29338235294));
#165141=CARTESIAN_POINT('Ctrl Pts',(-17.8167014103155,3.33051870318735,
1471.79926470588));
#165142=CARTESIAN_POINT('Ctrl Pts',(-17.3590292079831,4.93906964482096,
1470.30514705882));
#165143=CARTESIAN_POINT('Ctrl Pts',(-16.9013570056506,6.54762058645456,
1468.81102941177));
#165144=CARTESIAN_POINT('Ctrl Pts',(-16.1559070823762,8.04468584505497,
1467.31691176471));
#165145=CARTESIAN_POINT('Ctrl Pts',(-15.4104571591017,9.54175110365538,
1465.82279411765));
#165146=CARTESIAN_POINT('Ctrl Pts',(-14.4026149179538,10.8763499173728,
1464.32867647059));
#165147=CARTESIAN_POINT('Ctrl Pts',(-13.3947726768058,12.2109487310903,
1462.83455882353));
#165148=CARTESIAN_POINT('Ctrl Pts',(-12.1588589765331,13.3376329379985,
1461.34044117647));
#165149=CARTESIAN_POINT('Ctrl Pts',(-10.9229452762603,14.4643171449067,
1459.84632352941));
#165150=CARTESIAN_POINT('Ctrl Pts',(-9.50104767561052,15.3447188656481,
1458.35220588235));
#165151=CARTESIAN_POINT('Ctrl Pts',(-8.07915007496071,16.2251205863895,
1456.85808823529));
#165152=CARTESIAN_POINT('Ctrl Pts',(-6.51968959134574,16.8292587962898,
1455.36397058824));
#165153=CARTESIAN_POINT('Ctrl Pts',(-4.96022910773078,17.4333970061901,
1453.86985294118));
#165154=CARTESIAN_POINT('Ctrl Pts',(-3.31631129755346,17.7406985030951,
1452.37573529412));
#165155=CARTESIAN_POINT('Ctrl Pts',(-1.67239348737615,18.048,1450.88161764706));
#165156=CARTESIAN_POINT('Ctrl Pts',(-2.21024254310115E-15,18.048,1449.3875));
#165157=CARTESIAN_POINT('Ctrl Pts',(1.67239348737616,18.048,1447.89338235294));
#165158=CARTESIAN_POINT('Ctrl Pts',(3.31631129755346,17.7406985030951,1446.39926470588));
#165159=CARTESIAN_POINT('Ctrl Pts',(4.96022910773077,17.4333970061901,1444.90514705882));
#165160=CARTESIAN_POINT('Ctrl Pts',(6.51968959134575,16.8292587962898,1443.41102941176));
#165161=CARTESIAN_POINT('Ctrl Pts',(8.07915007496071,16.2251205863895,1441.91691176471));
#165162=CARTESIAN_POINT('Ctrl Pts',(9.50104767561053,15.3447188656481,1440.42279411765));
#165163=CARTESIAN_POINT('Ctrl Pts',(10.9229452762603,14.4643171449067,1438.92867647059));
#165164=CARTESIAN_POINT('Ctrl Pts',(12.1588589765331,13.3376329379985,1437.43455882353));
#165165=CARTESIAN_POINT('Ctrl Pts',(13.3947726768058,12.2109487310903,1435.94044117647));
#165166=CARTESIAN_POINT('Ctrl Pts',(14.4026149179538,10.8763499173728,1434.44632352941));
#165167=CARTESIAN_POINT('Ctrl Pts',(15.4104571591017,9.54175110365538,1432.95220588235));
#165168=CARTESIAN_POINT('Ctrl Pts',(16.1559070823762,8.04468584505496,1431.45808823529));
#165169=CARTESIAN_POINT('Ctrl Pts',(16.9013570056506,6.54762058645456,1429.96397058824));
#165170=CARTESIAN_POINT('Ctrl Pts',(17.3590292079831,4.93906964482096,1428.46985294118));
#165171=CARTESIAN_POINT('Ctrl Pts',(17.8167014103155,3.33051870318735,1426.97573529412));
#165172=CARTESIAN_POINT('Ctrl Pts',(17.9710104137728,1.66525935159367,1425.48161764706));
#165173=CARTESIAN_POINT('Ctrl Pts',(18.1253194172301,3.32956716117513E-15,
1423.9875));
#165174=CARTESIAN_POINT('Ctrl Pts',(17.9710104137728,-1.66525935159367,
1422.49338235294));
#165175=CARTESIAN_POINT('Ctrl Pts',(17.8167014103155,-3.33051870318736,
1420.99926470588));
#165176=CARTESIAN_POINT('Ctrl Pts',(17.3590292079831,-4.93906964482095,
1419.50514705882));
#165177=CARTESIAN_POINT('Ctrl Pts',(16.9013570056506,-6.54762058645456,
1418.01102941176));
#165178=CARTESIAN_POINT('Ctrl Pts',(16.1559070823762,-8.04468584505497,
1416.51691176471));
#165179=CARTESIAN_POINT('Ctrl Pts',(15.4104571591017,-9.54175110365538,
1415.02279411765));
#165180=CARTESIAN_POINT('Ctrl Pts',(14.4026149179538,-10.8763499173728,
1413.52867647059));
#165181=CARTESIAN_POINT('Ctrl Pts',(13.3947726768058,-12.2109487310903,
1412.03455882353));
#165182=CARTESIAN_POINT('Ctrl Pts',(12.1588589765331,-13.3376329379985,
1410.54044117647));
#165183=CARTESIAN_POINT('Ctrl Pts',(10.9229452762603,-14.4643171449067,
1409.04632352941));
#165184=CARTESIAN_POINT('Ctrl Pts',(9.50104767561053,-15.3447188656481,
1407.55220588235));
#165185=CARTESIAN_POINT('Ctrl Pts',(8.07915007496071,-16.2251205863895,
1406.05808823529));
#165186=CARTESIAN_POINT('Ctrl Pts',(6.51968959134574,-16.8292587962898,
1404.56397058824));
#165187=CARTESIAN_POINT('Ctrl Pts',(4.96022910773078,-17.4333970061901,
1403.06985294118));
#165188=CARTESIAN_POINT('Ctrl Pts',(3.31631129755346,-17.7406985030951,
1401.57573529412));
#165189=CARTESIAN_POINT('Ctrl Pts',(1.67239348737615,-18.048,1400.08161764706));
#165190=CARTESIAN_POINT('Ctrl Pts',(0.,-18.048,1398.5875));
#165191=CARTESIAN_POINT('Ctrl Pts',(-1.67239348737615,-18.048,1397.09338235294));
#165192=CARTESIAN_POINT('Ctrl Pts',(-3.31631129755346,-17.7406985030951,
1395.59926470588));
#165193=CARTESIAN_POINT('Ctrl Pts',(-4.96022910773077,-17.4333970061901,
1394.10514705882));
#165194=CARTESIAN_POINT('Ctrl Pts',(-6.51968959134574,-16.8292587962898,
1392.61102941176));
#165195=CARTESIAN_POINT('Ctrl Pts',(-8.07915007496071,-16.2251205863895,
1391.11691176471));
#165196=CARTESIAN_POINT('Ctrl Pts',(-9.50104767561052,-15.3447188656481,
1389.62279411765));
#165197=CARTESIAN_POINT('Ctrl Pts',(-10.9229452762603,-14.4643171449067,
1388.12867647059));
#165198=CARTESIAN_POINT('Ctrl Pts',(-12.1588589765331,-13.3376329379985,
1386.63455882353));
#165199=CARTESIAN_POINT('Ctrl Pts',(-13.3947726768058,-12.2109487310903,
1385.14044117647));
#165200=CARTESIAN_POINT('Ctrl Pts',(-14.4026149179538,-10.8763499173728,
1383.64632352941));
#165201=CARTESIAN_POINT('Ctrl Pts',(-15.4104571591017,-9.54175110365538,
1382.15220588235));
#165202=CARTESIAN_POINT('Ctrl Pts',(-16.1559070823762,-8.04468584505497,
1380.65808823529));
#165203=CARTESIAN_POINT('Ctrl Pts',(-16.9013570056506,-6.54762058645456,
1379.16397058824));
#165204=CARTESIAN_POINT('Ctrl Pts',(-17.3590292079831,-4.93906964482095,
1377.66985294118));
#165205=CARTESIAN_POINT('Ctrl Pts',(-17.8167014103155,-3.33051870318735,
1376.17573529412));
#165206=CARTESIAN_POINT('Ctrl Pts',(-17.9710104137728,-1.66525935159368,
1374.68161764706));
#165207=CARTESIAN_POINT('Ctrl Pts',(-18.1253194172301,-1.10985572039171E-15,
1373.1875));
#165208=CARTESIAN_POINT('Ctrl Pts',(-17.9710104137728,1.66525935159367,
1371.69338235294));
#165209=CARTESIAN_POINT('Ctrl Pts',(-17.8167014103155,3.33051870318735,
1370.19926470588));
#165210=CARTESIAN_POINT('Ctrl Pts',(-17.3590292079831,4.93906964482096,
1368.70514705882));
#165211=CARTESIAN_POINT('Ctrl Pts',(-16.9013570056506,6.54762058645456,
1367.21102941176));
#165212=CARTESIAN_POINT('Ctrl Pts',(-16.1559070823762,8.04468584505497,
1365.71691176471));
#165213=CARTESIAN_POINT('Ctrl Pts',(-15.4104571591017,9.54175110365538,
1364.22279411765));
#165214=CARTESIAN_POINT('Ctrl Pts',(-14.4026149179538,10.8763499173728,
1362.72867647059));
#165215=CARTESIAN_POINT('Ctrl Pts',(-13.3947726768058,12.2109487310903,
1361.23455882353));
#165216=CARTESIAN_POINT('Ctrl Pts',(-12.1588589765331,13.3376329379985,
1359.74044117647));
#165217=CARTESIAN_POINT('Ctrl Pts',(-10.9229452762603,14.4643171449067,
1358.24632352941));
#165218=CARTESIAN_POINT('Ctrl Pts',(-9.50104767561052,15.3447188656481,
1356.75220588235));
#165219=CARTESIAN_POINT('Ctrl Pts',(-8.07915007496071,16.2251205863895,
1355.25808823529));
#165220=CARTESIAN_POINT('Ctrl Pts',(-6.51968959134574,16.8292587962898,
1353.76397058824));
#165221=CARTESIAN_POINT('Ctrl Pts',(-4.96022910773078,17.4333970061901,
1352.26985294118));
#165222=CARTESIAN_POINT('Ctrl Pts',(-3.31631129755346,17.7406985030951,
1350.77573529412));
#165223=CARTESIAN_POINT('Ctrl Pts',(-1.67239348737615,18.048,1349.28161764706));
#165224=CARTESIAN_POINT('Ctrl Pts',(-2.21024254310115E-15,18.048,1347.7875));
#165225=CARTESIAN_POINT('Ctrl Pts',(1.67239348737616,18.048,1346.29338235294));
#165226=CARTESIAN_POINT('Ctrl Pts',(3.31631129755346,17.7406985030951,1344.79926470588));
#165227=CARTESIAN_POINT('Ctrl Pts',(4.96022910773077,17.4333970061901,1343.30514705882));
#165228=CARTESIAN_POINT('Ctrl Pts',(6.51968959134575,16.8292587962898,1341.81102941176));
#165229=CARTESIAN_POINT('Ctrl Pts',(8.07915007496071,16.2251205863895,1340.31691176471));
#165230=CARTESIAN_POINT('Ctrl Pts',(9.50104767561053,15.3447188656481,1338.82279411765));
#165231=CARTESIAN_POINT('Ctrl Pts',(10.9229452762603,14.4643171449067,1337.32867647059));
#165232=CARTESIAN_POINT('Ctrl Pts',(12.1588589765331,13.3376329379985,1335.83455882353));
#165233=CARTESIAN_POINT('Ctrl Pts',(13.3947726768058,12.2109487310903,1334.34044117647));
#165234=CARTESIAN_POINT('Ctrl Pts',(14.4026149179538,10.8763499173728,1332.84632352941));
#165235=CARTESIAN_POINT('Ctrl Pts',(15.4104571591017,9.54175110365538,1331.35220588235));
#165236=CARTESIAN_POINT('Ctrl Pts',(16.1559070823762,8.04468584505496,1329.85808823529));
#165237=CARTESIAN_POINT('Ctrl Pts',(16.9013570056506,6.54762058645456,1328.36397058824));
#165238=CARTESIAN_POINT('Ctrl Pts',(17.3590292079831,4.93906964482096,1326.86985294118));
#165239=CARTESIAN_POINT('Ctrl Pts',(17.8167014103155,3.33051870318735,1325.37573529412));
#165240=CARTESIAN_POINT('Ctrl Pts',(17.9710104137728,1.66525935159367,1323.88161764706));
#165241=CARTESIAN_POINT('Ctrl Pts',(18.1253194172301,3.32956716117513E-15,
1322.3875));
#165242=CARTESIAN_POINT('Ctrl Pts',(17.9710104137728,-1.66525935159367,
1320.89338235294));
#165243=CARTESIAN_POINT('Ctrl Pts',(17.8167014103155,-3.33051870318736,
1319.39926470588));
#165244=CARTESIAN_POINT('Ctrl Pts',(17.3590292079831,-4.93906964482095,
1317.90514705882));
#165245=CARTESIAN_POINT('Ctrl Pts',(16.9013570056506,-6.54762058645456,
1316.41102941176));
#165246=CARTESIAN_POINT('Ctrl Pts',(16.1559070823762,-8.04468584505497,
1314.91691176471));
#165247=CARTESIAN_POINT('Ctrl Pts',(15.4104571591017,-9.54175110365538,
1313.42279411765));
#165248=CARTESIAN_POINT('Ctrl Pts',(14.4026149179538,-10.8763499173728,
1311.92867647059));
#165249=CARTESIAN_POINT('Ctrl Pts',(13.3947726768058,-12.2109487310903,
1310.43455882353));
#165250=CARTESIAN_POINT('Ctrl Pts',(12.1588589765331,-13.3376329379985,
1308.94044117647));
#165251=CARTESIAN_POINT('Ctrl Pts',(10.9229452762603,-14.4643171449067,
1307.44632352941));
#165252=CARTESIAN_POINT('Ctrl Pts',(9.50104767561053,-15.3447188656481,
1305.95220588235));
#165253=CARTESIAN_POINT('Ctrl Pts',(8.07915007496071,-16.2251205863895,
1304.45808823529));
#165254=CARTESIAN_POINT('Ctrl Pts',(6.51968959134574,-16.8292587962898,
1302.96397058824));
#165255=CARTESIAN_POINT('Ctrl Pts',(4.96022910773078,-17.4333970061901,
1301.46985294118));
#165256=CARTESIAN_POINT('Ctrl Pts',(3.31631129755346,-17.7406985030951,
1299.97573529412));
#165257=CARTESIAN_POINT('Ctrl Pts',(1.67239348737615,-18.048,1298.48161764706));
#165258=CARTESIAN_POINT('Ctrl Pts',(0.,-18.048,1296.9875));
#165259=CARTESIAN_POINT('Ctrl Pts',(-1.67239348737615,-18.048,1295.49338235294));
#165260=CARTESIAN_POINT('Ctrl Pts',(-3.31631129755346,-17.7406985030951,
1293.99926470588));
#165261=CARTESIAN_POINT('Ctrl Pts',(-4.96022910773077,-17.4333970061901,
1292.50514705882));
#165262=CARTESIAN_POINT('Ctrl Pts',(-6.51968959134574,-16.8292587962898,
1291.01102941176));
#165263=CARTESIAN_POINT('Ctrl Pts',(-8.07915007496071,-16.2251205863895,
1289.51691176471));
#165264=CARTESIAN_POINT('Ctrl Pts',(-9.50104767561052,-15.3447188656481,
1288.02279411765));
#165265=CARTESIAN_POINT('Ctrl Pts',(-10.9229452762603,-14.4643171449067,
1286.52867647059));
#165266=CARTESIAN_POINT('Ctrl Pts',(-12.1588589765331,-13.3376329379985,
1285.03455882353));
#165267=CARTESIAN_POINT('Ctrl Pts',(-13.3947726768058,-12.2109487310903,
1283.54044117647));
#165268=CARTESIAN_POINT('Ctrl Pts',(-14.4026149179538,-10.8763499173728,
1282.04632352941));
#165269=CARTESIAN_POINT('Ctrl Pts',(-15.4104571591017,-9.54175110365538,
1280.55220588235));
#165270=CARTESIAN_POINT('Ctrl Pts',(-16.1559070823762,-8.04468584505497,
1279.05808823529));
#165271=CARTESIAN_POINT('Ctrl Pts',(-16.9013570056506,-6.54762058645456,
1277.56397058824));
#165272=CARTESIAN_POINT('Ctrl Pts',(-17.3590292079831,-4.93906964482095,
1276.06985294118));
#165273=CARTESIAN_POINT('Ctrl Pts',(-17.8167014103155,-3.33051870318735,
1274.57573529412));
#165274=CARTESIAN_POINT('Ctrl Pts',(-17.9710104137728,-1.66525935159368,
1273.08161764706));
#165275=CARTESIAN_POINT('Ctrl Pts',(-18.1253194172301,-1.10985572039171E-15,
1271.5875));
#165276=CARTESIAN_POINT('Ctrl Pts',(-17.9710104137728,1.66525935159367,
1270.09338235294));
#165277=CARTESIAN_POINT('Ctrl Pts',(-17.8167014103155,3.33051870318735,
1268.59926470588));
#165278=CARTESIAN_POINT('Ctrl Pts',(-17.3590292079831,4.93906964482096,
1267.10514705882));
#165279=CARTESIAN_POINT('Ctrl Pts',(-16.9013570056506,6.54762058645456,
1265.61102941176));
#165280=CARTESIAN_POINT('Ctrl Pts',(-16.1559070823762,8.04468584505497,
1264.11691176471));
#165281=CARTESIAN_POINT('Ctrl Pts',(-15.4104571591017,9.54175110365538,
1262.62279411765));
#165282=CARTESIAN_POINT('Ctrl Pts',(-14.4026149179538,10.8763499173728,
1261.12867647059));
#165283=CARTESIAN_POINT('Ctrl Pts',(-13.3947726768058,12.2109487310903,
1259.63455882353));
#165284=CARTESIAN_POINT('Ctrl Pts',(-12.1588589765331,13.3376329379985,
1258.14044117647));
#165285=CARTESIAN_POINT('Ctrl Pts',(-10.9229452762603,14.4643171449067,
1256.64632352941));
#165286=CARTESIAN_POINT('Ctrl Pts',(-9.50104767561052,15.3447188656481,
1255.15220588235));
#165287=CARTESIAN_POINT('Ctrl Pts',(-8.07915007496071,16.2251205863895,
1253.65808823529));
#165288=CARTESIAN_POINT('Ctrl Pts',(-6.51968959134574,16.8292587962898,
1252.16397058824));
#165289=CARTESIAN_POINT('Ctrl Pts',(-4.96022910773078,17.4333970061901,
1250.66985294118));
#165290=CARTESIAN_POINT('Ctrl Pts',(-3.31631129755346,17.7406985030951,
1249.17573529412));
#165291=CARTESIAN_POINT('Ctrl Pts',(-1.67239348737615,18.048,1247.68161764706));
#165292=CARTESIAN_POINT('Ctrl Pts',(-2.21024254310115E-15,18.048,1246.1875));
#165293=CARTESIAN_POINT('Ctrl Pts',(1.67239348737616,18.048,1244.69338235294));
#165294=CARTESIAN_POINT('Ctrl Pts',(3.31631129755346,17.7406985030951,1243.19926470588));
#165295=CARTESIAN_POINT('Ctrl Pts',(4.96022910773077,17.4333970061901,1241.70514705882));
#165296=CARTESIAN_POINT('Ctrl Pts',(6.51968959134575,16.8292587962898,1240.21102941176));
#165297=CARTESIAN_POINT('Ctrl Pts',(8.07915007496071,16.2251205863895,1238.71691176471));
#165298=CARTESIAN_POINT('Ctrl Pts',(9.50104767561053,15.3447188656481,1237.22279411765));
#165299=CARTESIAN_POINT('Ctrl Pts',(10.9229452762603,14.4643171449067,1235.72867647059));
#165300=CARTESIAN_POINT('Ctrl Pts',(12.1588589765331,13.3376329379985,1234.23455882353));
#165301=CARTESIAN_POINT('Ctrl Pts',(13.3947726768058,12.2109487310903,1232.74044117647));
#165302=CARTESIAN_POINT('Ctrl Pts',(14.4026149179538,10.8763499173728,1231.24632352941));
#165303=CARTESIAN_POINT('Ctrl Pts',(15.4104571591017,9.54175110365538,1229.75220588235));
#165304=CARTESIAN_POINT('Ctrl Pts',(16.1559070823762,8.04468584505496,1228.25808823529));
#165305=CARTESIAN_POINT('Ctrl Pts',(16.9013570056506,6.54762058645456,1226.76397058824));
#165306=CARTESIAN_POINT('Ctrl Pts',(17.3590292079831,4.93906964482096,1225.26985294118));
#165307=CARTESIAN_POINT('Ctrl Pts',(17.8167014103155,3.33051870318735,1223.77573529412));
#165308=CARTESIAN_POINT('Ctrl Pts',(17.9710104137728,1.66525935159367,1222.28161764706));
#165309=CARTESIAN_POINT('Ctrl Pts',(18.1253194172301,3.32956716117513E-15,
1220.7875));
#165310=CARTESIAN_POINT('Ctrl Pts',(17.9710104137728,-1.66525935159367,
1219.29338235294));
#165311=CARTESIAN_POINT('Ctrl Pts',(17.8167014103155,-3.33051870318736,
1217.79926470588));
#165312=CARTESIAN_POINT('Ctrl Pts',(17.3590292079831,-4.93906964482095,
1216.30514705882));
#165313=CARTESIAN_POINT('Ctrl Pts',(16.9013570056506,-6.54762058645456,
1214.81102941176));
#165314=CARTESIAN_POINT('Ctrl Pts',(16.1559070823762,-8.04468584505497,
1213.31691176471));
#165315=CARTESIAN_POINT('Ctrl Pts',(15.4104571591017,-9.54175110365538,
1211.82279411765));
#165316=CARTESIAN_POINT('Ctrl Pts',(14.4026149179538,-10.8763499173728,
1210.32867647059));
#165317=CARTESIAN_POINT('Ctrl Pts',(13.3947726768058,-12.2109487310903,
1208.83455882353));
#165318=CARTESIAN_POINT('Ctrl Pts',(12.1588589765331,-13.3376329379985,
1207.34044117647));
#165319=CARTESIAN_POINT('Ctrl Pts',(10.9229452762603,-14.4643171449067,
1205.84632352941));
#165320=CARTESIAN_POINT('Ctrl Pts',(9.50104767561053,-15.3447188656481,
1204.35220588235));
#165321=CARTESIAN_POINT('Ctrl Pts',(8.07915007496071,-16.2251205863895,
1202.85808823529));
#165322=CARTESIAN_POINT('Ctrl Pts',(6.51968959134574,-16.8292587962898,
1201.36397058824));
#165323=CARTESIAN_POINT('Ctrl Pts',(4.96022910773078,-17.4333970061901,
1199.86985294118));
#165324=CARTESIAN_POINT('Ctrl Pts',(3.31631129755346,-17.7406985030951,
1198.37573529412));
#165325=CARTESIAN_POINT('Ctrl Pts',(1.67239348737615,-18.048,1196.88161764706));
#165326=CARTESIAN_POINT('Ctrl Pts',(0.,-18.048,1195.3875));
#165327=CARTESIAN_POINT('Ctrl Pts',(-1.67239348737615,-18.048,1193.89338235294));
#165328=CARTESIAN_POINT('Ctrl Pts',(-3.31631129755346,-17.7406985030951,
1192.39926470588));
#165329=CARTESIAN_POINT('Ctrl Pts',(-4.96022910773077,-17.4333970061901,
1190.90514705882));
#165330=CARTESIAN_POINT('Ctrl Pts',(-6.51968959134574,-16.8292587962898,
1189.41102941176));
#165331=CARTESIAN_POINT('Ctrl Pts',(-8.07915007496071,-16.2251205863895,
1187.91691176471));
#165332=CARTESIAN_POINT('Ctrl Pts',(-9.50104767561052,-15.3447188656481,
1186.42279411765));
#165333=CARTESIAN_POINT('Ctrl Pts',(-10.9229452762603,-14.4643171449067,
1184.92867647059));
#165334=CARTESIAN_POINT('Ctrl Pts',(-12.1588589765331,-13.3376329379985,
1183.43455882353));
#165335=CARTESIAN_POINT('Ctrl Pts',(-13.3947726768058,-12.2109487310903,
1181.94044117647));
#165336=CARTESIAN_POINT('Ctrl Pts',(-14.4026149179538,-10.8763499173728,
1180.44632352941));
#165337=CARTESIAN_POINT('Ctrl Pts',(-15.4104571591017,-9.54175110365538,
1178.95220588235));
#165338=CARTESIAN_POINT('Ctrl Pts',(-16.1559070823762,-8.04468584505497,
1177.45808823529));
#165339=CARTESIAN_POINT('Ctrl Pts',(-16.9013570056506,-6.54762058645456,
1175.96397058824));
#165340=CARTESIAN_POINT('Ctrl Pts',(-17.3590292079831,-4.93906964482095,
1174.46985294118));
#165341=CARTESIAN_POINT('Ctrl Pts',(-17.8167014103155,-3.33051870318735,
1172.97573529412));
#165342=CARTESIAN_POINT('Ctrl Pts',(-17.9710104137728,-1.66525935159368,
1171.48161764706));
#165343=CARTESIAN_POINT('Ctrl Pts',(-18.1253194172301,-1.10985572039171E-15,
1169.9875));
#165344=CARTESIAN_POINT('Ctrl Pts',(-17.9710104137728,1.66525935159367,
1168.49338235294));
#165345=CARTESIAN_POINT('Ctrl Pts',(-17.8167014103155,3.33051870318735,
1166.99926470588));
#165346=CARTESIAN_POINT('Ctrl Pts',(-17.3590292079831,4.93906964482096,
1165.50514705882));
#165347=CARTESIAN_POINT('Ctrl Pts',(-16.9013570056506,6.54762058645456,
1164.01102941176));
#165348=CARTESIAN_POINT('Ctrl Pts',(-16.1559070823762,8.04468584505497,
1162.51691176471));
#165349=CARTESIAN_POINT('Ctrl Pts',(-15.4104571591017,9.54175110365538,
1161.02279411765));
#165350=CARTESIAN_POINT('Ctrl Pts',(-14.4026149179538,10.8763499173728,
1159.52867647059));
#165351=CARTESIAN_POINT('Ctrl Pts',(-13.3947726768058,12.2109487310903,
1158.03455882353));
#165352=CARTESIAN_POINT('Ctrl Pts',(-12.1588589765331,13.3376329379985,
1156.54044117647));
#165353=CARTESIAN_POINT('Ctrl Pts',(-10.9229452762603,14.4643171449067,
1155.04632352941));
#165354=CARTESIAN_POINT('Ctrl Pts',(-9.50104767561052,15.3447188656481,
1153.55220588235));
#165355=CARTESIAN_POINT('Ctrl Pts',(-8.07915007496071,16.2251205863895,
1152.05808823529));
#165356=CARTESIAN_POINT('Ctrl Pts',(-6.51968959134574,16.8292587962898,
1150.56397058824));
#165357=CARTESIAN_POINT('Ctrl Pts',(-4.96022910773078,17.4333970061901,
1149.06985294118));
#165358=CARTESIAN_POINT('Ctrl Pts',(-3.31631129755346,17.7406985030951,
1147.57573529412));
#165359=CARTESIAN_POINT('Ctrl Pts',(-1.67239348737615,18.048,1146.08161764706));
#165360=CARTESIAN_POINT('Ctrl Pts',(-2.21024254310115E-15,18.048,1144.5875));
#165361=CARTESIAN_POINT('Ctrl Pts',(1.67239348737616,18.048,1143.09338235294));
#165362=CARTESIAN_POINT('Ctrl Pts',(3.31631129755346,17.7406985030951,1141.59926470588));
#165363=CARTESIAN_POINT('Ctrl Pts',(4.96022910773077,17.4333970061901,1140.10514705882));
#165364=CARTESIAN_POINT('Ctrl Pts',(6.51968959134575,16.8292587962898,1138.61102941176));
#165365=CARTESIAN_POINT('Ctrl Pts',(8.07915007496071,16.2251205863895,1137.11691176471));
#165366=CARTESIAN_POINT('Ctrl Pts',(9.50104767561053,15.3447188656481,1135.62279411765));
#165367=CARTESIAN_POINT('Ctrl Pts',(10.9229452762603,14.4643171449067,1134.12867647059));
#165368=CARTESIAN_POINT('Ctrl Pts',(12.1588589765331,13.3376329379985,1132.63455882353));
#165369=CARTESIAN_POINT('Ctrl Pts',(13.3947726768058,12.2109487310903,1131.14044117647));
#165370=CARTESIAN_POINT('Ctrl Pts',(14.4026149179538,10.8763499173728,1129.64632352941));
#165371=CARTESIAN_POINT('Ctrl Pts',(15.4104571591017,9.54175110365538,1128.15220588235));
#165372=CARTESIAN_POINT('Ctrl Pts',(16.1559070823762,8.04468584505496,1126.65808823529));
#165373=CARTESIAN_POINT('Ctrl Pts',(16.9013570056506,6.54762058645456,1125.16397058824));
#165374=CARTESIAN_POINT('Ctrl Pts',(17.3590292079831,4.93906964482096,1123.66985294118));
#165375=CARTESIAN_POINT('Ctrl Pts',(17.8167014103155,3.33051870318735,1122.17573529412));
#165376=CARTESIAN_POINT('Ctrl Pts',(17.9710104137728,1.66525935159367,1120.68161764706));
#165377=CARTESIAN_POINT('Ctrl Pts',(18.1253194172301,3.32956716117513E-15,
1119.1875));
#165378=CARTESIAN_POINT('Ctrl Pts',(17.9710104137728,-1.66525935159367,
1117.69338235294));
#165379=CARTESIAN_POINT('Ctrl Pts',(17.8167014103155,-3.33051870318736,
1116.19926470588));
#165380=CARTESIAN_POINT('Ctrl Pts',(17.3590292079831,-4.93906964482095,
1114.70514705882));
#165381=CARTESIAN_POINT('Ctrl Pts',(16.9013570056506,-6.54762058645456,
1113.21102941176));
#165382=CARTESIAN_POINT('Ctrl Pts',(16.1559070823762,-8.04468584505497,
1111.71691176471));
#165383=CARTESIAN_POINT('Ctrl Pts',(15.4104571591017,-9.54175110365538,
1110.22279411765));
#165384=CARTESIAN_POINT('Ctrl Pts',(14.4026149179538,-10.8763499173728,
1108.72867647059));
#165385=CARTESIAN_POINT('Ctrl Pts',(13.3947726768058,-12.2109487310903,
1107.23455882353));
#165386=CARTESIAN_POINT('Ctrl Pts',(12.1588589765331,-13.3376329379985,
1105.74044117647));
#165387=CARTESIAN_POINT('Ctrl Pts',(10.9229452762603,-14.4643171449067,
1104.24632352941));
#165388=CARTESIAN_POINT('Ctrl Pts',(9.50104767561053,-15.3447188656481,
1102.75220588235));
#165389=CARTESIAN_POINT('Ctrl Pts',(8.07915007496071,-16.2251205863895,
1101.25808823529));
#165390=CARTESIAN_POINT('Ctrl Pts',(6.51968959134574,-16.8292587962898,
1099.76397058824));
#165391=CARTESIAN_POINT('Ctrl Pts',(4.96022910773078,-17.4333970061901,
1098.26985294118));
#165392=CARTESIAN_POINT('Ctrl Pts',(3.31631129755346,-17.7406985030951,
1096.77573529412));
#165393=CARTESIAN_POINT('Ctrl Pts',(1.67239348737615,-18.048,1095.28161764706));
#165394=CARTESIAN_POINT('Ctrl Pts',(0.,-18.048,1093.7875));
#165395=CARTESIAN_POINT('Ctrl Pts',(-1.67239348737615,-18.048,1092.29338235294));
#165396=CARTESIAN_POINT('Ctrl Pts',(-3.31631129755346,-17.7406985030951,
1090.79926470588));
#165397=CARTESIAN_POINT('Ctrl Pts',(-4.96022910773077,-17.4333970061901,
1089.30514705882));
#165398=CARTESIAN_POINT('Ctrl Pts',(-6.51968959134574,-16.8292587962898,
1087.81102941176));
#165399=CARTESIAN_POINT('Ctrl Pts',(-8.07915007496071,-16.2251205863895,
1086.31691176471));
#165400=CARTESIAN_POINT('Ctrl Pts',(-9.50104767561052,-15.3447188656481,
1084.82279411765));
#165401=CARTESIAN_POINT('Ctrl Pts',(-10.9229452762603,-14.4643171449067,
1083.32867647059));
#165402=CARTESIAN_POINT('Ctrl Pts',(-12.1588589765331,-13.3376329379985,
1081.83455882353));
#165403=CARTESIAN_POINT('Ctrl Pts',(-13.3947726768058,-12.2109487310903,
1080.34044117647));
#165404=CARTESIAN_POINT('Ctrl Pts',(-14.4026149179538,-10.8763499173728,
1078.84632352941));
#165405=CARTESIAN_POINT('Ctrl Pts',(-15.4104571591017,-9.54175110365538,
1077.35220588235));
#165406=CARTESIAN_POINT('Ctrl Pts',(-16.1559070823762,-8.04468584505497,
1075.85808823529));
#165407=CARTESIAN_POINT('Ctrl Pts',(-16.9013570056506,-6.54762058645456,
1074.36397058824));
#165408=CARTESIAN_POINT('Ctrl Pts',(-17.3590292079831,-4.93906964482095,
1072.86985294118));
#165409=CARTESIAN_POINT('Ctrl Pts',(-17.8167014103155,-3.33051870318735,
1071.37573529412));
#165410=CARTESIAN_POINT('Ctrl Pts',(-17.9710104137728,-1.66525935159368,
1069.88161764706));
#165411=CARTESIAN_POINT('Ctrl Pts',(-18.1253194172301,-1.10985572039171E-15,
1068.3875));
#165412=CARTESIAN_POINT('Ctrl Pts',(-17.9710104137728,1.66525935159367,
1066.89338235294));
#165413=CARTESIAN_POINT('Ctrl Pts',(-17.8167014103155,3.33051870318735,
1065.39926470588));
#165414=CARTESIAN_POINT('Ctrl Pts',(-17.3590292079831,4.93906964482096,
1063.90514705882));
#165415=CARTESIAN_POINT('Ctrl Pts',(-16.9013570056506,6.54762058645456,
1062.41102941176));
#165416=CARTESIAN_POINT('Ctrl Pts',(-16.1559070823762,8.04468584505497,
1060.91691176471));
#165417=CARTESIAN_POINT('Ctrl Pts',(-15.4104571591017,9.54175110365538,
1059.42279411765));
#165418=CARTESIAN_POINT('Ctrl Pts',(-14.4026149179538,10.8763499173728,
1057.92867647059));
#165419=CARTESIAN_POINT('Ctrl Pts',(-13.3947726768058,12.2109487310903,
1056.43455882353));
#165420=CARTESIAN_POINT('Ctrl Pts',(-12.1588589765331,13.3376329379985,
1054.94044117647));
#165421=CARTESIAN_POINT('Ctrl Pts',(-10.9229452762603,14.4643171449067,
1053.44632352941));
#165422=CARTESIAN_POINT('Ctrl Pts',(-9.50104767561052,15.3447188656481,
1051.95220588235));
#165423=CARTESIAN_POINT('Ctrl Pts',(-8.07915007496071,16.2251205863895,
1050.45808823529));
#165424=CARTESIAN_POINT('Ctrl Pts',(-6.51968959134574,16.8292587962898,
1048.96397058824));
#165425=CARTESIAN_POINT('Ctrl Pts',(-4.96022910773078,17.4333970061901,
1047.46985294118));
#165426=CARTESIAN_POINT('Ctrl Pts',(-3.31631129755346,17.7406985030951,
1045.97573529412));
#165427=CARTESIAN_POINT('Ctrl Pts',(-1.67239348737615,18.048,1044.48161764706));
#165428=CARTESIAN_POINT('Ctrl Pts',(-2.21024254310115E-15,18.048,1042.9875));
#165429=CARTESIAN_POINT('Ctrl Pts',(1.67239348737616,18.048,1041.49338235294));
#165430=CARTESIAN_POINT('Ctrl Pts',(3.31631129755346,17.7406985030951,1039.99926470588));
#165431=CARTESIAN_POINT('Ctrl Pts',(4.96022910773077,17.4333970061901,1038.50514705882));
#165432=CARTESIAN_POINT('Ctrl Pts',(6.51968959134575,16.8292587962898,1037.01102941176));
#165433=CARTESIAN_POINT('Ctrl Pts',(8.07915007496071,16.2251205863895,1035.51691176471));
#165434=CARTESIAN_POINT('Ctrl Pts',(9.50104767561053,15.3447188656481,1034.02279411765));
#165435=CARTESIAN_POINT('Ctrl Pts',(10.9229452762603,14.4643171449067,1032.52867647059));
#165436=CARTESIAN_POINT('Ctrl Pts',(12.1588589765331,13.3376329379985,1031.03455882353));
#165437=CARTESIAN_POINT('Ctrl Pts',(13.3947726768058,12.2109487310903,1029.54044117647));
#165438=CARTESIAN_POINT('Ctrl Pts',(14.4026149179538,10.8763499173728,1028.04632352941));
#165439=CARTESIAN_POINT('Ctrl Pts',(15.4104571591017,9.54175110365538,1026.55220588235));
#165440=CARTESIAN_POINT('Ctrl Pts',(16.1559070823762,8.04468584505496,1025.05808823529));
#165441=CARTESIAN_POINT('Ctrl Pts',(16.9013570056506,6.54762058645456,1023.56397058824));
#165442=CARTESIAN_POINT('Ctrl Pts',(17.3590292079831,4.93906964482096,1022.06985294118));
#165443=CARTESIAN_POINT('Ctrl Pts',(17.8167014103155,3.33051870318735,1020.57573529412));
#165444=CARTESIAN_POINT('Ctrl Pts',(17.9710104137728,1.66525935159367,1019.08161764706));
#165445=CARTESIAN_POINT('Ctrl Pts',(18.1253194172301,3.32956716117513E-15,
1017.5875));
#165446=CARTESIAN_POINT('Ctrl Pts',(17.9710104137728,-1.66525935159367,
1016.09338235294));
#165447=CARTESIAN_POINT('Ctrl Pts',(17.8167014103155,-3.33051870318736,
1014.59926470588));
#165448=CARTESIAN_POINT('Ctrl Pts',(17.3590292079831,-4.93906964482095,
1013.10514705882));
#165449=CARTESIAN_POINT('Ctrl Pts',(16.9013570056506,-6.54762058645456,
1011.61102941176));
#165450=CARTESIAN_POINT('Ctrl Pts',(16.1559070823762,-8.04468584505497,
1010.11691176471));
#165451=CARTESIAN_POINT('Ctrl Pts',(15.4104571591017,-9.54175110365538,
1008.62279411765));
#165452=CARTESIAN_POINT('Ctrl Pts',(14.4026149179538,-10.8763499173728,
1007.12867647059));
#165453=CARTESIAN_POINT('Ctrl Pts',(13.3947726768058,-12.2109487310903,
1005.63455882353));
#165454=CARTESIAN_POINT('Ctrl Pts',(12.1588589765331,-13.3376329379985,
1004.14044117647));
#165455=CARTESIAN_POINT('Ctrl Pts',(10.9229452762603,-14.4643171449067,
1002.64632352941));
#165456=CARTESIAN_POINT('Ctrl Pts',(9.50104767561053,-15.3447188656481,
1001.15220588235));
#165457=CARTESIAN_POINT('Ctrl Pts',(8.07915007496071,-16.2251205863895,
999.658088235294));
#165458=CARTESIAN_POINT('Ctrl Pts',(6.51968959134574,-16.8292587962898,
998.163970588235));
#165459=CARTESIAN_POINT('Ctrl Pts',(4.96022910773078,-17.4333970061901,
996.669852941177));
#165460=CARTESIAN_POINT('Ctrl Pts',(3.31631129755346,-17.7406985030951,
995.175735294118));
#165461=CARTESIAN_POINT('Ctrl Pts',(1.67239348737615,-18.048,993.681617647059));
#165462=CARTESIAN_POINT('Ctrl Pts',(0.,-18.048,992.1875));
#165463=CARTESIAN_POINT('Ctrl Pts',(-1.67239348737615,-18.048,990.693382352941));
#165464=CARTESIAN_POINT('Ctrl Pts',(-3.31631129755346,-17.7406985030951,
989.199264705882));
#165465=CARTESIAN_POINT('Ctrl Pts',(-4.96022910773077,-17.4333970061901,
987.705147058824));
#165466=CARTESIAN_POINT('Ctrl Pts',(-6.51968959134574,-16.8292587962898,
986.211029411765));
#165467=CARTESIAN_POINT('Ctrl Pts',(-8.07915007496071,-16.2251205863895,
984.716911764706));
#165468=CARTESIAN_POINT('Ctrl Pts',(-9.50104767561052,-15.3447188656481,
983.222794117647));
#165469=CARTESIAN_POINT('Ctrl Pts',(-10.9229452762603,-14.4643171449067,
981.728676470589));
#165470=CARTESIAN_POINT('Ctrl Pts',(-12.1588589765331,-13.3376329379985,
980.234558823529));
#165471=CARTESIAN_POINT('Ctrl Pts',(-13.3947726768058,-12.2109487310903,
978.740441176471));
#165472=CARTESIAN_POINT('Ctrl Pts',(-14.4026149179538,-10.8763499173728,
977.246323529412));
#165473=CARTESIAN_POINT('Ctrl Pts',(-15.4104571591017,-9.54175110365538,
975.752205882353));
#165474=CARTESIAN_POINT('Ctrl Pts',(-16.1559070823762,-8.04468584505497,
974.258088235294));
#165475=CARTESIAN_POINT('Ctrl Pts',(-16.9013570056506,-6.54762058645456,
972.763970588235));
#165476=CARTESIAN_POINT('Ctrl Pts',(-17.3590292079831,-4.93906964482095,
971.269852941177));
#165477=CARTESIAN_POINT('Ctrl Pts',(-17.8167014103155,-3.33051870318735,
969.775735294118));
#165478=CARTESIAN_POINT('Ctrl Pts',(-17.9710104137728,-1.66525935159368,
968.281617647059));
#165479=CARTESIAN_POINT('Ctrl Pts',(-18.1253194172301,-1.10985572039171E-15,
966.7875));
#165480=CARTESIAN_POINT('Ctrl Pts',(-17.9710104137728,1.66525935159367,
965.293382352941));
#165481=CARTESIAN_POINT('Ctrl Pts',(-17.8167014103155,3.33051870318735,
963.799264705882));
#165482=CARTESIAN_POINT('Ctrl Pts',(-17.3590292079831,4.93906964482096,
962.305147058824));
#165483=CARTESIAN_POINT('Ctrl Pts',(-16.9013570056506,6.54762058645456,
960.811029411765));
#165484=CARTESIAN_POINT('Ctrl Pts',(-16.1559070823762,8.04468584505497,
959.316911764706));
#165485=CARTESIAN_POINT('Ctrl Pts',(-15.4104571591017,9.54175110365538,
957.822794117647));
#165486=CARTESIAN_POINT('Ctrl Pts',(-14.4026149179538,10.8763499173728,
956.328676470588));
#165487=CARTESIAN_POINT('Ctrl Pts',(-13.3947726768058,12.2109487310903,
954.834558823529));
#165488=CARTESIAN_POINT('Ctrl Pts',(-12.1588589765331,13.3376329379985,
953.340441176471));
#165489=CARTESIAN_POINT('Ctrl Pts',(-10.9229452762603,14.4643171449067,
951.846323529412));
#165490=CARTESIAN_POINT('Ctrl Pts',(-9.50104767561052,15.3447188656481,
950.352205882353));
#165491=CARTESIAN_POINT('Ctrl Pts',(-8.07915007496071,16.2251205863895,
948.858088235294));
#165492=CARTESIAN_POINT('Ctrl Pts',(-6.51968959134574,16.8292587962898,
947.363970588235));
#165493=CARTESIAN_POINT('Ctrl Pts',(-4.96022910773078,17.4333970061901,
945.869852941177));
#165494=CARTESIAN_POINT('Ctrl Pts',(-3.31631129755346,17.7406985030951,
944.375735294118));
#165495=CARTESIAN_POINT('Ctrl Pts',(-1.67239348737615,18.048,942.881617647059));
#165496=CARTESIAN_POINT('Ctrl Pts',(-2.21024254310115E-15,18.048,941.3875));
#165497=CARTESIAN_POINT('Ctrl Pts',(1.67239348737616,18.048,939.893382352941));
#165498=CARTESIAN_POINT('Ctrl Pts',(3.31631129755346,17.7406985030951,938.399264705882));
#165499=CARTESIAN_POINT('Ctrl Pts',(4.96022910773077,17.4333970061901,936.905147058824));
#165500=CARTESIAN_POINT('Ctrl Pts',(6.51968959134575,16.8292587962898,935.411029411765));
#165501=CARTESIAN_POINT('Ctrl Pts',(8.07915007496071,16.2251205863895,933.916911764706));
#165502=CARTESIAN_POINT('Ctrl Pts',(9.50104767561053,15.3447188656481,932.422794117647));
#165503=CARTESIAN_POINT('Ctrl Pts',(10.9229452762603,14.4643171449067,930.928676470588));
#165504=CARTESIAN_POINT('Ctrl Pts',(12.1588589765331,13.3376329379985,929.43455882353));
#165505=CARTESIAN_POINT('Ctrl Pts',(13.3947726768058,12.2109487310903,927.94044117647));
#165506=CARTESIAN_POINT('Ctrl Pts',(14.4026149179538,10.8763499173728,926.446323529412));
#165507=CARTESIAN_POINT('Ctrl Pts',(15.4104571591017,9.54175110365538,924.952205882353));
#165508=CARTESIAN_POINT('Ctrl Pts',(16.1559070823762,8.04468584505496,923.458088235294));
#165509=CARTESIAN_POINT('Ctrl Pts',(16.9013570056506,6.54762058645456,921.963970588235));
#165510=CARTESIAN_POINT('Ctrl Pts',(17.3590292079831,4.93906964482096,920.469852941176));
#165511=CARTESIAN_POINT('Ctrl Pts',(17.8167014103155,3.33051870318735,918.975735294118));
#165512=CARTESIAN_POINT('Ctrl Pts',(17.9710104137728,1.66525935159367,917.481617647059));
#165513=CARTESIAN_POINT('Ctrl Pts',(18.1253194172301,3.32956716117513E-15,
915.9875));
#165514=CARTESIAN_POINT('Ctrl Pts',(17.9710104137728,-1.66525935159367,
914.493382352941));
#165515=CARTESIAN_POINT('Ctrl Pts',(17.8167014103155,-3.33051870318736,
912.999264705882));
#165516=CARTESIAN_POINT('Ctrl Pts',(17.3590292079831,-4.93906964482095,
911.505147058824));
#165517=CARTESIAN_POINT('Ctrl Pts',(16.9013570056506,-6.54762058645456,
910.011029411765));
#165518=CARTESIAN_POINT('Ctrl Pts',(16.1559070823762,-8.04468584505497,
908.516911764706));
#165519=CARTESIAN_POINT('Ctrl Pts',(15.4104571591017,-9.54175110365538,
907.022794117647));
#165520=CARTESIAN_POINT('Ctrl Pts',(14.4026149179538,-10.8763499173728,
905.528676470588));
#165521=CARTESIAN_POINT('Ctrl Pts',(13.3947726768058,-12.2109487310903,
904.034558823529));
#165522=CARTESIAN_POINT('Ctrl Pts',(12.1588589765331,-13.3376329379985,
902.540441176471));
#165523=CARTESIAN_POINT('Ctrl Pts',(10.9229452762603,-14.4643171449067,
901.046323529412));
#165524=CARTESIAN_POINT('Ctrl Pts',(9.50104767561053,-15.3447188656481,
899.552205882353));
#165525=CARTESIAN_POINT('Ctrl Pts',(8.07915007496071,-16.2251205863895,
898.058088235294));
#165526=CARTESIAN_POINT('Ctrl Pts',(6.51968959134574,-16.8292587962898,
896.563970588235));
#165527=CARTESIAN_POINT('Ctrl Pts',(4.96022910773078,-17.4333970061901,
895.069852941177));
#165528=CARTESIAN_POINT('Ctrl Pts',(3.31631129755346,-17.7406985030951,
893.575735294118));
#165529=CARTESIAN_POINT('Ctrl Pts',(1.67239348737615,-18.048,892.081617647059));
#165530=CARTESIAN_POINT('Ctrl Pts',(0.,-18.048,890.5875));
#165531=CARTESIAN_POINT('Ctrl Pts',(-1.67239348737615,-18.048,889.093382352941));
#165532=CARTESIAN_POINT('Ctrl Pts',(-3.31631129755346,-17.7406985030951,
887.599264705882));
#165533=CARTESIAN_POINT('Ctrl Pts',(-4.96022910773077,-17.4333970061901,
886.105147058824));
#165534=CARTESIAN_POINT('Ctrl Pts',(-6.51968959134574,-16.8292587962898,
884.611029411765));
#165535=CARTESIAN_POINT('Ctrl Pts',(-8.07915007496071,-16.2251205863895,
883.116911764706));
#165536=CARTESIAN_POINT('Ctrl Pts',(-9.50104767561052,-15.3447188656481,
881.622794117647));
#165537=CARTESIAN_POINT('Ctrl Pts',(-10.9229452762603,-14.4643171449067,
880.128676470588));
#165538=CARTESIAN_POINT('Ctrl Pts',(-12.1588589765331,-13.3376329379985,
878.634558823529));
#165539=CARTESIAN_POINT('Ctrl Pts',(-13.3947726768058,-12.2109487310903,
877.140441176471));
#165540=CARTESIAN_POINT('Ctrl Pts',(-14.4026149179538,-10.8763499173728,
875.646323529412));
#165541=CARTESIAN_POINT('Ctrl Pts',(-15.4104571591017,-9.54175110365538,
874.152205882353));
#165542=CARTESIAN_POINT('Ctrl Pts',(-16.1559070823762,-8.04468584505497,
872.658088235294));
#165543=CARTESIAN_POINT('Ctrl Pts',(-16.9013570056506,-6.54762058645456,
871.163970588236));
#165544=CARTESIAN_POINT('Ctrl Pts',(-17.3590292079831,-4.93906964482095,
869.669852941176));
#165545=CARTESIAN_POINT('Ctrl Pts',(-17.8167014103155,-3.33051870318735,
868.175735294118));
#165546=CARTESIAN_POINT('Ctrl Pts',(-17.9710104137728,-1.66525935159368,
866.681617647059));
#165547=CARTESIAN_POINT('Ctrl Pts',(-18.1253194172301,-1.10985572039171E-15,
865.1875));
#165548=CARTESIAN_POINT('Ctrl Pts',(-17.9710104137728,1.66525935159367,
863.693382352941));
#165549=CARTESIAN_POINT('Ctrl Pts',(-17.8167014103155,3.33051870318735,
862.199264705883));
#165550=CARTESIAN_POINT('Ctrl Pts',(-17.3590292079831,4.93906964482096,
860.705147058824));
#165551=CARTESIAN_POINT('Ctrl Pts',(-16.9013570056506,6.54762058645456,
859.211029411765));
#165552=CARTESIAN_POINT('Ctrl Pts',(-16.1559070823762,8.04468584505497,
857.716911764706));
#165553=CARTESIAN_POINT('Ctrl Pts',(-15.4104571591017,9.54175110365538,
856.222794117647));
#165554=CARTESIAN_POINT('Ctrl Pts',(-14.4026149179538,10.8763499173728,
854.728676470588));
#165555=CARTESIAN_POINT('Ctrl Pts',(-13.3947726768058,12.2109487310903,
853.234558823529));
#165556=CARTESIAN_POINT('Ctrl Pts',(-12.1588589765331,13.3376329379985,
851.740441176471));
#165557=CARTESIAN_POINT('Ctrl Pts',(-10.9229452762603,14.4643171449067,
850.246323529412));
#165558=CARTESIAN_POINT('Ctrl Pts',(-9.50104767561052,15.3447188656481,
848.752205882353));
#165559=CARTESIAN_POINT('Ctrl Pts',(-8.07915007496071,16.2251205863895,
847.258088235294));
#165560=CARTESIAN_POINT('Ctrl Pts',(-6.51968959134574,16.8292587962898,
845.763970588235));
#165561=CARTESIAN_POINT('Ctrl Pts',(-4.96022910773078,17.4333970061901,
844.269852941177));
#165562=CARTESIAN_POINT('Ctrl Pts',(-3.31631129755346,17.7406985030951,
842.775735294118));
#165563=CARTESIAN_POINT('Ctrl Pts',(-1.67239348737615,18.048,841.281617647059));
#165564=CARTESIAN_POINT('Ctrl Pts',(-2.21024254310115E-15,18.048,839.7875));
#165565=CARTESIAN_POINT('Ctrl Pts',(1.67239348737616,18.048,838.293382352941));
#165566=CARTESIAN_POINT('Ctrl Pts',(3.31631129755346,17.7406985030951,836.799264705882));
#165567=CARTESIAN_POINT('Ctrl Pts',(4.96022910773077,17.4333970061901,835.305147058824));
#165568=CARTESIAN_POINT('Ctrl Pts',(6.51968959134575,16.8292587962898,833.811029411765));
#165569=CARTESIAN_POINT('Ctrl Pts',(8.07915007496071,16.2251205863895,832.316911764706));
#165570=CARTESIAN_POINT('Ctrl Pts',(9.50104767561053,15.3447188656481,830.822794117647));
#165571=CARTESIAN_POINT('Ctrl Pts',(10.9229452762603,14.4643171449067,829.328676470588));
#165572=CARTESIAN_POINT('Ctrl Pts',(12.1588589765331,13.3376329379985,827.834558823529));
#165573=CARTESIAN_POINT('Ctrl Pts',(13.3947726768058,12.2109487310903,826.340441176471));
#165574=CARTESIAN_POINT('Ctrl Pts',(14.4026149179538,10.8763499173728,824.846323529412));
#165575=CARTESIAN_POINT('Ctrl Pts',(15.4104571591017,9.54175110365538,823.352205882353));
#165576=CARTESIAN_POINT('Ctrl Pts',(16.1559070823762,8.04468584505496,821.858088235294));
#165577=CARTESIAN_POINT('Ctrl Pts',(16.9013570056506,6.54762058645456,820.363970588236));
#165578=CARTESIAN_POINT('Ctrl Pts',(17.3590292079831,4.93906964482096,818.869852941177));
#165579=CARTESIAN_POINT('Ctrl Pts',(17.8167014103155,3.33051870318735,817.375735294118));
#165580=CARTESIAN_POINT('Ctrl Pts',(17.9710104137728,1.66525935159367,815.881617647059));
#165581=CARTESIAN_POINT('Ctrl Pts',(18.1253194172301,3.32956716117513E-15,
814.3875));
#165582=CARTESIAN_POINT('Ctrl Pts',(17.9710104137728,-1.66525935159367,
812.893382352941));
#165583=CARTESIAN_POINT('Ctrl Pts',(17.8167014103155,-3.33051870318736,
811.399264705883));
#165584=CARTESIAN_POINT('Ctrl Pts',(17.3590292079831,-4.93906964482095,
809.905147058824));
#165585=CARTESIAN_POINT('Ctrl Pts',(16.9013570056506,-6.54762058645456,
808.411029411765));
#165586=CARTESIAN_POINT('Ctrl Pts',(16.1559070823762,-8.04468584505497,
806.916911764706));
#165587=CARTESIAN_POINT('Ctrl Pts',(15.4104571591017,-9.54175110365538,
805.422794117647));
#165588=CARTESIAN_POINT('Ctrl Pts',(14.4026149179538,-10.8763499173728,
803.928676470588));
#165589=CARTESIAN_POINT('Ctrl Pts',(13.3947726768058,-12.2109487310903,
802.434558823529));
#165590=CARTESIAN_POINT('Ctrl Pts',(12.1588589765331,-13.3376329379985,
800.940441176471));
#165591=CARTESIAN_POINT('Ctrl Pts',(10.9229452762603,-14.4643171449067,
799.446323529412));
#165592=CARTESIAN_POINT('Ctrl Pts',(9.50104767561053,-15.3447188656481,
797.952205882353));
#165593=CARTESIAN_POINT('Ctrl Pts',(8.07915007496071,-16.2251205863895,
796.458088235294));
#165594=CARTESIAN_POINT('Ctrl Pts',(6.51968959134574,-16.8292587962898,
794.963970588235));
#165595=CARTESIAN_POINT('Ctrl Pts',(4.96022910773078,-17.4333970061901,
793.469852941176));
#165596=CARTESIAN_POINT('Ctrl Pts',(3.31631129755346,-17.7406985030951,
791.975735294118));
#165597=CARTESIAN_POINT('Ctrl Pts',(1.67239348737615,-18.048,790.481617647059));
#165598=CARTESIAN_POINT('Ctrl Pts',(0.,-18.048,788.9875));
#165599=CARTESIAN_POINT('Ctrl Pts',(-1.67239348737615,-18.048,787.493382352941));
#165600=CARTESIAN_POINT('Ctrl Pts',(-3.31631129755346,-17.7406985030951,
785.999264705882));
#165601=CARTESIAN_POINT('Ctrl Pts',(-4.96022910773077,-17.4333970061901,
784.505147058824));
#165602=CARTESIAN_POINT('Ctrl Pts',(-6.51968959134574,-16.8292587962898,
783.011029411765));
#165603=CARTESIAN_POINT('Ctrl Pts',(-8.07915007496071,-16.2251205863895,
781.516911764706));
#165604=CARTESIAN_POINT('Ctrl Pts',(-9.50104767561052,-15.3447188656481,
780.022794117647));
#165605=CARTESIAN_POINT('Ctrl Pts',(-10.9229452762603,-14.4643171449067,
778.528676470588));
#165606=CARTESIAN_POINT('Ctrl Pts',(-12.1588589765331,-13.3376329379985,
777.03455882353));
#165607=CARTESIAN_POINT('Ctrl Pts',(-13.3947726768058,-12.2109487310903,
775.540441176471));
#165608=CARTESIAN_POINT('Ctrl Pts',(-14.4026149179538,-10.8763499173728,
774.046323529412));
#165609=CARTESIAN_POINT('Ctrl Pts',(-15.4104571591017,-9.54175110365538,
772.552205882353));
#165610=CARTESIAN_POINT('Ctrl Pts',(-16.1559070823762,-8.04468584505497,
771.058088235294));
#165611=CARTESIAN_POINT('Ctrl Pts',(-16.9013570056506,-6.54762058645456,
769.563970588235));
#165612=CARTESIAN_POINT('Ctrl Pts',(-17.3590292079831,-4.93906964482095,
768.069852941177));
#165613=CARTESIAN_POINT('Ctrl Pts',(-17.8167014103155,-3.33051870318735,
766.575735294118));
#165614=CARTESIAN_POINT('Ctrl Pts',(-17.9710104137728,-1.66525935159368,
765.081617647059));
#165615=CARTESIAN_POINT('Ctrl Pts',(-18.1253194172301,-1.10985572039171E-15,
763.5875));
#165616=CARTESIAN_POINT('Ctrl Pts',(-17.9710104137728,1.66525935159367,
762.093382352941));
#165617=CARTESIAN_POINT('Ctrl Pts',(-17.8167014103155,3.33051870318735,
760.599264705883));
#165618=CARTESIAN_POINT('Ctrl Pts',(-17.3590292079831,4.93906964482096,
759.105147058824));
#165619=CARTESIAN_POINT('Ctrl Pts',(-16.9013570056506,6.54762058645456,
757.611029411765));
#165620=CARTESIAN_POINT('Ctrl Pts',(-16.1559070823762,8.04468584505497,
756.116911764706));
#165621=CARTESIAN_POINT('Ctrl Pts',(-15.4104571591017,9.54175110365538,
754.622794117647));
#165622=CARTESIAN_POINT('Ctrl Pts',(-14.4026149179538,10.8763499173728,
753.128676470588));
#165623=CARTESIAN_POINT('Ctrl Pts',(-13.3947726768058,12.2109487310903,
751.634558823529));
#165624=CARTESIAN_POINT('Ctrl Pts',(-12.1588589765331,13.3376329379985,
750.140441176471));
#165625=CARTESIAN_POINT('Ctrl Pts',(-10.9229452762603,14.4643171449067,
748.646323529412));
#165626=CARTESIAN_POINT('Ctrl Pts',(-9.50104767561052,15.3447188656481,
747.152205882353));
#165627=CARTESIAN_POINT('Ctrl Pts',(-8.07915007496071,16.2251205863895,
745.658088235294));
#165628=CARTESIAN_POINT('Ctrl Pts',(-6.51968959134574,16.8292587962898,
744.163970588235));
#165629=CARTESIAN_POINT('Ctrl Pts',(-4.96022910773078,17.4333970061901,
742.669852941176));
#165630=CARTESIAN_POINT('Ctrl Pts',(-3.31631129755346,17.7406985030951,
741.175735294118));
#165631=CARTESIAN_POINT('Ctrl Pts',(-1.67239348737615,18.048,739.681617647059));
#165632=CARTESIAN_POINT('Ctrl Pts',(-2.21024254310115E-15,18.048,738.1875));
#165633=CARTESIAN_POINT('Ctrl Pts',(1.67239348737616,18.048,736.693382352941));
#165634=CARTESIAN_POINT('Ctrl Pts',(3.31631129755346,17.7406985030951,735.199264705882));
#165635=CARTESIAN_POINT('Ctrl Pts',(4.96022910773077,17.4333970061901,733.705147058824));
#165636=CARTESIAN_POINT('Ctrl Pts',(6.51968959134575,16.8292587962898,732.211029411765));
#165637=CARTESIAN_POINT('Ctrl Pts',(8.07915007496071,16.2251205863895,730.716911764706));
#165638=CARTESIAN_POINT('Ctrl Pts',(9.50104767561053,15.3447188656481,729.222794117647));
#165639=CARTESIAN_POINT('Ctrl Pts',(10.9229452762603,14.4643171449067,727.728676470588));
#165640=CARTESIAN_POINT('Ctrl Pts',(12.1588589765331,13.3376329379985,726.234558823529));
#165641=CARTESIAN_POINT('Ctrl Pts',(13.3947726768058,12.2109487310903,724.740441176471));
#165642=CARTESIAN_POINT('Ctrl Pts',(14.4026149179538,10.8763499173728,723.246323529412));
#165643=CARTESIAN_POINT('Ctrl Pts',(15.4104571591017,9.54175110365538,721.752205882353));
#165644=CARTESIAN_POINT('Ctrl Pts',(16.1559070823762,8.04468584505496,720.258088235294));
#165645=CARTESIAN_POINT('Ctrl Pts',(16.9013570056506,6.54762058645456,718.763970588235));
#165646=CARTESIAN_POINT('Ctrl Pts',(17.3590292079831,4.93906964482096,717.269852941177));
#165647=CARTESIAN_POINT('Ctrl Pts',(17.8167014103155,3.33051870318735,715.775735294118));
#165648=CARTESIAN_POINT('Ctrl Pts',(17.9710104137728,1.66525935159367,714.281617647059));
#165649=CARTESIAN_POINT('Ctrl Pts',(18.1253194172301,3.32956716117513E-15,
712.7875));
#165650=CARTESIAN_POINT('Ctrl Pts',(17.9710104137728,-1.66525935159367,
711.293382352941));
#165651=CARTESIAN_POINT('Ctrl Pts',(17.8167014103155,-3.33051870318736,
709.799264705883));
#165652=CARTESIAN_POINT('Ctrl Pts',(17.3590292079831,-4.93906964482095,
708.305147058824));
#165653=CARTESIAN_POINT('Ctrl Pts',(16.9013570056506,-6.54762058645456,
706.811029411765));
#165654=CARTESIAN_POINT('Ctrl Pts',(16.1559070823762,-8.04468584505497,
705.316911764706));
#165655=CARTESIAN_POINT('Ctrl Pts',(15.4104571591017,-9.54175110365538,
703.822794117647));
#165656=CARTESIAN_POINT('Ctrl Pts',(14.4026149179538,-10.8763499173728,
702.328676470588));
#165657=CARTESIAN_POINT('Ctrl Pts',(13.3947726768058,-12.2109487310903,
700.83455882353));
#165658=CARTESIAN_POINT('Ctrl Pts',(12.1588589765331,-13.3376329379985,
699.340441176471));
#165659=CARTESIAN_POINT('Ctrl Pts',(10.9229452762603,-14.4643171449067,
697.846323529412));
#165660=CARTESIAN_POINT('Ctrl Pts',(9.50104767561053,-15.3447188656481,
696.352205882353));
#165661=CARTESIAN_POINT('Ctrl Pts',(8.07915007496071,-16.2251205863895,
694.858088235294));
#165662=CARTESIAN_POINT('Ctrl Pts',(6.51968959134574,-16.8292587962898,
693.363970588235));
#165663=CARTESIAN_POINT('Ctrl Pts',(4.96022910773078,-17.4333970061901,
691.869852941177));
#165664=CARTESIAN_POINT('Ctrl Pts',(3.31631129755346,-17.7406985030951,
690.375735294118));
#165665=CARTESIAN_POINT('Ctrl Pts',(1.67239348737615,-18.048,688.881617647059));
#165666=CARTESIAN_POINT('Ctrl Pts',(0.,-18.048,687.3875));
#165667=CARTESIAN_POINT('Ctrl Pts',(-1.67239348737615,-18.048,685.893382352941));
#165668=CARTESIAN_POINT('Ctrl Pts',(-3.31631129755346,-17.7406985030951,
684.399264705883));
#165669=CARTESIAN_POINT('Ctrl Pts',(-4.96022910773077,-17.4333970061901,
682.905147058824));
#165670=CARTESIAN_POINT('Ctrl Pts',(-6.51968959134574,-16.8292587962898,
681.411029411765));
#165671=CARTESIAN_POINT('Ctrl Pts',(-8.07915007496071,-16.2251205863895,
679.916911764706));
#165672=CARTESIAN_POINT('Ctrl Pts',(-9.50104767561052,-15.3447188656481,
678.422794117647));
#165673=CARTESIAN_POINT('Ctrl Pts',(-10.9229452762603,-14.4643171449067,
676.928676470588));
#165674=CARTESIAN_POINT('Ctrl Pts',(-12.1588589765331,-13.3376329379985,
675.434558823529));
#165675=CARTESIAN_POINT('Ctrl Pts',(-13.3947726768058,-12.2109487310903,
673.940441176471));
#165676=CARTESIAN_POINT('Ctrl Pts',(-14.4026149179538,-10.8763499173728,
672.446323529412));
#165677=CARTESIAN_POINT('Ctrl Pts',(-15.4104571591017,-9.54175110365538,
670.952205882353));
#165678=CARTESIAN_POINT('Ctrl Pts',(-16.1559070823762,-8.04468584505497,
669.458088235294));
#165679=CARTESIAN_POINT('Ctrl Pts',(-16.9013570056506,-6.54762058645456,
667.963970588235));
#165680=CARTESIAN_POINT('Ctrl Pts',(-17.3590292079831,-4.93906964482095,
666.469852941176));
#165681=CARTESIAN_POINT('Ctrl Pts',(-17.8167014103155,-3.33051870318735,
664.975735294118));
#165682=CARTESIAN_POINT('Ctrl Pts',(-17.9710104137728,-1.66525935159368,
663.481617647059));
#165683=CARTESIAN_POINT('Ctrl Pts',(-18.1253194172301,-1.10985572039171E-15,
661.9875));
#165684=CARTESIAN_POINT('Ctrl Pts',(-17.9710104137728,1.66525935159367,
660.493382352941));
#165685=CARTESIAN_POINT('Ctrl Pts',(-17.8167014103155,3.33051870318735,
658.999264705882));
#165686=CARTESIAN_POINT('Ctrl Pts',(-17.3590292079831,4.93906964482096,
657.505147058824));
#165687=CARTESIAN_POINT('Ctrl Pts',(-16.9013570056506,6.54762058645456,
656.011029411765));
#165688=CARTESIAN_POINT('Ctrl Pts',(-16.1559070823762,8.04468584505497,
654.516911764706));
#165689=CARTESIAN_POINT('Ctrl Pts',(-15.4104571591017,9.54175110365538,
653.022794117647));
#165690=CARTESIAN_POINT('Ctrl Pts',(-14.4026149179538,10.8763499173728,
651.528676470588));
#165691=CARTESIAN_POINT('Ctrl Pts',(-13.3947726768058,12.2109487310903,
650.03455882353));
#165692=CARTESIAN_POINT('Ctrl Pts',(-12.1588589765331,13.3376329379985,
648.540441176471));
#165693=CARTESIAN_POINT('Ctrl Pts',(-10.9229452762603,14.4643171449067,
647.046323529412));
#165694=CARTESIAN_POINT('Ctrl Pts',(-9.50104767561052,15.3447188656481,
645.552205882353));
#165695=CARTESIAN_POINT('Ctrl Pts',(-8.07915007496071,16.2251205863895,
644.058088235294));
#165696=CARTESIAN_POINT('Ctrl Pts',(-6.51968959134574,16.8292587962898,
642.563970588235));
#165697=CARTESIAN_POINT('Ctrl Pts',(-4.96022910773078,17.4333970061901,
641.069852941176));
#165698=CARTESIAN_POINT('Ctrl Pts',(-3.31631129755346,17.7406985030951,
639.575735294118));
#165699=CARTESIAN_POINT('Ctrl Pts',(-1.67239348737615,18.048,638.081617647059));
#165700=CARTESIAN_POINT('Ctrl Pts',(-2.21024254310115E-15,18.048,636.5875));
#165701=CARTESIAN_POINT('Ctrl Pts',(1.67239348737616,18.048,635.093382352941));
#165702=CARTESIAN_POINT('Ctrl Pts',(3.31631129755346,17.7406985030951,633.599264705882));
#165703=CARTESIAN_POINT('Ctrl Pts',(4.96022910773077,17.4333970061901,632.105147058824));
#165704=CARTESIAN_POINT('Ctrl Pts',(6.51968959134575,16.8292587962898,630.611029411765));
#165705=CARTESIAN_POINT('Ctrl Pts',(8.07915007496071,16.2251205863895,629.116911764706));
#165706=CARTESIAN_POINT('Ctrl Pts',(9.50104767561053,15.3447188656481,627.622794117647));
#165707=CARTESIAN_POINT('Ctrl Pts',(10.9229452762603,14.4643171449067,626.128676470588));
#165708=CARTESIAN_POINT('Ctrl Pts',(12.1588589765331,13.3376329379985,624.634558823529));
#165709=CARTESIAN_POINT('Ctrl Pts',(13.3947726768058,12.2109487310903,623.140441176471));
#165710=CARTESIAN_POINT('Ctrl Pts',(14.4026149179538,10.8763499173728,621.646323529412));
#165711=CARTESIAN_POINT('Ctrl Pts',(15.4104571591017,9.54175110365538,620.152205882353));
#165712=CARTESIAN_POINT('Ctrl Pts',(16.1559070823762,8.04468584505496,618.658088235294));
#165713=CARTESIAN_POINT('Ctrl Pts',(16.9013570056506,6.54762058645456,617.163970588235));
#165714=CARTESIAN_POINT('Ctrl Pts',(17.3590292079831,4.93906964482096,615.669852941176));
#165715=CARTESIAN_POINT('Ctrl Pts',(17.8167014103155,3.33051870318735,614.175735294118));
#165716=CARTESIAN_POINT('Ctrl Pts',(17.9710104137728,1.66525935159367,612.681617647059));
#165717=CARTESIAN_POINT('Ctrl Pts',(18.1253194172301,3.32956716117513E-15,
611.1875));
#165718=CARTESIAN_POINT('Ctrl Pts',(17.9710104137728,-1.66525935159367,
609.693382352941));
#165719=CARTESIAN_POINT('Ctrl Pts',(17.8167014103155,-3.33051870318736,
608.199264705882));
#165720=CARTESIAN_POINT('Ctrl Pts',(17.3590292079831,-4.93906964482095,
606.705147058824));
#165721=CARTESIAN_POINT('Ctrl Pts',(16.9013570056506,-6.54762058645456,
605.211029411765));
#165722=CARTESIAN_POINT('Ctrl Pts',(16.1559070823762,-8.04468584505497,
603.716911764706));
#165723=CARTESIAN_POINT('Ctrl Pts',(15.4104571591017,-9.54175110365538,
602.222794117647));
#165724=CARTESIAN_POINT('Ctrl Pts',(14.4026149179538,-10.8763499173728,
600.728676470588));
#165725=CARTESIAN_POINT('Ctrl Pts',(13.3947726768058,-12.2109487310903,
599.23455882353));
#165726=CARTESIAN_POINT('Ctrl Pts',(12.1588589765331,-13.3376329379985,
597.740441176471));
#165727=CARTESIAN_POINT('Ctrl Pts',(10.9229452762603,-14.4643171449067,
596.246323529412));
#165728=CARTESIAN_POINT('Ctrl Pts',(9.50104767561053,-15.3447188656481,
594.752205882353));
#165729=CARTESIAN_POINT('Ctrl Pts',(8.07915007496071,-16.2251205863895,
593.258088235294));
#165730=CARTESIAN_POINT('Ctrl Pts',(6.51968959134574,-16.8292587962898,
591.763970588235));
#165731=CARTESIAN_POINT('Ctrl Pts',(4.96022910773078,-17.4333970061901,
590.269852941177));
#165732=CARTESIAN_POINT('Ctrl Pts',(3.31631129755346,-17.7406985030951,
588.775735294118));
#165733=CARTESIAN_POINT('Ctrl Pts',(1.67239348737615,-18.048,587.281617647059));
#165734=CARTESIAN_POINT('Ctrl Pts',(0.,-18.048,585.7875));
#165735=CARTESIAN_POINT('Ctrl Pts',(-1.67239348737615,-18.048,584.293382352941));
#165736=CARTESIAN_POINT('Ctrl Pts',(-3.31631129755346,-17.7406985030951,
582.799264705882));
#165737=CARTESIAN_POINT('Ctrl Pts',(-4.96022910773077,-17.4333970061901,
581.305147058824));
#165738=CARTESIAN_POINT('Ctrl Pts',(-6.51968959134574,-16.8292587962898,
579.811029411765));
#165739=CARTESIAN_POINT('Ctrl Pts',(-8.07915007496071,-16.2251205863895,
578.316911764706));
#165740=CARTESIAN_POINT('Ctrl Pts',(-9.50104767561052,-15.3447188656481,
576.822794117647));
#165741=CARTESIAN_POINT('Ctrl Pts',(-10.9229452762603,-14.4643171449067,
575.328676470588));
#165742=CARTESIAN_POINT('Ctrl Pts',(-12.1588589765331,-13.3376329379985,
573.834558823529));
#165743=CARTESIAN_POINT('Ctrl Pts',(-13.3947726768058,-12.2109487310903,
572.340441176471));
#165744=CARTESIAN_POINT('Ctrl Pts',(-14.4026149179538,-10.8763499173728,
570.846323529412));
#165745=CARTESIAN_POINT('Ctrl Pts',(-15.4104571591017,-9.54175110365538,
569.352205882353));
#165746=CARTESIAN_POINT('Ctrl Pts',(-16.1559070823762,-8.04468584505497,
567.858088235294));
#165747=CARTESIAN_POINT('Ctrl Pts',(-16.9013570056506,-6.54762058645456,
566.363970588235));
#165748=CARTESIAN_POINT('Ctrl Pts',(-17.3590292079831,-4.93906964482095,
564.869852941177));
#165749=CARTESIAN_POINT('Ctrl Pts',(-17.8167014103155,-3.33051870318735,
563.375735294118));
#165750=CARTESIAN_POINT('Ctrl Pts',(-17.9710104137728,-1.66525935159368,
561.881617647059));
#165751=CARTESIAN_POINT('Ctrl Pts',(-18.1253194172301,-1.10985572039171E-15,
560.3875));
#165752=CARTESIAN_POINT('Ctrl Pts',(-17.9710104137728,1.66525935159367,
558.893382352941));
#165753=CARTESIAN_POINT('Ctrl Pts',(-17.8167014103155,3.33051870318735,
557.399264705882));
#165754=CARTESIAN_POINT('Ctrl Pts',(-17.3590292079831,4.93906964482096,
555.905147058824));
#165755=CARTESIAN_POINT('Ctrl Pts',(-16.9013570056506,6.54762058645456,
554.411029411765));
#165756=CARTESIAN_POINT('Ctrl Pts',(-16.1559070823762,8.04468584505497,
552.916911764706));
#165757=CARTESIAN_POINT('Ctrl Pts',(-15.4104571591017,9.54175110365538,
551.422794117647));
#165758=CARTESIAN_POINT('Ctrl Pts',(-14.4026149179538,10.8763499173728,
549.928676470588));
#165759=CARTESIAN_POINT('Ctrl Pts',(-13.3947726768058,12.2109487310903,
548.43455882353));
#165760=CARTESIAN_POINT('Ctrl Pts',(-12.1588589765331,13.3376329379985,
546.940441176471));
#165761=CARTESIAN_POINT('Ctrl Pts',(-10.9229452762603,14.4643171449067,
545.446323529412));
#165762=CARTESIAN_POINT('Ctrl Pts',(-9.50104767561052,15.3447188656481,
543.952205882353));
#165763=CARTESIAN_POINT('Ctrl Pts',(-8.07915007496071,16.2251205863895,
542.458088235294));
#165764=CARTESIAN_POINT('Ctrl Pts',(-6.51968959134574,16.8292587962898,
540.963970588235));
#165765=CARTESIAN_POINT('Ctrl Pts',(-4.96022910773078,17.4333970061901,
539.469852941177));
#165766=CARTESIAN_POINT('Ctrl Pts',(-3.31631129755346,17.7406985030951,
537.975735294118));
#165767=CARTESIAN_POINT('Ctrl Pts',(-1.67239348737615,18.048,536.481617647059));
#165768=CARTESIAN_POINT('Ctrl Pts',(-2.21024254310115E-15,18.048,534.9875));
#165769=CARTESIAN_POINT('Ctrl Pts',(1.67239348737616,18.048,533.493382352941));
#165770=CARTESIAN_POINT('Ctrl Pts',(3.31631129755346,17.7406985030951,531.999264705882));
#165771=CARTESIAN_POINT('Ctrl Pts',(4.96022910773077,17.4333970061901,530.505147058824));
#165772=CARTESIAN_POINT('Ctrl Pts',(6.51968959134575,16.8292587962898,529.011029411765));
#165773=CARTESIAN_POINT('Ctrl Pts',(8.07915007496071,16.2251205863895,527.516911764706));
#165774=CARTESIAN_POINT('Ctrl Pts',(9.50104767561053,15.3447188656481,526.022794117647));
#165775=CARTESIAN_POINT('Ctrl Pts',(10.9229452762603,14.4643171449067,524.528676470588));
#165776=CARTESIAN_POINT('Ctrl Pts',(12.1588589765331,13.3376329379985,523.03455882353));
#165777=CARTESIAN_POINT('Ctrl Pts',(13.3947726768058,12.2109487310903,521.540441176471));
#165778=CARTESIAN_POINT('Ctrl Pts',(14.4026149179538,10.8763499173728,520.046323529412));
#165779=CARTESIAN_POINT('Ctrl Pts',(15.4104571591017,9.54175110365538,518.552205882353));
#165780=CARTESIAN_POINT('Ctrl Pts',(16.1559070823762,8.04468584505496,517.058088235294));
#165781=CARTESIAN_POINT('Ctrl Pts',(16.9013570056506,6.54762058645456,515.563970588235));
#165782=CARTESIAN_POINT('Ctrl Pts',(17.3590292079831,4.93906964482096,514.069852941176));
#165783=CARTESIAN_POINT('Ctrl Pts',(17.8167014103155,3.33051870318735,512.575735294118));
#165784=CARTESIAN_POINT('Ctrl Pts',(17.9710104137728,1.66525935159367,511.081617647059));
#165785=CARTESIAN_POINT('Ctrl Pts',(18.1253194172301,3.32956716117513E-15,
509.5875));
#165786=CARTESIAN_POINT('Ctrl Pts',(17.9710104137728,-1.66525935159367,
508.093382352941));
#165787=CARTESIAN_POINT('Ctrl Pts',(17.8167014103155,-3.33051870318736,
506.599264705882));
#165788=CARTESIAN_POINT('Ctrl Pts',(17.3590292079831,-4.93906964482095,
505.105147058824));
#165789=CARTESIAN_POINT('Ctrl Pts',(16.9013570056506,-6.54762058645456,
503.611029411765));
#165790=CARTESIAN_POINT('Ctrl Pts',(16.1559070823762,-8.04468584505497,
502.116911764706));
#165791=CARTESIAN_POINT('Ctrl Pts',(15.4104571591017,-9.54175110365538,
500.622794117647));
#165792=CARTESIAN_POINT('Ctrl Pts',(14.4026149179538,-10.8763499173728,
499.128676470588));
#165793=CARTESIAN_POINT('Ctrl Pts',(13.3947726768058,-12.2109487310903,
497.63455882353));
#165794=CARTESIAN_POINT('Ctrl Pts',(12.1588589765331,-13.3376329379985,
496.140441176471));
#165795=CARTESIAN_POINT('Ctrl Pts',(10.9229452762603,-14.4643171449067,
494.646323529412));
#165796=CARTESIAN_POINT('Ctrl Pts',(9.50104767561053,-15.3447188656481,
493.152205882353));
#165797=CARTESIAN_POINT('Ctrl Pts',(8.07915007496071,-16.2251205863895,
491.658088235294));
#165798=CARTESIAN_POINT('Ctrl Pts',(6.51968959134574,-16.8292587962898,
490.163970588235));
#165799=CARTESIAN_POINT('Ctrl Pts',(4.96022910773078,-17.4333970061901,
488.669852941177));
#165800=CARTESIAN_POINT('Ctrl Pts',(3.31631129755346,-17.7406985030951,
487.175735294118));
#165801=CARTESIAN_POINT('Ctrl Pts',(1.67239348737615,-18.048,485.681617647059));
#165802=CARTESIAN_POINT('Ctrl Pts',(0.,-18.048,484.1875));
#165803=CARTESIAN_POINT('Ctrl Pts',(-1.67239348737615,-18.048,482.693382352941));
#165804=CARTESIAN_POINT('Ctrl Pts',(-3.31631129755346,-17.7406985030951,
481.199264705882));
#165805=CARTESIAN_POINT('Ctrl Pts',(-4.96022910773077,-17.4333970061901,
479.705147058824));
#165806=CARTESIAN_POINT('Ctrl Pts',(-6.51968959134574,-16.8292587962898,
478.211029411765));
#165807=CARTESIAN_POINT('Ctrl Pts',(-8.07915007496071,-16.2251205863895,
476.716911764706));
#165808=CARTESIAN_POINT('Ctrl Pts',(-9.50104767561052,-15.3447188656481,
475.222794117647));
#165809=CARTESIAN_POINT('Ctrl Pts',(-10.9229452762603,-14.4643171449067,
473.728676470588));
#165810=CARTESIAN_POINT('Ctrl Pts',(-12.1588589765331,-13.3376329379985,
472.234558823529));
#165811=CARTESIAN_POINT('Ctrl Pts',(-13.3947726768058,-12.2109487310903,
470.740441176471));
#165812=CARTESIAN_POINT('Ctrl Pts',(-14.4026149179538,-10.8763499173728,
469.246323529412));
#165813=CARTESIAN_POINT('Ctrl Pts',(-15.4104571591017,-9.54175110365538,
467.752205882353));
#165814=CARTESIAN_POINT('Ctrl Pts',(-16.1559070823762,-8.04468584505497,
466.258088235294));
#165815=CARTESIAN_POINT('Ctrl Pts',(-16.9013570056506,-6.54762058645456,
464.763970588236));
#165816=CARTESIAN_POINT('Ctrl Pts',(-17.3590292079831,-4.93906964482095,
463.269852941177));
#165817=CARTESIAN_POINT('Ctrl Pts',(-17.8167014103155,-3.33051870318735,
461.775735294118));
#165818=CARTESIAN_POINT('Ctrl Pts',(-17.9710104137728,-1.66525935159368,
460.281617647059));
#165819=CARTESIAN_POINT('Ctrl Pts',(-18.1253194172301,-1.10985572039171E-15,
458.7875));
#165820=CARTESIAN_POINT('Ctrl Pts',(-17.9710104137728,1.66525935159367,
457.293382352941));
#165821=CARTESIAN_POINT('Ctrl Pts',(-17.8167014103155,3.33051870318735,
455.799264705882));
#165822=CARTESIAN_POINT('Ctrl Pts',(-17.3590292079831,4.93906964482096,
454.305147058824));
#165823=CARTESIAN_POINT('Ctrl Pts',(-16.9013570056506,6.54762058645456,
452.811029411765));
#165824=CARTESIAN_POINT('Ctrl Pts',(-16.1559070823762,8.04468584505497,
451.316911764706));
#165825=CARTESIAN_POINT('Ctrl Pts',(-15.4104571591017,9.54175110365538,
449.822794117647));
#165826=CARTESIAN_POINT('Ctrl Pts',(-14.4026149179538,10.8763499173728,
448.328676470588));
#165827=CARTESIAN_POINT('Ctrl Pts',(-13.3947726768058,12.2109487310903,
446.83455882353));
#165828=CARTESIAN_POINT('Ctrl Pts',(-12.1588589765331,13.3376329379985,
445.340441176471));
#165829=CARTESIAN_POINT('Ctrl Pts',(-10.9229452762603,14.4643171449067,
443.846323529412));
#165830=CARTESIAN_POINT('Ctrl Pts',(-9.50104767561052,15.3447188656481,
442.352205882353));
#165831=CARTESIAN_POINT('Ctrl Pts',(-8.07915007496071,16.2251205863895,
440.858088235294));
#165832=CARTESIAN_POINT('Ctrl Pts',(-6.51968959134574,16.8292587962898,
439.363970588235));
#165833=CARTESIAN_POINT('Ctrl Pts',(-4.96022910773078,17.4333970061901,
437.869852941176));
#165834=CARTESIAN_POINT('Ctrl Pts',(-3.31631129755346,17.7406985030951,
436.375735294118));
#165835=CARTESIAN_POINT('Ctrl Pts',(-1.67239348737615,18.048,434.881617647059));
#165836=CARTESIAN_POINT('Ctrl Pts',(-2.21024254310115E-15,18.048,433.3875));
#165837=CARTESIAN_POINT('Ctrl Pts',(1.67239348737616,18.048,431.893382352941));
#165838=CARTESIAN_POINT('Ctrl Pts',(3.31631129755346,17.7406985030951,430.399264705882));
#165839=CARTESIAN_POINT('Ctrl Pts',(4.96022910773077,17.4333970061901,428.905147058824));
#165840=CARTESIAN_POINT('Ctrl Pts',(6.51968959134575,16.8292587962898,427.411029411765));
#165841=CARTESIAN_POINT('Ctrl Pts',(8.07915007496071,16.2251205863895,425.916911764706));
#165842=CARTESIAN_POINT('Ctrl Pts',(9.50104767561053,15.3447188656481,424.422794117647));
#165843=CARTESIAN_POINT('Ctrl Pts',(10.9229452762603,14.4643171449067,422.928676470588));
#165844=CARTESIAN_POINT('Ctrl Pts',(12.1588589765331,13.3376329379985,421.43455882353));
#165845=CARTESIAN_POINT('Ctrl Pts',(13.3947726768058,12.2109487310903,419.940441176471));
#165846=CARTESIAN_POINT('Ctrl Pts',(14.4026149179538,10.8763499173728,418.446323529412));
#165847=CARTESIAN_POINT('Ctrl Pts',(15.4104571591017,9.54175110365538,416.952205882353));
#165848=CARTESIAN_POINT('Ctrl Pts',(16.1559070823762,8.04468584505496,415.458088235294));
#165849=CARTESIAN_POINT('Ctrl Pts',(16.9013570056506,6.54762058645456,413.963970588235));
#165850=CARTESIAN_POINT('Ctrl Pts',(17.3590292079831,4.93906964482096,412.469852941177));
#165851=CARTESIAN_POINT('Ctrl Pts',(17.8167014103155,3.33051870318735,410.975735294118));
#165852=CARTESIAN_POINT('Ctrl Pts',(17.9710104137728,1.66525935159367,409.481617647059));
#165853=CARTESIAN_POINT('Ctrl Pts',(18.1253194172301,3.32956716117513E-15,
407.9875));
#165854=CARTESIAN_POINT('Ctrl Pts',(17.9710104137728,-1.66525935159367,
406.493382352941));
#165855=CARTESIAN_POINT('Ctrl Pts',(17.8167014103155,-3.33051870318736,
404.999264705882));
#165856=CARTESIAN_POINT('Ctrl Pts',(17.3590292079831,-4.93906964482095,
403.505147058824));
#165857=CARTESIAN_POINT('Ctrl Pts',(16.9013570056506,-6.54762058645456,
402.011029411765));
#165858=CARTESIAN_POINT('Ctrl Pts',(16.1559070823762,-8.04468584505497,
400.516911764706));
#165859=CARTESIAN_POINT('Ctrl Pts',(15.4104571591017,-9.54175110365538,
399.022794117647));
#165860=CARTESIAN_POINT('Ctrl Pts',(14.4026149179538,-10.8763499173728,
397.528676470588));
#165861=CARTESIAN_POINT('Ctrl Pts',(13.3947726768058,-12.2109487310903,
396.034558823529));
#165862=CARTESIAN_POINT('Ctrl Pts',(12.1588589765331,-13.3376329379985,
394.540441176471));
#165863=CARTESIAN_POINT('Ctrl Pts',(10.9229452762603,-14.4643171449067,
393.046323529412));
#165864=CARTESIAN_POINT('Ctrl Pts',(9.50104767561053,-15.3447188656481,
391.552205882353));
#165865=CARTESIAN_POINT('Ctrl Pts',(8.07915007496071,-16.2251205863895,
390.058088235294));
#165866=CARTESIAN_POINT('Ctrl Pts',(6.51968959134574,-16.8292587962898,
388.563970588235));
#165867=CARTESIAN_POINT('Ctrl Pts',(4.96022910773078,-17.4333970061901,
387.069852941177));
#165868=CARTESIAN_POINT('Ctrl Pts',(3.31631129755346,-17.7406985030951,
385.575735294118));
#165869=CARTESIAN_POINT('Ctrl Pts',(1.67239348737615,-18.048,384.081617647059));
#165870=CARTESIAN_POINT('Ctrl Pts',(0.,-18.048,382.5875));
#165871=CARTESIAN_POINT('Ctrl Pts',(-1.67239348737615,-18.048,381.093382352941));
#165872=CARTESIAN_POINT('Ctrl Pts',(-3.31631129755346,-17.7406985030951,
379.599264705882));
#165873=CARTESIAN_POINT('Ctrl Pts',(-4.96022910773077,-17.4333970061901,
378.105147058823));
#165874=CARTESIAN_POINT('Ctrl Pts',(-6.51968959134574,-16.8292587962898,
376.611029411765));
#165875=CARTESIAN_POINT('Ctrl Pts',(-8.07915007496071,-16.2251205863895,
375.116911764706));
#165876=CARTESIAN_POINT('Ctrl Pts',(-9.50104767561052,-15.3447188656481,
373.622794117647));
#165877=CARTESIAN_POINT('Ctrl Pts',(-10.9229452762603,-14.4643171449067,
372.128676470588));
#165878=CARTESIAN_POINT('Ctrl Pts',(-12.1588589765331,-13.3376329379985,
370.634558823529));
#165879=CARTESIAN_POINT('Ctrl Pts',(-13.3947726768058,-12.2109487310903,
369.140441176471));
#165880=CARTESIAN_POINT('Ctrl Pts',(-14.4026149179538,-10.8763499173728,
367.646323529412));
#165881=CARTESIAN_POINT('Ctrl Pts',(-15.4104571591017,-9.54175110365538,
366.152205882353));
#165882=CARTESIAN_POINT('Ctrl Pts',(-16.1559070823762,-8.04468584505497,
364.658088235294));
#165883=CARTESIAN_POINT('Ctrl Pts',(-16.9013570056506,-6.54762058645456,
363.163970588235));
#165884=CARTESIAN_POINT('Ctrl Pts',(-17.3590292079831,-4.93906964482095,
361.669852941177));
#165885=CARTESIAN_POINT('Ctrl Pts',(-17.8167014103155,-3.33051870318735,
360.175735294118));
#165886=CARTESIAN_POINT('Ctrl Pts',(-17.9710104137728,-1.66525935159368,
358.681617647059));
#165887=CARTESIAN_POINT('Ctrl Pts',(-18.1253194172301,-1.10985572039171E-15,
357.1875));
#165888=CARTESIAN_POINT('Ctrl Pts',(-17.9710104137728,1.66525935159367,
355.693382352941));
#165889=CARTESIAN_POINT('Ctrl Pts',(-17.8167014103155,3.33051870318735,
354.199264705883));
#165890=CARTESIAN_POINT('Ctrl Pts',(-17.3590292079831,4.93906964482096,
352.705147058824));
#165891=CARTESIAN_POINT('Ctrl Pts',(-16.9013570056506,6.54762058645456,
351.211029411765));
#165892=CARTESIAN_POINT('Ctrl Pts',(-16.1559070823762,8.04468584505497,
349.716911764706));
#165893=CARTESIAN_POINT('Ctrl Pts',(-15.4104571591017,9.54175110365538,
348.222794117647));
#165894=CARTESIAN_POINT('Ctrl Pts',(-14.4026149179538,10.8763499173728,
346.728676470588));
#165895=CARTESIAN_POINT('Ctrl Pts',(-13.3947726768058,12.2109487310903,
345.234558823529));
#165896=CARTESIAN_POINT('Ctrl Pts',(-12.1588589765331,13.3376329379985,
343.740441176471));
#165897=CARTESIAN_POINT('Ctrl Pts',(-10.9229452762603,14.4643171449067,
342.246323529412));
#165898=CARTESIAN_POINT('Ctrl Pts',(-9.50104767561052,15.3447188656481,
340.752205882353));
#165899=CARTESIAN_POINT('Ctrl Pts',(-8.07915007496071,16.2251205863895,
339.258088235294));
#165900=CARTESIAN_POINT('Ctrl Pts',(-6.51968959134574,16.8292587962898,
337.763970588235));
#165901=CARTESIAN_POINT('Ctrl Pts',(-4.96022910773078,17.4333970061901,
336.269852941177));
#165902=CARTESIAN_POINT('Ctrl Pts',(-3.31631129755346,17.7406985030951,
334.775735294118));
#165903=CARTESIAN_POINT('Ctrl Pts',(-1.67239348737615,18.048,333.281617647059));
#165904=CARTESIAN_POINT('Ctrl Pts',(-2.21024254310115E-15,18.048,331.7875));
#165905=CARTESIAN_POINT('Ctrl Pts',(1.67239348737616,18.048,330.293382352941));
#165906=CARTESIAN_POINT('Ctrl Pts',(3.31631129755346,17.7406985030951,328.799264705882));
#165907=CARTESIAN_POINT('Ctrl Pts',(4.96022910773077,17.4333970061901,327.305147058824));
#165908=CARTESIAN_POINT('Ctrl Pts',(6.51968959134575,16.8292587962898,325.811029411765));
#165909=CARTESIAN_POINT('Ctrl Pts',(8.07915007496071,16.2251205863895,324.316911764706));
#165910=CARTESIAN_POINT('Ctrl Pts',(9.50104767561053,15.3447188656481,322.822794117647));
#165911=CARTESIAN_POINT('Ctrl Pts',(10.9229452762603,14.4643171449067,321.328676470588));
#165912=CARTESIAN_POINT('Ctrl Pts',(12.1588589765331,13.3376329379985,319.834558823529));
#165913=CARTESIAN_POINT('Ctrl Pts',(13.3947726768058,12.2109487310903,318.340441176471));
#165914=CARTESIAN_POINT('Ctrl Pts',(14.4026149179538,10.8763499173728,316.846323529412));
#165915=CARTESIAN_POINT('Ctrl Pts',(15.4104571591017,9.54175110365538,315.352205882353));
#165916=CARTESIAN_POINT('Ctrl Pts',(16.1559070823762,8.04468584505496,313.858088235294));
#165917=CARTESIAN_POINT('Ctrl Pts',(16.9013570056506,6.54762058645456,312.363970588235));
#165918=CARTESIAN_POINT('Ctrl Pts',(17.3590292079831,4.93906964482096,310.869852941176));
#165919=CARTESIAN_POINT('Ctrl Pts',(17.8167014103155,3.33051870318735,309.375735294118));
#165920=CARTESIAN_POINT('Ctrl Pts',(17.9710104137728,1.66525935159367,307.881617647059));
#165921=CARTESIAN_POINT('Ctrl Pts',(18.1253194172301,3.32956716117513E-15,
306.3875));
#165922=CARTESIAN_POINT('Ctrl Pts',(17.9710104137728,-1.66525935159367,
304.893382352941));
#165923=CARTESIAN_POINT('Ctrl Pts',(17.8167014103155,-3.33051870318736,
303.399264705882));
#165924=CARTESIAN_POINT('Ctrl Pts',(17.3590292079831,-4.93906964482095,
301.905147058824));
#165925=CARTESIAN_POINT('Ctrl Pts',(16.9013570056506,-6.54762058645456,
300.411029411765));
#165926=CARTESIAN_POINT('Ctrl Pts',(16.1559070823762,-8.04468584505497,
298.916911764706));
#165927=CARTESIAN_POINT('Ctrl Pts',(15.4104571591017,-9.54175110365538,
297.422794117647));
#165928=CARTESIAN_POINT('Ctrl Pts',(14.4026149179538,-10.8763499173728,
295.928676470588));
#165929=CARTESIAN_POINT('Ctrl Pts',(13.3947726768058,-12.2109487310903,
294.43455882353));
#165930=CARTESIAN_POINT('Ctrl Pts',(12.1588589765331,-13.3376329379985,
292.940441176471));
#165931=CARTESIAN_POINT('Ctrl Pts',(10.9229452762603,-14.4643171449067,
291.446323529412));
#165932=CARTESIAN_POINT('Ctrl Pts',(9.50104767561053,-15.3447188656481,
289.952205882353));
#165933=CARTESIAN_POINT('Ctrl Pts',(8.07915007496071,-16.2251205863895,
288.458088235294));
#165934=CARTESIAN_POINT('Ctrl Pts',(6.51968959134574,-16.8292587962898,
286.963970588235));
#165935=CARTESIAN_POINT('Ctrl Pts',(4.96022910773078,-17.4333970061901,
285.469852941177));
#165936=CARTESIAN_POINT('Ctrl Pts',(3.31631129755346,-17.7406985030951,
283.975735294118));
#165937=CARTESIAN_POINT('Ctrl Pts',(1.67239348737615,-18.048,282.481617647059));
#165938=CARTESIAN_POINT('Ctrl Pts',(0.,-18.048,280.9875));
#165939=CARTESIAN_POINT('Ctrl Pts',(-1.67239348737615,-18.048,279.493382352941));
#165940=CARTESIAN_POINT('Ctrl Pts',(-3.31631129755346,-17.7406985030951,
277.999264705882));
#165941=CARTESIAN_POINT('Ctrl Pts',(-4.96022910773077,-17.4333970061901,
276.505147058824));
#165942=CARTESIAN_POINT('Ctrl Pts',(-6.51968959134574,-16.8292587962898,
275.011029411765));
#165943=CARTESIAN_POINT('Ctrl Pts',(-8.07915007496071,-16.2251205863895,
273.516911764706));
#165944=CARTESIAN_POINT('Ctrl Pts',(-9.50104767561052,-15.3447188656481,
272.022794117647));
#165945=CARTESIAN_POINT('Ctrl Pts',(-10.9229452762603,-14.4643171449067,
270.528676470588));
#165946=CARTESIAN_POINT('Ctrl Pts',(-12.1588589765331,-13.3376329379985,
269.034558823529));
#165947=CARTESIAN_POINT('Ctrl Pts',(-13.3947726768058,-12.2109487310903,
267.540441176471));
#165948=CARTESIAN_POINT('Ctrl Pts',(-14.4026149179538,-10.8763499173728,
266.046323529412));
#165949=CARTESIAN_POINT('Ctrl Pts',(-15.4104571591017,-9.54175110365538,
264.552205882353));
#165950=CARTESIAN_POINT('Ctrl Pts',(-16.1559070823762,-8.04468584505497,
263.058088235294));
#165951=CARTESIAN_POINT('Ctrl Pts',(-16.9013570056506,-6.54762058645456,
261.563970588235));
#165952=CARTESIAN_POINT('Ctrl Pts',(-17.3590292079831,-4.93906964482095,
260.069852941176));
#165953=CARTESIAN_POINT('Ctrl Pts',(-17.8167014103155,-3.33051870318735,
258.575735294118));
#165954=CARTESIAN_POINT('Ctrl Pts',(-17.9710104137728,-1.66525935159368,
257.081617647059));
#165955=CARTESIAN_POINT('Ctrl Pts',(-18.1253194172301,-1.10985572039171E-15,
255.5875));
#165956=CARTESIAN_POINT('Ctrl Pts',(-17.9710104137728,1.66525935159367,
254.093382352941));
#165957=CARTESIAN_POINT('Ctrl Pts',(-17.8167014103155,3.33051870318735,
252.599264705882));
#165958=CARTESIAN_POINT('Ctrl Pts',(-17.3590292079831,4.93906964482096,
251.105147058823));
#165959=CARTESIAN_POINT('Ctrl Pts',(-16.9013570056506,6.54762058645456,
249.611029411765));
#165960=CARTESIAN_POINT('Ctrl Pts',(-16.1559070823762,8.04468584505497,
248.116911764706));
#165961=CARTESIAN_POINT('Ctrl Pts',(-15.4104571591017,9.54175110365538,
246.622794117647));
#165962=CARTESIAN_POINT('Ctrl Pts',(-14.4026149179538,10.8763499173728,
245.128676470588));
#165963=CARTESIAN_POINT('Ctrl Pts',(-13.3947726768058,12.2109487310903,
243.634558823529));
#165964=CARTESIAN_POINT('Ctrl Pts',(-12.1588589765331,13.3376329379985,
242.140441176471));
#165965=CARTESIAN_POINT('Ctrl Pts',(-10.9229452762603,14.4643171449067,
240.646323529412));
#165966=CARTESIAN_POINT('Ctrl Pts',(-9.50104767561052,15.3447188656481,
239.152205882353));
#165967=CARTESIAN_POINT('Ctrl Pts',(-8.07915007496071,16.2251205863895,
237.658088235294));
#165968=CARTESIAN_POINT('Ctrl Pts',(-6.51968959134574,16.8292587962898,
236.163970588235));
#165969=CARTESIAN_POINT('Ctrl Pts',(-4.96022910773078,17.4333970061901,
234.669852941177));
#165970=CARTESIAN_POINT('Ctrl Pts',(-3.31631129755346,17.7406985030951,
233.175735294118));
#165971=CARTESIAN_POINT('Ctrl Pts',(-1.67239348737615,18.048,231.681617647059));
#165972=CARTESIAN_POINT('Ctrl Pts',(-2.21024254310115E-15,18.048,230.1875));
#165973=CARTESIAN_POINT('Ctrl Pts',(1.67239348737616,18.048,228.693382352941));
#165974=CARTESIAN_POINT('Ctrl Pts',(3.31631129755346,17.7406985030951,227.199264705882));
#165975=CARTESIAN_POINT('Ctrl Pts',(4.96022910773077,17.4333970061901,225.705147058824));
#165976=CARTESIAN_POINT('Ctrl Pts',(6.51968959134575,16.8292587962898,224.211029411765));
#165977=CARTESIAN_POINT('Ctrl Pts',(8.07915007496071,16.2251205863895,222.716911764706));
#165978=CARTESIAN_POINT('Ctrl Pts',(9.50104767561053,15.3447188656481,221.222794117647));
#165979=CARTESIAN_POINT('Ctrl Pts',(10.9229452762603,14.4643171449067,219.728676470588));
#165980=CARTESIAN_POINT('Ctrl Pts',(12.1588589765331,13.3376329379985,218.234558823529));
#165981=CARTESIAN_POINT('Ctrl Pts',(13.3947726768058,12.2109487310903,216.740441176471));
#165982=CARTESIAN_POINT('Ctrl Pts',(14.4026149179538,10.8763499173728,215.246323529412));
#165983=CARTESIAN_POINT('Ctrl Pts',(15.4104571591017,9.54175110365538,213.752205882353));
#165984=CARTESIAN_POINT('Ctrl Pts',(16.1559070823762,8.04468584505496,212.258088235294));
#165985=CARTESIAN_POINT('Ctrl Pts',(16.9013570056506,6.54762058645456,210.763970588235));
#165986=CARTESIAN_POINT('Ctrl Pts',(17.3590292079831,4.93906964482096,209.269852941177));
#165987=CARTESIAN_POINT('Ctrl Pts',(17.8167014103155,3.33051870318735,207.775735294118));
#165988=CARTESIAN_POINT('Ctrl Pts',(17.9710104137728,1.66525935159367,206.281617647059));
#165989=CARTESIAN_POINT('Ctrl Pts',(18.1253194172301,3.32956716117513E-15,
204.7875));
#165990=CARTESIAN_POINT('Ctrl Pts',(17.9710104137728,-1.66525935159367,
203.293382352941));
#165991=CARTESIAN_POINT('Ctrl Pts',(17.8167014103155,-3.33051870318736,
201.799264705882));
#165992=CARTESIAN_POINT('Ctrl Pts',(17.3590292079831,-4.93906964482095,
200.305147058824));
#165993=CARTESIAN_POINT('Ctrl Pts',(16.9013570056506,-6.54762058645456,
198.811029411765));
#165994=CARTESIAN_POINT('Ctrl Pts',(16.1559070823762,-8.04468584505497,
197.316911764706));
#165995=CARTESIAN_POINT('Ctrl Pts',(15.4104571591017,-9.54175110365538,
195.822794117647));
#165996=CARTESIAN_POINT('Ctrl Pts',(14.4026149179538,-10.8763499173728,
194.328676470588));
#165997=CARTESIAN_POINT('Ctrl Pts',(13.3947726768058,-12.2109487310903,
192.834558823529));
#165998=CARTESIAN_POINT('Ctrl Pts',(12.1588589765331,-13.3376329379985,
191.340441176471));
#165999=CARTESIAN_POINT('Ctrl Pts',(10.9229452762603,-14.4643171449067,
189.846323529412));
#166000=CARTESIAN_POINT('Ctrl Pts',(9.50104767561053,-15.3447188656481,
188.352205882353));
#166001=CARTESIAN_POINT('Ctrl Pts',(8.07915007496071,-16.2251205863895,
186.858088235294));
#166002=CARTESIAN_POINT('Ctrl Pts',(6.51968959134574,-16.8292587962898,
185.363970588235));
#166003=CARTESIAN_POINT('Ctrl Pts',(4.96022910773078,-17.4333970061901,
183.869852941176));
#166004=CARTESIAN_POINT('Ctrl Pts',(3.31631129755346,-17.7406985030951,
182.375735294118));
#166005=CARTESIAN_POINT('Ctrl Pts',(1.67239348737615,-18.048,180.881617647059));
#166006=CARTESIAN_POINT('Ctrl Pts',(0.,-18.048,179.3875));
#166007=CARTESIAN_POINT('Ctrl Pts',(-1.67239348737615,-18.048,177.893382352941));
#166008=CARTESIAN_POINT('Ctrl Pts',(-3.31631129755346,-17.7406985030951,
176.399264705882));
#166009=CARTESIAN_POINT('Ctrl Pts',(-4.96022910773077,-17.4333970061901,
174.905147058824));
#166010=CARTESIAN_POINT('Ctrl Pts',(-6.51968959134574,-16.8292587962898,
173.411029411765));
#166011=CARTESIAN_POINT('Ctrl Pts',(-8.07915007496071,-16.2251205863895,
171.916911764706));
#166012=CARTESIAN_POINT('Ctrl Pts',(-9.50104767561052,-15.3447188656481,
170.422794117647));
#166013=CARTESIAN_POINT('Ctrl Pts',(-10.9229452762603,-14.4643171449067,
168.928676470588));
#166014=CARTESIAN_POINT('Ctrl Pts',(-12.1588589765331,-13.3376329379985,
167.43455882353));
#166015=CARTESIAN_POINT('Ctrl Pts',(-13.3947726768058,-12.2109487310903,
165.940441176471));
#166016=CARTESIAN_POINT('Ctrl Pts',(-14.4026149179538,-10.8763499173728,
164.446323529412));
#166017=CARTESIAN_POINT('Ctrl Pts',(-15.4104571591017,-9.54175110365538,
162.952205882353));
#166018=CARTESIAN_POINT('Ctrl Pts',(-16.1559070823762,-8.04468584505497,
161.458088235294));
#166019=CARTESIAN_POINT('Ctrl Pts',(-16.9013570056506,-6.54762058645456,
159.963970588235));
#166020=CARTESIAN_POINT('Ctrl Pts',(-17.3590292079831,-4.93906964482095,
158.469852941177));
#166021=CARTESIAN_POINT('Ctrl Pts',(-17.8167014103155,-3.33051870318735,
156.975735294118));
#166022=CARTESIAN_POINT('Ctrl Pts',(-17.9710104137728,-1.66525935159368,
155.481617647059));
#166023=CARTESIAN_POINT('Ctrl Pts',(-18.1253194172301,-1.10985572039171E-15,
153.9875));
#166024=CARTESIAN_POINT('Ctrl Pts',(-17.9710104137728,1.66525935159367,
152.493382352941));
#166025=CARTESIAN_POINT('Ctrl Pts',(-17.8167014103155,3.33051870318735,
150.999264705882));
#166026=CARTESIAN_POINT('Ctrl Pts',(-17.3590292079831,4.93906964482096,
149.505147058824));
#166027=CARTESIAN_POINT('Ctrl Pts',(-16.9013570056506,6.54762058645456,
148.011029411765));
#166028=CARTESIAN_POINT('Ctrl Pts',(-16.1559070823762,8.04468584505497,
146.516911764706));
#166029=CARTESIAN_POINT('Ctrl Pts',(-15.4104571591017,9.54175110365538,
145.022794117647));
#166030=CARTESIAN_POINT('Ctrl Pts',(-14.4026149179538,10.8763499173728,
143.528676470588));
#166031=CARTESIAN_POINT('Ctrl Pts',(-13.3947726768058,12.2109487310903,
142.034558823529));
#166032=CARTESIAN_POINT('Ctrl Pts',(-12.1588589765331,13.3376329379985,
140.540441176471));
#166033=CARTESIAN_POINT('Ctrl Pts',(-10.9229452762603,14.4643171449067,
139.046323529412));
#166034=CARTESIAN_POINT('Ctrl Pts',(-9.50104767561052,15.3447188656481,
137.552205882353));
#166035=CARTESIAN_POINT('Ctrl Pts',(-8.07915007496071,16.2251205863895,
136.058088235294));
#166036=CARTESIAN_POINT('Ctrl Pts',(-6.51968959134574,16.8292587962898,
134.563970588235));
#166037=CARTESIAN_POINT('Ctrl Pts',(-4.96022910773078,17.4333970061901,
133.069852941176));
#166038=CARTESIAN_POINT('Ctrl Pts',(-3.31631129755346,17.7406985030951,
131.575735294118));
#166039=CARTESIAN_POINT('Ctrl Pts',(-1.67239348737615,18.048,130.081617647059));
#166040=CARTESIAN_POINT('Ctrl Pts',(-2.21024254310115E-15,18.048,128.5875));
#166041=CARTESIAN_POINT('Ctrl Pts',(1.67239348737616,18.048,127.093382352941));
#166042=CARTESIAN_POINT('Ctrl Pts',(3.31631129755346,17.7406985030951,125.599264705882));
#166043=CARTESIAN_POINT('Ctrl Pts',(4.96022910773077,17.4333970061901,124.105147058824));
#166044=CARTESIAN_POINT('Ctrl Pts',(6.51968959134575,16.8292587962898,122.611029411765));
#166045=CARTESIAN_POINT('Ctrl Pts',(8.07915007496071,16.2251205863895,121.116911764706));
#166046=CARTESIAN_POINT('Ctrl Pts',(9.50104767561053,15.3447188656481,119.622794117647));
#166047=CARTESIAN_POINT('Ctrl Pts',(10.9229452762603,14.4643171449067,118.128676470588));
#166048=CARTESIAN_POINT('Ctrl Pts',(12.1588589765331,13.3376329379985,116.634558823529));
#166049=CARTESIAN_POINT('Ctrl Pts',(13.3947726768058,12.2109487310903,115.140441176471));
#166050=CARTESIAN_POINT('Ctrl Pts',(14.4026149179538,10.8763499173728,113.646323529412));
#166051=CARTESIAN_POINT('Ctrl Pts',(15.4104571591017,9.54175110365538,112.152205882353));
#166052=CARTESIAN_POINT('Ctrl Pts',(16.1559070823762,8.04468584505496,110.658088235294));
#166053=CARTESIAN_POINT('Ctrl Pts',(16.9013570056506,6.54762058645456,109.163970588235));
#166054=CARTESIAN_POINT('Ctrl Pts',(17.3590292079831,4.93906964482096,107.669852941177));
#166055=CARTESIAN_POINT('Ctrl Pts',(17.8167014103155,3.33051870318735,106.175735294118));
#166056=CARTESIAN_POINT('Ctrl Pts',(17.9710104137728,1.66525935159367,104.681617647059));
#166057=CARTESIAN_POINT('Ctrl Pts',(18.1253194172301,3.32956716117513E-15,
103.1875));
#166058=CARTESIAN_POINT('Ctrl Pts',(17.9710104137728,-1.66525935159367,
101.693382352941));
#166059=CARTESIAN_POINT('Ctrl Pts',(17.8167014103155,-3.33051870318736,
100.199264705882));
#166060=CARTESIAN_POINT('Ctrl Pts',(17.3590292079831,-4.93906964482095,
98.7051470588236));
#166061=CARTESIAN_POINT('Ctrl Pts',(16.9013570056506,-6.54762058645456,
97.2110294117647));
#166062=CARTESIAN_POINT('Ctrl Pts',(16.1559070823762,-8.04468584505497,
95.7169117647059));
#166063=CARTESIAN_POINT('Ctrl Pts',(15.4104571591017,-9.54175110365538,
94.222794117647));
#166064=CARTESIAN_POINT('Ctrl Pts',(14.4026149179538,-10.8763499173728,
92.7286764705884));
#166065=CARTESIAN_POINT('Ctrl Pts',(13.3947726768058,-12.2109487310903,
91.2345588235295));
#166066=CARTESIAN_POINT('Ctrl Pts',(12.1588589765331,-13.3376329379985,
89.7404411764706));
#166067=CARTESIAN_POINT('Ctrl Pts',(10.9229452762603,-14.4643171449067,
88.2463235294117));
#166068=CARTESIAN_POINT('Ctrl Pts',(9.50104767561053,-15.3447188656481,
86.7522058823529));
#166069=CARTESIAN_POINT('Ctrl Pts',(8.07915007496071,-16.2251205863895,
85.2580882352942));
#166070=CARTESIAN_POINT('Ctrl Pts',(6.51968959134574,-16.8292587962898,
83.7639705882354));
#166071=CARTESIAN_POINT('Ctrl Pts',(4.96022910773078,-17.4333970061901,
82.2698529411765));
#166072=CARTESIAN_POINT('Ctrl Pts',(3.31631129755346,-17.7406985030951,
80.7757352941176));
#166073=CARTESIAN_POINT('Ctrl Pts',(1.67239348737615,-18.048,79.2816176470588));
#166074=CARTESIAN_POINT('Ctrl Pts',(0.,-18.048,77.7875000000001));
#166075=CARTESIAN_POINT('Ctrl Pts',(-1.67239348737615,-18.048,76.2933823529413));
#166076=CARTESIAN_POINT('Ctrl Pts',(-3.31631129755346,-17.7406985030951,
74.7992647058824));
#166077=CARTESIAN_POINT('Ctrl Pts',(-4.96022910773077,-17.4333970061901,
73.3051470588235));
#166078=CARTESIAN_POINT('Ctrl Pts',(-6.51968959134574,-16.8292587962898,
71.8110294117647));
#166079=CARTESIAN_POINT('Ctrl Pts',(-8.07915007496071,-16.2251205863895,
70.316911764706));
#166080=CARTESIAN_POINT('Ctrl Pts',(-9.50104767561052,-15.3447188656481,
68.8227941176471));
#166081=CARTESIAN_POINT('Ctrl Pts',(-10.9229452762603,-14.4643171449067,
67.3286764705883));
#166082=CARTESIAN_POINT('Ctrl Pts',(-12.1588589765331,-13.3376329379985,
65.8345588235294));
#166083=CARTESIAN_POINT('Ctrl Pts',(-13.3947726768058,-12.2109487310903,
64.3404411764705));
#166084=CARTESIAN_POINT('Ctrl Pts',(-14.4026149179538,-10.8763499173728,
62.8463235294119));
#166085=CARTESIAN_POINT('Ctrl Pts',(-15.4104571591017,-9.54175110365538,
61.352205882353));
#166086=CARTESIAN_POINT('Ctrl Pts',(-16.1559070823762,-8.04468584505497,
59.8580882352941));
#166087=CARTESIAN_POINT('Ctrl Pts',(-16.9013570056506,-6.54762058645456,
58.3639705882353));
#166088=CARTESIAN_POINT('Ctrl Pts',(-17.3590292079831,-4.93906964482095,
56.8698529411764));
#166089=CARTESIAN_POINT('Ctrl Pts',(-17.8167014103155,-3.33051870318735,
55.3757352941178));
#166090=CARTESIAN_POINT('Ctrl Pts',(-17.9710104137728,-1.66525935159368,
53.8816176470589));
#166091=CARTESIAN_POINT('Ctrl Pts',(-18.1253194172301,-1.10985572039171E-15,
52.3875));
#166092=CARTESIAN_POINT('Ctrl Pts',(-17.9710104137728,1.66525935159367,
50.8933823529412));
#166093=CARTESIAN_POINT('Ctrl Pts',(-17.8167014103155,3.33051870318735,
49.3992647058823));
#166094=CARTESIAN_POINT('Ctrl Pts',(-17.3590292079831,4.93906964482096,
47.9051470588237));
#166095=CARTESIAN_POINT('Ctrl Pts',(-16.9013570056506,6.54762058645456,
46.4110294117648));
#166096=CARTESIAN_POINT('Ctrl Pts',(-16.1559070823762,8.04468584505497,
44.9169117647059));
#166097=CARTESIAN_POINT('Ctrl Pts',(-15.4104571591017,9.54175110365538,
43.422794117647));
#166098=CARTESIAN_POINT('Ctrl Pts',(-14.4026149179538,10.8763499173728,
41.9286764705882));
#166099=CARTESIAN_POINT('Ctrl Pts',(-13.3947726768058,12.2109487310903,
40.4345588235295));
#166100=CARTESIAN_POINT('Ctrl Pts',(-12.1588589765331,13.3376329379985,
38.9404411764707));
#166101=CARTESIAN_POINT('Ctrl Pts',(-10.9229452762603,14.4643171449067,
37.4463235294118));
#166102=CARTESIAN_POINT('Ctrl Pts',(-9.50104767561052,15.3447188656481,
35.9522058823529));
#166103=CARTESIAN_POINT('Ctrl Pts',(-8.07915007496071,16.2251205863895,
34.4580882352941));
#166104=CARTESIAN_POINT('Ctrl Pts',(-6.51968959134574,16.8292587962898,
32.9639705882354));
#166105=CARTESIAN_POINT('Ctrl Pts',(-4.96022910773078,17.4333970061901,
31.4698529411765));
#166106=CARTESIAN_POINT('Ctrl Pts',(-3.31631129755346,17.7406985030951,
29.9757352941177));
#166107=CARTESIAN_POINT('Ctrl Pts',(-1.67239348737615,18.048,28.4816176470588));
#166108=CARTESIAN_POINT('Ctrl Pts',(-2.21024254310115E-15,18.048,26.9874999999999));
#166109=CARTESIAN_POINT('Ctrl Pts',(1.67239348737616,18.048,25.4933823529413));
#166110=CARTESIAN_POINT('Ctrl Pts',(3.31631129755346,17.7406985030951,23.9992647058824));
#166111=CARTESIAN_POINT('Ctrl Pts',(4.96022910773077,17.4333970061901,22.5051470588236));
#166112=CARTESIAN_POINT('Ctrl Pts',(6.51968959134575,16.8292587962898,21.0110294117647));
#166113=CARTESIAN_POINT('Ctrl Pts',(8.07915007496071,16.2251205863895,19.5169117647058));
#166114=CARTESIAN_POINT('Ctrl Pts',(9.50104767561053,15.3447188656481,18.0227941176472));
#166115=CARTESIAN_POINT('Ctrl Pts',(10.9229452762603,14.4643171449067,16.5286764705883));
#166116=CARTESIAN_POINT('Ctrl Pts',(12.1588589765331,13.3376329379985,15.0345588235294));
#166117=CARTESIAN_POINT('Ctrl Pts',(13.3947726768058,12.2109487310903,13.5404411764706));
#166118=CARTESIAN_POINT('Ctrl Pts',(14.4026149179538,10.8763499173728,12.0463235294117));
#166119=CARTESIAN_POINT('Ctrl Pts',(15.4104571591017,9.54175110365538,10.5522058823531));
#166120=CARTESIAN_POINT('Ctrl Pts',(16.1559070823762,8.04468584505496,9.05808823529419));
#166121=CARTESIAN_POINT('Ctrl Pts',(16.9013570056506,6.54762058645456,7.56397058823533));
#166122=CARTESIAN_POINT('Ctrl Pts',(17.3590292079831,4.93906964482096,6.06985294117646));
#166123=CARTESIAN_POINT('Ctrl Pts',(17.8167014103155,3.33051870318735,4.57573529411759));
#166124=CARTESIAN_POINT('Ctrl Pts',(17.9710104137728,1.66525935159367,3.08161764705894));
#166125=CARTESIAN_POINT('Ctrl Pts',(18.1253194172301,3.32956716117513E-15,
1.58750000000007));
#166126=CARTESIAN_POINT('Ctrl Pts',(17.9710104137728,-1.66525935159367,
0.093382352941207));
#166127=CARTESIAN_POINT('Ctrl Pts',(17.8167014103155,-3.33051870318736,
-1.40073529411766));
#166128=CARTESIAN_POINT('Ctrl Pts',(17.3590292079831,-4.93906964482095,
-2.89485294117653));
#166129=CARTESIAN_POINT('Ctrl Pts',(16.9013570056506,-6.54762058645456,
-4.38897058823517));
#166130=CARTESIAN_POINT('Ctrl Pts',(16.1559070823762,-8.04468584505497,
-5.88308823529404));
#166131=CARTESIAN_POINT('Ctrl Pts',(15.4104571591017,-9.54175110365538,
-7.37720588235291));
#166132=CARTESIAN_POINT('Ctrl Pts',(14.4026149179538,-10.8763499173728,
-8.87132352941178));
#166133=CARTESIAN_POINT('Ctrl Pts',(13.3947726768058,-12.2109487310903,
-10.3654411764706));
#166134=CARTESIAN_POINT('Ctrl Pts',(12.1588589765331,-13.3376329379985,
-11.8595588235293));
#166135=CARTESIAN_POINT('Ctrl Pts',(10.9229452762603,-14.4643171449067,
-13.3536764705882));
#166136=CARTESIAN_POINT('Ctrl Pts',(9.50104767561053,-15.3447188656481,
-14.847794117647));
#166137=CARTESIAN_POINT('Ctrl Pts',(8.07915007496071,-16.2251205863895,
-16.3419117647059));
#166138=CARTESIAN_POINT('Ctrl Pts',(6.51968959134574,-16.8292587962898,
-17.8360294117648));
#166139=CARTESIAN_POINT('Ctrl Pts',(4.96022910773078,-17.4333970061901,
-19.3301470588234));
#166140=CARTESIAN_POINT('Ctrl Pts',(3.31631129755346,-17.7406985030951,
-20.8242647058823));
#166141=CARTESIAN_POINT('Ctrl Pts',(1.67239348737615,-18.048,-22.3183823529411));
#166142=CARTESIAN_POINT('Ctrl Pts',(0.,-18.048,-23.8125));
#166143=CARTESIAN_POINT('Ctrl Pts',(-1.67239348737615,-18.048,-25.3066176470589));
#166144=CARTESIAN_POINT('Ctrl Pts',(-3.31631129755346,-17.7406985030951,
-26.8007352941175));
#166145=CARTESIAN_POINT('Ctrl Pts',(-4.96022910773077,-17.4333970061901,
-28.2948529411764));
#166146=CARTESIAN_POINT('Ctrl Pts',(-6.51968959134574,-16.8292587962898,
-29.7889705882353));
#166147=CARTESIAN_POINT('Ctrl Pts',(-8.07915007496071,-16.2251205863895,
-31.2830882352941));
#166148=CARTESIAN_POINT('Ctrl Pts',(-9.50104767561052,-15.3447188656481,
-32.777205882353));
#166149=CARTESIAN_POINT('Ctrl Pts',(-10.9229452762603,-14.4643171449067,
-34.2713235294116));
#166150=CARTESIAN_POINT('Ctrl Pts',(-12.1588589765331,-13.3376329379985,
-35.7654411764705));
#166151=CARTESIAN_POINT('Ctrl Pts',(-13.3947726768058,-12.2109487310903,
-37.2595588235294));
#166152=CARTESIAN_POINT('Ctrl Pts',(-14.4026149179538,-10.8763499173728,
-38.7536764705882));
#166153=CARTESIAN_POINT('Ctrl Pts',(-15.4104571591017,-9.54175110365538,
-40.2477941176471));
#166154=CARTESIAN_POINT('Ctrl Pts',(-16.1559070823762,-8.04468584505497,
-41.7419117647058));
#166155=CARTESIAN_POINT('Ctrl Pts',(-16.9013570056506,-6.54762058645456,
-43.2360294117646));
#166156=CARTESIAN_POINT('Ctrl Pts',(-17.3590292079831,-4.93906964482095,
-44.7301470588235));
#166157=CARTESIAN_POINT('Ctrl Pts',(-17.8167014103155,-3.33051870318735,
-46.2242647058824));
#166158=CARTESIAN_POINT('Ctrl Pts',(-17.9710104137728,-1.66525935159368,
-47.7183823529412));
#166159=CARTESIAN_POINT('Ctrl Pts',(-18.1253194172301,-1.10985572039171E-15,
-49.2124999999999));
#166160=CARTESIAN_POINT('Ctrl Pts',(-17.9710104137728,1.66525935159367,
-50.7066176470587));
#166161=CARTESIAN_POINT('Ctrl Pts',(-17.8167014103155,3.33051870318735,
-52.2007352941176));
#166162=CARTESIAN_POINT('Ctrl Pts',(-17.3590292079831,4.93906964482096,
-53.6948529411765));
#166163=CARTESIAN_POINT('Ctrl Pts',(-16.9013570056506,6.54762058645456,
-55.1889705882354));
#166164=CARTESIAN_POINT('Ctrl Pts',(-16.1559070823762,8.04468584505497,
-56.683088235294));
#166165=CARTESIAN_POINT('Ctrl Pts',(-15.4104571591017,9.54175110365538,
-58.1772058823529));
#166166=CARTESIAN_POINT('Ctrl Pts',(-14.4026149179538,10.8763499173728,
-59.6713235294117));
#166167=CARTESIAN_POINT('Ctrl Pts',(-13.3947726768058,12.2109487310903,
-61.1654411764706));
#166168=CARTESIAN_POINT('Ctrl Pts',(-12.1588589765331,13.3376329379985,
-62.6595588235295));
#166169=CARTESIAN_POINT('Ctrl Pts',(-10.9229452762603,14.4643171449067,
-64.1536764705881));
#166170=CARTESIAN_POINT('Ctrl Pts',(-9.50104767561052,15.3447188656481,
-65.647794117647));
#166171=CARTESIAN_POINT('Ctrl Pts',(-8.07915007496071,16.2251205863895,
-67.1419117647059));
#166172=CARTESIAN_POINT('Ctrl Pts',(-6.51968959134574,16.8292587962898,
-68.6360294117647));
#166173=CARTESIAN_POINT('Ctrl Pts',(-4.96022910773078,17.4333970061901,
-70.1301470588236));
#166174=CARTESIAN_POINT('Ctrl Pts',(-3.31631129755346,17.7406985030951,
-71.6242647058822));
#166175=CARTESIAN_POINT('Ctrl Pts',(-1.67239348737615,18.048,-73.1183823529411));
#166176=CARTESIAN_POINT('Ctrl Pts',(-2.21024254310115E-15,18.048,-74.6125));
#166177=CARTESIAN_POINT('Ctrl Pts',(1.67239348737616,18.048,-76.1066176470589));
#166178=CARTESIAN_POINT('Ctrl Pts',(3.31631129755346,17.7406985030951,-77.6007352941177));
#166179=CARTESIAN_POINT('Ctrl Pts',(4.96022910773077,17.4333970061901,-79.0948529411764));
#166180=CARTESIAN_POINT('Ctrl Pts',(6.51968959134575,16.8292587962898,-80.5889705882352));
#166181=CARTESIAN_POINT('Ctrl Pts',(8.07915007496071,16.2251205863895,-82.0830882352941));
#166182=CARTESIAN_POINT('Ctrl Pts',(9.50104767561053,15.3447188656481,-83.577205882353));
#166183=CARTESIAN_POINT('Ctrl Pts',(10.9229452762603,14.4643171449067,-85.0713235294118));
#166184=CARTESIAN_POINT('Ctrl Pts',(12.1588589765331,13.3376329379985,-86.5654411764705));
#166185=CARTESIAN_POINT('Ctrl Pts',(13.3947726768058,12.2109487310903,-88.0595588235294));
#166186=CARTESIAN_POINT('Ctrl Pts',(14.4026149179538,10.8763499173728,-89.5536764705882));
#166187=CARTESIAN_POINT('Ctrl Pts',(15.4104571591017,9.54175110365538,-91.0477941176471));
#166188=CARTESIAN_POINT('Ctrl Pts',(16.1559070823762,8.04468584505496,-92.541911764706));
#166189=CARTESIAN_POINT('Ctrl Pts',(16.9013570056506,6.54762058645456,-94.0360294117646));
#166190=CARTESIAN_POINT('Ctrl Pts',(17.3590292079831,4.93906964482096,-95.5301470588235));
#166191=CARTESIAN_POINT('Ctrl Pts',(17.8167014103155,3.33051870318735,-97.0242647058824));
#166192=CARTESIAN_POINT('Ctrl Pts',(17.9710104137728,1.66525935159367,-98.5183823529412));
#166193=CARTESIAN_POINT('Ctrl Pts',(18.1253194172301,3.32956716117513E-15,
-100.0125));
#166194=CARTESIAN_POINT('Ctrl Pts',(17.9710104137728,-1.66525935159367,
-101.506617647059));
#166195=CARTESIAN_POINT('Ctrl Pts',(17.8167014103155,-3.33051870318736,
-103.000735294118));
#166196=CARTESIAN_POINT('Ctrl Pts',(17.3590292079831,-4.93906964482095,
-104.494852941176));
#166197=CARTESIAN_POINT('Ctrl Pts',(16.9013570056506,-6.54762058645456,
-105.988970588235));
#166198=CARTESIAN_POINT('Ctrl Pts',(16.1559070823762,-8.04468584505497,
-107.483088235294));
#166199=CARTESIAN_POINT('Ctrl Pts',(15.4104571591017,-9.54175110365538,
-108.977205882353));
#166200=CARTESIAN_POINT('Ctrl Pts',(14.4026149179538,-10.8763499173728,
-110.471323529412));
#166201=CARTESIAN_POINT('Ctrl Pts',(13.3947726768058,-12.2109487310903,
-111.965441176471));
#166202=CARTESIAN_POINT('Ctrl Pts',(12.1588589765331,-13.3376329379985,
-113.459558823529));
#166203=CARTESIAN_POINT('Ctrl Pts',(10.9229452762603,-14.4643171449067,
-114.953676470588));
#166204=CARTESIAN_POINT('Ctrl Pts',(9.50104767561053,-15.3447188656481,
-116.447794117647));
#166205=CARTESIAN_POINT('Ctrl Pts',(8.07915007496071,-16.2251205863895,
-117.941911764706));
#166206=CARTESIAN_POINT('Ctrl Pts',(6.51968959134574,-16.8292587962898,
-119.436029411765));
#166207=CARTESIAN_POINT('Ctrl Pts',(4.96022910773078,-17.4333970061901,
-120.930147058824));
#166208=CARTESIAN_POINT('Ctrl Pts',(3.31631129755346,-17.7406985030951,
-122.424264705882));
#166209=CARTESIAN_POINT('Ctrl Pts',(1.67239348737615,-18.048,-123.918382352941));
#166210=CARTESIAN_POINT('Ctrl Pts',(0.,-18.048,-125.4125));
#166211=CARTESIAN_POINT('Ctrl Pts',(-1.67239348737615,-18.048,-126.906617647059));
#166212=CARTESIAN_POINT('Ctrl Pts',(-3.31631129755346,-17.7406985030951,
-128.400735294118));
#166213=CARTESIAN_POINT('Ctrl Pts',(-4.96022910773077,-17.4333970061901,
-129.894852941177));
#166214=CARTESIAN_POINT('Ctrl Pts',(-6.51968959134574,-16.8292587962898,
-131.388970588235));
#166215=CARTESIAN_POINT('Ctrl Pts',(-8.07915007496071,-16.2251205863895,
-132.883088235294));
#166216=CARTESIAN_POINT('Ctrl Pts',(-9.50104767561052,-15.3447188656481,
-134.377205882353));
#166217=CARTESIAN_POINT('Ctrl Pts',(-10.9229452762603,-14.4643171449067,
-135.871323529412));
#166218=CARTESIAN_POINT('Ctrl Pts',(-12.1588589765331,-13.3376329379985,
-137.365441176471));
#166219=CARTESIAN_POINT('Ctrl Pts',(-13.3947726768058,-12.2109487310903,
-138.859558823529));
#166220=CARTESIAN_POINT('Ctrl Pts',(-14.4026149179538,-10.8763499173728,
-140.353676470588));
#166221=CARTESIAN_POINT('Ctrl Pts',(-15.4104571591017,-9.54175110365538,
-141.847794117647));
#166222=CARTESIAN_POINT('Ctrl Pts',(-16.1559070823762,-8.04468584505497,
-143.341911764706));
#166223=CARTESIAN_POINT('Ctrl Pts',(-16.9013570056506,-6.54762058645456,
-144.836029411765));
#166224=CARTESIAN_POINT('Ctrl Pts',(-17.3590292079831,-4.93906964482095,
-146.330147058823));
#166225=CARTESIAN_POINT('Ctrl Pts',(-17.8167014103155,-3.33051870318735,
-147.824264705882));
#166226=CARTESIAN_POINT('Ctrl Pts',(-17.9710104137728,-1.66525935159368,
-149.318382352941));
#166227=CARTESIAN_POINT('Ctrl Pts',(-18.1253194172301,-1.10985572039171E-15,
-150.8125));
#166228=CARTESIAN_POINT('Ctrl Pts',(-17.9710104137728,1.66525935159367,
-152.306617647059));
#166229=CARTESIAN_POINT('Ctrl Pts',(-17.8167014103155,3.33051870318735,
-153.800735294118));
#166230=CARTESIAN_POINT('Ctrl Pts',(-17.3590292079831,4.93906964482096,
-155.294852941176));
#166231=CARTESIAN_POINT('Ctrl Pts',(-16.9013570056506,6.54762058645456,
-156.788970588235));
#166232=CARTESIAN_POINT('Ctrl Pts',(-16.1559070823762,8.04468584505497,
-158.283088235294));
#166233=CARTESIAN_POINT('Ctrl Pts',(-15.4104571591017,9.54175110365538,
-159.777205882353));
#166234=CARTESIAN_POINT('Ctrl Pts',(-14.4026149179538,10.8763499173728,
-161.271323529412));
#166235=CARTESIAN_POINT('Ctrl Pts',(-13.3947726768058,12.2109487310903,
-162.765441176471));
#166236=CARTESIAN_POINT('Ctrl Pts',(-12.1588589765331,13.3376329379985,
-164.259558823529));
#166237=CARTESIAN_POINT('Ctrl Pts',(-10.9229452762603,14.4643171449067,
-165.753676470588));
#166238=CARTESIAN_POINT('Ctrl Pts',(-9.50104767561052,15.3447188656481,
-167.247794117647));
#166239=CARTESIAN_POINT('Ctrl Pts',(-8.07915007496071,16.2251205863895,
-168.741911764706));
#166240=CARTESIAN_POINT('Ctrl Pts',(-6.51968959134574,16.8292587962898,
-170.236029411765));
#166241=CARTESIAN_POINT('Ctrl Pts',(-4.96022910773078,17.4333970061901,
-171.730147058823));
#166242=CARTESIAN_POINT('Ctrl Pts',(-3.31631129755346,17.7406985030951,
-173.224264705882));
#166243=CARTESIAN_POINT('Ctrl Pts',(-1.67239348737615,18.048,-174.718382352941));
#166244=CARTESIAN_POINT('Ctrl Pts',(-2.21024254310115E-15,18.048,-176.2125));
#166245=CARTESIAN_POINT('Ctrl Pts',(1.67239348737616,18.048,-177.706617647059));
#166246=CARTESIAN_POINT('Ctrl Pts',(3.31631129755346,17.7406985030951,-179.200735294118));
#166247=CARTESIAN_POINT('Ctrl Pts',(4.96022910773077,17.4333970061901,-180.694852941176));
#166248=CARTESIAN_POINT('Ctrl Pts',(6.51968959134575,16.8292587962898,-182.188970588235));
#166249=CARTESIAN_POINT('Ctrl Pts',(8.07915007496071,16.2251205863895,-183.683088235294));
#166250=CARTESIAN_POINT('Ctrl Pts',(9.50104767561053,15.3447188656481,-185.177205882353));
#166251=CARTESIAN_POINT('Ctrl Pts',(10.9229452762603,14.4643171449067,-186.671323529412));
#166252=CARTESIAN_POINT('Ctrl Pts',(12.1588589765331,13.3376329379985,-188.165441176471));
#166253=CARTESIAN_POINT('Ctrl Pts',(13.3947726768058,12.2109487310903,-189.659558823529));
#166254=CARTESIAN_POINT('Ctrl Pts',(14.4026149179538,10.8763499173728,-191.153676470588));
#166255=CARTESIAN_POINT('Ctrl Pts',(15.4104571591017,9.54175110365538,-192.647794117647));
#166256=CARTESIAN_POINT('Ctrl Pts',(16.1559070823762,8.04468584505496,-194.141911764706));
#166257=CARTESIAN_POINT('Ctrl Pts',(16.9013570056506,6.54762058645456,-195.636029411765));
#166258=CARTESIAN_POINT('Ctrl Pts',(17.3590292079831,4.93906964482096,-197.130147058824));
#166259=CARTESIAN_POINT('Ctrl Pts',(17.8167014103155,3.33051870318735,-198.624264705882));
#166260=CARTESIAN_POINT('Ctrl Pts',(17.9710104137728,1.66525935159367,-200.118382352941));
#166261=CARTESIAN_POINT('Ctrl Pts',(18.1253194172301,3.32956716117513E-15,
-201.6125));
#166262=CARTESIAN_POINT('Ctrl Pts',(17.9710104137728,-1.66525935159367,
-203.106617647059));
#166263=CARTESIAN_POINT('Ctrl Pts',(17.8167014103155,-3.33051870318736,
-204.600735294118));
#166264=CARTESIAN_POINT('Ctrl Pts',(17.3590292079831,-4.93906964482095,
-206.094852941176));
#166265=CARTESIAN_POINT('Ctrl Pts',(16.9013570056506,-6.54762058645456,
-207.588970588235));
#166266=CARTESIAN_POINT('Ctrl Pts',(16.1559070823762,-8.04468584505497,
-209.083088235294));
#166267=CARTESIAN_POINT('Ctrl Pts',(15.4104571591017,-9.54175110365538,
-210.577205882353));
#166268=CARTESIAN_POINT('Ctrl Pts',(14.4026149179538,-10.8763499173728,
-212.071323529412));
#166269=CARTESIAN_POINT('Ctrl Pts',(13.3947726768058,-12.2109487310903,
-213.56544117647));
#166270=CARTESIAN_POINT('Ctrl Pts',(12.1588589765331,-13.3376329379985,
-215.059558823529));
#166271=CARTESIAN_POINT('Ctrl Pts',(10.9229452762603,-14.4643171449067,
-216.553676470588));
#166272=CARTESIAN_POINT('Ctrl Pts',(9.50104767561053,-15.3447188656481,
-218.047794117647));
#166273=CARTESIAN_POINT('Ctrl Pts',(8.07915007496071,-16.2251205863895,
-219.541911764706));
#166274=CARTESIAN_POINT('Ctrl Pts',(6.51968959134574,-16.8292587962898,
-221.036029411765));
#166275=CARTESIAN_POINT('Ctrl Pts',(4.96022910773078,-17.4333970061901,
-222.530147058823));
#166276=CARTESIAN_POINT('Ctrl Pts',(3.31631129755346,-17.7406985030951,
-224.024264705882));
#166277=CARTESIAN_POINT('Ctrl Pts',(1.67239348737615,-18.048,-225.518382352941));
#166278=CARTESIAN_POINT('Ctrl Pts',(0.,-18.048,-227.0125));
#166279=CARTESIAN_POINT('Ctrl Pts',(-1.67239348737615,-18.048,-228.506617647059));
#166280=CARTESIAN_POINT('Ctrl Pts',(-3.31631129755346,-17.7406985030951,
-230.000735294118));
#166281=CARTESIAN_POINT('Ctrl Pts',(-4.96022910773077,-17.4333970061901,
-231.494852941176));
#166282=CARTESIAN_POINT('Ctrl Pts',(-6.51968959134574,-16.8292587962898,
-232.988970588235));
#166283=CARTESIAN_POINT('Ctrl Pts',(-8.07915007496071,-16.2251205863895,
-234.483088235294));
#166284=CARTESIAN_POINT('Ctrl Pts',(-9.50104767561052,-15.3447188656481,
-235.977205882353));
#166285=CARTESIAN_POINT('Ctrl Pts',(-10.9229452762603,-14.4643171449067,
-237.471323529412));
#166286=CARTESIAN_POINT('Ctrl Pts',(-12.1588589765331,-13.3376329379985,
-238.965441176471));
#166287=CARTESIAN_POINT('Ctrl Pts',(-13.3947726768058,-12.2109487310903,
-240.459558823529));
#166288=CARTESIAN_POINT('Ctrl Pts',(-14.4026149179538,-10.8763499173728,
-241.953676470588));
#166289=CARTESIAN_POINT('Ctrl Pts',(-15.4104571591017,-9.54175110365538,
-243.447794117647));
#166290=CARTESIAN_POINT('Ctrl Pts',(-16.1559070823762,-8.04468584505497,
-244.941911764706));
#166291=CARTESIAN_POINT('Ctrl Pts',(-16.9013570056506,-6.54762058645456,
-246.436029411765));
#166292=CARTESIAN_POINT('Ctrl Pts',(-17.3590292079831,-4.93906964482095,
-247.930147058824));
#166293=CARTESIAN_POINT('Ctrl Pts',(-17.8167014103155,-3.33051870318735,
-249.424264705882));
#166294=CARTESIAN_POINT('Ctrl Pts',(-17.9710104137728,-1.66525935159368,
-250.918382352941));
#166295=CARTESIAN_POINT('Ctrl Pts',(-18.1253194172301,-1.10985572039171E-15,
-252.4125));
#166296=CARTESIAN_POINT('Ctrl Pts',(-17.9710104137728,1.66525935159367,
-253.906617647059));
#166297=CARTESIAN_POINT('Ctrl Pts',(-17.8167014103155,3.33051870318735,
-255.400735294118));
#166298=CARTESIAN_POINT('Ctrl Pts',(-17.3590292079831,4.93906964482096,
-256.894852941177));
#166299=CARTESIAN_POINT('Ctrl Pts',(-16.9013570056506,6.54762058645456,
-258.388970588235));
#166300=CARTESIAN_POINT('Ctrl Pts',(-16.1559070823762,8.04468584505497,
-259.883088235294));
#166301=CARTESIAN_POINT('Ctrl Pts',(-15.4104571591017,9.54175110365538,
-261.377205882353));
#166302=CARTESIAN_POINT('Ctrl Pts',(-14.4026149179538,10.8763499173728,
-262.871323529412));
#166303=CARTESIAN_POINT('Ctrl Pts',(-13.3947726768058,12.2109487310903,
-264.365441176471));
#166304=CARTESIAN_POINT('Ctrl Pts',(-12.1588589765331,13.3376329379985,
-265.859558823529));
#166305=CARTESIAN_POINT('Ctrl Pts',(-10.9229452762603,14.4643171449067,
-267.353676470588));
#166306=CARTESIAN_POINT('Ctrl Pts',(-9.50104767561052,15.3447188656481,
-268.847794117647));
#166307=CARTESIAN_POINT('Ctrl Pts',(-8.07915007496071,16.2251205863895,
-270.341911764706));
#166308=CARTESIAN_POINT('Ctrl Pts',(-6.51968959134574,16.8292587962898,
-271.836029411765));
#166309=CARTESIAN_POINT('Ctrl Pts',(-4.96022910773078,17.4333970061901,
-273.330147058823));
#166310=CARTESIAN_POINT('Ctrl Pts',(-3.31631129755346,17.7406985030951,
-274.824264705882));
#166311=CARTESIAN_POINT('Ctrl Pts',(-1.67239348737615,18.048,-276.318382352941));
#166312=CARTESIAN_POINT('Ctrl Pts',(-2.21024254310115E-15,18.048,-277.8125));
#166313=CARTESIAN_POINT('Ctrl Pts',(1.67239348737616,18.048,-279.306617647059));
#166314=CARTESIAN_POINT('Ctrl Pts',(3.31631129755346,17.7406985030951,-280.800735294118));
#166315=CARTESIAN_POINT('Ctrl Pts',(4.96022910773077,17.4333970061901,-282.294852941176));
#166316=CARTESIAN_POINT('Ctrl Pts',(6.51968959134575,16.8292587962898,-283.788970588235));
#166317=CARTESIAN_POINT('Ctrl Pts',(8.07915007496071,16.2251205863895,-285.283088235294));
#166318=CARTESIAN_POINT('Ctrl Pts',(9.50104767561053,15.3447188656481,-286.777205882353));
#166319=CARTESIAN_POINT('Ctrl Pts',(10.9229452762603,14.4643171449067,-288.271323529412));
#166320=CARTESIAN_POINT('Ctrl Pts',(12.1588589765331,13.3376329379985,-289.765441176471));
#166321=CARTESIAN_POINT('Ctrl Pts',(13.3947726768058,12.2109487310903,-291.259558823529));
#166322=CARTESIAN_POINT('Ctrl Pts',(14.4026149179538,10.8763499173728,-292.753676470588));
#166323=CARTESIAN_POINT('Ctrl Pts',(15.4104571591017,9.54175110365538,-294.247794117647));
#166324=CARTESIAN_POINT('Ctrl Pts',(16.1559070823762,8.04468584505496,-295.741911764706));
#166325=CARTESIAN_POINT('Ctrl Pts',(16.9013570056506,6.54762058645456,-297.236029411765));
#166326=CARTESIAN_POINT('Ctrl Pts',(17.3590292079831,4.93906964482096,-298.730147058823));
#166327=CARTESIAN_POINT('Ctrl Pts',(17.8167014103155,3.33051870318735,-300.224264705882));
#166328=CARTESIAN_POINT('Ctrl Pts',(17.9710104137728,1.66525935159367,-301.718382352941));
#166329=CARTESIAN_POINT('Ctrl Pts',(18.1253194172301,3.32956716117513E-15,
-303.2125));
#166330=CARTESIAN_POINT('Ctrl Pts',(17.9710104137728,-1.66525935159367,
-304.706617647059));
#166331=CARTESIAN_POINT('Ctrl Pts',(17.8167014103155,-3.33051870318736,
-306.200735294118));
#166332=CARTESIAN_POINT('Ctrl Pts',(17.3590292079831,-4.93906964482095,
-307.694852941176));
#166333=CARTESIAN_POINT('Ctrl Pts',(16.9013570056506,-6.54762058645456,
-309.188970588235));
#166334=CARTESIAN_POINT('Ctrl Pts',(16.1559070823762,-8.04468584505497,
-310.683088235294));
#166335=CARTESIAN_POINT('Ctrl Pts',(15.4104571591017,-9.54175110365538,
-312.177205882353));
#166336=CARTESIAN_POINT('Ctrl Pts',(14.4026149179538,-10.8763499173728,
-313.671323529412));
#166337=CARTESIAN_POINT('Ctrl Pts',(13.3947726768058,-12.2109487310903,
-315.165441176471));
#166338=CARTESIAN_POINT('Ctrl Pts',(12.1588589765331,-13.3376329379985,
-316.659558823529));
#166339=CARTESIAN_POINT('Ctrl Pts',(10.9229452762603,-14.4643171449067,
-318.153676470588));
#166340=CARTESIAN_POINT('Ctrl Pts',(9.50104767561053,-15.3447188656481,
-319.647794117647));
#166341=CARTESIAN_POINT('Ctrl Pts',(8.07915007496071,-16.2251205863895,
-321.141911764706));
#166342=CARTESIAN_POINT('Ctrl Pts',(6.51968959134574,-16.8292587962898,
-322.636029411765));
#166343=CARTESIAN_POINT('Ctrl Pts',(4.96022910773078,-17.4333970061901,
-324.130147058824));
#166344=CARTESIAN_POINT('Ctrl Pts',(3.31631129755346,-17.7406985030951,
-325.624264705882));
#166345=CARTESIAN_POINT('Ctrl Pts',(1.67239348737615,-18.048,-327.118382352941));
#166346=CARTESIAN_POINT('Ctrl Pts',(0.,-18.048,-328.6125));
#166347=CARTESIAN_POINT('Ctrl Pts',(-1.67239348737615,-18.048,-330.106617647059));
#166348=CARTESIAN_POINT('Ctrl Pts',(-3.31631129755346,-17.7406985030951,
-331.600735294118));
#166349=CARTESIAN_POINT('Ctrl Pts',(-4.96022910773077,-17.4333970061901,
-333.094852941176));
#166350=CARTESIAN_POINT('Ctrl Pts',(-6.51968959134574,-16.8292587962898,
-334.588970588235));
#166351=CARTESIAN_POINT('Ctrl Pts',(-8.07915007496071,-16.2251205863895,
-336.083088235294));
#166352=CARTESIAN_POINT('Ctrl Pts',(-9.50104767561052,-15.3447188656481,
-337.577205882353));
#166353=CARTESIAN_POINT('Ctrl Pts',(-10.9229452762603,-14.4643171449067,
-339.071323529412));
#166354=CARTESIAN_POINT('Ctrl Pts',(-12.1588589765331,-13.3376329379985,
-340.56544117647));
#166355=CARTESIAN_POINT('Ctrl Pts',(-13.3947726768058,-12.2109487310903,
-342.059558823529));
#166356=CARTESIAN_POINT('Ctrl Pts',(-14.4026149179538,-10.8763499173728,
-343.553676470588));
#166357=CARTESIAN_POINT('Ctrl Pts',(-15.4104571591017,-9.54175110365538,
-345.047794117647));
#166358=CARTESIAN_POINT('Ctrl Pts',(-16.1559070823762,-8.04468584505497,
-346.541911764706));
#166359=CARTESIAN_POINT('Ctrl Pts',(-16.9013570056506,-6.54762058645456,
-348.036029411765));
#166360=CARTESIAN_POINT('Ctrl Pts',(-17.3590292079831,-4.93906964482095,
-349.530147058823));
#166361=CARTESIAN_POINT('Ctrl Pts',(-17.8167014103155,-3.33051870318735,
-351.024264705883));
#166362=CARTESIAN_POINT('Ctrl Pts',(-17.9710104137728,-1.66525935159368,
-352.518382352941));
#166363=CARTESIAN_POINT('Ctrl Pts',(-18.1253194172301,-1.10985572039171E-15,
-354.0125));
#166364=CARTESIAN_POINT('Ctrl Pts',(-17.9710104137728,1.66525935159367,
-355.506617647059));
#166365=CARTESIAN_POINT('Ctrl Pts',(-17.8167014103155,3.33051870318735,
-357.000735294118));
#166366=CARTESIAN_POINT('Ctrl Pts',(-17.3590292079831,4.93906964482096,
-358.494852941176));
#166367=CARTESIAN_POINT('Ctrl Pts',(-16.9013570056506,6.54762058645456,
-359.988970588235));
#166368=CARTESIAN_POINT('Ctrl Pts',(-16.1559070823762,8.04468584505497,
-361.483088235294));
#166369=CARTESIAN_POINT('Ctrl Pts',(-15.4104571591017,9.54175110365538,
-362.977205882353));
#166370=CARTESIAN_POINT('Ctrl Pts',(-14.4026149179538,10.8763499173728,
-364.471323529412));
#166371=CARTESIAN_POINT('Ctrl Pts',(-13.3947726768058,12.2109487310903,
-365.965441176471));
#166372=CARTESIAN_POINT('Ctrl Pts',(-12.1588589765331,13.3376329379985,
-367.459558823529));
#166373=CARTESIAN_POINT('Ctrl Pts',(-10.9229452762603,14.4643171449067,
-368.953676470588));
#166374=CARTESIAN_POINT('Ctrl Pts',(-9.50104767561052,15.3447188656481,
-370.447794117647));
#166375=CARTESIAN_POINT('Ctrl Pts',(-8.07915007496071,16.2251205863895,
-371.941911764706));
#166376=CARTESIAN_POINT('Ctrl Pts',(-6.51968959134574,16.8292587962898,
-373.436029411765));
#166377=CARTESIAN_POINT('Ctrl Pts',(-4.96022910773078,17.4333970061901,
-374.930147058824));
#166378=CARTESIAN_POINT('Ctrl Pts',(-3.31631129755346,17.7406985030951,
-376.424264705882));
#166379=CARTESIAN_POINT('Ctrl Pts',(-1.67239348737615,18.048,-377.918382352941));
#166380=CARTESIAN_POINT('Ctrl Pts',(-2.21024254310115E-15,18.048,-379.4125));
#166381=CARTESIAN_POINT('Ctrl Pts',(1.67239348737616,18.048,-380.906617647059));
#166382=CARTESIAN_POINT('Ctrl Pts',(3.31631129755346,17.7406985030951,-382.400735294118));
#166383=CARTESIAN_POINT('Ctrl Pts',(4.96022910773077,17.4333970061901,-383.894852941177));
#166384=CARTESIAN_POINT('Ctrl Pts',(6.51968959134575,16.8292587962898,-385.388970588235));
#166385=CARTESIAN_POINT('Ctrl Pts',(8.07915007496071,16.2251205863895,-386.883088235294));
#166386=CARTESIAN_POINT('Ctrl Pts',(9.50104767561053,15.3447188656481,-388.377205882353));
#166387=CARTESIAN_POINT('Ctrl Pts',(10.9229452762603,14.4643171449067,-389.871323529412));
#166388=CARTESIAN_POINT('Ctrl Pts',(12.1588589765331,13.3376329379985,-391.365441176471));
#166389=CARTESIAN_POINT('Ctrl Pts',(13.3947726768058,12.2109487310903,-392.859558823529));
#166390=CARTESIAN_POINT('Ctrl Pts',(14.4026149179538,10.8763499173728,-394.353676470588));
#166391=CARTESIAN_POINT('Ctrl Pts',(15.4104571591017,9.54175110365538,-395.847794117647));
#166392=CARTESIAN_POINT('Ctrl Pts',(16.1559070823762,8.04468584505496,-397.341911764706));
#166393=CARTESIAN_POINT('Ctrl Pts',(16.9013570056506,6.54762058645456,-398.836029411765));
#166394=CARTESIAN_POINT('Ctrl Pts',(17.3590292079831,4.93906964482096,-400.330147058823));
#166395=CARTESIAN_POINT('Ctrl Pts',(17.8167014103155,3.33051870318735,-401.824264705882));
#166396=CARTESIAN_POINT('Ctrl Pts',(17.9710104137728,1.66525935159367,-403.318382352941));
#166397=CARTESIAN_POINT('Ctrl Pts',(18.1253194172301,3.32956716117513E-15,
-404.8125));
#166398=CARTESIAN_POINT('Ctrl Pts',(17.9710104137728,-1.66525935159367,
-406.306617647059));
#166399=CARTESIAN_POINT('Ctrl Pts',(17.8167014103155,-3.33051870318736,
-407.800735294118));
#166400=CARTESIAN_POINT('Ctrl Pts',(17.3590292079831,-4.93906964482095,
-409.294852941176));
#166401=CARTESIAN_POINT('Ctrl Pts',(16.9013570056506,-6.54762058645456,
-410.788970588235));
#166402=CARTESIAN_POINT('Ctrl Pts',(16.1559070823762,-8.04468584505497,
-412.283088235294));
#166403=CARTESIAN_POINT('Ctrl Pts',(15.4104571591017,-9.54175110365538,
-413.777205882353));
#166404=CARTESIAN_POINT('Ctrl Pts',(14.4026149179538,-10.8763499173728,
-415.271323529412));
#166405=CARTESIAN_POINT('Ctrl Pts',(13.3947726768058,-12.2109487310903,
-416.765441176471));
#166406=CARTESIAN_POINT('Ctrl Pts',(12.1588589765331,-13.3376329379985,
-418.259558823529));
#166407=CARTESIAN_POINT('Ctrl Pts',(10.9229452762603,-14.4643171449067,
-419.753676470588));
#166408=CARTESIAN_POINT('Ctrl Pts',(9.50104767561053,-15.3447188656481,
-421.247794117647));
#166409=CARTESIAN_POINT('Ctrl Pts',(8.07915007496071,-16.2251205863895,
-422.741911764706));
#166410=CARTESIAN_POINT('Ctrl Pts',(6.51968959134574,-16.8292587962898,
-424.236029411765));
#166411=CARTESIAN_POINT('Ctrl Pts',(4.96022910773078,-17.4333970061901,
-425.730147058824));
#166412=CARTESIAN_POINT('Ctrl Pts',(3.31631129755346,-17.7406985030951,
-427.224264705882));
#166413=CARTESIAN_POINT('Ctrl Pts',(1.67239348737615,-18.048,-428.718382352941));
#166414=CARTESIAN_POINT('Ctrl Pts',(0.,-18.048,-430.2125));
#166415=CARTESIAN_POINT('Ctrl Pts',(-1.67239348737615,-18.048,-431.706617647059));
#166416=CARTESIAN_POINT('Ctrl Pts',(-3.31631129755346,-17.7406985030951,
-433.200735294118));
#166417=CARTESIAN_POINT('Ctrl Pts',(-4.96022910773077,-17.4333970061901,
-434.694852941176));
#166418=CARTESIAN_POINT('Ctrl Pts',(-6.51968959134574,-16.8292587962898,
-436.188970588235));
#166419=CARTESIAN_POINT('Ctrl Pts',(-8.07915007496071,-16.2251205863895,
-437.683088235294));
#166420=CARTESIAN_POINT('Ctrl Pts',(-9.50104767561052,-15.3447188656481,
-439.177205882353));
#166421=CARTESIAN_POINT('Ctrl Pts',(-10.9229452762603,-14.4643171449067,
-440.671323529412));
#166422=CARTESIAN_POINT('Ctrl Pts',(-12.1588589765331,-13.3376329379985,
-442.165441176471));
#166423=CARTESIAN_POINT('Ctrl Pts',(-13.3947726768058,-12.2109487310903,
-443.65955882353));
#166424=CARTESIAN_POINT('Ctrl Pts',(-14.4026149179538,-10.8763499173728,
-445.153676470588));
#166425=CARTESIAN_POINT('Ctrl Pts',(-15.4104571591017,-9.54175110365538,
-446.647794117647));
#166426=CARTESIAN_POINT('Ctrl Pts',(-16.1559070823762,-8.04468584505497,
-448.141911764706));
#166427=CARTESIAN_POINT('Ctrl Pts',(-16.9013570056506,-6.54762058645456,
-449.636029411765));
#166428=CARTESIAN_POINT('Ctrl Pts',(-17.3590292079831,-4.93906964482095,
-451.130147058824));
#166429=CARTESIAN_POINT('Ctrl Pts',(-17.8167014103155,-3.33051870318735,
-452.624264705882));
#166430=CARTESIAN_POINT('Ctrl Pts',(-17.9710104137728,-1.66525935159368,
-454.118382352941));
#166431=CARTESIAN_POINT('Ctrl Pts',(-18.1253194172301,-1.10985572039171E-15,
-455.6125));
#166432=CARTESIAN_POINT('Ctrl Pts',(-17.9710104137728,1.66525935159367,
-457.106617647059));
#166433=CARTESIAN_POINT('Ctrl Pts',(-17.8167014103155,3.33051870318735,
-458.600735294118));
#166434=CARTESIAN_POINT('Ctrl Pts',(-17.3590292079831,4.93906964482096,
-460.094852941176));
#166435=CARTESIAN_POINT('Ctrl Pts',(-16.9013570056506,6.54762058645456,
-461.588970588235));
#166436=CARTESIAN_POINT('Ctrl Pts',(-16.1559070823762,8.04468584505497,
-463.083088235294));
#166437=CARTESIAN_POINT('Ctrl Pts',(-15.4104571591017,9.54175110365538,
-464.577205882353));
#166438=CARTESIAN_POINT('Ctrl Pts',(-14.4026149179538,10.8763499173728,
-466.071323529412));
#166439=CARTESIAN_POINT('Ctrl Pts',(-13.3947726768058,12.2109487310903,
-467.565441176471));
#166440=CARTESIAN_POINT('Ctrl Pts',(-12.1588589765331,13.3376329379985,
-469.059558823529));
#166441=CARTESIAN_POINT('Ctrl Pts',(-10.9229452762603,14.4643171449067,
-470.553676470588));
#166442=CARTESIAN_POINT('Ctrl Pts',(-9.50104767561052,15.3447188656481,
-472.047794117647));
#166443=CARTESIAN_POINT('Ctrl Pts',(-8.07915007496071,16.2251205863895,
-473.541911764706));
#166444=CARTESIAN_POINT('Ctrl Pts',(-6.51968959134574,16.8292587962898,
-475.036029411765));
#166445=CARTESIAN_POINT('Ctrl Pts',(-4.96022910773078,17.4333970061901,
-476.530147058824));
#166446=CARTESIAN_POINT('Ctrl Pts',(-3.31631129755346,17.7406985030951,
-478.024264705882));
#166447=CARTESIAN_POINT('Ctrl Pts',(-1.67239348737615,18.048,-479.518382352941));
#166448=CARTESIAN_POINT('Ctrl Pts',(-2.21024254310115E-15,18.048,-481.0125));
#166449=CARTESIAN_POINT('Ctrl Pts',(1.67239348737616,18.048,-482.506617647059));
#166450=CARTESIAN_POINT('Ctrl Pts',(3.31631129755346,17.7406985030951,-484.000735294118));
#166451=CARTESIAN_POINT('Ctrl Pts',(4.96022910773077,17.4333970061901,-485.494852941177));
#166452=CARTESIAN_POINT('Ctrl Pts',(6.51968959134575,16.8292587962898,-486.988970588235));
#166453=CARTESIAN_POINT('Ctrl Pts',(8.07915007496071,16.2251205863895,-488.483088235294));
#166454=CARTESIAN_POINT('Ctrl Pts',(9.50104767561053,15.3447188656481,-489.977205882353));
#166455=CARTESIAN_POINT('Ctrl Pts',(10.9229452762603,14.4643171449067,-491.471323529412));
#166456=CARTESIAN_POINT('Ctrl Pts',(12.1588589765331,13.3376329379985,-492.965441176471));
#166457=CARTESIAN_POINT('Ctrl Pts',(13.3947726768058,12.2109487310903,-494.45955882353));
#166458=CARTESIAN_POINT('Ctrl Pts',(14.4026149179538,10.8763499173728,-495.953676470588));
#166459=CARTESIAN_POINT('Ctrl Pts',(15.4104571591017,9.54175110365538,-497.447794117647));
#166460=CARTESIAN_POINT('Ctrl Pts',(16.1559070823762,8.04468584505496,-498.941911764706));
#166461=CARTESIAN_POINT('Ctrl Pts',(16.9013570056506,6.54762058645456,-500.436029411765));
#166462=CARTESIAN_POINT('Ctrl Pts',(17.3590292079831,4.93906964482096,-501.930147058824));
#166463=CARTESIAN_POINT('Ctrl Pts',(17.8167014103155,3.33051870318735,-503.424264705883));
#166464=CARTESIAN_POINT('Ctrl Pts',(17.9710104137728,1.66525935159367,-504.918382352941));
#166465=CARTESIAN_POINT('Ctrl Pts',(18.1253194172301,3.32956716117513E-15,
-506.4125));
#166466=CARTESIAN_POINT('Ctrl Pts',(17.9710104137728,-1.66525935159367,
-507.906617647059));
#166467=CARTESIAN_POINT('Ctrl Pts',(17.8167014103155,-3.33051870318736,
-509.400735294117));
#166468=CARTESIAN_POINT('Ctrl Pts',(17.3590292079831,-4.93906964482095,
-510.894852941176));
#166469=CARTESIAN_POINT('Ctrl Pts',(16.9013570056506,-6.54762058645456,
-512.388970588235));
#166470=CARTESIAN_POINT('Ctrl Pts',(16.1559070823762,-8.04468584505497,
-513.883088235294));
#166471=CARTESIAN_POINT('Ctrl Pts',(15.4104571591017,-9.54175110365538,
-515.377205882353));
#166472=CARTESIAN_POINT('Ctrl Pts',(14.4026149179538,-10.8763499173728,
-516.871323529412));
#166473=CARTESIAN_POINT('Ctrl Pts',(13.3947726768058,-12.2109487310903,
-518.365441176471));
#166474=CARTESIAN_POINT('Ctrl Pts',(12.1588589765331,-13.3376329379985,
-519.85955882353));
#166475=CARTESIAN_POINT('Ctrl Pts',(10.9229452762603,-14.4643171449067,
-521.353676470588));
#166476=CARTESIAN_POINT('Ctrl Pts',(9.50104767561053,-15.3447188656481,
-522.847794117647));
#166477=CARTESIAN_POINT('Ctrl Pts',(8.07915007496071,-16.2251205863895,
-524.341911764706));
#166478=CARTESIAN_POINT('Ctrl Pts',(6.51968959134574,-16.8292587962898,
-525.836029411765));
#166479=CARTESIAN_POINT('Ctrl Pts',(4.96022910773078,-17.4333970061901,
-527.330147058823));
#166480=CARTESIAN_POINT('Ctrl Pts',(3.31631129755346,-17.7406985030951,
-528.824264705882));
#166481=CARTESIAN_POINT('Ctrl Pts',(1.67239348737615,-18.048,-530.318382352941));
#166482=CARTESIAN_POINT('Ctrl Pts',(0.,-18.048,-531.8125));
#166483=CARTESIAN_POINT('Ctrl Pts',(-1.67239348737615,-18.048,-533.306617647059));
#166484=CARTESIAN_POINT('Ctrl Pts',(-3.31631129755346,-17.7406985030951,
-534.800735294118));
#166485=CARTESIAN_POINT('Ctrl Pts',(-4.96022910773077,-17.4333970061901,
-536.294852941177));
#166486=CARTESIAN_POINT('Ctrl Pts',(-6.51968959134574,-16.8292587962898,
-537.788970588235));
#166487=CARTESIAN_POINT('Ctrl Pts',(-8.07915007496071,-16.2251205863895,
-539.283088235294));
#166488=CARTESIAN_POINT('Ctrl Pts',(-9.50104767561052,-15.3447188656481,
-540.777205882353));
#166489=CARTESIAN_POINT('Ctrl Pts',(-10.9229452762603,-14.4643171449067,
-542.271323529412));
#166490=CARTESIAN_POINT('Ctrl Pts',(-12.1588589765331,-13.3376329379985,
-543.765441176471));
#166491=CARTESIAN_POINT('Ctrl Pts',(-13.3947726768058,-12.2109487310903,
-545.259558823529));
#166492=CARTESIAN_POINT('Ctrl Pts',(-14.4026149179538,-10.8763499173728,
-546.753676470588));
#166493=CARTESIAN_POINT('Ctrl Pts',(-15.4104571591017,-9.54175110365538,
-548.247794117647));
#166494=CARTESIAN_POINT('Ctrl Pts',(-16.1559070823762,-8.04468584505497,
-549.741911764706));
#166495=CARTESIAN_POINT('Ctrl Pts',(-16.9013570056506,-6.54762058645456,
-551.236029411765));
#166496=CARTESIAN_POINT('Ctrl Pts',(-17.3590292079831,-4.93906964482095,
-552.730147058823));
#166497=CARTESIAN_POINT('Ctrl Pts',(-17.8167014103155,-3.33051870318735,
-554.224264705882));
#166498=CARTESIAN_POINT('Ctrl Pts',(-17.9710104137728,-1.66525935159368,
-555.718382352941));
#166499=CARTESIAN_POINT('Ctrl Pts',(-18.1253194172301,-1.10985572039171E-15,
-557.2125));
#166500=CARTESIAN_POINT('Ctrl Pts',(-17.9710104137728,1.66525935159367,
-558.706617647059));
#166501=CARTESIAN_POINT('Ctrl Pts',(-17.8167014103155,3.33051870318735,
-560.200735294118));
#166502=CARTESIAN_POINT('Ctrl Pts',(-17.3590292079831,4.93906964482096,
-561.694852941176));
#166503=CARTESIAN_POINT('Ctrl Pts',(-16.9013570056506,6.54762058645456,
-563.188970588235));
#166504=CARTESIAN_POINT('Ctrl Pts',(-16.1559070823762,8.04468584505497,
-564.683088235294));
#166505=CARTESIAN_POINT('Ctrl Pts',(-15.4104571591017,9.54175110365538,
-566.177205882353));
#166506=CARTESIAN_POINT('Ctrl Pts',(-14.4026149179538,10.8763499173728,
-567.671323529412));
#166507=CARTESIAN_POINT('Ctrl Pts',(-13.3947726768058,12.2109487310903,
-569.16544117647));
#166508=CARTESIAN_POINT('Ctrl Pts',(-12.1588589765331,13.3376329379985,
-570.659558823529));
#166509=CARTESIAN_POINT('Ctrl Pts',(-10.9229452762603,14.4643171449067,
-572.153676470588));
#166510=CARTESIAN_POINT('Ctrl Pts',(-9.50104767561052,15.3447188656481,
-573.647794117647));
#166511=CARTESIAN_POINT('Ctrl Pts',(-8.07915007496071,16.2251205863895,
-575.141911764706));
#166512=CARTESIAN_POINT('Ctrl Pts',(-6.51968959134574,16.8292587962898,
-576.636029411765));
#166513=CARTESIAN_POINT('Ctrl Pts',(-4.96022910773078,17.4333970061901,
-578.130147058824));
#166514=CARTESIAN_POINT('Ctrl Pts',(-3.31631129755346,17.7406985030951,
-579.624264705882));
#166515=CARTESIAN_POINT('Ctrl Pts',(-1.67239348737615,18.048,-581.118382352941));
#166516=CARTESIAN_POINT('Ctrl Pts',(-2.21024254310115E-15,18.048,-582.6125));
#166517=CARTESIAN_POINT('Ctrl Pts',(1.67239348737616,18.048,-584.106617647059));
#166518=CARTESIAN_POINT('Ctrl Pts',(3.31631129755346,17.7406985030951,-585.600735294117));
#166519=CARTESIAN_POINT('Ctrl Pts',(4.96022910773077,17.4333970061901,-587.094852941176));
#166520=CARTESIAN_POINT('Ctrl Pts',(6.51968959134575,16.8292587962898,-588.588970588235));
#166521=CARTESIAN_POINT('Ctrl Pts',(8.07915007496071,16.2251205863895,-590.083088235294));
#166522=CARTESIAN_POINT('Ctrl Pts',(9.50104767561053,15.3447188656481,-591.577205882353));
#166523=CARTESIAN_POINT('Ctrl Pts',(10.9229452762603,14.4643171449067,-593.071323529412));
#166524=CARTESIAN_POINT('Ctrl Pts',(12.1588589765331,13.3376329379985,-594.565441176471));
#166525=CARTESIAN_POINT('Ctrl Pts',(13.3947726768058,12.2109487310903,-596.05955882353));
#166526=CARTESIAN_POINT('Ctrl Pts',(14.4026149179538,10.8763499173728,-597.553676470588));
#166527=CARTESIAN_POINT('Ctrl Pts',(15.4104571591017,9.54175110365538,-599.047794117647));
#166528=CARTESIAN_POINT('Ctrl Pts',(16.1559070823762,8.04468584505496,-600.541911764706));
#166529=CARTESIAN_POINT('Ctrl Pts',(16.9013570056506,6.54762058645456,-602.036029411765));
#166530=CARTESIAN_POINT('Ctrl Pts',(17.3590292079831,4.93906964482096,-603.530147058823));
#166531=CARTESIAN_POINT('Ctrl Pts',(17.8167014103155,3.33051870318735,-605.024264705882));
#166532=CARTESIAN_POINT('Ctrl Pts',(17.9710104137728,1.66525935159367,-606.518382352941));
#166533=CARTESIAN_POINT('Ctrl Pts',(18.1253194172301,3.32956716117513E-15,
-608.0125));
#166534=CARTESIAN_POINT('Ctrl Pts',(17.9710104137728,-1.66525935159367,
-609.506617647059));
#166535=CARTESIAN_POINT('Ctrl Pts',(17.8167014103155,-3.33051870318736,
-611.000735294118));
#166536=CARTESIAN_POINT('Ctrl Pts',(17.3590292079831,-4.93906964482095,
-612.494852941176));
#166537=CARTESIAN_POINT('Ctrl Pts',(16.9013570056506,-6.54762058645456,
-613.988970588235));
#166538=CARTESIAN_POINT('Ctrl Pts',(16.1559070823762,-8.04468584505497,
-615.483088235294));
#166539=CARTESIAN_POINT('Ctrl Pts',(15.4104571591017,-9.54175110365538,
-616.977205882353));
#166540=CARTESIAN_POINT('Ctrl Pts',(14.4026149179538,-10.8763499173728,
-618.471323529412));
#166541=CARTESIAN_POINT('Ctrl Pts',(13.3947726768058,-12.2109487310903,
-619.96544117647));
#166542=CARTESIAN_POINT('Ctrl Pts',(12.1588589765331,-13.3376329379985,
-621.459558823529));
#166543=CARTESIAN_POINT('Ctrl Pts',(10.9229452762603,-14.4643171449067,
-622.953676470588));
#166544=CARTESIAN_POINT('Ctrl Pts',(9.50104767561053,-15.3447188656481,
-624.447794117647));
#166545=CARTESIAN_POINT('Ctrl Pts',(8.07915007496071,-16.2251205863895,
-625.941911764706));
#166546=CARTESIAN_POINT('Ctrl Pts',(6.51968959134574,-16.8292587962898,
-627.436029411764));
#166547=CARTESIAN_POINT('Ctrl Pts',(4.96022910773078,-17.4333970061901,
-628.930147058823));
#166548=CARTESIAN_POINT('Ctrl Pts',(3.31631129755346,-17.7406985030951,
-630.424264705882));
#166549=CARTESIAN_POINT('Ctrl Pts',(1.67239348737615,-18.048,-631.918382352941));
#166550=CARTESIAN_POINT('Ctrl Pts',(0.,-18.048,-633.4125));
#166551=CARTESIAN_POINT('Ctrl Pts',(-1.67239348737615,-18.048,-634.906617647059));
#166552=CARTESIAN_POINT('Ctrl Pts',(-3.31631129755346,-17.7406985030951,
-636.400735294118));
#166553=CARTESIAN_POINT('Ctrl Pts',(-4.96022910773077,-17.4333970061901,
-637.894852941177));
#166554=CARTESIAN_POINT('Ctrl Pts',(-6.51968959134574,-16.8292587962898,
-639.388970588235));
#166555=CARTESIAN_POINT('Ctrl Pts',(-8.07915007496071,-16.2251205863895,
-640.883088235294));
#166556=CARTESIAN_POINT('Ctrl Pts',(-9.50104767561052,-15.3447188656481,
-642.377205882353));
#166557=CARTESIAN_POINT('Ctrl Pts',(-10.9229452762603,-14.4643171449067,
-643.871323529412));
#166558=CARTESIAN_POINT('Ctrl Pts',(-12.1588589765331,-13.3376329379985,
-645.36544117647));
#166559=CARTESIAN_POINT('Ctrl Pts',(-13.3947726768058,-12.2109487310903,
-646.859558823529));
#166560=CARTESIAN_POINT('Ctrl Pts',(-14.4026149179538,-10.8763499173728,
-648.353676470588));
#166561=CARTESIAN_POINT('Ctrl Pts',(-15.4104571591017,-9.54175110365538,
-649.847794117647));
#166562=CARTESIAN_POINT('Ctrl Pts',(-16.1559070823762,-8.04468584505497,
-651.341911764706));
#166563=CARTESIAN_POINT('Ctrl Pts',(-16.9013570056506,-6.54762058645456,
-652.836029411765));
#166564=CARTESIAN_POINT('Ctrl Pts',(-17.3590292079831,-4.93906964482095,
-654.330147058824));
#166565=CARTESIAN_POINT('Ctrl Pts',(-17.8167014103155,-3.33051870318735,
-655.824264705882));
#166566=CARTESIAN_POINT('Ctrl Pts',(-17.9710104137728,-1.66525935159368,
-657.318382352941));
#166567=CARTESIAN_POINT('Ctrl Pts',(-18.1253194172301,-1.10985572039171E-15,
-658.8125));
#166568=CARTESIAN_POINT('Ctrl Pts',(-17.9710104137728,1.66525935159367,
-660.306617647059));
#166569=CARTESIAN_POINT('Ctrl Pts',(-17.8167014103155,3.33051870318735,
-661.800735294117));
#166570=CARTESIAN_POINT('Ctrl Pts',(-17.3590292079831,4.93906964482096,
-663.294852941176));
#166571=CARTESIAN_POINT('Ctrl Pts',(-16.9013570056506,6.54762058645456,
-664.788970588236));
#166572=CARTESIAN_POINT('Ctrl Pts',(-16.1559070823762,8.04468584505497,
-666.283088235294));
#166573=CARTESIAN_POINT('Ctrl Pts',(-15.4104571591017,9.54175110365538,
-667.777205882353));
#166574=CARTESIAN_POINT('Ctrl Pts',(-14.4026149179538,10.8763499173728,
-669.271323529412));
#166575=CARTESIAN_POINT('Ctrl Pts',(-13.3947726768058,12.2109487310903,
-670.765441176471));
#166576=CARTESIAN_POINT('Ctrl Pts',(-12.1588589765331,13.3376329379985,
-672.259558823529));
#166577=CARTESIAN_POINT('Ctrl Pts',(-10.9229452762603,14.4643171449067,
-673.753676470588));
#166578=CARTESIAN_POINT('Ctrl Pts',(-9.50104767561052,15.3447188656481,
-675.247794117647));
#166579=CARTESIAN_POINT('Ctrl Pts',(-8.07915007496071,16.2251205863895,
-676.741911764706));
#166580=CARTESIAN_POINT('Ctrl Pts',(-6.51968959134574,16.8292587962898,
-678.236029411765));
#166581=CARTESIAN_POINT('Ctrl Pts',(-4.96022910773078,17.4333970061901,
-679.730147058824));
#166582=CARTESIAN_POINT('Ctrl Pts',(-3.31631129755346,17.7406985030951,
-681.224264705883));
#166583=CARTESIAN_POINT('Ctrl Pts',(-1.67239348737615,18.048,-682.718382352941));
#166584=CARTESIAN_POINT('Ctrl Pts',(-2.21024254310115E-15,18.048,-684.2125));
#166585=CARTESIAN_POINT('Ctrl Pts',(1.67239348737616,18.048,-685.706617647059));
#166586=CARTESIAN_POINT('Ctrl Pts',(3.31631129755346,17.7406985030951,-687.200735294118));
#166587=CARTESIAN_POINT('Ctrl Pts',(4.96022910773077,17.4333970061901,-688.694852941176));
#166588=CARTESIAN_POINT('Ctrl Pts',(6.51968959134575,16.8292587962898,-690.188970588235));
#166589=CARTESIAN_POINT('Ctrl Pts',(8.07915007496071,16.2251205863895,-691.683088235294));
#166590=CARTESIAN_POINT('Ctrl Pts',(9.50104767561053,15.3447188656481,-693.177205882353));
#166591=CARTESIAN_POINT('Ctrl Pts',(10.9229452762603,14.4643171449067,-694.671323529412));
#166592=CARTESIAN_POINT('Ctrl Pts',(12.1588589765331,13.3376329379985,-696.165441176471));
#166593=CARTESIAN_POINT('Ctrl Pts',(13.3947726768058,12.2109487310903,-697.659558823529));
#166594=CARTESIAN_POINT('Ctrl Pts',(14.4026149179538,10.8763499173728,-699.153676470588));
#166595=CARTESIAN_POINT('Ctrl Pts',(15.4104571591017,9.54175110365538,-700.647794117647));
#166596=CARTESIAN_POINT('Ctrl Pts',(16.1559070823762,8.04468584505496,-702.141911764706));
#166597=CARTESIAN_POINT('Ctrl Pts',(16.9013570056506,6.54762058645456,-703.636029411765));
#166598=CARTESIAN_POINT('Ctrl Pts',(17.3590292079831,4.93906964482096,-705.130147058823));
#166599=CARTESIAN_POINT('Ctrl Pts',(17.8167014103155,3.33051870318735,-706.624264705882));
#166600=CARTESIAN_POINT('Ctrl Pts',(17.9710104137728,1.66525935159367,-708.118382352941));
#166601=CARTESIAN_POINT('Ctrl Pts',(18.1253194172301,3.32956716117513E-15,
-709.6125));
#166602=CARTESIAN_POINT('Ctrl Pts',(17.9710104137728,-1.66525935159367,
-711.106617647059));
#166603=CARTESIAN_POINT('Ctrl Pts',(17.8167014103155,-3.33051870318736,
-712.600735294118));
#166604=CARTESIAN_POINT('Ctrl Pts',(17.3590292079831,-4.93906964482095,
-714.094852941177));
#166605=CARTESIAN_POINT('Ctrl Pts',(16.9013570056506,-6.54762058645456,
-715.588970588235));
#166606=CARTESIAN_POINT('Ctrl Pts',(16.1559070823762,-8.04468584505497,
-717.083088235294));
#166607=CARTESIAN_POINT('Ctrl Pts',(15.4104571591017,-9.54175110365538,
-718.577205882353));
#166608=CARTESIAN_POINT('Ctrl Pts',(14.4026149179538,-10.8763499173728,
-720.071323529412));
#166609=CARTESIAN_POINT('Ctrl Pts',(13.3947726768058,-12.2109487310903,
-721.56544117647));
#166610=CARTESIAN_POINT('Ctrl Pts',(12.1588589765331,-13.3376329379985,
-723.059558823529));
#166611=CARTESIAN_POINT('Ctrl Pts',(10.9229452762603,-14.4643171449067,
-724.553676470588));
#166612=CARTESIAN_POINT('Ctrl Pts',(9.50104767561053,-15.3447188656481,
-726.047794117647));
#166613=CARTESIAN_POINT('Ctrl Pts',(8.07915007496071,-16.2251205863895,
-727.541911764706));
#166614=CARTESIAN_POINT('Ctrl Pts',(6.51968959134574,-16.8292587962898,
-729.036029411765));
#166615=CARTESIAN_POINT('Ctrl Pts',(4.96022910773078,-17.4333970061901,
-730.530147058824));
#166616=CARTESIAN_POINT('Ctrl Pts',(3.31631129755346,-17.7406985030951,
-732.024264705882));
#166617=CARTESIAN_POINT('Ctrl Pts',(1.67239348737615,-18.048,-733.518382352941));
#166618=CARTESIAN_POINT('Ctrl Pts',(0.,-18.048,-735.0125));
#166619=CARTESIAN_POINT('Ctrl Pts',(-1.67239348737615,-18.048,-736.506617647059));
#166620=CARTESIAN_POINT('Ctrl Pts',(-3.31631129755346,-17.7406985030951,
-738.000735294118));
#166621=CARTESIAN_POINT('Ctrl Pts',(-4.96022910773077,-17.4333970061901,
-739.494852941177));
#166622=CARTESIAN_POINT('Ctrl Pts',(-6.51968959134574,-16.8292587962898,
-740.988970588235));
#166623=CARTESIAN_POINT('Ctrl Pts',(-8.07915007496071,-16.2251205863895,
-742.483088235294));
#166624=CARTESIAN_POINT('Ctrl Pts',(-9.50104767561052,-15.3447188656481,
-743.977205882353));
#166625=CARTESIAN_POINT('Ctrl Pts',(-10.9229452762603,-14.4643171449067,
-745.471323529412));
#166626=CARTESIAN_POINT('Ctrl Pts',(-12.1588589765331,-13.3376329379985,
-746.96544117647));
#166627=CARTESIAN_POINT('Ctrl Pts',(-13.3947726768058,-12.2109487310903,
-748.459558823529));
#166628=CARTESIAN_POINT('Ctrl Pts',(-14.4026149179538,-10.8763499173728,
-749.953676470588));
#166629=CARTESIAN_POINT('Ctrl Pts',(-15.4104571591017,-9.54175110365538,
-751.447794117647));
#166630=CARTESIAN_POINT('Ctrl Pts',(-16.1559070823762,-8.04468584505497,
-752.941911764706));
#166631=CARTESIAN_POINT('Ctrl Pts',(-16.9013570056506,-6.54762058645456,
-754.436029411765));
#166632=CARTESIAN_POINT('Ctrl Pts',(-17.3590292079831,-4.93906964482095,
-755.930147058824));
#166633=CARTESIAN_POINT('Ctrl Pts',(-17.8167014103155,-3.33051870318735,
-757.424264705882));
#166634=CARTESIAN_POINT('Ctrl Pts',(-17.9710104137728,-1.66525935159368,
-758.918382352941));
#166635=CARTESIAN_POINT('Ctrl Pts',(-18.1253194172301,-1.10985572039171E-15,
-760.4125));
#166636=CARTESIAN_POINT('Ctrl Pts',(-17.9710104137728,1.66525935159367,
-761.906617647059));
#166637=CARTESIAN_POINT('Ctrl Pts',(-17.8167014103155,3.33051870318735,
-763.400735294118));
#166638=CARTESIAN_POINT('Ctrl Pts',(-17.3590292079831,4.93906964482096,
-764.894852941176));
#166639=CARTESIAN_POINT('Ctrl Pts',(-16.9013570056506,6.54762058645456,
-766.388970588235));
#166640=CARTESIAN_POINT('Ctrl Pts',(-16.1559070823762,8.04468584505497,
-767.883088235294));
#166641=CARTESIAN_POINT('Ctrl Pts',(-15.4104571591017,9.54175110365538,
-769.377205882353));
#166642=CARTESIAN_POINT('Ctrl Pts',(-14.4026149179538,10.8763499173728,
-770.871323529412));
#166643=CARTESIAN_POINT('Ctrl Pts',(-13.3947726768058,12.2109487310903,
-772.365441176471));
#166644=CARTESIAN_POINT('Ctrl Pts',(-12.1588589765331,13.3376329379985,
-773.85955882353));
#166645=CARTESIAN_POINT('Ctrl Pts',(-10.9229452762603,14.4643171449067,
-775.353676470589));
#166646=CARTESIAN_POINT('Ctrl Pts',(-9.50104767561052,15.3447188656481,
-776.847794117647));
#166647=CARTESIAN_POINT('Ctrl Pts',(-8.07915007496071,16.2251205863895,
-778.341911764706));
#166648=CARTESIAN_POINT('Ctrl Pts',(-6.51968959134574,16.8292587962898,
-779.836029411765));
#166649=CARTESIAN_POINT('Ctrl Pts',(-4.96022910773078,17.4333970061901,
-781.330147058823));
#166650=CARTESIAN_POINT('Ctrl Pts',(-3.31631129755346,17.7406985030951,
-782.824264705882));
#166651=CARTESIAN_POINT('Ctrl Pts',(-1.67239348737615,18.048,-784.318382352941));
#166652=CARTESIAN_POINT('Ctrl Pts',(-2.21024254310115E-15,18.048,-785.8125));
#166653=CARTESIAN_POINT('Ctrl Pts',(1.67239348737616,18.048,-787.306617647059));
#166654=CARTESIAN_POINT('Ctrl Pts',(3.31631129755346,17.7406985030951,-788.800735294118));
#166655=CARTESIAN_POINT('Ctrl Pts',(4.96022910773077,17.4333970061901,-790.294852941177));
#166656=CARTESIAN_POINT('Ctrl Pts',(6.51968959134575,16.8292587962898,-791.788970588235));
#166657=CARTESIAN_POINT('Ctrl Pts',(8.07915007496071,16.2251205863895,-793.283088235294));
#166658=CARTESIAN_POINT('Ctrl Pts',(9.50104767561053,15.3447188656481,-794.777205882353));
#166659=CARTESIAN_POINT('Ctrl Pts',(10.9229452762603,14.4643171449067,-796.271323529412));
#166660=CARTESIAN_POINT('Ctrl Pts',(12.1588589765331,13.3376329379985,-797.765441176471));
#166661=CARTESIAN_POINT('Ctrl Pts',(13.3947726768058,12.2109487310903,-799.259558823529));
#166662=CARTESIAN_POINT('Ctrl Pts',(14.4026149179538,10.8763499173728,-800.753676470588));
#166663=CARTESIAN_POINT('Ctrl Pts',(15.4104571591017,9.54175110365538,-802.247794117647));
#166664=CARTESIAN_POINT('Ctrl Pts',(16.1559070823762,8.04468584505496,-803.741911764706));
#166665=CARTESIAN_POINT('Ctrl Pts',(16.9013570056506,6.54762058645456,-805.236029411765));
#166666=CARTESIAN_POINT('Ctrl Pts',(17.3590292079831,4.93906964482096,-806.730147058823));
#166667=CARTESIAN_POINT('Ctrl Pts',(17.8167014103155,3.33051870318735,-808.224264705882));
#166668=CARTESIAN_POINT('Ctrl Pts',(17.9710104137728,1.66525935159367,-809.718382352941));
#166669=CARTESIAN_POINT('Ctrl Pts',(18.1253194172301,3.32956716117513E-15,
-811.2125));
#166670=CARTESIAN_POINT('Ctrl Pts',(17.9710104137728,-1.66525935159367,
-812.706617647059));
#166671=CARTESIAN_POINT('Ctrl Pts',(17.8167014103155,-3.33051870318736,
-814.200735294118));
#166672=CARTESIAN_POINT('Ctrl Pts',(17.3590292079831,-4.93906964482095,
-815.694852941177));
#166673=CARTESIAN_POINT('Ctrl Pts',(16.9013570056506,-6.54762058645456,
-817.188970588235));
#166674=CARTESIAN_POINT('Ctrl Pts',(16.1559070823762,-8.04468584505497,
-818.683088235294));
#166675=CARTESIAN_POINT('Ctrl Pts',(15.4104571591017,-9.54175110365538,
-820.177205882353));
#166676=CARTESIAN_POINT('Ctrl Pts',(14.4026149179538,-10.8763499173728,
-821.671323529412));
#166677=CARTESIAN_POINT('Ctrl Pts',(13.3947726768058,-12.2109487310903,
-823.16544117647));
#166678=CARTESIAN_POINT('Ctrl Pts',(12.1588589765331,-13.3376329379985,
-824.659558823529));
#166679=CARTESIAN_POINT('Ctrl Pts',(10.9229452762603,-14.4643171449067,
-826.153676470588));
#166680=CARTESIAN_POINT('Ctrl Pts',(9.50104767561053,-15.3447188656481,
-827.647794117647));
#166681=CARTESIAN_POINT('Ctrl Pts',(8.07915007496071,-16.2251205863895,
-829.141911764706));
#166682=CARTESIAN_POINT('Ctrl Pts',(6.51968959134574,-16.8292587962898,
-830.636029411765));
#166683=CARTESIAN_POINT('Ctrl Pts',(4.96022910773078,-17.4333970061901,
-832.130147058824));
#166684=CARTESIAN_POINT('Ctrl Pts',(3.31631129755346,-17.7406985030951,
-833.624264705883));
#166685=CARTESIAN_POINT('Ctrl Pts',(1.67239348737615,-18.048,-835.118382352941));
#166686=CARTESIAN_POINT('Ctrl Pts',(0.,-18.048,-836.6125));
#166687=CARTESIAN_POINT('Ctrl Pts',(-1.67239348737615,-18.048,-838.106617647059));
#166688=CARTESIAN_POINT('Ctrl Pts',(-3.31631129755346,-17.7406985030951,
-839.600735294118));
#166689=CARTESIAN_POINT('Ctrl Pts',(-4.96022910773077,-17.4333970061901,
-841.094852941176));
#166690=CARTESIAN_POINT('Ctrl Pts',(-6.51968959134574,-16.8292587962898,
-842.588970588235));
#166691=CARTESIAN_POINT('Ctrl Pts',(-8.07915007496071,-16.2251205863895,
-844.083088235294));
#166692=CARTESIAN_POINT('Ctrl Pts',(-9.50104767561052,-15.3447188656481,
-845.577205882353));
#166693=CARTESIAN_POINT('Ctrl Pts',(-10.9229452762603,-14.4643171449067,
-847.071323529412));
#166694=CARTESIAN_POINT('Ctrl Pts',(-12.1588589765331,-13.3376329379985,
-848.565441176471));
#166695=CARTESIAN_POINT('Ctrl Pts',(-13.3947726768058,-12.2109487310903,
-850.05955882353));
#166696=CARTESIAN_POINT('Ctrl Pts',(-14.4026149179538,-10.8763499173728,
-851.553676470588));
#166697=CARTESIAN_POINT('Ctrl Pts',(-15.4104571591017,-9.54175110365538,
-853.047794117647));
#166698=CARTESIAN_POINT('Ctrl Pts',(-16.1559070823762,-8.04468584505497,
-854.541911764706));
#166699=CARTESIAN_POINT('Ctrl Pts',(-16.9013570056506,-6.54762058645456,
-856.036029411765));
#166700=CARTESIAN_POINT('Ctrl Pts',(-17.3590292079831,-4.93906964482095,
-857.530147058824));
#166701=CARTESIAN_POINT('Ctrl Pts',(-17.8167014103155,-3.33051870318735,
-859.024264705882));
#166702=CARTESIAN_POINT('Ctrl Pts',(-17.9710104137728,-1.66525935159368,
-860.518382352941));
#166703=CARTESIAN_POINT('Ctrl Pts',(-18.1253194172301,-1.10985572039171E-15,
-862.0125));
#166704=CARTESIAN_POINT('Ctrl Pts',(-17.9710104137728,1.66525935159367,
-863.506617647059));
#166705=CARTESIAN_POINT('Ctrl Pts',(-17.8167014103155,3.33051870318735,
-865.000735294118));
#166706=CARTESIAN_POINT('Ctrl Pts',(-17.3590292079831,4.93906964482096,
-866.494852941176));
#166707=CARTESIAN_POINT('Ctrl Pts',(-16.9013570056506,6.54762058645456,
-867.988970588235));
#166708=CARTESIAN_POINT('Ctrl Pts',(-16.1559070823762,8.04468584505497,
-869.483088235294));
#166709=CARTESIAN_POINT('Ctrl Pts',(-15.4104571591017,9.54175110365538,
-870.977205882353));
#166710=CARTESIAN_POINT('Ctrl Pts',(-14.4026149179538,10.8763499173728,
-872.471323529412));
#166711=CARTESIAN_POINT('Ctrl Pts',(-13.3947726768058,12.2109487310903,
-873.965441176471));
#166712=CARTESIAN_POINT('Ctrl Pts',(-12.1588589765331,13.3376329379985,
-875.459558823529));
#166713=CARTESIAN_POINT('Ctrl Pts',(-10.9229452762603,14.4643171449067,
-876.953676470588));
#166714=CARTESIAN_POINT('Ctrl Pts',(-9.50104767561052,15.3447188656481,
-878.447794117647));
#166715=CARTESIAN_POINT('Ctrl Pts',(-8.07915007496071,16.2251205863895,
-879.941911764706));
#166716=CARTESIAN_POINT('Ctrl Pts',(-6.51968959134574,16.8292587962898,
-881.436029411765));
#166717=CARTESIAN_POINT('Ctrl Pts',(-4.96022910773078,17.4333970061901,
-882.930147058823));
#166718=CARTESIAN_POINT('Ctrl Pts',(-3.31631129755346,17.7406985030951,
-884.424264705882));
#166719=CARTESIAN_POINT('Ctrl Pts',(-1.67239348737615,18.048,-885.918382352941));
#166720=CARTESIAN_POINT('Ctrl Pts',(-2.21024254310115E-15,18.048,-887.4125));
#166721=CARTESIAN_POINT('Ctrl Pts',(1.67239348737616,18.048,-888.906617647059));
#166722=CARTESIAN_POINT('Ctrl Pts',(3.31631129755346,17.7406985030951,-890.400735294118));
#166723=CARTESIAN_POINT('Ctrl Pts',(4.96022910773077,17.4333970061901,-891.894852941177));
#166724=CARTESIAN_POINT('Ctrl Pts',(6.51968959134575,16.8292587962898,-893.388970588235));
#166725=CARTESIAN_POINT('Ctrl Pts',(8.07915007496071,16.2251205863895,-894.883088235295));
#166726=CARTESIAN_POINT('Ctrl Pts',(9.50104767561053,15.3447188656481,-896.377205882353));
#166727=CARTESIAN_POINT('Ctrl Pts',(10.9229452762603,14.4643171449067,-897.871323529412));
#166728=CARTESIAN_POINT('Ctrl Pts',(12.1588589765331,13.3376329379985,-899.36544117647));
#166729=CARTESIAN_POINT('Ctrl Pts',(13.3947726768058,12.2109487310903,-900.859558823529));
#166730=CARTESIAN_POINT('Ctrl Pts',(14.4026149179538,10.8763499173728,-902.353676470588));
#166731=CARTESIAN_POINT('Ctrl Pts',(15.4104571591017,9.54175110365538,-903.847794117647));
#166732=CARTESIAN_POINT('Ctrl Pts',(16.1559070823762,8.04468584505496,-905.341911764706));
#166733=CARTESIAN_POINT('Ctrl Pts',(16.9013570056506,6.54762058645456,-906.836029411765));
#166734=CARTESIAN_POINT('Ctrl Pts',(17.3590292079831,4.93906964482096,-908.330147058824));
#166735=CARTESIAN_POINT('Ctrl Pts',(17.8167014103155,3.33051870318735,-909.824264705883));
#166736=CARTESIAN_POINT('Ctrl Pts',(17.9710104137728,1.66525935159367,-911.318382352941));
#166737=CARTESIAN_POINT('Ctrl Pts',(18.1253194172301,3.32956716117513E-15,
-912.8125));
#166738=CARTESIAN_POINT('Ctrl Pts',(17.9710104137728,-1.66525935159367,
-914.306617647059));
#166739=CARTESIAN_POINT('Ctrl Pts',(17.8167014103155,-3.33051870318736,
-915.800735294118));
#166740=CARTESIAN_POINT('Ctrl Pts',(17.3590292079831,-4.93906964482095,
-917.294852941176));
#166741=CARTESIAN_POINT('Ctrl Pts',(16.9013570056506,-6.54762058645456,
-918.788970588235));
#166742=CARTESIAN_POINT('Ctrl Pts',(16.1559070823762,-8.04468584505497,
-920.283088235294));
#166743=CARTESIAN_POINT('Ctrl Pts',(15.4104571591017,-9.54175110365538,
-921.777205882353));
#166744=CARTESIAN_POINT('Ctrl Pts',(14.4026149179538,-10.8763499173728,
-923.271323529412));
#166745=CARTESIAN_POINT('Ctrl Pts',(13.3947726768058,-12.2109487310903,
-924.765441176471));
#166746=CARTESIAN_POINT('Ctrl Pts',(12.1588589765331,-13.3376329379985,
-926.259558823529));
#166747=CARTESIAN_POINT('Ctrl Pts',(10.9229452762603,-14.4643171449067,
-927.753676470588));
#166748=CARTESIAN_POINT('Ctrl Pts',(9.50104767561053,-15.3447188656481,
-929.247794117647));
#166749=CARTESIAN_POINT('Ctrl Pts',(8.07915007496071,-16.2251205863895,
-930.741911764706));
#166750=CARTESIAN_POINT('Ctrl Pts',(6.51968959134574,-16.8292587962898,
-932.236029411765));
#166751=CARTESIAN_POINT('Ctrl Pts',(4.96022910773078,-17.4333970061901,
-933.730147058824));
#166752=CARTESIAN_POINT('Ctrl Pts',(3.31631129755346,-17.7406985030951,
-935.224264705882));
#166753=CARTESIAN_POINT('Ctrl Pts',(1.67239348737615,-18.048,-936.718382352941));
#166754=CARTESIAN_POINT('Ctrl Pts',(0.,-18.048,-938.2125));
#166755=CARTESIAN_POINT('Ctrl Pts',(-1.67239348737615,-18.048,-939.706617647059));
#166756=CARTESIAN_POINT('Ctrl Pts',(-3.31631129755346,-17.7406985030951,
-941.200735294117));
#166757=CARTESIAN_POINT('Ctrl Pts',(-4.96022910773077,-17.4333970061901,
-942.694852941176));
#166758=CARTESIAN_POINT('Ctrl Pts',(-6.51968959134574,-16.8292587962898,
-944.188970588235));
#166759=CARTESIAN_POINT('Ctrl Pts',(-8.07915007496071,-16.2251205863895,
-945.683088235294));
#166760=CARTESIAN_POINT('Ctrl Pts',(-9.50104767561052,-15.3447188656481,
-947.177205882353));
#166761=CARTESIAN_POINT('Ctrl Pts',(-10.9229452762603,-14.4643171449067,
-948.671323529412));
#166762=CARTESIAN_POINT('Ctrl Pts',(-12.1588589765331,-13.3376329379985,
-950.165441176471));
#166763=CARTESIAN_POINT('Ctrl Pts',(-13.3947726768058,-12.2109487310903,
-951.65955882353));
#166764=CARTESIAN_POINT('Ctrl Pts',(-14.4026149179538,-10.8763499173728,
-953.153676470588));
#166765=CARTESIAN_POINT('Ctrl Pts',(-15.4104571591017,-9.54175110365538,
-954.647794117647));
#166766=CARTESIAN_POINT('Ctrl Pts',(-16.1559070823762,-8.04468584505497,
-956.141911764706));
#166767=CARTESIAN_POINT('Ctrl Pts',(-16.9013570056506,-6.54762058645456,
-957.636029411764));
#166768=CARTESIAN_POINT('Ctrl Pts',(-17.3590292079831,-4.93906964482095,
-959.130147058823));
#166769=CARTESIAN_POINT('Ctrl Pts',(-17.8167014103155,-3.33051870318735,
-960.624264705882));
#166770=CARTESIAN_POINT('Ctrl Pts',(-17.9710104137728,-1.66525935159368,
-962.118382352941));
#166771=CARTESIAN_POINT('Ctrl Pts',(-18.1253194172301,-1.10985572039171E-15,
-963.6125));
#166772=CARTESIAN_POINT('Ctrl Pts',(-17.9710104137728,1.66525935159367,
-965.106617647059));
#166773=CARTESIAN_POINT('Ctrl Pts',(-17.8167014103155,3.33051870318735,
-966.600735294118));
#166774=CARTESIAN_POINT('Ctrl Pts',(-17.3590292079831,4.93906964482096,
-968.094852941177));
#166775=CARTESIAN_POINT('Ctrl Pts',(-16.9013570056506,6.54762058645456,
-969.588970588235));
#166776=CARTESIAN_POINT('Ctrl Pts',(-16.1559070823762,8.04468584505497,
-971.083088235294));
#166777=CARTESIAN_POINT('Ctrl Pts',(-15.4104571591017,9.54175110365538,
-972.577205882353));
#166778=CARTESIAN_POINT('Ctrl Pts',(-14.4026149179538,10.8763499173728,
-974.071323529412));
#166779=CARTESIAN_POINT('Ctrl Pts',(-13.3947726768058,12.2109487310903,
-975.565441176471));
#166780=CARTESIAN_POINT('Ctrl Pts',(-12.1588589765331,13.3376329379985,
-977.059558823529));
#166781=CARTESIAN_POINT('Ctrl Pts',(-10.9229452762603,14.4643171449067,
-978.553676470588));
#166782=CARTESIAN_POINT('Ctrl Pts',(-9.50104767561052,15.3447188656481,
-980.047794117647));
#166783=CARTESIAN_POINT('Ctrl Pts',(-8.07915007496071,16.2251205863895,
-981.541911764706));
#166784=CARTESIAN_POINT('Ctrl Pts',(-6.51968959134574,16.8292587962898,
-983.036029411765));
#166785=CARTESIAN_POINT('Ctrl Pts',(-4.96022910773078,17.4333970061901,
-984.530147058824));
#166786=CARTESIAN_POINT('Ctrl Pts',(-3.31631129755346,17.7406985030951,
-986.024264705882));
#166787=CARTESIAN_POINT('Ctrl Pts',(-1.67239348737615,18.048,-987.518382352941));
#166788=CARTESIAN_POINT('Ctrl Pts',(-2.21024254310115E-15,18.048,-989.0125));
#166789=CARTESIAN_POINT('Ctrl Pts',(1.67239348737616,18.048,-990.506617647059));
#166790=CARTESIAN_POINT('Ctrl Pts',(3.31631129755346,17.7406985030951,-992.000735294118));
#166791=CARTESIAN_POINT('Ctrl Pts',(4.96022910773077,17.4333970061901,-993.494852941176));
#166792=CARTESIAN_POINT('Ctrl Pts',(6.51968959134575,16.8292587962898,-994.988970588235));
#166793=CARTESIAN_POINT('Ctrl Pts',(8.07915007496071,16.2251205863895,-996.483088235294));
#166794=CARTESIAN_POINT('Ctrl Pts',(9.50104767561053,15.3447188656481,-997.977205882353));
#166795=CARTESIAN_POINT('Ctrl Pts',(10.9229452762603,14.4643171449067,-999.471323529412));
#166796=CARTESIAN_POINT('Ctrl Pts',(12.1588589765331,13.3376329379985,-1000.96544117647));
#166797=CARTESIAN_POINT('Ctrl Pts',(13.3947726768058,12.2109487310903,-1002.45955882353));
#166798=CARTESIAN_POINT('Ctrl Pts',(14.4026149179538,10.8763499173728,-1003.95367647059));
#166799=CARTESIAN_POINT('Ctrl Pts',(15.4104571591017,9.54175110365538,-1005.44779411765));
#166800=CARTESIAN_POINT('Ctrl Pts',(16.1559070823762,8.04468584505496,-1006.94191176471));
#166801=CARTESIAN_POINT('Ctrl Pts',(16.9013570056506,6.54762058645456,-1008.43602941176));
#166802=CARTESIAN_POINT('Ctrl Pts',(17.3590292079831,4.93906964482096,-1009.93014705882));
#166803=CARTESIAN_POINT('Ctrl Pts',(17.8167014103155,3.33051870318735,-1011.42426470588));
#166804=CARTESIAN_POINT('Ctrl Pts',(17.9710104137728,1.66525935159367,-1012.91838235294));
#166805=CARTESIAN_POINT('Ctrl Pts',(18.1253194172301,3.32956716117513E-15,
-1014.4125));
#166806=CARTESIAN_POINT('Ctrl Pts',(17.9710104137728,-1.66525935159367,
-1015.90661764706));
#166807=CARTESIAN_POINT('Ctrl Pts',(17.8167014103155,-3.33051870318736,
-1017.40073529412));
#166808=CARTESIAN_POINT('Ctrl Pts',(17.3590292079831,-4.93906964482095,
-1018.89485294118));
#166809=CARTESIAN_POINT('Ctrl Pts',(16.9013570056506,-6.54762058645456,
-1020.38897058824));
#166810=CARTESIAN_POINT('Ctrl Pts',(16.1559070823762,-8.04468584505497,
-1021.88308823529));
#166811=CARTESIAN_POINT('Ctrl Pts',(15.4104571591017,-9.54175110365538,
-1023.37720588235));
#166812=CARTESIAN_POINT('Ctrl Pts',(14.4026149179538,-10.8763499173728,
-1024.87132352941));
#166813=CARTESIAN_POINT('Ctrl Pts',(13.3947726768058,-12.2109487310903,
-1026.36544117647));
#166814=CARTESIAN_POINT('Ctrl Pts',(12.1588589765331,-13.3376329379985,
-1027.85955882353));
#166815=CARTESIAN_POINT('Ctrl Pts',(10.9229452762603,-14.4643171449067,
-1029.35367647059));
#166816=CARTESIAN_POINT('Ctrl Pts',(9.50104767561053,-15.3447188656481,
-1030.84779411765));
#166817=CARTESIAN_POINT('Ctrl Pts',(8.07915007496071,-16.2251205863895,
-1032.34191176471));
#166818=CARTESIAN_POINT('Ctrl Pts',(6.51968959134574,-16.8292587962898,
-1033.83602941176));
#166819=CARTESIAN_POINT('Ctrl Pts',(4.96022910773078,-17.4333970061901,
-1035.33014705882));
#166820=CARTESIAN_POINT('Ctrl Pts',(3.31631129755346,-17.7406985030951,
-1036.82426470588));
#166821=CARTESIAN_POINT('Ctrl Pts',(1.67239348737615,-18.048,-1038.31838235294));
#166822=CARTESIAN_POINT('Ctrl Pts',(0.,-18.048,-1039.8125));
#166823=CARTESIAN_POINT('Ctrl Pts',(-1.67239348737615,-18.048,-1041.30661764706));
#166824=CARTESIAN_POINT('Ctrl Pts',(-3.31631129755346,-17.7406985030951,
-1042.80073529412));
#166825=CARTESIAN_POINT('Ctrl Pts',(-4.96022910773077,-17.4333970061901,
-1044.29485294118));
#166826=CARTESIAN_POINT('Ctrl Pts',(-6.51968959134574,-16.8292587962898,
-1045.78897058824));
#166827=CARTESIAN_POINT('Ctrl Pts',(-8.07915007496071,-16.2251205863895,
-1047.28308823529));
#166828=CARTESIAN_POINT('Ctrl Pts',(-9.50104767561052,-15.3447188656481,
-1048.77720588235));
#166829=CARTESIAN_POINT('Ctrl Pts',(-10.9229452762603,-14.4643171449067,
-1050.27132352941));
#166830=CARTESIAN_POINT('Ctrl Pts',(-12.1588589765331,-13.3376329379985,
-1051.76544117647));
#166831=CARTESIAN_POINT('Ctrl Pts',(-13.3947726768058,-12.2109487310903,
-1053.25955882353));
#166832=CARTESIAN_POINT('Ctrl Pts',(-14.4026149179538,-10.8763499173728,
-1054.75367647059));
#166833=CARTESIAN_POINT('Ctrl Pts',(-15.4104571591017,-9.54175110365538,
-1056.24779411765));
#166834=CARTESIAN_POINT('Ctrl Pts',(-16.1559070823762,-8.04468584505497,
-1057.74191176471));
#166835=CARTESIAN_POINT('Ctrl Pts',(-16.9013570056506,-6.54762058645456,
-1059.23602941177));
#166836=CARTESIAN_POINT('Ctrl Pts',(-17.3590292079831,-4.93906964482095,
-1060.73014705882));
#166837=CARTESIAN_POINT('Ctrl Pts',(-17.8167014103155,-3.33051870318735,
-1062.22426470588));
#166838=CARTESIAN_POINT('Ctrl Pts',(-17.9710104137728,-1.66525935159368,
-1063.71838235294));
#166839=CARTESIAN_POINT('Ctrl Pts',(-18.1253194172301,-1.10985572039171E-15,
-1065.2125));
#166840=CARTESIAN_POINT('Ctrl Pts',(-17.9710104137728,1.66525935159367,
-1066.70661764706));
#166841=CARTESIAN_POINT('Ctrl Pts',(-17.8167014103155,3.33051870318735,
-1068.20073529412));
#166842=CARTESIAN_POINT('Ctrl Pts',(-17.3590292079831,4.93906964482096,
-1069.69485294118));
#166843=CARTESIAN_POINT('Ctrl Pts',(-16.9013570056506,6.54762058645456,
-1071.18897058824));
#166844=CARTESIAN_POINT('Ctrl Pts',(-16.1559070823762,8.04468584505497,
-1072.68308823529));
#166845=CARTESIAN_POINT('Ctrl Pts',(-15.4104571591017,9.54175110365538,
-1074.17720588235));
#166846=CARTESIAN_POINT('Ctrl Pts',(-14.4026149179538,10.8763499173728,
-1075.67132352941));
#166847=CARTESIAN_POINT('Ctrl Pts',(-13.3947726768058,12.2109487310903,
-1077.16544117647));
#166848=CARTESIAN_POINT('Ctrl Pts',(-12.1588589765331,13.3376329379985,
-1078.65955882353));
#166849=CARTESIAN_POINT('Ctrl Pts',(-10.9229452762603,14.4643171449067,
-1080.15367647059));
#166850=CARTESIAN_POINT('Ctrl Pts',(-9.50104767561052,15.3447188656481,
-1081.64779411765));
#166851=CARTESIAN_POINT('Ctrl Pts',(-8.07915007496071,16.2251205863895,
-1083.14191176471));
#166852=CARTESIAN_POINT('Ctrl Pts',(-6.51968959134574,16.8292587962898,
-1084.63602941176));
#166853=CARTESIAN_POINT('Ctrl Pts',(-4.96022910773078,17.4333970061901,
-1086.13014705882));
#166854=CARTESIAN_POINT('Ctrl Pts',(-3.31631129755346,17.7406985030951,
-1087.62426470588));
#166855=CARTESIAN_POINT('Ctrl Pts',(-1.67239348737615,18.048,-1089.11838235294));
#166856=CARTESIAN_POINT('Ctrl Pts',(-2.21024254310115E-15,18.048,-1090.6125));
#166857=CARTESIAN_POINT('Ctrl Pts',(1.67239348737616,18.048,-1092.10661764706));
#166858=CARTESIAN_POINT('Ctrl Pts',(3.31631129755346,17.7406985030951,-1093.60073529412));
#166859=CARTESIAN_POINT('Ctrl Pts',(4.96022910773077,17.4333970061901,-1095.09485294118));
#166860=CARTESIAN_POINT('Ctrl Pts',(6.51968959134575,16.8292587962898,-1096.58897058824));
#166861=CARTESIAN_POINT('Ctrl Pts',(8.07915007496071,16.2251205863895,-1098.08308823529));
#166862=CARTESIAN_POINT('Ctrl Pts',(9.50104767561053,15.3447188656481,-1099.57720588235));
#166863=CARTESIAN_POINT('Ctrl Pts',(10.9229452762603,14.4643171449067,-1101.07132352941));
#166864=CARTESIAN_POINT('Ctrl Pts',(12.1588589765331,13.3376329379985,-1102.56544117647));
#166865=CARTESIAN_POINT('Ctrl Pts',(13.3947726768058,12.2109487310903,-1104.05955882353));
#166866=CARTESIAN_POINT('Ctrl Pts',(14.4026149179538,10.8763499173728,-1105.55367647059));
#166867=CARTESIAN_POINT('Ctrl Pts',(15.4104571591017,9.54175110365538,-1107.04779411765));
#166868=CARTESIAN_POINT('Ctrl Pts',(16.1559070823762,8.04468584505496,-1108.54191176471));
#166869=CARTESIAN_POINT('Ctrl Pts',(16.9013570056506,6.54762058645456,-1110.03602941176));
#166870=CARTESIAN_POINT('Ctrl Pts',(17.3590292079831,4.93906964482096,-1111.53014705882));
#166871=CARTESIAN_POINT('Ctrl Pts',(17.8167014103155,3.33051870318735,-1113.02426470588));
#166872=CARTESIAN_POINT('Ctrl Pts',(17.9710104137728,1.66525935159367,-1114.51838235294));
#166873=CARTESIAN_POINT('Ctrl Pts',(18.1253194172301,3.32956716117513E-15,
-1116.0125));
#166874=CARTESIAN_POINT('Ctrl Pts',(17.9710104137728,-1.66525935159367,
-1117.50661764706));
#166875=CARTESIAN_POINT('Ctrl Pts',(17.8167014103155,-3.33051870318736,
-1119.00073529412));
#166876=CARTESIAN_POINT('Ctrl Pts',(17.3590292079831,-4.93906964482095,
-1120.49485294118));
#166877=CARTESIAN_POINT('Ctrl Pts',(16.9013570056506,-6.54762058645456,
-1121.98897058824));
#166878=CARTESIAN_POINT('Ctrl Pts',(16.1559070823762,-8.04468584505497,
-1123.48308823529));
#166879=CARTESIAN_POINT('Ctrl Pts',(15.4104571591017,-9.54175110365538,
-1124.97720588235));
#166880=CARTESIAN_POINT('Ctrl Pts',(14.4026149179538,-10.8763499173728,
-1126.47132352941));
#166881=CARTESIAN_POINT('Ctrl Pts',(13.3947726768058,-12.2109487310903,
-1127.96544117647));
#166882=CARTESIAN_POINT('Ctrl Pts',(12.1588589765331,-13.3376329379985,
-1129.45955882353));
#166883=CARTESIAN_POINT('Ctrl Pts',(10.9229452762603,-14.4643171449067,
-1130.95367647059));
#166884=CARTESIAN_POINT('Ctrl Pts',(9.50104767561053,-15.3447188656481,
-1132.44779411765));
#166885=CARTESIAN_POINT('Ctrl Pts',(8.07915007496071,-16.2251205863895,
-1133.94191176471));
#166886=CARTESIAN_POINT('Ctrl Pts',(6.51968959134574,-16.8292587962898,
-1135.43602941176));
#166887=CARTESIAN_POINT('Ctrl Pts',(4.96022910773078,-17.4333970061901,
-1136.93014705882));
#166888=CARTESIAN_POINT('Ctrl Pts',(3.31631129755346,-17.7406985030951,
-1138.42426470588));
#166889=CARTESIAN_POINT('Ctrl Pts',(1.67239348737615,-18.048,-1139.91838235294));
#166890=CARTESIAN_POINT('Ctrl Pts',(0.,-18.048,-1141.4125));
#166891=CARTESIAN_POINT('Ctrl Pts',(-1.67239348737615,-18.048,-1142.90661764706));
#166892=CARTESIAN_POINT('Ctrl Pts',(-3.31631129755346,-17.7406985030951,
-1144.40073529412));
#166893=CARTESIAN_POINT('Ctrl Pts',(-4.96022910773077,-17.4333970061901,
-1145.89485294118));
#166894=CARTESIAN_POINT('Ctrl Pts',(-6.51968959134574,-16.8292587962898,
-1147.38897058824));
#166895=CARTESIAN_POINT('Ctrl Pts',(-8.07915007496071,-16.2251205863895,
-1148.88308823529));
#166896=CARTESIAN_POINT('Ctrl Pts',(-9.50104767561052,-15.3447188656481,
-1150.37720588235));
#166897=CARTESIAN_POINT('Ctrl Pts',(-10.9229452762603,-14.4643171449067,
-1151.87132352941));
#166898=CARTESIAN_POINT('Ctrl Pts',(-12.1588589765331,-13.3376329379985,
-1153.36544117647));
#166899=CARTESIAN_POINT('Ctrl Pts',(-13.3947726768058,-12.2109487310903,
-1154.85955882353));
#166900=CARTESIAN_POINT('Ctrl Pts',(-14.4026149179538,-10.8763499173728,
-1156.35367647059));
#166901=CARTESIAN_POINT('Ctrl Pts',(-15.4104571591017,-9.54175110365538,
-1157.84779411765));
#166902=CARTESIAN_POINT('Ctrl Pts',(-16.1559070823762,-8.04468584505497,
-1159.34191176471));
#166903=CARTESIAN_POINT('Ctrl Pts',(-16.9013570056506,-6.54762058645456,
-1160.83602941176));
#166904=CARTESIAN_POINT('Ctrl Pts',(-17.3590292079831,-4.93906964482095,
-1162.33014705882));
#166905=CARTESIAN_POINT('Ctrl Pts',(-17.8167014103155,-3.33051870318735,
-1163.82426470588));
#166906=CARTESIAN_POINT('Ctrl Pts',(-17.9710104137728,-1.66525935159368,
-1165.31838235294));
#166907=CARTESIAN_POINT('Ctrl Pts',(-18.1253194172301,-1.10985572039171E-15,
-1166.8125));
#166908=CARTESIAN_POINT('Ctrl Pts',(-17.9710104137728,1.66525935159367,
-1168.30661764706));
#166909=CARTESIAN_POINT('Ctrl Pts',(-17.8167014103155,3.33051870318735,
-1169.80073529412));
#166910=CARTESIAN_POINT('Ctrl Pts',(-17.3590292079831,4.93906964482096,
-1171.29485294118));
#166911=CARTESIAN_POINT('Ctrl Pts',(-16.9013570056506,6.54762058645456,
-1172.78897058824));
#166912=CARTESIAN_POINT('Ctrl Pts',(-16.1559070823762,8.04468584505497,
-1174.28308823529));
#166913=CARTESIAN_POINT('Ctrl Pts',(-15.4104571591017,9.54175110365538,
-1175.77720588235));
#166914=CARTESIAN_POINT('Ctrl Pts',(-14.4026149179538,10.8763499173728,
-1177.27132352941));
#166915=CARTESIAN_POINT('Ctrl Pts',(-13.3947726768058,12.2109487310903,
-1178.76544117647));
#166916=CARTESIAN_POINT('Ctrl Pts',(-12.1588589765331,13.3376329379985,
-1180.25955882353));
#166917=CARTESIAN_POINT('Ctrl Pts',(-10.9229452762603,14.4643171449067,
-1181.75367647059));
#166918=CARTESIAN_POINT('Ctrl Pts',(-9.50104767561052,15.3447188656481,
-1183.24779411765));
#166919=CARTESIAN_POINT('Ctrl Pts',(-8.07915007496071,16.2251205863895,
-1184.74191176471));
#166920=CARTESIAN_POINT('Ctrl Pts',(-6.51968959134574,16.8292587962898,
-1186.23602941176));
#166921=CARTESIAN_POINT('Ctrl Pts',(-4.96022910773078,17.4333970061901,
-1187.73014705882));
#166922=CARTESIAN_POINT('Ctrl Pts',(-3.31631129755346,17.7406985030951,
-1189.22426470588));
#166923=CARTESIAN_POINT('Ctrl Pts',(-1.67239348737615,18.048,-1190.71838235294));
#166924=CARTESIAN_POINT('Ctrl Pts',(-2.21024254310115E-15,18.048,-1192.2125));
#166925=CARTESIAN_POINT('Ctrl Pts',(1.67239348737616,18.048,-1193.70661764706));
#166926=CARTESIAN_POINT('Ctrl Pts',(3.31631129755346,17.7406985030951,-1195.20073529412));
#166927=CARTESIAN_POINT('Ctrl Pts',(4.96022910773077,17.4333970061901,-1196.69485294118));
#166928=CARTESIAN_POINT('Ctrl Pts',(6.51968959134575,16.8292587962898,-1198.18897058824));
#166929=CARTESIAN_POINT('Ctrl Pts',(8.07915007496071,16.2251205863895,-1199.68308823529));
#166930=CARTESIAN_POINT('Ctrl Pts',(9.50104767561053,15.3447188656481,-1201.17720588235));
#166931=CARTESIAN_POINT('Ctrl Pts',(10.9229452762603,14.4643171449067,-1202.67132352941));
#166932=CARTESIAN_POINT('Ctrl Pts',(12.1588589765331,13.3376329379985,-1204.16544117647));
#166933=CARTESIAN_POINT('Ctrl Pts',(13.3947726768058,12.2109487310903,-1205.65955882353));
#166934=CARTESIAN_POINT('Ctrl Pts',(14.4026149179538,10.8763499173728,-1207.15367647059));
#166935=CARTESIAN_POINT('Ctrl Pts',(15.4104571591017,9.54175110365538,-1208.64779411765));
#166936=CARTESIAN_POINT('Ctrl Pts',(16.1559070823762,8.04468584505496,-1210.14191176471));
#166937=CARTESIAN_POINT('Ctrl Pts',(16.9013570056506,6.54762058645456,-1211.63602941176));
#166938=CARTESIAN_POINT('Ctrl Pts',(17.3590292079831,4.93906964482096,-1213.13014705882));
#166939=CARTESIAN_POINT('Ctrl Pts',(17.8167014103155,3.33051870318735,-1214.62426470588));
#166940=CARTESIAN_POINT('Ctrl Pts',(17.9710104137728,1.66525935159367,-1216.11838235294));
#166941=CARTESIAN_POINT('Ctrl Pts',(18.1253194172301,3.32956716117513E-15,
-1217.6125));
#166942=CARTESIAN_POINT('Ctrl Pts',(17.9710104137728,-1.66525935159367,
-1219.10661764706));
#166943=CARTESIAN_POINT('Ctrl Pts',(17.8167014103155,-3.33051870318736,
-1220.60073529412));
#166944=CARTESIAN_POINT('Ctrl Pts',(17.3590292079831,-4.93906964482095,
-1222.09485294118));
#166945=CARTESIAN_POINT('Ctrl Pts',(16.9013570056506,-6.54762058645456,
-1223.58897058824));
#166946=CARTESIAN_POINT('Ctrl Pts',(16.1559070823762,-8.04468584505497,
-1225.08308823529));
#166947=CARTESIAN_POINT('Ctrl Pts',(15.4104571591017,-9.54175110365538,
-1226.57720588235));
#166948=CARTESIAN_POINT('Ctrl Pts',(14.4026149179538,-10.8763499173728,
-1228.07132352941));
#166949=CARTESIAN_POINT('Ctrl Pts',(13.3947726768058,-12.2109487310903,
-1229.56544117647));
#166950=CARTESIAN_POINT('Ctrl Pts',(12.1588589765331,-13.3376329379985,
-1231.05955882353));
#166951=CARTESIAN_POINT('Ctrl Pts',(10.9229452762603,-14.4643171449067,
-1232.55367647059));
#166952=CARTESIAN_POINT('Ctrl Pts',(9.50104767561053,-15.3447188656481,
-1234.04779411765));
#166953=CARTESIAN_POINT('Ctrl Pts',(8.07915007496071,-16.2251205863895,
-1235.54191176471));
#166954=CARTESIAN_POINT('Ctrl Pts',(6.51968959134574,-16.8292587962898,
-1237.03602941176));
#166955=CARTESIAN_POINT('Ctrl Pts',(4.96022910773078,-17.4333970061901,
-1238.53014705882));
#166956=CARTESIAN_POINT('Ctrl Pts',(3.31631129755346,-17.7406985030951,
-1240.02426470588));
#166957=CARTESIAN_POINT('Ctrl Pts',(1.67239348737615,-18.048,-1241.51838235294));
#166958=CARTESIAN_POINT('Ctrl Pts',(0.,-18.048,-1243.0125));
#166959=CARTESIAN_POINT('Ctrl Pts',(-1.67239348737615,-18.048,-1244.50661764706));
#166960=CARTESIAN_POINT('Ctrl Pts',(-3.31631129755346,-17.7406985030951,
-1246.00073529412));
#166961=CARTESIAN_POINT('Ctrl Pts',(-4.96022910773077,-17.4333970061901,
-1247.49485294118));
#166962=CARTESIAN_POINT('Ctrl Pts',(-6.51968959134574,-16.8292587962898,
-1248.98897058824));
#166963=CARTESIAN_POINT('Ctrl Pts',(-8.07915007496071,-16.2251205863895,
-1250.48308823529));
#166964=CARTESIAN_POINT('Ctrl Pts',(-9.50104767561052,-15.3447188656481,
-1251.97720588235));
#166965=CARTESIAN_POINT('Ctrl Pts',(-10.9229452762603,-14.4643171449067,
-1253.47132352941));
#166966=CARTESIAN_POINT('Ctrl Pts',(-12.1588589765331,-13.3376329379985,
-1254.96544117647));
#166967=CARTESIAN_POINT('Ctrl Pts',(-13.3947726768058,-12.2109487310903,
-1256.45955882353));
#166968=CARTESIAN_POINT('Ctrl Pts',(-14.4026149179538,-10.8763499173728,
-1257.95367647059));
#166969=CARTESIAN_POINT('Ctrl Pts',(-15.4104571591017,-9.54175110365538,
-1259.44779411765));
#166970=CARTESIAN_POINT('Ctrl Pts',(-16.1559070823762,-8.04468584505497,
-1260.94191176471));
#166971=CARTESIAN_POINT('Ctrl Pts',(-16.9013570056506,-6.54762058645456,
-1262.43602941176));
#166972=CARTESIAN_POINT('Ctrl Pts',(-17.3590292079831,-4.93906964482095,
-1263.93014705882));
#166973=CARTESIAN_POINT('Ctrl Pts',(-17.8167014103155,-3.33051870318735,
-1265.42426470588));
#166974=CARTESIAN_POINT('Ctrl Pts',(-17.9710104137728,-1.66525935159368,
-1266.91838235294));
#166975=CARTESIAN_POINT('Ctrl Pts',(-18.1253194172301,-1.10985572039171E-15,
-1268.4125));
#166976=CARTESIAN_POINT('Ctrl Pts',(-17.9710104137728,1.66525935159367,
-1269.90661764706));
#166977=CARTESIAN_POINT('Ctrl Pts',(-17.8167014103155,3.33051870318735,
-1271.40073529412));
#166978=CARTESIAN_POINT('Ctrl Pts',(-17.3590292079831,4.93906964482096,
-1272.89485294118));
#166979=CARTESIAN_POINT('Ctrl Pts',(-16.9013570056506,6.54762058645456,
-1274.38897058824));
#166980=CARTESIAN_POINT('Ctrl Pts',(-16.1559070823762,8.04468584505497,
-1275.88308823529));
#166981=CARTESIAN_POINT('Ctrl Pts',(-15.4104571591017,9.54175110365538,
-1277.37720588235));
#166982=CARTESIAN_POINT('Ctrl Pts',(-14.4026149179538,10.8763499173728,
-1278.87132352941));
#166983=CARTESIAN_POINT('Ctrl Pts',(-13.3947726768058,12.2109487310903,
-1280.36544117647));
#166984=CARTESIAN_POINT('Ctrl Pts',(-12.1588589765331,13.3376329379985,
-1281.85955882353));
#166985=CARTESIAN_POINT('Ctrl Pts',(-10.9229452762603,14.4643171449067,
-1283.35367647059));
#166986=CARTESIAN_POINT('Ctrl Pts',(-9.50104767561052,15.3447188656481,
-1284.84779411765));
#166987=CARTESIAN_POINT('Ctrl Pts',(-8.07915007496071,16.2251205863895,
-1286.34191176471));
#166988=CARTESIAN_POINT('Ctrl Pts',(-6.51968959134574,16.8292587962898,
-1287.83602941176));
#166989=CARTESIAN_POINT('Ctrl Pts',(-4.96022910773078,17.4333970061901,
-1289.33014705882));
#166990=CARTESIAN_POINT('Ctrl Pts',(-3.31631129755346,17.7406985030951,
-1290.82426470588));
#166991=CARTESIAN_POINT('Ctrl Pts',(-1.67239348737615,18.048,-1292.31838235294));
#166992=CARTESIAN_POINT('Ctrl Pts',(-2.21024254310115E-15,18.048,-1293.8125));
#166993=CARTESIAN_POINT('Ctrl Pts',(1.67239348737616,18.048,-1295.30661764706));
#166994=CARTESIAN_POINT('Ctrl Pts',(3.31631129755346,17.7406985030951,-1296.80073529412));
#166995=CARTESIAN_POINT('Ctrl Pts',(4.96022910773077,17.4333970061901,-1298.29485294118));
#166996=CARTESIAN_POINT('Ctrl Pts',(6.51968959134575,16.8292587962898,-1299.78897058824));
#166997=CARTESIAN_POINT('Ctrl Pts',(8.07915007496071,16.2251205863895,-1301.28308823529));
#166998=CARTESIAN_POINT('Ctrl Pts',(9.50104767561053,15.3447188656481,-1302.77720588235));
#166999=CARTESIAN_POINT('Ctrl Pts',(10.9229452762603,14.4643171449067,-1304.27132352941));
#167000=CARTESIAN_POINT('Ctrl Pts',(12.1588589765331,13.3376329379985,-1305.76544117647));
#167001=CARTESIAN_POINT('Ctrl Pts',(13.3947726768058,12.2109487310903,-1307.25955882353));
#167002=CARTESIAN_POINT('Ctrl Pts',(14.4026149179538,10.8763499173728,-1308.75367647059));
#167003=CARTESIAN_POINT('Ctrl Pts',(15.4104571591017,9.54175110365538,-1310.24779411765));
#167004=CARTESIAN_POINT('Ctrl Pts',(16.1559070823762,8.04468584505496,-1311.74191176471));
#167005=CARTESIAN_POINT('Ctrl Pts',(16.9013570056506,6.54762058645456,-1313.23602941176));
#167006=CARTESIAN_POINT('Ctrl Pts',(17.3590292079831,4.93906964482096,-1314.73014705882));
#167007=CARTESIAN_POINT('Ctrl Pts',(17.8167014103155,3.33051870318735,-1316.22426470588));
#167008=CARTESIAN_POINT('Ctrl Pts',(17.9710104137728,1.66525935159367,-1317.71838235294));
#167009=CARTESIAN_POINT('Ctrl Pts',(18.1253194172301,3.32956716117513E-15,
-1319.2125));
#167010=CARTESIAN_POINT('Ctrl Pts',(17.9710104137728,-1.66525935159367,
-1320.70661764706));
#167011=CARTESIAN_POINT('Ctrl Pts',(17.8167014103155,-3.33051870318736,
-1322.20073529412));
#167012=CARTESIAN_POINT('Ctrl Pts',(17.3590292079831,-4.93906964482095,
-1323.69485294118));
#167013=CARTESIAN_POINT('Ctrl Pts',(16.9013570056506,-6.54762058645456,
-1325.18897058824));
#167014=CARTESIAN_POINT('Ctrl Pts',(16.1559070823762,-8.04468584505497,
-1326.68308823529));
#167015=CARTESIAN_POINT('Ctrl Pts',(15.4104571591017,-9.54175110365538,
-1328.17720588235));
#167016=CARTESIAN_POINT('Ctrl Pts',(14.4026149179538,-10.8763499173728,
-1329.67132352941));
#167017=CARTESIAN_POINT('Ctrl Pts',(13.3947726768058,-12.2109487310903,
-1331.16544117647));
#167018=CARTESIAN_POINT('Ctrl Pts',(12.1588589765331,-13.3376329379985,
-1332.65955882353));
#167019=CARTESIAN_POINT('Ctrl Pts',(10.9229452762603,-14.4643171449067,
-1334.15367647059));
#167020=CARTESIAN_POINT('Ctrl Pts',(9.50104767561053,-15.3447188656481,
-1335.64779411765));
#167021=CARTESIAN_POINT('Ctrl Pts',(8.07915007496071,-16.2251205863895,
-1337.14191176471));
#167022=CARTESIAN_POINT('Ctrl Pts',(6.51968959134574,-16.8292587962898,
-1338.63602941176));
#167023=CARTESIAN_POINT('Ctrl Pts',(4.96022910773078,-17.4333970061901,
-1340.13014705882));
#167024=CARTESIAN_POINT('Ctrl Pts',(3.31631129755346,-17.7406985030951,
-1341.62426470588));
#167025=CARTESIAN_POINT('Ctrl Pts',(1.67239348737615,-18.048,-1343.11838235294));
#167026=CARTESIAN_POINT('Ctrl Pts',(0.,-18.048,-1344.6125));
#167027=CARTESIAN_POINT('Ctrl Pts',(-1.67239348737615,-18.048,-1346.10661764706));
#167028=CARTESIAN_POINT('Ctrl Pts',(-3.31631129755346,-17.7406985030951,
-1347.60073529412));
#167029=CARTESIAN_POINT('Ctrl Pts',(-4.96022910773077,-17.4333970061901,
-1349.09485294118));
#167030=CARTESIAN_POINT('Ctrl Pts',(-6.51968959134574,-16.8292587962898,
-1350.58897058824));
#167031=CARTESIAN_POINT('Ctrl Pts',(-8.07915007496071,-16.2251205863895,
-1352.08308823529));
#167032=CARTESIAN_POINT('Ctrl Pts',(-9.50104767561052,-15.3447188656481,
-1353.57720588235));
#167033=CARTESIAN_POINT('Ctrl Pts',(-10.9229452762603,-14.4643171449067,
-1355.07132352941));
#167034=CARTESIAN_POINT('Ctrl Pts',(-12.1588589765331,-13.3376329379985,
-1356.56544117647));
#167035=CARTESIAN_POINT('Ctrl Pts',(-13.3947726768058,-12.2109487310903,
-1358.05955882353));
#167036=CARTESIAN_POINT('Ctrl Pts',(-14.4026149179538,-10.8763499173728,
-1359.55367647059));
#167037=CARTESIAN_POINT('Ctrl Pts',(-15.4104571591017,-9.54175110365538,
-1361.04779411765));
#167038=CARTESIAN_POINT('Ctrl Pts',(-16.1559070823762,-8.04468584505497,
-1362.54191176471));
#167039=CARTESIAN_POINT('Ctrl Pts',(-16.9013570056506,-6.54762058645456,
-1364.03602941176));
#167040=CARTESIAN_POINT('Ctrl Pts',(-17.3590292079831,-4.93906964482095,
-1365.53014705882));
#167041=CARTESIAN_POINT('Ctrl Pts',(-17.8167014103155,-3.33051870318735,
-1367.02426470588));
#167042=CARTESIAN_POINT('Ctrl Pts',(-17.9710104137728,-1.66525935159368,
-1368.51838235294));
#167043=CARTESIAN_POINT('Ctrl Pts',(-18.1253194172301,-1.10985572039171E-15,
-1370.0125));
#167044=CARTESIAN_POINT('Ctrl Pts',(-17.9710104137728,1.66525935159367,
-1371.50661764706));
#167045=CARTESIAN_POINT('Ctrl Pts',(-17.8167014103155,3.33051870318735,
-1373.00073529412));
#167046=CARTESIAN_POINT('Ctrl Pts',(-17.3590292079831,4.93906964482096,
-1374.49485294118));
#167047=CARTESIAN_POINT('Ctrl Pts',(-16.9013570056506,6.54762058645456,
-1375.98897058824));
#167048=CARTESIAN_POINT('Ctrl Pts',(-16.1559070823762,8.04468584505497,
-1377.48308823529));
#167049=CARTESIAN_POINT('Ctrl Pts',(-15.4104571591017,9.54175110365538,
-1378.97720588235));
#167050=CARTESIAN_POINT('Ctrl Pts',(-14.4026149179538,10.8763499173728,
-1380.47132352941));
#167051=CARTESIAN_POINT('Ctrl Pts',(-13.3947726768058,12.2109487310903,
-1381.96544117647));
#167052=CARTESIAN_POINT('Ctrl Pts',(-12.1588589765331,13.3376329379985,
-1383.45955882353));
#167053=CARTESIAN_POINT('Ctrl Pts',(-10.9229452762603,14.4643171449067,
-1384.95367647059));
#167054=CARTESIAN_POINT('Ctrl Pts',(-9.50104767561052,15.3447188656481,
-1386.44779411765));
#167055=CARTESIAN_POINT('Ctrl Pts',(-8.07915007496071,16.2251205863895,
-1387.94191176471));
#167056=CARTESIAN_POINT('Ctrl Pts',(-6.51968959134574,16.8292587962898,
-1389.43602941176));
#167057=CARTESIAN_POINT('Ctrl Pts',(-4.96022910773078,17.4333970061901,
-1390.93014705882));
#167058=CARTESIAN_POINT('Ctrl Pts',(-3.31631129755346,17.7406985030951,
-1392.42426470588));
#167059=CARTESIAN_POINT('Ctrl Pts',(-1.67239348737615,18.048,-1393.91838235294));
#167060=CARTESIAN_POINT('Ctrl Pts',(-2.21024254310115E-15,18.048,-1395.4125));
#167061=CARTESIAN_POINT('Ctrl Pts',(1.67239348737616,18.048,-1396.90661764706));
#167062=CARTESIAN_POINT('Ctrl Pts',(3.31631129755346,17.7406985030951,-1398.40073529412));
#167063=CARTESIAN_POINT('Ctrl Pts',(4.96022910773077,17.4333970061901,-1399.89485294118));
#167064=CARTESIAN_POINT('Ctrl Pts',(6.51968959134575,16.8292587962898,-1401.38897058824));
#167065=CARTESIAN_POINT('Ctrl Pts',(8.07915007496071,16.2251205863895,-1402.88308823529));
#167066=CARTESIAN_POINT('Ctrl Pts',(9.50104767561053,15.3447188656481,-1404.37720588235));
#167067=CARTESIAN_POINT('Ctrl Pts',(10.9229452762603,14.4643171449067,-1405.87132352941));
#167068=CARTESIAN_POINT('Ctrl Pts',(12.1588589765331,13.3376329379985,-1407.36544117647));
#167069=CARTESIAN_POINT('Ctrl Pts',(13.3947726768058,12.2109487310903,-1408.85955882353));
#167070=CARTESIAN_POINT('Ctrl Pts',(14.4026149179538,10.8763499173728,-1410.35367647059));
#167071=CARTESIAN_POINT('Ctrl Pts',(15.4104571591017,9.54175110365538,-1411.84779411765));
#167072=CARTESIAN_POINT('Ctrl Pts',(16.1559070823762,8.04468584505496,-1413.34191176471));
#167073=CARTESIAN_POINT('Ctrl Pts',(16.9013570056506,6.54762058645456,-1414.83602941176));
#167074=CARTESIAN_POINT('Ctrl Pts',(17.3590292079831,4.93906964482096,-1416.33014705882));
#167075=CARTESIAN_POINT('Ctrl Pts',(17.8167014103155,3.33051870318735,-1417.82426470588));
#167076=CARTESIAN_POINT('Ctrl Pts',(17.9710104137728,1.66525935159367,-1419.31838235294));
#167077=CARTESIAN_POINT('Ctrl Pts',(18.1253194172301,3.32956716117513E-15,
-1420.8125));
#167078=CARTESIAN_POINT('Ctrl Pts',(17.9710104137728,-1.66525935159367,
-1422.30661764706));
#167079=CARTESIAN_POINT('Ctrl Pts',(17.8167014103155,-3.33051870318736,
-1423.80073529412));
#167080=CARTESIAN_POINT('Ctrl Pts',(17.3590292079831,-4.93906964482095,
-1425.29485294118));
#167081=CARTESIAN_POINT('Ctrl Pts',(16.9013570056506,-6.54762058645456,
-1426.78897058824));
#167082=CARTESIAN_POINT('Ctrl Pts',(16.1559070823762,-8.04468584505497,
-1428.28308823529));
#167083=CARTESIAN_POINT('Ctrl Pts',(15.4104571591017,-9.54175110365538,
-1429.77720588235));
#167084=CARTESIAN_POINT('Ctrl Pts',(14.4026149179538,-10.8763499173728,
-1431.27132352941));
#167085=CARTESIAN_POINT('Ctrl Pts',(13.3947726768058,-12.2109487310903,
-1432.76544117647));
#167086=CARTESIAN_POINT('Ctrl Pts',(12.1588589765331,-13.3376329379985,
-1434.25955882353));
#167087=CARTESIAN_POINT('Ctrl Pts',(10.9229452762603,-14.4643171449067,
-1435.75367647059));
#167088=CARTESIAN_POINT('Ctrl Pts',(9.50104767561053,-15.3447188656481,
-1437.24779411765));
#167089=CARTESIAN_POINT('Ctrl Pts',(8.07915007496071,-16.2251205863895,
-1438.74191176471));
#167090=CARTESIAN_POINT('Ctrl Pts',(6.51968959134574,-16.8292587962898,
-1440.23602941176));
#167091=CARTESIAN_POINT('Ctrl Pts',(4.96022910773078,-17.4333970061901,
-1441.73014705882));
#167092=CARTESIAN_POINT('Ctrl Pts',(3.31631129755346,-17.7406985030951,
-1443.22426470588));
#167093=CARTESIAN_POINT('Ctrl Pts',(1.67239348737615,-18.048,-1444.71838235294));
#167094=CARTESIAN_POINT('Ctrl Pts',(0.,-18.048,-1446.2125));
#167095=CARTESIAN_POINT('Ctrl Pts',(-1.67239348737615,-18.048,-1447.70661764706));
#167096=CARTESIAN_POINT('Ctrl Pts',(-3.31631129755346,-17.7406985030951,
-1449.20073529412));
#167097=CARTESIAN_POINT('Ctrl Pts',(-4.96022910773077,-17.4333970061901,
-1450.69485294118));
#167098=CARTESIAN_POINT('Ctrl Pts',(-6.51968959134574,-16.8292587962898,
-1452.18897058824));
#167099=CARTESIAN_POINT('Ctrl Pts',(-8.07915007496071,-16.2251205863895,
-1453.68308823529));
#167100=CARTESIAN_POINT('Ctrl Pts',(-9.50104767561052,-15.3447188656481,
-1455.17720588235));
#167101=CARTESIAN_POINT('Ctrl Pts',(-10.9229452762603,-14.4643171449067,
-1456.67132352941));
#167102=CARTESIAN_POINT('Ctrl Pts',(-12.1588589765331,-13.3376329379985,
-1458.16544117647));
#167103=CARTESIAN_POINT('Ctrl Pts',(-13.3947726768058,-12.2109487310903,
-1459.65955882353));
#167104=CARTESIAN_POINT('Ctrl Pts',(-14.4026149179538,-10.8763499173728,
-1461.15367647059));
#167105=CARTESIAN_POINT('Ctrl Pts',(-15.4104571591017,-9.54175110365538,
-1462.64779411765));
#167106=CARTESIAN_POINT('Ctrl Pts',(-16.1559070823762,-8.04468584505497,
-1464.14191176471));
#167107=CARTESIAN_POINT('Ctrl Pts',(-16.9013570056506,-6.54762058645456,
-1465.63602941176));
#167108=CARTESIAN_POINT('Ctrl Pts',(-17.3590292079831,-4.93906964482095,
-1467.13014705882));
#167109=CARTESIAN_POINT('Ctrl Pts',(-17.8167014103155,-3.33051870318735,
-1468.62426470588));
#167110=CARTESIAN_POINT('Ctrl Pts',(-17.9710104137728,-1.66525935159368,
-1470.11838235294));
#167111=CARTESIAN_POINT('Ctrl Pts',(-18.1253194172301,-1.10985572039171E-15,
-1471.6125));
#167112=CARTESIAN_POINT('Ctrl Pts',(-17.9710104137728,1.66525935159367,
-1473.10661764706));
#167113=CARTESIAN_POINT('Ctrl Pts',(-17.8167014103155,3.33051870318735,
-1474.60073529412));
#167114=CARTESIAN_POINT('Ctrl Pts',(-17.3590292079831,4.93906964482096,
-1476.09485294118));
#167115=CARTESIAN_POINT('Ctrl Pts',(-16.9013570056506,6.54762058645456,
-1477.58897058824));
#167116=CARTESIAN_POINT('Ctrl Pts',(-16.1559070823762,8.04468584505497,
-1479.08308823529));
#167117=CARTESIAN_POINT('Ctrl Pts',(-15.4104571591017,9.54175110365538,
-1480.57720588235));
#167118=CARTESIAN_POINT('Ctrl Pts',(-14.4026149179538,10.8763499173728,
-1482.07132352941));
#167119=CARTESIAN_POINT('Ctrl Pts',(-13.3947726768058,12.2109487310903,
-1483.56544117647));
#167120=CARTESIAN_POINT('Ctrl Pts',(-12.1588589765331,13.3376329379985,
-1485.05955882353));
#167121=CARTESIAN_POINT('Ctrl Pts',(-10.9229452762603,14.4643171449067,
-1486.55367647059));
#167122=CARTESIAN_POINT('Ctrl Pts',(-9.50104767561052,15.3447188656481,
-1488.04779411765));
#167123=CARTESIAN_POINT('Ctrl Pts',(-8.07915007496071,16.2251205863895,
-1489.54191176471));
#167124=CARTESIAN_POINT('Ctrl Pts',(-6.51968959134574,16.8292587962898,
-1491.03602941176));
#167125=CARTESIAN_POINT('Ctrl Pts',(-4.96022910773078,17.4333970061901,
-1492.53014705882));
#167126=CARTESIAN_POINT('Ctrl Pts',(-3.31631129755346,17.7406985030951,
-1494.02426470588));
#167127=CARTESIAN_POINT('Ctrl Pts',(-1.67239348737615,18.048,-1495.51838235294));
#167128=CARTESIAN_POINT('Ctrl Pts',(-2.21024254310115E-15,18.048,-1497.0125));
#167129=CARTESIAN_POINT('Ctrl Pts',(1.67239348737616,18.048,-1498.50661764706));
#167130=CARTESIAN_POINT('Ctrl Pts',(3.31631129755346,17.7406985030951,-1500.00073529412));
#167131=CARTESIAN_POINT('Ctrl Pts',(4.96022910773077,17.4333970061901,-1501.49485294118));
#167132=CARTESIAN_POINT('Ctrl Pts',(6.51968959134575,16.8292587962898,-1502.98897058824));
#167133=CARTESIAN_POINT('Ctrl Pts',(7.54128438222173,16.4334908658498,-1503.96775961253));
#167134=CARTESIAN_POINT('Ctrl Pts',(8.50750525179015,15.9170555816949,-1504.9503325767));
#167135=CARTESIAN_POINT('Ctrl Pts',(23.3054664377218,8.00769496792138,-1519.99873097503));
#167136=CARTESIAN_POINT('Ctrl Pts',(38.1034276236535,0.0983343541478931,
-1535.04712937335));
#167137=CARTESIAN_POINT('Origin',(-4.55601018023444E-6,1.49069329302698E-5,
692.00000002901));
#167138=CARTESIAN_POINT('',(0.,-18.048,1500.28886941341));
#167139=CARTESIAN_POINT('Origin',(5.37704275891775E-14,4.44089209850063E-14,
1504.8993152933));
#167140=CARTESIAN_POINT('Origin',(1.20502921845816E-6,0.00017779754810876,
692.00000007199));
#167141=CARTESIAN_POINT('Origin',(0.,-16.524,1504.95));
#167142=CARTESIAN_POINT('Origin',(0.,15.,1504.95));
#167143=CARTESIAN_POINT('Origin',(0.,0.,692.));
#276449=UNCERTAINTY_MEASURE_WITH_UNIT(LENGTH_MEASURE(0.01),#276463,
'DISTANCE_ACCURACY_VALUE',
'Maximum model space distance between geometric entities at asserted c
onnectivities');
#276454=UNCERTAINTY_MEASURE_WITH_UNIT(LENGTH_MEASURE(0.01),#276463,
'DISTANCE_ACCURACY_VALUE',
'Maximum model space distance between geometric entities at asserted c
onnectivities');
#276457=(
GEOMETRIC_REPRESENTATION_CONTEXT(3)
GLOBAL_UNCERTAINTY_ASSIGNED_CONTEXT((#276449))
GLOBAL_UNIT_ASSIGNED_CONTEXT((#276463,#276465,#276466))
REPRESENTATION_CONTEXT('','3D')
);
#276462=(
GEOMETRIC_REPRESENTATION_CONTEXT(3)
GLOBAL_UNCERTAINTY_ASSIGNED_CONTEXT((#276454))
GLOBAL_UNIT_ASSIGNED_CONTEXT((#276463,#276465,#276466))
REPRESENTATION_CONTEXT('','3D')
);
#276463=(
LENGTH_UNIT()
NAMED_UNIT(*)
SI_UNIT(.MILLI.,.METRE.)
);
#276465=(
NAMED_UNIT(*)
PLANE_ANGLE_UNIT()
SI_UNIT($,.RADIAN.)
);
#276466=(
NAMED_UNIT(*)
SI_UNIT($,.STERADIAN.)
SOLID_ANGLE_UNIT()
);
#276469=SHAPE_DEFINITION_REPRESENTATION(#276476,#276489);
#276476=PRODUCT_DEFINITION_SHAPE('',$,#276497);
#276489=SHAPE_REPRESENTATION('',(#98875),#276457);
#276494=PRODUCT_DEFINITION_CONTEXT('part definition',#276517,'design');
#276497=PRODUCT_DEFINITION('Vertical Precision Auger Screw_5866K521',
'Vertical Precision Auger Screw',#276504,#276494);
#276504=PRODUCT_DEFINITION_FORMATION('',$,#276521);
#276517=APPLICATION_CONTEXT(
'Core Data for Automotive Mechanical Design Process');
#276518=PRODUCT_CONTEXT('part definition',#276517,'mechanical');
#276521=PRODUCT('Vertical Precision Auger Screw_5866K521',
'Vertical Precision Auger Screw',$,(#276518));
#276528=PRESENTATION_STYLE_ASSIGNMENT((#276533));
#276533=SURFACE_STYLE_USAGE(.BOTH.,#276538);
#276538=SURFACE_SIDE_STYLE('',(#276543));
#276543=SURFACE_STYLE_FILL_AREA(#276548);
#276548=FILL_AREA_STYLE('Opaque(31,36,43)',(#276553));
#276553=FILL_AREA_STYLE_COLOUR('Opaque(31,36,43)',#276558);
#276558=COLOUR_RGB('Opaque(31,36,43)',0.12156862745098,0.141176470588235,
0.168627450980392);
ENDSEC;
END-ISO-10303-21;
